ISO-10303-21;
HEADER;
FILE_DESCRIPTION (('STEP AP214'),
    '1' );
FILE_NAME ('Swivel Caster Main Housing.step',
    '2026-10-09T12:05:53',
    ( '' ),
    ( '' ),
    'SwSTEP 2.0',
    'SolidWorks 2026',
    '' );
FILE_SCHEMA (( 'AUTOMOTIVE_DESIGN' ));
ENDSEC;

DATA;
#2=CARTESIAN_POINT ( 'NONE',  ( 11.13393739769619906, -63.46281540124650178, -43.92385611378949761 ) ) ;
#3=CARTESIAN_POINT ( 'NONE',  ( 70.83745409581372598, 17.98087126524719892, -68.79648330188406646 ) ) ;
#6=CARTESIAN_POINT ( 'NONE',  ( 56.87954270074080654, 19.13328173822429790, -52.82794281668999758 ) ) ;
#11=LINE ( 'NONE', #18878, #28379 ) ;
#19=VERTEX_POINT ( 'NONE', #48082 ) ;
#20=CIRCLE ( 'NONE', #41004, 2.999999999999999112 ) ;
#21=CIRCLE ( 'NONE', #50217, 3.400000000022779911 ) ;
#23=AXIS2_PLACEMENT_3D ( 'NONE', #28907, #44909, #49375 ) ;
#27=CARTESIAN_POINT ( 'NONE',  ( 47.24444964797500290, 23.22446773931700292, -75.11580175282739447 ) ) ;
#29=CARTESIAN_POINT ( 'NONE',  ( 58.45382029077139663, 15.48193787282010092, -47.52511337483110054 ) ) ;
#30=CARTESIAN_POINT ( 'NONE',  ( 12.20485434016749871, 33.73368687413830003, -16.27613458663830315 ) ) ;
#32=DIRECTION ( 'NONE',  ( 0.05023550054956202326, 0.000000000000000000, 0.9987374001630934250 ) ) ;
#33=CARTESIAN_POINT ( 'NONE',  ( 11.13393739769619906, -55.30245861064819479, -43.74348518090240390 ) ) ;
#35=CARTESIAN_POINT ( 'NONE',  ( 61.45197839950609620, 13.95077426323470071, -46.74199412580669843 ) ) ;
#39=VERTEX_POINT ( 'NONE', #5102 ) ;
#40=CARTESIAN_POINT ( 'NONE',  ( 52.81826494772970193, -49.66694110389089900, -48.49938242813500011 ) ) ;
#41=CARTESIAN_POINT ( 'NONE',  ( 61.28932554653079734, -45.22069038368779559, -27.95515929525059917 ) ) ;
#43=CARTESIAN_POINT ( 'NONE',  ( 61.24946240356100446, 14.29281268270219840, -47.58806468664730005 ) ) ;
#45=CARTESIAN_POINT ( 'NONE',  ( 51.50850403090049667, 17.46583278780749993, -76.79363216376158618 ) ) ;
#46=CARTESIAN_POINT ( 'NONE',  ( 53.43953639093020058, 18.12785922017320317, -48.94167477993919846 ) ) ;
#49=EDGE_CURVE ( 'NONE', #3712, #26115, #46078, .T. ) ;
#53=CARTESIAN_POINT ( 'NONE',  ( 47.61264694707350031, -54.54714935536990339, -55.11842961798419793 ) ) ;
#55=CONICAL_SURFACE ( 'NONE', #5063, 44.00000000000000000, 0.8066715494215099813 ) ;
#57=CARTESIAN_POINT ( 'NONE',  ( 60.90067199252950303, -29.96820827507399798, -16.03697021813930235 ) ) ;
#61=AXIS2_PLACEMENT_3D ( 'NONE', #5299, #13423, #12639 ) ;
#64=DIRECTION ( 'NONE',  ( 0.8933039976646619529, 0.3805134419105545285, 0.2392017731575520056 ) ) ;
#69=ORIENTED_EDGE ( 'NONE', *, *, #51815, .T. ) ;
#71=CARTESIAN_POINT ( 'NONE',  ( 55.90694558577502704, 19.65285642343416939, -74.84539568267780396 ) ) ;
#73=CARTESIAN_POINT ( 'NONE',  ( 11.04126890615173195, 33.67834000696034735, -23.14699238744169563 ) ) ;
#76=EDGE_CURVE ( 'NONE', #45466, #37955, #44145, .T. ) ;
#80=EDGE_CURVE ( 'NONE', #28603, #19573, #33103, .T. ) ;
#81=CARTESIAN_POINT ( 'NONE',  ( 63.96520777976849814, -30.70443757047150157, -16.53667252483340278 ) ) ;
#84=CARTESIAN_POINT ( 'NONE',  ( 41.93136269540350014, 14.16859103147459997, -6.436551634680689915 ) ) ;
#85=CARTESIAN_POINT ( 'NONE',  ( 15.05440318628110141, 21.88381105532300097, -76.14999999999999147 ) ) ;
#88=CARTESIAN_POINT ( 'NONE',  ( 83.58549413295790487, -44.91149346033729728, -47.23752224019400359 ) ) ;
#89=CARTESIAN_POINT ( 'NONE',  ( 9.633937397696209715, -15.61618894467929941, -22.64999999999999858 ) ) ;
#93=CARTESIAN_POINT ( 'NONE',  ( 54.39552376178149018, -47.99669817431590246, -26.49407277081109768 ) ) ;
#94=CARTESIAN_POINT ( 'NONE',  ( 13.75381683890189954, -50.28652857585829850, -20.97887788433540024 ) ) ;
#100=CARTESIAN_POINT ( 'NONE',  ( -8.352063028131979650, -44.76125978986279819, -5.675626772346689997 ) ) ;
#104=CARTESIAN_POINT ( 'NONE',  ( 57.49560449525049677, -50.20980267308190292, -52.71571619239969664 ) ) ;
#105=CARTESIAN_POINT ( 'NONE',  ( 41.47267182510199746, 13.45740503867699900, -5.287754110957130216 ) ) ;
#107=DIRECTION ( 'NONE',  ( 0.000000000000000000, 0.000000000000000000, 1.000000000000000000 ) ) ;
#108=CARTESIAN_POINT ( 'NONE',  ( 53.43679795856239423, -49.34287432940249829, -48.83615822498679648 ) ) ;
#112=CARTESIAN_POINT ( 'NONE',  ( 17.46250221217660226, -52.82751997460400162, -76.12812327221449493 ) ) ;
#119=ORIENTED_EDGE ( 'NONE', *, *, #5990, .F. ) ;
#120=CARTESIAN_POINT ( 'NONE',  ( 17.35323444535940141, 21.52412519331699770, -76.12563501418100032 ) ) ;
#121=VERTEX_POINT ( 'NONE', #9296 ) ;
#122=ORIENTED_EDGE ( 'NONE', *, *, #30558, .T. ) ;
#123=CARTESIAN_POINT ( 'NONE',  ( 41.13393739769620083, -15.61618894467929941, -76.14999999999999147 ) ) ;
#126=CARTESIAN_POINT ( 'NONE',  ( 61.67728155832050163, 13.96021777555640142, -46.92123163896760474 ) ) ;
#128=CARTESIAN_POINT ( 'NONE',  ( 13.00893747662790112, -65.51843693869379592, -23.32157303180050079 ) ) ;
#130=CARTESIAN_POINT ( 'NONE',  ( 11.13393741218609989, -63.52234717531779751, -24.14942545402350049 ) ) ;
#134=ORIENTED_EDGE ( 'NONE', *, *, #16581, .T. ) ;
#135=CARTESIAN_POINT ( 'NONE',  ( 68.13393739769630031, 16.88381105532069881, -71.50000000000000000 ) ) ;
#136=CARTESIAN_POINT ( 'NONE',  ( 60.78215478534439598, 14.37029503885610104, -47.53399852477849663 ) ) ;
#138=CARTESIAN_POINT ( 'NONE',  ( 41.55663456559440050, -43.85962873145390262, -3.466044033466880059 ) ) ;
#139=CARTESIAN_POINT ( 'NONE',  ( -7.981053360220990101, 13.77072044879260027, -5.285160133845220543 ) ) ;
#141=DIRECTION ( 'NONE',  ( -1.000000000000000000, -1.007258792502662152E-15, 0.000000000000000000 ) ) ;
#144=CARTESIAN_POINT ( 'NONE',  ( 16.13393739769620083, -15.61618894467929941, -8.050000000000000711 ) ) ;
#145=CARTESIAN_POINT ( 'NONE',  ( 41.69946260611190070, 14.48490530928729925, -6.580410751903029265 ) ) ;
#146=CARTESIAN_POINT ( 'NONE',  ( 11.25398292734820060, 32.98847748127889901, -44.13762314110879714 ) ) ;
#150=AXIS2_PLACEMENT_3D ( 'NONE', #7482, #19780, #50726 ) ;
#151=DIRECTION ( 'NONE',  ( 0.4646601886423053496, 0.000000000000000000, 0.8854890790353641128 ) ) ;
#152=CIRCLE ( 'NONE', #47026, 15.56227766016840164 ) ;
#153=CARTESIAN_POINT ( 'NONE',  ( 13.08915387332580060, 18.89706364897919855, -21.07935023198889724 ) ) ;
#154=CARTESIAN_POINT ( 'NONE',  ( 47.08254214957229777, 23.29430871593149632, -75.17655545168919673 ) ) ;
#155=CARTESIAN_POINT ( 'NONE',  ( 48.68907877926229588, -53.99330233976530025, -54.71376368574509996 ) ) ;
#156=CARTESIAN_POINT ( 'NONE',  ( 51.77632594796870080, -32.59667852913690922, -18.40929238398544854 ) ) ;
#158=DIRECTION ( 'NONE',  ( -9.834501533011740460E-16, -2.054487543405499690E-16, -1.000000000000000000 ) ) ;
#164=CARTESIAN_POINT ( 'NONE',  ( 83.89200044194980421, -48.61618894467930119, -53.92796738110899923 ) ) ;
#167=CARTESIAN_POINT ( 'NONE',  ( 60.57174147421439869, -45.61905813271650345, -47.32280480079099760 ) ) ;
#169=EDGE_CURVE ( 'NONE', #3359, #16152, #45412, .T. ) ;
#172=ORIENTED_EDGE ( 'NONE', *, *, #12898, .T. ) ;
#173=CARTESIAN_POINT ( 'NONE',  ( 82.86439673227779679, -45.43596139653639909, -47.48719404937710209 ) ) ;
#178=CARTESIAN_POINT ( 'NONE',  ( 12.13393739769500357, -55.41568642894398522, -22.88367089793594999 ) ) ;
#179=CARTESIAN_POINT ( 'NONE',  ( 76.39443566142985276, -13.50186642808351678, -12.77252636400736918 ) ) ;
#180=CARTESIAN_POINT ( 'NONE',  ( 53.40601104668340326, -52.07939714610260040, -54.18165646226010068 ) ) ;
#184=CARTESIAN_POINT ( 'NONE',  ( 57.10566319413430136, -45.15673104066610222, -25.30628267469290194 ) ) ;
#185=CARTESIAN_POINT ( 'NONE',  ( 56.36581729833090293, -50.64752597117900024, -53.07181749496119494 ) ) ;
#187=CARTESIAN_POINT ( 'NONE',  ( 58.91901068275170417, -2.751350989218700249, -15.64940685286009980 ) ) ;
#190=AXIS2_PLACEMENT_3D ( 'NONE', #21830, #26535, #49643 ) ;
#191=ORIENTED_EDGE ( 'NONE', *, *, #12053, .T. ) ;
#194=CARTESIAN_POINT ( 'NONE',  ( 53.11717557676140444, -50.37380613066250135, -77.21703359256949284 ) ) ;
#195=CARTESIAN_POINT ( 'NONE',  ( 60.26025110216912850, 14.55536647234954906, -47.43140372362420010 ) ) ;
#196=CARTESIAN_POINT ( 'NONE',  ( 12.16981617636240109, -50.04926268091029584, -21.14999999999999858 ) ) ;
#198=CARTESIAN_POINT ( 'NONE',  ( 13.05744206701320209, -50.32199602849929931, -21.18087822640150364 ) ) ;
#199=CARTESIAN_POINT ( 'NONE',  ( 18.48744068327825829, -51.29015062620795362, -15.70679445625363257 ) ) ;
#200=CARTESIAN_POINT ( 'NONE',  ( 10.91611746120075743, -65.09563545678379626, -18.17421237897874065 ) ) ;
#201=CARTESIAN_POINT ( 'NONE',  ( 61.22433221214529908, -45.66722181782489542, -47.75777089857670177 ) ) ;
#206=CARTESIAN_POINT ( 'NONE',  ( 14.27557618103930004, -51.11617952483079108, -74.35192203308750436 ) ) ;
#207=CARTESIAN_POINT ( 'NONE',  ( 47.38398407523909839, -54.66303005604620324, -54.71474001952109489 ) ) ;
#210=CARTESIAN_POINT ( 'NONE',  ( 14.48969159609045931, -51.52597369351618539, -75.36997958377637019 ) ) ;
#215=CARTESIAN_POINT ( 'NONE',  ( 11.13393739769619906, 32.28996931002959769, -24.14942631645369886 ) ) ;
#216=DIRECTION ( 'NONE',  ( 1.000000000000000000, 1.435277183835595142E-25, -2.812429781167509836E-09 ) ) ;
#217=CARTESIAN_POINT ( 'NONE',  ( 48.63544209855220402, 22.87909972998859587, -55.27856191273439634 ) ) ;
#220=CARTESIAN_POINT ( 'NONE',  ( 53.03258586660929552, -49.57550701127339465, -48.98438927054080239 ) ) ;
#221=VECTOR ( 'NONE', #20603, 1000.000000000000000 ) ;
#225=CARTESIAN_POINT ( 'NONE',  ( 16.13393739769620083, -15.61618894467929941, -10.44999999999999929 ) ) ;
#226=CARTESIAN_POINT ( 'NONE',  ( 84.44784216359251161, 11.88381105532070059, -47.47585302082339354 ) ) ;
#227=CARTESIAN_POINT ( 'NONE',  ( 55.09561028961779527, 15.74612775871969994, -25.81326377834329833 ) ) ;
#229=CARTESIAN_POINT ( 'NONE',  ( 52.88388581274700329, 18.44024018630440409, -49.00306432449180249 ) ) ;
#230=EDGE_CURVE ( 'NONE', #16151, #14500, #48277, .T. ) ;
#231=CARTESIAN_POINT ( 'NONE',  ( 57.24436304063220149, -45.12772278369259737, -17.93020339716479938 ) ) ;
#232=CARTESIAN_POINT ( 'NONE',  ( 15.82997274078853067, -51.11618894467930119, -21.91305730704813115 ) ) ;
#236=CARTESIAN_POINT ( 'NONE',  ( 11.16919192711069897, -65.09379547448669712, -17.21576935268850050 ) ) ;
#237=CARTESIAN_POINT ( 'NONE',  ( 12.92951305397479977, 34.28108550583429803, -47.71245015580439741 ) ) ;
#239=CARTESIAN_POINT ( 'NONE',  ( 48.15382033460080180, -54.02300406733139937, -53.72956514560460306 ) ) ;
#240=CARTESIAN_POINT ( 'NONE',  ( 8.799473741179280495, 31.95986279266500318, -46.67015979934819825 ) ) ;
#246=CARTESIAN_POINT ( 'NONE',  ( 70.83745409581388230, 17.98087126524299606, -74.20351669811765305 ) ) ;
#249=CARTESIAN_POINT ( 'NONE',  ( 50.13210307247129549, -48.90653279581949420, -76.14999999999999147 ) ) ;
#254=LINE ( 'NONE', #44274, #11685 ) ;
#257=CARTESIAN_POINT ( 'NONE',  ( 10.37119768687602317, -55.19981235010300935, -21.14999999999890079 ) ) ;
#260=VERTEX_POINT ( 'NONE', #568 ) ;
#264=CARTESIAN_POINT ( 'NONE',  ( 52.69422391758440227, -49.76824816101610338, -48.79572285777990004 ) ) ;
#266=DIRECTION ( 'NONE',  ( 0.000000000000000000, -1.000000000000000000, 0.000000000000000000 ) ) ;
#269=CARTESIAN_POINT ( 'NONE',  ( 47.30322462833210295, 23.47865774688779794, -74.36100594765079563 ) ) ;
#272=CARTESIAN_POINT ( 'NONE',  ( 59.65718820948480783, 14.85145970413650041, -47.32570903220330649 ) ) ;
#273=CARTESIAN_POINT ( 'NONE',  ( 12.23212070002750096, 33.47637228114889751, -15.94047990888659783 ) ) ;
#275=AXIS2_PLACEMENT_3D ( 'NONE', #225, #8098, #24041 ) ;
#276=CARTESIAN_POINT ( 'NONE',  ( 54.17120420068020081, -50.61618894747770270, -77.01278694698871163 ) ) ;
#280=CARTESIAN_POINT ( 'NONE',  ( 61.31292087637410049, 14.04174110780009954, -47.04181882197700304 ) ) ;
#283=ORIENTED_EDGE ( 'NONE', *, *, #13602, .F. ) ;
#284=CARTESIAN_POINT ( 'NONE',  ( 52.85589391196879916, -49.64722623523429945, -48.63421165633150167 ) ) ;
#285=CARTESIAN_POINT ( 'NONE',  ( 61.33763625571969413, -45.19708596712810333, -27.94521875216469908 ) ) ;
#287=CARTESIAN_POINT ( 'NONE',  ( 56.26879455738869495, 14.75277753040210094, -26.06397138246319756 ) ) ;
#289=CARTESIAN_POINT ( 'NONE',  ( 50.28917926387119763, 18.40713679194410091, -76.14999999999999147 ) ) ;
#290=CARTESIAN_POINT ( 'NONE',  ( 52.72266114154869854, 18.49315592538880182, -48.47378032971769812 ) ) ;
#298=CARTESIAN_POINT ( 'NONE',  ( 47.55572014686639903, -54.56393835125380321, -54.83404589176390687 ) ) ;
#300=CARTESIAN_POINT ( 'NONE',  ( 33.83393739769619657, -15.61618894467939711, -6.649999999999999467 ) ) ;
#301=CARTESIAN_POINT ( 'NONE',  ( 59.27112701105020420, 16.84091543466239926, -50.37593205019099685 ) ) ;
#308=ORIENTED_EDGE ( 'NONE', *, *, #24146, .F. ) ;
#312=ORIENTED_EDGE ( 'NONE', *, *, #15491, .T. ) ;
#313=CARTESIAN_POINT ( 'NONE',  ( 56.04842253378700434, -45.73510956910900660, -25.30965062049470049 ) ) ;
#314=CARTESIAN_POINT ( 'NONE',  ( 54.83367525942058052, 19.86242937399058306, -75.27593038797637348 ) ) ;
#316=CYLINDRICAL_SURFACE ( 'NONE', #61, 1.000000000000000888 ) ;
#325=CARTESIAN_POINT ( 'NONE',  ( 11.84646636965089961, -64.37535564892330342, -24.61798141452300115 ) ) ;
#327=CARTESIAN_POINT ( 'NONE',  ( 41.50829725104460266, 14.07267842887970133, -6.113795638072149430 ) ) ;
#328=EDGE_CURVE ( 'NONE', #9603, #32428, #39376, .T. ) ;
#329=CARTESIAN_POINT ( 'NONE',  ( 14.89540806449589994, 21.53776777092619810, -76.12726769927830617 ) ) ;
#332=CARTESIAN_POINT ( 'NONE',  ( 52.15297977881749603, 18.44951849047100367, -77.15976221510139510 ) ) ;
#333=CARTESIAN_POINT ( 'NONE',  ( 83.78435757737699419, -44.62302606491700629, -47.11582429421620333 ) ) ;
#337=CARTESIAN_POINT ( 'NONE',  ( 53.32987016954000126, -49.16639059516919730, -27.25060986079260061 ) ) ;
#338=CARTESIAN_POINT ( 'NONE',  ( 12.47078628662380062, -64.90377506766920135, -16.09719858678619886 ) ) ;
#341=CARTESIAN_POINT ( 'NONE',  ( 68.13393739769620083, -33.11618894467940066, -65.65000000000000568 ) ) ;
#343=CARTESIAN_POINT ( 'NONE',  ( -5.211271184535770651, -47.35087631705189892, -5.409249467409000367 ) ) ;
#344=CARTESIAN_POINT ( 'NONE',  ( 47.43699537176610193, 23.38932764359389793, -54.65593435207329520 ) ) ;
#347=CARTESIAN_POINT ( 'NONE',  ( 12.80406157968140057, 19.41979416798140079, -21.33287590401240053 ) ) ;
#349=CARTESIAN_POINT ( 'NONE',  ( 42.00047115798010111, 12.65453701896299954, -4.514521080317789981 ) ) ;
#354=CARTESIAN_POINT ( 'NONE',  ( 58.37494088879699206, -46.85178433881189619, -47.96570233379380710 ) ) ;
#356=AXIS2_PLACEMENT_3D ( 'NONE', #1615, #5303, #5043 ) ;
#358=CARTESIAN_POINT ( 'NONE',  ( 17.66259199974900085, -52.33797002293529488, -75.98739629952659413 ) ) ;
#359=EDGE_CURVE ( 'NONE', #15227, #17198, #33478, .T. ) ;
#362=VERTEX_POINT ( 'NONE', #30409 ) ;
#364=CARTESIAN_POINT ( 'NONE',  ( 8.803701492139829554, 31.98286322187070141, -46.67019247816079286 ) ) ;
#368=CARTESIAN_POINT ( 'NONE',  ( 18.39143759339100015, 20.51618323985760028, -75.32473453343510528 ) ) ;
#372=FACE_OUTER_BOUND ( 'NONE', #24038, .T. ) ;
#373=FACE_OUTER_BOUND ( 'NONE', #2514, .T. ) ;
#375=CARTESIAN_POINT ( 'NONE',  ( 61.73752130501190294, 13.89709510481169907, -46.60858937970350269 ) ) ;
#376=ORIENTED_EDGE ( 'NONE', *, *, #2345, .F. ) ;
#377=CARTESIAN_POINT ( 'NONE',  ( 75.37149648727124429, 8.404366805738446189, -12.88285088340076712 ) ) ;
#378=CARTESIAN_POINT ( 'NONE',  ( 11.93174526809839975, 34.20691394249479345, -17.93019253464870033 ) ) ;
#380=CARTESIAN_POINT ( 'NONE',  ( 11.18157709302775693, -63.96091097623292399, -24.11720355368492008 ) ) ;
#383=ORIENTED_EDGE ( 'NONE', *, *, #15032, .F. ) ;
#384=DIRECTION ( 'NONE',  ( 0.000000000000000000, -1.000000000000000000, 0.000000000000000000 ) ) ;
#386=CARTESIAN_POINT ( 'NONE',  ( 60.90370348410529999, 14.44994567453569978, -47.72079593689969812 ) ) ;
#387=CARTESIAN_POINT ( 'NONE',  ( 50.95711422415039493, 14.35971216196159794, -12.63805038270279901 ) ) ;
#390=CARTESIAN_POINT ( 'NONE',  ( 14.34417029198830029, 20.88381105532299742, -21.14999999999999858 ) ) ;
#391=CARTESIAN_POINT ( 'NONE',  ( -10.44638207467119884, 11.54816621806459942, -6.014155644910160525 ) ) ;
#393=CARTESIAN_POINT ( 'NONE',  ( 57.33093049919349937, 14.58258304156659868, -26.26999088063260146 ) ) ;
#395=ORIENTED_EDGE ( 'NONE', *, *, #27626, .F. ) ;
#399=CARTESIAN_POINT ( 'NONE',  ( 12.74573753497439910, 34.25580809235049884, -47.28532827175700248 ) ) ;
#402=CARTESIAN_POINT ( 'NONE',  ( 12.36324357420019915, -64.54680782163349306, -15.76420532458509882 ) ) ;
#403=CARTESIAN_POINT ( 'NONE',  ( 13.61804211761770134, 18.93546665499809833, -20.94890276653890027 ) ) ;
#404=CARTESIAN_POINT ( 'NONE',  ( 46.95604843068529988, 23.06042629058710247, -75.52284352240690168 ) ) ;
#405=CARTESIAN_POINT ( 'NONE',  ( 48.72504344960400147, -54.07331086023980049, -55.30415983355479881 ) ) ;
#406=DIRECTION ( 'NONE',  ( 0.000000000000000000, 0.000000000000000000, 1.000000000000000000 ) ) ;
#412=DIRECTION ( 'NONE',  ( 0.6415444970810859626, -0.4854844151940995167, 0.5939070136550161916 ) ) ;
#415=CARTESIAN_POINT ( 'NONE',  ( 60.63173930441830350, -45.57621591238160619, -47.21435140852850054 ) ) ;
#417=CARTESIAN_POINT ( 'NONE',  ( 73.89392149341017557, -43.37877748987173732, -12.94883270627985183 ) ) ;
#420=CARTESIAN_POINT ( 'NONE',  ( 87.61621807841599718, 1.883811055320649963, -61.12885639714370001 ) ) ;
#423=CARTESIAN_POINT ( 'NONE',  ( 84.44784216359251161, -43.11618894467930119, -47.47585302082339354 ) ) ;
#424=CIRCLE ( 'NONE', #49007, 20.79999999999999716 ) ;
#428=ORIENTED_EDGE ( 'NONE', *, *, #30931, .T. ) ;
#429=CARTESIAN_POINT ( 'NONE',  ( 61.51108476807580416, -45.14457241600359794, -46.37195364498460037 ) ) ;
#431=CARTESIAN_POINT ( 'NONE',  ( 76.39418201693595734, -13.59255262052404056, -12.77143339381032838 ) ) ;
#432=CARTESIAN_POINT ( 'NONE',  ( 53.55397377960559879, -51.73583884506710717, -53.25782589811129242 ) ) ;
#433=ORIENTED_EDGE ( 'NONE', *, *, #41777, .F. ) ;
#437=CARTESIAN_POINT ( 'NONE',  ( 56.50529462384820079, -50.75959910210979587, -53.84464729327209653 ) ) ;
#442=CARTESIAN_POINT ( 'NONE',  ( 52.53691734465949992, -50.17408895096939858, -76.99573695420890829 ) ) ;
#443=CARTESIAN_POINT ( 'NONE',  ( 60.24866557976250192, 14.54998834221814796, -47.36885438232269507 ) ) ;
#444=CARTESIAN_POINT ( 'NONE',  ( 82.13853704237929776, 15.88381105532069704, -46.37203261889099792 ) ) ;
#446=FACE_OUTER_BOUND ( 'NONE', #23223, .T. ) ;
#450=CARTESIAN_POINT ( 'NONE',  ( 70.83393739769717001, -48.11618894467018492, -75.95000000000109708 ) ) ;
#453=EDGE_CURVE ( 'NONE', #24512, #4326, #17346, .T. ) ;
#458=EDGE_LOOP ( 'NONE', ( #21605, #10515, #19262, #50340, #19221 ) ) ;
#459=VECTOR ( 'NONE', #50948, 999.9999999999998863 ) ;
#460=CARTESIAN_POINT ( 'NONE',  ( 14.53113689391020102, -51.97808261890150305, -75.79330468503940210 ) ) ;
#461=CARTESIAN_POINT ( 'NONE',  ( 47.30697531817629908, -54.71648428534599873, -54.76104250077580815 ) ) ;
#462=PRESENTATION_STYLE_ASSIGNMENT (( #44492 ) ) ;
#463=LINE ( 'NONE', #28751, #28813 ) ;
#466=CARTESIAN_POINT ( 'NONE',  ( 10.77197593522630115, 33.74263483046039624, -18.02693217510839929 ) ) ;
#467=CARTESIAN_POINT ( 'NONE',  ( 83.89200044194980421, 17.38381105532069881, -53.92796738110899923 ) ) ;
#468=CARTESIAN_POINT ( 'NONE',  ( -9.500613363851449833, -43.72129052405930594, -5.962761149281509354 ) ) ;
#469=DIRECTION ( 'NONE',  ( -1.000000000000000000, 0.000000000000000000, 0.000000000000000000 ) ) ;
#471=CARTESIAN_POINT ( 'NONE',  ( 48.42313109053679909, 22.83113193936399909, -54.61340708730690352 ) ) ;
#472=ORIENTED_EDGE ( 'NONE', *, *, #37574, .F. ) ;
#473=CARTESIAN_POINT ( 'NONE',  ( 52.98874192681579842, -49.59627630596699532, -48.96317220553530092 ) ) ;
#474=ORIENTED_EDGE ( 'NONE', *, *, #40095, .T. ) ;
#475=CARTESIAN_POINT ( 'NONE',  ( -5.366062602303798279, -15.61618894467929586, -11.05000000000000071 ) ) ;
#477=CARTESIAN_POINT ( 'NONE',  ( 57.02861371936400303, -50.62805676435459645, -53.87746547587289569 ) ) ;
#478=CARTESIAN_POINT ( 'NONE',  ( 84.42999065749789622, 12.06718754213130040, -47.39892822416609874 ) ) ;
#480=CARTESIAN_POINT ( 'NONE',  ( 52.97768851982059601, 18.39522800273699943, -49.05519422600419688 ) ) ;
#481=CARTESIAN_POINT ( 'NONE',  ( 56.06159152657470202, -45.29125632613430241, -16.02375003208479853 ) ) ;
#483=VERTEX_POINT ( 'NONE', #37512 ) ;
#485=CARTESIAN_POINT ( 'NONE',  ( 11.50291103294089901, -65.34958077267680210, -17.75618544430749779 ) ) ;
#486=CARTESIAN_POINT ( 'NONE',  ( 11.18028273825089869, 33.73068083865630484, -46.79252262002829355 ) ) ;
#488=CARTESIAN_POINT ( 'NONE',  ( 61.75019796695539753, 13.88381105532070059, -28.15000000000000213 ) ) ;
#489=CARTESIAN_POINT ( 'NONE',  ( 10.63867076987313176, -63.67733169492935730, -23.65473337217691352 ) ) ;
#494=CARTESIAN_POINT ( 'NONE',  ( 13.06064429528559323, 19.66369995475592347, -21.55066630772461878 ) ) ;
#496=CARTESIAN_POINT ( 'NONE',  ( 10.97912920880960108, -63.30540042885840535, -44.74308033447209709 ) ) ;
#499=CARTESIAN_POINT ( 'NONE',  ( 50.39461351434329828, -50.13496434787850120, -76.14999999999999147 ) ) ;
#500=CARTESIAN_POINT ( 'NONE',  ( 11.93174526809839975, -65.43929183185349530, -17.93019253464870033 ) ) ;
#505=CARTESIAN_POINT ( 'NONE',  ( 58.35672585773610166, 17.12870549263289988, -50.48250036787379003 ) ) ;
#508=CARTESIAN_POINT ( 'NONE',  ( 56.46528349507870814, 19.54388576035330161, -74.14939842031650130 ) ) ;
#510=CARTESIAN_POINT ( 'NONE',  ( 46.98568754098660349, -53.76726209812860446, -75.86283294038038605 ) ) ;
#513=EDGE_CURVE ( 'NONE', #23355, #5619, #23708, .T. ) ;
#515=CARTESIAN_POINT ( 'NONE',  ( 53.23879025501499740, -49.52941110961769766, -49.17697456386299848 ) ) ;
#516=CARTESIAN_POINT ( 'NONE',  ( 14.34417029198830029, 20.88381105532299742, -76.14999999999999147 ) ) ;
#518=EDGE_CURVE ( 'NONE', #26843, #25744, #48572, .T. ) ;
#519=VECTOR ( 'NONE', #18468, 1000.000000000000227 ) ;
#520=CARTESIAN_POINT ( 'NONE',  ( 47.04991247857869752, 22.88708854419270011, -75.60848552117779775 ) ) ;
#521=CARTESIAN_POINT ( 'NONE',  ( 19.04590477917927061, -52.29702409155545695, -15.95254375907780364 ) ) ;
#524=AXIS2_PLACEMENT_3D ( 'NONE', #10350, #26309, #30759 ) ;
#527=CARTESIAN_POINT ( 'NONE',  ( 54.55443780522559649, -50.61618894718989736, -76.86024425967369211 ) ) ;
#530=CARTESIAN_POINT ( 'NONE',  ( 61.25020875759329897, 14.02882808903070000, -46.85262742158650440 ) ) ;
#532=CARTESIAN_POINT ( 'NONE',  ( -12.80120649412780054, -56.90739261401959936, -52.53814278327499920 ) ) ;
#534=CARTESIAN_POINT ( 'NONE',  ( 52.87019085405700025, -49.63973566670129856, -48.66536726492419263 ) ) ;
#535=CARTESIAN_POINT ( 'NONE',  ( 59.27658655098359475, -45.11618906053649880, -25.77369910084199844 ) ) ;
#537=CARTESIAN_POINT ( 'NONE',  ( 13.68344161607869935, 19.38032502360789877, -21.30676595101419935 ) ) ;
#538=CARTESIAN_POINT ( 'NONE',  ( 57.00662312664200471, 14.67649396222829949, -26.24686926800940157 ) ) ;
#540=CARTESIAN_POINT ( 'NONE',  ( 50.91412666205799553, 17.97650990569060170, -76.31682797917909511 ) ) ;
#541=CARTESIAN_POINT ( 'NONE',  ( 53.03884170327399517, 18.32633884920069889, -48.90887833971159893 ) ) ;
#544=CARTESIAN_POINT ( 'NONE',  ( 75.20701160720210510, -44.95918647008760161, -14.39058221657740155 ) ) ;
#546=CARTESIAN_POINT ( 'NONE',  ( 47.73134908716809832, -54.46630275052049086, -54.83109498023989659 ) ) ;
#549=CARTESIAN_POINT ( 'NONE',  ( 41.27829246776259708, 12.87545685813370078, -3.596739354799320054 ) ) ;
#550=CARTESIAN_POINT ( 'NONE',  ( 58.09124814586559893, 17.43042520853399679, -50.80790410914660526 ) ) ;
#552=CARTESIAN_POINT ( 'NONE',  ( 61.75019796695539753, 14.88381105532069881, -28.15000000000000213 ) ) ;
#554=EDGE_CURVE ( 'NONE', #8993, #16411, #16877, .T. ) ;
#558=ADVANCED_FACE ( 'NONE', ( #34862 ), #38557, .T. ) ;
#559=ORIENTED_EDGE ( 'NONE', *, *, #15390, .T. ) ;
#560=CARTESIAN_POINT ( 'NONE',  ( 14.16335350998109988, -51.13178799506830075, -22.70850810526620123 ) ) ;
#562=ORIENTED_EDGE ( 'NONE', *, *, #13602, .T. ) ;
#564=CARTESIAN_POINT ( 'NONE',  ( 13.00893739761190027, -65.51843714052189682, -47.75434321210310173 ) ) ;
#565=CARTESIAN_POINT ( 'NONE',  ( 54.70456362050531851, 19.88764045771333500, -75.31516034446933361 ) ) ;
#566=VERTEX_POINT ( 'NONE', #15220 ) ;
#568=CARTESIAN_POINT ( 'NONE',  ( 66.72561048563109409, -33.11618894467930829, -20.64999999980150136 ) ) ;
#569=VECTOR ( 'NONE', #35500, 1000.000000000000114 ) ;
#574=ORIENTED_EDGE ( 'NONE', *, *, #8895, .T. ) ;
#578=CARTESIAN_POINT ( 'NONE',  ( 40.70149984973559754, 14.09668779090960022, -5.681031432320810204 ) ) ;
#581=CARTESIAN_POINT ( 'NONE',  ( 14.25117074270229978, 20.49345067490170180, -75.53710645103458887 ) ) ;
#582=CARTESIAN_POINT ( 'NONE',  ( 52.23705703117550314, 18.52650809402000220, -77.18591267702620939 ) ) ;
#584=DIRECTION ( 'NONE',  ( -5.226026857244350872E-28, -1.000000000000000000, -1.469246684736110336E-14 ) ) ;
#587=CARTESIAN_POINT ( 'NONE',  ( 52.82930795109979272, -49.63909307504320623, -27.85263494685039731 ) ) ;
#588=CARTESIAN_POINT ( 'NONE',  ( 11.66463330127890075, -65.13871550253499265, -16.69890713983809860 ) ) ;
#589=CARTESIAN_POINT ( 'NONE',  ( 50.37629383861175825, -36.29100334579137410, -76.18004623245177243 ) ) ;
#591=CARTESIAN_POINT ( 'NONE',  ( 16.13393739769620083, -15.61618894467929941, -6.928362978644219794 ) ) ;
#592=CARTESIAN_POINT ( 'NONE',  ( 51.83642112035360583, 14.98332062161530054, -13.79430700932419995 ) ) ;
#594=CARTESIAN_POINT ( 'NONE',  ( -10.40425463635500059, -42.83144259959529165, -6.155050416280118952 ) ) ;
#595=CARTESIAN_POINT ( 'NONE',  ( 47.39512065225470394, 23.42572006056330025, -54.76405005057330300 ) ) ;
#599=CARTESIAN_POINT ( 'NONE',  ( 54.84969908772705338, 16.62357410610304598, -26.66241143700859695 ) ) ;
#600=CARTESIAN_POINT ( 'NONE',  ( 43.09344256900070036, 12.72802089279420024, -5.051331041914770559 ) ) ;
#601=CARTESIAN_POINT ( 'NONE',  ( 11.13393739770729951, 32.24969779483610210, -22.73390400586109905 ) ) ;
#603=CYLINDRICAL_SURFACE ( 'NONE', #2404, 1.999999999999999556 ) ;
#604=CARTESIAN_POINT ( 'NONE',  ( 55.64975804555480465, -48.32680575653600386, -48.64277601874709944 ) ) ;
#605=CARTESIAN_POINT ( 'NONE',  ( 69.22748654599971019, -50.70395984887900909, -74.34354914830332461 ) ) ;
#607=CARTESIAN_POINT ( 'NONE',  ( 17.33798092487360165, -52.97186080988799972, -76.14999999999999147 ) ) ;
#613=CARTESIAN_POINT ( 'NONE',  ( 9.285737161019211428, 31.96511163084949558, -46.53047815523170527 ) ) ;
#614=CARTESIAN_POINT ( 'NONE',  ( 11.13393739769619906, -63.48206547090349972, -24.15000000000000213 ) ) ;
#618=CARTESIAN_POINT ( 'NONE',  ( 17.87986931031349869, 20.00715776053360173, -74.86150924066380696 ) ) ;
#622=B_SPLINE_CURVE_WITH_KNOTS ( 'NONE', 3,
 ( #47156, #27206, #3638, #27724, #11765, #210, #47411, #27973 ),
 .UNSPECIFIED., .F., .F.,
 ( 4, 2, 2, 4 ),
 ( 0.000000000000000000, 0.1882768039227099566, 0.3749999999997639666, 0.5000003605116074556 ),
 .UNSPECIFIED. ) ;
#624=CARTESIAN_POINT ( 'NONE',  ( 12.93454037390620037, -65.51377821817899871, -47.66712770179820069 ) ) ;
#625=CARTESIAN_POINT ( 'NONE',  ( 57.29425095410220337, -45.82021646256149694, -26.26548405410519749 ) ) ;
#629=DIRECTION ( 'NONE',  ( 0.000000000000000000, 0.000000000000000000, -1.000000000000000000 ) ) ;
#634=CARTESIAN_POINT ( 'NONE',  ( 11.25474628969880442, -64.20711136671845054, -24.08007506827187427 ) ) ;
#635=CARTESIAN_POINT ( 'NONE',  ( 14.14309834359610463, -52.38391192218928438, -75.82251645567293963 ) ) ;
#636=CARTESIAN_POINT ( 'NONE',  ( 51.96094199614199738, 2.175120467137570124, -77.41819485969911341 ) ) ;
#639=CARTESIAN_POINT ( 'NONE',  ( 66.72561048563099462, 1.883811055320649963, -20.64999999980150136 ) ) ;
#640=CARTESIAN_POINT ( 'NONE',  ( 61.51122975691190220, 13.91278366405482636, -46.37203261889099792 ) ) ;
#641=CARTESIAN_POINT ( 'NONE',  ( 70.82480173460169226, 13.72863524801690005, -13.13951160535810025 ) ) ;
#643=CARTESIAN_POINT ( 'NONE',  ( 53.05450034938409942, -49.59539206943890122, -49.09560404125600286 ) ) ;
#644=ADVANCED_FACE ( 'NONE', ( #32710 ), #44798, .T. ) ;
#645=CARTESIAN_POINT ( 'NONE',  ( 45.86983905350170687, 14.32280688279350045, -9.052205324345139914 ) ) ;
#646=CIRCLE ( 'NONE', #34945, 1.999999999999998446 ) ;
#648=CARTESIAN_POINT ( 'NONE',  ( -7.106986607165590719, 14.44895595893859941, -4.821389471371529289 ) ) ;
#649=CARTESIAN_POINT ( 'NONE',  ( 15.67962062535580081, -50.86266781815560023, -15.65622421709140077 ) ) ;
#650=CARTESIAN_POINT ( 'NONE',  ( 61.35346592530439835, 13.96312120787509947, -28.05093155658810034 ) ) ;
#652=ORIENTED_EDGE ( 'NONE', *, *, #31324, .T. ) ;
#654=FACE_OUTER_BOUND ( 'NONE', #22978, .T. ) ;
#655=CARTESIAN_POINT ( 'NONE',  ( 11.61686812457489992, 33.60076664006019342, -45.15427369068040520 ) ) ;
#658=CARTESIAN_POINT ( 'NONE',  ( 46.52115624802139848, 22.06631489729150175, -76.11314272684450088 ) ) ;
#659=CARTESIAN_POINT ( 'NONE',  ( 48.95357505128730224, -53.97596511168260491, -55.27962234102679417 ) ) ;
#664=ORIENTED_EDGE ( 'NONE', *, *, #24146, .T. ) ;
#668=DIRECTION ( 'NONE',  ( 1.000000000000000000, 0.000000000000000000, 0.000000000000000000 ) ) ;
#669=CARTESIAN_POINT ( 'NONE',  ( 60.77842532433790268, -45.71912871634670239, -47.73153708891739910 ) ) ;
#672=CARTESIAN_POINT ( 'NONE',  ( 12.53549335446709989, 18.74519657356650271, -21.12176656635870131 ) ) ;
#675=CARTESIAN_POINT ( 'NONE',  ( 52.32303883665399979, -51.41740952823399624, -75.90202711987829787 ) ) ;
#678=CARTESIAN_POINT ( 'NONE',  ( 84.44066163939218939, -43.31757366620339411, -47.44491107334449964 ) ) ;
#679=VERTEX_POINT ( 'NONE', #1033 ) ;
#680=EDGE_CURVE ( 'NONE', #47514, #50462, #13087, .T. ) ;
#681=ORIENTED_EDGE ( 'NONE', *, *, #42316, .T. ) ;
#682=ORIENTED_EDGE ( 'NONE', *, *, #11523, .T. ) ;
#683=CARTESIAN_POINT ( 'NONE',  ( 61.55619681691449330, -45.18291742677050138, -46.87336930385270506 ) ) ;
#685=CARTESIAN_POINT ( 'NONE',  ( 76.39242090978348187, -14.36197311350646189, -12.76384447145835921 ) ) ;
#686=CARTESIAN_POINT ( 'NONE',  ( 49.72648160330919609, -53.64673639094019819, -55.11972614036090334 ) ) ;
#688=ORIENTED_EDGE ( 'NONE', *, *, #39970, .F. ) ;
#689=CARTESIAN_POINT ( 'NONE',  ( 49.40552051342540096, 22.26542118999089936, -54.15739458345379376 ) ) ;
#692=CARTESIAN_POINT ( 'NONE',  ( 8.803322232233091071, -63.21315167929310519, -46.67017412665830278 ) ) ;
#694=CARTESIAN_POINT ( 'NONE',  ( 51.88873324421900435, -49.34589961264539681, -77.07841372369080091 ) ) ;
#695=( BOUNDED_CURVE ( )  B_SPLINE_CURVE ( 3, ( #42862, #34451, #14549, #46541 ),
 .UNSPECIFIED., .F., .T. ) 
 B_SPLINE_CURVE_WITH_KNOTS ( ( 4, 4 ),
 ( 5.229612381435808643, 5.497787143782143282 ),
 .UNSPECIFIED. ) 
 CURVE ( )  GEOMETRIC_REPRESENTATION_ITEM ( )  RATIONAL_B_SPLINE_CURVE ( ( 1.000000000000000000, 0.9940158321278117493, 0.9940158321278117493, 1.000000000000000000 ) ) 
 REPRESENTATION_ITEM ( '' )  );
#696=ORIENTED_EDGE ( 'NONE', *, *, #45315, .F. ) ;
#697=DIRECTION ( 'NONE',  ( 1.000000000000000000, 1.390415240674919644E-25, -1.562192859871379910E-09 ) ) ;
#698=DIRECTION ( 'NONE',  ( 0.6888026391158329487, -0.7071067811865494601, 0.1598465650148944150 ) ) ;
#700=CARTESIAN_POINT ( 'NONE',  ( 7.492845759203685674, -61.18022026567161475, -20.13893727953967172 ) ) ;
#705=CARTESIAN_POINT ( 'NONE',  ( 43.17397272625170501, -43.29126248660180210, -4.721727401537160418 ) ) ;
#706=CARTESIAN_POINT ( 'NONE',  ( 18.29473438519294604, -51.18612221100339355, -15.69049832779063536 ) ) ;
#707=CARTESIAN_POINT ( 'NONE',  ( 57.41961387009129680, 13.88381105532070059, -17.68493601882729749 ) ) ;
#709=CIRCLE ( 'NONE', #8266, 4.000000000000059508 ) ;
#711=DIRECTION ( 'NONE',  ( 4.486507500526829843E-12, 3.054623595244970244E-12, -1.000000000000000000 ) ) ;
#713=ORIENTED_EDGE ( 'NONE', *, *, #169, .F. ) ;
#714=CARTESIAN_POINT ( 'NONE',  ( 14.63221749635400037, -52.02998614742870132, -75.83262351151711300 ) ) ;
#715=CARTESIAN_POINT ( 'NONE',  ( 47.23936566397109971, -54.76392035971989714, -54.65942029303390370 ) ) ;
#717=CARTESIAN_POINT ( 'NONE',  ( 56.55522355860080097, -46.21195502513410247, -26.26695352263039851 ) ) ;
#721=CARTESIAN_POINT ( 'NONE',  ( 62.09157612670949788, 4.883811055320659733, -65.34607522167520699 ) ) ;
#722=CARTESIAN_POINT ( 'NONE',  ( 12.16981617636240109, -50.04926268091029584, -21.14999999999999858 ) ) ;
#724=CARTESIAN_POINT ( 'NONE',  ( 48.40030353798399432, 22.94693014320370139, -54.96840899516890033 ) ) ;
#731=CARTESIAN_POINT ( 'NONE',  ( 84.16059178761608450, 12.81961614156949913, -47.12825410637790213 ) ) ;
#732=CARTESIAN_POINT ( 'NONE',  ( 52.87209705597740594, 18.30414775337619915, -27.32974920830639931 ) ) ;
#734=CARTESIAN_POINT ( 'NONE',  ( 10.87995435926834631, 33.74311107132334087, -17.51161114007551944 ) ) ;
#735=CARTESIAN_POINT ( 'NONE',  ( 55.85381426216799383, -45.42888099847450434, -16.16583135229329926 ) ) ;
#739=EDGE_LOOP ( 'NONE', ( #14867, #33257, #22548, #39008 ) ) ;
#740=CARTESIAN_POINT ( 'NONE',  ( 11.60439326024719975, -64.93477792032190621, -16.46429631545650096 ) ) ;
#741=CARTESIAN_POINT ( 'NONE',  ( 9.879544118219747872, 32.17924895645339944, -46.22143104348720044 ) ) ;
#742=CARTESIAN_POINT ( 'NONE',  ( -5.866062602303799167, -15.61618894467929586, -11.65000000000000036 ) ) ;
#743=CARTESIAN_POINT ( 'NONE',  ( 50.02329611982750635, -52.39131470799049595, -51.61201215204189907 ) ) ;
#748=ORIENTED_EDGE ( 'NONE', *, *, #1783, .T. ) ;
#749=DIRECTION ( 'NONE',  ( -0.000000000000000000, -1.000000000000000000, -0.000000000000000000 ) ) ;
#750=CARTESIAN_POINT ( 'NONE',  ( 57.21905121524339677, 14.60424898410619932, -26.25836237551570207 ) ) ;
#751=CARTESIAN_POINT ( 'NONE',  ( 53.64030340482580073, 18.11865384669719603, -49.15850183287659547 ) ) ;
#752=CARTESIAN_POINT ( 'NONE',  ( 47.40322300430459990, 23.42336669154519768, -54.88279555090589668 ) ) ;
#753=CARTESIAN_POINT ( 'NONE',  ( 50.61164247096510138, -50.32864445627969729, -76.14999999999999147 ) ) ;
#754=CARTESIAN_POINT ( 'NONE',  ( 13.39998208309999939, 20.55440457967890211, -74.14999999999999147 ) ) ;
#757=CARTESIAN_POINT ( 'NONE',  ( 16.13393739769620083, -15.61618894467929941, -10.44999999999999929 ) ) ;
#758=DIRECTION ( 'NONE',  ( 0.3569024281753349626, 0.000000000000000000, 0.9341416684649872515 ) ) ;
#760=CARTESIAN_POINT ( 'NONE',  ( 56.46340970796750014, -50.48601309047270291, -52.83593731299979623 ) ) ;
#763=CARTESIAN_POINT ( 'NONE',  ( 13.75277754671100006, -51.30789837932719877, -22.95878748375140077 ) ) ;
#766=CARTESIAN_POINT ( 'NONE',  ( 47.50309824425850280, -54.59962336152860019, -74.17398805956220542 ) ) ;
#768=CYLINDRICAL_SURFACE ( 'NONE', #36235, 5.000000000000000000 ) ;
#772=CARTESIAN_POINT ( 'NONE',  ( 47.16564561314290671, 23.08780115241070163, -75.35584192875380438 ) ) ;
#773=CARTESIAN_POINT ( 'NONE',  ( 19.66714325812582942, -54.07769960979511836, -17.19998964887385995 ) ) ;
#775=AXIS2_PLACEMENT_3D ( 'NONE', #12372, #28335, #4501 ) ;
#777=VECTOR ( 'NONE', #14475, 1000.000000000000000 ) ;
#778=FACE_OUTER_BOUND ( 'NONE', #5985, .T. ) ;
#779=TOROIDAL_SURFACE ( 'NONE', #18371, 23.00000000000000000, 1.000000000000000000 ) ;
#785=CARTESIAN_POINT ( 'NONE',  ( 61.47583438558680058, 13.93519676881970071, -46.65924605088270027 ) ) ;
#786=CARTESIAN_POINT ( 'NONE',  ( -29.90810223010410240, -36.12363263534039248, -56.68161292995529976 ) ) ;
#788=CARTESIAN_POINT ( 'NONE',  ( 53.39264886329749515, -49.37353566164819796, -48.88676049917400235 ) ) ;
#791=CARTESIAN_POINT ( 'NONE',  ( 57.43883263735640554, 14.20764915532410022, -26.07839150191840005 ) ) ;
#793=CARTESIAN_POINT ( 'NONE',  ( 50.57709982134520033, 17.50796619428020406, -76.21964822811550277 ) ) ;
#794=CARTESIAN_POINT ( 'NONE',  ( 52.90392156722190009, 18.39178596602710059, -48.79551525360960085 ) ) ;
#796=DIRECTION ( 'NONE',  ( 1.000000000000000000, 0.000000000000000000, 0.000000000000000000 ) ) ;
#797=CARTESIAN_POINT ( 'NONE',  ( 87.61621807841599718, 17.38381105532069881, -61.12885639714370001 ) ) ;
#798=ORIENTED_EDGE ( 'NONE', *, *, #51697, .F. ) ;
#802=B_SPLINE_CURVE_WITH_KNOTS ( 'NONE', 3,
 ( #21670, #32685, #734, #48979, #33479, #33731, #45550, #45033, #37423, #9645, #1779, #41608, #1267, #49236, #24829, #12816, #13834, #9133 ),
 .UNSPECIFIED., .F., .F.,
 ( 4, 2, 2, 2, 2, 2, 2, 2, 4 ),
 ( 0.000000000000000000, 0.03292105691051003952, 0.2434313698576751894, 0.3750003154496525659, 0.5000002523597224524, 0.5625002208147573679, 0.6625001703428121669, 0.8225000895877013773, 1.000000000000000000 ),
 .UNSPECIFIED. ) ;
#804=CARTESIAN_POINT ( 'NONE',  ( 47.49204623235880263, -54.60559727471500224, -54.98543878004470287 ) ) ;
#805=LINE ( 'NONE', #16806, #569 ) ;
#808=ADVANCED_FACE ( 'NONE', ( #4964 ), #20932, .T. ) ;
#814=VERTEX_POINT ( 'NONE', #46105 ) ;
#815=ORIENTED_EDGE ( 'NONE', *, *, #42486, .F. ) ;
#823=CARTESIAN_POINT ( 'NONE',  ( 52.61122371366529649, 19.76723091249260023, -76.13271378951098711 ) ) ;
#828=EDGE_CURVE ( 'NONE', #27219, #30000, #4327, .T. ) ;
#829=CARTESIAN_POINT ( 'NONE',  ( 60.83513156569119928, 14.48683582043410034, -47.74920551991019835 ) ) ;
#831=B_SPLINE_SURFACE_WITH_KNOTS ( 'NONE', 3, 3, ( 
 ( #44153, #11940, #27897, #43900, #9557, #21322, #5113, #26029, #9814, #13748, #29702, #2205, #49142, #1684, #13999, #42039, #22099, #33895, #49396, #6140, #45194, #24983, #17412, #18182, #14258, #38108 ),
 ( #34148, #37327, #1427, #50161, #9035, #21067, #44935, #33113, #10068, #17924, #33381, #45713, #5630, #25508, #40998, #45456, #25766, #9306, #21579, #37067, #49906, #25253, #41514, #37850, #1165, #17162 ),
 ( #13238, #33641, #13495, #37578, #29189, #29958, #41256, #45976, #29451, #5367, #21843, #17671, #49657, #41773, #5876, #1946, #35195, #27074, #11110, #30997, #11366, #10332, #2981, #39145, #47276, #51198 ),
 ( #3502, #18437, #27329, #3238, #6657, #50934, #42826, #46764, #19471, #30742, #47023, #30483, #6920, #51453, #19213, #46504, #10851, #23131, #46245, #22360, #34675, #18697, #2726, #50675, #43082, #43335 ),
 ( #7427, #31246, #38633, #23376, #7173, #22617, #22873, #15292, #34933, #39400, #35458, #30226, #26293, #42302, #6401, #38364, #18955, #2457, #34414, #50425, #14514, #10595, #26549, #42565, #14773, #26813 ),
 ( #38893, #15030, #8642, #48478, #31505, #4706, #4970, #36663, #9164, #33250, #43588, #37453, #24594, #45062, #45326, #5241, #20674, #49010, #21193, #49266, #1299, #12845, #8908, #36405, #23636, #9431 ),
 ( #13361, #7692, #20415, #28803, #12579, #39652, #20938, #40607, #24858, #44804, #15548, #28544, #11621, #47524, #27584, #29320, #48742, #17032, #25380, #44542, #25119, #16761, #17289, #40866, #766, #32715 ),
 ( #41381, #37200, #36937, #5498, #16499, #4448, #1038, #21454, #510, #32451, #32983, #13115, #29066, #41130, #34543, #30607, #50027, #18566, #6522, #13615, #37711, #50294, #49775, #50546, #37974, #2073 ),
 ( #1552, #38490, #41905, #2326, #26156, #1810, #6005, #17790, #18052, #42166, #17540, #38234, #14637, #22225, #34017, #18300, #10714, #33763, #10459, #21703, #13868, #14120, #34271, #14382, #6266, #30347 ),
 ( #29824, #46371, #22484, #33510, #6787, #2591, #25634, #46628, #26670, #42691, #9930, #45842, #22740, #49524, #41638, #30086, #25892, #29576, #45582, #26413, #42432, #9676, #5747, #21964, #10197, #46111 ) ),
 .UNSPECIFIED., .F., .F., .F.,
 ( 4, 1, 1, 1, 1, 1, 1, 4 ),
 ( 4, 2, 2, 2, 2, 2, 2, 2, 2, 2, 2, 2, 4 ),
 ( 0.000000000000000000, 0.1428571428571430157, 0.2857142857142860315, 0.4285714285714289917, 0.5714285714285709528, 0.7142857142857139685, 0.8571428571428569843, 1.000000000000000000 ),
 ( -6.280768244545899215, -5.577335479905130455, -4.969878459065930620, -4.447679305953560203, -3.925480152841189785, -3.140384122272949607, -2.747836106988829741, -2.273209145326620106, -1.893507575996860037, -1.513806006667089976, -0.9873533102557310315, -0.1450289959975500087, 0.000000000000000000 ),
 .UNSPECIFIED. ) ;
#834=AXIS2_PLACEMENT_3D ( 'NONE', #41617, #26389, #38468 ) ;
#838=CARTESIAN_POINT ( 'NONE',  ( 11.79202694837120013, -65.42741386353530686, -22.35240830876180240 ) ) ;
#840=CARTESIAN_POINT ( 'NONE',  ( 41.30042210802800184, 14.36233479846170091, -6.243946835590840294 ) ) ;
#841=CARTESIAN_POINT ( 'NONE',  ( 14.61074770980889959, 21.25914908875220277, -76.03975947796449475 ) ) ;
#843=CARTESIAN_POINT ( 'NONE',  ( 84.22920232233470017, -43.79788717120040076, -47.02060905303799387 ) ) ;
#844=CARTESIAN_POINT ( 'NONE',  ( 11.09249001374801580, 33.92026773320360888, -17.64371731248376918 ) ) ;
#847=ORIENTED_EDGE ( 'NONE', *, *, #20418, .F. ) ;
#848=CARTESIAN_POINT ( 'NONE',  ( 53.95086563731030083, -48.56598208401319994, -26.86748755849900050 ) ) ;
#849=CARTESIAN_POINT ( 'NONE',  ( 14.59756433005749976, -51.11618894047399664, -22.39374700643829996 ) ) ;
#850=CARTESIAN_POINT ( 'NONE',  ( 50.91427647938718337, -35.37289624976227032, -76.35606773506994216 ) ) ;
#851=CARTESIAN_POINT ( 'NONE',  ( 49.23286883301968686, 12.27403435862436076, -6.320887061515723992 ) ) ;
#853=CARTESIAN_POINT ( 'NONE',  ( 57.55751162087899786, 17.38381105532069881, -53.92796738110899923 ) ) ;
#855=ORIENTED_EDGE ( 'NONE', *, *, #20913, .T. ) ;
#856=AXIS2_PLACEMENT_3D ( 'NONE', #22499, #6022, #38511 ) ;
#857=( BOUNDED_CURVE ( )  B_SPLINE_CURVE ( 3, ( #37730, #33264, #1828, #49540 ),
 .UNSPECIFIED., .F., .T. ) 
 B_SPLINE_CURVE_WITH_KNOTS ( ( 4, 4 ),
 ( 3.588596993660940093, 3.993185569951394953 ),
 .UNSPECIFIED. ) 
 CURVE ( )  GEOMETRIC_REPRESENTATION_ITEM ( )  RATIONAL_B_SPLINE_CURVE ( ( 1.000000000000000000, 0.9864054627567289124, 0.9864054627567289124, 1.000000000000000000 ) ) 
 REPRESENTATION_ITEM ( '' )  );
#858=CARTESIAN_POINT ( 'NONE',  ( -10.40801357085099887, -42.82558555462620120, -6.134105759845330574 ) ) ;
#859=CIRCLE ( 'NONE', #38507, 14.50000000000000178 ) ;
#860=CARTESIAN_POINT ( 'NONE',  ( 47.36460231065780135, 23.44677451268669799, -54.83710734467110370 ) ) ;
#864=CARTESIAN_POINT ( 'NONE',  ( 13.31438294250619947, 19.11297466560260361, -21.15359004513850039 ) ) ;
#865=CARTESIAN_POINT ( 'NONE',  ( 68.13393739769790614, -49.95860450174320277, -71.35146707679190570 ) ) ;
#866=CARTESIAN_POINT ( 'NONE',  ( 42.48652068188589936, 13.02449556106640038, -5.094659062314931042 ) ) ;
#870=CARTESIAN_POINT ( 'NONE',  ( 57.81670062735999949, -47.19152184943609996, -48.15401930624599913 ) ) ;
#873=CARTESIAN_POINT ( 'NONE',  ( 17.80031357392610047, -52.43578441516969946, -75.98739629952659413 ) ) ;
#874=EDGE_CURVE ( 'NONE', #24832, #9203, #1827, .T. ) ;
#876=CARTESIAN_POINT ( 'NONE',  ( 53.38983091188899266, 13.88381105532070059, -12.71718895241959935 ) ) ;
#877=ORIENTED_EDGE ( 'NONE', *, *, #49208, .F. ) ;
#879=CARTESIAN_POINT ( 'NONE',  ( 9.290087568746971058, 31.99567791594350297, -46.53000049651490144 ) ) ;
#883=EDGE_LOOP ( 'NONE', ( #14827, #681, #23999, #42091, #3747, #27412 ) ) ;
#884=CARTESIAN_POINT ( 'NONE',  ( 18.01670405268210118, 20.49345067490170180, -75.53710645103458887 ) ) ;
#888=CARTESIAN_POINT ( 'NONE',  ( 10.30800061085760078, -63.35057298049469665, -45.84700176360160384 ) ) ;
#892=CARTESIAN_POINT ( 'NONE',  ( 61.57064344927020016, 13.99512139804009969, -47.02885309622070054 ) ) ;
#893=EDGE_LOOP ( 'NONE', ( #27966, #19071, #32570, #8359 ) ) ;
#898=CARTESIAN_POINT ( 'NONE',  ( 14.33740833808102266, -52.54004929525823542, -75.96019247807949171 ) ) ;
#899=DIRECTION ( 'NONE',  ( 1.000000000000000000, 0.000000000000000000, 0.000000000000000000 ) ) ;
#901=ORIENTED_EDGE ( 'NONE', *, *, #11130, .T. ) ;
#904=SPHERICAL_SURFACE ( 'NONE', #48457, 3.000000000000000000 ) ;
#905=CARTESIAN_POINT ( 'NONE',  ( 11.22168610241799058, -65.22927118061893736, -17.68872724077263925 ) ) ;
#907=CARTESIAN_POINT ( 'NONE',  ( 60.33694438359629686, 14.62750282847430050, -47.70890968787150399 ) ) ;
#909=CARTESIAN_POINT ( 'NONE',  ( 51.32664003060159530, 13.97355598320289971, -12.12331377635689833 ) ) ;
#911=CARTESIAN_POINT ( 'NONE',  ( -2.623662902750090176, 17.43154064403359982, -4.296538304793199536 ) ) ;
#912=CARTESIAN_POINT ( 'NONE',  ( 59.12150967144670233, 14.27486571672459981, -26.57366796877520088 ) ) ;
#918=CARTESIAN_POINT ( 'NONE',  ( -10.84475574424750022, -41.90441115894699919, -5.029302241765080339 ) ) ;
#919=CARTESIAN_POINT ( 'NONE',  ( 12.39013027391890098, 34.14800971689950160, -46.54379730649250035 ) ) ;
#925=CARTESIAN_POINT ( 'NONE',  ( 47.20301239504629365, 23.55868320956959749, -74.19770771953690769 ) ) ;
#926=CARTESIAN_POINT ( 'NONE',  ( 49.02351734455730536, -53.72042385326109581, -54.35736896012630126 ) ) ;
#927=CARTESIAN_POINT ( 'NONE',  ( 16.13393739769620083, -15.61618894467929941, -11.54999999999999893 ) ) ;
#931=ORIENTED_EDGE ( 'NONE', *, *, #23127, .F. ) ;
#936=CARTESIAN_POINT ( 'NONE',  ( 55.10455769617425403, -45.21089673182738267, -14.92011165637105918 ) ) ;
#938=CARTESIAN_POINT ( 'NONE',  ( 60.93213094286049625, -45.54223981210000005, -47.50418379069640196 ) ) ;
#940=CARTESIAN_POINT ( 'NONE',  ( 50.93003717695669508, 19.69401293973280076, -76.14999999999999147 ) ) ;
#942=CARTESIAN_POINT ( 'NONE',  ( 82.13853704237929776, -45.64188066427789892, -47.72348187592560009 ) ) ;
#943=CARTESIAN_POINT ( 'NONE',  ( 13.39998208309999939, 20.55440457967890211, -23.15000000000000213 ) ) ;
#944=FACE_OUTER_BOUND ( 'NONE', #51750, .T. ) ;
#945=EDGE_CURVE ( 'NONE', #47824, #22043, #25991, .T. ) ;
#946=EDGE_LOOP ( 'NONE', ( #10571, #40119, #3556, #2907 ) ) ;
#947=CARTESIAN_POINT ( 'NONE',  ( 84.08245047910018855, -44.49819807295929763, -47.41523600659849791 ) ) ;
#948=ORIENTED_EDGE ( 'NONE', *, *, #16610, .T. ) ;
#951=CARTESIAN_POINT ( 'NONE',  ( 61.46275447282020110, -45.32732362765139555, -47.26394423894119257 ) ) ;
#953=CARTESIAN_POINT ( 'NONE',  ( 76.44602326054074126, -6.632694491568091877, -12.99482443176448854 ) ) ;
#956=ORIENTED_EDGE ( 'NONE', *, *, #9755, .F. ) ;
#959=CARTESIAN_POINT ( 'NONE',  ( 43.91475033527959937, -43.54611815821230891, -5.093413304872340674 ) ) ;
#961=CARTESIAN_POINT ( 'NONE',  ( 63.88393739769619373, 4.883811055320659733, -61.44999999999999574 ) ) ;
#962=CARTESIAN_POINT ( 'NONE',  ( 62.11841997430489926, -0.01765245207902430002, -16.72251539323920255 ) ) ;
#965=CARTESIAN_POINT ( 'NONE',  ( 6.297163323809750857, 27.24491678059309407, -10.85005457635984882 ) ) ;
#968=FACE_OUTER_BOUND ( 'NONE', #35369, .T. ) ;
#971=CARTESIAN_POINT ( 'NONE',  ( 42.86117915456519967, -43.50499890879240183, -4.698036889839340091 ) ) ;
#973=CARTESIAN_POINT ( 'NONE',  ( 67.04038824939736685, -50.70395984888064334, -74.34354914830332461 ) ) ;
#974=CARTESIAN_POINT ( 'NONE',  ( 61.05708829393459780, -45.70443442833619940, -47.78546717324650217 ) ) ;
#977=CARTESIAN_POINT ( 'NONE',  ( 16.13393739769620083, -15.61618894467929941, -17.93019253464870033 ) ) ;
#978=VECTOR ( 'NONE', #20340, 1000.000000000000114 ) ;
#979=CARTESIAN_POINT ( 'NONE',  ( 66.61546637871180110, 0.7712952386763189949, -17.88089885441980087 ) ) ;
#981=CARTESIAN_POINT ( 'NONE',  ( 13.54479388721200017, -51.82694627962620615, -74.93568190819630104 ) ) ;
#983=CARTESIAN_POINT ( 'NONE',  ( 47.35896996165279660, -54.68274079166319979, -54.83032919328549326 ) ) ;
#985=LINE ( 'NONE', #36352, #4641 ) ;
#990=CARTESIAN_POINT ( 'NONE',  ( 47.81771439681010349, -54.40006451610999960, -54.73537641861789638 ) ) ;
#993=CARTESIAN_POINT ( 'NONE',  ( 56.40268793340759856, 19.51504490916650170, -53.40073823777059658 ) ) ;
#994=CARTESIAN_POINT ( 'NONE',  ( 43.27084646106766996, 12.63989574180925324, -5.051381113503446763 ) ) ;
#995=CARTESIAN_POINT ( 'NONE',  ( 48.58275665155029799, 22.89281328164460305, -55.12556760934580069 ) ) ;
#998=VERTEX_POINT ( 'NONE', #10970 ) ;
#999=CARTESIAN_POINT ( 'NONE',  ( 68.13393739769620083, 11.88381105532070059, -73.64407879467491114 ) ) ;
#1001=CARTESIAN_POINT ( 'NONE',  ( 57.24718408831279959, -50.61618894896510312, -53.91456318529609604 ) ) ;
#1002=CARTESIAN_POINT ( 'NONE',  ( 84.37258452300260103, 12.21853262853879940, -47.24504068948059654 ) ) ;
#1003=CARTESIAN_POINT ( 'NONE',  ( 53.07092938598290033, 18.14261795147120182, -27.35050432211490090 ) ) ;
#1005=CARTESIAN_POINT ( 'NONE',  ( 58.92073396209919878, -15.61618894467929941, -18.64999999999999858 ) ) ;
#1006=CARTESIAN_POINT ( 'NONE',  ( 56.21699821026070509, -45.11618894467940066, -15.04108316657150013 ) ) ;
#1007=EDGE_CURVE ( 'NONE', #9540, #40179, #42785, .T. ) ;
#1009=VERTEX_POINT ( 'NONE', #14633 ) ;
#1010=ADVANCED_FACE ( 'NONE', ( #34536 ), #42685, .T. ) ;
#1012=CARTESIAN_POINT ( 'NONE',  ( 11.73339007446299931, -65.00805721967299178, -16.50122832064900180 ) ) ;
#1013=CARTESIAN_POINT ( 'NONE',  ( 12.68175862228480177, 34.24734278266799947, -47.36921765020689890 ) ) ;
#1015=AXIS2_PLACEMENT_3D ( 'NONE', #38013, #45883, #2108 ) ;
#1017=CARTESIAN_POINT ( 'NONE',  ( 48.01951627911569886, -54.26780672149330087, -54.65612569015529942 ) ) ;
#1022=CARTESIAN_POINT ( 'NONE',  ( 52.83862607968303848, 18.42092619350584570, -28.03263386382830191 ) ) ;
#1023=CARTESIAN_POINT ( 'NONE',  ( 68.13393739769620083, -48.11618894467930119, -76.75000000000000000 ) ) ;
#1024=CARTESIAN_POINT ( 'NONE',  ( 16.13393739769620083, -15.61618894467929941, 7.530187386896120216 ) ) ;
#1026=CARTESIAN_POINT ( 'NONE',  ( 50.57758489713300065, -49.85242741362580432, -76.16361833591838604 ) ) ;
#1031=CARTESIAN_POINT ( 'NONE',  ( 75.13393739769618662, 4.883811055320659733, -84.38499399519520239 ) ) ;
#1032=ORIENTED_EDGE ( 'NONE', *, *, #49842, .F. ) ;
#1033=CARTESIAN_POINT ( 'NONE',  ( 87.04559528857578243, -50.03040250705240055, -61.26127762739950811 ) ) ;
#1034=CARTESIAN_POINT ( 'NONE',  ( 53.39341759735100368, -46.23760979563440543, -14.95068015331019851 ) ) ;
#1036=CARTESIAN_POINT ( 'NONE',  ( 13.89448997836719890, -51.22164804421920081, -22.84403551404049892 ) ) ;
#1037=CARTESIAN_POINT ( 'NONE',  ( 54.78125077669279364, 19.75549256766539941, -75.45543939936278832 ) ) ;
#1038=CARTESIAN_POINT ( 'NONE',  ( 46.84429319214610388, -53.57519873512780606, -75.98322477344710535 ) ) ;
#1041=CARTESIAN_POINT ( 'NONE',  ( 57.12444643026329771, -50.61921117834419448, -53.89324253480139504 ) ) ;
#1044=CARTESIAN_POINT ( 'NONE',  ( 46.79390132917320244, 22.44306139706349867, -75.96020792128800281 ) ) ;
#1046=CARTESIAN_POINT ( 'NONE',  ( 10.85466640524320070, 33.73459223951330443, -17.55961383757199812 ) ) ;
#1047=DIRECTION ( 'NONE',  ( 1.000000000000000000, 0.000000000000000000, 0.000000000000000000 ) ) ;
#1048=VECTOR ( 'NONE', #44595, 1000.000000000000114 ) ;
#1056=CARTESIAN_POINT ( 'NONE',  ( 6.354289799260980587, -65.11185414427920648, -49.17526497145230735 ) ) ;
#1058=CARTESIAN_POINT ( 'NONE',  ( 52.76678904663840086, -49.69688782720479736, -48.54391748749920055 ) ) ;
#1059=CARTESIAN_POINT ( 'NONE',  ( 58.00948627897130194, -45.11615097667539942, -25.49324546217139797 ) ) ;
#1060=CARTESIAN_POINT ( 'NONE',  ( 48.95357505128730224, -53.97596511168250544, -55.27962234102679417 ) ) ;
#1061=CARTESIAN_POINT ( 'NONE',  ( 57.20888602249090127, 14.08682267489909989, -25.90208572559579991 ) ) ;
#1063=CARTESIAN_POINT ( 'NONE',  ( 50.57709999312739768, 17.38380754905400138, -76.21964823130210220 ) ) ;
#1064=CARTESIAN_POINT ( 'NONE',  ( 52.65621920618569618, 18.54360875905199890, -48.47378032971769812 ) ) ;
#1066=CARTESIAN_POINT ( 'NONE',  ( 46.90960454922193890, 22.37535576646249424, -75.96332490880217847 ) ) ;
#1072=CARTESIAN_POINT ( 'NONE',  ( 47.46325745728530165, -54.62024053978399962, -54.87604833503670676 ) ) ;
#1076=CARTESIAN_POINT ( 'NONE',  ( 52.87018954733399312, 18.40735846197139836, -48.66536493865070412 ) ) ;
#1077=DIRECTION ( 'NONE',  ( 0.000000000000000000, 1.000000000000000000, 0.000000000000000000 ) ) ;
#1083=CARTESIAN_POINT ( 'NONE',  ( 8.796734227443069543, -63.17759121671350186, -46.67028841929619887 ) ) ;
#1084=DIRECTION ( 'NONE',  ( 1.000000000000000000, 0.000000000000000000, 0.000000000000000000 ) ) ;
#1085=EDGE_LOOP ( 'NONE', ( #33468, #22180, #43746, #6700 ) ) ;
#1087=DIRECTION ( 'NONE',  ( 0.000000000000000000, 0.000000000000000000, 1.000000000000000000 ) ) ;
#1089=CARTESIAN_POINT ( 'NONE',  ( 52.53869629129660268, 19.33658919202579796, -76.53474691679770103 ) ) ;
#1091=ORIENTED_EDGE ( 'NONE', *, *, #23754, .F. ) ;
#1092=AXIS2_PLACEMENT_3D ( 'NONE', #37068, #29452, #29190 ) ;
#1093=DIRECTION ( 'NONE',  ( 1.000000000000000000, 0.000000000000000000, 0.000000000000000000 ) ) ;
#1100=CARTESIAN_POINT ( 'NONE',  ( 11.38296080374989927, -63.50148532158249282, -24.39902340605380004 ) ) ;
#1105=CARTESIAN_POINT ( 'NONE',  ( 14.35648533949829897, 20.67521890232639947, -75.71427953954510315 ) ) ;
#1106=EDGE_CURVE ( 'NONE', #14173, #483, #41913, .T. ) ;
#1108=ADVANCED_FACE ( 'NONE', ( #35047, #10710 ), #26663, .T. ) ;
#1109=CARTESIAN_POINT ( 'NONE',  ( 83.45566905280610115, -44.67438416926519551, -46.48561260377719861 ) ) ;
#1113=CARTESIAN_POINT ( 'NONE',  ( 53.29233422487229888, -49.24065040618290112, -27.36763233434339782 ) ) ;
#1114=CARTESIAN_POINT ( 'NONE',  ( 16.65429250103910164, -51.11618894347319753, -20.30769847209390022 ) ) ;
#1117=CARTESIAN_POINT ( 'NONE',  ( 83.89200044194980421, 17.38381105532069881, -53.92796738110899923 ) ) ;
#1119=ORIENTED_EDGE ( 'NONE', *, *, #22600, .T. ) ;
#1120=CARTESIAN_POINT ( 'NONE',  ( -3.322299359250789674, -48.33316442662350454, -4.794339771350640156 ) ) ;
#1121=AXIS2_PLACEMENT_3D ( 'NONE', #26654, #30332, #31102 ) ;
#1122=CARTESIAN_POINT ( 'NONE',  ( 47.25269221664989772, 23.52078290745969724, -54.62328044731309973 ) ) ;
#1123=PLANE ( 'NONE',  #43774 ) ;
#1126=CARTESIAN_POINT ( 'NONE',  ( 10.86720897088950011, 33.73900725339469631, -17.53558621447849930 ) ) ;
#1130=CARTESIAN_POINT ( 'NONE',  ( 56.66108174125150043, -47.79774483192920087, -48.40197048052689865 ) ) ;
#1131=CARTESIAN_POINT ( 'NONE',  ( 52.82976730393809817, 18.42853680774779690, -28.15002497595520126 ) ) ;
#1132=CARTESIAN_POINT ( 'NONE',  ( 52.73680207265829978, 20.85125113597840141, -53.40499982253649591 ) ) ;
#1138=CARTESIAN_POINT ( 'NONE',  ( 10.14269527681349992, 32.00387675655870368, -45.99343597682049989 ) ) ;
#1140=CARTESIAN_POINT ( 'NONE',  ( 67.02524171442360057, -29.91412924832570042, -17.24420288053820016 ) ) ;
#1142=CARTESIAN_POINT ( 'NONE',  ( 17.94181465708570045, 20.01251569944690090, -74.87640169473949925 ) ) ;
#1143=ORIENTED_EDGE ( 'NONE', *, *, #5904, .T. ) ;
#1145=CARTESIAN_POINT ( 'NONE',  ( 47.68999173674550462, 23.28182553471719984, -55.17369749140770097 ) ) ;
#1147=CARTESIAN_POINT ( 'NONE',  ( 10.51296283413299903, -64.44909923135459451, -46.46298057769340062 ) ) ;
#1148=CARTESIAN_POINT ( 'NONE',  ( 57.12778779988809674, -45.34015298987380049, -25.89881448804210251 ) ) ;
#1150=CARTESIAN_POINT ( 'NONE',  ( 61.57131126144769695, 13.93819913114500153, -46.80234620618990249 ) ) ;
#1152=ORIENTED_EDGE ( 'NONE', *, *, #30983, .T. ) ;
#1154=DIRECTION ( 'NONE',  ( 0.000000000000000000, -1.000000000000000000, 0.000000000000000000 ) ) ;
#1155=DIRECTION ( 'NONE',  ( -1.000000000000000000, 0.000000000000000000, 0.000000000000000000 ) ) ;
#1156=ORIENTED_EDGE ( 'NONE', *, *, #45674, .T. ) ;
#1157=CARTESIAN_POINT ( 'NONE',  ( 51.67634973896889505, -45.99404415929730305, -13.53858448670719916 ) ) ;
#1160=DIRECTION ( 'NONE',  ( -2.217154000000000151E-17, -9.040936000000000316E-17, 1.000000000000000000 ) ) ;
#1161=ORIENTED_EDGE ( 'NONE', *, *, #38814, .F. ) ;
#1163=DIRECTION ( 'NONE',  ( 0.000000000000000000, 0.000000000000000000, -1.000000000000000000 ) ) ;
#1164=CIRCLE ( 'NONE', #51377, 1.999999999999999556 ) ;
#1165=CARTESIAN_POINT ( 'NONE',  ( 47.20319696544930110, -54.79145866998830172, -74.17413012813480577 ) ) ;
#1166=CARTESIAN_POINT ( 'NONE',  ( 73.28401566534610367, 12.46528443789909879, -12.81730577991920050 ) ) ;
#1167=CARTESIAN_POINT ( 'NONE',  ( 53.12059660037449760, -49.56856005606769600, -49.12440250185819934 ) ) ;
#1171=CARTESIAN_POINT ( 'NONE',  ( -6.895251857565479980, 14.63674971373709965, -5.069369356803940185 ) ) ;
#1173=CARTESIAN_POINT ( 'NONE',  ( 61.34394966329610099, 13.89927047214030154, -27.35702754952210114 ) ) ;
#1174=EDGE_CURVE ( 'NONE', #7868, #5274, #3430, .T. ) ;
#1177=CARTESIAN_POINT ( 'NONE',  ( 53.43679795862760074, 18.11049644000969749, -48.83615822496579995 ) ) ;
#1179=CARTESIAN_POINT ( 'NONE',  ( -9.920770761350539146, -43.31452625206590312, -5.970037222519819942 ) ) ;
#1180=FACE_OUTER_BOUND ( 'NONE', #24859, .T. ) ;
#1182=FACE_OUTER_BOUND ( 'NONE', #28159, .T. ) ;
#1184=FACE_OUTER_BOUND ( 'NONE', #22076, .T. ) ;
#1185=CARTESIAN_POINT ( 'NONE',  ( 47.06490539288780184, 23.30732543520909772, -75.17786433282310554 ) ) ;
#1186=CARTESIAN_POINT ( 'NONE',  ( 49.02675822138120054, -53.86209816185859722, -54.70857181914429646 ) ) ;
#1187=CARTESIAN_POINT ( 'NONE',  ( 41.93138893772210452, -44.52284172065920131, -5.197898045262170363 ) ) ;
#1188=AXIS2_PLACEMENT_3D ( 'NONE', #30496, #50437, #50946 ) ;
#1192=EDGE_CURVE ( 'NONE', #36035, #22605, #51866, .T. ) ;
#1193=ORIENTED_EDGE ( 'NONE', *, *, #2776, .F. ) ;
#1197=CARTESIAN_POINT ( 'NONE',  ( 85.66799001034409855, 19.38381105532069881, -61.58097075742929860 ) ) ;
#1198=CARTESIAN_POINT ( 'NONE',  ( 60.82911148122739320, -45.58366361498899977, -47.52550039496580325 ) ) ;
#1199=CARTESIAN_POINT ( 'NONE',  ( 56.93701001016370356, 19.40825549114710213, -53.86363390760720193 ) ) ;
#1200=CARTESIAN_POINT ( 'NONE',  ( 12.69621344236849936, 18.74918026471999966, -21.09935757923890165 ) ) ;
#1202=FACE_OUTER_BOUND ( 'NONE', #23308, .T. ) ;
#1203=CARTESIAN_POINT ( 'NONE',  ( 52.03944403422909915, -51.37790098174010467, -75.97489327030881157 ) ) ;
#1205=ORIENTED_EDGE ( 'NONE', *, *, #18866, .T. ) ;
#1206=CARTESIAN_POINT ( 'NONE',  ( 84.25371145582080601, -44.18318432820999675, -47.43624648648039965 ) ) ;
#1208=ORIENTED_EDGE ( 'NONE', *, *, #16789, .F. ) ;
#1210=CARTESIAN_POINT ( 'NONE',  ( 61.50405222244170034, -45.37411808438429262, -47.35446793284499734 ) ) ;
#1211=CARTESIAN_POINT ( 'NONE',  ( 52.74431155066509547, -49.74087895501130419, -48.86925626324400440 ) ) ;
#1212=CARTESIAN_POINT ( 'NONE',  ( 61.26174344272975958, 14.35308087949198708, -47.65928943619329061 ) ) ;
#1213=DIRECTION ( 'NONE',  ( -1.451784999999999966E-10, 6.183944999999999577E-11, 1.000000000000000000 ) ) ;
#1218=ORIENTED_EDGE ( 'NONE', *, *, #7596, .F. ) ;
#1219=CARTESIAN_POINT ( 'NONE',  ( 56.74347695815399817, 19.18629571232069964, -52.86071028956509821 ) ) ;
#1222=CARTESIAN_POINT ( 'NONE',  ( 14.16187783161290170, -50.35113599914600258, -20.85710678118659800 ) ) ;
#1224=CARTESIAN_POINT ( 'NONE',  ( 17.92370450339619836, 19.88381105532299742, -74.14999999999999147 ) ) ;
#1226=EDGE_LOOP ( 'NONE', ( #51735, #40981, #47829, #33821, #877, #37585, #23815, #23897, #32974, #29371 ) ) ;
#1227=CARTESIAN_POINT ( 'NONE',  ( 57.49008833992955658, -50.10650853560072449, -52.59398466008588002 ) ) ;
#1228=CARTESIAN_POINT ( 'NONE',  ( 51.81517742741720411, -50.18339821138420120, -76.50774528515320583 ) ) ;
#1233=CARTESIAN_POINT ( 'NONE',  ( 45.06709565917970650, 13.92152238313070178, -7.502891261494740505 ) ) ;
#1235=CARTESIAN_POINT ( 'NONE',  ( 41.93138893772210452, -44.52284172065920131, -5.197898045262170363 ) ) ;
#1237=DIRECTION ( 'NONE',  ( -1.000000000000000000, 0.000000000000000000, 0.000000000000000000 ) ) ;
#1238=AXIS2_PLACEMENT_3D ( 'NONE', #41872, #6756, #3080 ) ;
#1241=CARTESIAN_POINT ( 'NONE',  ( -23.86606260230380272, -15.61618894467908092, -53.92777777777782688 ) ) ;
#1242=CARTESIAN_POINT ( 'NONE',  ( 65.61836598397030684, 0.5117851582676719024, -17.32554831824890229 ) ) ;
#1243=ADVANCED_FACE ( 'NONE', ( #14771 ), #24019, .T. ) ;
#1245=CARTESIAN_POINT ( 'NONE',  ( 13.87305293863050082, -51.45286096150079658, -74.99552951438440118 ) ) ;
#1246=CARTESIAN_POINT ( 'NONE',  ( 57.28958349610260115, 19.33036382309920143, -53.44848231829909935 ) ) ;
#1248=CARTESIAN_POINT ( 'NONE',  ( 83.71507592998568725, 13.22434697382143298, -46.59591546942163376 ) ) ;
#1251=CARTESIAN_POINT ( 'NONE',  ( 57.35132949813925762, 14.51266520188007902, -26.25078878154161188 ) ) ;
#1252=CARTESIAN_POINT ( 'NONE',  ( 47.69530821581999902, -54.51124612977650230, -55.10855014336240032 ) ) ;
#1254=CARTESIAN_POINT ( 'NONE',  ( 38.13393739769620083, -15.61618894467929941, -13.15000000000000036 ) ) ;
#1256=CARTESIAN_POINT ( 'NONE',  ( 56.38979760733869995, 19.45007144631160045, -53.17790575662699837 ) ) ;
#1257=CARTESIAN_POINT ( 'NONE',  ( 48.76650864246020234, 22.82327037976499895, -55.26805329862090588 ) ) ;
#1258=ORIENTED_EDGE ( 'NONE', *, *, #24321, .T. ) ;
#1264=CARTESIAN_POINT ( 'NONE',  ( 83.43488124258610128, 13.92192429134099996, -47.39353206303620425 ) ) ;
#1265=CARTESIAN_POINT ( 'NONE',  ( 54.74050131502779948, 16.39029591686540144, -26.36129443285850016 ) ) ;
#1267=CARTESIAN_POINT ( 'NONE',  ( 11.74347662707552153, 33.65273995683249808, -16.31133514116600125 ) ) ;
#1269=B_SPLINE_SURFACE_WITH_KNOTS ( 'NONE', 3, 3, ( 
 ( #40469, #20277, #44928, #28659, #44663, #8767, #16363, #12972, #40733, #12436, #24717, #4831, #16894, #9029, #10325, #14249 ),
 ( #38103, #13487, #6394, #30219, #1157, #33375, #49135, #17153, #13233, #34142, #33633, #1936, #46238, #49391, #29953, #1679 ),
 ( #9807, #29446, #45451, #1420, #26022, #5869, #9552, #2199, #13994, #25756, #33889, #22090, #42034, #9298, #17666, #21836 ),
 ( #13742, #25503, #26286, #37843, #45706, #41767, #41250, #18175, #6133, #41508, #21575, #5620, #50154, #42294, #22354, #33106 ),
 ( #17918, #21318, #29184, #17406, #37571, #49899, #45968, #10061, #45185, #49650, #25248, #29695, #5362, #37319, #14506, #22863 ),
 ( #34404, #15286, #30476, #26543, #38884, #42558, #2717, #35188, #43329, #11356, #47269, #39139, #6649, #7168, #51192, #31240 ) ),
 .UNSPECIFIED., .F., .F., .F.,
 ( 4, 1, 1, 4 ),
 ( 4, 2, 2, 2, 2, 2, 2, 4 ),
 ( -7.901482146000000741E-06, 0.3333333333333329818, 0.6666666666666670737, 1.000000000266519917 ),
 ( -7.901482146000000741E-06, 2.041349754395100025, 4.374320902275219858, 5.832427869700300249, 6.561481353412840001, 7.727966927352889925, 9.594343845656990055, 11.66486364088270022 ),
 .UNSPECIFIED. ) ;
#1271=ORIENTED_EDGE ( 'NONE', *, *, #30459, .T. ) ;
#1273=CARTESIAN_POINT ( 'NONE',  ( 12.08205748224309950, -65.27925620804988682, -16.92411159753779870 ) ) ;
#1274=CARTESIAN_POINT ( 'NONE',  ( 12.89154239176200001, 34.27648701824740129, -47.61655765160880094 ) ) ;
#1277=CARTESIAN_POINT ( 'NONE',  ( 51.45476138140149658, 3.156784108801740985, -76.74519123628812167 ) ) ;
#1280=CARTESIAN_POINT ( 'NONE',  ( 59.49262858449159808, -50.48013859002959691, -53.20292136905285929 ) ) ;
#1282=CARTESIAN_POINT ( 'NONE',  ( 13.55699286802090420, 20.68057025407604499, -75.01676221294341929 ) ) ;
#1288=CARTESIAN_POINT ( 'NONE',  ( 54.75911359420939561, -47.36916784795560176, -25.73144026446449928 ) ) ;
#1293=AXIS2_PLACEMENT_3D ( 'NONE', #39345, #27526, #11829 ) ;
#1295=CARTESIAN_POINT ( 'NONE',  ( 52.88663104391009995, -49.66786150580319514, -48.99336411538499902 ) ) ;
#1297=CARTESIAN_POINT ( 'NONE',  ( 60.34379259250669492, 14.63564649040839960, -47.72732609510669732 ) ) ;
#1298=CARTESIAN_POINT ( 'NONE',  ( 54.70440021269280351, 19.88794248854869906, -75.31486140208340885 ) ) ;
#1299=CARTESIAN_POINT ( 'NONE',  ( 47.39174436423379433, -54.56554572047070195, -74.72285389774751252 ) ) ;
#1300=ORIENTED_EDGE ( 'NONE', *, *, #10372, .T. ) ;
#1301=CARTESIAN_POINT ( 'NONE',  ( 55.96902517572589630, 14.60256971682040117, -17.77637908280700429 ) ) ;
#1302=CARTESIAN_POINT ( 'NONE',  ( 57.00264675662779723, -50.63106778522559637, -53.72993499349190216 ) ) ;
#1303=CARTESIAN_POINT ( 'NONE',  ( 52.56369620065810011, -49.86341771588610072, -48.47378032971909789 ) ) ;
#1306=ADVANCED_FACE ( 'NONE', ( #5017 ), #28656, .T. ) ;
#1307=AXIS2_PLACEMENT_3D ( 'NONE', #50998, #30544, #15617 ) ;
#1308=VERTEX_POINT ( 'NONE', #21495 ) ;
#1309=CARTESIAN_POINT ( 'NONE',  ( 46.71512400210709615, 22.30641209017640136, -76.02645024177060407 ) ) ;
#1311=CARTESIAN_POINT ( 'NONE',  ( 41.38327847047529673, -45.62082798267930173, -6.314269469673459589 ) ) ;
#1312=CARTESIAN_POINT ( 'NONE',  ( 12.32961272724990032, 33.41202109490849637, -15.85993007184249848 ) ) ;
#1314=CARTESIAN_POINT ( 'NONE',  ( 60.31639983754979539, -45.83544975381219189, -47.65366050515983432 ) ) ;
#1319=CARTESIAN_POINT ( 'NONE',  ( -26.90058206776739880, -41.85481090454489816, -56.03720707547429924 ) ) ;
#1321=( BOUNDED_CURVE ( )  B_SPLINE_CURVE ( 3, ( #30585, #50783, #14615, #35565 ),
 .UNSPECIFIED., .F., .T. ) 
 B_SPLINE_CURVE_WITH_KNOTS ( ( 4, 4 ),
 ( 5.497787143782143282, 5.746835782486941824 ),
 .UNSPECIFIED. ) 
 CURVE ( )  GEOMETRIC_REPRESENTATION_ITEM ( )  RATIONAL_B_SPLINE_CURVE ( ( 1.000000000000000000, 0.9948379068877977183, 0.9948379068877977183, 1.000000000000000000 ) ) 
 REPRESENTATION_ITEM ( '' )  );
#1322=CARTESIAN_POINT ( 'NONE',  ( 52.78519993256289666, -49.68938364784359152, -48.68758331618039392 ) ) ;
#1323=CARTESIAN_POINT ( 'NONE',  ( 59.21978530496789972, -45.12527060529160394, -25.93003219259560055 ) ) ;
#1325=CARTESIAN_POINT ( 'NONE',  ( 48.72504344960389489, -54.07331086023990707, -55.30415983355479881 ) ) ;
#1326=CARTESIAN_POINT ( 'NONE',  ( 56.88551911260069716, 14.51619878703609956, -26.16768187466989559 ) ) ;
#1328=CARTESIAN_POINT ( 'NONE',  ( 50.13210307260710152, 17.67415490553439739, -76.14999999999999147 ) ) ;
#1329=CARTESIAN_POINT ( 'NONE',  ( 52.66273062025209839, 18.53842598467419833, -48.50781030805210037 ) ) ;
#1332=CARTESIAN_POINT ( 'NONE',  ( 46.52565834994577898, 21.89345249407521621, -76.13734531344884715 ) ) ;
#1334=EDGE_LOOP ( 'NONE', ( #1354, #15466, #17577, #13098, #33374 ) ) ;
#1337=CARTESIAN_POINT ( 'NONE',  ( 47.40218600936929505, -54.65618228108590415, -54.84992837070570459 ) ) ;
#1340=CARTESIAN_POINT ( 'NONE',  ( 60.25958433222680100, 14.85042903512990087, -48.01680402935890157 ) ) ;
#1341=CARTESIAN_POINT ( 'NONE',  ( -31.86606260230380627, -15.61618894467930474, -76.14999999999999147 ) ) ;
#1342=FACE_OUTER_BOUND ( 'NONE', #34261, .T. ) ;
#1347=CARTESIAN_POINT ( 'NONE',  ( 9.293307013010640105, -63.25115262801180194, -46.52992041538980317 ) ) ;
#1348=ADVANCED_FACE ( 'NONE', ( #6049 ), #12789, .T. ) ;
#1353=CARTESIAN_POINT ( 'NONE',  ( 53.91131433573680454, 19.51725069840180282, -76.32773059538270388 ) ) ;
#1354=ORIENTED_EDGE ( 'NONE', *, *, #2281, .F. ) ;
#1355=CARTESIAN_POINT ( 'NONE',  ( 10.47406283454438203, 31.88305279702909800, -45.62066736167659542 ) ) ;
#1362=EDGE_LOOP ( 'NONE', ( #37307, #7671, #15273, #21352 ) ) ;
#1363=CARTESIAN_POINT ( 'NONE',  ( 59.11315108609827007, -47.49289742320240038, -49.51859781974984998 ) ) ;
#1365=CARTESIAN_POINT ( 'NONE',  ( 52.62851868536470334, -49.80923738442960769, -48.67162951074860189 ) ) ;
#1366=CIRCLE ( 'NONE', #21432, 1.999999999999999778 ) ;
#1369=AXIS2_PLACEMENT_3D ( 'NONE', #35812, #18788, #43171 ) ;
#1371=CARTESIAN_POINT ( 'NONE',  ( 13.98848244166460120, 20.97417580057960151, -75.67041253543310120 ) ) ;
#1372=CARTESIAN_POINT ( 'NONE',  ( 51.68229386154369820, 17.53316009977629975, -77.01557736631420426 ) ) ;
#1376=CARTESIAN_POINT ( 'NONE',  ( 55.61276803169860017, -46.45957139663980229, -25.89158459899769582 ) ) ;
#1377=CARTESIAN_POINT ( 'NONE',  ( 14.04279605691000121, -50.94365768270629502, -21.72007173761920029 ) ) ;
#1378=CARTESIAN_POINT ( 'NONE',  ( 11.93454077925219892, 32.88420340368310235, -15.38530629706399999 ) ) ;
#1380=CARTESIAN_POINT ( 'NONE',  ( -11.00461184790416524, -51.23639054309960983, -51.06967761013345353 ) ) ;
#1382=CARTESIAN_POINT ( 'NONE',  ( -8.382319638490058011, -44.65444820222590039, -5.282248192611979754 ) ) ;
#1383=CARTESIAN_POINT ( 'NONE',  ( 47.23442391913490468, 23.53533408100059887, -54.66895834688099853 ) ) ;
#1384=AXIS2_PLACEMENT_3D ( 'NONE', #341, #51214, #43856 ) ;
#1385=CARTESIAN_POINT ( 'NONE',  ( 56.48539520774843226, -50.76770210929910832, -53.84780620286824160 ) ) ;
#1387=CARTESIAN_POINT ( 'NONE',  ( 74.17629866868290378, -33.11618894467940066, -65.34607522167520699 ) ) ;
#1388=CARTESIAN_POINT ( 'NONE',  ( 11.82896774831129960, 34.18482258325850154, -17.62577553875959779 ) ) ;
#1390=CARTESIAN_POINT ( 'NONE',  ( 53.05372063824089679, 18.31120138125479713, -48.79446872373849686 ) ) ;
#1392=CARTESIAN_POINT ( 'NONE',  ( 57.22322293371580315, -47.50141109488779989, -48.27531557238859961 ) ) ;
#1393=CARTESIAN_POINT ( 'NONE',  ( 53.20717401374850652, 18.10213357476860097, -27.47939579088139794 ) ) ;
#1394=CARTESIAN_POINT ( 'NONE',  ( 52.21238886552460201, 21.07428037441609803, -53.50655909053360659 ) ) ;
#1396=CARTESIAN_POINT ( 'NONE',  ( 52.88720174365979432, 13.88381105532070059, -12.35033059909330078 ) ) ;
#1399=CARTESIAN_POINT ( 'NONE',  ( 9.731815933137479391, 31.93091152407239619, -46.29980776193180247 ) ) ;
#1403=CARTESIAN_POINT ( 'NONE',  ( 17.96427685920679806, 20.25300558755819935, -75.29799846200430125 ) ) ;
#1406=VERTEX_POINT ( 'NONE', #6830 ) ;
#1409=VERTEX_POINT ( 'NONE', #22781 ) ;
#1410=CARTESIAN_POINT ( 'NONE',  ( 11.17576989425459999, -64.81915578497500974, -46.44971693985230132 ) ) ;
#1411=CARTESIAN_POINT ( 'NONE',  ( 57.41360129382550070, -45.61097492619999372, -26.20065532981040235 ) ) ;
#1413=DIRECTION ( 'NONE',  ( 0.000000000000000000, 0.000000000000000000, 1.000000000000000000 ) ) ;
#1414=ADVANCED_FACE ( 'NONE', ( #19383 ), #47187, .T. ) ;
#1415=CARTESIAN_POINT ( 'NONE',  ( 61.71045229757179840, 13.90353478476480120, -46.65737748138349872 ) ) ;
#1418=CARTESIAN_POINT ( 'NONE',  ( 75.20566382767655966, 0.9154195451593050148, -12.07278360623682190 ) ) ;
#1420=CARTESIAN_POINT ( 'NONE',  ( 52.47575601967660219, -45.60254204323580041, -13.75339527049669996 ) ) ;
#1423=DIRECTION ( 'NONE',  ( -0.7288689868556610385, 0.6846531968814593139, 0.000000000000000000 ) ) ;
#1427=CARTESIAN_POINT ( 'NONE',  ( 46.45131131807830371, -53.13009906462109910, -76.13977852870850427 ) ) ;
#1428=CARTESIAN_POINT ( 'NONE',  ( 75.20081098849910006, 13.72681413341010170, -14.38878604297190122 ) ) ;
#1430=CARTESIAN_POINT ( 'NONE',  ( 45.31002628895360118, 14.31856235321039961, -8.676032249097868743 ) ) ;
#1431=EDGE_CURVE ( 'NONE', #22850, #15006, #38801, .T. ) ;
#1433=LINE ( 'NONE', #34877, #17322 ) ;
#1435=CARTESIAN_POINT ( 'NONE',  ( 11.12431739752382320, 24.06965717816936845, -21.40301502515332999 ) ) ;
#1437=CARTESIAN_POINT ( 'NONE',  ( 58.35547055286580331, 14.14095518617109981, -26.20742642234660025 ) ) ;
#1444=CARTESIAN_POINT ( 'NONE',  ( 11.47551314106880049, -64.97235711416220738, -16.61573023122599935 ) ) ;
#1447=CARTESIAN_POINT ( 'NONE',  ( 49.25252623552799491, -53.65403535679590163, -54.36973269069940073 ) ) ;
#1455=CARTESIAN_POINT ( 'NONE',  ( 83.67474313643315043, -44.49425646638592724, -46.57587831639807519 ) ) ;
#1456=CARTESIAN_POINT ( 'NONE',  ( 60.85786081670519820, -45.57206638213919803, -47.51990102095140145 ) ) ;
#1458=CARTESIAN_POINT ( 'NONE',  ( 13.50362950008909912, 18.90074601879630123, -20.96762847675789843 ) ) ;
#1462=CARTESIAN_POINT ( 'NONE',  ( 60.40024892680336421, -45.69452726455055114, -47.21879065637983075 ) ) ;
#1469=CARTESIAN_POINT ( 'NONE',  ( 61.73009793398990297, -45.11618193111070241, -46.50780714789189574 ) ) ;
#1470=CARTESIAN_POINT ( 'NONE',  ( 47.65701684106380043, -54.43194395141289732, -54.14467735021966632 ) ) ;
#1471=ADVANCED_FACE ( 'NONE', ( #50845 ), #29523, .T. ) ;
#1473=EDGE_CURVE ( 'NONE', #38811, #24770, #23474, .T. ) ;
#1475=ORIENTED_EDGE ( 'NONE', *, *, #32075, .T. ) ;
#1476=VERTEX_POINT ( 'NONE', #488 ) ;
#1477=EDGE_CURVE ( 'NONE', #34084, #28709, #47785, .T. ) ;
#1478=ORIENTED_EDGE ( 'NONE', *, *, #24385, .T. ) ;
#1485=ORIENTED_EDGE ( 'NONE', *, *, #20741, .F. ) ;
#1487=CARTESIAN_POINT ( 'NONE',  ( 52.51047230659040110, -50.98242248866299775, -76.15156771093519694 ) ) ;
#1489=CARTESIAN_POINT ( 'NONE',  ( 83.87141997220982148, -44.85900116921240510, -47.47133103328876302 ) ) ;
#1493=CARTESIAN_POINT ( 'NONE',  ( 43.82162984104279957, 13.85296797899130006, -6.692196338156839452 ) ) ;
#1495=CARTESIAN_POINT ( 'NONE',  ( 42.16203264904510206, -44.19296810100679807, -4.955231405260050792 ) ) ;
#1497=CARTESIAN_POINT ( 'NONE',  ( 56.61650758228095270, 14.09311236904805575, -25.29355102104276298 ) ) ;
#1500=CARTESIAN_POINT ( 'NONE',  ( 65.88923117608129587, 0.1772000611986560004, -17.14611195593310100 ) ) ;
#1502=CARTESIAN_POINT ( 'NONE',  ( 13.51893541109899921, -51.88241111310259868, -74.91994212301230505 ) ) ;
#1503=CARTESIAN_POINT ( 'NONE',  ( 47.20789789792050328, -54.78773433559100425, -54.64276886469819772 ) ) ;
#1505=CARTESIAN_POINT ( 'NONE',  ( 15.67962062493570130, 19.63028992856250099, -20.15000000000000213 ) ) ;
#1509=CARTESIAN_POINT ( 'NONE',  ( 47.79491795492819506, -54.42065591789820189, -54.76904050234069388 ) ) ;
#1510=CARTESIAN_POINT ( 'NONE',  ( 14.25134537629159937, 19.88704348313540393, -22.60288543027370167 ) ) ;
#1513=CARTESIAN_POINT ( 'NONE',  ( 48.02894741700589520, 23.13744333908370265, -55.28037973459740329 ) ) ;
#1514=ORIENTED_EDGE ( 'NONE', *, *, #8021, .T. ) ;
#1516=VERTEX_POINT ( 'NONE', #10173 ) ;
#1517=LINE ( 'NONE', #475, #34553 ) ;
#1520=CARTESIAN_POINT ( 'NONE',  ( 82.76927220787719364, 14.00476221583219960, -47.14638044783710313 ) ) ;
#1521=CARTESIAN_POINT ( 'NONE',  ( 54.52192486798780635, 16.42131495964800436, -25.85211914981980286 ) ) ;
#1524=CARTESIAN_POINT ( 'NONE',  ( 57.38548500607319625, -45.11618894467940066, -16.91114573195289950 ) ) ;
#1525=CARTESIAN_POINT ( 'NONE',  ( 68.13393739769620083, -29.61618894467929763, -65.65000000000000568 ) ) ;
#1528=CARTESIAN_POINT ( 'NONE',  ( 11.77474680306579913, -65.05674245715520954, -16.56178175561650079 ) ) ;
#1529=CARTESIAN_POINT ( 'NONE',  ( 11.95619557619699869, 33.96145947778699536, -46.48573944864449459 ) ) ;
#1533=CARTESIAN_POINT ( 'NONE',  ( 11.19961559249191474, -65.24734874261105233, -46.39999999999999858 ) ) ;
#1534=ORIENTED_EDGE ( 'NONE', *, *, #47452, .T. ) ;
#1535=EDGE_CURVE ( 'NONE', #21630, #5671, #42400, .T. ) ;
#1537=CARTESIAN_POINT ( 'NONE',  ( 54.10074222690910517, 17.30990981831594766, -26.94461139255280457 ) ) ;
#1539=CARTESIAN_POINT ( 'NONE',  ( 48.53787819235320455, 22.50666767116170064, -53.55604134326550536 ) ) ;
#1540=CARTESIAN_POINT ( 'NONE',  ( 63.10112488574510792, -1.418970404380659911, -16.22863366573779587 ) ) ;
#1541=CARTESIAN_POINT ( 'NONE',  ( 50.83757470097779674, -48.72856112802359263, -76.31330844465840357 ) ) ;
#1545=VERTEX_POINT ( 'NONE', #9657 ) ;
#1548=CARTESIAN_POINT ( 'NONE',  ( 16.13393739769620083, -15.61618894467929941, -76.14999999999999147 ) ) ;
#1550=CARTESIAN_POINT ( 'NONE',  ( 14.25092085129799990, -51.11945063234009723, -22.60339916836199947 ) ) ;
#1551=CARTESIAN_POINT ( 'NONE',  ( 56.79308212940160416, 19.43544009391369798, -74.33926175450910989 ) ) ;
#1552=CARTESIAN_POINT ( 'NONE',  ( 46.35275103504449845, -52.90993241930539881, -76.14999999999999147 ) ) ;
#1554=CARTESIAN_POINT ( 'NONE',  ( 55.83827540872459849, 14.63062675802740031, -17.19948835330949777 ) ) ;
#1555=CARTESIAN_POINT ( 'NONE',  ( 57.16059588472099762, -50.58286358578039454, -53.44447636780149935 ) ) ;
#1556=CARTESIAN_POINT ( 'NONE',  ( 52.69370164499209608, -49.76876103374040383, -48.79614663361950022 ) ) ;
#1558=CARTESIAN_POINT ( 'NONE',  ( 61.28293951594075395, 14.37135162400847577, -47.68063998569994055 ) ) ;
#1559=ORIENTED_EDGE ( 'NONE', *, *, #50815, .T. ) ;
#1560=CARTESIAN_POINT ( 'NONE',  ( 47.14495913819140327, 22.93959528134109860, -75.51614565245159838 ) ) ;
#1562=B_SPLINE_CURVE_WITH_KNOTS ( 'NONE', 3,
 ( #6945, #42060, #38659, #2747, #49929, #33912, #2483, #22119, #18464, #34437, #14020 ),
 .UNSPECIFIED., .F., .F.,
 ( 4, 2, 1, 2, 2, 4 ),
 ( 0.5057982913668825908, 0.5366858981564543996, 0.5675735049460263193, 0.6293487185251679383, 0.7528991456834492890, 1.000000000000000000 ),
 .UNSPECIFIED. ) ;
#1563=CARTESIAN_POINT ( 'NONE',  ( 60.83524288460374407, -45.71913028275803725, -47.74946701498301138 ) ) ;
#1567=CARTESIAN_POINT ( 'NONE',  ( 82.45640976213999807, 13.86031052324960022, -46.38984575855459980 ) ) ;
#1571=CARTESIAN_POINT ( 'NONE',  ( 61.26297983503680200, 14.01014034993499990, -46.58707769322979431 ) ) ;
#1573=CARTESIAN_POINT ( 'NONE',  ( 6.156981251802729815, -64.53629940273539489, -47.78905844757039745 ) ) ;
#1576=CARTESIAN_POINT ( 'NONE',  ( 52.85276835010299834, -49.64923573467969931, -48.69281397809770340 ) ) ;
#1578=CIRCLE ( 'NONE', #34180, 2.000000000000001776 ) ;
#1579=CARTESIAN_POINT ( 'NONE',  ( 57.69121261463050132, -45.19183260204550834, -25.76919019428369850 ) ) ;
#1581=CARTESIAN_POINT ( 'NONE',  ( 57.24727847454269636, 13.89208492953430074, -25.38222954899870132 ) ) ;
#1584=CARTESIAN_POINT ( 'NONE',  ( 50.03007040746729928, 17.38380685021119731, -76.14999999999999147 ) ) ;
#1585=CARTESIAN_POINT ( 'NONE',  ( 52.79729137842230102, 18.45889402858979977, -48.80671571307529888 ) ) ;
#1586=CARTESIAN_POINT ( 'NONE',  ( 60.23362534523650424, -45.78182602740779572, -47.26357634580359246 ) ) ;
#1587=CARTESIAN_POINT ( 'NONE',  ( 67.05761679591040547, -45.11618894467940066, -12.74175955172660046 ) ) ;
#1592=CARTESIAN_POINT ( 'NONE',  ( 47.43684003301049756, -54.63141987875069816, -54.76595269979989666 ) ) ;
#1595=CARTESIAN_POINT ( 'NONE',  ( 10.74148174179099868, -64.95262810519260199, -18.12706498543029809 ) ) ;
#1596=CARTESIAN_POINT ( 'NONE',  ( 53.05372063824079731, 18.31120138125489660, -48.79446872373860344 ) ) ;
#1600=EDGE_CURVE ( 'NONE', #13869, #21630, #35583, .T. ) ;
#1603=CARTESIAN_POINT ( 'NONE',  ( 9.284331854864920075, -63.18779374651679603, -46.53073416084929903 ) ) ;
#1604=ORIENTED_EDGE ( 'NONE', *, *, #15882, .T. ) ;
#1606=CARTESIAN_POINT ( 'NONE',  ( 85.17508943611196059, 18.35477988570885444, -52.74015335379900904 ) ) ;
#1608=CARTESIAN_POINT ( 'NONE',  ( 52.02578739311559985, 19.35467404128699798, -76.37778590630358622 ) ) ;
#1609=B_SPLINE_CURVE_WITH_KNOTS ( 'NONE', 3,
 ( #39533, #4135, #51838, #51330, #51583 ),
 .UNSPECIFIED., .F., .F.,
 ( 4, 1, 4 ),
 ( 0.4999950733969018013, 0.6666633822707539458, 1.000000000000000000 ),
 .UNSPECIFIED. ) ;
#1611=CARTESIAN_POINT ( 'NONE',  ( -11.32734370190460105, 10.64934056395049922, -19.14999999999999858 ) ) ;
#1615=CARTESIAN_POINT ( 'NONE',  ( 8.133937397696209715, 8.337936262032100032, -43.74348518090240390 ) ) ;
#1618=CIRCLE ( 'NONE', #33396, 18.00000000000000355 ) ;
#1619=CARTESIAN_POINT ( 'NONE',  ( 57.20752091846340193, -45.84035874391049958, -26.25769493244969865 ) ) ;
#1622=CARTESIAN_POINT ( 'NONE',  ( 53.50485636675099954, -49.42567878242080326, -49.20411384802949328 ) ) ;
#1625=CARTESIAN_POINT ( 'NONE',  ( 13.52746909241120044, 20.57970132932399920, -74.87640169473949925 ) ) ;
#1626=DIRECTION ( 'NONE',  ( 1.000000000000000000, 0.000000000000000000, 0.000000000000000000 ) ) ;
#1628=CARTESIAN_POINT ( 'NONE',  ( 41.24056053114340159, -44.83149236909930124, -5.438981521421270671 ) ) ;
#1629=CARTESIAN_POINT ( 'NONE',  ( 83.70899958829811283, -44.46275198668180195, -46.59258846095890050 ) ) ;
#1632=CARTESIAN_POINT ( 'NONE',  ( 52.92338564704119364, -49.48118464961610385, -27.26198717260970028 ) ) ;
#1634=CARTESIAN_POINT ( 'NONE',  ( 55.47560955148180284, -50.96964303883889613, -75.04526988654890829 ) ) ;
#1636=CARTESIAN_POINT ( 'NONE',  ( 2.204417066470079956, 24.53158638618599952, -10.01932650448550000 ) ) ;
#1638=CARTESIAN_POINT ( 'NONE',  ( -23.86606260230380272, -15.61618894467908092, -53.92777777777782688 ) ) ;
#1641=CARTESIAN_POINT ( 'NONE',  ( -9.106445543791931385, -44.03001587129549677, -5.504031293643000033 ) ) ;
#1642=CARTESIAN_POINT ( 'NONE',  ( 47.46194251081040250, 23.38593605885670001, -54.80975913085070061 ) ) ;
#1643=DIRECTION ( 'NONE',  ( 1.000000000000000000, 0.000000000000000000, 5.637851296925361431E-15 ) ) ;
#1645=CARTESIAN_POINT ( 'NONE',  ( 60.98478001766370227, 14.15589715924580005, -46.95039023230899744 ) ) ;
#1646=CARTESIAN_POINT ( 'NONE',  ( 11.11465748640249984, 33.92433621588410375, -17.59315317980379945 ) ) ;
#1647=DIRECTION ( 'NONE',  ( -1.000000000000000000, -8.935017999999999834E-14, 2.044407999999999825E-12 ) ) ;
#1648=CARTESIAN_POINT ( 'NONE',  ( 52.86023839377149613, 18.41257215013510162, -48.64479331233690829 ) ) ;
#1649=CARTESIAN_POINT ( 'NONE',  ( 18.06932202639800167, 24.33696219936669891, -76.14999999999999147 ) ) ;
#1651=CARTESIAN_POINT ( 'NONE',  ( 53.50528692585089630, 17.84081850706130012, -27.26091398553390022 ) ) ;
#1652=CARTESIAN_POINT ( 'NONE',  ( 52.25041881653689302, 21.33925748481399864, -54.52050471625830141 ) ) ;
#1655=CARTESIAN_POINT ( 'NONE',  ( 51.23808412292059700, 13.88381105532070059, -11.16296171957920080 ) ) ;
#1658=CARTESIAN_POINT ( 'NONE',  ( 10.77213051274009992, 32.03892353611769295, -45.20477560231249470 ) ) ;
#1664=VERTEX_POINT ( 'NONE', #23228 ) ;
#1666=B_SPLINE_CURVE_WITH_KNOTS ( 'NONE', 3,
 ( #722, #24294, #12533, #16713, #40309, #4144, #35859, #13070, #24815, #12275 ),
 .UNSPECIFIED., .F., .F.,
 ( 4, 2, 2, 2, 4 ),
 ( 0.000000000000000000, 0.2500000000000000000, 0.5000000000000000000, 0.7500000000000000000, 1.000000000000000000 ),
 .UNSPECIFIED. ) ;
#1670=CARTESIAN_POINT ( 'NONE',  ( 10.24662431634200033, -64.14781499658329267, -46.34409721753970501 ) ) ;
#1671=CARTESIAN_POINT ( 'NONE',  ( 56.60481287756580571, -45.54075046089940315, -25.88701370651539690 ) ) ;
#1674=CARTESIAN_POINT ( 'NONE',  ( 61.37880515396449965, 14.09585059423469922, -47.24540677760579399 ) ) ;
#1679=CARTESIAN_POINT ( 'NONE',  ( 45.14275739423920442, -45.91162181551540300, -8.929573315219988316 ) ) ;
#1682=ORIENTED_EDGE ( 'NONE', *, *, #4769, .F. ) ;
#1684=CARTESIAN_POINT ( 'NONE',  ( 47.01289497786039817, -54.42182676496869931, -75.36291177546809195 ) ) ;
#1685=CARTESIAN_POINT ( 'NONE',  ( 75.47257744440361193, 12.45848636096840067, -13.44587694045140047 ) ) ;
#1686=CARTESIAN_POINT ( 'NONE',  ( 51.04010994546690227, 13.88381105532070059, -11.02192607414670000 ) ) ;
#1687=CARTESIAN_POINT ( 'NONE',  ( 50.22323044735963293, 21.91892061222964472, -53.94765380580868452 ) ) ;
#1688=AXIS2_PLACEMENT_3D ( 'NONE', #46753, #26537, #38878 ) ;
#1689=VECTOR ( 'NONE', #33658, 1000.000000000000000 ) ;
#1692=CARTESIAN_POINT ( 'NONE',  ( 60.46851295127660109, 13.88923079682050066, -26.48073026131960006 ) ) ;
#1693=CIRCLE ( 'NONE', #14232, 2.000000000000000000 ) ;
#1696=B_SPLINE_SURFACE_WITH_KNOTS ( 'NONE', 3, 3, ( 
 ( #23166, #39695, #31802, #15839, #35236, #50972, #20011, #11927, #7471 ),
 ( #11664, #12172, #47821, #24185, #36003, #18992, #4047, #23422, #19771 ),
 ( #3280, #39443, #19254, #19513, #7735, #34973, #3801, #120, #35760 ),
 ( #51743, #28131, #51243, #27878, #39183, #15335, #35504, #43881, #7978 ),
 ( #23930, #44137, #16094, #47063, #31287, #31548, #47319, #43121, #23678 ),
 ( #27627, #47566, #15069, #11409, #31037, #39952, #11147, #27370, #32052 ),
 ( #48074, #51493, #15594, #8233, #43632, #40206, #43376, #27117, #7212 ),
 ( #44912, #24702, #49120, #21301, #32306, #25488, #48591, #33089, #33358 ),
 ( #44647, #37045, #9282, #37305, #41236, #884, #48850, #24442, #12424 ),
 ( #8753, #13473, #20521, #9016, #25229, #36258, #9538, #5347, #28388 ),
 ( #32825, #4294, #36516, #368, #20266, #16349, #1403, #36775, #5089 ),
 ( #21043, #24960, #40976, #29429, #8495, #12955, #17392, #49376, #45436 ),
 ( #40720, #48328, #4550, #44394, #4816, #40456, #16878, #1142, #618 ),
 ( #16603, #32560, #12692, #28646, #28909, #13219, #20783, #17138, #29169 ),
 ( #45170, #26270, #49886, #22594, #2431, #13980, #46221, #22074, #14749 ),
 ( #6119, #42277, #38610, #17901, #50401, #14489, #25743, #45692, #30204 ) ),
 .UNSPECIFIED., .F., .F., .F.,
 ( 4, 2, 2, 2, 2, 2, 2, 4 ),
 ( 4, 1, 1, 1, 1, 1, 4 ),
 ( -1.570796326794899889, -1.295906969605790104, -0.9817477042468120141, -0.7853981633974489451, -0.6872233929727680213, -0.5301437602932779214, -0.2788163480060950050, 2.850064269800000171E-05 ),
 ( -2.850064267999999931E-05, 0.1666666666666670182, 0.3333333333333329818, 0.5000000000000000000, 0.6666666666666670737, 0.8333333333333330373, 1.000028500642689888 ),
 .UNSPECIFIED. ) ;
#1700=CARTESIAN_POINT ( 'NONE',  ( -10.41252972610489991, -41.50076126836940205, -4.265331396025359822 ) ) ;
#1701=CARTESIAN_POINT ( 'NONE',  ( 76.79000011994270380, -42.06488460674430030, -14.47554790092480026 ) ) ;
#1705=B_SPLINE_CURVE_WITH_KNOTS ( 'NONE', 3,
 ( #16444, #24018, #44486, #33190, #48953, #32398, #40042, #32143, #41073, #48419 ),
 .UNSPECIFIED., .F., .F.,
 ( 4, 2, 2, 2, 4 ),
 ( 0.5000003605016758446, 0.5624999999907476234, 0.6624999999928627981, 0.8224999999962434583, 1.000000000000000000 ),
 .UNSPECIFIED. ) ;
#1707=CARTESIAN_POINT ( 'NONE',  ( 49.05945480412340487, -53.75841287389920353, -54.45983108200709921 ) ) ;
#1708=CARTESIAN_POINT ( 'NONE',  ( 43.09344256554030750, -43.96039878386999789, -5.051331041927119792 ) ) ;
#1710=CARTESIAN_POINT ( 'NONE',  ( 55.52075019247980237, -50.89749466248539989, -52.96229217805840506 ) ) ;
#1717=CARTESIAN_POINT ( 'NONE',  ( 61.19107041010649795, -45.55858923584479925, -47.61997709501220299 ) ) ;
#1718=DIRECTION ( 'NONE',  ( 0.3281607301299678814, 0.6263469766835031427, 0.7071067811865485719 ) ) ;
#1719=CARTESIAN_POINT ( 'NONE',  ( 14.19855276898620033, -55.56934008872499930, -76.14999999999999147 ) ) ;
#1721=CARTESIAN_POINT ( 'NONE',  ( 52.26504646883520167, -49.78354544620959388, -77.19463087837650050 ) ) ;
#1722=CARTESIAN_POINT ( 'NONE',  ( 51.84413677266599763, -51.33743803777170456, -76.02231597519390505 ) ) ;
#1727=EDGE_CURVE ( 'NONE', #36299, #14841, #11730, .T. ) ;
#1728=ORIENTED_EDGE ( 'NONE', *, *, #9218, .F. ) ;
#1729=CARTESIAN_POINT ( 'NONE',  ( 61.28609324400200364, -45.23040860746230152, -46.44124428239370417 ) ) ;
#1731=CARTESIAN_POINT ( 'NONE',  ( 14.16187783161720048, 19.11875810978959933, -20.85710678118659800 ) ) ;
#1737=DIRECTION ( 'NONE',  ( -3.489701575733883348E-12, -0.02843704686102061993, -0.9995955854073307334 ) ) ;
#1740=ORIENTED_EDGE ( 'NONE', *, *, #20357, .T. ) ;
#1742=CARTESIAN_POINT ( 'NONE',  ( 52.66575370896529762, -50.80825905356590511, -76.31205015067719444 ) ) ;
#1745=CARTESIAN_POINT ( 'NONE',  ( 45.73978377946800578, 13.90695855600979947, -7.826106078158160173 ) ) ;
#1746=CARTESIAN_POINT ( 'NONE',  ( 41.62693577203659601, -43.81499318205119664, -3.742293455806500191 ) ) ;
#1747=CARTESIAN_POINT ( 'NONE',  ( 67.04038824939742369, -50.70395984888145335, -73.25000000000218847 ) ) ;
#1751=CARTESIAN_POINT ( 'NONE',  ( 17.71568204744891517, -51.70197554413384466, -75.56421372420066973 ) ) ;
#1752=ORIENTED_EDGE ( 'NONE', *, *, #10725, .F. ) ;
#1753=CARTESIAN_POINT ( 'NONE',  ( 14.90551652343050115, -52.98917440366089693, -76.14999999999999147 ) ) ;
#1757=EDGE_CURVE ( 'NONE', #20534, #18008, #24256, .T. ) ;
#1758=CARTESIAN_POINT ( 'NONE',  ( 11.55608217430013873, 33.52247355198553436, -44.82755758702938920 ) ) ;
#1762=AXIS2_PLACEMENT_3D ( 'NONE', #1024, #49251, #36919 ) ;
#1763=EDGE_CURVE ( 'NONE', #40179, #42937, #47476, .T. ) ;
#1769=CARTESIAN_POINT ( 'NONE',  ( 48.25528797735780273, 23.04103089059060139, -55.30957496453530098 ) ) ;
#1774=CARTESIAN_POINT ( 'NONE',  ( 53.59007319635684041, -49.40623578145638106, -49.22505640097209323 ) ) ;
#1776=CARTESIAN_POINT ( 'NONE',  ( 83.77685426296399385, 13.49366907108930036, -47.23654203728539613 ) ) ;
#1777=CARTESIAN_POINT ( 'NONE',  ( 55.88720985982159561, 14.71003042163810015, -25.33276895956559827 ) ) ;
#1779=CARTESIAN_POINT ( 'NONE',  ( 11.60439326025533013, 33.70240003096060377, -16.46429631544720351 ) ) ;
#1780=CARTESIAN_POINT ( 'NONE',  ( 57.48392867679269358, -45.11618894467940066, -17.43413672685039728 ) ) ;
#1783=EDGE_CURVE ( 'NONE', #20901, #45666, #28073, .T. ) ;
#1785=CARTESIAN_POINT ( 'NONE',  ( 12.29766918195309877, -64.63049967510049498, -15.84900139482509829 ) ) ;
#1786=CARTESIAN_POINT ( 'NONE',  ( 10.93111994017589872, 32.28751451308780673, -44.89712406839979764 ) ) ;
#1788=CARTESIAN_POINT ( 'NONE',  ( -0.3347231778593094398, 32.07101016863870768, -50.60099389661314007 ) ) ;
#1793=CARTESIAN_POINT ( 'NONE',  ( 51.39286536822110207, 19.84796399938319666, -49.98540144959209641 ) ) ;
#1794=CARTESIAN_POINT ( 'NONE',  ( 62.41274088580539825, -1.258673626276660018, -16.17370678346230051 ) ) ;
#1795=CARTESIAN_POINT ( 'NONE',  ( 50.87835763800730149, -49.82993816064299608, -76.22533641326209874 ) ) ;
#1796=CARTESIAN_POINT ( 'NONE',  ( 60.67850367109549836, -46.09186595282459820, -48.19625756050770349 ) ) ;
#1798=EDGE_LOOP ( 'NONE', ( #30055, #3306, #45630, #43946 ) ) ;
#1800=AXIS2_PLACEMENT_3D ( 'NONE', #28318, #47246, #4229 ) ;
#1802=VERTEX_POINT ( 'NONE', #15531 ) ;
#1804=DIRECTION ( 'NONE',  ( 1.000000000000000000, 0.000000000000000000, 0.000000000000000000 ) ) ;
#1809=CARTESIAN_POINT ( 'NONE',  ( 53.91121292163150258, 19.51725716617239925, -76.32774465143938869 ) ) ;
#1810=CARTESIAN_POINT ( 'NONE',  ( 46.81166088778630296, -53.49946929133769657, -76.01705645362530106 ) ) ;
#1812=CARTESIAN_POINT ( 'NONE',  ( 55.62561308564289675, 14.67649059877530071, -16.78101652394359888 ) ) ;
#1814=CARTESIAN_POINT ( 'NONE',  ( 57.32356178811300396, -50.41450853367899754, -53.00097362968700310 ) ) ;
#1819=CARTESIAN_POINT ( 'NONE',  ( 47.45533712166319873, 23.17465650934340360, -75.00623913050900171 ) ) ;
#1821=CARTESIAN_POINT ( 'NONE',  ( 53.41693480158270546, -49.35328119387190071, -48.75416851881869462 ) ) ;
#1823=TOROIDAL_SURFACE ( 'NONE', #37700, 15.56227766038949945, 0.9999999999568489617 ) ;
#1827=B_SPLINE_CURVE_WITH_KNOTS ( 'NONE', 3,
 ( #13861, #32978, #9158, #41124, #45055, #37194, #29818, #25886, #41900, #18043, #5999 ),
 .UNSPECIFIED., .F., .F.,
 ( 4, 2, 1, 2, 2, 4 ),
 ( 0.5057982913667791181, 0.5366858981563504827, 0.5675735049459218473, 0.6293487185250745686, 0.7528991456833793450, 1.000000000000000000 ),
 .UNSPECIFIED. ) ;
#1828=CARTESIAN_POINT ( 'NONE',  ( 60.60297408742504643, 14.35593598357043099, -47.14360528713132936 ) ) ;
#1830=CARTESIAN_POINT ( 'NONE',  ( 16.13393739769620083, -15.61618894467929941, -19.14999999999999858 ) ) ;
#1832=FACE_OUTER_BOUND ( 'NONE', #18083, .T. ) ;
#1833=CARTESIAN_POINT ( 'NONE',  ( -18.46117119614969937, 21.06649955959539966, -53.76231701354929982 ) ) ;
#1834=ORIENTED_EDGE ( 'NONE', *, *, #24084, .T. ) ;
#1835=VECTOR ( 'NONE', #3592, 1000.000000000000000 ) ;
#1836=CARTESIAN_POINT ( 'NONE',  ( 52.80366530508379697, -49.67681281767760026, -48.66066742733800510 ) ) ;
#1837=CIRCLE ( 'NONE', #34479, 19.56371635397779940 ) ;
#1838=ORIENTED_EDGE ( 'NONE', *, *, #5333, .T. ) ;
#1840=CARTESIAN_POINT ( 'NONE',  ( 48.59292341170780105, -54.12958895873340026, -55.31326040662610666 ) ) ;
#1841=CARTESIAN_POINT ( 'NONE',  ( 56.72616477557319570, 14.12792985703750048, -25.70465367030369919 ) ) ;
#1844=CARTESIAN_POINT ( 'NONE',  ( 53.33276493848160271, 18.22256187676000039, -49.10545657411340414 ) ) ;
#1846=CARTESIAN_POINT ( 'NONE',  ( 60.32811079037119839, -45.73232245539999496, -47.24891709412590046 ) ) ;
#1847=CARTESIAN_POINT ( 'NONE',  ( 16.13393739769620083, -15.61618894467929941, -74.14999999999999147 ) ) ;
#1848=VERTEX_POINT ( 'NONE', #47764 ) ;
#1852=CARTESIAN_POINT ( 'NONE',  ( 47.50772827459159942, -54.57838557763199816, -54.69148953378340394 ) ) ;
#1855=CARTESIAN_POINT ( 'NONE',  ( 11.73919149117240046, -65.42291996908740259, -18.11861173573770145 ) ) ;
#1862=CARTESIAN_POINT ( 'NONE',  ( 8.970405606519269881, -63.23339553274689706, -46.63272187348500353 ) ) ;
#1867=CARTESIAN_POINT ( 'NONE',  ( 57.09195614716849576, 16.19545665448480065, -46.39999999999999858 ) ) ;
#1868=CARTESIAN_POINT ( 'NONE',  ( 52.68970887852299967, 19.39006498537879963, -76.51771730001300398 ) ) ;
#1869=ORIENTED_EDGE ( 'NONE', *, *, #28540, .F. ) ;
#1875=EDGE_CURVE ( 'NONE', #6515, #29501, #26789, .T. ) ;
#1880=VECTOR ( 'NONE', #40014, 1000.000000000000000 ) ;
#1881=CARTESIAN_POINT ( 'NONE',  ( 57.03837479396619869, -45.89653934241670186, -26.24811324117309752 ) ) ;
#1883=AXIS2_PLACEMENT_3D ( 'NONE', #9159, #9670, #1804 ) ;
#1884=CARTESIAN_POINT ( 'NONE',  ( 52.77399506770059645, -49.72485891806019964, -48.90117834109280182 ) ) ;
#1886=CARTESIAN_POINT ( 'NONE',  ( 14.40819075579249997, 20.22256044820920096, -75.26885115310530239 ) ) ;
#1889=CARTESIAN_POINT ( 'NONE',  ( 41.74197467272710327, -45.06540362037719660, -5.934314133911740008 ) ) ;
#1892=ADVANCED_FACE ( 'NONE', ( #33035 ), #8441, .F. ) ;
#1894=CARTESIAN_POINT ( 'NONE',  ( 52.64678251747500326, -49.77729224470360236, -27.84346069079800401 ) ) ;
#1895=CARTESIAN_POINT ( 'NONE',  ( 16.36414204281640039, -51.09682298092410235, -20.27640028196719868 ) ) ;
#1896=CARTESIAN_POINT ( 'NONE',  ( 10.97326672351239907, 33.19570593983480222, -16.07944711293080076 ) ) ;
#1901=CARTESIAN_POINT ( 'NONE',  ( -2.700142689170709875, -48.79866302901520214, -5.083883930088719971 ) ) ;
#1902=CARTESIAN_POINT ( 'NONE',  ( 47.48638238263849587, 23.36238434565460054, -54.71109617728680519 ) ) ;
#1903=SPHERICAL_SURFACE ( 'NONE', #11986, 1.999999999999739764 ) ;
#1905=DIRECTION ( 'NONE',  ( -1.000000000000000000, 0.000000000000000000, 0.000000000000000000 ) ) ;
#1906=CARTESIAN_POINT ( 'NONE',  ( 11.50001307144090035, 33.75586786865649458, -16.62227806133670072 ) ) ;
#1907=CARTESIAN_POINT ( 'NONE',  ( 51.88873276978809912, 18.11352090822219907, -77.07841357864730014 ) ) ;
#1908=DIRECTION ( 'NONE',  ( 0.000000000000000000, 0.000000000000000000, 1.000000000000000000 ) ) ;
#1909=CARTESIAN_POINT ( 'NONE',  ( 19.44911581942429635, 24.24611119365071588, -75.64152464225232109 ) ) ;
#1910=CARTESIAN_POINT ( 'NONE',  ( 56.66172278421190356, -47.79833722945330265, -48.40341972513039792 ) ) ;
#1912=CARTESIAN_POINT ( 'NONE',  ( 51.97963026116360652, 21.17322201635790080, -53.55374510773989982 ) ) ;
#1914=CARTESIAN_POINT ( 'NONE',  ( 12.08205748224309950, -65.27925620804988682, -16.92411159753779870 ) ) ;
#1915=CARTESIAN_POINT ( 'NONE',  ( 50.03007040746459921, -48.61618894467930119, -76.14999999999999147 ) ) ;
#1918=CARTESIAN_POINT ( 'NONE',  ( 10.77081499238640028, 31.97176150883899837, -45.20487661762840048 ) ) ;
#1921=CARTESIAN_POINT ( 'NONE',  ( 67.09948588395030811, -33.06559114426190149, -20.09058981816900058 ) ) ;
#1924=ORIENTED_EDGE ( 'NONE', *, *, #31100, .T. ) ;
#1926=CARTESIAN_POINT ( 'NONE',  ( 11.13393739769619906, -15.61618894467929941, -46.14999999999999858 ) ) ;
#1928=CARTESIAN_POINT ( 'NONE',  ( 11.08968279120479927, -64.22844165307741093, -45.26598027972680427 ) ) ;
#1929=CARTESIAN_POINT ( 'NONE',  ( 57.39717139072750030, -45.73959026386049942, -26.25633027675440090 ) ) ;
#1930=B_SPLINE_CURVE_WITH_KNOTS ( 'NONE', 3,
 ( #2424, #22588, #34384, #26519, #46216, #38605, #10302, #50396, #10562, #47044, #23150, #3783, #6944, #50954, #31019, #28115, #11132, #27610, #19752 ),
 .UNSPECIFIED., .F., .F.,
 ( 4, 3, 3, 3, 3, 3, 4 ),
 ( 8.130128712166969862, 8.744224101849910724, 18.73762479188560093, 24.98350022315790397, 28.10643793879390273, 33.10313828381179491, 38.04558972261919791 ),
 .UNSPECIFIED. ) ;
#1935=ORIENTED_EDGE ( 'NONE', *, *, #9755, .T. ) ;
#1936=CARTESIAN_POINT ( 'NONE',  ( 47.84831528495369213, -45.94688046902010115, -10.78657639741869900 ) ) ;
#1937=EDGE_CURVE ( 'NONE', #13386, #49388, #40659, .T. ) ;
#1940=CARTESIAN_POINT ( 'NONE',  ( 15.78755803686370029, 19.77187500835140099, -20.74412215666090020 ) ) ;
#1943=( BOUNDED_SURFACE ( )  B_SPLINE_SURFACE ( 2, 2, ( 
 ( #3885, #44220, #36094, #24014, #36341, #450, #35840, #12006, #31885 ),
 ( #12259, #51577, #27961, #32394, #8844, #32653, #39527, #8322, #20104 ),
 ( #35589, #43964, #40037, #4128, #16179, #13554, #33187, #17479, #48950 ),
 ( #37647, #20880, #1747, #973, #13051, #25318, #29004, #41070, #21640 ),
 ( #49718, #33701, #25573, #45002, #45522, #17731, #13806, #5180, #4905 ) ),
 .UNSPECIFIED., .F., .T., .T. ) 
 B_SPLINE_SURFACE_WITH_KNOTS ( ( 3, 2, 3 ),
 ( 3, 2, 2, 2, 3 ),
 ( -0.003205554299145560102, 0.8238407534178779912, 1.650887061134900025 ),
 ( -3.141592653589790007, -1.570796326794899889, 0.000000000000000000, 1.570796326794899889, 3.141592653589790007 ),
 .UNSPECIFIED. ) 
 GEOMETRIC_REPRESENTATION_ITEM ( )  RATIONAL_B_SPLINE_SURFACE ( (
 ( 1.000000000000000000, 0.7071067811865480168, 1.000000000000000000, 0.7071067811865480168, 1.000000000000000000, 0.7071067811865480168, 1.000000000000000000, 0.7071067811865480168, 1.000000000000000000),
 ( 0.9157107718028779653, 0.6475052963473819645, 0.9157107718028779653, 0.6475052963473819645, 0.9157107718028779653, 0.6475052963473819645, 0.9157107718028779653, 0.6475052963473819645, 0.9157107718028779653),
 ( 1.000000000000000000, 0.7071067811865480168, 1.000000000000000000, 0.7071067811865480168, 1.000000000000000000, 0.7071067811865480168, 1.000000000000000000, 0.7071067811865480168, 1.000000000000000000),
 ( 0.9157107718028449916, 0.6475052963473589829, 0.9157107718028449916, 0.6475052963473589829, 0.9157107718028449916, 0.6475052963473589829, 0.9157107718028449916, 0.6475052963473589829, 0.9157107718028449916),
 ( 1.000000000000000000, 0.7071067811865480168, 1.000000000000000000, 0.7071067811865480168, 1.000000000000000000, 0.7071067811865480168, 1.000000000000000000, 0.7071067811865480168, 1.000000000000000000) ) ) 
 REPRESENTATION_ITEM ( '' )  SURFACE ( )  );
#1946=CARTESIAN_POINT ( 'NONE',  ( 47.11818671551210258, -54.50110806056969892, -75.17436503908771783 ) ) ;
#1947=CARTESIAN_POINT ( 'NONE',  ( 64.87946167155979538, 12.49593138203690046, -10.46016357390099927 ) ) ;
#1948=CARTESIAN_POINT ( 'NONE',  ( 50.20000625561069540, -49.66915949483620096, -76.14999999999999147 ) ) ;
#1949=CARTESIAN_POINT ( 'NONE',  ( 54.69511575210409404, 20.01728140309300130, -53.07518616905519337 ) ) ;
#1950=VECTOR ( 'NONE', #6293, 1000.000000000000227 ) ;
#1952=CARTESIAN_POINT ( 'NONE',  ( 52.57481508192889663, 20.19967092288990074, -75.83555757118479335 ) ) ;
#1953=CARTESIAN_POINT ( 'NONE',  ( 61.66984244049909591, 13.88595911880170064, -28.15148628585509982 ) ) ;
#1967=CARTESIAN_POINT ( 'NONE',  ( 42.70036219403750266, -44.15320494937070350, -5.071714815372149410 ) ) ;
#1974=ORIENTED_EDGE ( 'NONE', *, *, #4701, .T. ) ;
#1975=CARTESIAN_POINT ( 'NONE',  ( 9.944902970854920810, 32.89001708672019930, -17.55158127909980337 ) ) ;
#1978=CARTESIAN_POINT ( 'NONE',  ( 47.81335647231750130, -54.39749252970050009, -54.71582838609450050 ) ) ;
#1987=CARTESIAN_POINT ( 'NONE',  ( 61.14293679174719642, -45.32076580385039932, -46.99585847235690039 ) ) ;
#1988=CARTESIAN_POINT ( 'NONE',  ( 51.35032894455923014, -51.12106501579054907, -50.03594749790474339 ) ) ;
#1991=AXIS2_PLACEMENT_3D ( 'NONE', #23507, #35591, #51834 ) ;
#1995=EDGE_CURVE ( 'NONE', #17152, #14356, #25174, .T. ) ;
#1999=CARTESIAN_POINT ( 'NONE',  ( 53.50362398765149408, -50.77013085338330001, -76.38491628186639559 ) ) ;
#2000=CARTESIAN_POINT ( 'NONE',  ( 60.68849784050689777, 14.37619509097770099, -47.46714534019130127 ) ) ;
#2002=FACE_OUTER_BOUND ( 'NONE', #11935, .T. ) ;
#2004=CARTESIAN_POINT ( 'NONE',  ( 41.35124225329579417, 13.74788993297780060, -5.668943192347540183 ) ) ;
#2005=CARTESIAN_POINT ( 'NONE',  ( 42.25542674110280217, -43.34247267206160359, -3.898748443015970011 ) ) ;
#2007=CARTESIAN_POINT ( 'NONE',  ( -7.099872940393900045, 14.68218975379929958, -5.638321079196820129 ) ) ;
#2010=CARTESIAN_POINT ( 'NONE',  ( 66.56329404978689013, -1.021671608844639811, -16.96526467878980071 ) ) ;
#2011=EDGE_CURVE ( 'NONE', #27433, #50743, #51160, .T. ) ;
#2013=CARTESIAN_POINT ( 'NONE',  ( 14.40115328186280053, -52.48721817738829287, -75.97756937697440094 ) ) ;
#2014=CIRCLE ( 'NONE', #20434, 14.50000000000000178 ) ;
#2015=CARTESIAN_POINT ( 'NONE',  ( 47.18324198357289845, -54.80726809202429450, -54.61058319554170026 ) ) ;
#2018=LINE ( 'NONE', #25062, #33928 ) ;
#2021=B_SPLINE_CURVE_WITH_KNOTS ( 'NONE', 3,
 ( #25618, #40850, #4951, #5226, #1537, #17524, #25364, #33493, #13851, #17775, #48726, #24841, #33233, #1022, #44788, #21688 ),
 .UNSPECIFIED., .F., .F.,
 ( 4, 2, 2, 2, 2, 2, 2, 4 ),
 ( 0.000000000000000000, 0.08300154222485658928, 0.3122511566686436146, 0.4625707003009139617, 0.6128902439331841423, 0.7672452152475061071, 0.9236669617927576459, 1.000000000000000000 ),
 .UNSPECIFIED. ) ;
#2022=CARTESIAN_POINT ( 'NONE',  ( 46.57724752952230318, -53.42760099267549379, -76.07728942632040514 ) ) ;
#2024=CARTESIAN_POINT ( 'NONE',  ( 48.08549546625859961, -54.25909977946169960, -54.72858777524749740 ) ) ;
#2026=CARTESIAN_POINT ( 'NONE',  ( 56.50306386193680908, 19.52810639402949988, -53.80671218419070101 ) ) ;
#2027=CARTESIAN_POINT ( 'NONE',  ( 47.96924620030790010, 23.16287378102880012, -55.24392577788600533 ) ) ;
#2034=CARTESIAN_POINT ( 'NONE',  ( 84.44784216359251161, 11.88381105532070059, -47.47585302082339354 ) ) ;
#2035=CARTESIAN_POINT ( 'NONE',  ( 52.58045726257309838, 18.61320901487979995, -28.15003661640620081 ) ) ;
#2038=CARTESIAN_POINT ( 'NONE',  ( 55.87821755845719451, -45.11618894467940066, -14.71204629713069956 ) ) ;
#2039=CARTESIAN_POINT ( 'NONE',  ( 16.13393739769620083, -15.61618894467929941, 7.849999999999999645 ) ) ;
#2042=AXIS2_PLACEMENT_3D ( 'NONE', #26480, #34345, #26221 ) ;
#2044=ORIENTED_EDGE ( 'NONE', *, *, #20741, .T. ) ;
#2045=CARTESIAN_POINT ( 'NONE',  ( 12.31509292276649958, -64.63808111159269743, -15.85496248754649962 ) ) ;
#2048=CARTESIAN_POINT ( 'NONE',  ( 11.71633469864940125, -65.33094175685840810, -47.42091646943509886 ) ) ;
#2053=CARTESIAN_POINT ( 'NONE',  ( 56.96266348647149869, 14.69613425542049967, -26.24590930288369961 ) ) ;
#2054=CARTESIAN_POINT ( 'NONE',  ( 53.52648000331849687, -49.40009412630509900, -49.17036629546220183 ) ) ;
#2055=EDGE_CURVE ( 'NONE', #8993, #4830, #49318, .T. ) ;
#2056=VECTOR ( 'NONE', #41210, 1000.000000000000114 ) ;
#2057=CARTESIAN_POINT ( 'NONE',  ( 53.13593891953769344, 18.17654723902450087, -48.71694933965890328 ) ) ;
#2058=CARTESIAN_POINT ( 'NONE',  ( 64.95030386029479530, -1.381558580551719873, -16.48070782218119845 ) ) ;
#2059=CARTESIAN_POINT ( 'NONE',  ( 50.88311850207449538, -49.08192913539919289, -76.31540042335409169 ) ) ;
#2060=EDGE_CURVE ( 'NONE', #2815, #12686, #24904, .T. ) ;
#2061=CARTESIAN_POINT ( 'NONE',  ( 56.76964376401279821, -50.36013064195670097, -52.79151955495370174 ) ) ;
#2065=CARTESIAN_POINT ( 'NONE',  ( 65.43042069958039519, 17.98087126524892909, -71.50000000000090949 ) ) ;
#2068=CARTESIAN_POINT ( 'NONE',  ( 46.20926621405610035, -46.13066349458740234, -9.791022513314830533 ) ) ;
#2069=EDGE_CURVE ( 'NONE', #34462, #31947, #12409, .T. ) ;
#2071=CARTESIAN_POINT ( 'NONE',  ( 13.58337773622180045, -50.81123558615350078, -21.57342365037870024 ) ) ;
#2072=CARTESIAN_POINT ( 'NONE',  ( 54.26191342777159576, 19.70404036202970133, -75.79539126991741682 ) ) ;
#2073=CARTESIAN_POINT ( 'NONE',  ( 47.57154850773469690, -54.56571258662719970, -74.14999999999999147 ) ) ;
#2075=CARTESIAN_POINT ( 'NONE',  ( 56.06575504548730038, 14.47328901277619906, -17.60699513660309989 ) ) ;
#2077=CARTESIAN_POINT ( 'NONE',  ( 57.05931830690970230, -50.59304237665070048, -53.44572518174189923 ) ) ;
#2080=CARTESIAN_POINT ( 'NONE',  ( 47.64116069630630790, 23.30216092776590031, -74.19778950654200855 ) ) ;
#2083=CARTESIAN_POINT ( 'NONE',  ( 60.68789125469645995, -45.76122483410996011, -47.75606074947312152 ) ) ;
#2085=FACE_OUTER_BOUND ( 'NONE', #46082, .T. ) ;
#2086=DIRECTION ( 'NONE',  ( 0.000000000000000000, -1.000000000000000000, 0.000000000000000000 ) ) ;
#2088=CARTESIAN_POINT ( 'NONE',  ( 52.68908936341578908, 18.51792035577400242, -38.31189016485890875 ) ) ;
#2091=AXIS2_PLACEMENT_3D ( 'NONE', #3053, #19287, #46833 ) ;
#2094=CARTESIAN_POINT ( 'NONE',  ( 6.354289799265040450, 33.87947625492100201, -49.17526497145149733 ) ) ;
#2096=CARTESIAN_POINT ( 'NONE',  ( 52.75373701181550246, -49.71023522919640669, -48.68700931713409830 ) ) ;
#2097=ORIENTED_EDGE ( 'NONE', *, *, #15032, .T. ) ;
#2098=EDGE_CURVE ( 'NONE', #46021, #12521, #13664, .T. ) ;
#2099=AXIS2_PLACEMENT_3D ( 'NONE', #41942, #26976, #21999 ) ;
#2100=DIRECTION ( 'NONE',  ( 0.6888026391158399431, 0.7071067811865427988, 0.1598465650148944706 ) ) ;
#2101=CARTESIAN_POINT ( 'NONE',  ( 57.05854516459380221, 13.92570298991769917, -25.37276671555040153 ) ) ;
#2104=CARTESIAN_POINT ( 'NONE',  ( 52.92824256686530049, 18.39304521719179775, -48.92669088499940244 ) ) ;
#2105=DIRECTION ( 'NONE',  ( 0.000000000000000000, 0.000000000000000000, 1.000000000000000000 ) ) ;
#2106=ORIENTED_EDGE ( 'NONE', *, *, #45125, .F. ) ;
#2108=DIRECTION ( 'NONE',  ( 1.000000000000000000, 0.000000000000000000, 0.000000000000000000 ) ) ;
#2111=CARTESIAN_POINT ( 'NONE',  ( 10.78192289011060012, -64.93864051461240194, -17.70651626566360193 ) ) ;
#2113=DIRECTION ( 'NONE',  ( 0.000000000000000000, -1.000000000000000000, 0.000000000000000000 ) ) ;
#2116=ORIENTED_EDGE ( 'NONE', *, *, #30735, .T. ) ;
#2119=CARTESIAN_POINT ( 'NONE',  ( 9.279764201640460897, -63.15676077487329820, -46.53183983118100286 ) ) ;
#2121=EDGE_LOOP ( 'NONE', ( #28707, #38998 ) ) ;
#2123=CARTESIAN_POINT ( 'NONE',  ( 56.92789888016839939, 19.40969084676650169, -53.72375501523509911 ) ) ;
#2124=B_SPLINE_CURVE_WITH_KNOTS ( 'NONE', 3,
 ( #27180, #35570, #39509, #50530, #38743, #3096, #2837, #14621, #47130, #14878, #35036, #51044, #42411, #18803, #2575, #6506 ),
 .UNSPECIFIED., .F., .F.,
 ( 4, 2, 2, 2, 2, 2, 2, 4 ),
 ( 0.1345846079508339899, 1.324410793755629978, 2.838023129476340056, 3.784030839301789850, 4.257034694214520520, 5.013840862074870230, 6.224730730651439892, 7.568061678603579701 ),
 .UNSPECIFIED. ) ;
#2126=CARTESIAN_POINT ( 'NONE',  ( 52.63691515807389720, 19.18298782300839989, -76.75103203969149490 ) ) ;
#2127=B_SPLINE_CURVE_WITH_KNOTS ( 'NONE', 3,
 ( #26876, #19016, #22933, #10653, #26611, #50229, #2266, #50992, #2528, #15095 ),
 .UNSPECIFIED., .F., .F.,
 ( 4, 1, 1, 1, 1, 1, 1, 4 ),
 ( 0.000000000000000000, 0.1428610187999453662, 0.2857180173656790334, 0.4285750159314126728, 0.5714320144971452020, 0.7142890130628789525, 0.8571460116286125919, 1.000000000000000000 ),
 .UNSPECIFIED. ) ;
#2128=ORIENTED_EDGE ( 'NONE', *, *, #41690, .F. ) ;
#2134=EDGE_CURVE ( 'NONE', #41237, #2815, #48649, .T. ) ;
#2138=EDGE_LOOP ( 'NONE', ( #696, #20214, #8362, #43316 ) ) ;
#2143=CARTESIAN_POINT ( 'NONE',  ( 13.76101809979590129, 20.06273926763419979, -74.14993629405250886 ) ) ;
#2145=CARTESIAN_POINT ( 'NONE',  ( 17.27947978972579079, -52.93031137935258812, -76.14999999999999147 ) ) ;
#2146=CARTESIAN_POINT ( 'NONE',  ( 45.55527100000080054, -45.23107034338350019, -8.104338965901980885 ) ) ;
#2148=CIRCLE ( 'NONE', #28920, 38.00000000000000000 ) ;
#2150=EDGE_LOOP ( 'NONE', ( #3023, #42729, #51132, #1559, #13182 ) ) ;
#2151=CARTESIAN_POINT ( 'NONE',  ( 52.66971685105150414, -49.76276386869629675, -28.00590812673040020 ) ) ;
#2153=CARTESIAN_POINT ( 'NONE',  ( 55.05458601726860479, -50.70842107373549368, -75.94395387307670831 ) ) ;
#2154=CARTESIAN_POINT ( 'NONE',  ( 2.889165181869819854, 24.41604209844609841, -9.165974378419068813 ) ) ;
#2156=CARTESIAN_POINT ( 'NONE',  ( 47.77491216306469823, -54.41753965447119867, -54.70980729587230229 ) ) ;
#2157=CARTESIAN_POINT ( 'NONE',  ( 16.13393739769620083, -15.61618894467929941, -21.14999999999999858 ) ) ;
#2159=CARTESIAN_POINT ( 'NONE',  ( -9.084335010050759607, -44.06577152659710350, -5.655813564461040777 ) ) ;
#2160=CARTESIAN_POINT ( 'NONE',  ( 47.45221640967909593, 23.39300712745730237, -54.83348072773369353 ) ) ;
#2162=DIRECTION ( 'NONE',  ( 0.9987374001630935361, 0.000000000000000000, -0.05023550054956103100 ) ) ;
#2165=CARTESIAN_POINT ( 'NONE',  ( 11.98643056009569996, 34.18553739082079801, -17.50083518280339945 ) ) ;
#2166=CARTESIAN_POINT ( 'NONE',  ( 51.85719454310479648, 18.05925402898169807, -77.06877199832730696 ) ) ;
#2167=CARTESIAN_POINT ( 'NONE',  ( 53.20761889774500020, 18.23056977116550215, -48.79936051936330443 ) ) ;
#2170=CARTESIAN_POINT ( 'NONE',  ( 53.42450764587109546, 17.84354127545960012, -27.17986344697500201 ) ) ;
#2171=EDGE_CURVE ( 'NONE', #34516, #48296, #25943, .T. ) ;
#2172=CARTESIAN_POINT ( 'NONE',  ( 54.91646384901309830, 20.20362395552430002, -54.04939823774950014 ) ) ;
#2176=CARTESIAN_POINT ( 'NONE',  ( 53.91121044660913242, 19.99510753048234335, -75.56421356237309794 ) ) ;
#2177=CARTESIAN_POINT ( 'NONE',  ( 11.10554433198240076, 32.07361188791999496, -44.25245290781410290 ) ) ;
#2178=CARTESIAN_POINT ( 'NONE',  ( 16.65420337942459739, 19.88381105532299742, -15.67544741556190324 ) ) ;
#2179=CARTESIAN_POINT ( 'NONE',  ( 66.61544058241169353, -32.00365722899270082, -17.88087248512020011 ) ) ;
#2181=CARTESIAN_POINT ( 'NONE',  ( 12.13393739769649926, 24.18330853958550364, -74.14999999999999147 ) ) ;
#2183=EDGE_LOOP ( 'NONE', ( #39248, #38356, #16893, #27058, #13122, #35973, #29171, #24670, #19454, #46637 ) ) ;
#2184=CARTESIAN_POINT ( 'NONE',  ( 86.75761129539395711, -50.03040250705240055, -60.02031173921621132 ) ) ;
#2185=CARTESIAN_POINT ( 'NONE',  ( 76.49544124310347115, -3.188935732503785925, -13.20777387361363964 ) ) ;
#2187=CARTESIAN_POINT ( 'NONE',  ( 12.13443654887529988, -65.25725380275149234, -46.16574950220010010 ) ) ;
#2188=CARTESIAN_POINT ( 'NONE',  ( 56.44903381556829913, -45.81280302780699998, -26.04903467481380019 ) ) ;
#2193=EDGE_LOOP ( 'NONE', ( #5154, #18273, #39175, #11087 ) ) ;
#2194=DIRECTION ( 'NONE',  ( 0.000000000000000000, 0.000000000000000000, -1.000000000000000000 ) ) ;
#2197=EDGE_CURVE ( 'NONE', #1545, #19377, #26208, .T. ) ;
#2199=CARTESIAN_POINT ( 'NONE',  ( 49.86167560267210064, -45.58438661543760162, -11.84535681539230012 ) ) ;
#2200=AXIS2_PLACEMENT_3D ( 'NONE', #41223, #45423, #17890 ) ;
#2202=CARTESIAN_POINT ( 'NONE',  ( 14.50346589897350036, 19.73949337933519743, -21.59847332898520023 ) ) ;
#2205=CARTESIAN_POINT ( 'NONE',  ( 46.95605112289660354, -54.29280230291429632, -75.52284329973289800 ) ) ;
#2206=CARTESIAN_POINT ( 'NONE',  ( 64.89208931730020424, 12.18390113865149971, -10.41451813566090046 ) ) ;
#2207=CARTESIAN_POINT ( 'NONE',  ( 47.03372200559340399, 13.88381105525409964, -8.530834882583718581 ) ) ;
#2209=CARTESIAN_POINT ( 'NONE',  ( 53.64468172387730505, 20.03465317324409867, -75.63087525020739577 ) ) ;
#2211=CARTESIAN_POINT ( 'NONE',  ( 61.43364056055730060, 13.93410018439400133, -28.15121868926310000 ) ) ;
#2216=CARTESIAN_POINT ( 'NONE',  ( 5.980931312570809233, -59.92332712615679924, -13.42879642680019892 ) ) ;
#2219=CARTESIAN_POINT ( 'NONE',  ( 19.57495879260927296, -55.46790799353475165, -75.52237511312991103 ) ) ;
#2222=ADVANCED_FACE ( 'NONE', ( #17842 ), #6318, .T. ) ;
#2224=CARTESIAN_POINT ( 'NONE',  ( 40.73531902818009343, 13.41031014730079995, -4.523453215150309958 ) ) ;
#2225=CARTESIAN_POINT ( 'NONE',  ( 47.32200660942530845, -54.12888409431639758, -75.47293010958831871 ) ) ;
#2227=AXIS2_PLACEMENT_3D ( 'NONE', #6594, #22558, #33324 ) ;
#2228=DIRECTION ( 'NONE',  ( 0.000000000000000000, 0.000000000000000000, -1.000000000000000000 ) ) ;
#2229=ADVANCED_FACE ( 'NONE', ( #2374 ), #25329, .F. ) ;
#2231=FACE_OUTER_BOUND ( 'NONE', #31489, .T. ) ;
#2236=ORIENTED_EDGE ( 'NONE', *, *, #23575, .T. ) ;
#2238=FACE_OUTER_BOUND ( 'NONE', #30126, .T. ) ;
#2243=DIRECTION ( 'NONE',  ( -0.6047562208151069374, 0.7964106436917012255, 0.000000000000000000 ) ) ;
#2244=DIRECTION ( 'NONE',  ( 0.000000000000000000, 1.000000000000000000, 0.000000000000000000 ) ) ;
#2245=ORIENTED_EDGE ( 'NONE', *, *, #26707, .F. ) ;
#2246=ORIENTED_EDGE ( 'NONE', *, *, #46970, .F. ) ;
#2248=CARTESIAN_POINT ( 'NONE',  ( 61.28608632866890105, -45.23041223059910010, -46.37198050166980323 ) ) ;
#2251=AXIS2_PLACEMENT_3D ( 'NONE', #50041, #37466, #29839 ) ;
#2256=CARTESIAN_POINT ( 'NONE',  ( 58.92073396209919878, -28.11618894467929763, -15.65000000000000036 ) ) ;
#2258=DIRECTION ( 'NONE',  ( 0.000000000000000000, 0.000000000000000000, -1.000000000000000000 ) ) ;
#2259=CARTESIAN_POINT ( 'NONE',  ( 52.69947344156820179, -50.44413467004440577, -76.74590226450008856 ) ) ;
#2260=CARTESIAN_POINT ( 'NONE',  ( 61.00673202071669721, 14.19811893154319904, -47.28177263109790118 ) ) ;
#2263=LINE ( 'NONE', #25822, #41461 ) ;
#2264=CARTESIAN_POINT ( 'NONE',  ( 41.54742305948139602, 13.60457115157169916, -5.527274669639810512 ) ) ;
#2265=CARTESIAN_POINT ( 'NONE',  ( 41.89087153576700473, -43.57633437332699344, -3.657595758776970296 ) ) ;
#2266=CARTESIAN_POINT ( 'NONE',  ( 65.36617373303984380, -0.6361151674937697287, -16.64867384814720808 ) ) ;
#2267=CARTESIAN_POINT ( 'NONE',  ( 65.70575104159891566, 1.626048249155310099, -18.95023426183129800 ) ) ;
#2270=CARTESIAN_POINT ( 'NONE',  ( 54.17308945005400034, -50.61618894467930119, -77.01198594373980200 ) ) ;
#2271=ORIENTED_EDGE ( 'NONE', *, *, #43902, .T. ) ;
#2272=CARTESIAN_POINT ( 'NONE',  ( 14.92239907274469957, -52.74444847917729362, -76.12391999848780699 ) ) ;
#2274=CARTESIAN_POINT ( 'NONE',  ( 47.18324198357289845, -54.80726809202429450, -54.61058319554170026 ) ) ;
#2279=CARTESIAN_POINT ( 'NONE',  ( 48.21851895114659925, -54.27397483391509780, -55.06726167884789902 ) ) ;
#2281=EDGE_CURVE ( 'NONE', #1516, #43574, #3420, .T. ) ;
#2282=CARTESIAN_POINT ( 'NONE',  ( -10.89209614962082995, -42.33678087180149419, -6.195842417289838089 ) ) ;
#2284=CARTESIAN_POINT ( 'NONE',  ( 47.83780165944460094, 23.21886414354259998, -55.23279884646720461 ) ) ;
#2291=CARTESIAN_POINT ( 'NONE',  ( 83.69028012310354825, 13.83793465666272482, -47.49659995924119471 ) ) ;
#2293=CARTESIAN_POINT ( 'NONE',  ( 84.43354761919439966, 12.07319023258030022, -47.41425570151039892 ) ) ;
#2294=CARTESIAN_POINT ( 'NONE',  ( 55.86629951729040044, 14.73742367376410023, -25.42247174273690291 ) ) ;
#2301=ORIENTED_EDGE ( 'NONE', *, *, #34873, .F. ) ;
#2303=CARTESIAN_POINT ( 'NONE',  ( 12.32961272725700219, -64.64439898424720354, -15.85993007182080028 ) ) ;
#2305=CARTESIAN_POINT ( 'NONE',  ( 11.67619942398430055, 33.65927571709689659, -45.08494251881550241 ) ) ;
#2308=ORIENTED_EDGE ( 'NONE', *, *, #15977, .F. ) ;
#2309=EDGE_CURVE ( 'NONE', #34738, #45666, #19276, .T. ) ;
#2312=CARTESIAN_POINT ( 'NONE',  ( 51.76793811538249912, 19.62547313263230109, -50.48796164790370256 ) ) ;
#2314=CARTESIAN_POINT ( 'NONE',  ( 60.33936747781210386, -2.295495892611130184, -15.82216635100610169 ) ) ;
#2315=CARTESIAN_POINT ( 'NONE',  ( 50.57709982134520033, -48.74034408314059874, -76.21964822811550277 ) ) ;
#2316=CARTESIAN_POINT ( 'NONE',  ( 57.03554082408360415, -49.83830780016760542, -52.10329396591820483 ) ) ;
#2319=CARTESIAN_POINT ( 'NONE',  ( 70.03247032090601465, 18.72622661238470343, -69.60146707679315625 ) ) ;
#2320=EDGE_LOOP ( 'NONE', ( #40995, #36084, #19829, #17081 ) ) ;
#2322=CARTESIAN_POINT ( 'NONE',  ( 57.81609062655950027, -47.19091213400450613, -48.15256270216469403 ) ) ;
#2324=CARTESIAN_POINT ( 'NONE',  ( 13.87200042841950065, -51.20037006225030751, -22.54888207536149736 ) ) ;
#2325=CARTESIAN_POINT ( 'NONE',  ( 53.85265205760590135, 19.88976859782529871, -75.70177109258371217 ) ) ;
#2326=CARTESIAN_POINT ( 'NONE',  ( 46.63703890305789912, -53.27462879060840351, -76.10201724918678678 ) ) ;
#2327=CARTESIAN_POINT ( 'NONE',  ( 56.70268528983609713, 13.88381105532070059, -15.64847180727820053 ) ) ;
#2328=CARTESIAN_POINT ( 'NONE',  ( 11.13393739769619906, 32.27621211514449584, -43.92731420739779225 ) ) ;
#2329=CARTESIAN_POINT ( 'NONE',  ( 56.84210777396779690, -50.65785230063129774, -53.85131221196560602 ) ) ;
#2334=CARTESIAN_POINT ( 'NONE',  ( 47.61403878904570064, 23.30730827445200148, -74.36225195369628693 ) ) ;
#2335=AXIS2_PLACEMENT_3D ( 'NONE', #23663, #107, #48060 ) ;
#2336=CARTESIAN_POINT ( 'NONE',  ( 20.10261140139872182, -55.32589573411479478, -19.54203465799566430 ) ) ;
#2337=CARTESIAN_POINT ( 'NONE',  ( 60.34379258661509482, -45.86802437805019395, -47.72732609191810127 ) ) ;
#2340=DIRECTION ( 'NONE',  ( 1.000000000000000000, -4.005157696510369650E-32, -3.556943099846429769E-14 ) ) ;
#2341=LINE ( 'NONE', #34817, #50999 ) ;
#2345=EDGE_CURVE ( 'NONE', #17152, #35735, #24333, .T. ) ;
#2347=CARTESIAN_POINT ( 'NONE',  ( 6.312816564084299920, 31.89199177866499468, -47.22137548220790393 ) ) ;
#2349=CARTESIAN_POINT ( 'NONE',  ( 52.69435697169009813, -49.74608733290399698, -48.50602906872329356 ) ) ;
#2350=ORIENTED_EDGE ( 'NONE', *, *, #46645, .F. ) ;
#2353=CARTESIAN_POINT ( 'NONE',  ( 14.21330390444039971, 19.89053608221549752, -22.50776184251580148 ) ) ;
#2356=DIRECTION ( 'NONE',  ( 0.000000000000000000, 0.000000000000000000, 1.000000000000000000 ) ) ;
#2357=CARTESIAN_POINT ( 'NONE',  ( 52.80437707413480553, 18.46123689847469862, -48.85649626243960597 ) ) ;
#2358=CARTESIAN_POINT ( 'NONE',  ( 55.34109141907249807, -45.97060569714729894, -16.40367016765270236 ) ) ;
#2362=CYLINDRICAL_SURFACE ( 'NONE', #1015, 40.00000000000000711 ) ;
#2363=CARTESIAN_POINT ( 'NONE',  ( 9.002245878291878611, 32.05387020899590311, -46.62846274566239657 ) ) ;
#2365=CARTESIAN_POINT ( 'NONE',  ( 11.17220089305429909, -65.21595029614879024, -17.67193522364469871 ) ) ;
#2366=CARTESIAN_POINT ( 'NONE',  ( 53.12218299101002117, -49.57312743959001722, -49.13784299743716133 ) ) ;
#2369=CIRCLE ( 'NONE', #18252, 1.999999999999997113 ) ;
#2373=CARTESIAN_POINT ( 'NONE',  ( 10.13886454369750112, -63.17879643090980579, -45.99496747666990615 ) ) ;
#2374=FACE_OUTER_BOUND ( 'NONE', #43123, .T. ) ;
#2378=CARTESIAN_POINT ( 'NONE',  ( 56.93466172174790074, 19.03186587073140146, -52.70269903729370498 ) ) ;
#2379=CARTESIAN_POINT ( 'NONE',  ( 53.03699914620550260, 19.13327433011199830, -77.13749948101029474 ) ) ;
#2381=DIRECTION ( 'NONE',  ( 0.000000000000000000, 0.000000000000000000, -1.000000000000000000 ) ) ;
#2382=DIRECTION ( 'NONE',  ( 0.000000000000000000, 0.000000000000000000, 1.000000000000000000 ) ) ;
#2383=DIRECTION ( 'NONE',  ( -9.816708849317168638E-16, 1.000000000000000000, 0.000000000000000000 ) ) ;
#2386=DIRECTION ( 'NONE',  ( 1.000000000000000000, 0.000000000000000000, 0.000000000000000000 ) ) ;
#2389=CARTESIAN_POINT ( 'NONE',  ( 56.77148119808899907, -46.03634836625910509, -26.24810600973490082 ) ) ;
#2391=DIRECTION ( 'NONE',  ( -0.000000000000000000, -1.000000000000000000, -0.000000000000000000 ) ) ;
#2392=CARTESIAN_POINT ( 'NONE',  ( 13.50200499130249909, 20.63642445556759952, -74.86150924066380696 ) ) ;
#2394=CARTESIAN_POINT ( 'NONE',  ( 42.70541728070560339, -45.00675845543869968, -6.147241989062049328 ) ) ;
#2396=AXIS2_PLACEMENT_3D ( 'NONE', #6919, #2980, #7172 ) ;
#2398=ORIENTED_EDGE ( 'NONE', *, *, #32972, .F. ) ;
#2399=CARTESIAN_POINT ( 'NONE',  ( 53.27340400499669926, -49.09268838209659691, -26.76986176472670209 ) ) ;
#2400=CARTESIAN_POINT ( 'NONE',  ( 55.46462020123170333, -50.75003295001909720, -75.55576601992819974 ) ) ;
#2401=CARTESIAN_POINT ( 'NONE',  ( 11.43906257866700038, 33.09497493101680021, -15.68575602140459857 ) ) ;
#2404=AXIS2_PLACEMENT_3D ( 'NONE', #33345, #24688, #49361 ) ;
#2405=CARTESIAN_POINT ( 'NONE',  ( 47.35501076093819961, -54.67813530284840340, -54.64069690081250030 ) ) ;
#2407=VERTEX_POINT ( 'NONE', #44789 ) ;
#2409=EDGE_CURVE ( 'NONE', #30947, #24819, #31893, .T. ) ;
#2410=CARTESIAN_POINT ( 'NONE',  ( 47.55449607009450119, 23.31128263483790164, -54.66330429744959218 ) ) ;
#2414=CARTESIAN_POINT ( 'NONE',  ( 11.31571024077640075, 33.79537190493880416, -16.86897517425000004 ) ) ;
#2415=ADVANCED_FACE ( 'NONE', ( #8373 ), #5482, .T. ) ;
#2416=CARTESIAN_POINT ( 'NONE',  ( 51.67588099511389998, 17.45826125070719925, -77.01364301606231777 ) ) ;
#2417=CARTESIAN_POINT ( 'NONE',  ( 53.27426930170610575, 18.19673474085740139, -48.84492426196599979 ) ) ;
#2419=CARTESIAN_POINT ( 'NONE',  ( 58.40646430935630207, -46.88458887768990735, -48.04310473389099911 ) ) ;
#2420=CARTESIAN_POINT ( 'NONE',  ( 54.16532707871409968, 17.12274662488560040, -26.76512942855410060 ) ) ;
#2423=CARTESIAN_POINT ( 'NONE',  ( 53.36465014982429977, 18.25085194934079880, -49.20420490330940311 ) ) ;
#2424=CARTESIAN_POINT ( 'NONE',  ( 46.03121886948380137, -45.11618894467940066, -7.582877905987319700 ) ) ;
#2426=CARTESIAN_POINT ( 'NONE',  ( 10.76899899952330131, 31.88305279702909800, -45.20723331625340791 ) ) ;
#2429=DIRECTION ( 'NONE',  ( 0.6676418852214537347, -0.2329255526947816568, 0.7071067811863875896 ) ) ;
#2431=CARTESIAN_POINT ( 'NONE',  ( 18.50686101264880179, 20.06273318926150040, -74.35769860268439402 ) ) ;
#2432=VERTEX_POINT ( 'NONE', #21179 ) ;
#2434=CARTESIAN_POINT ( 'NONE',  ( 41.50224533218029421, 12.67611161623769966, -3.489448898335199889 ) ) ;
#2435=CARTESIAN_POINT ( 'NONE',  ( 49.41913868843145252, -2.245867004874552819, -15.72629724680255414 ) ) ;
#2437=ADVANCED_FACE ( 'NONE', ( #20661 ), #21573, .T. ) ;
#2438=CARTESIAN_POINT ( 'NONE',  ( 11.15230508032369805, -64.00960885307659964, -44.57032717116720022 ) ) ;
#2439=CARTESIAN_POINT ( 'NONE',  ( 56.21080665499489726, -45.60151275163879347, -25.51026796885810199 ) ) ;
#2449=ORIENTED_EDGE ( 'NONE', *, *, #15158, .T. ) ;
#2451=DIRECTION ( 'NONE',  ( 0.000000000000000000, 0.000000000000000000, 1.000000000000000000 ) ) ;
#2452=AXIS2_PLACEMENT_3D ( 'NONE', #39112, #35156, #43556 ) ;
#2453=CARTESIAN_POINT ( 'NONE',  ( 16.22101879095299992, 19.83813843325669879, -20.26096174765840274 ) ) ;
#2456=DIRECTION ( 'NONE',  ( -0.3918900565005491998, 0.9200120562340454722, 0.000000000000000000 ) ) ;
#2457=CARTESIAN_POINT ( 'NONE',  ( 47.27368826427839821, -54.50755326446490301, -75.00321679105040573 ) ) ;
#2458=CARTESIAN_POINT ( 'NONE',  ( 43.23251398108950383, 13.74603371045659905, -6.010618268419490207 ) ) ;
#2461=CARTESIAN_POINT ( 'NONE',  ( 53.35839899967449895, 20.15050419475459975, -75.63635010498570921 ) ) ;
#2462=CARTESIAN_POINT ( 'NONE',  ( 61.75043778037309750, 13.88381108430640154, -28.15157759350370270 ) ) ;
#2466=CARTESIAN_POINT ( 'NONE',  ( 5.641888144657690063, -58.94988526653390437, -11.71462473494669965 ) ) ;
#2467=CARTESIAN_POINT ( 'NONE',  ( 75.05098508634559096, -12.48077121835190084, -11.32537598484450037 ) ) ;
#2471=AXIS2_PLACEMENT_3D ( 'NONE', #48276, #29123, #1093 ) ;
#2472=PLANE ( 'NONE',  #49858 ) ;
#2476=CARTESIAN_POINT ( 'NONE',  ( 82.50625024752521597, -45.42892848413679729, -47.45620293274949830 ) ) ;
#2477=CARTESIAN_POINT ( 'NONE',  ( 13.65323342483580049, 20.15922856511949846, -23.15000000000000213 ) ) ;
#2479=CARTESIAN_POINT ( 'NONE',  ( 41.88234443671479568, 12.44058544459540094, -3.969549609002189783 ) ) ;
#2480=EDGE_CURVE ( 'NONE', #40057, #16152, #2840, .T. ) ;
#2483=CARTESIAN_POINT ( 'NONE',  ( 19.86710128871024850, 24.20909934830549659, -75.14570525072024054 ) ) ;
#2484=CARTESIAN_POINT ( 'NONE',  ( 66.23540447448814916, -49.95860450174190248, -75.14853292321149070 ) ) ;
#2487=CARTESIAN_POINT ( 'NONE',  ( 18.50685669541299916, -51.29511715723860732, -74.14992839339309683 ) ) ;
#2489=LINE ( 'NONE', #9580, #519 ) ;
#2490=VERTEX_POINT ( 'NONE', #19838 ) ;
#2493=VERTEX_POINT ( 'NONE', #3868 ) ;
#2494=CARTESIAN_POINT ( 'NONE',  ( -10.41130465719239950, 11.60708275212090079, -6.431269174833519564 ) ) ;
#2500=CARTESIAN_POINT ( 'NONE',  ( 16.13393739769609780, -15.61618894467929941, 8.449999999999999289 ) ) ;
#2505=CARTESIAN_POINT ( 'NONE',  ( 61.18213688343650603, -45.28487339755239560, -46.74705100057859397 ) ) ;
#2506=CARTESIAN_POINT ( 'NONE',  ( 53.51474650799030286, -49.43356839336680508, -49.22562654179730401 ) ) ;
#2507=CARTESIAN_POINT ( 'NONE',  ( 82.68190288415928535, -45.40220004952831800, -47.42733033421982469 ) ) ;
#2514=EDGE_LOOP ( 'NONE', ( #23570, #6495, #48068, #50962 ) ) ;
#2516=CARTESIAN_POINT ( 'NONE',  ( 51.93948718480190507, -51.08957512830220082, -76.10418645920529457 ) ) ;
#2517=VECTOR ( 'NONE', #47503, 1000.000000000000227 ) ;
#2518=CARTESIAN_POINT ( 'NONE',  ( 60.40971711783320330, 14.45930241792809845, -47.28043267387079851 ) ) ;
#2525=CARTESIAN_POINT ( 'NONE',  ( 45.08955516288700238, 14.59038207675800081, -8.804749820302610885 ) ) ;
#2526=CARTESIAN_POINT ( 'NONE',  ( 40.47914112739019998, -44.80448066467319990, -4.470311448230490647 ) ) ;
#2528=CARTESIAN_POINT ( 'NONE',  ( 65.44700751694060159, -1.324274634346296775, -16.55186757724361968 ) ) ;
#2529=CARTESIAN_POINT ( 'NONE',  ( 66.50380103983820845, 1.883526056381209512, -20.28031759223009445 ) ) ;
#2532=CARTESIAN_POINT ( 'NONE',  ( 74.93037295002230280, 11.88381105532070059, -15.31098073120859837 ) ) ;
#2535=CARTESIAN_POINT ( 'NONE',  ( 57.55751162087899786, 19.14609342572249773, -52.97747665988080001 ) ) ;
#2540=EDGE_CURVE ( 'NONE', #50841, #24756, #18562, .T. ) ;
#2542=CARTESIAN_POINT ( 'NONE',  ( 48.03324057931929758, -54.36799250499229430, -55.25634970046999683 ) ) ;
#2543=DIRECTION ( 'NONE',  ( 1.000000000000000000, 0.000000000000000000, 0.000000000000000000 ) ) ;
#2544=CARTESIAN_POINT ( 'NONE',  ( 56.40159749620720220, 19.40038761406519896, -53.06856178888660480 ) ) ;
#2545=CARTESIAN_POINT ( 'NONE',  ( 47.83059346947020174, 23.21195136793840064, -55.02665008976270400 ) ) ;
#2548=AXIS2_PLACEMENT_3D ( 'NONE', #19188, #3737, #3990 ) ;
#2550=( BOUNDED_CURVE ( )  B_SPLINE_CURVE ( 3, ( #20735, #5036, #45385, #20471 ),
 .UNSPECIFIED., .F., .T. ) 
 B_SPLINE_CURVE_WITH_KNOTS ( ( 4, 4 ),
 ( 5.769749740152300355, 6.283185307179586232 ),
 .UNSPECIFIED. ) 
 CURVE ( )  GEOMETRIC_REPRESENTATION_ITEM ( )  RATIONAL_B_SPLINE_CURVE ( ( 1.000000000000000000, 0.9781523768112219130, 0.9781523768112219130, 1.000000000000000000 ) ) 
 REPRESENTATION_ITEM ( '' )  );
#2551=ORIENTED_EDGE ( 'NONE', *, *, #25464, .F. ) ;
#2553=AXIS2_PLACEMENT_3D ( 'NONE', #20985, #36982, #21499 ) ;
#2554=CARTESIAN_POINT ( 'NONE',  ( 82.64649737942757213, 14.08998960694586344, -47.29316709580923117 ) ) ;
#2555=DIRECTION ( 'NONE',  ( 0.000000000000000000, 0.000000000000000000, 1.000000000000000000 ) ) ;
#2557=CARTESIAN_POINT ( 'NONE',  ( 61.75019796695539753, 13.88381105532070059, -28.15000000000000213 ) ) ;
#2558=CARTESIAN_POINT ( 'NONE',  ( 53.46882080935260007, 17.64232885596709721, -26.54419876889340202 ) ) ;
#2564=B_SPLINE_SURFACE_WITH_KNOTS ( 'NONE', 3, 3, ( 
 ( #16198, #32154, #43470, #12531, #35337, #44235 ),
 ( #8337, #39792, #40052, #31902, #24547, #48429 ),
 ( #24292, #51338, #11771, #4401, #20370, #19612 ),
 ( #4142, #19865, #27976, #7577, #36358, #15436 ),
 ( #35856, #466, #31388, #27729, #43979, #47417 ),
 ( #11510, #27468, #39540, #3642, #15689, #31643 ),
 ( #8084, #47663, #51845, #47922, #32670, #4922 ),
 ( #13316, #13818, #17493, #25841, #37660, #20629 ),
 ( #9117, #21406, #45277, #37155, #37408, #17746 ),
 ( #29532, #45536, #20893, #24813, #9387, #29021 ) ),
 .UNSPECIFIED., .F., .F., .F.,
 ( 4, 2, 2, 2, 4 ),
 ( 4, 1, 1, 4 ),
 ( -0.2468266944438050059, -0.2159733576383290055, -0.1666080187495679876, -0.08762347652754901017, 1.941358000000000020E-15 ),
 ( 0.000000000000000000, 0.3333333333333329818, 0.6666666666666670737, 1.000000000000000000 ),
 .UNSPECIFIED. ) ;
#2567=ORIENTED_EDGE ( 'NONE', *, *, #6462, .T. ) ;
#2568=EDGE_LOOP ( 'NONE', ( #17814, #45757, #35941, #44641, #4819 ) ) ;
#2569=CARTESIAN_POINT ( 'NONE',  ( 11.98449920101150035, -64.78734946337890221, -16.08642242878890016 ) ) ;
#2572=CARTESIAN_POINT ( 'NONE',  ( 9.886195853582540494, -64.20534592295300058, -46.62515117760860051 ) ) ;
#2573=ORIENTED_EDGE ( 'NONE', *, *, #14370, .F. ) ;
#2575=CARTESIAN_POINT ( 'NONE',  ( 50.12648257197400170, 22.24397334070430077, -55.01261709213260076 ) ) ;
#2576=CARTESIAN_POINT ( 'NONE',  ( 57.50723795381379944, -45.11618894467940066, -25.33268388717609909 ) ) ;
#2577=CARTESIAN_POINT ( 'NONE',  ( 50.12452099567399699, 21.34276116794150369, -52.77544220100040206 ) ) ;
#2578=CARTESIAN_POINT ( 'NONE',  ( 63.13518000424760146, -1.636848992617379928, -16.22147126600509637 ) ) ;
#2579=CARTESIAN_POINT ( 'NONE',  ( 50.97631566918259693, -50.00474991773980094, -76.22722522842570925 ) ) ;
#2580=CARTESIAN_POINT ( 'NONE',  ( 56.64011576333900422, -50.33902915376989995, -52.69731447354050147 ) ) ;
#2583=CARTESIAN_POINT ( 'NONE',  ( 68.13393739769814772, 19.38381105532029736, -71.50000000000200373 ) ) ;
#2584=EDGE_LOOP ( 'NONE', ( #41859, #16154, #11938, #44412, #38669 ) ) ;
#2586=CARTESIAN_POINT ( 'NONE',  ( 47.18077425662879421, -45.11618894467940066, -8.347046103084750257 ) ) ;
#2589=CARTESIAN_POINT ( 'NONE',  ( 13.56095021366290077, -51.24259045802140378, -22.27874983821260102 ) ) ;
#2590=CARTESIAN_POINT ( 'NONE',  ( 56.10489411446869212, 19.52080739473450066, -75.03274246618039456 ) ) ;
#2591=CARTESIAN_POINT ( 'NONE',  ( 46.81978912889830013, -53.49478526707780190, -76.01748491306379663 ) ) ;
#2593=CARTESIAN_POINT ( 'NONE',  ( 57.24436304061489977, 13.89534489433389908, -17.93020804353299980 ) ) ;
#2594=LINE ( 'NONE', #26415, #14815 ) ;
#2598=CYLINDRICAL_SURFACE ( 'NONE', #20103, 1.999999999999996225 ) ;
#2599=AXIS2_PLACEMENT_3D ( 'NONE', #19074, #18560, #30600 ) ;
#2601=CARTESIAN_POINT ( 'NONE',  ( 47.63737930067980386, 23.29734254719310016, -74.36261479959799203 ) ) ;
#2605=CARTESIAN_POINT ( 'NONE',  ( 45.82851118213719843, -45.11588810659969795, -7.494127385217890236 ) ) ;
#2609=CARTESIAN_POINT ( 'NONE',  ( 82.53030587998239298, 14.28927347135980064, -47.58595373936260842 ) ) ;
#2614=CARTESIAN_POINT ( 'NONE',  ( 56.61928439928507828, -45.32411236664518839, -17.93019253464870033 ) ) ;
#2616=CARTESIAN_POINT ( 'NONE',  ( -29.55684472351650172, 4.629324287396400450, -55.62305524083090091 ) ) ;
#2618=CARTESIAN_POINT ( 'NONE',  ( 52.69140955423309691, -49.74818585651569691, -48.48983962412659565 ) ) ;
#2622=CARTESIAN_POINT ( 'NONE',  ( 13.65323342448890109, 20.15922856535879859, -23.15000001653130113 ) ) ;
#2623=CARTESIAN_POINT ( 'NONE',  ( 83.84453551654050329, 13.09585956956080111, -46.66649649553750123 ) ) ;
#2626=CARTESIAN_POINT ( 'NONE',  ( 52.83551389523529451, 18.45330133924599991, -48.92570522021940604 ) ) ;
#2627=CARTESIAN_POINT ( 'NONE',  ( 55.95161226490260020, -45.83867278594010486, -17.62594177103509807 ) ) ;
#2628=CARTESIAN_POINT ( 'NONE',  ( 13.20770907579910158, -46.26637462015160196, -23.15000000000000213 ) ) ;
#2631=CARTESIAN_POINT ( 'NONE',  ( 10.89208540626859900, -65.00086834622119625, -17.57297890437749999 ) ) ;
#2632=CARTESIAN_POINT ( 'NONE',  ( 9.618181907774909334, 33.17626444807680031, -46.87734673202830038 ) ) ;
#2634=CIRCLE ( 'NONE', #10144, 2.000000000000001776 ) ;
#2635=CARTESIAN_POINT ( 'NONE',  ( 10.98984918190470061, -65.15326276073609790, -18.13296861429880380 ) ) ;
#2636=DIRECTION ( 'NONE',  ( 0.000000000000000000, 0.000000000000000000, 1.000000000000000000 ) ) ;
#2642=ORIENTED_EDGE ( 'NONE', *, *, #20677, .F. ) ;
#2645=CARTESIAN_POINT ( 'NONE',  ( 10.97982788474749860, -63.40303658660428709, -44.74674020368789940 ) ) ;
#2649=CARTESIAN_POINT ( 'NONE',  ( 57.07954899399199888, 19.06789840296940142, -52.78599243482480574 ) ) ;
#2650=CARTESIAN_POINT ( 'NONE',  ( 52.47683853037149504, 18.72915222723299777, -77.24560337738110150 ) ) ;
#2652=CARTESIAN_POINT ( 'NONE',  ( 9.127478424014915603, -63.94375969568785933, -46.75102854448083889 ) ) ;
#2661=CARTESIAN_POINT ( 'NONE',  ( 61.55415490858686667, -1.843864237299252862, -15.99574535869863823 ) ) ;
#2666=CARTESIAN_POINT ( 'NONE',  ( 68.13393739769745139, -49.21324915460109395, -75.95351669811962836 ) ) ;
#2667=CARTESIAN_POINT ( 'NONE',  ( 41.37000474207589917, -45.26882832540889723, -6.004987957165030643 ) ) ;
#2674=CARTESIAN_POINT ( 'NONE',  ( 56.18572637789630164, -50.74534604707739760, -74.96558747352590046 ) ) ;
#2675=CARTESIAN_POINT ( 'NONE',  ( -2.285077198058380166, 18.61977639420179642, -5.969580375927669991 ) ) ;
#2678=EDGE_CURVE ( 'NONE', #19040, #5062, #8304, .T. ) ;
#2679=CARTESIAN_POINT ( 'NONE',  ( 87.61621807841599718, -15.61618894467929941, -61.12885639714370001 ) ) ;
#2680=ORIENTED_EDGE ( 'NONE', *, *, #33098, .F. ) ;
#2681=CARTESIAN_POINT ( 'NONE',  ( 15.05440318628110141, 21.88381105532300097, -76.14999999999999147 ) ) ;
#2682=CARTESIAN_POINT ( 'NONE',  ( 47.41723297365239631, 23.41216560487029952, -54.77931948513369775 ) ) ;
#2686=CARTESIAN_POINT ( 'NONE',  ( 11.99376942192360040, 34.12659637466200024, -17.21195695013489768 ) ) ;
#2688=CARTESIAN_POINT ( 'NONE',  ( 53.13650386459389807, 18.26782892954070192, -48.81774254411430292 ) ) ;
#2690=CARTESIAN_POINT ( 'NONE',  ( 60.34488827473360573, -45.86932735725469712, -47.73027270518679899 ) ) ;
#2691=CARTESIAN_POINT ( 'NONE',  ( 52.82924303383909859, 18.40678474754740179, -27.83106633233370175 ) ) ;
#2692=CARTESIAN_POINT ( 'NONE',  ( 20.13393739496619972, 24.18330852864180258, -20.65000000000000213 ) ) ;
#2693=CARTESIAN_POINT ( 'NONE',  ( 52.85423108789519375, -49.63991540118476564, -27.95802159601835157 ) ) ;
#2697=CARTESIAN_POINT ( 'NONE',  ( 10.77261237629559965, 32.06410662680400492, -45.20506416186449883 ) ) ;
#2700=CARTESIAN_POINT ( 'NONE',  ( 12.73007005307443329, 24.23871925420958462, -75.55954122747003510 ) ) ;
#2701=EDGE_LOOP ( 'NONE', ( #4927, #24902, #44543, #10126 ) ) ;
#2704=CARTESIAN_POINT ( 'NONE',  ( 48.82567944589380460, -3.116188925162400203, -15.64999999106299988 ) ) ;
#2706=CARTESIAN_POINT ( 'NONE',  ( 11.66108919451019865, -64.87818593170879922, -45.24345066936370330 ) ) ;
#2707=CARTESIAN_POINT ( 'NONE',  ( 55.89127853695700310, -45.96104820497279775, -25.54022091618979928 ) ) ;
#2708=CARTESIAN_POINT ( 'NONE',  ( 11.19961949155312908, -65.24734059375452944, -18.17421237899869979 ) ) ;
#2710=( BOUNDED_CURVE ( )  B_SPLINE_CURVE ( 3, ( #40308, #40054, #12274, #8338 ),
 .UNSPECIFIED., .F., .T. ) 
 B_SPLINE_CURVE_WITH_KNOTS ( ( 4, 4 ),
 ( 5.578367201137250042, 5.769749740152300355 ),
 .UNSPECIFIED. ) 
 CURVE ( )  GEOMETRIC_REPRESENTATION_ITEM ( )  RATIONAL_B_SPLINE_CURVE ( ( 1.000000000000000000, 0.9969500553618734218, 0.9969500553618734218, 1.000000000000000000 ) ) 
 REPRESENTATION_ITEM ( '' )  );
#2712=ORIENTED_EDGE ( 'NONE', *, *, #10147, .F. ) ;
#2713=CARTESIAN_POINT ( 'NONE',  ( 11.63574103177584185, 34.14703465354016032, -22.51277960591899685 ) ) ;
#2715=CARTESIAN_POINT ( 'NONE',  ( 12.16706694049450022, 34.22772821235970042, -22.71320579729880151 ) ) ;
#2717=CARTESIAN_POINT ( 'NONE',  ( 51.23833940013359722, -45.11618894467940066, -11.16259862780779955 ) ) ;
#2722=EDGE_CURVE ( 'NONE', #1545, #28603, #44726, .T. ) ;
#2724=EDGE_CURVE ( 'NONE', #13650, #27748, #30261, .T. ) ;
#2726=CARTESIAN_POINT ( 'NONE',  ( 47.30318258422299493, -54.71095611916120305, -74.36173831268348522 ) ) ;
#2727=CARTESIAN_POINT ( 'NONE',  ( 66.82519403554060489, 13.09192299164059925, -11.25137922129169965 ) ) ;
#2728=EDGE_CURVE ( 'NONE', #6692, #43986, #46190, .T. ) ;
#2730=CARTESIAN_POINT ( 'NONE',  ( 52.75030376661270282, 20.12775360152859960, -75.83477265320939864 ) ) ;
#2731=LINE ( 'NONE', #38642, #41516 ) ;
#2734=CARTESIAN_POINT ( 'NONE',  ( 53.91527575946920336, -48.70888914390349811, -27.03219125244680043 ) ) ;
#2735=CARTESIAN_POINT ( 'NONE',  ( 10.35404411787279955, -63.79155264719249629, -15.51648447543499998 ) ) ;
#2736=CARTESIAN_POINT ( 'NONE',  ( 76.39184943767510561, -18.71884955068060208, -12.76139016365400103 ) ) ;
#2737=CARTESIAN_POINT ( 'NONE',  ( 75.29474438729376118, 13.39011681956304045, -14.04674746638269767 ) ) ;
#2738=EDGE_CURVE ( 'NONE', #26146, #23479, #4370, .T. ) ;
#2739=CARTESIAN_POINT ( 'NONE',  ( 61.10787018228941037, -45.48724546724425721, -47.48172069074966828 ) ) ;
#2741=AXIS2_PLACEMENT_3D ( 'NONE', #9925, #33245, #25887 ) ;
#2742=DIRECTION ( 'NONE',  ( -0.06672502100504953959, -0.04847856544221940817, 0.9965929962951476373 ) ) ;
#2743=CARTESIAN_POINT ( 'NONE',  ( 82.43660516933499594, -45.21753288021749739, -47.02797074234310060 ) ) ;
#2744=LINE ( 'NONE', #42582, #14789 ) ;
#2745=CARTESIAN_POINT ( 'NONE',  ( 41.54582584773770293, 12.73228223202879938, -4.072799719962560516 ) ) ;
#2746=CARTESIAN_POINT ( 'NONE',  ( 61.43325308111587901, -45.44830257304832344, -47.47808681911117645 ) ) ;
#2747=CARTESIAN_POINT ( 'NONE',  ( 19.62692545003119449, 24.23099720707456584, -75.46694760810223102 ) ) ;
#2748=CARTESIAN_POINT ( 'NONE',  ( 65.43042069957888884, -49.21324915460513694, -73.25000000000119371 ) ) ;
#2750=CARTESIAN_POINT ( 'NONE',  ( 18.05183576353649855, -51.93578155835659516, -75.67800190747080080 ) ) ;
#2751=CARTESIAN_POINT ( 'NONE',  ( 41.51083608087070331, -44.40732572871969808, -4.911476834593860197 ) ) ;
#2755=EDGE_LOOP ( 'NONE', ( #50519, #36386, #18610, #21044 ) ) ;
#2757=CARTESIAN_POINT ( 'NONE',  ( 61.09252571675989429, -45.64957244923589741, -47.71760867771700276 ) ) ;
#2760=ADVANCED_FACE ( 'NONE', ( #37126 ), #36964, .F. ) ;
#2762=CARTESIAN_POINT ( 'NONE',  ( 40.79813849721050190, -45.21264691650740275, -5.648537283802860465 ) ) ;
#2763=ORIENTED_EDGE ( 'NONE', *, *, #5622, .F. ) ;
#2767=FACE_OUTER_BOUND ( 'NONE', #41206, .T. ) ;
#2768=CARTESIAN_POINT ( 'NONE',  ( 61.13177402460449628, -45.31381189176509849, -46.88387570683920558 ) ) ;
#2769=DIRECTION ( 'NONE',  ( 0.000000000000000000, 1.000000000000000000, 0.000000000000000000 ) ) ;
#2771=CARTESIAN_POINT ( 'NONE',  ( 16.13393739769620083, -51.11618894467930119, -15.65000000000000036 ) ) ;
#2774=B_SPLINE_CURVE_WITH_KNOTS ( 'NONE', 3,
 ( #43181, #7274, #26647, #20331, #20849, #15908, #25028, #43944, #32372 ),
 .UNSPECIFIED., .F., .F.,
 ( 4, 1, 1, 1, 1, 1, 4 ),
 ( 0.000000000000000000, 0.1666583021584449043, 0.3333266417267553017, 0.4999949812950666983, 0.6666633208633782059, 0.8333316604316886034, 1.000000000000000000 ),
 .UNSPECIFIED. ) ;
#2776=EDGE_CURVE ( 'NONE', #13640, #25200, #38652, .T. ) ;
#2778=ORIENTED_EDGE ( 'NONE', *, *, #17160, .F. ) ;
#2781=CARTESIAN_POINT ( 'NONE',  ( 52.03834266725660740, -51.29072892105509851, -76.00976796454538942 ) ) ;
#2782=CARTESIAN_POINT ( 'NONE',  ( 60.86852778604830405, 14.26338112473730035, -47.33036891254590728 ) ) ;
#2783=CIRCLE ( 'NONE', #36236, 2.000000000000002220 ) ;
#2784=ADVANCED_FACE ( 'NONE', ( #48666 ), #28568, .T. ) ;
#2786=CARTESIAN_POINT ( 'NONE',  ( 40.74969953824990654, -44.70763297598060149, -4.809312831994500215 ) ) ;
#2788=CARTESIAN_POINT ( 'NONE',  ( -7.615929272822939744, 14.09493422113850158, -5.327442894417729669 ) ) ;
#2790=CARTESIAN_POINT ( 'NONE',  ( 72.38393739769620083, 4.883811055320659733, -61.44999999999999574 ) ) ;
#2791=CARTESIAN_POINT ( 'NONE',  ( 87.61621807841599718, -48.61618894467930119, -61.12885639714370001 ) ) ;
#2793=ORIENTED_EDGE ( 'NONE', *, *, #38533, .T. ) ;
#2794=CARTESIAN_POINT ( 'NONE',  ( 14.33739625361640080, -52.54005950962240235, -75.96018872839380265 ) ) ;
#2796=CARTESIAN_POINT ( 'NONE',  ( 57.55751162087899786, 19.27819942682179999, -53.27961218320869818 ) ) ;
#2799=EDGE_CURVE ( 'NONE', #7053, #39784, #13043, .T. ) ;
#2801=CARTESIAN_POINT ( 'NONE',  ( 15.80832228677579643, 19.69806892893299732, -20.21644471496479767 ) ) ;
#2802=CARTESIAN_POINT ( 'NONE',  ( 18.86789271228509790, -51.78678246903520233, -74.14999999999999147 ) ) ;
#2805=CARTESIAN_POINT ( 'NONE',  ( 47.87139909866390752, -54.42646853815559638, -55.03639171593840018 ) ) ;
#2806=CARTESIAN_POINT ( 'NONE',  ( 6.293131413228051585, -65.09536678314599101, -49.18705164837409427 ) ) ;
#2807=AXIS2_PLACEMENT_3D ( 'NONE', #1005, #37170, #45292 ) ;
#2810=LINE ( 'NONE', #19037, #40669 ) ;
#2811=VERTEX_POINT ( 'NONE', #41824 ) ;
#2815=VERTEX_POINT ( 'NONE', #2256 ) ;
#2817=CARTESIAN_POINT ( 'NONE',  ( 60.72865454444709599, -45.52246636016900538, -47.10836437988919556 ) ) ;
#2818=CARTESIAN_POINT ( 'NONE',  ( 82.57795157571968048, 13.96423584352574743, -47.00703096682629933 ) ) ;
#2831=CARTESIAN_POINT ( 'NONE',  ( 12.23389792222440065, -64.89608577200989714, -16.17187715587200003 ) ) ;
#2834=CARTESIAN_POINT ( 'NONE',  ( 10.60384355420380054, -64.91168656924629943, -47.04674094553849528 ) ) ;
#2837=CARTESIAN_POINT ( 'NONE',  ( 53.42290160909190178, 20.83982452118389972, -54.29362578891399949 ) ) ;
#2838=CARTESIAN_POINT ( 'NONE',  ( -14.86606260230379917, -15.61618894467933139, -15.65000000000000036 ) ) ;
#2839=VECTOR ( 'NONE', #44271, 1000.000000000000114 ) ;
#2840=LINE ( 'NONE', #35575, #50338 ) ;
#2841=CARTESIAN_POINT ( 'NONE',  ( 62.16233645777079886, -0.1749398299712949800, -16.60655181478709963 ) ) ;
#2842=CARTESIAN_POINT ( 'NONE',  ( 51.62358001281820208, -48.61618677531440369, -76.93789421597479361 ) ) ;
#2843=CARTESIAN_POINT ( 'NONE',  ( 57.17297709606850020, -50.49682799391059973, -53.01978805370689685 ) ) ;
#2845=ORIENTED_EDGE ( 'NONE', *, *, #17164, .T. ) ;
#2848=ORIENTED_EDGE ( 'NONE', *, *, #1192, .F. ) ;
#2849=CARTESIAN_POINT ( 'NONE',  ( 35.13393739769620083, -15.61618894467929941, 8.349999999999999645 ) ) ;
#2853=CARTESIAN_POINT ( 'NONE',  ( 14.24102869631719948, -51.10273149057969988, -22.22788221432130129 ) ) ;
#2855=CARTESIAN_POINT ( 'NONE',  ( 56.82341722989219335, 13.94957864525430047, -16.89538187380119894 ) ) ;
#2861=CARTESIAN_POINT ( 'NONE',  ( 47.02416321684500389, 22.58718688193119917, -75.82399966601029462 ) ) ;
#2867=CARTESIAN_POINT ( 'NONE',  ( 82.48420028019749850, 13.86594486706619911, -46.54735908456930815 ) ) ;
#2868=CONICAL_SURFACE ( 'NONE', #5419, 44.00000000000000000, 0.8066715494215099813 ) ;
#2871=CARTESIAN_POINT ( 'NONE',  ( 53.31390735437268802, 19.22904354471013733, -77.17777228777733001 ) ) ;
#2874=CARTESIAN_POINT ( 'NONE',  ( -28.69324816627959862, 4.182983592527669714, -54.99967661823389875 ) ) ;
#2875=VERTEX_POINT ( 'NONE', #29751 ) ;
#2876=CARTESIAN_POINT ( 'NONE',  ( 52.65621920618569618, -49.77598664841080733, -48.47378032971909789 ) ) ;
#2877=ORIENTED_EDGE ( 'NONE', *, *, #19055, .T. ) ;
#2878=LINE ( 'NONE', #45872, #1950 ) ;
#2880=CARTESIAN_POINT ( 'NONE',  ( 13.77909129202510030, 19.73319454833459830, -21.81863451142220001 ) ) ;
#2883=CARTESIAN_POINT ( 'NONE',  ( 52.77947503461199830, 18.47416142194530053, -48.82716066735080318 ) ) ;
#2884=CARTESIAN_POINT ( 'NONE',  ( 54.50030068701860131, -46.15578316411880166, -15.72721191834270194 ) ) ;
#2893=CARTESIAN_POINT ( 'NONE',  ( 13.00893739769619906, 34.28605925116850273, -47.75434321273180416 ) ) ;
#2895=CARTESIAN_POINT ( 'NONE',  ( 54.13393739769620083, -15.61618894467929941, 1.600000000000000089 ) ) ;
#2896=CARTESIAN_POINT ( 'NONE',  ( 52.82359347161857954, -49.70062430464942338, -48.95125679539614083 ) ) ;
#2898=CARTESIAN_POINT ( 'NONE',  ( 50.51702630346309775, -53.30999449162459314, -54.91376886094779763 ) ) ;
#2899=ORIENTED_EDGE ( 'NONE', *, *, #23030, .F. ) ;
#2901=ORIENTED_EDGE ( 'NONE', *, *, #359, .F. ) ;
#2902=CARTESIAN_POINT ( 'NONE',  ( 10.14269678154489895, -63.23625467025420477, -45.99342279163030156 ) ) ;
#2903=DIRECTION ( 'NONE',  ( -1.000000000000000000, 0.000000000000000000, 0.000000000000000000 ) ) ;
#2905=DIRECTION ( 'NONE',  ( 0.000000000000000000, -1.000000000000000000, 0.000000000000000000 ) ) ;
#2906=CARTESIAN_POINT ( 'NONE',  ( 53.07595676737840762, 19.15211386111450054, -77.13124878406790685 ) ) ;
#2907=ORIENTED_EDGE ( 'NONE', *, *, #3499, .T. ) ;
#2908=CARTESIAN_POINT ( 'NONE',  ( 12.13162407143141941, -65.41884435351431648, -47.52833372959231895 ) ) ;
#2915=CARTESIAN_POINT ( 'NONE',  ( 61.75019796695539753, -46.11618894467930119, -46.37203261889099792 ) ) ;
#2919=CARTESIAN_POINT ( 'NONE',  ( 74.17629866868290378, 1.883811055320649963, -65.34607522167520699 ) ) ;
#2922=LINE ( 'NONE', #30420, #45089 ) ;
#2923=VECTOR ( 'NONE', #49668, 1000.000000000000000 ) ;
#2925=CARTESIAN_POINT ( 'NONE',  ( 16.13393739769620083, -15.61618894467929941, -46.39999999999999858 ) ) ;
#2926=CARTESIAN_POINT ( 'NONE',  ( 11.74706319441980007, 33.70588526301440169, -16.38446683800539816 ) ) ;
#2928=CARTESIAN_POINT ( 'NONE',  ( 52.87639532687919797, -49.52782412333860407, -27.19604750702729845 ) ) ;
#2929=CARTESIAN_POINT ( 'NONE',  ( 55.50491188657730390, -50.93693546367299518, -75.08273106147520082 ) ) ;
#2930=CARTESIAN_POINT ( 'NONE',  ( -5.479087955498720852, 16.54576887086220083, -6.304622368372980290 ) ) ;
#2931=DIRECTION ( 'NONE',  ( 0.000000000000000000, 0.000000000000000000, -1.000000000000000000 ) ) ;
#2933=CARTESIAN_POINT ( 'NONE',  ( 47.51629483024640166, -54.56948809585979632, -54.66793506916069845 ) ) ;
#2934=DIRECTION ( 'NONE',  ( 0.000000000000000000, 0.000000000000000000, -1.000000000000000000 ) ) ;
#2936=CARTESIAN_POINT ( 'NONE',  ( -9.549430425165668979, -43.62870283194010312, -5.615282516777119426 ) ) ;
#2937=CARTESIAN_POINT ( 'NONE',  ( 47.68653297382180511, 23.26174403522189849, -54.85872168688340622 ) ) ;
#2940=CARTESIAN_POINT ( 'NONE',  ( 13.44563218319239972, 19.36637353181840027, -21.34300943931999939 ) ) ;
#2941=CARTESIAN_POINT ( 'NONE',  ( 61.36953742131760237, 14.18133800638229935, -47.42052028026720478 ) ) ;
#2942=CARTESIAN_POINT ( 'NONE',  ( 11.47551314107550091, 33.73997922480180023, -16.61573023121770021 ) ) ;
#2943=CARTESIAN_POINT ( 'NONE',  ( 52.14531965947149672, 18.65759927364149817, -76.93285152251199577 ) ) ;
#2944=CARTESIAN_POINT ( 'NONE',  ( 53.13654529785400626, 18.26855529545099799, -48.84750850883899886 ) ) ;
#2945=DIRECTION ( 'NONE',  ( -0.000000000000000000, 1.000000000000000000, 0.000000000000000000 ) ) ;
#2947=CARTESIAN_POINT ( 'NONE',  ( 52.81005473481379653, 18.43886536192449910, -28.08974515321689935 ) ) ;
#2948=ADVANCED_FACE ( 'NONE', ( #16860 ), #32808, .F. ) ;
#2951=CARTESIAN_POINT ( 'NONE',  ( 52.67198247596510186, 18.54881933231609992, -48.75776900890529930 ) ) ;
#2952=CARTESIAN_POINT ( 'NONE',  ( 37.13393739769620083, -15.61618894467929941, -12.65000000000000036 ) ) ;
#2954=CARTESIAN_POINT ( 'NONE',  ( 11.13393739769619906, 32.04700499139590164, -43.91469645497959817 ) ) ;
#2956=CARTESIAN_POINT ( 'NONE',  ( 66.85053874715731581, -33.11604528757069943, -20.46403489035089862 ) ) ;
#2957=CARTESIAN_POINT ( 'NONE',  ( 11.13393739769619906, 32.24968758154479787, -24.15000000000000213 ) ) ;
#2959=ORIENTED_EDGE ( 'NONE', *, *, #31324, .F. ) ;
#2960=CARTESIAN_POINT ( 'NONE',  ( 42.62644315548489971, 11.62703185229469938, -3.197525305353829950 ) ) ;
#2961=CARTESIAN_POINT ( 'NONE',  ( 50.03950439116019311, -1.319789489291227857, -15.98383729154298116 ) ) ;
#2963=CARTESIAN_POINT ( 'NONE',  ( 11.89007180640820138, -65.09421494503590111, -45.69968209956180516 ) ) ;
#2964=CARTESIAN_POINT ( 'NONE',  ( 57.65063410596479798, -45.12128949765089914, -25.41617693766169950 ) ) ;
#2969=CARTESIAN_POINT ( 'NONE',  ( 11.71770650845053829, 34.17304478383466204, -22.42848135754658045 ) ) ;
#2971=CARTESIAN_POINT ( 'NONE',  ( 11.79202840372359873, 34.19503632603060339, -22.35240682345929741 ) ) ;
#2973=EDGE_CURVE ( 'NONE', #50743, #27433, #16057, .T. ) ;
#2975=CARTESIAN_POINT ( 'NONE',  ( 51.86285139979289482, 1.501691761424130522, -18.73280815860681159 ) ) ;
#2976=CARTESIAN_POINT ( 'NONE',  ( 15.92174032690060059, 19.82163670650420073, -20.83925419535739820 ) ) ;
#2979=CARTESIAN_POINT ( 'NONE',  ( 59.22431851757179544, -28.11149781888600074, -15.66519468461460107 ) ) ;
#2980=DIRECTION ( 'NONE',  ( 0.000000000000000000, 0.000000000000000000, 1.000000000000000000 ) ) ;
#2981=CARTESIAN_POINT ( 'NONE',  ( 47.24086420343820691, -54.75472043013769508, -74.36236381585459299 ) ) ;
#2982=CARTESIAN_POINT ( 'NONE',  ( 45.33440053090729549, 12.30260350233129962, -5.407269074095729877 ) ) ;
#2985=DIRECTION ( 'NONE',  ( -0.5110015285683598973, 0.4887508954475665024, -0.7071067811865485719 ) ) ;
#2986=CARTESIAN_POINT ( 'NONE',  ( 65.24498301373863285, -31.35931339248442029, -16.97693345051512637 ) ) ;
#2988=B_SPLINE_SURFACE_WITH_KNOTS ( 'NONE', 3, 3, ( 
 ( #49772, #24856, #24591, #13359, #44539, #36660, #5496, #17787, #29317, #17287, #45324, #8640, #44802, #1550, #12843, #8905 ),
 ( #21451, #40863, #49008, #763, #16759, #33247, #1036, #37451, #49264, #25632, #21701, #45579, #4968, #32713, #37709, #48739 ),
 ( #20935, #17030, #32981, #41636, #9428, #17538, #9674, #5744, #2324, #42945, #38758, #46886, #18049, #26409, #30084, #2853 ),
 ( #6263, #30858, #42688, #2589, #10713, #51059, #22739, #14891, #34799, #50544, #6784, #42429, #42164, #50804, #22223, #14636 ),
 ( #41903, #9928, #30345, #10973, #18817, #29821, #26940, #7042, #39015, #22994, #37971, #18564, #50025, #35052, #46109, #26154 ),
 ( #34269, #38230, #34015, #3110, #19078, #45839, #25890, #6003, #21962, #50292, #30606, #2071, #14118, #10195, #18298, #38488 ),
 ( #14380, #46624, #46368, #10456, #6519, #22481, #34540, #26668, #27957, #12002, #31370, #47142, #16175, #8066, #23762, #35322 ),
 ( #8317, #43961, #24012, #32133, #20101, #27193, #36090, #43206, #198, #43707, #51573, #15672, #24270, #31626, #47902, #51320 ),
 ( #15417, #48152, #11494, #3881, #28215, #40291, #12256, #47645, #44216, #40033, #4382, #4126, #3624, #20350, #36336, #15156 ),
 ( #19339, #47399, #7810, #31117, #19595, #39776, #31883, #35586, #27450, #11231, #7295, #23246, #39264, #3365, #43453, #11751 ) ),
 .UNSPECIFIED., .F., .F., .F.,
 ( 4, 1, 1, 1, 1, 1, 1, 4 ),
 ( 4, 2, 2, 2, 2, 2, 2, 4 ),
 ( -5.223814999999999915E-09, 0.1428571428571430157, 0.2857142857142860315, 0.4285714285714289917, 0.5714285714285709528, 0.7142857142857139685, 0.8571428571428569843, 1.000000005223810051 ),
 ( -5.223816000000000234E-09, 0.4421363464883489858, 0.9474350281893190173, 1.263246704252430019, 1.421152542283979914, 1.673801883134460100, 2.076007908835539872, 2.526493408654630013 ),
 .UNSPECIFIED. ) ;
#2990=AXIS2_PLACEMENT_3D ( 'NONE', #15099, #4070, #141 ) ;
#2991=DIRECTION ( 'NONE',  ( -0.2260571801428161165, 0.000000000000000000, 0.9741140340359943917 ) ) ;
#2993=CARTESIAN_POINT ( 'NONE',  ( 0.1207629063369290018, -53.60130123069310315, -8.684987670772850166 ) ) ;
#2994=CARTESIAN_POINT ( 'NONE',  ( 76.41176102376428503, -21.82315656738479959, -12.84719217718200035 ) ) ;
#2995=CARTESIAN_POINT ( 'NONE',  ( 75.40794329062271117, 12.89811451530892938, -13.65441625236441325 ) ) ;
#2996=CARTESIAN_POINT ( 'NONE',  ( 20.08285034307092687, -55.42068993749968797, -74.66535148654590159 ) ) ;
#2997=LINE ( 'NONE', #18967, #459 ) ;
#2998=CARTESIAN_POINT ( 'NONE',  ( 47.18324198357279897, 23.57489020266570279, -54.61058319554400242 ) ) ;
#2999=CARTESIAN_POINT ( 'NONE',  ( 82.13853704237929776, -45.35390657427750227, -47.32252334011910477 ) ) ;
#3000=CARTESIAN_POINT ( 'NONE',  ( 57.35806099734729457, -50.23336412204299961, -52.73965739960290477 ) ) ;
#3001=CARTESIAN_POINT ( 'NONE',  ( 41.84726577509989909, 12.36321918212159865, -3.460729483473919732 ) ) ;
#3002=CARTESIAN_POINT ( 'NONE',  ( 67.20199456633837087, -29.99687375860984062, -17.36203811242810957 ) ) ;
#3005=CARTESIAN_POINT ( 'NONE',  ( 67.04038824939742369, -50.70395984888145335, -73.25000000000218847 ) ) ;
#3007=CARTESIAN_POINT ( 'NONE',  ( 75.74828555535219721, -43.35025879547261951, -13.50093798269990053 ) ) ;
#3008=CARTESIAN_POINT ( 'NONE',  ( 17.87926713331770046, -52.17875626651990473, -75.87012052777591009 ) ) ;
#3009=CARTESIAN_POINT ( 'NONE',  ( 53.17864038894789758, -45.11618894467940066, -9.007559113946960849 ) ) ;
#3011=( BOUNDED_CURVE ( )  B_SPLINE_CURVE ( 3, ( #22961, #38453, #19308, #2557 ),
 .UNSPECIFIED., .F., .T. ) 
 B_SPLINE_CURVE_WITH_KNOTS ( ( 4, 4 ),
 ( 5.063167621403719565, 6.283185307179586232 ),
 .UNSPECIFIED. ) 
 CURVE ( )  GEOMETRIC_REPRESENTATION_ITEM ( )  RATIONAL_B_SPLINE_CURVE ( ( 1.000000000000000000, 0.8797619680071214754, 0.8797619680071214754, 1.000000000000000000 ) ) 
 REPRESENTATION_ITEM ( '' )  );
#3014=CARTESIAN_POINT ( 'NONE',  ( 2.774651518975000286, 25.39333629030980433, -11.69507786875200139 ) ) ;
#3018=AXIS2_PLACEMENT_3D ( 'NONE', #927, #12465, #4082 ) ;
#3020=CARTESIAN_POINT ( 'NONE',  ( 45.08949527824870529, -45.82276084545720352, -8.804711001959010019 ) ) ;
#3023=ORIENTED_EDGE ( 'NONE', *, *, #31311, .T. ) ;
#3027=CARTESIAN_POINT ( 'NONE',  ( 53.55386411653459788, -49.42051784504710099, -49.22808815827509932 ) ) ;
#3028=LINE ( 'NONE', #46551, #19304 ) ;
#3029=EDGE_LOOP ( 'NONE', ( #40475, #35569 ) ) ;
#3037=CARTESIAN_POINT ( 'NONE',  ( 52.14830239089789643, -51.14206852341889942, -76.06502807251010267 ) ) ;
#3038=CARTESIAN_POINT ( 'NONE',  ( 60.69566241836140819, 14.32434429444830037, -47.28745234666029518 ) ) ;
#3042=B_SPLINE_CURVE_WITH_KNOTS ( 'NONE', 3,
 ( #13509, #17175, #33906, #29464 ),
 .UNSPECIFIED., .F., .F.,
 ( 4, 4 ),
 ( 6.761997042909579925, 6.813952014709780514 ),
 .UNSPECIFIED. ) ;
#3043=CARTESIAN_POINT ( 'NONE',  ( 42.11778985043759604, -43.34518763914169881, -3.278435071288769542 ) ) ;
#3044=PLANE ( 'NONE',  #41262 ) ;
#3045=CARTESIAN_POINT ( 'NONE',  ( -6.129785861383029832, 15.32157675170519973, -5.280748218974210317 ) ) ;
#3048=FACE_OUTER_BOUND ( 'NONE', #4439, .T. ) ;
#3051=ORIENTED_EDGE ( 'NONE', *, *, #5133, .T. ) ;
#3053=CARTESIAN_POINT ( 'NONE',  ( 61.29923170577789904, 16.44081181233369904, -45.87705507641510394 ) ) ;
#3054=CARTESIAN_POINT ( 'NONE',  ( 57.43212237869229853, 18.98854805440929994, -52.72827966158989454 ) ) ;
#3057=CARTESIAN_POINT ( 'NONE',  ( 15.94236692260559884, 19.75473188654670054, -20.14988694616360121 ) ) ;
#3058=DIRECTION ( 'NONE',  ( 0.4646601886423053496, 0.000000000000000000, 0.8854890790353641128 ) ) ;
#3061=CARTESIAN_POINT ( 'NONE',  ( 47.91340349060840254, -54.37608934015739948, -54.84711144667770810 ) ) ;
#3063=AXIS2_PLACEMENT_3D ( 'NONE', #5647, #49672, #10086 ) ;
#3065=CARTESIAN_POINT ( 'NONE',  ( 56.41630124387919665, 19.34388386770270074, -52.96295731896090331 ) ) ;
#3067=CARTESIAN_POINT ( 'NONE',  ( 47.75515754607199881, 23.22926032546549990, -54.87660553739110014 ) ) ;
#3071=EDGE_CURVE ( 'NONE', #1664, #31547, #152, .T. ) ;
#3072=VERTEX_POINT ( 'NONE', #32289 ) ;
#3074=CARTESIAN_POINT ( 'NONE',  ( 13.00893739769619906, 34.28605925116850273, -47.75434321204170374 ) ) ;
#3076=CARTESIAN_POINT ( 'NONE',  ( 48.73678662100336823, -53.88539940205524914, -54.49010856789386281 ) ) ;
#3077=CARTESIAN_POINT ( 'NONE',  ( 53.29384558423090112, 19.31433099946569953, -28.15000000000000213 ) ) ;
#3080=DIRECTION ( 'NONE',  ( -0.08481436951012806535, 0.9963967697281035374, 0.000000000000000000 ) ) ;
#3083=DIRECTION ( 'NONE',  ( 0.000000000000000000, -1.000000000000000000, 0.000000000000000000 ) ) ;
#3084=ORIENTED_EDGE ( 'NONE', *, *, #11613, .T. ) ;
#3087=ORIENTED_EDGE ( 'NONE', *, *, #20357, .F. ) ;
#3088=DIRECTION ( 'NONE',  ( -0.04251717301921301151, 0.000000000000000000, 0.9990957361526743297 ) ) ;
#3091=CARTESIAN_POINT ( 'NONE',  ( 11.15267625120379869, -65.14072497951910634, -47.20537807037530342 ) ) ;
#3093=EDGE_CURVE ( 'NONE', #20898, #15133, #12365, .T. ) ;
#3094=ORIENTED_EDGE ( 'NONE', *, *, #49692, .F. ) ;
#3095=ORIENTED_EDGE ( 'NONE', *, *, #32922, .F. ) ;
#3096=CARTESIAN_POINT ( 'NONE',  ( 53.70964822437330355, 20.71768139653399743, -54.24308104583559498 ) ) ;
#3097=VECTOR ( 'NONE', #18125, 1000.000000000000000 ) ;
#3101=CARTESIAN_POINT ( 'NONE',  ( 64.80898460781330073, -0.3417096974386910624, -16.69305045354919770 ) ) ;
#3103=CARTESIAN_POINT ( 'NONE',  ( 51.64973235580259825, -49.25056687465429661, -76.82386385094510217 ) ) ;
#3110=CARTESIAN_POINT ( 'NONE',  ( 13.17520392672940055, -50.89446949932710851, -21.60492300268700205 ) ) ;
#3111=CARTESIAN_POINT ( 'NONE',  ( 56.07939589478549891, 19.38381105532069881, -75.94606253248319661 ) ) ;
#3112=FACE_OUTER_BOUND ( 'NONE', #29817, .T. ) ;
#3113=CARTESIAN_POINT ( 'NONE',  ( 56.76189318125270233, 13.89673976699089941, -16.10745061695219960 ) ) ;
#3120=CARTESIAN_POINT ( 'NONE',  ( 14.33439054234879961, -51.26614876192449799, -74.93568190819630104 ) ) ;
#3123=CARTESIAN_POINT ( 'NONE',  ( 17.71568183981793609, 20.46959823935371503, -75.56421430877649925 ) ) ;
#3125=AXIS2_PLACEMENT_3D ( 'NONE', #49091, #44619, #21274 ) ;
#3126=DIRECTION ( 'NONE',  ( -1.000000000000000000, -9.178581432917707304E-26, 1.529205156547310004E-10 ) ) ;
#3127=CARTESIAN_POINT ( 'NONE',  ( 82.37381124112360453, 13.88258767056099963, -46.56085682599739783 ) ) ;
#3129=CARTESIAN_POINT ( 'NONE',  ( 47.64143405046823432, 23.30250931194617436, -74.17387245449363320 ) ) ;
#3133=CARTESIAN_POINT ( 'NONE',  ( 68.13393739769620083, -15.61618894467929941, -65.65000000000000568 ) ) ;
#3134=ORIENTED_EDGE ( 'NONE', *, *, #31521, .T. ) ;
#3136=CARTESIAN_POINT ( 'NONE',  ( 52.93745306185230248, -49.61473117453819981, -48.89566031930959866 ) ) ;
#3140=CARTESIAN_POINT ( 'NONE',  ( 14.05648281248510045, 19.92572429859249894, -22.83284005205619849 ) ) ;
#3141=CARTESIAN_POINT ( 'NONE',  ( 51.99247890846820042, -49.49757107862999561, -77.11022715351130330 ) ) ;
#3143=CARTESIAN_POINT ( 'NONE',  ( 53.15617284440619983, 18.31170051411429966, -49.11047172704059705 ) ) ;
#3145=CARTESIAN_POINT ( 'NONE',  ( 54.56504510741340397, -45.97009618579260604, -15.64073160589219924 ) ) ;
#3149=EDGE_LOOP ( 'NONE', ( #47032, #20928, #29403, #20478, #18997, #6953, #32467, #41663 ) ) ;
#3150=CARTESIAN_POINT ( 'NONE',  ( 53.59007319875249920, 18.17385789302069554, -49.22505640236219904 ) ) ;
#3151=CARTESIAN_POINT ( 'NONE',  ( 11.74846882065989995, 34.09090366579489739, -47.38045816806030075 ) ) ;
#3153=CARTESIAN_POINT ( 'NONE',  ( 49.98909701452470244, -52.82152540991150147, -53.22897615407840277 ) ) ;
#3154=DIRECTION ( 'NONE',  ( 1.000000000000000000, 0.000000000000000000, 0.000000000000000000 ) ) ;
#3156=CARTESIAN_POINT ( 'NONE',  ( 52.62939598134340002, -52.19035112265739684, -53.52988853690619919 ) ) ;
#3158=PLANE ( 'NONE',  #13451 ) ;
#3159=CARTESIAN_POINT ( 'NONE',  ( 10.77213108896340010, -63.27130156652651038, -45.20475918482989641 ) ) ;
#3160=CARTESIAN_POINT ( 'NONE',  ( 69.22748654599826068, 19.47158195952208004, -70.40645085170191919 ) ) ;
#3161=ORIENTED_EDGE ( 'NONE', *, *, #11523, .F. ) ;
#3163=DIRECTION ( 'NONE',  ( 1.000000000000000000, 0.000000000000000000, 0.000000000000000000 ) ) ;
#3164=CARTESIAN_POINT ( 'NONE',  ( 53.36305338436599754, 19.31849222244400011, -76.89765214543919569 ) ) ;
#3166=DIRECTION ( 'NONE',  ( 0.000000000000000000, 0.000000000000000000, 1.000000000000000000 ) ) ;
#3167=CARTESIAN_POINT ( 'NONE',  ( 51.19516202202958510, 19.86383965925710626, -76.13919812682924260 ) ) ;
#3170=CARTESIAN_POINT ( 'NONE',  ( 32.63393739769630031, -15.61618894467929941, -6.649999999999999467 ) ) ;
#3173=DIRECTION ( 'NONE',  ( -0.000000000000000000, -1.000000000000000000, -0.000000000000000000 ) ) ;
#3174=AXIS2_PLACEMENT_3D ( 'NONE', #21807, #1647, #5591 ) ;
#3176=ORIENTED_EDGE ( 'NONE', *, *, #46926, .T. ) ;
#3180=CARTESIAN_POINT ( 'NONE',  ( 50.04794199436929603, 13.88381105532070059, -10.32001505388980078 ) ) ;
#3182=EDGE_CURVE ( 'NONE', #2875, #11745, #13280, .T. ) ;
#3183=CARTESIAN_POINT ( 'NONE',  ( 56.61928439928508539, 14.09173447728649720, -31.98003398807230369 ) ) ;
#3185=EDGE_CURVE ( 'NONE', #30141, #12739, #17382, .T. ) ;
#3186=FACE_OUTER_BOUND ( 'NONE', #42684, .T. ) ;
#3187=CARTESIAN_POINT ( 'NONE',  ( 11.80495200725580140, 33.73638531772620297, -16.40176568414450031 ) ) ;
#3190=CARTESIAN_POINT ( 'NONE',  ( 55.10512401493469525, -51.00770816830609533, -75.23756392707410612 ) ) ;
#3191=CARTESIAN_POINT ( 'NONE',  ( -1.714040913996900173, 19.72568320566199773, -6.699893841482610135 ) ) ;
#3194=DIRECTION ( 'NONE',  ( -1.000000000000000000, 0.000000000000000000, 0.000000000000000000 ) ) ;
#3196=CARTESIAN_POINT ( 'NONE',  ( -10.89209614968750017, -42.33678087173180415, -6.195842417017019876 ) ) ;
#3197=CARTESIAN_POINT ( 'NONE',  ( 47.67808432772210381, 23.28069921495480088, -55.00342241055910364 ) ) ;
#3198=AXIS2_PLACEMENT_3D ( 'NONE', #34860, #2381, #45902 ) ;
#3200=DIRECTION ( 'NONE',  ( 0.000000000000000000, 0.000000000000000000, -1.000000000000000000 ) ) ;
#3201=CARTESIAN_POINT ( 'NONE',  ( 61.20223082393160041, 14.41488311889550111, -47.73662807001939967 ) ) ;
#3203=CARTESIAN_POINT ( 'NONE',  ( 51.69077939775340269, 18.09910883672219839, -76.83272513777849611 ) ) ;
#3204=CARTESIAN_POINT ( 'NONE',  ( 52.83011278983949666, 18.42835579809699809, -48.49876830664469907 ) ) ;
#3207=CARTESIAN_POINT ( 'NONE',  ( 53.36494266454960211, -49.38052133118390685, -48.76947209987829979 ) ) ;
#3208=CARTESIAN_POINT ( 'NONE',  ( 52.77133031265780261, 18.46082998801760056, -28.15002739903220075 ) ) ;
#3210=CARTESIAN_POINT ( 'NONE',  ( 10.98008937475129976, -63.44096224164839981, -44.74889856825390666 ) ) ;
#3211=CARTESIAN_POINT ( 'NONE',  ( 52.57435089425080577, 18.62009177781090230, -48.51307714252150305 ) ) ;
#3212=CARTESIAN_POINT ( 'NONE',  ( 59.91580961932370286, -29.59054676811280160, -15.87157813189650213 ) ) ;
#3214=CARTESIAN_POINT ( 'NONE',  ( 11.13393739769619906, 32.12568940449459376, -43.74939087321740061 ) ) ;
#3216=CARTESIAN_POINT ( 'NONE',  ( 51.35985510312087143, -34.56615178299539082, -76.65611151696774073 ) ) ;
#3217=CARTESIAN_POINT ( 'NONE',  ( 65.03603135424570780, -29.76883965895069650, -19.52361391316379979 ) ) ;
#3218=ORIENTED_EDGE ( 'NONE', *, *, #42829, .T. ) ;
#3220=DIRECTION ( 'NONE',  ( 0.000000000000000000, 1.000000000000000000, 0.000000000000000000 ) ) ;
#3221=CARTESIAN_POINT ( 'NONE',  ( 51.12546901458399162, 0.3428415324802153163, -17.03913216448443180 ) ) ;
#3223=CARTESIAN_POINT ( 'NONE',  ( 57.55914395453869759, -45.13105435620409622, -25.54764931287219909 ) ) ;
#3229=CARTESIAN_POINT ( 'NONE',  ( 11.37709144110930026, 32.70230954837069959, -24.34844091950509792 ) ) ;
#3232=CARTESIAN_POINT ( 'NONE',  ( 51.21170306502393998, 0.4771360739093502001, -17.17315678632984799 ) ) ;
#3233=CARTESIAN_POINT ( 'NONE',  ( 10.62399636376403222, 33.60002598301907994, -18.14935807941716561 ) ) ;
#3235=CARTESIAN_POINT ( 'NONE',  ( 61.83357513733750466, -29.34433711196260219, -16.03557146812989842 ) ) ;
#3236=B_SPLINE_CURVE_WITH_KNOTS ( 'NONE', 3,
 ( #15853, #24459, #36270, #4310, #44408, #21061, #12184, #47833, #36528, #4564, #31812, #634, #48864, #16620, #380, #32574, #24975, #130 ),
 .UNSPECIFIED., .F., .F.,
 ( 4, 2, 1, 1, 2, 2, 2, 1, 1, 2, 4 ),
 ( 0.5114743812812451162, 0.5267408068662060572, 0.5420072324511669981, 0.5725400836210982058, 0.6336057859609515175, 0.7557371906406565865, 0.7710036162256185266, 0.7862700418105804667, 0.8168028929804922456, 0.8778685953203280157, 1.000000000000000000 ),
 .UNSPECIFIED. ) ;
#3237=CARTESIAN_POINT ( 'NONE',  ( 14.48179410283199431, 20.27135663923558084, -75.33783710295330138 ) ) ;
#3238=CARTESIAN_POINT ( 'NONE',  ( 46.56684587109570117, -53.31662439353189598, -76.10144452841760199 ) ) ;
#3239=CARTESIAN_POINT ( 'NONE',  ( 83.89200044194980421, 17.38381105532069881, -53.92796738110899923 ) ) ;
#3244=ADVANCED_FACE ( 'NONE', ( #45675 ), #33706, .T. ) ;
#3245=CARTESIAN_POINT ( 'NONE',  ( 83.96875769672529088, -44.33360226143160787, -47.04741150093960300 ) ) ;
#3248=ORIENTED_EDGE ( 'NONE', *, *, #42965, .T. ) ;
#3249=CARTESIAN_POINT ( 'NONE',  ( 52.95491184103799753, -49.55317193531470110, -27.75869128885100068 ) ) ;
#3250=CARTESIAN_POINT ( 'NONE',  ( 7.377761082898449452, -59.78252037510630856, -11.86817158160470065 ) ) ;
#3251=CARTESIAN_POINT ( 'NONE',  ( 75.83364580603620198, 0.5632187979614480255, -12.28588720292489889 ) ) ;
#3252=CARTESIAN_POINT ( 'NONE',  ( 75.32649906090206571, 13.28935024932845543, -13.93656188709756272 ) ) ;
#3254=FACE_OUTER_BOUND ( 'NONE', #19514, .T. ) ;
#3256=CARTESIAN_POINT ( 'NONE',  ( 82.13853704237929776, -45.43815991012449729, -47.46441090728419709 ) ) ;
#3257=CARTESIAN_POINT ( 'NONE',  ( 57.29916422955370336, -50.56256534964890648, -53.44854448085349929 ) ) ;
#3258=CARTESIAN_POINT ( 'NONE',  ( 41.72814282206219616, 12.57486269224770048, -4.012820143008159590 ) ) ;
#3262=CARTESIAN_POINT ( 'NONE',  ( 53.48663704675579567, -49.34136594389470076, -49.00013169077909936 ) ) ;
#3265=CARTESIAN_POINT ( 'NONE',  ( 17.68198299984170063, -51.79680004542600358, -75.65449215554859563 ) ) ;
#3267=CARTESIAN_POINT ( 'NONE',  ( 43.34846246081870191, -44.39964076787359915, -5.297725289369729751 ) ) ;
#3272=CYLINDRICAL_SURFACE ( 'NONE', #30970, 3.500000000000003109 ) ;
#3278=CARTESIAN_POINT ( 'NONE',  ( 41.02380400077039724, -45.31415305091180556, -5.860748674566660377 ) ) ;
#3280=CARTESIAN_POINT ( 'NONE',  ( 17.51665066424190087, 21.64019965034970028, -76.12465403027070465 ) ) ;
#3281=VERTEX_POINT ( 'NONE', #26189 ) ;
#3287=VERTEX_POINT ( 'NONE', #45876 ) ;
#3293=CARTESIAN_POINT ( 'NONE',  ( 51.19067522064119657, -50.75340530090790025, -76.16618595621679333 ) ) ;
#3294=CARTESIAN_POINT ( 'NONE',  ( 61.13208011586430501, 14.28537189261369988, -47.54663226922669850 ) ) ;
#3298=CARTESIAN_POINT ( 'NONE',  ( -7.972635851128819340, 13.79869975764560053, -5.396154554284530391 ) ) ;
#3299=AXIS2_PLACEMENT_3D ( 'NONE', #36928, #12572, #758 ) ;
#3300=TOROIDAL_SURFACE ( 'NONE', #47640, 36.00000000000000000, 2.000000000000000000 ) ;
#3304=CIRCLE ( 'NONE', #16693, 39.39359268544610870 ) ;
#3306=ORIENTED_EDGE ( 'NONE', *, *, #34954, .T. ) ;
#3308=FACE_OUTER_BOUND ( 'NONE', #3812, .T. ) ;
#3313=DIRECTION ( 'NONE',  ( -1.000000000000000000, 0.000000000000000000, 0.000000000000000000 ) ) ;
#3315=FACE_OUTER_BOUND ( 'NONE', #12503, .T. ) ;
#3318=CARTESIAN_POINT ( 'NONE',  ( 48.49374681402279919, -54.15253515020039998, -55.04500232426880046 ) ) ;
#3321=ADVANCED_FACE ( 'NONE', ( #22256 ), #38263, .F. ) ;
#3322=CARTESIAN_POINT ( 'NONE',  ( 47.64964229006460528, 23.29901286050539966, -55.13082436213569792 ) ) ;
#3323=ORIENTED_EDGE ( 'NONE', *, *, #7860, .F. ) ;
#3325=B_SPLINE_CURVE_WITH_KNOTS ( 'NONE', 3,
 ( #4241, #32248, #20463, #560, #16545, #5547, #36986, #49827, #9980, #13918, #21240, #29874, #41689, #41180, #41431, #17841 ),
 .UNSPECIFIED., .F., .F.,
 ( 4, 2, 2, 2, 2, 2, 2, 4 ),
 ( -8.881783999999999608E-16, 0.4504854996693090086, 0.8526915253703870601, 1.105340866220869911, 1.263246704252430019, 1.579058380315530030, 2.084357062016500173, 2.526493408504850269 ),
 .UNSPECIFIED. ) ;
#3329=CARTESIAN_POINT ( 'NONE',  ( 61.28610897262619517, 13.99802247707942549, -27.88820104294108049 ) ) ;
#3330=CARTESIAN_POINT ( 'NONE',  ( 82.45630311851421368, 13.86034003618500066, -46.38988467804559690 ) ) ;
#3331=CARTESIAN_POINT ( 'NONE',  ( 83.85375176557759858, 13.60279395407959946, -47.43402238021350570 ) ) ;
#3335=CARTESIAN_POINT ( 'NONE',  ( 13.00893739761190027, 34.28605925116320208, -47.75434321210310173 ) ) ;
#3336=ORIENTED_EDGE ( 'NONE', *, *, #76, .F. ) ;
#3337=CARTESIAN_POINT ( 'NONE',  ( 84.44421879469800274, -43.32357668338529777, -47.46023938497990002 ) ) ;
#3338=ORIENTED_EDGE ( 'NONE', *, *, #27033, .F. ) ;
#3345=CARTESIAN_POINT ( 'NONE',  ( 76.47407931131914438, -26.68129154492521593, -13.11572213019135269 ) ) ;
#3346=CARTESIAN_POINT ( 'NONE',  ( 10.80326701815859991, -65.00358748232589789, -47.10395893127729749 ) ) ;
#3347=AXIS2_PLACEMENT_3D ( 'NONE', #9560, #14261, #37581 ) ;
#3348=EDGE_LOOP ( 'NONE', ( #26588, #12846, #38879, #28504, #5324, #24502, #22940, #36585, #42126 ) ) ;
#3352=CARTESIAN_POINT ( 'NONE',  ( 56.97449864924389829, -45.18768938411730574, -25.30071454757920435 ) ) ;
#3353=CARTESIAN_POINT ( 'NONE',  ( 56.45679588454890308, -50.65543487096700659, -53.17273421675590583 ) ) ;
#3356=CARTESIAN_POINT ( 'NONE',  ( 61.22840165282480029, -0.4342326450878930544, -16.42153289494959978 ) ) ;
#3357=CARTESIAN_POINT ( 'NONE',  ( 52.21414320235400197, -49.80349422312119856, -77.10081889737340077 ) ) ;
#3358=CARTESIAN_POINT ( 'NONE',  ( 14.46582891625718048, -52.64324137128869552, -76.02665054608532103 ) ) ;
#3359=VERTEX_POINT ( 'NONE', #23974 ) ;
#3361=FACE_OUTER_BOUND ( 'NONE', #4018, .T. ) ;
#3363=CARTESIAN_POINT ( 'NONE',  ( 53.59003930803689997, -49.40628012469949937, -49.22510501142529904 ) ) ;
#3365=CARTESIAN_POINT ( 'NONE',  ( 13.50258242280349918, -50.13280576151589685, -20.96779971433539913 ) ) ;
#3368=CARTESIAN_POINT ( 'NONE',  ( 56.63655303576899769, 13.89710862042509909, -15.89230735191339861 ) ) ;
#3369=CARTESIAN_POINT ( 'NONE',  ( 61.06130050885990102, -45.43944728382009401, -47.36071542247660204 ) ) ;
#3371=ADVANCED_FACE ( 'NONE', ( #23725 ), #26599, .T. ) ;
#3377=CARTESIAN_POINT ( 'NONE',  ( 14.28772440699220070, -51.14708712906860200, -74.55381114264599773 ) ) ;
#3379=CIRCLE ( 'NONE', #36019, 1.000000000000000888 ) ;
#3380=CARTESIAN_POINT ( 'NONE',  ( 41.58940156010519473, -45.68696317153209918, -6.490026235633630236 ) ) ;
#3382=CIRCLE ( 'NONE', #21765, 3.000000000000001776 ) ;
#3385=EDGE_CURVE ( 'NONE', #15485, #43570, #11557, .T. ) ;
#3387=CARTESIAN_POINT ( 'NONE',  ( 46.87137491217979601, -53.55967532393449915, -75.98463753095340678 ) ) ;
#3389=CARTESIAN_POINT ( 'NONE',  ( 82.55523265057320259, 14.39697247100306043, -47.70981245347169875 ) ) ;
#3391=CARTESIAN_POINT ( 'NONE',  ( 51.67587649748560352, -48.61618894467930119, -77.01363636363639387 ) ) ;
#3394=EDGE_CURVE ( 'NONE', #12214, #19324, #646, .T. ) ;
#3395=CARTESIAN_POINT ( 'NONE',  ( 49.18437675156140187, 22.63228536849929995, -55.01176516154440321 ) ) ;
#3396=ORIENTED_EDGE ( 'NONE', *, *, #43459, .T. ) ;
#3397=CARTESIAN_POINT ( 'NONE',  ( 53.46717762220459491, -49.39950009416709520, -49.11454733997430111 ) ) ;
#3401=CARTESIAN_POINT ( 'NONE',  ( 13.90975851214690096, 19.95031597149180058, -22.51682738170260123 ) ) ;
#3402=FACE_OUTER_BOUND ( 'NONE', #33535, .T. ) ;
#3404=CARTESIAN_POINT ( 'NONE',  ( 52.97994248284770435, 18.38655893702810218, -49.03242408102300232 ) ) ;
#3405=CARTESIAN_POINT ( 'NONE',  ( 55.89887109364280349, -45.90872632089149619, -17.63256066653320175 ) ) ;
#3406=CARTESIAN_POINT ( 'NONE',  ( 83.89200044194980421, -50.48013859002959691, -53.20292136905285929 ) ) ;
#3407=VERTEX_POINT ( 'NONE', #19559 ) ;
#3410=CARTESIAN_POINT ( 'NONE',  ( 11.25424580253960016, -65.03526282482160070, -16.95782958517590089 ) ) ;
#3411=CARTESIAN_POINT ( 'NONE',  ( 12.48759467934699963, 34.23991394352330531, -47.62022110721400026 ) ) ;
#3413=CARTESIAN_POINT ( 'NONE',  ( 52.21171052997630113, -50.80767995673200232, -50.87743900096490535 ) ) ;
#3414=CARTESIAN_POINT ( 'NONE',  ( 52.97667589433369528, -49.63212252085852327, -49.06651684377276723 ) ) ;
#3416=EDGE_CURVE ( 'NONE', #9581, #17232, #26702, .T. ) ;
#3418=CARTESIAN_POINT ( 'NONE',  ( -15.86606260230380094, -15.61618894467929941, -20.15000000000000213 ) ) ;
#3419=CARTESIAN_POINT ( 'NONE',  ( 10.49497832658790131, -63.36864664907449196, -45.62743361653370044 ) ) ;
#3420=LINE ( 'NONE', #35372, #25198 ) ;
#3421=VERTEX_POINT ( 'NONE', #16138 ) ;
#3422=CARTESIAN_POINT ( 'NONE',  ( 67.45368031047163981, -32.84183613245724587, -19.55784004926478303 ) ) ;
#3423=CARTESIAN_POINT ( 'NONE',  ( 56.41694091142689871, 19.34565818385159730, -52.96189704198110348 ) ) ;
#3425=VERTEX_POINT ( 'NONE', #35549 ) ;
#3427=CARTESIAN_POINT ( 'NONE',  ( 51.42797782268906559, 19.97168430531649719, -76.10787250224279887 ) ) ;
#3428=CARTESIAN_POINT ( 'NONE',  ( 82.45630311851421368, -45.09271792554360303, -46.38988467804559690 ) ) ;
#3430=CIRCLE ( 'NONE', #17636, 3.500000000000003109 ) ;
#3432=PLANE ( 'NONE',  #48129 ) ;
#3433=CARTESIAN_POINT ( 'NONE',  ( 61.04001029137710077, -45.35933836075930259, -46.86320535112459851 ) ) ;
#3436=ORIENTED_EDGE ( 'NONE', *, *, #6939, .T. ) ;
#3438=DIRECTION ( 'NONE',  ( -0.4316160343590931259, -0.9020574254913764634, 0.000000000000000000 ) ) ;
#3440=CARTESIAN_POINT ( 'NONE',  ( 53.41947877929930399, -49.46401953720199884, -49.21225703112880012 ) ) ;
#3441=CARTESIAN_POINT ( 'NONE',  ( 50.39461351434339775, -50.13496434787850120, -76.14999999999999147 ) ) ;
#3444=CARTESIAN_POINT ( 'NONE',  ( 47.20691373745980002, 23.45218668536150020, -74.72489560329549363 ) ) ;
#3445=DIRECTION ( 'NONE',  ( -0.5779418439120764805, 0.8120748150972384449, -0.08073239585380144467 ) ) ;
#3446=DIRECTION ( 'NONE',  ( -0.5110015285683607855, -0.4887508954475661693, -0.7071067811865481278 ) ) ;
#3447=CARTESIAN_POINT ( 'NONE',  ( 12.21465728044820054, 33.46871344512319979, -15.93455456221940025 ) ) ;
#3450=CARTESIAN_POINT ( 'NONE',  ( 55.74676111446309790, -50.61618894632059806, -76.24128155003170093 ) ) ;
#3451=CARTESIAN_POINT ( 'NONE',  ( -9.494487167629941382, 12.56563882403370158, -6.502785074734050319 ) ) ;
#3454=ADVANCED_FACE ( 'NONE', ( #35495, #20003 ), #19761, .T. ) ;
#3455=LINE ( 'NONE', #35677, #7197 ) ;
#3457=CIRCLE ( 'NONE', #9331, 1.999999999999996669 ) ;
#3458=CARTESIAN_POINT ( 'NONE',  ( -9.120882960642459736, -44.01580188134359872, -5.427931969706110138 ) ) ;
#3459=TOROIDAL_SURFACE ( 'NONE', #13496, 2.999999897106000013, 1.999999999830609942 ) ;
#3460=CARTESIAN_POINT ( 'NONE',  ( 47.74455983969129846, 23.22759274665880014, -54.83598561554559581 ) ) ;
#3463=CARTESIAN_POINT ( 'NONE',  ( 61.31447405025300412, 14.34038816827110097, -47.65179949294859796 ) ) ;
#3465=CARTESIAN_POINT ( 'NONE',  ( 52.21413925781470056, 18.57111292375499900, -77.10081778803849772 ) ) ;
#3466=CARTESIAN_POINT ( 'NONE',  ( 53.18571383884999904, 18.24204644525839925, -48.81732522206360159 ) ) ;
#3469=CARTESIAN_POINT ( 'NONE',  ( 51.00410689780089513, 21.58760788935499875, -53.76372497442359588 ) ) ;
#3473=CARTESIAN_POINT ( 'NONE',  ( 59.04235398677249691, -28.10938722064719641, -15.65226459872759790 ) ) ;
#3481=ADVANCED_FACE ( 'NONE', ( #51485 ), #16102, .T. ) ;
#3486=CARTESIAN_POINT ( 'NONE',  ( 57.38200685792909894, -45.11824297016489993, -25.39251393572369864 ) ) ;
#3491=CARTESIAN_POINT ( 'NONE',  ( 10.64863409883700029, 32.21085600226960111, -23.66469670114080159 ) ) ;
#3493=CARTESIAN_POINT ( 'NONE',  ( 12.34051464139020027, 34.21035364286279901, -23.27951631307980307 ) ) ;
#3494=VERTEX_POINT ( 'NONE', #44129 ) ;
#3497=CARTESIAN_POINT ( 'NONE',  ( 65.46029542295769943, -1.463538230407920082, -16.55376543218019947 ) ) ;
#3498=CARTESIAN_POINT ( 'NONE',  ( 59.44268701500750041, -28.43641637611329998, -15.69409845278869930 ) ) ;
#3499=EDGE_CURVE ( 'NONE', #33091, #3494, #5082, .T. ) ;
#3502=CARTESIAN_POINT ( 'NONE',  ( 46.35275103504449845, -52.90993241930539881, -76.14999999999999147 ) ) ;
#3506=CARTESIAN_POINT ( 'NONE',  ( 40.78718667651179430, 13.97481543807150040, -5.637855851295809906 ) ) ;
#3507=EDGE_CURVE ( 'NONE', #35613, #9275, #29894, .T. ) ;
#3508=CARTESIAN_POINT ( 'NONE',  ( 10.25785795057082872, 23.94995057986916365, -45.86872051532979100 ) ) ;
#3509=CARTESIAN_POINT ( 'NONE',  ( 84.38271246941039294, -43.47090129257950508, -47.29654027836490116 ) ) ;
#3513=CARTESIAN_POINT ( 'NONE',  ( 53.31766142530319996, -49.23794969896809448, -27.39069684441169983 ) ) ;
#3514=CARTESIAN_POINT ( 'NONE',  ( 14.22165922049939901, -50.54429837671820280, -21.01402899346189912 ) ) ;
#3515=CARTESIAN_POINT ( 'NONE',  ( 75.31916300594728853, -5.906200963950169580, -11.62634963242759945 ) ) ;
#3516=CARTESIAN_POINT ( 'NONE',  ( 75.41772322313477162, 12.83423812364906169, -13.62006770663721689 ) ) ;
#3521=CARTESIAN_POINT ( 'NONE',  ( 82.13853704237929776, -45.17484520962380401, -46.86219204859769860 ) ) ;
#3522=CARTESIAN_POINT ( 'NONE',  ( 57.34721623897170417, -50.32126388940520201, -52.87018747239729777 ) ) ;
#3523=CARTESIAN_POINT ( 'NONE',  ( 42.16203278445299674, 12.96059013387869818, -4.955231385700390234 ) ) ;
#3525=CYLINDRICAL_SURFACE ( 'NONE', #20727, 14.50000000000000178 ) ;
#3526=CARTESIAN_POINT ( 'NONE',  ( 53.82714908703680123, -49.13835843630199918, -48.71552173647079798 ) ) ;
#3529=CARTESIAN_POINT ( 'NONE',  ( 17.82691427187729971, -51.53888401296669741, -75.38689171750549178 ) ) ;
#3530=CARTESIAN_POINT ( 'NONE',  ( 43.19159875137410154, -44.97844352163669868, -6.001981098335629206 ) ) ;
#3533=DIRECTION ( 'NONE',  ( 0.000000000000000000, 0.000000000000000000, -1.000000000000000000 ) ) ;
#3535=ORIENTED_EDGE ( 'NONE', *, *, #13510, .T. ) ;
#3538=SPHERICAL_SURFACE ( 'NONE', #19274, 2.000000000000000000 ) ;
#3543=FACE_OUTER_BOUND ( 'NONE', #47129, .T. ) ;
#3547=PLANE ( 'NONE',  #36927 ) ;
#3550=CARTESIAN_POINT ( 'NONE',  ( 61.53725015800320364, 14.07761012407289947, -47.23307395042449741 ) ) ;
#3551=ORIENTED_EDGE ( 'NONE', *, *, #2309, .F. ) ;
#3553=ORIENTED_EDGE ( 'NONE', *, *, #50879, .T. ) ;
#3554=CARTESIAN_POINT ( 'NONE',  ( 82.55417034916375485, 14.39382471871442881, -47.70637854188409221 ) ) ;
#3555=CYLINDRICAL_SURFACE ( 'NONE', #36846, 1.000000000000000888 ) ;
#3556=ORIENTED_EDGE ( 'NONE', *, *, #15841, .F. ) ;
#3558=CARTESIAN_POINT ( 'NONE',  ( 51.18087450742270050, -50.74724387720399932, -76.16568686308029612 ) ) ;
#3559=CARTESIAN_POINT ( 'NONE',  ( 60.28868092514770893, 14.57684442129959912, -47.55394404419389787 ) ) ;
#3560=ADVANCED_FACE ( 'NONE', ( #4542, #36508 ), #48584, .T. ) ;
#3564=CARTESIAN_POINT ( 'NONE',  ( -2.836119465579209908, 17.80585329168859943, -5.545754995944120580 ) ) ;
#3566=B_SPLINE_CURVE_WITH_KNOTS ( 'NONE', 3,
 ( #9262, #17882, #29149, #45415, #28889, #5329, #49867, #17633, #44892, #25210 ),
 .UNSPECIFIED., .F., .F.,
 ( 4, 2, 2, 2, 4 ),
 ( 0.000000000000000000, 0.03537882351746304832, 0.3488581273460797383, 0.9706547651737063021, 1.000000000000000000 ),
 .UNSPECIFIED. ) ;
#3568=CIRCLE ( 'NONE', #27789, 2.000000000000060396 ) ;
#3570=CARTESIAN_POINT ( 'NONE',  ( -33.86606260230380627, -15.61618894467930474, -74.14999999999999147 ) ) ;
#3572=ORIENTED_EDGE ( 'NONE', *, *, #2480, .F. ) ;
#3573=DIRECTION ( 'NONE',  ( 0.8732394366197182567, 0.4872913772396111343, 1.665334536937735304E-16 ) ) ;
#3574=CARTESIAN_POINT ( 'NONE',  ( 57.46463958512929793, 19.38381105532060289, -53.92796738110899923 ) ) ;
#3577=CARTESIAN_POINT ( 'NONE',  ( 14.89545651469759946, 19.58260512638929640, -21.03875510983240105 ) ) ;
#3581=CARTESIAN_POINT ( 'NONE',  ( 48.44792705533350130, -54.06183843665910160, -54.63497078953220409 ) ) ;
#3582=CYLINDRICAL_SURFACE ( 'NONE', #37346, 1.999999999999995559 ) ;
#3584=CARTESIAN_POINT ( 'NONE',  ( 47.82967227365460161, 23.17104661939929855, -54.77576043164239650 ) ) ;
#3587=DIRECTION ( 'NONE',  ( -0.7782863420137342558, 0.3536342755907660451, 0.5188575613424891708 ) ) ;
#3590=CARTESIAN_POINT ( 'NONE',  ( 60.94474915215729993, -45.41359427234949919, -47.07753893340869666 ) ) ;
#3592=DIRECTION ( 'NONE',  ( 0.000000000000000000, 0.000000000000000000, -1.000000000000000000 ) ) ;
#3593=CARTESIAN_POINT ( 'NONE',  ( 84.32823919854369876, 12.72937383798579880, -47.43652016892809797 ) ) ;
#3595=DIRECTION ( 'NONE',  ( 0.000000000000000000, -8.635067969306036542E-13, -1.000000000000000000 ) ) ;
#3596=CARTESIAN_POINT ( 'NONE',  ( 56.72051766553079943, 19.45439143119499903, -53.84018978621899976 ) ) ;
#3602=CARTESIAN_POINT ( 'NONE',  ( 61.13393739769620083, -33.11618894467940066, -84.38499399519520239 ) ) ;
#3604=CIRCLE ( 'NONE', #29537, 18.50000000000000000 ) ;
#3605=CARTESIAN_POINT ( 'NONE',  ( 76.42354666252261097, -22.55147712810201810, -12.89797355987789018 ) ) ;
#3606=CARTESIAN_POINT ( 'NONE',  ( 9.496404720408110123, -64.31007826197829047, -46.84592557732370466 ) ) ;
#3607=VECTOR ( 'NONE', #5631, 1000.000000000000114 ) ;
#3610=DIRECTION ( 'NONE',  ( 1.000000000000000000, 0.000000000000000000, 0.000000000000000000 ) ) ;
#3612=DIRECTION ( 'NONE',  ( 0.000000000000000000, 0.000000000000000000, 1.000000000000000000 ) ) ;
#3614=CARTESIAN_POINT ( 'NONE',  ( 59.15655000470670188, -2.504444135221610246, -15.68085838234140006 ) ) ;
#3615=CARTESIAN_POINT ( 'NONE',  ( 51.73306673000479350, -49.00921834144799760, -77.03096706476540589 ) ) ;
#3616=CARTESIAN_POINT ( 'NONE',  ( 15.05440318628160057, -53.11618894467930119, -76.14999999999999147 ) ) ;
#3619=CARTESIAN_POINT ( 'NONE',  ( 47.18324198357289845, -54.80726809202429450, -74.14999999999999147 ) ) ;
#3620=DIRECTION ( 'NONE',  ( 0.000000000000000000, -1.000000000000000000, 0.000000000000000000 ) ) ;
#3621=DIRECTION ( 'NONE',  ( 0.000000000000000000, 0.000000000000000000, -1.000000000000000000 ) ) ;
#3623=EDGE_CURVE ( 'NONE', #42328, #18363, #40012, .T. ) ;
#3624=CARTESIAN_POINT ( 'NONE',  ( 13.32596385126870153, -50.17279131214790056, -21.04426679283869817 ) ) ;
#3626=CARTESIAN_POINT ( 'NONE',  ( 46.85765394103209758, -52.69486303297070151, -55.14905519569939685 ) ) ;
#3627=CARTESIAN_POINT ( 'NONE',  ( 60.98011298575943329, -45.39072023738052764, -46.91885902351079807 ) ) ;
#3628=CARTESIAN_POINT ( 'NONE',  ( 60.86406070507459987, -45.56987455658860142, -47.52785903502709886 ) ) ;
#3634=CARTESIAN_POINT ( 'NONE',  ( 14.27557881312050014, -51.11618622139269519, -74.14993436883828792 ) ) ;
#3637=AXIS2_PLACEMENT_3D ( 'NONE', #50198, #34179, #33670 ) ;
#3638=CARTESIAN_POINT ( 'NONE',  ( 14.35459849512296238, -51.14555453227163184, -74.54430098194714560 ) ) ;
#3640=CARTESIAN_POINT ( 'NONE',  ( 8.784728771152170879, -54.93525725209899235, -46.67204636145419983 ) ) ;
#3641=CARTESIAN_POINT ( 'NONE',  ( 10.62399383826485710, -64.83240141107415866, -18.14936727198398358 ) ) ;
#3642=CARTESIAN_POINT ( 'NONE',  ( 11.45636326042960107, 34.13238412238349895, -18.01147071074940342 ) ) ;
#3649=CARTESIAN_POINT ( 'NONE',  ( 49.71697407881379860, 22.41840834450090014, -55.07777775019549438 ) ) ;
#3650=ORIENTED_EDGE ( 'NONE', *, *, #17260, .T. ) ;
#3651=CARTESIAN_POINT ( 'NONE',  ( 53.50261634512969522, -49.38508019297159990, -49.11501020125410122 ) ) ;
#3652=ORIENTED_EDGE ( 'NONE', *, *, #49696, .T. ) ;
#3658=CARTESIAN_POINT ( 'NONE',  ( 53.51287195967390176, 18.19965013284789990, -49.22146522496750265 ) ) ;
#3659=CARTESIAN_POINT ( 'NONE',  ( 55.59742021819219815, -45.60898701366559749, -16.21687166337950003 ) ) ;
#3661=AXIS2_PLACEMENT_3D ( 'NONE', #22445, #3533, #38452 ) ;
#3663=EDGE_CURVE ( 'NONE', #5274, #7868, #44156, .T. ) ;
#3665=ORIENTED_EDGE ( 'NONE', *, *, #28898, .T. ) ;
#3667=CARTESIAN_POINT ( 'NONE',  ( 11.88973812647869899, -65.43508066229159681, -17.85918014674359711 ) ) ;
#3668=CARTESIAN_POINT ( 'NONE',  ( 10.81618306470670099, 33.23750078974720168, -46.19159279582959954 ) ) ;
#3671=CARTESIAN_POINT ( 'NONE',  ( 8.812209671510000675, 32.03058768159100111, -46.67110737466700243 ) ) ;
#3673=DIRECTION ( 'NONE',  ( 0.6676418852213039656, 0.2329255526947077437, 0.7071067811865533459 ) ) ;
#3676=CARTESIAN_POINT ( 'NONE',  ( 11.13393739769619906, -63.41372582578870265, -43.92068416175130352 ) ) ;
#3677=CARTESIAN_POINT ( 'NONE',  ( 13.39998208309999939, 20.55440457967890211, -74.14999999999999147 ) ) ;
#3680=CARTESIAN_POINT ( 'NONE',  ( 56.46340970881719556, 19.25363520061540257, -52.83593731267799143 ) ) ;
#3682=ORIENTED_EDGE ( 'NONE', *, *, #13821, .T. ) ;
#3687=CARTESIAN_POINT ( 'NONE',  ( 49.42285922342860260, 22.23360713278520251, -54.10983389954889589 ) ) ;
#3691=SHAPE_DEFINITION_REPRESENTATION ( #26116, #4683 ) ;
#3699=CARTESIAN_POINT ( 'NONE',  ( 46.35275103504439898, 21.67755452994670406, -76.14999999999999147 ) ) ;
#3700=DIRECTION ( 'NONE',  ( 1.000000000000000000, 0.000000000000000000, 5.637851296924970156E-15 ) ) ;
#3701=DIRECTION ( 'NONE',  ( -0.6911981449639432729, 0.7226652920947591596, 0.000000000000000000 ) ) ;
#3702=ADVANCED_FACE ( 'NONE', ( #18154, #6367 ), #13720, .T. ) ;
#3704=CARTESIAN_POINT ( 'NONE',  ( 52.58045726207989645, -49.84558690476340104, -28.06891840855830011 ) ) ;
#3705=CARTESIAN_POINT ( 'NONE',  ( 56.13041345539360094, -50.64099428910919443, -75.55393924165630892 ) ) ;
#3706=CARTESIAN_POINT ( 'NONE',  ( -11.32741173536820156, 10.64927170302630088, -6.269854646706059853 ) ) ;
#3707=CARTESIAN_POINT ( 'NONE',  ( 10.57536502229777220, -55.22799900453085797, -45.48887427433546549 ) ) ;
#3708=CIRCLE ( 'NONE', #18768, 0.9999999999568496278 ) ;
#3710=CARTESIAN_POINT ( 'NONE',  ( 61.14456834629570636, 14.07465811252290067, -46.86919079265500443 ) ) ;
#3712=VERTEX_POINT ( 'NONE', #34120 ) ;
#3713=CARTESIAN_POINT ( 'NONE',  ( 52.80356385740750369, -49.67514632639190353, -48.56463695142829806 ) ) ;
#3714=CARTESIAN_POINT ( 'NONE',  ( 47.66693464750959919, 23.24250025773469730, -54.67859957007570415 ) ) ;
#3717=FACE_OUTER_BOUND ( 'NONE', #29745, .T. ) ;
#3719=CARTESIAN_POINT ( 'NONE',  ( 51.78789577860580806, 18.59342600884450292, -76.67262230958300506 ) ) ;
#3720=CARTESIAN_POINT ( 'NONE',  ( 53.00021627873709917, 18.34579924662379824, -48.89297487182130197 ) ) ;
#3722=CARTESIAN_POINT ( 'NONE',  ( 53.39109823518269593, -49.36681769490010652, -48.76214596301609561 ) ) ;
#3724=EDGE_CURVE ( 'NONE', #51441, #12739, #28238, .T. ) ;
#3726=EDGE_CURVE ( 'NONE', #50083, #10111, #5850, .T. ) ;
#3727=CARTESIAN_POINT ( 'NONE',  ( 47.72346410858899901, -54.45426597620080145, -54.74160369805280624 ) ) ;
#3728=DIRECTION ( 'NONE',  ( 0.2260571801428161165, -1.387778780781444597E-17, -0.9741140340359943917 ) ) ;
#3730=CARTESIAN_POINT ( 'NONE',  ( 59.81249386774219801, -29.83678189827580240, -15.94359662707469916 ) ) ;
#3735=DIRECTION ( 'NONE',  ( 1.495533000000000082E-10, 6.370073999999999783E-11, -1.000000000000000000 ) ) ;
#3736=EDGE_CURVE ( 'NONE', #40665, #23799, #1930, .T. ) ;
#3737=DIRECTION ( 'NONE',  ( 0.000000000000000000, 0.000000000000000000, -1.000000000000000000 ) ) ;
#3742=CARTESIAN_POINT ( 'NONE',  ( 50.82041483519691383, -31.10319463887767455, -16.62067175138126274 ) ) ;
#3743=ORIENTED_EDGE ( 'NONE', *, *, #42316, .F. ) ;
#3744=DIRECTION ( 'NONE',  ( 0.000000000000000000, 0.000000000000000000, -1.000000000000000000 ) ) ;
#3747=ORIENTED_EDGE ( 'NONE', *, *, #35785, .F. ) ;
#3756=EDGE_CURVE ( 'NONE', #21139, #28005, #11909, .T. ) ;
#3757=CARTESIAN_POINT ( 'NONE',  ( 65.32733128089900276, -30.99350611824779733, -16.78960899708049936 ) ) ;
#3758=CARTESIAN_POINT ( 'NONE',  ( 14.52013050453804688, 20.37931109195778845, -75.46937998419714688 ) ) ;
#3760=CARTESIAN_POINT ( 'NONE',  ( 55.54883708180769730, 14.75989776373999973, -16.75766202486890322 ) ) ;
#3761=CARTESIAN_POINT ( 'NONE',  ( 40.85469175895860161, 14.12133229819039926, -5.792857911654750502 ) ) ;
#3762=DIRECTION ( 'NONE',  ( 0.000000000000000000, 0.000000000000000000, 1.000000000000000000 ) ) ;
#3763=CARTESIAN_POINT ( 'NONE',  ( 84.37646258656080533, -43.45890480302480796, -47.26568110888489826 ) ) ;
#3764=DIRECTION ( 'NONE',  ( -0.7071067811865475727, 0.000000000000000000, 0.7071067811865475727 ) ) ;
#3771=CIRCLE ( 'NONE', #38902, 2.000000000000002220 ) ;
#3772=FACE_OUTER_BOUND ( 'NONE', #6181, .T. ) ;
#3773=CARTESIAN_POINT ( 'NONE',  ( 50.48003419941433378, -36.11835380732057388, -76.20110286221279239 ) ) ;
#3774=CARTESIAN_POINT ( 'NONE',  ( 61.65798985235609564, -45.21281149609252736, -46.99565652671198990 ) ) ;
#3775=CARTESIAN_POINT ( 'NONE',  ( 13.50258242564699884, -50.13280577118869985, -20.96779971931389852 ) ) ;
#3777=CARTESIAN_POINT ( 'NONE',  ( -5.178173089599670043, -47.26880399451710701, -5.229689596307480315 ) ) ;
#3778=CARTESIAN_POINT ( 'NONE',  ( 47.18324198357279897, 23.57489020266570279, -54.61058319554400242 ) ) ;
#3780=CARTESIAN_POINT ( 'NONE',  ( 57.55751162058999881, -50.37847131510899601, -52.97747665993289701 ) ) ;
#3781=CARTESIAN_POINT ( 'NONE',  ( 43.17397272685330023, 12.05888459682840086, -4.721727401627280329 ) ) ;
#3783=CARTESIAN_POINT ( 'NONE',  ( 64.36428085589631110, -45.11618894467940066, -12.32250341870529908 ) ) ;
#3784=CARTESIAN_POINT ( 'NONE',  ( 58.28839273895309248, -46.80098789154040162, -47.64211241846629719 ) ) ;
#3787=CARTESIAN_POINT ( 'NONE',  ( 17.27947697856539833, -52.93030938277399855, -76.14999999999999147 ) ) ;
#3788=B_SPLINE_CURVE_WITH_KNOTS ( 'NONE', 3,
 ( #4598, #40767, #13008, #28963, #21097, #9335, #44962, #9064, #1455, #37100 ),
 .UNSPECIFIED., .F., .F.,
 ( 4, 2, 2, 2, 4 ),
 ( 0.000000000000000000, 0.1750000000135994438, 0.3750000000291418001, 0.5000000000388558075, 0.5540946774305016698 ),
 .UNSPECIFIED. ) ;
#3793=ORIENTED_EDGE ( 'NONE', *, *, #10880, .T. ) ;
#3801=CARTESIAN_POINT ( 'NONE',  ( 17.37246673088850102, 21.53776777092619810, -76.12726769927830617 ) ) ;
#3804=CARTESIAN_POINT ( 'NONE',  ( 57.11002074634209436, -45.86944388580869969, -26.25113386676060045 ) ) ;
#3806=CARTESIAN_POINT ( 'NONE',  ( 61.66564617331420095, 13.97241000098359898, -46.96226704611760283 ) ) ;
#3812=EDGE_LOOP ( 'NONE', ( #44592, #44226, #6302, #17764 ) ) ;
#3816=CARTESIAN_POINT ( 'NONE',  ( 10.85466640530910176, -64.96697012893029921, -17.55961383758990024 ) ) ;
#3817=CARTESIAN_POINT ( 'NONE',  ( 60.44876012278479749, 14.56718382513089871, -47.68802017693349882 ) ) ;
#3819=CARTESIAN_POINT ( 'NONE',  ( 40.40277276999439948, -44.85701247348080045, -4.354462746277440566 ) ) ;
#3820=CARTESIAN_POINT ( 'NONE',  ( -6.168089167389290139, 15.43748276452459933, -5.539338566224690119 ) ) ;
#3821=CARTESIAN_POINT ( 'NONE',  ( 47.17214967034067286, 23.54985037105774026, -74.50417146786301714 ) ) ;
#3826=ADVANCED_FACE ( 'NONE', ( #43103 ), #3525, .F. ) ;
#3827=CARTESIAN_POINT ( 'NONE',  ( 41.08565836803850146, 14.27946363452990042, -6.051015727772759867 ) ) ;
#3829=EDGE_CURVE ( 'NONE', #5028, #39996, #43349, .T. ) ;
#3831=CARTESIAN_POINT ( 'NONE',  ( 14.14835400967140089, 19.11410306511140078, -20.86158003109679981 ) ) ;
#3835=CARTESIAN_POINT ( 'NONE',  ( 48.31420000707529994, -54.21845507221640048, -54.97975724495599792 ) ) ;
#3836=AXIS2_PLACEMENT_3D ( 'NONE', #18832, #50819, #14910 ) ;
#3837=CARTESIAN_POINT ( 'NONE',  ( 51.99322000344975692, -32.94168956680540106, -19.32981501234134569 ) ) ;
#3844=ORIENTED_EDGE ( 'NONE', *, *, #28430, .F. ) ;
#3845=FACE_OUTER_BOUND ( 'NONE', #4508, .T. ) ;
#3846=CARTESIAN_POINT ( 'NONE',  ( 61.00611420029130727, -45.43078731296289874, -47.28201515225099882 ) ) ;
#3847=LINE ( 'NONE', #31852, #11193 ) ;
#3848=DIRECTION ( 'NONE',  ( 1.000000000000000000, 0.000000000000000000, 0.000000000000000000 ) ) ;
#3852=DIRECTION ( 'NONE',  ( 0.000000000000000000, 1.000000000000000000, 0.000000000000000000 ) ) ;
#3855=CARTESIAN_POINT ( 'NONE',  ( 51.67587649748560352, 17.38381105532069881, -77.01363636363639387 ) ) ;
#3857=ORIENTED_EDGE ( 'NONE', *, *, #38749, .T. ) ;
#3862=ORIENTED_EDGE ( 'NONE', *, *, #14967, .T. ) ;
#3863=ORIENTED_EDGE ( 'NONE', *, *, #2197, .T. ) ;
#3864=CARTESIAN_POINT ( 'NONE',  ( 48.54525988008339255, 22.76209179570290075, -54.56845936111729856 ) ) ;
#3867=CARTESIAN_POINT ( 'NONE',  ( 56.48240963976540030, -50.76892851967889442, -53.80988698027800154 ) ) ;
#3868=CARTESIAN_POINT ( 'NONE',  ( 13.73527022026340028, -50.20735447812900532, -20.93080062776369843 ) ) ;
#3869=CARTESIAN_POINT ( 'NONE',  ( 59.99603231228150690, -1.358522701324750059, -15.95392620586269850 ) ) ;
#3870=CARTESIAN_POINT ( 'NONE',  ( 51.97624292331419582, -50.01153706258679676, -76.70088690366090134 ) ) ;
#3871=B_SPLINE_SURFACE_WITH_KNOTS ( 'NONE', 3, 3, ( 
 ( #42721, #47430, #51606, #31655, #15700, #23790, #2623, #6816, #4670, #4156, #28511, #40834, #48182, #4933, #16727, #20905 ),
 ( #40063, #36902, #1002, #48709, #48975, #12813, #28247, #13081, #20643, #20130, #44508, #17002, #12286, #32949, #32682, #29034 ),
 ( #36122, #45030, #9130, #28767, #39806, #44769, #44245, #8873, #8351, #3914, #24826, #19877, #35868, #51860, #8611, #24303 ),
 ( #226, #40319, #4415, #15961, #20381, #36629, #8099, #31914, #24042, #47936, #16209, #24560, #12037, #27990, #43993, #36370 ),
 ( #32167, #478, #16465, #32420, #731, #48443, #12544, #40573, #33728, #42132, #29544, #41867, #45547, #17757, #5971, #9642 ),
 ( #41097, #2293, #22187, #38197, #37674, #25083, #37940, #26121, #33474, #21418, #34234, #46336, #13328, #41605, #1520, #6231 ),
 ( #49492, #25852, #25598, #21928, #5710, #21667, #5464, #5208, #1776, #14344, #30047, #17505, #21161, #49233, #29288, #49741 ),
 ( #2034, #45809, #18014, #13831, #37419, #50257, #18266, #30314, #37167, #45289, #33980, #1264, #29788, #49995, #17252, #33216 ),
 ( #9398, #25347, #41347, #9896, #13579, #14086, #46073, #10160, #3331, #14861, #22708, #14603, #15386, #31339, #42392, #46593 ),
 ( #6752, #51025, #23472, #3593, #7524, #26907, #39495, #39233, #19566, #51288, #50772, #43170, #47365, #43424, #11463, #19046 ) ),
 .UNSPECIFIED., .F., .F., .F.,
 ( 4, 1, 1, 1, 1, 1, 1, 4 ),
 ( 4, 2, 2, 2, 2, 2, 2, 4 ),
 ( -1.469098915510469939E-05, 0.1428571428571430157, 0.2857142857142860315, 0.4285714285714289917, 0.5714285714285709528, 0.7142857142857139685, 0.8571428571428569843, 1.000011663802299999 ),
 ( -1.570796326794899889, -1.322743703599180032, -1.039254991375500037, -0.8620745462357000122, -0.7734843236657999999, -0.6317399675539610016, -0.4049489977750169722, -0.1533416749778110100 ),
 .UNSPECIFIED. ) ;
#3872=CARTESIAN_POINT ( 'NONE',  ( 68.13393739769620083, -43.11618894467930119, -65.65000000000000568 ) ) ;
#3874=CARTESIAN_POINT ( 'NONE',  ( 16.13393739769620083, -15.61618894467929941, -11.65000000000000036 ) ) ;
#3877=DIRECTION ( 'NONE',  ( 1.000000000000000000, 0.000000000000000000, 0.000000000000000000 ) ) ;
#3878=VECTOR ( 'NONE', #44820, 1000.000000000000000 ) ;
#3881=CARTESIAN_POINT ( 'NONE',  ( 12.52592233819879830, -50.09802290064689601, -21.14436588474130119 ) ) ;
#3882=CARTESIAN_POINT ( 'NONE',  ( 56.00869119085820103, 19.38893017032829746, -75.85262141779099920 ) ) ;
#3884=B_SPLINE_CURVE_WITH_KNOTS ( 'NONE', 3,
 ( #23548, #48196, #3671, #15713, #15974, #51619, #27757, #32180, #35880, #240, #39820, #44260, #31669, #4169, #12301, #28260 ),
 .UNSPECIFIED., .F., .F.,
 ( 4, 2, 2, 2, 2, 2, 2, 4 ),
 ( 0.000000000000000000, 0.1775000000000006573, 0.3375000000000000222, 0.4374999999999991118, 0.4999999999999999445, 0.6249999999999994449, 0.8249999999999999556, 1.000000000000000000 ),
 .UNSPECIFIED. ) ;
#3885=CARTESIAN_POINT ( 'NONE',  ( 68.13393739769649926, -48.11618894467630270, -70.54999999999999716 ) ) ;
#3886=CARTESIAN_POINT ( 'NONE',  ( 60.89660960531970346, -45.43840501675690291, -47.10135066908280521 ) ) ;
#3891=DIRECTION ( 'NONE',  ( 0.000000000000000000, 0.000000000000000000, -1.000000000000000000 ) ) ;
#3893=CARTESIAN_POINT ( 'NONE',  ( 47.24561095051279835, -54.75899299496529693, -54.64386179031699697 ) ) ;
#3894=SURFACE_SIDE_STYLE ('',( #36351 ) ) ;
#3895=CARTESIAN_POINT ( 'NONE',  ( 10.42914237396198196, 33.65646982228821571, -47.08729022406233611 ) ) ;
#3896=CARTESIAN_POINT ( 'NONE',  ( 56.06467566929225654, -46.69807061730856645, -26.34903397246540635 ) ) ;
#3899=CARTESIAN_POINT ( 'NONE',  ( 10.61752692138360032, -64.82564047392860118, -18.17418372802830007 ) ) ;
#3905=CARTESIAN_POINT ( 'NONE',  ( 49.03027862569489770, 22.68258847135309964, -54.93684304997719892 ) ) ;
#3907=EDGE_LOOP ( 'NONE', ( #21243, #50346, #15812, #6714, #11117 ) ) ;
#3908=CARTESIAN_POINT ( 'NONE',  ( 52.85422459453599231, -49.67664456668449446, -48.94261454323000748 ) ) ;
#3912=CARTESIAN_POINT ( 'NONE',  ( 68.13393739769620083, 17.38381105532069881, -83.65000000000000568 ) ) ;
#3914=CARTESIAN_POINT ( 'NONE',  ( 83.54531734280119792, 13.40902645347810029, -46.66630366969080512 ) ) ;
#3916=CARTESIAN_POINT ( 'NONE',  ( 52.60294686985729840, 18.59530815018699812, -48.60888033553569443 ) ) ;
#3917=CARTESIAN_POINT ( 'NONE',  ( 56.20733314801729819, -45.19218008104289908, -15.77257108625240001 ) ) ;
#3919=CARTESIAN_POINT ( 'NONE',  ( 52.82512926767439865, 18.35096675686769885, -27.26906326477459785 ) ) ;
#3921=EDGE_LOOP ( 'NONE', ( #23053, #38154, #15338, #36303 ) ) ;
#3925=CARTESIAN_POINT ( 'NONE',  ( 11.81751875573920074, -65.31523040516019307, -17.14434872735650117 ) ) ;
#3926=CARTESIAN_POINT ( 'NONE',  ( 12.12676297962169869, 34.11083646916790002, -47.13081205359050330 ) ) ;
#3928=DIRECTION ( 'NONE',  ( 0.000000000000000000, 0.000000000000000000, 1.000000000000000000 ) ) ;
#3929=CARTESIAN_POINT ( 'NONE',  ( 11.38213983923405337, -65.24847911815764689, -22.77752646547867954 ) ) ;
#3930=DIRECTION ( 'NONE',  ( 0.000000000000000000, 0.000000000000000000, 1.000000000000000000 ) ) ;
#3931=ORIENTED_EDGE ( 'NONE', *, *, #43527, .T. ) ;
#3933=CARTESIAN_POINT ( 'NONE',  ( 10.97882772194960133, -63.26469174528480721, -44.74230523385489988 ) ) ;
#3934=CARTESIAN_POINT ( 'NONE',  ( 68.13393739769630031, 16.88381105532149817, -68.79999999999999716 ) ) ;
#3935=ORIENTED_EDGE ( 'NONE', *, *, #17729, .F. ) ;
#3940=( BOUNDED_CURVE ( )  B_SPLINE_CURVE ( 3, ( #17954, #7204, #40202, #47313 ),
 .UNSPECIFIED., .F., .T. ) 
 B_SPLINE_CURVE_WITH_KNOTS ( ( 4, 4 ),
 ( 1.485879941667409998, 1.496022784645234083 ),
 .UNSPECIFIED. ) 
 CURVE ( )  GEOMETRIC_REPRESENTATION_ITEM ( )  RATIONAL_B_SPLINE_CURVE ( ( 1.000000000000000000, 0.9999914269130683042, 0.9999914269130683042, 1.000000000000000000 ) ) 
 REPRESENTATION_ITEM ( '' )  );
#3942=DIRECTION ( 'NONE',  ( 1.000000000000000000, 0.000000000000000000, 0.000000000000000000 ) ) ;
#3944=CIRCLE ( 'NONE', #5632, 1.999999999999998668 ) ;
#3948=DIRECTION ( 'NONE',  ( 0.3918900565005459247, -0.9200120562340468044, 0.000000000000000000 ) ) ;
#3952=CARTESIAN_POINT ( 'NONE',  ( 53.51347036073359931, -49.43255037905120730, -49.22285071034340120 ) ) ;
#3956=CARTESIAN_POINT ( 'NONE',  ( 46.69150152944290255, 22.32070490622299985, -76.02679354016848379 ) ) ;
#3960=CARTESIAN_POINT ( 'NONE',  ( 11.73339007446990045, 33.77567933031070169, -16.50122832063929934 ) ) ;
#3962=CARTESIAN_POINT ( 'NONE',  ( 55.71241392848639862, -50.61618636397409432, -76.18756357822059044 ) ) ;
#3965=CARTESIAN_POINT ( 'NONE',  ( 61.43594907124419535, 13.96124516595140008, -46.78941255914340047 ) ) ;
#3966=DIRECTION ( 'NONE',  ( 0.000000000000000000, -0.7071067811865582309, 0.7071067811865366926 ) ) ;
#3968=CARTESIAN_POINT ( 'NONE',  ( 53.02240710655750178, -49.55998530720779627, -48.78672999826219581 ) ) ;
#3969=FACE_OUTER_BOUND ( 'NONE', #16953, .T. ) ;
#3970=DIRECTION ( 'NONE',  ( 1.000000000000000000, 0.000000000000000000, 0.000000000000000000 ) ) ;
#3971=CARTESIAN_POINT ( 'NONE',  ( 61.44924444735519842, 14.16613670727899965, -47.39916440910469930 ) ) ;
#3973=CARTESIAN_POINT ( 'NONE',  ( 51.64973234263280233, 18.01818895620939998, -76.82386384811070457 ) ) ;
#3974=CARTESIAN_POINT ( 'NONE',  ( 53.42701933212400434, 18.14767980575969730, -49.00234330185679710 ) ) ;
#3976=CARTESIAN_POINT ( 'NONE',  ( 75.13393739769618662, 1.883811055320649963, -84.38499399519520239 ) ) ;
#3979=CARTESIAN_POINT ( 'NONE',  ( 53.35699421374690132, 18.69401400300939642, -74.14999999999999147 ) ) ;
#3981=CARTESIAN_POINT ( 'NONE',  ( 47.67996957097940225, -54.51610847055570019, -55.06157314954699444 ) ) ;
#3982=CARTESIAN_POINT ( 'NONE',  ( -10.89822638428740120, 11.09799366572489987, -6.199143116732470205 ) ) ;
#3984=CARTESIAN_POINT ( 'NONE',  ( 62.76787785535929487, -30.70400768739660080, -16.43756860717520141 ) ) ;
#3986=DIRECTION ( 'NONE',  ( 0.000000000000000000, 1.000000000000000000, 0.000000000000000000 ) ) ;
#3988=AXIS2_PLACEMENT_3D ( 'NONE', #24676, #44110, #12396 ) ;
#3990=DIRECTION ( 'NONE',  ( 1.000000000000000000, 0.000000000000000000, 0.000000000000000000 ) ) ;
#3991=ORIENTED_EDGE ( 'NONE', *, *, #50405, .T. ) ;
#3993=CARTESIAN_POINT ( 'NONE',  ( 57.36123081079020380, 18.90300135422739913, -52.61896059691729732 ) ) ;
#3997=CARTESIAN_POINT ( 'NONE',  ( 55.41808927438875543, 19.74831332310506227, -75.07139216123769643 ) ) ;
#3999=CARTESIAN_POINT ( 'NONE',  ( 11.44965733209057390, 34.05957685831252491, -22.70627853750865199 ) ) ;
#4001=CARTESIAN_POINT ( 'NONE',  ( 61.22588934636690539, 14.38309530880740006, -47.69104795661070284 ) ) ;
#4004=FACE_OUTER_BOUND ( 'NONE', #32311, .T. ) ;
#4006=CARTESIAN_POINT ( 'NONE',  ( 59.22256780989010139, -28.32779697543540109, -15.66491663685500058 ) ) ;
#4009=CARTESIAN_POINT ( 'NONE',  ( 41.33277327098829801, 14.31091597718369890, -6.226138135101860094 ) ) ;
#4011=CARTESIAN_POINT ( 'NONE',  ( -11.07640030671909948, 8.018182000708311108, -19.14999999999999858 ) ) ;
#4013=CARTESIAN_POINT ( 'NONE',  ( 83.71674455129429759, -44.49277106579119589, -46.72760658838089398 ) ) ;
#4014=AXIS2_PLACEMENT_3D ( 'NONE', #1830, #41658, #33529 ) ;
#4016=ADVANCED_FACE ( 'NONE', ( #17378 ), #603, .T. ) ;
#4018=EDGE_LOOP ( 'NONE', ( #1208, #17337, #50078, #12723 ) ) ;
#4019=CARTESIAN_POINT ( 'NONE',  ( 54.55982533688380443, -47.81947338028329852, -26.42778140218189975 ) ) ;
#4020=CARTESIAN_POINT ( 'NONE',  ( 10.88038546904039983, -65.03853012327121519, -17.65323373620159941 ) ) ;
#4022=AXIS2_PLACEMENT_3D ( 'NONE', #32356, #10745, #39489 ) ;
#4025=CARTESIAN_POINT ( 'NONE',  ( 61.75019796695539753, -46.11618894467930119, -37.26101630944549470 ) ) ;
#4026=ORIENTED_EDGE ( 'NONE', *, *, #28835, .F. ) ;
#4027=CARTESIAN_POINT ( 'NONE',  ( -6.917791992670210277, -46.04619488212870237, -5.579573692652759931 ) ) ;
#4031=CARTESIAN_POINT ( 'NONE',  ( 57.55751162057470083, -50.45075475114750674, -53.12582022100689727 ) ) ;
#4032=CARTESIAN_POINT ( 'NONE',  ( 41.87064654090709581, 13.25620980835100049, -5.149960901716640116 ) ) ;
#4033=DIRECTION ( 'NONE',  ( -1.000000000000000000, -1.040834085586084257E-16, 0.000000000000000000 ) ) ;
#4036=CARTESIAN_POINT ( 'NONE',  ( 68.13393739769847457, -50.70395984888145335, -72.15645085170113759 ) ) ;
#4038=CARTESIAN_POINT ( 'NONE',  ( 17.21347160910390173, -53.11618894467930119, -76.14999999999999147 ) ) ;
#4039=ADVANCED_FACE ( 'NONE', ( #16588 ), #5746, .T. ) ;
#4042=EDGE_LOOP ( 'NONE', ( #42727, #4940, #2959, #32771 ) ) ;
#4043=CARTESIAN_POINT ( 'NONE',  ( 8.812209671510000675, 32.03058768159100111, -46.67110737466700243 ) ) ;
#4044=CARTESIAN_POINT ( 'NONE',  ( 61.31807987947320271, 14.40950277385760003, -47.72348187476750070 ) ) ;
#4046=EDGE_LOOP ( 'NONE', ( #26630, #19959, #21704 ) ) ;
#4047=CARTESIAN_POINT ( 'NONE',  ( 17.29296856898550061, 21.71079195693500097, -76.14999999999999147 ) ) ;
#4054=ADVANCED_FACE ( 'NONE', ( #32541 ), #24167, .F. ) ;
#4055=EDGE_LOOP ( 'NONE', ( #48221, #8044, #14685, #18845 ) ) ;
#4056=EDGE_LOOP ( 'NONE', ( #43631, #23206, #8346, #7539 ) ) ;
#4057=FACE_OUTER_BOUND ( 'NONE', #46291, .T. ) ;
#4058=DIRECTION ( 'NONE',  ( 0.000000000000000000, 0.000000000000000000, -1.000000000000000000 ) ) ;
#4059=VERTEX_POINT ( 'NONE', #40442 ) ;
#4062=CARTESIAN_POINT ( 'NONE',  ( 11.35626934712506220, -65.29495918738072646, -17.73521848461691874 ) ) ;
#4063=CARTESIAN_POINT ( 'NONE',  ( 60.36512744982970702, 14.56893724137899859, -47.62198983653560447 ) ) ;
#4065=CARTESIAN_POINT ( 'NONE',  ( 40.68015302493939345, -44.62521549934429999, -4.085853159663479950 ) ) ;
#4067=CARTESIAN_POINT ( 'NONE',  ( -6.423975383169469922, 14.97160766071710114, -4.833031552625280725 ) ) ;
#4068=B_SPLINE_CURVE_WITH_KNOTS ( 'NONE', 3,
 ( #7040, #35319, #6261, #14377, #39012, #30082, #30343, #34795, #26665, #50542, #10971, #14889, #38228, #2586, #46366, #42686 ),
 .UNSPECIFIED., .F., .F.,
 ( 4, 2, 2, 2, 2, 2, 2, 4 ),
 ( 0.000000000000000000, 2.041349754395100025, 4.374320902275219858, 5.832427869700300249, 6.561481353412840001, 7.727966927352889925, 9.594343845656990055, 11.66485573940060050 ),
 .UNSPECIFIED. ) ;
#4069=CARTESIAN_POINT ( 'NONE',  ( 46.46257399784555986, 21.93137732320808553, -76.13734531346138112 ) ) ;
#4070=DIRECTION ( 'NONE',  ( 0.000000000000000000, 0.000000000000000000, -1.000000000000000000 ) ) ;
#4075=CARTESIAN_POINT ( 'NONE',  ( 11.92002530253619952, 33.88340405295690516, -45.75731838001080121 ) ) ;
#4078=FACE_OUTER_BOUND ( 'NONE', #44012, .T. ) ;
#4080=CARTESIAN_POINT ( 'NONE',  ( 47.02944413358449793, 23.17759013347800234, -75.36156511192869800 ) ) ;
#4081=CARTESIAN_POINT ( 'NONE',  ( 48.70705169239410282, -54.01489688557619218, -54.80929227398259940 ) ) ;
#4082=DIRECTION ( 'NONE',  ( 1.000000000000000000, 0.000000000000000000, 0.000000000000000000 ) ) ;
#4083=CARTESIAN_POINT ( 'NONE',  ( 16.13393739769620083, -15.61618894467929941, -48.64999999999999858 ) ) ;
#4090=CARTESIAN_POINT ( 'NONE',  ( 60.33724287810149889, -45.72939421683570060, -47.29483955813599749 ) ) ;
#4091=CARTESIAN_POINT ( 'NONE',  ( 55.04426526048000312, -48.50067717176560222, -48.28429872967510050 ) ) ;
#4094=DIRECTION ( 'NONE',  ( 0.000000000000000000, 1.000000000000000000, 0.000000000000000000 ) ) ;
#4096=ORIENTED_EDGE ( 'NONE', *, *, #22619, .T. ) ;
#4098=EDGE_LOOP ( 'NONE', ( #30063, #38795, #31362, #19912, #6388, #948, #13536 ) ) ;
#4101=CARTESIAN_POINT ( 'NONE',  ( 53.27448929283489321, -49.51683810077160075, -49.18721518522060165 ) ) ;
#4103=CARTESIAN_POINT ( 'NONE',  ( 76.39889423561334070, -19.26091417457611854, -12.79178202693621813 ) ) ;
#4104=CARTESIAN_POINT ( 'NONE',  ( 49.85166797725670307, -53.37057052038269944, -54.14856546049170305 ) ) ;
#4108=ORIENTED_EDGE ( 'NONE', *, *, #47218, .F. ) ;
#4109=CARTESIAN_POINT ( 'NONE',  ( 47.94837612362730539, 23.09355010960259946, -54.72220175608870107 ) ) ;
#4111=ADVANCED_FACE ( 'NONE', ( #50124 ), #49621, .T. ) ;
#4112=CARTESIAN_POINT ( 'NONE',  ( 56.41630124387939560, -50.57626175706130311, -52.96295731896090331 ) ) ;
#4114=CARTESIAN_POINT ( 'NONE',  ( 64.53955642881849997, 0.8952382593903849273, -17.65707518710819812 ) ) ;
#4115=CARTESIAN_POINT ( 'NONE',  ( 52.08784388273989663, -49.61362219112419325, -77.13961893560180272 ) ) ;
#4116=EDGE_CURVE ( 'NONE', #48985, #14240, #25473, .T. ) ;
#4120=CARTESIAN_POINT ( 'NONE',  ( 53.36305439838449871, -50.55087041970300277, -76.89765195167041156 ) ) ;
#4121=CARTESIAN_POINT ( 'NONE',  ( 60.28868092514782973, 14.57684442129954761, -47.55394404419391918 ) ) ;
#4126=CARTESIAN_POINT ( 'NONE',  ( 13.23341202568920139, -50.15389934968320063, -21.05834214923379832 ) ) ;
#4128=CARTESIAN_POINT ( 'NONE',  ( 66.23540447448814916, -49.95860450174190248, -75.14853292321149070 ) ) ;
#4129=CARTESIAN_POINT ( 'NONE',  ( 60.80455843160299878, -45.48718825086960038, -47.16343365292970446 ) ) ;
#4130=DIRECTION ( 'NONE',  ( -0.6377178376947741922, -0.7702700562049011879, 0.000000000000000000 ) ) ;
#4133=EDGE_CURVE ( 'NONE', #27748, #44502, #4915, .T. ) ;
#4134=ORIENTED_EDGE ( 'NONE', *, *, #38233, .F. ) ;
#4135=CARTESIAN_POINT ( 'NONE',  ( 11.27206271272561011, -65.28199317941199809, -18.17421237899035447 ) ) ;
#4136=CARTESIAN_POINT ( 'NONE',  ( 47.32580105348969823, -54.70279562150209784, -54.71536561081010319 ) ) ;
#4142=CARTESIAN_POINT ( 'NONE',  ( 10.64977475916229999, 33.62388472332079914, -18.05902683574160150 ) ) ;
#4144=CARTESIAN_POINT ( 'NONE',  ( 13.32898877073008848, -51.15116428088592926, -21.92090656186747211 ) ) ;
#4146=CARTESIAN_POINT ( 'NONE',  ( 48.42521416700790127, 25.14253336855949783, -60.76348542011150045 ) ) ;
#4147=CARTESIAN_POINT ( 'NONE',  ( 49.32485110899289538, 22.33724018645339982, -54.24613943530840032 ) ) ;
#4149=CIRCLE ( 'NONE', #41787, 2.999999999999999112 ) ;
#4150=CARTESIAN_POINT ( 'NONE',  ( 52.95534740401019747, -49.62986309362070614, -49.01774101255579552 ) ) ;
#4152=AXIS2_PLACEMENT_3D ( 'NONE', #36944, #32724, #49020 ) ;
#4156=CARTESIAN_POINT ( 'NONE',  ( 83.53665286397169609, 13.38078810466280011, -46.51476939800780741 ) ) ;
#4157=CARTESIAN_POINT ( 'NONE',  ( 53.54812521361419897, 17.65605455213760067, -26.94805828179969964 ) ) ;
#4159=CARTESIAN_POINT ( 'NONE',  ( 52.69474333003019950, 18.53535902989789719, -48.79529474154600166 ) ) ;
#4160=CARTESIAN_POINT ( 'NONE',  ( 56.32660178866539979, -45.39391173880739672, -16.96744964118260057 ) ) ;
#4164=EDGE_LOOP ( 'NONE', ( #18936, #34770 ) ) ;
#4165=CARTESIAN_POINT ( 'NONE',  ( 11.36506045489740124, -65.29567750107250390, -17.70888282129770275 ) ) ;
#4166=CARTESIAN_POINT ( 'NONE',  ( 12.83617943148310125, 34.27320782901589524, -47.68841635077260577 ) ) ;
#4168=CARTESIAN_POINT ( 'NONE',  ( 47.41031548299500287, -54.68188730245149998, -54.95579447497389936 ) ) ;
#4169=CARTESIAN_POINT ( 'NONE',  ( 8.788582027835408539, 31.90262041517649649, -46.67125809046000029 ) ) ;
#4171=ORIENTED_EDGE ( 'NONE', *, *, #45777, .F. ) ;
#4172=CARTESIAN_POINT ( 'NONE',  ( 10.83485818036387371, 24.03123212219991345, -45.05995267079551780 ) ) ;
#4173=CARTESIAN_POINT ( 'NONE',  ( 11.13393739769619906, -63.22724917335859374, -43.91336038921839702 ) ) ;
#4174=EDGE_CURVE ( 'NONE', #11477, #17310, #6617, .T. ) ;
#4175=CARTESIAN_POINT ( 'NONE',  ( 13.39998208309985550, 20.55440457967879553, -74.33587756533620450 ) ) ;
#4178=CARTESIAN_POINT ( 'NONE',  ( 56.77163878576220668, 19.44106416691489869, -53.71547587232010557 ) ) ;
#4179=LINE ( 'NONE', #34921, #51035 ) ;
#4182=ORIENTED_EDGE ( 'NONE', *, *, #38309, .T. ) ;
#4186=CARTESIAN_POINT ( 'NONE',  ( 59.27104365041189027, 16.03377513504399943, -49.27951717864250725 ) ) ;
#4189=CARTESIAN_POINT ( 'NONE',  ( 54.37485829101720469, 19.90489201363050142, -75.46191895107959624 ) ) ;
#4192=VECTOR ( 'NONE', #49646, 1000.000000000000000 ) ;
#4197=VECTOR ( 'NONE', #1154, 1000.000000000000000 ) ;
#4199=CARTESIAN_POINT ( 'NONE',  ( 47.11820049732209981, 23.26876160514180114, -75.17431011251740358 ) ) ;
#4200=EDGE_CURVE ( 'NONE', #8473, #5858, #45646, .T. ) ;
#4202=CARTESIAN_POINT ( 'NONE',  ( 61.72540784289278548, -31.18892121339349899, -16.65167593768012821 ) ) ;
#4206=CARTESIAN_POINT ( 'NONE',  ( 53.99435962611450179, -50.67304520127230205, -76.55038729938830500 ) ) ;
#4210=CARTESIAN_POINT ( 'NONE',  ( 61.39588077177570824, 13.94803686931489928, -46.41028556702730157 ) ) ;
#4212=ORIENTED_EDGE ( 'NONE', *, *, #33100, .F. ) ;
#4213=CARTESIAN_POINT ( 'NONE',  ( 53.30277398520830445, -49.41309324413840187, -48.78464791978749560 ) ) ;
#4214=CARTESIAN_POINT ( 'NONE',  ( 61.35843256309839688, -45.19499326282659979, -28.04812333717190143 ) ) ;
#4216=CARTESIAN_POINT ( 'NONE',  ( 56.51875352494170102, 14.92161442796829895, -26.24278457129210196 ) ) ;
#4218=CARTESIAN_POINT ( 'NONE',  ( 50.90450009015570032, 18.64662547016060046, -76.22583872417631312 ) ) ;
#4219=CARTESIAN_POINT ( 'NONE',  ( 52.85417440126129662, 18.42047290032009954, -48.78849739474269853 ) ) ;
#4224=CIRCLE ( 'NONE', #29322, 29.70020322226740106 ) ;
#4225=CARTESIAN_POINT ( 'NONE',  ( 47.76095205451260739, -54.43479718813880197, -54.75002775354360551 ) ) ;
#4226=CARTESIAN_POINT ( 'NONE',  ( -6.923399356020619066, 14.58998760014879892, -4.778090148566289663 ) ) ;
#4227=CIRCLE ( 'NONE', #41860, 1.000000000000000888 ) ;
#4228=( BOUNDED_CURVE ( )  B_SPLINE_CURVE ( 3, ( #16661, #44965, #9068, #25016 ),
 .UNSPECIFIED., .F., .T. ) 
 B_SPLINE_CURVE_WITH_KNOTS ( ( 4, 4 ),
 ( 0.000000000000000000, 0.3709736340029385904 ),
 .UNSPECIFIED. ) 
 CURVE ( )  GEOMETRIC_REPRESENTATION_ITEM ( )  RATIONAL_B_SPLINE_CURVE ( ( 1.000000000000000000, 0.9885643905736447579, 0.9885643905736447579, 1.000000000000000000 ) ) 
 REPRESENTATION_ITEM ( '' )  );
#4229=DIRECTION ( 'NONE',  ( 0.1414213562373085320, 0.000000000000000000, 0.9899494936611666907 ) ) ;
#4230=CARTESIAN_POINT ( 'NONE',  ( 61.61848170108899581, -30.28435294235449859, -16.19051669735609877 ) ) ;
#4237=CARTESIAN_POINT ( 'NONE',  ( 51.23435946743376945, -34.79825311741358007, -76.55133624385516100 ) ) ;
#4240=ORIENTED_EDGE ( 'NONE', *, *, #42017, .F. ) ;
#4241=CARTESIAN_POINT ( 'NONE',  ( 14.34417029198879945, -51.11618894467930119, -22.49240188329099865 ) ) ;
#4244=ORIENTED_EDGE ( 'NONE', *, *, #12983, .T. ) ;
#4245=CARTESIAN_POINT ( 'NONE',  ( 56.76523583744410217, -45.25640930880150137, -25.29480072339120156 ) ) ;
#4246=CARTESIAN_POINT ( 'NONE',  ( 53.76111468063071896, 20.07186374916310712, -75.55241714225449812 ) ) ;
#4248=CARTESIAN_POINT ( 'NONE',  ( 10.84316497021790227, 33.36836038292673123, -23.37164403024571513 ) ) ;
#4255=VERTEX_POINT ( 'NONE', #22581 ) ;
#4258=CARTESIAN_POINT ( 'NONE',  ( 45.38213474528080127, 14.14634435393059952, -8.365266594206339335 ) ) ;
#4260=CARTESIAN_POINT ( 'NONE',  ( 14.46981516282570013, 20.61263520652270032, -75.69337827730609547 ) ) ;
#4263=CARTESIAN_POINT ( 'NONE',  ( 82.81544245083729550, -45.32786319503500039, -47.32222464724249988 ) ) ;
#4266=ORIENTED_EDGE ( 'NONE', *, *, #15303, .F. ) ;
#4267=CARTESIAN_POINT ( 'NONE',  ( 52.86928981489899826, -49.61879012794779698, -27.87016756703999931 ) ) ;
#4268=CARTESIAN_POINT ( 'NONE',  ( 15.72192118513690140, -50.88627069933389890, -20.20712476364090193 ) ) ;
#4269=CARTESIAN_POINT ( 'NONE',  ( 50.83473830212534494, -35.51255236623077138, -76.31871491474301195 ) ) ;
#4272=CARTESIAN_POINT ( 'NONE',  ( 13.19554430456510019, -50.05398003317129962, -21.01912116927340435 ) ) ;
#4273=ORIENTED_EDGE ( 'NONE', *, *, #28109, .T. ) ;
#4274=CARTESIAN_POINT ( 'NONE',  ( -9.067911617064609686, -44.12703459110060322, -5.856042089190190758 ) ) ;
#4275=CARTESIAN_POINT ( 'NONE',  ( 47.44010287600260511, 23.38619148779610057, -54.64745420776859675 ) ) ;
#4279=CARTESIAN_POINT ( 'NONE',  ( 43.67695093021549724, 12.07467661710849960, -4.963296560282329573 ) ) ;
#4281=CARTESIAN_POINT ( 'NONE',  ( 16.13393739769620083, -15.61618894467929941, -49.12910085600329779 ) ) ;
#4283=CARTESIAN_POINT ( 'NONE',  ( 68.13393739769840352, -50.61618894467879670, -73.25000000000220268 ) ) ;
#4289=CARTESIAN_POINT ( 'NONE',  ( 68.13393739769630031, 16.88381105531836823, -74.20000000000023022 ) ) ;
#4293=ORIENTED_EDGE ( 'NONE', *, *, #30139, .F. ) ;
#4294=CARTESIAN_POINT ( 'NONE',  ( 18.56913828510419862, 20.72643819036759893, -75.26885115310530239 ) ) ;
#4296=EDGE_CURVE ( 'NONE', #47510, #44411, #34113, .T. ) ;
#4297=VERTEX_POINT ( 'NONE', #29417 ) ;
#4298=CARTESIAN_POINT ( 'NONE',  ( 56.70262180045499889, -46.08091195091049741, -26.25054577630639940 ) ) ;
#4301=AXIS2_PLACEMENT_3D ( 'NONE', #5206, #17250, #44767 ) ;
#4306=VECTOR ( 'NONE', #24386, 1000.000000000000000 ) ;
#4307=ADVANCED_FACE ( 'NONE', ( #31212 ), #26772, .T. ) ;
#4308=CARTESIAN_POINT ( 'NONE',  ( 11.96242356392005846, 34.20360893564268423, -17.67418118889332490 ) ) ;
#4310=CARTESIAN_POINT ( 'NONE',  ( 11.63254243215296135, -64.84373839395865957, -23.90641762642841783 ) ) ;
#4312=ORIENTED_EDGE ( 'NONE', *, *, #51576, .T. ) ;
#4313=EDGE_LOOP ( 'NONE', ( #41035, #49809, #2848, #24121 ) ) ;
#4314=DIRECTION ( 'NONE',  ( 0.000000000000000000, 1.000000000000000000, 0.000000000000000000 ) ) ;
#4315=CARTESIAN_POINT ( 'NONE',  ( 10.96947365136730923, -65.06555258025436217, -17.60046481881581215 ) ) ;
#4316=CARTESIAN_POINT ( 'NONE',  ( 60.96233653960639742, 14.34520385656299979, -47.58503771552609862 ) ) ;
#4317=EDGE_CURVE ( 'NONE', #5478, #3425, #19940, .T. ) ;
#4318=B_SPLINE_CURVE_WITH_KNOTS ( 'NONE', 3,
 ( #32621, #17706, #49180, #37363, #48650, #675, #45753, #1203, #45493, #1722, #24763, #13271, #36838, #9591, #41292, #13014, #37617, #49434 ),
 .UNSPECIFIED., .F., .F.,
 ( 4, 2, 2, 2, 2, 2, 2, 2, 4 ),
 ( 0.000000000000000000, 0.2367773115722650590, 0.3750000000000009437, 0.5000000000000017764, 0.5625000000000022204, 0.6625000000000008660, 0.8225000000000022293, 0.9835464721590492232, 1.000000000000000000 ),
 .UNSPECIFIED. ) ;
#4319=CARTESIAN_POINT ( 'NONE',  ( 48.01232633225529867, 14.92653732367729980, -11.04036235616349870 ) ) ;
#4322=CARTESIAN_POINT ( 'NONE',  ( -7.646760217796759740, 14.02655874010070036, -5.000276550805019760 ) ) ;
#4324=CARTESIAN_POINT ( 'NONE',  ( 54.67238578969960372, 14.97123595123641415, -15.88465852508373999 ) ) ;
#4326=VERTEX_POINT ( 'NONE', #35686 ) ;
#4327=B_SPLINE_CURVE_WITH_KNOTS ( 'NONE', 3,
 ( #30081, #17283, #49003, #41376, #42160, #38227 ),
 .UNSPECIFIED., .F., .F.,
 ( 4, 2, 4 ),
 ( 0.000000000000000000, 0.4925159341063432006, 0.9850318682126864012 ),
 .UNSPECIFIED. ) ;
#4328=CARTESIAN_POINT ( 'NONE',  ( 57.31674080195730170, 16.10205221464649838, -48.00267488721029707 ) ) ;
#4330=CARTESIAN_POINT ( 'NONE',  ( 11.23465093859169883, 32.93573061327259666, -44.29738226443560478 ) ) ;
#4331=B_SPLINE_CURVE_WITH_KNOTS ( 'NONE', 3,
 ( #36813, #44167, #8007, #23962, #8262, #40239, #12455, #28425, #40490, #4583 ),
 .UNSPECIFIED., .F., .F.,
 ( 4, 1, 1, 1, 1, 1, 1, 4 ),
 ( 0.000000000000000000, 0.1428489515031106383, 0.2857044903109892675, 0.4285600291188678690, 0.5714155679267454158, 0.7142711067346241283, 0.8571266455425027297, 1.000000000000000000 ),
 .UNSPECIFIED. ) ;
#4334=AXIS2_PLACEMENT_3D ( 'NONE', #15389, #47116, #11205 ) ;
#4337=CARTESIAN_POINT ( 'NONE',  ( 46.52573464699440109, 22.06354468997819751, -76.11300885443861830 ) ) ;
#4338=CARTESIAN_POINT ( 'NONE',  ( 48.65218399916620484, -54.01178499192519666, -54.72548888424969959 ) ) ;
#4339=CARTESIAN_POINT ( 'NONE',  ( 51.45119095509264184, -32.08428337519749363, -17.60359467805431777 ) ) ;
#4345=DIRECTION ( 'NONE',  ( 1.000000000000000000, 0.000000000000000000, 0.000000000000000000 ) ) ;
#4348=CARTESIAN_POINT ( 'NONE',  ( 60.28868092514740340, -45.80922231065850525, -47.55394404419410392 ) ) ;
#4350=CARTESIAN_POINT ( 'NONE',  ( 82.13853704237929776, 13.88381105532070059, -46.37203261889099792 ) ) ;
#4353=LINE ( 'NONE', #420, #12540 ) ;
#4356=CARTESIAN_POINT ( 'NONE',  ( 84.41203222934960593, -43.51893176132989538, -47.41895602134449916 ) ) ;
#4359=CARTESIAN_POINT ( 'NONE',  ( 61.31728467875730360, -45.31601413538380285, -47.18620263350000243 ) ) ;
#4360=CARTESIAN_POINT ( 'NONE',  ( 11.87263544330925846, -55.38869636903399396, -22.13631662224942787 ) ) ;
#4361=CARTESIAN_POINT ( 'NONE',  ( 76.39892101097316868, -19.26612468183901328, -12.79189735567145902 ) ) ;
#4362=CARTESIAN_POINT ( 'NONE',  ( 51.12088197827599600, -52.83173572655250183, -53.84322824623650661 ) ) ;
#4363=ADVANCED_FACE ( 'NONE', ( #46989 ), #11666, .T. ) ;
#4367=CARTESIAN_POINT ( 'NONE',  ( 16.13393739769620083, -15.61618894467929941, -15.65000000000000036 ) ) ;
#4368=CARTESIAN_POINT ( 'NONE',  ( 56.70649773145339623, -45.28348190995249922, -25.29428280798650164 ) ) ;
#4369=CARTESIAN_POINT ( 'NONE',  ( 56.48532837834070364, -50.76773061328089653, -53.84782101877240024 ) ) ;
#4370=LINE ( 'NONE', #961, #51202 ) ;
#4375=VERTEX_POINT ( 'NONE', #19177 ) ;
#4376=CARTESIAN_POINT ( 'NONE',  ( 0.4723711254741681520, 21.40360305360503901, -7.245998062423555375 ) ) ;
#4378=CARTESIAN_POINT ( 'NONE',  ( 53.31396980585229528, -50.46140905625839679, -77.17790061419020731 ) ) ;
#4382=CARTESIAN_POINT ( 'NONE',  ( 13.08906387764550061, -50.12942787500359998, -21.07936304675460093 ) ) ;
#4387=CARTESIAN_POINT ( 'NONE',  ( 53.59007319875249920, 18.17385789302069554, -49.22505640236219904 ) ) ;
#4388=CARTESIAN_POINT ( 'NONE',  ( 61.28085239525059791, 14.36939662108470017, -47.67834120296360112 ) ) ;
#4390=CARTESIAN_POINT ( 'NONE',  ( 40.36721523010790236, 13.65407319109839790, -4.296538310233780855 ) ) ;
#4391=ORIENTED_EDGE ( 'NONE', *, *, #13433, .F. ) ;
#4392=CARTESIAN_POINT ( 'NONE',  ( 14.63260219478210011, -51.92834279550939414, -75.76244777734170555 ) ) ;
#4393=CARTESIAN_POINT ( 'NONE',  ( 47.23726808012239786, -54.76554284521510141, -54.66460646074769869 ) ) ;
#4396=CARTESIAN_POINT ( 'NONE',  ( 12.24650116548775003, 34.20510744208135634, -47.55800081747561592 ) ) ;
#4398=CARTESIAN_POINT ( 'NONE',  ( 60.92372936349968171, -45.44413726905956707, -47.20208884485387557 ) ) ;
#4399=EDGE_CURVE ( 'NONE', #34917, #38938, #45135, .T. ) ;
#4400=CARTESIAN_POINT ( 'NONE',  ( 55.82671577406989627, -45.92588907196979875, -17.31876445303114309 ) ) ;
#4401=CARTESIAN_POINT ( 'NONE',  ( 11.42280562906969976, 34.12559483387010317, -18.14299411086210156 ) ) ;
#4405=LINE ( 'NONE', #36362, #6671 ) ;
#4406=CARTESIAN_POINT ( 'NONE',  ( 43.75992006955644342, 12.39321587538100822, -5.076600544086916855 ) ) ;
#4407=CARTESIAN_POINT ( 'NONE',  ( 48.55446773597019927, 22.85509828786500108, -54.84877711739730444 ) ) ;
#4409=CARTESIAN_POINT ( 'NONE',  ( 52.72600133020739577, -49.74232360282439913, -48.79686034740650058 ) ) ;
#4410=CONICAL_SURFACE ( 'NONE', #21127, 14.87302494707580180, 1.249045772398249987 ) ;
#4411=EDGE_LOOP ( 'NONE', ( #10415, #31036, #10999, #24776 ) ) ;
#4413=CARTESIAN_POINT ( 'NONE',  ( 48.42521416700790127, -56.37491125791819968, -64.38029159777090626 ) ) ;
#4414=CARTESIAN_POINT ( 'NONE',  ( 56.93701003829870189, -50.64063337602150483, -53.86363391158519676 ) ) ;
#4415=CARTESIAN_POINT ( 'NONE',  ( 84.38271246941039294, 12.23852340322079968, -47.29654027836490116 ) ) ;
#4416=CARTESIAN_POINT ( 'NONE',  ( 53.98867551104529383, 17.11644939637280061, -26.51198043128849946 ) ) ;
#4418=CARTESIAN_POINT ( 'NONE',  ( 52.75108811105570084, 18.50140338450120225, -48.86094477483089804 ) ) ;
#4419=CARTESIAN_POINT ( 'NONE',  ( 56.51485985564450232, -45.12984804823710050, -15.71382745701569839 ) ) ;
#4421=VERTEX_POINT ( 'NONE', #23093 ) ;
#4422=ORIENTED_EDGE ( 'NONE', *, *, #41330, .T. ) ;
#4423=CARTESIAN_POINT ( 'NONE',  ( 11.37461208536520019, -65.06764363074510982, -16.88571178953269936 ) ) ;
#4424=CARTESIAN_POINT ( 'NONE',  ( 11.63281624934139913, 33.81340851509290246, -46.46564656908429924 ) ) ;
#4425=CARTESIAN_POINT ( 'NONE',  ( 18.83587408709283650, 20.46262858050933886, -15.79022535844386965 ) ) ;
#4427=CARTESIAN_POINT ( 'NONE',  ( 44.34239523011500239, -43.97607093873300244, -3.187564294433600232 ) ) ;
#4428=CARTESIAN_POINT ( 'NONE',  ( 10.89822354151269934, -64.67713789139354219, -23.30988825783105511 ) ) ;
#4430=ORIENTED_EDGE ( 'NONE', *, *, #17903, .F. ) ;
#4433=CARTESIAN_POINT ( 'NONE',  ( 10.97839846337910075, -63.20796340677059533, -44.74189274530859706 ) ) ;
#4435=CARTESIAN_POINT ( 'NONE',  ( 59.49262858449159808, -48.61618894467930119, -53.92796738110899923 ) ) ;
#4438=CARTESIAN_POINT ( 'NONE',  ( 52.38386464390320185, 18.65344693462920134, -77.22931088682960876 ) ) ;
#4439=EDGE_LOOP ( 'NONE', ( #45347, #26205, #5406, #13616 ) ) ;
#4443=CARTESIAN_POINT ( 'NONE',  ( 55.50962190611750202, 15.95222788008109838, -46.54932604926320039 ) ) ;
#4445=CARTESIAN_POINT ( 'NONE',  ( 11.12422127314902731, -55.30202234704525921, -21.40295201840961070 ) ) ;
#4448=CARTESIAN_POINT ( 'NONE',  ( 46.79542243668350210, -53.50887967020530311, -76.01632185952030341 ) ) ;
#4449=ORIENTED_EDGE ( 'NONE', *, *, #48595, .T. ) ;
#4455=CARTESIAN_POINT ( 'NONE',  ( 46.48058913279649573, 21.92052743937680148, -76.13714234130850400 ) ) ;
#4456=CARTESIAN_POINT ( 'NONE',  ( 16.13393739769620083, -15.61618894467929941, 6.349999999999999645 ) ) ;
#4458=CARTESIAN_POINT ( 'NONE',  ( 33.53393739769619231, -15.61618894467929763, -10.44999999999999929 ) ) ;
#4462=CARTESIAN_POINT ( 'NONE',  ( 56.39839003427439934, -50.66188084753460430, -75.14917411940758996 ) ) ;
#4466=CARTESIAN_POINT ( 'NONE',  ( 61.26594051415460029, 14.01037552971329880, -46.68275217642920438 ) ) ;
#4467=CARTESIAN_POINT ( 'NONE',  ( -28.48658230523989943, -35.31887766905860104, -54.95457219459440523 ) ) ;
#4470=CARTESIAN_POINT ( 'NONE',  ( 52.87578377016760101, -49.63680538124820885, -48.67531175415550138 ) ) ;
#4471=CARTESIAN_POINT ( 'NONE',  ( 61.10919664416649510, -45.15820646057929366, -27.23097577694250049 ) ) ;
#4473=CARTESIAN_POINT ( 'NONE',  ( 56.72744220692439399, 14.83176467157860046, -26.24945950869589950 ) ) ;
#4475=CARTESIAN_POINT ( 'NONE',  ( 51.13982992927869731, 19.47025619440540112, -76.16554326337229952 ) ) ;
#4476=CARTESIAN_POINT ( 'NONE',  ( 53.00693766222299530, 18.33849153667809873, -48.85763909861859844 ) ) ;
#4478=CARTESIAN_POINT ( 'NONE',  ( 43.42022383785410256, -43.54919953056790405, -4.975730455609930658 ) ) ;
#4482=CARTESIAN_POINT ( 'NONE',  ( 47.66583891269780082, -54.50953961429650008, -54.89454647195640291 ) ) ;
#4485=CARTESIAN_POINT ( 'NONE',  ( 59.34568438161719683, 16.86995364085609950, -50.40761009331129827 ) ) ;
#4488=CIRCLE ( 'NONE', #35431, 4.065501003882420861 ) ;
#4490=LINE ( 'NONE', #9215, #44415 ) ;
#4491=ADVANCED_FACE ( 'NONE', ( #3845 ), #8026, .F. ) ;
#4495=CARTESIAN_POINT ( 'NONE',  ( 57.35856957515439092, 18.90358493360990266, -52.61941485521469986 ) ) ;
#4498=CARTESIAN_POINT ( 'NONE',  ( 56.92979928365449638, -45.19979990857069652, -25.29906707419310052 ) ) ;
#4501=DIRECTION ( 'NONE',  ( 0.000000000000000000, 1.000000000000000000, 0.000000000000000000 ) ) ;
#4508=EDGE_LOOP ( 'NONE', ( #28300, #30974, #7549, #21789, #13623 ) ) ;
#4509=CARTESIAN_POINT ( 'NONE',  ( 11.89321894728460016, -65.43602743322060178, -22.25048311349110008 ) ) ;
#4512=CARTESIAN_POINT ( 'NONE',  ( 14.49461893737620066, 21.34486587698399873, -76.03043890231919022 ) ) ;
#4513=CARTESIAN_POINT ( 'NONE',  ( 51.78349585950329725, 17.91029630874730216, -77.04629326439351189 ) ) ;
#4514=CARTESIAN_POINT ( 'NONE',  ( 84.37071767335301331, -43.44691413872259744, -47.23470317516529349 ) ) ;
#4518=CARTESIAN_POINT ( 'NONE',  ( 54.67056220863920402, -47.85029607447599886, -26.56517469137810039 ) ) ;
#4520=CARTESIAN_POINT ( 'NONE',  ( 10.69486856911679773, -64.90650667235888704, -18.00056245200230265 ) ) ;
#4521=CARTESIAN_POINT ( 'NONE',  ( 50.92222208382837323, -35.35889331638581012, -76.36000770886168709 ) ) ;
#4522=CARTESIAN_POINT ( 'NONE',  ( 57.35094531453410127, 19.00534567308480050, -52.73804475687700233 ) ) ;
#4524=DIRECTION ( 'NONE',  ( 0.000000000000000000, 1.000000000000000000, 0.000000000000000000 ) ) ;
#4526=CARTESIAN_POINT ( 'NONE',  ( -11.32734370190460105, -41.88171845330919751, -6.430192534648670133 ) ) ;
#4527=CARTESIAN_POINT ( 'NONE',  ( 47.36546503952629905, 23.43920771176249929, -54.65494689270030193 ) ) ;
#4530=CARTESIAN_POINT ( 'NONE',  ( 56.24183557072737472, 15.29150438182242944, -26.31651977536066767 ) ) ;
#4531=CARTESIAN_POINT ( 'NONE',  ( 41.32046355873320209, 13.29656256355710120, -4.975096813130970297 ) ) ;
#4534=CARTESIAN_POINT ( 'NONE',  ( 53.97862732855089263, -49.20418162442920362, -49.10777757132959920 ) ) ;
#4538=CARTESIAN_POINT ( 'NONE',  ( 17.35260714571270313, -52.98224883304730071, -76.14999999999999147 ) ) ;
#4542=FACE_BOUND ( 'NONE', #42157, .T. ) ;
#4545=CARTESIAN_POINT ( 'NONE',  ( 10.14752524939349954, 32.07972278140049838, -45.99340881354279986 ) ) ;
#4547=CARTESIAN_POINT ( 'NONE',  ( 68.11938491324369238, -30.76296629286689921, -18.02961409148510086 ) ) ;
#4548=ORIENTED_EDGE ( 'NONE', *, *, #51697, .T. ) ;
#4549=EDGE_CURVE ( 'NONE', #4830, #40276, #37563, .T. ) ;
#4550=CARTESIAN_POINT ( 'NONE',  ( 18.67864726532610220, 20.47004600267149854, -74.90176971618339508 ) ) ;
#4553=VECTOR ( 'NONE', #12928, 1000.000000000000000 ) ;
#4555=ORIENTED_EDGE ( 'NONE', *, *, #12898, .F. ) ;
#4556=CARTESIAN_POINT ( 'NONE',  ( 10.69868903310229946, -63.71459361368848562, -45.45668842281379796 ) ) ;
#4561=CARTESIAN_POINT ( 'NONE',  ( 75.25805505272104767, 3.492023333372584304, -12.32941048424839714 ) ) ;
#4563=ORIENTED_EDGE ( 'NONE', *, *, #42965, .F. ) ;
#4564=CARTESIAN_POINT ( 'NONE',  ( 11.27243636593874321, -64.25380594475855389, -24.07146289791958083 ) ) ;
#4565=CARTESIAN_POINT ( 'NONE',  ( 51.67587649748470113, 2.735120682347050192, -77.01363636363508647 ) ) ;
#4566=ORIENTED_EDGE ( 'NONE', *, *, #27452, .F. ) ;
#4569=DIRECTION ( 'NONE',  ( 0.000000000000000000, 0.000000000000000000, 1.000000000000000000 ) ) ;
#4570=CARTESIAN_POINT ( 'NONE',  ( 72.83796717360608852, 13.88381330399790059, -14.37527876787380166 ) ) ;
#4571=CARTESIAN_POINT ( 'NONE',  ( 46.77197036051299506, 13.96716929081839886, -8.919993557679239515 ) ) ;
#4572=AXIS2_PLACEMENT_3D ( 'NONE', #20874, #40799, #13047 ) ;
#4574=CARTESIAN_POINT ( 'NONE',  ( -7.653322383143519758, 14.02129102275489991, -4.959142628649059859 ) ) ;
#4575=CARTESIAN_POINT ( 'NONE',  ( 9.849809295681199117, -62.03066548993875529, -13.59693312241669538 ) ) ;
#4576=CARTESIAN_POINT ( 'NONE',  ( 61.29464672451849339, 13.96904609170759848, -27.75181424375799821 ) ) ;
#4579=CARTESIAN_POINT ( 'NONE',  ( 60.34379256561150129, 14.63564648314799932, -47.72732608210890248 ) ) ;
#4580=EDGE_CURVE ( 'NONE', #30985, #23531, #19208, .T. ) ;
#4581=VECTOR ( 'NONE', #6997, 1000.000000000000000 ) ;
#4583=CARTESIAN_POINT ( 'NONE',  ( 54.17308945005400034, -50.61618894467930119, -77.01198594373980200 ) ) ;
#4586=DIRECTION ( 'NONE',  ( -0.6209860917175333839, 0.7838215829468996310, 0.000000000000000000 ) ) ;
#4587=CARTESIAN_POINT ( 'NONE',  ( 47.13701186032770352, 23.47047141344530274, -74.81156593794960941 ) ) ;
#4588=CARTESIAN_POINT ( 'NONE',  ( 49.54719217692459665, -53.70731863405879380, -54.90723160129140012 ) ) ;
#4594=EDGE_CURVE ( 'NONE', #21370, #1802, #16307, .T. ) ;
#4598=CARTESIAN_POINT ( 'NONE',  ( 84.44784216359251161, -43.11618894467930119, -47.47585302082339354 ) ) ;
#4599=CARTESIAN_POINT ( 'NONE',  ( 60.68483835214470190, -45.58309487373249880, -47.38195381330299938 ) ) ;
#4600=CARTESIAN_POINT ( 'NONE',  ( 56.91872540560049742, 19.41123227373109827, -53.86107397111689465 ) ) ;
#4601=CARTESIAN_POINT ( 'NONE',  ( 53.58978845500833188, -43.47732832942402581, -7.400799757652920974 ) ) ;
#4605=CARTESIAN_POINT ( 'NONE',  ( 57.34776335324270491, 14.57942837581910034, -26.27178905609630277 ) ) ;
#4607=ORIENTED_EDGE ( 'NONE', *, *, #42486, .T. ) ;
#4608=CARTESIAN_POINT ( 'NONE',  ( 84.40405423732200063, -43.50691743144619750, -47.38850513265820297 ) ) ;
#4611=ORIENTED_EDGE ( 'NONE', *, *, #18736, .F. ) ;
#4615=CARTESIAN_POINT ( 'NONE',  ( 53.42052211308229914, -49.46494215952650109, -49.21491387939300211 ) ) ;
#4616=LINE ( 'NONE', #20587, #47502 ) ;
#4617=AXIS2_PLACEMENT_3D ( 'NONE', #27838, #18951, #35190 ) ;
#4618=CARTESIAN_POINT ( 'NONE',  ( 76.44636317954351057, -6.604856247326271301, -12.99628919329122567 ) ) ;
#4620=CARTESIAN_POINT ( 'NONE',  ( 49.93407130271199890, -53.44037199461649834, -54.35262932774689659 ) ) ;
#4623=CARTESIAN_POINT ( 'NONE',  ( 16.13393739769620083, -15.61618894467929941, -15.65000000000000036 ) ) ;
#4624=CARTESIAN_POINT ( 'NONE',  ( 56.39270785951039500, 19.29512406318060158, -52.86271188469099513 ) ) ;
#4627=CARTESIAN_POINT ( 'NONE',  ( 61.88703750214839516, -0.1196547126231959912, -16.64423871873319882 ) ) ;
#4629=FACE_OUTER_BOUND ( 'NONE', #21935, .T. ) ;
#4630=CARTESIAN_POINT ( 'NONE',  ( 52.62506682249000534, -50.12296729442330445, -77.17021719677750013 ) ) ;
#4632=CARTESIAN_POINT ( 'NONE',  ( 83.07525789764410717, -45.50438969202907913, -47.60488146813197829 ) ) ;
#4635=DIRECTION ( 'NONE',  ( 1.000000000000000000, 0.000000000000000000, 0.000000000000000000 ) ) ;
#4636=CARTESIAN_POINT ( 'NONE',  ( 43.46307289448600386, -43.09202836464690023, -4.765184494693460060 ) ) ;
#4637=CARTESIAN_POINT ( 'NONE',  ( 18.46789571041282230, -51.27714561189082332, -15.70464893408844276 ) ) ;
#4638=CARTESIAN_POINT ( 'NONE',  ( 56.07568387335299320, 13.88381105532070059, -14.74720100809580003 ) ) ;
#4641=VECTOR ( 'NONE', #24025, 1000.000000000000000 ) ;
#4645=CARTESIAN_POINT ( 'NONE',  ( 14.15218391821419885, -52.24722748763079494, -75.79330468503940210 ) ) ;
#4647=CARTESIAN_POINT ( 'NONE',  ( 47.28316422028650123, -54.73279202814679678, -54.73281782041389931 ) ) ;
#4649=EDGE_CURVE ( 'NONE', #17198, #22850, #10005, .T. ) ;
#4652=CARTESIAN_POINT ( 'NONE',  ( 61.01465046515617274, -45.45355287326128746, -47.35110780635755390 ) ) ;
#4655=EDGE_CURVE ( 'NONE', #14522, #39228, #39303, .T. ) ;
#4661=CARTESIAN_POINT ( 'NONE',  ( 43.60412366721264732, 12.47234831454305848, -5.064848483119741118 ) ) ;
#4662=CARTESIAN_POINT ( 'NONE',  ( 48.40438293219020238, 22.95961779500990119, -55.05471046037709471 ) ) ;
#4663=ORIENTED_EDGE ( 'NONE', *, *, #43243, .F. ) ;
#4666=CARTESIAN_POINT ( 'NONE',  ( 82.81464131963001307, 11.88381105532070059, -49.28546657628889704 ) ) ;
#4668=CARTESIAN_POINT ( 'NONE',  ( 14.16379049631229847, 19.89932139981819859, -22.70798728939849909 ) ) ;
#4669=EDGE_CURVE ( 'NONE', #17870, #23355, #3788, .T. ) ;
#4670=CARTESIAN_POINT ( 'NONE',  ( 83.66217889154638954, 13.27350842653780028, -46.56966809452239886 ) ) ;
#4671=CARTESIAN_POINT ( 'NONE',  ( 55.57695098842009429, 15.27039860521809977, -25.90100721923549898 ) ) ;
#4673=LINE ( 'NONE', #25856, #43488 ) ;
#4674=CARTESIAN_POINT ( 'NONE',  ( 54.68760425043940643, -45.72106579749050326, -15.47702710567550000 ) ) ;
#4677=VERTEX_POINT ( 'NONE', #1197 ) ;
#4679=ORIENTED_EDGE ( 'NONE', *, *, #9772, .F. ) ;
#4680=CARTESIAN_POINT ( 'NONE',  ( 12.17742765526699955, -65.07456428805339499, -16.46016921340210004 ) ) ;
#4681=CARTESIAN_POINT ( 'NONE',  ( 9.991756373883710296, 32.50750339410230083, -46.24817865174940579 ) ) ;
#4682=CARTESIAN_POINT ( 'NONE',  ( 61.48314149772338766, -45.36441574363837503, -47.33726207365202043 ) ) ;
#4683=SHAPE_REPRESENTATION ( 'Swivel Caster Main Housing', ( #20940 ), #5952 ) ;
#4684=CARTESIAN_POINT ( 'NONE',  ( 52.44527164998969937, -50.16109774121770215, -49.63631393125859859 ) ) ;
#4685=CARTESIAN_POINT ( 'NONE',  ( 38.13393739769620083, -15.61618894467929941, -11.65000000000000036 ) ) ;
#4686=AXIS2_PLACEMENT_3D ( 'NONE', #42969, #7065, #31135 ) ;
#4687=EDGE_LOOP ( 'NONE', ( #16161, #11162, #14067, #13168, #7804, #45026, #23795, #41306, #40315, #4026, #17541, #8817, #48344 ) ) ;
#4690=CARTESIAN_POINT ( 'NONE',  ( 11.10555363379370064, -63.31361069873520364, -44.25268286828919884 ) ) ;
#4691=DIRECTION ( 'NONE',  ( 1.000000000000000000, 0.000000000000000000, 0.000000000000000000 ) ) ;
#4693=CARTESIAN_POINT ( 'NONE',  ( 50.32395457461500143, -49.73758701539929916, -76.14999999999999147 ) ) ;
#4696=FACE_OUTER_BOUND ( 'NONE', #37476, .T. ) ;
#4701=EDGE_CURVE ( 'NONE', #15133, #12469, #22280, .T. ) ;
#4703=CARTESIAN_POINT ( 'NONE',  ( 52.84698449767209638, -49.68627056466029757, -48.96050383872009348 ) ) ;
#4705=CARTESIAN_POINT ( 'NONE',  ( 54.83350709104630027, 19.86271698526680041, -75.27563804332019970 ) ) ;
#4706=CARTESIAN_POINT ( 'NONE',  ( 46.74688800147040268, -53.53748093643939399, -76.01521976086429788 ) ) ;
#4710=CARTESIAN_POINT ( 'NONE',  ( 53.55249253148920019, -49.41945639387319744, -49.22526694372639611 ) ) ;
#4712=CARTESIAN_POINT ( 'NONE',  ( 54.63655381128389621, -48.05296878824569973, -26.73577887340519865 ) ) ;
#4714=CARTESIAN_POINT ( 'NONE',  ( 46.39783855510299304, 21.74930147051340157, -76.14870548336060097 ) ) ;
#4715=CARTESIAN_POINT ( 'NONE',  ( 19.75782039012221603, -54.33761034372771093, -17.50926154277789948 ) ) ;
#4716=CARTESIAN_POINT ( 'NONE',  ( 63.02122824129657630, -31.65172625870799195, -17.11446970408973201 ) ) ;
#4717=EDGE_CURVE ( 'NONE', #39634, #49564, #51006, .T. ) ;
#4718=CARTESIAN_POINT ( 'NONE',  ( 12.26572565712310059, 33.38422248552610228, -15.83807272485699968 ) ) ;
#4722=CIRCLE ( 'NONE', #30557, 2.000000000000001776 ) ;
#4726=CARTESIAN_POINT ( 'NONE',  ( 61.45294235306059960, 13.92837752391369932, -46.41419044209769851 ) ) ;
#4728=CARTESIAN_POINT ( 'NONE',  ( -18.46512919571979694, -52.41504996104650616, -54.23003070569399853 ) ) ;
#4729=ORIENTED_EDGE ( 'NONE', *, *, #45631, .T. ) ;
#4730=CARTESIAN_POINT ( 'NONE',  ( 52.82298710676560205, -49.66654477726660843, -48.69818472591780534 ) ) ;
#4731=DIRECTION ( 'NONE',  ( -0.3294064756440890918, 0.9441882088883233326, 0.000000000000000000 ) ) ;
#4732=CARTESIAN_POINT ( 'NONE',  ( 48.31044912363459787, -54.24991223489359982, -55.31379430672990338 ) ) ;
#4733=CARTESIAN_POINT ( 'NONE',  ( 56.41325250503939515, 14.84688818548599976, -26.18647423063130120 ) ) ;
#4735=CARTESIAN_POINT ( 'NONE',  ( 51.01140993929779910, 18.25269707675350261, -76.32135044011170066 ) ) ;
#4736=CARTESIAN_POINT ( 'NONE',  ( 53.19189966491499888, 18.24357405876429894, -48.89717422996369578 ) ) ;
#4738=CYLINDRICAL_SURFACE ( 'NONE', #15871, 1.999999999999999112 ) ;
#4744=CARTESIAN_POINT ( 'NONE',  ( 47.56760501474590086, -54.55410667736709485, -54.80386054826420406 ) ) ;
#4747=CARTESIAN_POINT ( 'NONE',  ( 42.29536634374500181, 11.94537196368429832, -3.241362035758810212 ) ) ;
#4748=CARTESIAN_POINT ( 'NONE',  ( 57.15466225109279463, 18.99064698095470405, -52.70648794892409938 ) ) ;
#4752=AXIS2_PLACEMENT_3D ( 'NONE', #37533, #25205, #40949 ) ;
#4753=DIRECTION ( 'NONE',  ( -1.000000000000000000, 0.000000000000000000, 0.000000000000000000 ) ) ;
#4756=VERTEX_POINT ( 'NONE', #30515 ) ;
#4759=ORIENTED_EDGE ( 'NONE', *, *, #8913, .F. ) ;
#4760=CARTESIAN_POINT ( 'NONE',  ( 12.10067367342139910, -65.23675915737399578, -45.96376737918109967 ) ) ;
#4763=CARTESIAN_POINT ( 'NONE',  ( 52.64727086977080006, 19.37578117508699904, -76.52291747780199671 ) ) ;
#4768=CARTESIAN_POINT ( 'NONE',  ( 37.63393739769591662, -15.61618894467939711, -10.44999999999999929 ) ) ;
#4769=EDGE_CURVE ( 'NONE', #31549, #43692, #43204, .T. ) ;
#4772=CARTESIAN_POINT ( 'NONE',  ( 16.13393739769620083, -15.61618894467929941, 8.349999999999999645 ) ) ;
#4775=VERTEX_POINT ( 'NONE', #42069 ) ;
#4776=CARTESIAN_POINT ( 'NONE',  ( 12.55603873008839955, -65.48958817767790208, -23.08740377524289755 ) ) ;
#4778=CARTESIAN_POINT ( 'NONE',  ( 40.72222893655849418, 14.05123486567899960, -5.660115700743969747 ) ) ;
#4779=CARTESIAN_POINT ( 'NONE',  ( 14.80888071766799996, 21.59920855125570327, -76.12873484255680978 ) ) ;
#4781=CARTESIAN_POINT ( 'NONE',  ( 83.71081252132769634, -44.47204336813729952, -46.63777445865510174 ) ) ;
#4782=CARTESIAN_POINT ( 'NONE',  ( 10.96947365134820629, 33.83317469089056573, -17.60046481885576952 ) ) ;
#4785=EDGE_LOOP ( 'NONE', ( #7919, #39560 ) ) ;
#4786=CARTESIAN_POINT ( 'NONE',  ( 52.93377756553670110, -49.56154788943119627, -27.74629457784710240 ) ) ;
#4787=CARTESIAN_POINT ( 'NONE',  ( 14.30960224998150032, -51.11619537004450109, -22.40439468542479773 ) ) ;
#4788=CARTESIAN_POINT ( 'NONE',  ( 76.10260541693969571, 10.92673604474729920, -13.51091013548749942 ) ) ;
#4789=CARTESIAN_POINT ( 'NONE',  ( 11.13393739769619906, 24.07008072128950005, -24.15000000000000213 ) ) ;
#4791=DIRECTION ( 'NONE',  ( -1.000000000000000000, 0.000000000000000000, 0.000000000000000000 ) ) ;
#4792=ORIENTED_EDGE ( 'NONE', *, *, #47727, .T. ) ;
#4793=CARTESIAN_POINT ( 'NONE',  ( -3.467811284925150339, -48.61559609778869628, -5.474417138839919872 ) ) ;
#4794=CARTESIAN_POINT ( 'NONE',  ( 47.37190771255519905, 23.43321186050379978, -54.63786165043430287 ) ) ;
#4799=CARTESIAN_POINT ( 'NONE',  ( 11.08386349027339968, 33.85827347894340278, -17.36951630520609768 ) ) ;
#4803=CARTESIAN_POINT ( 'NONE',  ( 59.53476406250169362, -46.29126728519970158, -47.84522406268589378 ) ) ;
#4804=CARTESIAN_POINT ( 'NONE',  ( 68.13393739769841773, -50.61618894467878960, -73.25000000000220268 ) ) ;
#4806=CARTESIAN_POINT ( 'NONE',  ( 17.48526846705000182, -52.41676442117930179, -76.03098605356829864 ) ) ;
#4807=CARTESIAN_POINT ( 'NONE',  ( 0.8878875035446542885, -15.61618894467929763, -7.101316701949489385 ) ) ;
#4808=CARTESIAN_POINT ( 'NONE',  ( 11.93488811383480019, -65.43955691952199061, -17.90291648171000105 ) ) ;
#4809=CARTESIAN_POINT ( 'NONE',  ( 48.37121793203289855, 13.88381105532070059, -9.155085387781159767 ) ) ;
#4811=CARTESIAN_POINT ( 'NONE',  ( 68.13393739769620083, 16.88381105532069881, -67.99999999999998579 ) ) ;
#4812=CARTESIAN_POINT ( 'NONE',  ( 9.737940527390820833, 31.99035019930730073, -46.29782643814709786 ) ) ;
#4813=CARTESIAN_POINT ( 'NONE',  ( 11.13393739769619906, -63.11543068638779630, -43.74348518090240390 ) ) ;
#4814=CARTESIAN_POINT ( 'NONE',  ( 67.77843577628229355, -31.93894155608530028, -18.45138847496160039 ) ) ;
#4816=CARTESIAN_POINT ( 'NONE',  ( 18.41048271170079786, 20.19843276291189937, -74.93307507168100301 ) ) ;
#4819=ORIENTED_EDGE ( 'NONE', *, *, #513, .T. ) ;
#4820=CARTESIAN_POINT ( 'NONE',  ( 11.03295843064409887, -64.45566759814450108, -45.85509474990620049 ) ) ;
#4821=DIRECTION ( 'NONE',  ( 0.3294064756441309472, 0.9441882088883087887, 3.053113317719179500E-16 ) ) ;
#4824=CARTESIAN_POINT ( 'NONE',  ( 61.65692969715129834, 13.95730600902359875, -46.91096927817520168 ) ) ;
#4825=B_SPLINE_CURVE_WITH_KNOTS ( 'NONE', 3,
 ( #12810, #20902, #49489, #24557, #24300, #29030, #48973, #40316 ),
 .UNSPECIFIED., .F., .F.,
 ( 4, 2, 2, 4 ),
 ( 0.000000000000000000, 0.1882768039131864080, 0.3749999999922790650, 0.5000003605016758446 ),
 .UNSPECIFIED. ) ;
#4826=ORIENTED_EDGE ( 'NONE', *, *, #40807, .T. ) ;
#4830=VERTEX_POINT ( 'NONE', #46538 ) ;
#4831=CARTESIAN_POINT ( 'NONE',  ( 47.78347364068760328, -46.15536227680040327, -10.88058668116050143 ) ) ;
#4833=CARTESIAN_POINT ( 'NONE',  ( 61.51122975691189509, -45.14516155341349446, -46.37203261889099792 ) ) ;
#4836=ORIENTED_EDGE ( 'NONE', *, *, #3385, .T. ) ;
#4838=DIRECTION ( 'NONE',  ( 0.000000000000000000, 0.000000000000000000, 1.000000000000000000 ) ) ;
#4839=CARTESIAN_POINT ( 'NONE',  ( 62.88393739769619373, 11.88381105532070059, -84.94863984844531046 ) ) ;
#4841=AXIS2_PLACEMENT_3D ( 'NONE', #7105, #43008, #22283 ) ;
#4842=CARTESIAN_POINT ( 'NONE',  ( 45.14275768348990425, 14.67924369193939960, -8.929573269535710622 ) ) ;
#4845=CARTESIAN_POINT ( 'NONE',  ( 11.53606103740170674, 24.11867657901759188, -21.73577486392030167 ) ) ;
#4846=CARTESIAN_POINT ( 'NONE',  ( 55.57909954016480469, 14.75263197375267765, -16.80477431159009782 ) ) ;
#4848=EDGE_CURVE ( 'NONE', #51191, #12580, #3940, .T. ) ;
#4849=ORIENTED_EDGE ( 'NONE', *, *, #13792, .F. ) ;
#4850=CARTESIAN_POINT ( 'NONE',  ( 58.92301001618189815, 15.23611622987800018, -47.52857555498080444 ) ) ;
#4851=CARTESIAN_POINT ( 'NONE',  ( 11.36895924000850044, 33.23916916644579800, -44.41074867359769485 ) ) ;
#4852=ADVANCED_FACE ( 'NONE', ( #45747 ), #51487, .T. ) ;
#4855=CARTESIAN_POINT ( 'NONE',  ( 48.42521416700790127, -56.37491125791819968, -74.14999999999999147 ) ) ;
#4858=CARTESIAN_POINT ( 'NONE',  ( 47.07822479275279903, 23.33748360234629970, -75.12259518105788914 ) ) ;
#4859=CARTESIAN_POINT ( 'NONE',  ( 48.84430051460839906, -53.91533838276139790, -54.66094892452610310 ) ) ;
#4860=CARTESIAN_POINT ( 'NONE',  ( -2.927827710953269769, 17.96742650791509988, -5.740515240579870060 ) ) ;
#4867=VERTEX_POINT ( 'NONE', #11401 ) ;
#4869=CARTESIAN_POINT ( 'NONE',  ( 61.23319982858109967, -45.48283502369449849, -47.51874276278909548 ) ) ;
#4871=CARTESIAN_POINT ( 'NONE',  ( 12.22498197106229867, 18.79317372273670017, -21.14999999999999858 ) ) ;
#4875=EDGE_LOOP ( 'NONE', ( #25712, #23871, #69, #2308 ) ) ;
#4876=CARTESIAN_POINT ( 'NONE',  ( 83.36355911687300591, -45.34682523223490591, -47.55049236202179230 ) ) ;
#4877=B_SPLINE_CURVE_WITH_KNOTS ( 'NONE', 3,
 ( #26076, #50208, #10639, #2507, #14820, #18488, #6187, #46288, #30527, #42870, #6705, #22662 ),
 .UNSPECIFIED., .F., .F.,
 ( 4, 1, 1, 1, 1, 1, 1, 1, 1, 4 ),
 ( 0.000000000000000000, 0.1111152296621469165, 0.2222304593242938331, 0.3333456889864405137, 0.4444609186485874441, 0.5555761483107353182, 0.6666913779728821376, 0.7778066076350290681, 0.8889218372971758875, 1.000000000000000000 ),
 .UNSPECIFIED. ) ;
#4878=ORIENTED_EDGE ( 'NONE', *, *, #11252, .T. ) ;
#4880=ORIENTED_EDGE ( 'NONE', *, *, #1937, .T. ) ;
#4882=CARTESIAN_POINT ( 'NONE',  ( 52.90396775623960224, -49.66420589288500054, -49.02012042725169749 ) ) ;
#4883=CARTESIAN_POINT ( 'NONE',  ( 60.84441632817985379, 14.22943762888878005, -47.04815909370046256 ) ) ;
#4884=CARTESIAN_POINT ( 'NONE',  ( 76.40750186186460269, -10.73206780545592487, -12.82882999751005393 ) ) ;
#4885=CARTESIAN_POINT ( 'NONE',  ( 55.75774054045910333, -51.07765005165450134, -53.93517881746969778 ) ) ;
#4887=EDGE_LOOP ( 'NONE', ( #26863, #36509, #18735, #27371 ) ) ;
#4888=CARTESIAN_POINT ( 'NONE',  ( 49.00556831830410687, 22.49847617784580223, -54.36652964084350259 ) ) ;
#4892=CARTESIAN_POINT ( 'NONE',  ( 8.792282373222519709, -63.15413706425750462, -46.67070408018280148 ) ) ;
#4893=CARTESIAN_POINT ( 'NONE',  ( 62.74890333807501008, 0.2393393690175290023, -16.93594147870210165 ) ) ;
#4897=CARTESIAN_POINT ( 'NONE',  ( -2.235188499061480538, 18.67038793989973655, -5.998756751858821623 ) ) ;
#4898=CARTESIAN_POINT ( 'NONE',  ( -5.833909485681573415, -15.61618894467930119, 5.729250452415290518 ) ) ;
#4900=CARTESIAN_POINT ( 'NONE',  ( 60.42907245139279837, 14.44704792307930141, -47.19657908371780053 ) ) ;
#4903=CARTESIAN_POINT ( 'NONE',  ( 41.18706455731800276, -44.61555498641789796, -5.042666981957509620 ) ) ;
#4904=CARTESIAN_POINT ( 'NONE',  ( 17.92370450347650035, -51.11618894467930119, -15.67980085856620143 ) ) ;
#4905=CARTESIAN_POINT ( 'NONE',  ( 68.13393739769840352, -50.61618894467879670, -73.25000000000220268 ) ) ;
#4911=CARTESIAN_POINT ( 'NONE',  ( 66.02286391504910057, 1.436401451597350221, -18.53624686056960158 ) ) ;
#4913=CARTESIAN_POINT ( 'NONE',  ( 14.54748625655889960, -51.81226317974009987, -75.66803551354809088 ) ) ;
#4914=CARTESIAN_POINT ( 'NONE',  ( 47.34550006616409945, -54.68667022654160803, -54.66557013501159901 ) ) ;
#4915=CIRCLE ( 'NONE', #16622, 2.000000000000000888 ) ;
#4916=EDGE_CURVE ( 'NONE', #44194, #35613, #4980, .T. ) ;
#4918=CARTESIAN_POINT ( 'NONE',  ( 84.44784216359251161, 11.88381105532070059, -47.47585302082339354 ) ) ;
#4919=CARTESIAN_POINT ( 'NONE',  ( 61.03029461452958770, -45.45771770995002470, -47.37445190977187082 ) ) ;
#4921=CARTESIAN_POINT ( 'NONE',  ( 57.34776335324270491, 14.57942837581910034, -26.27178905609630277 ) ) ;
#4922=CARTESIAN_POINT ( 'NONE',  ( 11.90332973438740005, 34.20450943514180153, -18.04110290859920340 ) ) ;
#4924=CARTESIAN_POINT ( 'NONE',  ( -5.256770087461370089, -47.44903047538170426, -5.577592548843699483 ) ) ;
#4926=CARTESIAN_POINT ( 'NONE',  ( 48.47801679748619819, 22.94615690571940192, -55.28610629251650010 ) ) ;
#4927=ORIENTED_EDGE ( 'NONE', *, *, #35785, .T. ) ;
#4930=CYLINDRICAL_SURFACE ( 'NONE', #32849, 1.999999999999997113 ) ;
#4933=CARTESIAN_POINT ( 'NONE',  ( 82.78852321480360388, 13.78813943271330089, -46.36931865296670452 ) ) ;
#4934=CARTESIAN_POINT ( 'NONE',  ( 55.99380635880790180, 14.75626973559459998, -25.81789497692459889 ) ) ;
#4937=CARTESIAN_POINT ( 'NONE',  ( 3.755977383759285360, -24.60930330475428462, -6.649999999999999467 ) ) ;
#4940=ORIENTED_EDGE ( 'NONE', *, *, #28237, .F. ) ;
#4941=CARTESIAN_POINT ( 'NONE',  ( 11.47551314106880049, -64.97235711416220738, -16.61573023122599935 ) ) ;
#4942=CARTESIAN_POINT ( 'NONE',  ( 10.93332210773090019, 32.19736207414519669, -44.88523382134809481 ) ) ;
#4944=CARTESIAN_POINT ( 'NONE',  ( 49.68126013218329717, -52.84574376966489950, -52.91783866924430413 ) ) ;
#4950=CARTESIAN_POINT ( 'NONE',  ( 8.133937397696209715, 28.10308010054979988, -21.14999999999999858 ) ) ;
#4951=CARTESIAN_POINT ( 'NONE',  ( 54.50979703755457706, 16.93725552086487340, -26.78135896009203520 ) ) ;
#4954=CARTESIAN_POINT ( 'NONE',  ( 49.26469448778690463, 22.42219932542450067, -54.34642017524310376 ) ) ;
#4956=CARTESIAN_POINT ( 'NONE',  ( 50.30621308613430642, -48.61618509234789798, -76.16272939236809236 ) ) ;
#4959=ORIENTED_EDGE ( 'NONE', *, *, #40157, .F. ) ;
#4964=FACE_OUTER_BOUND ( 'NONE', #1226, .T. ) ;
#4968=CARTESIAN_POINT ( 'NONE',  ( 14.12377191986709946, -51.13901785078579820, -22.60596972032639940 ) ) ;
#4969=CARTESIAN_POINT ( 'NONE',  ( 56.57215025654439700, 19.50075534991569981, -74.14931637192330527 ) ) ;
#4970=CARTESIAN_POINT ( 'NONE',  ( 46.79040325823919488, -53.60681267845629350, -75.98188598372340152 ) ) ;
#4972=CARTESIAN_POINT ( 'NONE',  ( 55.38284522413690070, 14.79968809196030044, -16.52949576727229797 ) ) ;
#4973=CARTESIAN_POINT ( 'NONE',  ( 57.25859902730019968, -50.61616371649569857, -53.75766468090039751 ) ) ;
#4974=EDGE_CURVE ( 'NONE', #34590, #34588, #34256, .T. ) ;
#4977=CARTESIAN_POINT ( 'NONE',  ( 47.18938042008029754, 23.12896336020899923, -75.29141078596350667 ) ) ;
#4980=B_SPLINE_CURVE_WITH_KNOTS ( 'NONE', 3,
 ( #16089, #39689, #7462, #23416, #19763, #27363 ),
 .UNSPECIFIED., .F., .F.,
 ( 4, 1, 1, 4 ),
 ( 0.000000000000000000, 0.3333333332445601038, 0.6666666664890206206, 1.000000000000000000 ),
 .UNSPECIFIED. ) ;
#4981=VECTOR ( 'NONE', #38444, 1000.000000000000000 ) ;
#4982=CARTESIAN_POINT ( 'NONE',  ( 58.92073396209919878, -28.11618894467929763, -15.65000000000000036 ) ) ;
#4985=VECTOR ( 'NONE', #43340, 1000.000000000000000 ) ;
#4986=VECTOR ( 'NONE', #39113, 1000.000000000000000 ) ;
#4988=AXIS2_PLACEMENT_3D ( 'NONE', #39937, #36243, #4033 ) ;
#4996=CARTESIAN_POINT ( 'NONE',  ( -12.67430703014960081, -56.52710054866469847, -51.91878751810809689 ) ) ;
#4999=CARTESIAN_POINT ( 'NONE',  ( 53.32368397926410353, -49.40866304911550344, -48.89504827794529973 ) ) ;
#5000=ADVANCED_FACE ( 'NONE', ( #20005 ), #40812, .T. ) ;
#5003=CARTESIAN_POINT ( 'NONE',  ( 56.72799476710019917, 14.59936194371569940, -26.16780803237229946 ) ) ;
#5005=CARTESIAN_POINT ( 'NONE',  ( 51.38507389488840005, 19.29610779897900130, -76.23533787841168419 ) ) ;
#5006=CARTESIAN_POINT ( 'NONE',  ( 52.98874186162730382, 18.36389844763469625, -48.96317217183759851 ) ) ;
#5008=CARTESIAN_POINT ( 'NONE',  ( 42.11778985043759604, -43.34518763914159933, -3.278435071288769542 ) ) ;
#5009=CARTESIAN_POINT ( 'NONE',  ( 72.23296425804250021, -44.31211235131849691, -12.76840841843079843 ) ) ;
#5010=ORIENTED_EDGE ( 'NONE', *, *, #14896, .F. ) ;
#5012=ORIENTED_EDGE ( 'NONE', *, *, #50529, .T. ) ;
#5014=CARTESIAN_POINT ( 'NONE',  ( 47.45216272503800070, -54.62528982994189874, -54.83349227997879893 ) ) ;
#5015=CARTESIAN_POINT ( 'NONE',  ( -11.32734372065470119, 10.64934054434680100, -6.430561461456250072 ) ) ;
#5017=FACE_OUTER_BOUND ( 'NONE', #23671, .T. ) ;
#5021=CARTESIAN_POINT ( 'NONE',  ( 66.72561048531049721, -33.11618894467940066, -20.65000000000000213 ) ) ;
#5023=ORIENTED_EDGE ( 'NONE', *, *, #45322, .T. ) ;
#5024=ORIENTED_EDGE ( 'NONE', *, *, #8621, .F. ) ;
#5025=CARTESIAN_POINT ( 'NONE',  ( 8.797781558458089179, -63.18317285479920997, -46.67022811708060459 ) ) ;
#5028=VERTEX_POINT ( 'NONE', #39120 ) ;
#5031=CARTESIAN_POINT ( 'NONE',  ( 56.46551622901163370, 19.54378670599449919, -74.28390251812621159 ) ) ;
#5033=CARTESIAN_POINT ( 'NONE',  ( 51.81517742707350749, 18.95102032179380203, -76.50774528508080152 ) ) ;
#5036=CARTESIAN_POINT ( 'NONE',  ( 61.20224358684065180, 14.04196190244037368, -46.71246603851685109 ) ) ;
#5038=CARTESIAN_POINT ( 'NONE',  ( 60.34379259250669492, 14.63564649040839960, -47.72732609510669732 ) ) ;
#5040=ADVANCED_FACE ( 'NONE', ( #11339 ), #23102, .T. ) ;
#5043=DIRECTION ( 'NONE',  ( 0.7800418122827239564, 0.000000000000000000, -0.6257273935913973961 ) ) ;
#5047=CARTESIAN_POINT ( 'NONE',  ( 12.17383947079069983, -65.46069624394010589, -22.71972408461549975 ) ) ;
#5050=CARTESIAN_POINT ( 'NONE',  ( 14.56816760167549951, 21.04130707244170040, -75.96082109999758814 ) ) ;
#5053=CARTESIAN_POINT ( 'NONE',  ( 83.45793240077840380, -44.68224995836130375, -46.53859470524309216 ) ) ;
#5055=ORIENTED_EDGE ( 'NONE', *, *, #42227, .T. ) ;
#5056=CARTESIAN_POINT ( 'NONE',  ( 53.38096221179280576, -49.16063623257220172, -27.30168355108260059 ) ) ;
#5057=CARTESIAN_POINT ( 'NONE',  ( 16.19818216287970003, -51.11138666575850209, -21.03492549854079741 ) ) ;
#5062=VERTEX_POINT ( 'NONE', #11861 ) ;
#5063=AXIS2_PLACEMENT_3D ( 'NONE', #28786, #12304, #47952 ) ;
#5064=CARTESIAN_POINT ( 'NONE',  ( -7.435201089644969841, -45.47238293868839776, -5.298195296883859484 ) ) ;
#5066=CARTESIAN_POINT ( 'NONE',  ( 47.28790744643029598, 23.49698345083890061, -54.73855453374710578 ) ) ;
#5069=VECTOR ( 'NONE', #48799, 1000.000000000000114 ) ;
#5072=CARTESIAN_POINT ( 'NONE',  ( 42.35079399890570784, 13.08996448889170061, -5.113119482875689847 ) ) ;
#5074=FACE_OUTER_BOUND ( 'NONE', #22721, .T. ) ;
#5076=CARTESIAN_POINT ( 'NONE',  ( 60.34434042017240074, -45.86867586488080661, -47.72879939364779744 ) ) ;
#5077=FACE_OUTER_BOUND ( 'NONE', #29029, .T. ) ;
#5079=CARTESIAN_POINT ( 'NONE',  ( 52.99344130519229878, 21.02275823560599832, -54.37359777462930310 ) ) ;
#5082=LINE ( 'NONE', #21294, #34116 ) ;
#5085=CARTESIAN_POINT ( 'NONE',  ( 10.13537795804320041, 31.89605224914739878, -45.99742856566899718 ) ) ;
#5089=CARTESIAN_POINT ( 'NONE',  ( 17.80738288411419745, 20.21128881784739661, -75.25165125838280744 ) ) ;
#5092=CARTESIAN_POINT ( 'NONE',  ( 49.08512682873279687, 22.68755118111490177, -55.26163594736860318 ) ) ;
#5094=CARTESIAN_POINT ( 'NONE',  ( 10.51395742882619899, -64.02946666124979913, -45.97815992060260726 ) ) ;
#5095=CARTESIAN_POINT ( 'NONE',  ( 57.15508372626799627, -45.65320873106580279, -26.17772718789539965 ) ) ;
#5097=EDGE_CURVE ( 'NONE', #44163, #47510, #44344, .T. ) ;
#5098=B_SPLINE_CURVE_WITH_KNOTS ( 'NONE', 3,
 ( #49582, #6060, #33817, #36718, #45379, #5294, #25177, #49321 ),
 .UNSPECIFIED., .F., .F.,
 ( 4, 2, 2, 4 ),
 ( 0.000000000000000000, 0.1749999999962247588, 0.3749999999919103599, 0.4999997377388590292 ),
 .UNSPECIFIED. ) ;
#5099=CARTESIAN_POINT ( 'NONE',  ( 61.61622621241649966, 13.95300478508159969, -46.89001122893169793 ) ) ;
#5101=EDGE_LOOP ( 'NONE', ( #37784, #33545, #50537, #27702 ) ) ;
#5102=CARTESIAN_POINT ( 'NONE',  ( 85.26960572018148810, -50.03040250705240055, -53.60827425107920874 ) ) ;
#5104=CARTESIAN_POINT ( 'NONE',  ( 12.33251668000310808, 33.41328466589543922, -15.86092358591091589 ) ) ;
#5108=CARTESIAN_POINT ( 'NONE',  ( 58.54079899187081537, -45.63568207302990487, -26.46003400569485464 ) ) ;
#5110=ORIENTED_EDGE ( 'NONE', *, *, #23506, .F. ) ;
#5112=DIRECTION ( 'NONE',  ( 0.000000000000000000, 1.000000000000000000, 0.000000000000000000 ) ) ;
#5113=CARTESIAN_POINT ( 'NONE',  ( 46.68381635779479666, -53.67199518238830080, -75.98463753095340678 ) ) ;
#5115=CARTESIAN_POINT ( 'NONE',  ( 60.59736966202989805, 14.55571675506389973, -47.75487759591599968 ) ) ;
#5117=CARTESIAN_POINT ( 'NONE',  ( 50.27314737944030298, 14.74472902852030032, -12.51578207897900086 ) ) ;
#5119=CARTESIAN_POINT ( 'NONE',  ( -4.842671363392640593, 16.07518510873240203, -4.485484122326420575 ) ) ;
#5121=CARTESIAN_POINT ( 'NONE',  ( 59.45158862381180143, 14.23092646871359968, -26.67082509506299814 ) ) ;
#5124=CARTESIAN_POINT ( 'NONE',  ( 59.74618096160109815, 14.90151641663299920, -47.73567920125140063 ) ) ;
#5125=CARTESIAN_POINT ( 'NONE',  ( -10.65957727951819933, -41.24256659105780187, -4.264195539817489333 ) ) ;
#5129=CARTESIAN_POINT ( 'NONE',  ( 11.49562787870944014, 34.14054113714986016, -18.17421237829643843 ) ) ;
#5130=CARTESIAN_POINT ( 'NONE',  ( 47.16778299211050296, 23.48143463812749943, -74.72646181054710723 ) ) ;
#5131=CARTESIAN_POINT ( 'NONE',  ( 48.81910031065179822, -53.88745037611909794, -54.56221240745009737 ) ) ;
#5133=EDGE_CURVE ( 'NONE', #26643, #35688, #49380, .T. ) ;
#5134=CARTESIAN_POINT ( 'NONE',  ( 76.73547614042425380, -43.17979320943853594, -14.45192718277627009 ) ) ;
#5135=CARTESIAN_POINT ( 'NONE',  ( 65.70572778047942109, -32.85841247341685545, -18.95019540820560877 ) ) ;
#5138=ORIENTED_EDGE ( 'NONE', *, *, #13611, .T. ) ;
#5144=CARTESIAN_POINT ( 'NONE',  ( 60.55906510858309844, -45.72613536122689482, -47.62951512971719836 ) ) ;
#5145=DIRECTION ( 'NONE',  ( 0.000000000000000000, -1.000000000000000000, 0.000000000000000000 ) ) ;
#5153=CARTESIAN_POINT ( 'NONE',  ( 83.82044569750020457, -44.78926617021760848, -47.35730118573349756 ) ) ;
#5154=ORIENTED_EDGE ( 'NONE', *, *, #51140, .F. ) ;
#5157=CARTESIAN_POINT ( 'NONE',  ( 61.75020731935619267, -45.11618170104340209, -46.51046377108719554 ) ) ;
#5158=CARTESIAN_POINT ( 'NONE',  ( 76.43577037016747511, -7.494458964928895739, -12.95064323996461653 ) ) ;
#5159=LINE ( 'NONE', #21115, #49443 ) ;
#5160=ORIENTED_EDGE ( 'NONE', *, *, #15390, .F. ) ;
#5161=EDGE_LOOP ( 'NONE', ( #18099, #21194, #41304 ) ) ;
#5163=CARTESIAN_POINT ( 'NONE',  ( 11.63514989718968273, 34.14682459674944681, -22.51338914225708621 ) ) ;
#5165=CARTESIAN_POINT ( 'NONE',  ( 56.58636862632249631, 19.37200252008349821, -53.13121941621520250 ) ) ;
#5166=CARTESIAN_POINT ( 'NONE',  ( 10.64863409883700029, 32.21085600226960111, -23.66469670114080159 ) ) ;
#5172=CARTESIAN_POINT ( 'NONE',  ( -0.1957178007246416773, 20.73075855749606689, -6.909876211445776129 ) ) ;
#5173=CARTESIAN_POINT ( 'NONE',  ( 52.28361278957570590, -49.79955569159500328, -77.20042821566700297 ) ) ;
#5175=CARTESIAN_POINT ( 'NONE',  ( 60.75684423228010189, 14.27531910353349964, -47.09517711229599968 ) ) ;
#5178=CARTESIAN_POINT ( 'NONE',  ( 42.70540900715619870, 13.77437978117109907, -6.147237832590779938 ) ) ;
#5179=CARTESIAN_POINT ( 'NONE',  ( 42.63373764987009906, -44.09845193377589823, -5.023048285612619956 ) ) ;
#5180=CARTESIAN_POINT ( 'NONE',  ( 68.13393739769841773, -50.61618894467878960, -73.25000000000220268 ) ) ;
#5187=CARTESIAN_POINT ( 'NONE',  ( 67.77237649856910195, 1.249209544680260242, -19.08110282771260202 ) ) ;
#5189=CARTESIAN_POINT ( 'NONE',  ( 14.00496991351040066, -51.89834789502650381, -75.53980707817230211 ) ) ;
#5190=CARTESIAN_POINT ( 'NONE',  ( 57.34209066734109683, 19.16565926987989599, -53.00664426348080127 ) ) ;
#5192=CARTESIAN_POINT ( 'NONE',  ( 83.67474298203126182, 13.26187872094980946, -46.57587824071405436 ) ) ;
#5195=CARTESIAN_POINT ( 'NONE',  ( 55.89888397486434002, -45.90870921158190043, -17.63255904996966095 ) ) ;
#5200=CARTESIAN_POINT ( 'NONE',  ( 56.33973134792619675, 19.37458302847869973, -52.96823346731370208 ) ) ;
#5201=CARTESIAN_POINT ( 'NONE',  ( 48.72449300217610357, 22.67606569047629961, -54.53033886993310375 ) ) ;
#5202=ORIENTED_EDGE ( 'NONE', *, *, #42442, .T. ) ;
#5204=ORIENTED_EDGE ( 'NONE', *, *, #5633, .F. ) ;
#5205=FACE_OUTER_BOUND ( 'NONE', #21731, .T. ) ;
#5206=CARTESIAN_POINT ( 'NONE',  ( 53.29384558423090112, 19.31433099946569953, -48.47378032971769812 ) ) ;
#5207=DIRECTION ( 'NONE',  ( -0.8732394366197182567, 0.4872913772396111343, -1.665334536937735304E-16 ) ) ;
#5208=CARTESIAN_POINT ( 'NONE',  ( 83.82017571155999747, 13.44570198998940036, -47.23783155238629661 ) ) ;
#5209=CARTESIAN_POINT ( 'NONE',  ( 53.76692370360909479, 17.31591783857309963, -26.47372352232380166 ) ) ;
#5212=CARTESIAN_POINT ( 'NONE',  ( 57.05054250623780376, -45.11618894467940066, -16.05309365090189999 ) ) ;
#5213=CARTESIAN_POINT ( 'NONE',  ( 52.56521993351449851, 18.62941884369810097, -28.15000000000000213 ) ) ;
#5215=VERTEX_POINT ( 'NONE', #20456 ) ;
#5216=CARTESIAN_POINT ( 'NONE',  ( 12.06856799516239853, -65.14762389849769875, -16.61922514011519780 ) ) ;
#5217=CARTESIAN_POINT ( 'NONE',  ( 11.35079409783939930, 33.43282641247379416, -45.67788118199990066 ) ) ;
#5219=CIRCLE ( 'NONE', #47894, 1.000000000000003109 ) ;
#5220=CARTESIAN_POINT ( 'NONE',  ( 49.31205535909459314, -53.03485293375030096, -52.41062034357430122 ) ) ;
#5223=ORIENTED_EDGE ( 'NONE', *, *, #23856, .T. ) ;
#5224=EDGE_CURVE ( 'NONE', #40777, #11419, #40652, .T. ) ;
#5226=CARTESIAN_POINT ( 'NONE',  ( 54.27274129413513748, 17.15418818842660542, -26.87180614142805624 ) ) ;
#5228=ADVANCED_FACE ( 'NONE', ( #49051, #1342 ), #17075, .T. ) ;
#5232=ORIENTED_EDGE ( 'NONE', *, *, #16379, .T. ) ;
#5240=CARTESIAN_POINT ( 'NONE',  ( 56.16528524747329953, 19.58792304710189924, -74.72304216316619829 ) ) ;
#5241=CARTESIAN_POINT ( 'NONE',  ( 47.28500118035560007, -54.39529810738689974, -75.17099345517469544 ) ) ;
#5242=ORIENTED_EDGE ( 'NONE', *, *, #21442, .F. ) ;
#5243=CARTESIAN_POINT ( 'NONE',  ( 55.51083792958409902, 14.38702645469839858, -16.12015598830499741 ) ) ;
#5244=CARTESIAN_POINT ( 'NONE',  ( 57.18740755751830562, -50.43062217190990282, -53.01833411754459746 ) ) ;
#5247=ORIENTED_EDGE ( 'NONE', *, *, #8981, .F. ) ;
#5248=CARTESIAN_POINT ( 'NONE',  ( 47.37718579482119452, 23.30994691619889991, -74.80618026387681141 ) ) ;
#5249=CARTESIAN_POINT ( 'NONE',  ( 19.95138792988717569, -54.89243911056428260, -18.38918865259743285 ) ) ;
#5250=CARTESIAN_POINT ( 'NONE',  ( 40.93885366971109363, -45.45026610025310276, -5.915603290955130156 ) ) ;
#5251=VECTOR ( 'NONE', #12315, 1000.000000000000000 ) ;
#5252=CARTESIAN_POINT ( 'NONE',  ( 12.33251669429169972, 33.41328467211270237, -15.86092359079939840 ) ) ;
#5254=CARTESIAN_POINT ( 'NONE',  ( 60.34379258661509482, -45.86802437805019395, -47.72732609191810127 ) ) ;
#5258=CARTESIAN_POINT ( 'NONE',  ( 52.56522529778620623, -49.86179102641759897, -48.47379134784809906 ) ) ;
#5260=CARTESIAN_POINT ( 'NONE',  ( -26.85818705357539926, -41.76596063699349770, -55.57881993978430302 ) ) ;
#5262=ORIENTED_EDGE ( 'NONE', *, *, #12390, .F. ) ;
#5263=CARTESIAN_POINT ( 'NONE',  ( 53.28342433172029757, -49.42919346652210066, -48.89794257291740109 ) ) ;
#5264=CARTESIAN_POINT ( 'NONE',  ( 61.57714813399910270, -45.11618897791640137, -27.37584119844559893 ) ) ;
#5266=CARTESIAN_POINT ( 'NONE',  ( 56.63434221316140338, 14.45566336728010093, -26.04414657594499971 ) ) ;
#5268=CARTESIAN_POINT ( 'NONE',  ( 51.06184042306900039, 18.36344697847389895, -76.32371533076559444 ) ) ;
#5269=CARTESIAN_POINT ( 'NONE',  ( 52.87494882852160316, 18.41383132391699817, -48.84793717290940407 ) ) ;
#5272=CARTESIAN_POINT ( 'NONE',  ( 63.61124308565409535, -44.96453999798260526, -11.13477462305379895 ) ) ;
#5273=AXIS2_PLACEMENT_3D ( 'NONE', #39370, #3728, #7662 ) ;
#5274=VERTEX_POINT ( 'NONE', #36446 ) ;
#5276=VERTEX_POINT ( 'NONE', #16538 ) ;
#5278=CARTESIAN_POINT ( 'NONE',  ( 47.38360762733800158, -54.66752147347639834, -54.85966442921209563 ) ) ;
#5281=CARTESIAN_POINT ( 'NONE',  ( 57.51923301339540728, 18.59880830977609989, -52.27870191450410431 ) ) ;
#5283=DIRECTION ( 'NONE',  ( -0.4640893551880601597, -0.8857883891771953788, 0.000000000000000000 ) ) ;
#5289=CARTESIAN_POINT ( 'NONE',  ( 9.746758075853771075, -63.31345910889199757, -46.29788637164419640 ) ) ;
#5290=DIRECTION ( 'NONE',  ( 0.000000000000000000, 1.000000000000000000, 0.000000000000000000 ) ) ;
#5294=CARTESIAN_POINT ( 'NONE',  ( 84.09627343997037485, 13.28281128162446123, -47.44643142069161712 ) ) ;
#5295=CARTESIAN_POINT ( 'NONE',  ( 76.30797822825405774, -44.53040250705239345, -14.99128760117881676 ) ) ;
#5296=CARTESIAN_POINT ( 'NONE',  ( 52.66575367246569783, 19.57588115571789800, -76.31205015641521072 ) ) ;
#5298=AXIS2_PLACEMENT_3D ( 'NONE', #3239, #48744, #39402 ) ;
#5299=CARTESIAN_POINT ( 'NONE',  ( 17.92370450339619836, 20.88381105532299742, -76.14999999999999147 ) ) ;
#5303=DIRECTION ( 'NONE',  ( 0.000000000000000000, 1.000000000000000000, 0.000000000000000000 ) ) ;
#5306=LINE ( 'NONE', #38045, #43451 ) ;
#5310=CARTESIAN_POINT ( 'NONE',  ( 14.86656154879790037, 21.55824172761710145, -76.12873484255680978 ) ) ;
#5311=CARTESIAN_POINT ( 'NONE',  ( 51.70989020191399277, 17.69254107218870331, -77.02393701207040522 ) ) ;
#5312=( BOUNDED_CURVE ( )  B_SPLINE_CURVE ( 3, ( #23473, #35022, #39748, #39496 ),
 .UNSPECIFIED., .F., .F. ) 
 B_SPLINE_CURVE_WITH_KNOTS ( ( 4, 4 ),
 ( 1.696124157962962009, 1.772154247585227438 ),
 .UNSPECIFIED. ) 
 CURVE ( )  GEOMETRIC_REPRESENTATION_ITEM ( )  RATIONAL_B_SPLINE_CURVE ( ( 1.000000000000000000, 0.9995183434654335564, 0.9995183434654335564, 1.000000000000000000 ) ) 
 REPRESENTATION_ITEM ( '' )  );
#5315=ORIENTED_EDGE ( 'NONE', *, *, #3726, .T. ) ;
#5316=CARTESIAN_POINT ( 'NONE',  ( 53.36461225810830200, -49.03029623232499290, -26.93512695430979775 ) ) ;
#5317=CARTESIAN_POINT ( 'NONE',  ( 14.28039018033829954, -50.95837531346739979, -21.66377081666569993 ) ) ;
#5320=DIRECTION ( 'NONE',  ( -1.000000000000000000, 0.000000000000000000, 0.000000000000000000 ) ) ;
#5321=CARTESIAN_POINT ( 'NONE',  ( 53.37798040714660175, 15.00501951321539984, -14.93908783775269988 ) ) ;
#5324=ORIENTED_EDGE ( 'NONE', *, *, #12996, .T. ) ;
#5325=CARTESIAN_POINT ( 'NONE',  ( -7.633825585628259525, -45.26999001540249878, -5.085140908233610091 ) ) ;
#5328=CARTESIAN_POINT ( 'NONE',  ( 47.33274584257549833, 23.46610149159290160, -54.73778455475569871 ) ) ;
#5329=CARTESIAN_POINT ( 'NONE',  ( 56.18863030605354680, -45.60033839355901364, -25.30081866562760595 ) ) ;
#5331=CARTESIAN_POINT ( 'NONE',  ( 56.52272905643124545, 15.01203539575427470, -26.27184597304366420 ) ) ;
#5332=CARTESIAN_POINT ( 'NONE',  ( 11.31751849877900007, 34.00431797603069839, -17.44711658514470187 ) ) ;
#5333=EDGE_CURVE ( 'NONE', #22521, #22272, #25801, .T. ) ;
#5335=CARTESIAN_POINT ( 'NONE',  ( 53.00700879704349688, 18.33567502363469970, -48.78176283131590196 ) ) ;
#5337=CARTESIAN_POINT ( 'NONE',  ( 59.93898548971230156, -46.07977442274060564, -47.78350827547860291 ) ) ;
#5338=CARTESIAN_POINT ( 'NONE',  ( 52.88961653141840458, 18.37708373222320191, -27.85917056015219728 ) ) ;
#5339=CARTESIAN_POINT ( 'NONE',  ( 52.47879378027149500, 21.24197845805030127, -54.47385978244439997 ) ) ;
#5344=CARTESIAN_POINT ( 'NONE',  ( 9.741373805871779368, 32.02484854115400026, -46.29737847346199686 ) ) ;
#5347=CARTESIAN_POINT ( 'NONE',  ( 17.83576269003119918, 20.28384221772149942, -75.35480091913980516 ) ) ;
#5348=ORIENTED_EDGE ( 'NONE', *, *, #4133, .T. ) ;
#5354=CARTESIAN_POINT ( 'NONE',  ( 11.31507257915889930, -64.92605157093250057, -46.54990891655389618 ) ) ;
#5355=CARTESIAN_POINT ( 'NONE',  ( 57.33744283413420106, -45.74625952484549885, -26.24889444639509861 ) ) ;
#5357=CARTESIAN_POINT ( 'NONE',  ( 61.62976587840800136, 13.89047832419320017, -46.37201467644069908 ) ) ;
#5359=VERTEX_POINT ( 'NONE', #26459 ) ;
#5361=ORIENTED_EDGE ( 'NONE', *, *, #31501, .F. ) ;
#5362=CARTESIAN_POINT ( 'NONE',  ( 48.13289152230240120, -45.11618894461150120, -9.279551874200048900 ) ) ;
#5364=CYLINDRICAL_SURFACE ( 'NONE', #25948, 2.000000000000000444 ) ;
#5367=CARTESIAN_POINT ( 'NONE',  ( 46.89485130532320056, -54.03863484889780011, -75.74144252524291687 ) ) ;
#5370=CARTESIAN_POINT ( 'NONE',  ( 52.39798347658840072, 14.77016143927119884, -14.07243307208769956 ) ) ;
#5371=CARTESIAN_POINT ( 'NONE',  ( 16.13393739769620083, -15.61618894467929941, -21.14999999999999858 ) ) ;
#5372=DIRECTION ( 'NONE',  ( 1.000000000000000000, 0.000000000000000000, -0.000000000000000000 ) ) ;
#5374=CARTESIAN_POINT ( 'NONE',  ( 60.63521576136469804, 13.98548221933389968, -26.99365743681530105 ) ) ;
#5376=ORIENTED_EDGE ( 'NONE', *, *, #46932, .F. ) ;
#5382=ADVANCED_FACE ( 'NONE', ( #42212 ), #38278, .T. ) ;
#5386=CARTESIAN_POINT ( 'NONE',  ( 48.86762024612250599, -53.93826904077799611, -54.76140763573010162 ) ) ;
#5387=CARTESIAN_POINT ( 'NONE',  ( 43.91475033527959937, -43.54611815821230891, -5.093413304872340674 ) ) ;
#5388=CIRCLE ( 'NONE', #26288, 1.500000000000001332 ) ;
#5390=CARTESIAN_POINT ( 'NONE',  ( 18.53970998326800057, -51.57539031256270334, -74.98719232986280758 ) ) ;
#5392=AXIS2_PLACEMENT_3D ( 'NONE', #15260, #7908, #32749 ) ;
#5397=CARTESIAN_POINT ( 'NONE',  ( 61.07408082200849719, -45.63407273295089794, -47.69645918351529446 ) ) ;
#5401=CARTESIAN_POINT ( 'NONE',  ( 50.03007040746459921, -48.61618894467930119, -78.14999999999999147 ) ) ;
#5402=LINE ( 'NONE', #25802, #32634 ) ;
#5403=DIRECTION ( 'NONE',  ( 0.3294064756441054120, -0.9441882088883177815, 9.436895709313929201E-16 ) ) ;
#5404=ORIENTED_EDGE ( 'NONE', *, *, #51815, .F. ) ;
#5405=EDGE_LOOP ( 'NONE', ( #44711, #13793, #9636, #25058 ) ) ;
#5406=ORIENTED_EDGE ( 'NONE', *, *, #34703, .F. ) ;
#5408=CARTESIAN_POINT ( 'NONE',  ( 61.73009099606229455, -45.11618889822939593, -46.37193037902550685 ) ) ;
#5409=CARTESIAN_POINT ( 'NONE',  ( 52.67030364760460515, -49.78282448137120042, -48.75888224404449289 ) ) ;
#5410=CARTESIAN_POINT ( 'NONE',  ( 16.13393739769620083, -15.61618894467929941, 6.349999999999999645 ) ) ;
#5411=CARTESIAN_POINT ( 'NONE',  ( 56.11441691986449598, -50.90435229196089750, -53.54520117640679899 ) ) ;
#5419=AXIS2_PLACEMENT_3D ( 'NONE', #29638, #21776, #5810 ) ;
#5420=CARTESIAN_POINT ( 'NONE',  ( 53.27996121806140195, -52.13308956689839846, -54.32024439625399737 ) ) ;
#5422=EDGE_LOOP ( 'NONE', ( #23903, #31091, #17461, #14082 ) ) ;
#5424=CARTESIAN_POINT ( 'NONE',  ( 52.83096447931749395, -51.02617954204369966, -76.09006724408109790 ) ) ;
#5426=CARTESIAN_POINT ( 'NONE',  ( 60.60271022049670364, 14.35607423084729994, -47.13139168423140291 ) ) ;
#5427=ADVANCED_FACE ( 'NONE', ( #49820 ), #13911, .F. ) ;
#5428=B_SPLINE_CURVE_WITH_KNOTS ( 'NONE', 3,
 ( #11974, #15895, #23212, #11199, #23979, #14860, #3076, #31337, #43168, #26905, #47871, #31592, #51543, #15640, #40002, #19043, #23470, #35808, #27929, #43931 ),
 .UNSPECIFIED., .F., .F.,
 ( 4, 2, 2, 2, 2, 2, 2, 2, 2, 4 ),
 ( 0.000000000000000000, 0.1775000000000006850, 0.3374999999999994671, 0.4374999999999980571, 0.4999999999999978906, 0.6249999999999994449, 0.7746634686404010317, 0.8753061185820656398, 0.9759487685237305810, 1.000000000000000000 ),
 .UNSPECIFIED. ) ;
#5430=EDGE_CURVE ( 'NONE', #29238, #39800, #36692, .T. ) ;
#5431=DIRECTION ( 'NONE',  ( 0.9441882088883221114, 0.3294064756440927000, 0.000000000000000000 ) ) ;
#5432=CARTESIAN_POINT ( 'NONE',  ( 43.87445613097960262, 13.83391143939489965, -6.621204841358950155 ) ) ;
#5434=CARTESIAN_POINT ( 'NONE',  ( 43.37850551083089812, -43.48449350341319786, -4.923475879740440320 ) ) ;
#5440=CARTESIAN_POINT ( 'NONE',  ( 68.23802810435169874, 0.1965232615743089939, -18.38247172703000132 ) ) ;
#5442=CARTESIAN_POINT ( 'NONE',  ( 13.92281821510519890, -52.20693806470120535, -75.61048537065340724 ) ) ;
#5446=CARTESIAN_POINT ( 'NONE',  ( 84.41931977240820117, 12.04917947078452301, -47.35294579213341848 ) ) ;
#5448=CARTESIAN_POINT ( 'NONE',  ( 55.01976271995791024, -46.11948192427576032, -16.15584652683488898 ) ) ;
#5451=VECTOR ( 'NONE', #2386, 1000.000000000000000 ) ;
#5457=CARTESIAN_POINT ( 'NONE',  ( 48.08607070564750074, 23.01868680830909852, -54.70522948828759979 ) ) ;
#5461=DIRECTION ( 'NONE',  ( 0.000000000000000000, 0.000000000000000000, -1.000000000000000000 ) ) ;
#5464=CARTESIAN_POINT ( 'NONE',  ( 83.94526921706011535, 13.29514832796600032, -47.24461768887499602 ) ) ;
#5465=CARTESIAN_POINT ( 'NONE',  ( 53.72005416868749705, 17.35859260027000062, -26.34191669766340382 ) ) ;
#5469=B_SPLINE_SURFACE_WITH_KNOTS ( 'NONE', 3, 3, ( 
 ( #15197, #34317, #14418, #26454, #42469, #22523, #18857, #38535, #34842, #2631, #18603 ),
 ( #50585, #46927, #31410, #7851, #485, #4165, #47438, #11792, #24054, #47184, #23284 ),
 ( #19637, #3667, #51615, #12046, #12297, #7336, #15708, #44005, #27231, #8108, #39307 ),
 ( #31665, #19378, #11533, #27999, #40072, #47688, #20393, #27752, #35361, #51150, #20142 ),
 ( #27490, #11271, #32176, #36131, #35629, #39815, #23801, #24312, #236, #36380, #48192 ),
 ( #16221, #43749, #31923, #3925, #31156, #43497, #43249, #15969, #19885, #3410, #47945 ),
 ( #28256, #35876, #44256, #40330, #15460, #8363, #51360, #7599, #4423, #23543, #39561 ),
 ( #1273, #9654, #13588, #44516, #20652, #29043, #48717, #40582, #21171, #40842, #9138 ),
 ( #5722, #13091, #36637, #37176, #29297, #13337, #32692, #48451, #17514, #9407, #4941 ),
 ( #25094, #25608, #45298, #21676, #33486, #16474, #1528, #20916, #17264, #41106, #37687 ),
 ( #12556, #33224, #5216, #32429, #49242, #49500, #25355, #1012, #41358, #41613, #740 ),
 ( #29553, #45039, #5473, #16738, #24569, #28519, #36910, #8622, #12821, #21427, #37430 ),
 ( #4680, #45556, #28779, #44778, #8883, #24835, #17010, #32958, #48987, #22973, #41879 ),
 ( #30057, #13842, #34775, #18541, #22456, #38465, #10953, #5981, #10434, #22717, #50782 ),
 ( #6765, #2831, #14614, #26386, #34518, #22199, #33991, #18027, #37950, #2569, #30584 ),
 ( #14095, #46864, #17766, #29800, #26917, #21938, #18796, #26646, #46088, #50523, #14358 ),
 ( #42923, #2303, #46604, #2045, #30323, #1785, #42663, #50006, #34244, #10691, #33737 ),
 ( #6241, #42143, #26131, #38208, #38734, #14872, #45818, #18277, #30835, #49752, #7021 ) ),
 .UNSPECIFIED., .F., .F., .F.,
 ( 4, 2, 2, 2, 2, 2, 2, 2, 4 ),
 ( 4, 1, 1, 1, 1, 1, 1, 1, 4 ),
 ( -4.407659109999999858E-07, 0.02874937896918200106, 0.2125859696587990011, 0.3274838388398100264, 0.4366451184530800167, 0.4912257582597150396, 0.5785547819503310540, 0.7182812198553160110, 0.8732902369061590342 ),
 ( -4.407659119999999895E-07, 0.1250000000000000000, 0.2500000000000000000, 0.3750000000000000000, 0.5000000000000000000, 0.6250000000000000000, 0.7500000000000000000, 0.8750000000000000000, 1.000000000000000000 ),
 .UNSPECIFIED. ) ;
#5473=CARTESIAN_POINT ( 'NONE',  ( 12.10148745386320002, -65.09303518706980185, -16.50605066007160104 ) ) ;
#5474=CARTESIAN_POINT ( 'NONE',  ( 13.00893739769619906, 34.28605925116850273, -47.75434321273180416 ) ) ;
#5477=CARTESIAN_POINT ( 'NONE',  ( 9.897519164466769936, -64.60056534484279211, -46.94956808900870016 ) ) ;
#5478=VERTEX_POINT ( 'NONE', #47189 ) ;
#5482=CYLINDRICAL_SURFACE ( 'NONE', #9341, 1.999999999999997113 ) ;
#5483=CARTESIAN_POINT ( 'NONE',  ( 59.32539931833549929, -3.119615929214149652, -15.67734707553489848 ) ) ;
#5484=CARTESIAN_POINT ( 'NONE',  ( 50.77828552747430280, -50.74762180099720865, -76.14999999999999147 ) ) ;
#5485=CARTESIAN_POINT ( 'NONE',  ( 57.24929578313069811, 19.38381105532069881, -53.91492796121699627 ) ) ;
#5487=CARTESIAN_POINT ( 'NONE',  ( 53.34500566076300032, -49.01310193610010657, -26.65466145037910195 ) ) ;
#5488=CARTESIAN_POINT ( 'NONE',  ( 68.13393739769819035, 19.47158195952289717, -70.40645085170196182 ) ) ;
#5496=CARTESIAN_POINT ( 'NONE',  ( 13.92806294839289905, -51.20625126854269382, -22.96889535537080107 ) ) ;
#5497=CARTESIAN_POINT ( 'NONE',  ( 55.90344875862429319, 19.41190792946789756, -75.71352352466739433 ) ) ;
#5498=CARTESIAN_POINT ( 'NONE',  ( 46.62699164054490097, -53.28059046267329535, -76.10173089639540933 ) ) ;
#5500=CARTESIAN_POINT ( 'NONE',  ( 56.28192901139959758, 14.29581952047969828, -17.75665406777029887 ) ) ;
#5501=CARTESIAN_POINT ( 'NONE',  ( 56.94152844520889545, -50.61086428661570125, -53.44912207859540132 ) ) ;
#5502=CARTESIAN_POINT ( 'NONE',  ( 52.66033724191510146, -49.78877526119400443, -48.73956177349010943 ) ) ;
#5505=VERTEX_POINT ( 'NONE', #46933 ) ;
#5506=CARTESIAN_POINT ( 'NONE',  ( 47.34726563384639775, 23.26222549619640034, -74.94563673128509151 ) ) ;
#5507=CARTESIAN_POINT ( 'NONE',  ( 19.92389628699634940, -54.81363894426598904, -18.23936587176626745 ) ) ;
#5508=CARTESIAN_POINT ( 'NONE',  ( 61.25267155084156201, -45.60875457951716072, -47.68505357991368498 ) ) ;
#5514=CARTESIAN_POINT ( 'NONE',  ( 18.86789271246039945, 20.55440458018300021, -15.81497037201279987 ) ) ;
#5518=CYLINDRICAL_SURFACE ( 'NONE', #15944, 1.999999999999996891 ) ;
#5520=CARTESIAN_POINT ( 'NONE',  ( -29.90021944857959824, -36.14291753250989814, -56.90940863684170381 ) ) ;
#5522=CARTESIAN_POINT ( 'NONE',  ( 52.72459160374280174, -49.72420427742829929, -48.48895090856409951 ) ) ;
#5523=ORIENTED_EDGE ( 'NONE', *, *, #49275, .T. ) ;
#5524=CARTESIAN_POINT ( 'NONE',  ( 61.49805056874480158, -45.11879423640499454, -27.42091738664879941 ) ) ;
#5527=CARTESIAN_POINT ( 'NONE',  ( 56.44557979832819683, 14.18613123430430001, -25.36404871676379713 ) ) ;
#5530=CARTESIAN_POINT ( 'NONE',  ( 52.70373694452960223, 18.51116282284399972, -48.64345963606820078 ) ) ;
#5531=DIRECTION ( 'NONE',  ( 0.6415444970810859626, -0.4854844151940995167, 0.5939070136550161916 ) ) ;
#5532=CARTESIAN_POINT ( 'NONE',  ( 72.31053544666039556, -43.38410770150959905, -12.49652231024070126 ) ) ;
#5533=VECTOR ( 'NONE', #12798, 1000.000000000000000 ) ;
#5537=CARTESIAN_POINT ( 'NONE',  ( 47.44122687894220292, -54.63357073524160512, -54.92718653334570433 ) ) ;
#5547=CARTESIAN_POINT ( 'NONE',  ( 14.05644111844239852, -51.15811488399830154, -22.83288692000170172 ) ) ;
#5549=EDGE_LOOP ( 'NONE', ( #13561, #16421, #26281, #25041 ) ) ;
#5550=CARTESIAN_POINT ( 'NONE',  ( 11.66017304635799867, -64.87584527432149173, -45.05114943332709743 ) ) ;
#5553=CARTESIAN_POINT ( 'NONE',  ( 51.41399438364850027, 19.32188539444780062, -76.23672007490239366 ) ) ;
#5555=FACE_OUTER_BOUND ( 'NONE', #17909, .T. ) ;
#5557=DIRECTION ( 'NONE',  ( -1.000000000000000000, -8.673617379884043361E-16, 0.000000000000000000 ) ) ;
#5562=CARTESIAN_POINT ( 'NONE',  ( 46.03122142033570441, 13.88381105532070059, -7.582879021622040305 ) ) ;
#5565=ORIENTED_EDGE ( 'NONE', *, *, #27750, .T. ) ;
#5566=CARTESIAN_POINT ( 'NONE',  ( 18.76585674228498135, 20.63639536069459268, -74.86151687926869158 ) ) ;
#5568=CIRCLE ( 'NONE', #33180, 3.799999999999829736 ) ;
#5569=CARTESIAN_POINT ( 'NONE',  ( 44.98357750381669007, 14.87860355809039881, -8.963129099644900677 ) ) ;
#5571=CARTESIAN_POINT ( 'NONE',  ( 14.18747379400850051, 20.38364582413100123, -75.40982873507010709 ) ) ;
#5576=CARTESIAN_POINT ( 'NONE',  ( 53.92255937822079659, -48.37029822198850582, -26.37636367547430183 ) ) ;
#5578=CARTESIAN_POINT ( 'NONE',  ( 14.83504272149919956, -51.11618894083779452, -22.28508381815780126 ) ) ;
#5579=CARTESIAN_POINT ( 'NONE',  ( 10.02064309493579941, 32.96920898343689998, -17.37848894768429986 ) ) ;
#5582=CARTESIAN_POINT ( 'NONE',  ( 49.03396717343779443, 14.94208145987820124, -11.76399146459199940 ) ) ;
#5583=VERTEX_POINT ( 'NONE', #43254 ) ;
#5584=CARTESIAN_POINT ( 'NONE',  ( -7.434493659210470007, -45.51118646461110018, -5.423941065748909551 ) ) ;
#5585=CARTESIAN_POINT ( 'NONE',  ( 47.46268832744230082, 23.38928987100490176, -54.95184613728230261 ) ) ;
#5589=CARTESIAN_POINT ( 'NONE',  ( 61.05628869985170581, 14.11843175711090126, -46.88525980312950026 ) ) ;
#5590=CARTESIAN_POINT ( 'NONE',  ( 10.98135320218699995, 33.83639044753279990, -17.57575610280199996 ) ) ;
#5591=DIRECTION ( 'NONE',  ( 2.044963717693971196E-12, -0.08197919874685707931, 0.9966340406452226519 ) ) ;
#5592=CARTESIAN_POINT ( 'NONE',  ( 52.96846354095290366, 18.35586996326500042, -48.76456332840299979 ) ) ;
#5594=CARTESIAN_POINT ( 'NONE',  ( 54.36655688846699519, -48.99971972129989695, -48.99196827366439777 ) ) ;
#5595=CARTESIAN_POINT ( 'NONE',  ( 11.19961949155312553, 34.01496270439587732, -18.17421237848505911 ) ) ;
#5596=CARTESIAN_POINT ( 'NONE',  ( 53.70964822437340302, 20.71768139653410046, -54.24308104583550261 ) ) ;
#5598=CARTESIAN_POINT ( 'NONE',  ( 47.16461990496790690, 13.88381105532070059, -8.336227306136100523 ) ) ;
#5601=CARTESIAN_POINT ( 'NONE',  ( 10.14147289287149967, 31.98528096571020285, -45.99377946889909907 ) ) ;
#5602=CARTESIAN_POINT ( 'NONE',  ( 45.82863309824571729, 13.88351055973502213, -7.494180813464123680 ) ) ;
#5603=VECTOR ( 'NONE', #6358, 1000.000000000000114 ) ;
#5604=CARTESIAN_POINT ( 'NONE',  ( 66.35712195075809916, -30.62653953495700065, -16.95628802592780104 ) ) ;
#5605=DIRECTION ( 'NONE',  ( -0.6653150774959307734, 0.7465626883635315680, 0.000000000000000000 ) ) ;
#5608=VERTEX_POINT ( 'NONE', #11797 ) ;
#5611=CARTESIAN_POINT ( 'NONE',  ( 10.17097458880020078, -64.04334660451389993, -46.31317360413619610 ) ) ;
#5612=CARTESIAN_POINT ( 'NONE',  ( 56.81616149493390111, -45.43712851969070243, -25.88809970019270068 ) ) ;
#5615=CARTESIAN_POINT ( 'NONE',  ( 61.63193477201050285, 13.93849808901580012, -46.83132799652889844 ) ) ;
#5617=ORIENTED_EDGE ( 'NONE', *, *, #28660, .F. ) ;
#5619=VERTEX_POINT ( 'NONE', #31161 ) ;
#5620=CARTESIAN_POINT ( 'NONE',  ( 48.37455542296130062, -45.20184122439500385, -10.02357746685530060 ) ) ;
#5622=EDGE_CURVE ( 'NONE', #39487, #20020, #16616, .T. ) ;
#5625=ADVANCED_FACE ( 'NONE', ( #39312 ), #43754, .F. ) ;
#5626=( BOUNDED_CURVE ( )  B_SPLINE_CURVE ( 3, ( #33716, #48963, #25588, #41593 ),
 .UNSPECIFIED., .F., .T. ) 
 B_SPLINE_CURVE_WITH_KNOTS ( ( 4, 4 ),
 ( 5.657409142292634030, 6.193758666985289985 ),
 .UNSPECIFIED. ) 
 CURVE ( )  GEOMETRIC_REPRESENTATION_ITEM ( )  RATIONAL_B_SPLINE_CURVE ( ( 1.000000000000000000, 0.9761707593066160094, 0.9761707593066160094, 1.000000000000000000 ) ) 
 REPRESENTATION_ITEM ( '' )  );
#5630=CARTESIAN_POINT ( 'NONE',  ( 46.99011664277529832, -54.32342547810879552, -75.47331621149609759 ) ) ;
#5631=DIRECTION ( 'NONE',  ( 0.2260571801428030714, 0.000000000000000000, -0.9741140340359972782 ) ) ;
#5632=AXIS2_PLACEMENT_3D ( 'NONE', #1117, #28622, #44621 ) ;
#5633=EDGE_CURVE ( 'NONE', #29321, #48345, #50107, .T. ) ;
#5634=CARTESIAN_POINT ( 'NONE',  ( 51.09737042232929838, 13.88381105524950065, -11.36023950572089802 ) ) ;
#5639=CARTESIAN_POINT ( 'NONE',  ( 57.64776587906369798, 14.05990909772789976, -25.94377082751820041 ) ) ;
#5642=CARTESIAN_POINT ( 'NONE',  ( 61.75019796695539753, 13.88381105532070059, -46.37203261889099792 ) ) ;
#5643=CARTESIAN_POINT ( 'NONE',  ( -10.53607080544539976, -41.37169853536430253, -4.264176651484540059 ) ) ;
#5644=CARTESIAN_POINT ( 'NONE',  ( 16.13393739769609780, -15.61618894467929941, 8.449999999999999289 ) ) ;
#5646=EDGE_CURVE ( 'NONE', #15133, #43823, #15975, .T. ) ;
#5647=CARTESIAN_POINT ( 'NONE',  ( 82.13853704237929776, -47.11618894467930119, -46.37203261889099792 ) ) ;
#5650=CARTESIAN_POINT ( 'NONE',  ( 48.94619156065270005, -53.78419483245289712, -54.43336765931639576 ) ) ;
#5652=CARTESIAN_POINT ( 'NONE',  ( 76.69624363483841023, -43.19219574469177303, -14.37506098188831949 ) ) ;
#5653=CARTESIAN_POINT ( 'NONE',  ( 18.84530626205710035, -51.72201361531850239, -74.35192203308130843 ) ) ;
#5654=CYLINDRICAL_SURFACE ( 'NONE', #6410, 1.000000000000029976 ) ;
#5660=CARTESIAN_POINT ( 'NONE',  ( 60.92390599033139864, -45.64103330176020279, -47.67030853226700060 ) ) ;
#5666=CYLINDRICAL_SURFACE ( 'NONE', #21768, 1.000000000000000444 ) ;
#5667=CARTESIAN_POINT ( 'NONE',  ( 43.88907883820460398, -46.06587682131880257, -8.216673521218469389 ) ) ;
#5670=ORIENTED_EDGE ( 'NONE', *, *, #46381, .F. ) ;
#5671=VERTEX_POINT ( 'NONE', #38803 ) ;
#5672=CARTESIAN_POINT ( 'NONE',  ( 61.03994009699120227, -45.35937513829429690, -46.86322148818550204 ) ) ;
#5674=CARTESIAN_POINT ( 'NONE',  ( 55.55115492324519266, -50.88452601480440052, -52.95812837848109211 ) ) ;
#5675=AXIS2_PLACEMENT_3D ( 'NONE', #50524, #31094, #47123 ) ;
#5676=ORIENTED_EDGE ( 'NONE', *, *, #17468, .F. ) ;
#5680=CARTESIAN_POINT ( 'NONE',  ( 51.36789317581919789, -52.94755764699560530, -54.71052196913720422 ) ) ;
#5682=VERTEX_POINT ( 'NONE', #50847 ) ;
#5684=CARTESIAN_POINT ( 'NONE',  ( 53.29069942456280273, -51.03998195050350262, -75.99878208018989767 ) ) ;
#5688=CARTESIAN_POINT ( 'NONE',  ( 41.29354876163589694, 13.54338451021459910, -5.375173354248380164 ) ) ;
#5689=CARTESIAN_POINT ( 'NONE',  ( 42.08165231488229807, -44.23899420458050002, -4.969335818164180907 ) ) ;
#5694=CARTESIAN_POINT ( 'NONE',  ( 65.95899839816510735, 0.8661402160289060070, -17.73196870731459995 ) ) ;
#5695=ORIENTED_EDGE ( 'NONE', *, *, #7236, .F. ) ;
#5696=CARTESIAN_POINT ( 'NONE',  ( 14.68717196201729891, -52.47980496485550361, -76.04476946176040997 ) ) ;
#5697=CARTESIAN_POINT ( 'NONE',  ( 57.32763710804100299, 19.16690701097390104, -53.00790326582389866 ) ) ;
#5699=DIRECTION ( 'NONE',  ( -0.7226652920947586045, -0.6911981449639438280, 0.000000000000000000 ) ) ;
#5700=AXIS2_PLACEMENT_3D ( 'NONE', #25395, #14397, #21471 ) ;
#5702=CARTESIAN_POINT ( 'NONE',  ( 47.77546308418789778, -54.44195670944800014, -54.82267176637049744 ) ) ;
#5704=CARTESIAN_POINT ( 'NONE',  ( 47.91428909763650523, 23.15602325637470216, -54.91125936546870179 ) ) ;
#5710=CARTESIAN_POINT ( 'NONE',  ( 84.20053740572899414, 12.88281201546480048, -47.28523898137510173 ) ) ;
#5711=CARTESIAN_POINT ( 'NONE',  ( 52.90929476643909624, 18.25992211886340044, -27.14407627714519933 ) ) ;
#5714=CARTESIAN_POINT ( 'NONE',  ( 82.13853704237929776, -45.64188066427789892, -47.72348187592560009 ) ) ;
#5715=CARTESIAN_POINT ( 'NONE',  ( 57.50723796700749801, -45.11618894467940066, -17.93020416573320119 ) ) ;
#5716=CARTESIAN_POINT ( 'NONE',  ( 56.48921795443543203, -46.16653356619494275, -26.24159223014568099 ) ) ;
#5720=ORIENTED_EDGE ( 'NONE', *, *, #26420, .F. ) ;
#5722=CARTESIAN_POINT ( 'NONE',  ( 12.09990282912350068, -65.24532120969969640, -16.83009741455080288 ) ) ;
#5723=CARTESIAN_POINT ( 'NONE',  ( 12.29700469235899973, 34.12962537319510403, -46.90718399448299891 ) ) ;
#5725=CARTESIAN_POINT ( 'NONE',  ( -26.88703640771693770, 10.64567781361937904, -56.26548710561206690 ) ) ;
#5730=CARTESIAN_POINT ( 'NONE',  ( 52.74159186887090556, 18.44087211712770014, -48.34114423306549924 ) ) ;
#5731=CARTESIAN_POINT ( 'NONE',  ( 59.22431762257839694, -3.120768426202699786, -15.66519454250340004 ) ) ;
#5733=CARTESIAN_POINT ( 'NONE',  ( 51.34919179766620090, -49.60438797113280174, -76.46527068533909244 ) ) ;
#5734=CARTESIAN_POINT ( 'NONE',  ( 56.48499257286630382, -50.43009329692559817, -52.75538019139929702 ) ) ;
#5735=VERTEX_POINT ( 'NONE', #4685 ) ;
#5737=CARTESIAN_POINT ( 'NONE',  ( 65.43393739769584272, 16.88381105531917825, -74.20000000000047180 ) ) ;
#5741=CARTESIAN_POINT ( 'NONE',  ( 60.23130391297029718, 14.55066440145539985, -47.24246919202519734 ) ) ;
#5742=EDGE_CURVE ( 'NONE', #33786, #48345, #12302, .T. ) ;
#5744=CARTESIAN_POINT ( 'NONE',  ( 13.85787483888649874, -51.20742914540719681, -22.56068819944239934 ) ) ;
#5745=CARTESIAN_POINT ( 'NONE',  ( 56.68181436161830078, 19.46489750539030084, -74.32030992971661476 ) ) ;
#5746=TOROIDAL_SURFACE ( 'NONE', #39223, 18.00000000000000000, 2.000000000000000000 ) ;
#5747=CARTESIAN_POINT ( 'NONE',  ( 47.63732208602310436, -54.52964753308490486, -74.36335264244719667 ) ) ;
#5748=ORIENTED_EDGE ( 'NONE', *, *, #4296, .T. ) ;
#5749=CARTESIAN_POINT ( 'NONE',  ( 55.49736661512110203, 14.70425851891470082, -16.59168144405439804 ) ) ;
#5750=CARTESIAN_POINT ( 'NONE',  ( -21.86606260230379561, -15.61618894467929231, 6.349999999999999645 ) ) ;
#5751=CARTESIAN_POINT ( 'NONE',  ( 56.94695455049200206, -50.48167892581339800, -53.05466020099660085 ) ) ;
#5753=DIRECTION ( 'NONE',  ( 0.7702700562048789834, 0.6377178376948009486, -1.693090112579540101E-15 ) ) ;
#5754=CARTESIAN_POINT ( 'NONE',  ( 47.30207934339009768, 23.19015752006689723, -75.11580175282739447 ) ) ;
#5756=CARTESIAN_POINT ( 'NONE',  ( 60.62539537963965586, -45.77966094345966042, -47.75584023230192088 ) ) ;
#5761=CARTESIAN_POINT ( 'NONE',  ( 8.133937397696209715, 28.10308010054979988, -21.14999999999999858 ) ) ;
#5763=CARTESIAN_POINT ( 'NONE',  ( 61.16115695917979878, 14.06348816002850022, -46.76869981922120445 ) ) ;
#5764=CARTESIAN_POINT ( 'NONE',  ( 14.34417029198879945, -52.11618894467940066, -23.15000000000000213 ) ) ;
#5765=CARTESIAN_POINT ( 'NONE',  ( -0.2991137081852789925, 30.89086735222949898, -48.78634498590000135 ) ) ;
#5766=VERTEX_POINT ( 'NONE', #44522 ) ;
#5767=CARTESIAN_POINT ( 'NONE',  ( 53.40532901998560789, -49.36081156069519693, -48.82229769749290682 ) ) ;
#5770=CARTESIAN_POINT ( 'NONE',  ( 61.33704255976599740, -45.11618898598639760, -27.03744896294960043 ) ) ;
#5772=CARTESIAN_POINT ( 'NONE',  ( 13.64409289200350095, 19.76484905899049949, -21.86436953804059868 ) ) ;
#5773=CARTESIAN_POINT ( 'NONE',  ( 56.30911185033799882, 14.37708950283650111, -25.70913536183260462 ) ) ;
#5777=CARTESIAN_POINT ( 'NONE',  ( 52.75373265657299982, 18.47785976625320004, -48.68700065433350233 ) ) ;
#5779=CARTESIAN_POINT ( 'NONE',  ( 60.91431180673350809, -45.42519531869549354, -47.01365133320230427 ) ) ;
#5780=CARTESIAN_POINT ( 'NONE',  ( 73.61871130914850880, -44.95982266748999479, -13.93477351660789942 ) ) ;
#5786=CARTESIAN_POINT ( 'NONE',  ( 47.53365938598520302, -54.56237310633869697, -54.69765973086329325 ) ) ;
#5789=CARTESIAN_POINT ( 'NONE',  ( 10.81643727139639921, -64.95351341576260040, -17.63284883035869655 ) ) ;
#5793=DIRECTION ( 'NONE',  ( -0.05023550054956202326, 0.000000000000000000, -0.9987374001630934250 ) ) ;
#5797=CARTESIAN_POINT ( 'NONE',  ( 8.799470649396189614, -63.19223985362448559, -46.67016919464409597 ) ) ;
#5798=CARTESIAN_POINT ( 'NONE',  ( 17.92370450339619836, 19.88381105532299742, -74.14999999999999147 ) ) ;
#5803=CARTESIAN_POINT ( 'NONE',  ( 51.73525796840619506, 19.20063007591929960, -76.36782568579080532 ) ) ;
#5810=DIRECTION ( 'NONE',  ( 1.000000000000000000, 0.000000000000000000, 0.000000000000000000 ) ) ;
#5814=AXIS2_PLACEMENT_3D ( 'NONE', #16238, #48733, #16492 ) ;
#5815=CYLINDRICAL_SURFACE ( 'NONE', #50148, 0.9999999999999407141 ) ;
#5820=CIRCLE ( 'NONE', #8314, 1.000000000000000888 ) ;
#5821=CARTESIAN_POINT ( 'NONE',  ( 13.90784298899419902, 20.26946707534090208, -75.09610479291009710 ) ) ;
#5822=CARTESIAN_POINT ( 'NONE',  ( 17.71568204744891517, -51.70197554413384466, -75.56421372420066973 ) ) ;
#5823=CARTESIAN_POINT ( 'NONE',  ( 44.26786790321339993, -45.40684719649339485, -7.720938881823640187 ) ) ;
#5827=CARTESIAN_POINT ( 'NONE',  ( 53.39205224544679851, -48.96840769728560616, -26.76104151705999712 ) ) ;
#5829=CARTESIAN_POINT ( 'NONE',  ( 16.50882131665070318, -51.11266530063170421, -20.29200666522890018 ) ) ;
#5830=CARTESIAN_POINT ( 'NONE',  ( 10.88039558896599956, 33.80616322986560363, -17.65320609993409917 ) ) ;
#5831=DIRECTION ( 'NONE',  ( 0.000000000000000000, 0.000000000000000000, 1.000000000000000000 ) ) ;
#5833=CARTESIAN_POINT ( 'NONE',  ( 51.35061793337657576, 19.88840392264928880, -50.03559567676038711 ) ) ;
#5835=CARTESIAN_POINT ( 'NONE',  ( -3.971359608989250223, -47.88178280679790078, -4.564193690396530556 ) ) ;
#5836=CARTESIAN_POINT ( 'NONE',  ( 47.49598700288770203, 23.35309783937709938, -54.68536711013020124 ) ) ;
#5839=CARTESIAN_POINT ( 'NONE',  ( 60.80448350504249788, 14.25485008339019899, -47.16347503790071016 ) ) ;
#5840=CARTESIAN_POINT ( 'NONE',  ( 11.90855646482910046, 33.99907130593510374, -16.85546526172750248 ) ) ;
#5841=CARTESIAN_POINT ( 'NONE',  ( 52.23706089893619975, 18.52650580724129981, -77.18592072748609212 ) ) ;
#5842=CARTESIAN_POINT ( 'NONE',  ( 52.89416328055860106, 18.39479795143680008, -48.70339646180270421 ) ) ;
#5844=CARTESIAN_POINT ( 'NONE',  ( 57.22447440519270145, -47.50261249455419232, -48.27822118512559513 ) ) ;
#5847=CARTESIAN_POINT ( 'NONE',  ( 52.09210036518850018, 21.29014856838869818, -53.85655248009329910 ) ) ;
#5849=CONICAL_SURFACE ( 'NONE', #19228, 20.98392344168889778, 0.7480182347898678419 ) ;
#5850=LINE ( 'NONE', #1915, #23224 ) ;
#5853=CARTESIAN_POINT ( 'NONE',  ( 10.49390830983270106, 32.10632801932060687, -45.62647078093240083 ) ) ;
#5855=AXIS2_PLACEMENT_3D ( 'NONE', #22836, #18917, #31981 ) ;
#5856=CARTESIAN_POINT ( 'NONE',  ( 65.81143242515639713, -32.80576248147190199, -18.80816254862149961 ) ) ;
#5858=VERTEX_POINT ( 'NONE', #36914 ) ;
#5859=ORIENTED_EDGE ( 'NONE', *, *, #27076, .T. ) ;
#5862=CARTESIAN_POINT ( 'NONE',  ( 11.09507093703399860, -63.56477272120999800, -44.34938846766090137 ) ) ;
#5863=CARTESIAN_POINT ( 'NONE',  ( 56.86965732674089935, -45.75598051248179843, -26.16748850934180126 ) ) ;
#5868=ORIENTED_EDGE ( 'NONE', *, *, #40978, .F. ) ;
#5869=CARTESIAN_POINT ( 'NONE',  ( 50.84007792687270211, -45.59127768917590373, -12.55259730091349901 ) ) ;
#5871=CARTESIAN_POINT ( 'NONE',  ( 15.72113303934720108, 19.87699618195869888, -21.50711442615470048 ) ) ;
#5872=EDGE_CURVE ( 'NONE', #13261, #11543, #43105, .T. ) ;
#5873=CARTESIAN_POINT ( 'NONE',  ( 50.95939078474919626, -32.48240620400619605, -76.37902184192930122 ) ) ;
#5876=CARTESIAN_POINT ( 'NONE',  ( 47.08375996125450058, -54.42988687340879750, -75.29488275581999801 ) ) ;
#5877=CARTESIAN_POINT ( 'NONE',  ( 61.59958201630909969, 13.73326013108119881, -10.58817094626940047 ) ) ;
#5878=CARTESIAN_POINT ( 'NONE',  ( 50.90853148534860395, -50.90159658081540073, -76.14999999999999147 ) ) ;
#5879=CARTESIAN_POINT ( 'NONE',  ( 52.59105628395929699, 20.91324755812640035, -53.43271834460720271 ) ) ;
#5881=CIRCLE ( 'NONE', #31816, 1.999999999999996669 ) ;
#5883=CARTESIAN_POINT ( 'NONE',  ( 52.46419965653649342, 19.96388597204279947, -75.99844946084689923 ) ) ;
#5884=CARTESIAN_POINT ( 'NONE',  ( 57.36436529245580118, 14.21344931724819993, -26.07125751596730012 ) ) ;
#5886=AXIS2_PLACEMENT_3D ( 'NONE', #41970, #2383, #5557 ) ;
#5888=B_SPLINE_SURFACE_WITH_KNOTS ( 'NONE', 3, 3, ( 
 ( #1978, #30259, #10366, #24111, #20451, #48004, #8426, #12351, #35691, #3981, #28316, #35934, #8681 ),
 ( #44317, #27811, #4225, #48779, #546, #43811, #8167, #36441, #43560, #19699, #31984, #16028, #53 ),
 ( #24373, #24633, #3727, #12103, #40388, #23604, #4482, #51675, #15769, #28060, #31723, #7909, #16533 ),
 ( #44063, #16804, #40131, #47748, #48257, #32485, #48513, #23859, #7661, #28577, #12617, #20201, #36188 ),
 ( #20711, #44577, #32753, #40646, #27552, #4744, #298, #36702, #16280, #11856, #32234, #39882, #804 ),
 ( #39624, #19944, #5786, #41419, #21229, #25417, #17830, #17069, #49567, #1072, #33021, #37239, #5537 ),
 ( #9469, #21492, #1852, #21746, #24891, #36975, #49306, #13152, #5014, #37492, #25159, #13401, #29359 ),
 ( #29102, #44844, #12885, #40904, #37754, #33290, #1592, #33803, #45100, #33550, #1337, #25676, #45365 ),
 ( #41166, #17580, #13653, #49814, #45617, #41678, #29614, #9717, #13906, #17327, #9207, #49046, #5278 ),
 ( #28841, #8949, #20976, #40556, #28227, #40045, #24023, #43973, #28749, #36882, #36104, #16188, #983 ),
 ( #19858, #32929, #47913, #24804, #32661, #207, #28490, #20363, #24282, #48957, #8329, #8594, #8077 ),
 ( #20887, #40302, #24538, #4914, #32147, #16705, #48691, #4136, #12016, #48423, #48164, #461, #31896 ),
 ( #16982, #8854, #12266, #40815, #36609, #44229, #36350, #12793, #12524, #44748, #13060, #4647, #20621 ),
 ( #29013, #39787, #32401, #7822, #23774, #3893, #35849, #20111, #715, #4393, #51839, #16447, #44491 ),
 ( #15938, #27969, #37402, #25326, #9111, #33453, #33710, #13563, #37921, #10141, #21142, #14324, #1503 ),
 ( #29527, #13813, #2274, #29267, #2015, #13308, #45269, #45530, #45790, #29772, #49725, #9879, #38180 ) ),
 .UNSPECIFIED., .F., .F., .F.,
 ( 4, 2, 2, 2, 2, 2, 2, 4 ),
 ( 4, 1, 1, 1, 1, 1, 1, 1, 1, 1, 4 ),
 ( -1.191294110796560002, -0.9822786339451109461, -0.7434038032577410249, -0.5941070340781360315, -0.5194586494883330907, -0.4000212341446480191, -0.2089213695947530203, 0.003080042640286999919 ),
 ( 0.000000000000000000, 0.1000000000000000056, 0.2000000000000000111, 0.2999999999999999889, 0.4000000000000000222, 0.5000000000000000000, 0.5999999999999999778, 0.6999999999999999556, 0.8000000000000000444, 0.9000000000000000222, 1.000000000000000000 ),
 .UNSPECIFIED. ) ;
#5892=CARTESIAN_POINT ( 'NONE',  ( 75.41176871543700599, -41.13033092184089412, -13.09038441766009875 ) ) ;
#5898=CARTESIAN_POINT ( 'NONE',  ( 51.23914219048663909, -31.75230732063590011, -17.21756681101922126 ) ) ;
#5903=ORIENTED_EDGE ( 'NONE', *, *, #26068, .F. ) ;
#5904=EDGE_CURVE ( 'NONE', #17310, #362, #46045, .T. ) ;
#5909=CARTESIAN_POINT ( 'NONE',  ( 60.61386341819070367, -45.76930238140869989, -47.73570512132659616 ) ) ;
#5914=EDGE_CURVE ( 'NONE', #34588, #5583, #43532, .T. ) ;
#5916=CARTESIAN_POINT ( 'NONE',  ( 45.01569400174280133, -46.01157251195749609, -8.915078500992239086 ) ) ;
#5918=VERTEX_POINT ( 'NONE', #49756 ) ;
#5919=ORIENTED_EDGE ( 'NONE', *, *, #13821, .F. ) ;
#5920=CARTESIAN_POINT ( 'NONE',  ( 61.39588016320150388, -45.18041509599279948, -46.37196697359190267 ) ) ;
#5921=VECTOR ( 'NONE', #37323, 1000.000000000000000 ) ;
#5922=CARTESIAN_POINT ( 'NONE',  ( 53.36596843580329619, -49.48455262995090465, -49.20806672364570034 ) ) ;
#5923=CARTESIAN_POINT ( 'NONE',  ( 61.09347322899138533, 14.24408283890917204, -47.46698883568873129 ) ) ;
#5924=( BOUNDED_CURVE ( )  B_SPLINE_CURVE ( 3, ( #20149, #12055, #24319, #44265 ),
 .UNSPECIFIED., .F., .T. ) 
 B_SPLINE_CURVE_WITH_KNOTS ( ( 4, 4 ),
 ( 0.9533855775336180782, 1.098605931781428069 ),
 .UNSPECIFIED. ) 
 CURVE ( )  GEOMETRIC_REPRESENTATION_ITEM ( )  RATIONAL_B_SPLINE_CURVE ( ( 1.000000000000000000, 0.9982433593817650053, 0.9982433593817650053, 1.000000000000000000 ) ) 
 REPRESENTATION_ITEM ( '' )  );
#5929=ORIENTED_EDGE ( 'NONE', *, *, #16241, .T. ) ;
#5931=CARTESIAN_POINT ( 'NONE',  ( 51.82317580592130213, -52.75362460619960103, -54.60923380648279846 ) ) ;
#5933=PLANE ( 'NONE',  #23392 ) ;
#5936=CARTESIAN_POINT ( 'NONE',  ( 15.98649569970556072, 19.77667957984293423, -15.66524362255343839 ) ) ;
#5937=CARTESIAN_POINT ( 'NONE',  ( 52.48374445785739795, -50.75964131328780127, -76.33825989612010687 ) ) ;
#5938=CARTESIAN_POINT ( 'NONE',  ( 7.441840577107678101, -61.50537939366137152, -19.49871569355901002 ) ) ;
#5940=CARTESIAN_POINT ( 'NONE',  ( 51.67587649748560352, 17.38381105532069881, -77.01363636363639387 ) ) ;
#5941=CARTESIAN_POINT ( 'NONE',  ( 41.30531720498969861, 13.54650839412840035, -5.382424522816090295 ) ) ;
#5942=CARTESIAN_POINT ( 'NONE',  ( 42.13038056454769986, -43.33336100108030564, -3.383138906590309691 ) ) ;
#5948=CARTESIAN_POINT ( 'NONE',  ( 67.51508810499439051, 1.181331450973390096, -18.81107296211990132 ) ) ;
#5949=ORIENTED_EDGE ( 'NONE', *, *, #49532, .T. ) ;
#5950=CARTESIAN_POINT ( 'NONE',  ( 15.05440318628160057, -53.11618894467930119, -76.14999999999999147 ) ) ;
#5951=FACE_OUTER_BOUND ( 'NONE', #31352, .T. ) ;
#5952=( GEOMETRIC_REPRESENTATION_CONTEXT ( 3 ) GLOBAL_UNCERTAINTY_ASSIGNED_CONTEXT ( ( #51007 ) ) GLOBAL_UNIT_ASSIGNED_CONTEXT ( ( #47775, #40161, #40672 ) ) REPRESENTATION_CONTEXT ( 'NONE', 'WORKASPACE' ) );
#5956=CARTESIAN_POINT ( 'NONE',  ( 46.65068702493330477, -53.59610475534989860, -76.01748491306379663 ) ) ;
#5957=VECTOR ( 'NONE', #34067, 1000.000000000000114 ) ;
#5959=CARTESIAN_POINT ( 'NONE',  ( 47.77308976098110094, -54.47805619242490138, -55.14252499832750232 ) ) ;
#5960=CARTESIAN_POINT ( 'NONE',  ( 16.65420337941495887, 19.88381105532299387, -21.07727733026571926 ) ) ;
#5962=CARTESIAN_POINT ( 'NONE',  ( 48.19528691875230209, 22.98443981604779651, -54.75792617359909542 ) ) ;
#5964=EDGE_CURVE ( 'NONE', #18453, #24585, #14361, .T. ) ;
#5966=EDGE_CURVE ( 'NONE', #5359, #1409, #25869, .T. ) ;
#5969=DIRECTION ( 'NONE',  ( 0.000000000000000000, 0.000000000000000000, 1.000000000000000000 ) ) ;
#5970=CARTESIAN_POINT ( 'NONE',  ( 13.88443978363230613, 19.02525189127405625, -20.90776614285195834 ) ) ;
#5971=CARTESIAN_POINT ( 'NONE',  ( 82.72635976414500192, 13.93234363556419986, -46.96146434100139544 ) ) ;
#5976=CARTESIAN_POINT ( 'NONE',  ( 57.29927415537260060, -45.11618894467940066, -16.93367793570499558 ) ) ;
#5977=CARTESIAN_POINT ( 'NONE',  ( 56.36054294385242258, -46.08205199474749492, -26.17081565480442151 ) ) ;
#5978=CARTESIAN_POINT ( 'NONE',  ( 51.96093394445609448, -33.40751490558020009, -77.41818406554270382 ) ) ;
#5981=CARTESIAN_POINT ( 'NONE',  ( 11.96713421143980050, -64.86694020486450540, -16.19173486066560130 ) ) ;
#5984=CARTESIAN_POINT ( 'NONE',  ( 11.24959018551579959, -65.20486053971309559, -47.30001788089079895 ) ) ;
#5985=EDGE_LOOP ( 'NONE', ( #48972, #30833, #28071, #13920 ) ) ;
#5988=CARTESIAN_POINT ( 'NONE',  ( 52.08657362407299729, 19.57909417788119910, -50.79540346422049879 ) ) ;
#5989=CARTESIAN_POINT ( 'NONE',  ( 63.55185157652021388, -1.570504493222709907, -16.28098074310999621 ) ) ;
#5990=EDGE_CURVE ( 'NONE', #18792, #24734, #29557, .T. ) ;
#5991=CARTESIAN_POINT ( 'NONE',  ( 51.78079136204299715, -50.15135418014879320, -76.50453849984249644 ) ) ;
#5992=CARTESIAN_POINT ( 'NONE',  ( 58.95041639152130131, -47.63872770396720568, -49.67920619127879434 ) ) ;
#5994=ORIENTED_EDGE ( 'NONE', *, *, #18197, .T. ) ;
#5996=CIRCLE ( 'NONE', #35274, 3.800000000000001155 ) ;
#5997=CARTESIAN_POINT ( 'NONE',  ( 65.43393739769578588, 16.88381105532129922, -71.50000000000000000 ) ) ;
#5999=CARTESIAN_POINT ( 'NONE',  ( 12.13393739769600010, -55.41568642894409180, -74.14999999999999147 ) ) ;
#6003=CARTESIAN_POINT ( 'NONE',  ( 13.38188356245069954, -50.84254990746399727, -21.60457932969460160 ) ) ;
#6004=CARTESIAN_POINT ( 'NONE',  ( 53.99619597978309571, 19.44063915672739995, -76.54984132165219535 ) ) ;
#6005=CARTESIAN_POINT ( 'NONE',  ( 46.86233940950339871, -53.56483039667740087, -75.98411709232810551 ) ) ;
#6007=CARTESIAN_POINT ( 'NONE',  ( 55.06067154038679945, 14.25733030481009855, -15.42310526391529990 ) ) ;
#6008=CARTESIAN_POINT ( 'NONE',  ( 47.65800422766920263, 23.29553884563950206, -55.16662536789920068 ) ) ;
#6009=CARTESIAN_POINT ( 'NONE',  ( 56.94659880849959421, -50.63911411607320190, -53.72521300055049664 ) ) ;
#6012=DIRECTION ( 'NONE',  ( -0.4412403921425845921, 0.5329539830406733181, -0.7219882050995984901 ) ) ;
#6014=ADVANCED_FACE ( 'NONE', ( #14098 ), #48338, .T. ) ;
#6015=CARTESIAN_POINT ( 'NONE',  ( 47.27618702399679762, 22.86794904519689808, -75.52157719890340104 ) ) ;
#6016=CARTESIAN_POINT ( 'NONE',  ( 20.03241719490254624, -55.12469585795458471, -18.94537924066331414 ) ) ;
#6018=CARTESIAN_POINT ( 'NONE',  ( 75.13751216009411849, -27.93201665058723293, -11.73726326173032852 ) ) ;
#6019=CARTESIAN_POINT ( 'NONE',  ( 13.00893747662790112, -65.51843693869379592, -23.32157303180050079 ) ) ;
#6020=CYLINDRICAL_SURFACE ( 'NONE', #37373, 2.000000000000003997 ) ;
#6021=DIRECTION ( 'NONE',  ( -0.1686178020941689892, 0.6660492713794449182, 0.7265992051412129005 ) ) ;
#6022=DIRECTION ( 'NONE',  ( 2.375726999999999900E-16, -1.726067000000000108E-16, 1.000000000000000000 ) ) ;
#6025=CARTESIAN_POINT ( 'NONE',  ( 61.08444520316569282, 14.10367956201559991, -46.85801524881159708 ) ) ;
#6026=CARTESIAN_POINT ( 'NONE',  ( -0.4230338164521119659, 31.94242356383909964, -49.86202923830639833 ) ) ;
#6030=CARTESIAN_POINT ( 'NONE',  ( 52.70374190456139729, -49.74353769694130278, -48.64347189729229370 ) ) ;
#6031=AXIS2_PLACEMENT_3D ( 'NONE', #43428, #3852, #8033 ) ;
#6032=ORIENTED_EDGE ( 'NONE', *, *, #35622, .T. ) ;
#6035=CARTESIAN_POINT ( 'NONE',  ( 13.38497028141870082, 19.86898531093049769, -21.91519145123350043 ) ) ;
#6036=CARTESIAN_POINT ( 'NONE',  ( 56.20448449522419310, 14.46648588902639965, -25.71422073399899944 ) ) ;
#6039=CARTESIAN_POINT ( 'NONE',  ( 53.35046855971329194, 18.18352159517930389, -49.00406222516500065 ) ) ;
#6042=CARTESIAN_POINT ( 'NONE',  ( 60.86251426101320305, -45.45233350416659590, -47.00312498071580336 ) ) ;
#6043=CARTESIAN_POINT ( 'NONE',  ( -1.266062602303798856, -15.61618894467929941, -6.649999999999999467 ) ) ;
#6049=FACE_OUTER_BOUND ( 'NONE', #27689, .T. ) ;
#6051=CARTESIAN_POINT ( 'NONE',  ( 57.50723796702470025, 15.88381105532069704, -17.93019253464870033 ) ) ;
#6056=CARTESIAN_POINT ( 'NONE',  ( 8.962063992902059795, -63.18440697733050371, -46.63297166286719886 ) ) ;
#6060=CARTESIAN_POINT ( 'NONE',  ( 84.44421850426766696, 12.09119830389948014, -47.46023813347235176 ) ) ;
#6062=CARTESIAN_POINT ( 'NONE',  ( 52.15433714350280070, 18.66469978627599957, -76.93549836835239830 ) ) ;
#6065=B_SPLINE_SURFACE_WITH_KNOTS ( 'NONE', 3, 3, ( 
 ( #27588, #85, #15555, #51458, #31510, #26815, #47529, #7698, #30999 ),
 ( #43593, #19732, #47781, #15033, #43085, #39147, #51707, #15801, #31763 ),
 ( #23892, #9247, #329, #5310, #48812, #4779, #32014, #12385, #28093 ),
 ( #44099, #13186, #12650, #32785, #841, #37007, #4512, #45136, #40940 ),
 ( #20231, #28610, #32269, #5050, #36734, #8458, #33056, #44877, #20747 ),
 ( #28874, #49082, #16836, #8980, #24926, #21009, #44611, #44352, #21263 ),
 ( #29135, #25194, #4260, #1105, #41201, #17103, #37270, #1371, #48039 ),
 ( #12138, #8199, #40166, #24144, #16313, #36219, #48290, #28350, #24407 ),
 ( #40419, #20484, #36475, #581, #16565, #32520, #48549, #8717, #40679 ),
 ( #13438, #46183, #45398, #5571, #25707, #25450, #49848, #33323, #37790 ),
 ( #42504, #1886, #17865, #33835, #22298, #29396, #33584, #49340, #18375 ),
 ( #29897, #46446, #41980, #37523, #5821, #26490, #34088, #49601, #6083 ),
 ( #41712, #50366, #10271, #14452, #22037, #17616, #30421, #1625, #2392 ),
 ( #45652, #21783, #26233, #13941, #6593, #42240, #10531, #38305, #9503 ),
 ( #41451, #45916, #13687, #14197, #22557, #38572, #17358, #25969, #10008 ),
 ( #38051, #21527, #29647, #9752, #2143, #18124, #50097, #30167, #6338 ) ),
 .UNSPECIFIED., .F., .F., .F.,
 ( 4, 2, 2, 2, 2, 2, 2, 4 ),
 ( 4, 1, 1, 1, 1, 1, 4 ),
 ( -1.570796326794899889, -1.295906969605790104, -0.9817477042468110149, -0.7853981633974489451, -0.6872233929727680213, -0.5301437602932779214, -0.2788163480060940058, 2.850064270699999782E-05 ),
 ( -2.850064270699999782E-05, 0.1666666666666670182, 0.3333333333333329818, 0.5000000000000000000, 0.6666666666666670737, 0.8333333333333330373, 1.000028500642649920 ),
 .UNSPECIFIED. ) ;
#6074=( BOUNDED_CURVE ( )  B_SPLINE_CURVE ( 3, ( #43652, #31310, #28671, #41002 ),
 .UNSPECIFIED., .F., .T. ) 
 B_SPLINE_CURVE_WITH_KNOTS ( ( 4, 4 ),
 ( 1.485879941667409998, 1.508255586718169949 ),
 .UNSPECIFIED. ) 
 CURVE ( )  GEOMETRIC_REPRESENTATION_ITEM ( )  RATIONAL_B_SPLINE_CURVE ( ( 1.000000000000000000, 0.9999582779775693098, 0.9999582779775693098, 1.000000000000000000 ) ) 
 REPRESENTATION_ITEM ( '' )  );
#6075=CARTESIAN_POINT ( 'NONE',  ( 18.86789271228450104, 20.55440457967890211, -74.14999999999999147 ) ) ;
#6078=CARTESIAN_POINT ( 'NONE',  ( 52.69474619017670136, -49.76773528829180293, -48.79529908194029986 ) ) ;
#6083=CARTESIAN_POINT ( 'NONE',  ( 13.55697919800630125, 20.68059730019900044, -75.01675372117850316 ) ) ;
#6086=CARTESIAN_POINT ( 'NONE',  ( 40.91146328487249662, -45.10909871309650754, -5.616201299875400288 ) ) ;
#6090=CARTESIAN_POINT ( 'NONE',  ( 52.71775171463769993, -49.71300855879460556, -27.79849493049370324 ) ) ;
#6091=CARTESIAN_POINT ( 'NONE',  ( 53.75292032863279701, -50.98834292138020174, -75.91908533967558981 ) ) ;
#6092=CARTESIAN_POINT ( 'NONE',  ( 11.31966774034260048, 33.55174231454390110, -16.38775631906590036 ) ) ;
#6094=CARTESIAN_POINT ( 'NONE',  ( -12.09840336385581949, 8.995683791603443780, -20.56421356237309794 ) ) ;
#6095=DIRECTION ( 'NONE',  ( 0.000000000000000000, -1.000000000000000000, 0.000000000000000000 ) ) ;
#6097=CARTESIAN_POINT ( 'NONE',  ( -10.42673545829310022, -42.80093869873649481, -6.039852268628239429 ) ) ;
#6098=CARTESIAN_POINT ( 'NONE',  ( 47.44708028012349388, 23.39794963804610006, -54.93391004409950540 ) ) ;
#6099=DIRECTION ( 'NONE',  ( 0.3281607301299682700, -0.6263469766835021435, 0.7071067811865493491 ) ) ;
#6102=CARTESIAN_POINT ( 'NONE',  ( 11.46543043511809934, 33.89017917862779683, -16.91315252355219911 ) ) ;
#6103=CARTESIAN_POINT ( 'NONE',  ( 7.695097139525095109, 29.51999919305320219, -20.68192065308967997 ) ) ;
#6106=DIRECTION ( 'NONE',  ( -0.7226652920947586045, 0.6911981449639438280, 0.000000000000000000 ) ) ;
#6107=CARTESIAN_POINT ( 'NONE',  ( 58.40586952783630181, -46.88396992412620534, -48.04164431124769408 ) ) ;
#6108=CARTESIAN_POINT ( 'NONE',  ( 52.93425510534450495, 18.32883259169719992, -27.73986516523889989 ) ) ;
#6109=CARTESIAN_POINT ( 'NONE',  ( 55.99237516468339493, 19.62876559806929677, -53.22104904766129607 ) ) ;
#6114=CARTESIAN_POINT ( 'NONE',  ( 31.69621505884970247, -15.61618894405949654, -8.049999999868621359 ) ) ;
#6115=CARTESIAN_POINT ( 'NONE',  ( 10.76969664418740003, 31.91660660290840212, -45.20603937285839891 ) ) ;
#6118=CARTESIAN_POINT ( 'NONE',  ( 67.51507903343110684, -32.41370693817690096, -18.81106344304309985 ) ) ;
#6119=CARTESIAN_POINT ( 'NONE',  ( 18.86790430670709995, 20.55443781750869903, -74.14994299942661371 ) ) ;
#6120=ORIENTED_EDGE ( 'NONE', *, *, #32590, .T. ) ;
#6123=CARTESIAN_POINT ( 'NONE',  ( 50.86235438802759745, -0.06463905938872580026, -16.68603828160338765 ) ) ;
#6125=CARTESIAN_POINT ( 'NONE',  ( 11.24623595844510149, -64.51626478753739491, -45.52110913008969817 ) ) ;
#6126=CARTESIAN_POINT ( 'NONE',  ( 56.22872378878379607, -46.03156578494489537, -26.06926613992889941 ) ) ;
#6129=ORIENTED_EDGE ( 'NONE', *, *, #12829, .T. ) ;
#6133=CARTESIAN_POINT ( 'NONE',  ( 50.02848935589319979, -45.20415504953729879, -11.19050354007790027 ) ) ;
#6134=TOROIDAL_SURFACE ( 'NONE', #32867, 25.10000000000000142, 4.000000000000050626 ) ;
#6135=B_SPLINE_CURVE_WITH_KNOTS ( 'NONE', 3,
 ( #47102, #42120, #30817, #42904, #10672, #46844, #21920, #38973, #10931, #37928, #6220, #22177, #26628, #38188, #2282, #50245 ),
 .UNSPECIFIED., .F., .F.,
 ( 4, 2, 2, 2, 2, 2, 2, 4 ),
 ( 0.000000000000000000, 0.2085309826310009773, 0.3750000003143186822, 0.5000000002514550790, 0.5625000002200234439, 0.6625000001697317620, 0.8225000000892668250, 1.000000000000000000 ),
 .UNSPECIFIED. ) ;
#6137=CARTESIAN_POINT ( 'NONE',  ( 15.80909573685769942, 19.88381431121090159, -21.61146777486800019 ) ) ;
#6138=CARTESIAN_POINT ( 'NONE',  ( 0.5406133260286609676, 12.32747302715160131, -20.15000000000000213 ) ) ;
#6139=CARTESIAN_POINT ( 'NONE',  ( 57.24929578595760660, -52.61618894467940066, -74.14999999999999147 ) ) ;
#6140=CARTESIAN_POINT ( 'NONE',  ( 47.13698192568809731, -54.70277146169920712, -74.81178025453719727 ) ) ;
#6141=CARTESIAN_POINT ( 'NONE',  ( 43.46129097223089843, 12.31710076222960026, -4.984571623251230044 ) ) ;
#6142=LINE ( 'NONE', #38111, #7144 ) ;
#6148=CARTESIAN_POINT ( 'NONE',  ( 52.36927096055270425, 20.10938754437729870, -75.93037474112890095 ) ) ;
#6149=CARTESIAN_POINT ( 'NONE',  ( 59.73986354666979537, 13.88378808363800054, -26.01995814806780061 ) ) ;
#6153=CARTESIAN_POINT ( 'NONE',  ( -10.89909870438290085, -41.47166246998200023, -4.617948214634860271 ) ) ;
#6158=CARTESIAN_POINT ( 'NONE',  ( 11.89321892211240161, 34.20364954171930094, -18.17421237891140251 ) ) ;
#6159=CARTESIAN_POINT ( 'NONE',  ( 42.25542674435120460, 12.11009477977519921, -3.898748442682229864 ) ) ;
#6162=CARTESIAN_POINT ( 'NONE',  ( 54.17308944977700236, 19.38381105532069881, -77.01198594365929750 ) ) ;
#6164=CARTESIAN_POINT ( 'NONE',  ( 75.63614713166808201, -43.36095494122034921, -13.45287883108393956 ) ) ;
#6165=ADVANCED_FACE ( 'NONE', ( #49061 ), #28348, .F. ) ;
#6172=CARTESIAN_POINT ( 'NONE',  ( 60.89859637212030918, -45.70159618970230042, -47.74371479433310128 ) ) ;
#6180=ORIENTED_EDGE ( 'NONE', *, *, #45974, .T. ) ;
#6181=EDGE_LOOP ( 'NONE', ( #32885, #27780, #3665, #5247, #43447, #46871 ) ) ;
#6182=ORIENTED_EDGE ( 'NONE', *, *, #12178, .F. ) ;
#6183=ORIENTED_EDGE ( 'NONE', *, *, #49170, .T. ) ;
#6187=CARTESIAN_POINT ( 'NONE',  ( 82.57794276518897902, -45.19659166770669145, -47.00700528987445637 ) ) ;
#6188=VECTOR ( 'NONE', #21122, 1000.000000000000114 ) ;
#6189=ORIENTED_EDGE ( 'NONE', *, *, #23864, .F. ) ;
#6193=CARTESIAN_POINT ( 'NONE',  ( 53.79565702846219466, -51.91342281481009735, -54.22862211494859963 ) ) ;
#6197=CARTESIAN_POINT ( 'NONE',  ( 53.99629484594630213, -50.67301330453769737, -76.54982658320740541 ) ) ;
#6198=CARTESIAN_POINT ( 'NONE',  ( 60.86321315385399799, 14.29876455231970134, -47.42926630397769827 ) ) ;
#6200=DIRECTION ( 'NONE',  ( -0.000000000000000000, 1.000000000000000000, 0.000000000000000000 ) ) ;
#6202=CARTESIAN_POINT ( 'NONE',  ( 41.35566246811119839, 13.52648421961340119, -5.363889536437749683 ) ) ;
#6204=CARTESIAN_POINT ( 'NONE',  ( 41.46604536830830057, -44.03292034146659972, -4.103344335168969792 ) ) ;
#6205=DIRECTION ( 'NONE',  ( 0.000000000000000000, 0.000000000000000000, -1.000000000000000000 ) ) ;
#6206=CARTESIAN_POINT ( 'NONE',  ( -11.32734370190460105, 10.64934056395049922, -6.430192534648650593 ) ) ;
#6213=CARTESIAN_POINT ( 'NONE',  ( 57.26339702283340216, 19.38381105532069881, -53.86342145260750414 ) ) ;
#6218=CARTESIAN_POINT ( 'NONE',  ( 48.05932801370259710, -54.34400791176139478, -55.06214228100389363 ) ) ;
#6219=LINE ( 'NONE', #17242, #8888 ) ;
#6220=CARTESIAN_POINT ( 'NONE',  ( -8.399016668315434586, -44.63805185223194627, -5.182633195203329102 ) ) ;
#6222=CARTESIAN_POINT ( 'NONE',  ( 48.00082595223879878, 23.13732979179570037, -55.05693380849600516 ) ) ;
#6225=( BOUNDED_CURVE ( )  B_SPLINE_CURVE ( 3, ( #45736, #26313, #25785, #34169 ),
 .UNSPECIFIED., .F., .T. ) 
 B_SPLINE_CURVE_WITH_KNOTS ( ( 4, 4 ),
 ( 0.6960202569534489347, 0.7967575818190610892 ),
 .UNSPECIFIED. ) 
 CURVE ( )  GEOMETRIC_REPRESENTATION_ITEM ( )  RATIONAL_B_SPLINE_CURVE ( ( 1.000000000000000000, 0.9991545113881226126, 0.9991545113881226126, 1.000000000000000000 ) ) 
 REPRESENTATION_ITEM ( '' )  );
#6226=ORIENTED_EDGE ( 'NONE', *, *, #32012, .F. ) ;
#6229=CARTESIAN_POINT ( 'NONE',  ( 61.28610861176739633, -45.23040055550220018, -28.15000000000000213 ) ) ;
#6230=CARTESIAN_POINT ( 'NONE',  ( 15.41380632618001023, 19.54070139485968838, -20.47803115614054192 ) ) ;
#6231=CARTESIAN_POINT ( 'NONE',  ( 82.61657258396949999, 14.02918563699070020, -47.17378930654919600 ) ) ;
#6232=CARTESIAN_POINT ( 'NONE',  ( 53.10197615768310442, 18.04954227246929932, -26.94626597811889823 ) ) ;
#6237=ORIENTED_EDGE ( 'NONE', *, *, #16974, .T. ) ;
#6240=ORIENTED_EDGE ( 'NONE', *, *, #33653, .T. ) ;
#6241=CARTESIAN_POINT ( 'NONE',  ( 12.36320305068320025, -64.54682834576858852, -15.76422791927960176 ) ) ;
#6242=DIRECTION ( 'NONE',  ( -0.8224686640529101922, -0.3976080002595576146, -0.4067593573362719428 ) ) ;
#6243=CARTESIAN_POINT ( 'NONE',  ( -18.43768031504481897, 21.20943201602872108, -54.46295789858282888 ) ) ;
#6248=CARTESIAN_POINT ( 'NONE',  ( 30.63393739769620083, -15.61618894467929941, -7.139181489322110608 ) ) ;
#6249=CARTESIAN_POINT ( 'NONE',  ( 52.61152491900050165, -49.81922436508880025, -48.60684586696110188 ) ) ;
#6251=CARTESIAN_POINT ( 'NONE',  ( 51.62687445589580193, 19.67932366877230166, -50.32393917942640371 ) ) ;
#6252=CARTESIAN_POINT ( 'NONE',  ( 59.93069137380890510, -2.467633955725609951, -15.76379753216029833 ) ) ;
#6253=CARTESIAN_POINT ( 'NONE',  ( 51.30775049128980214, -48.61618637183489966, -76.60305691058019306 ) ) ;
#6254=CARTESIAN_POINT ( 'NONE',  ( 61.25350616478739596, -45.59157681858799549, -47.66860495335490100 ) ) ;
#6255=CIRCLE ( 'NONE', #5392, 24.90000000000000213 ) ;
#6257=CARTESIAN_POINT ( 'NONE',  ( 52.56521993351449851, -49.86179673305689874, -28.15000000000000213 ) ) ;
#6258=CARTESIAN_POINT ( 'NONE',  ( 68.13393739769630031, 16.88381105531719939, -74.20000000000000284 ) ) ;
#6259=VERTEX_POINT ( 'NONE', #21761 ) ;
#6261=CARTESIAN_POINT ( 'NONE',  ( 54.46258938185140153, -45.11618894467940066, -13.50670374307950006 ) ) ;
#6263=CARTESIAN_POINT ( 'NONE',  ( 13.48683992790079955, -51.30121652062240400, -22.27491888996000213 ) ) ;
#6264=CARTESIAN_POINT ( 'NONE',  ( 54.99824089832750218, 19.63007236206330219, -75.56194783846839869 ) ) ;
#6266=CARTESIAN_POINT ( 'NONE',  ( 47.61801185652239354, -54.54486410850540068, -74.17413012813480577 ) ) ;
#6267=CARTESIAN_POINT ( 'NONE',  ( 56.07276868759860378, 14.18019669060810095, -16.47680628068019715 ) ) ;
#6268=CARTESIAN_POINT ( 'NONE',  ( 10.98008937475129976, 32.20858435228970507, -44.74889856825390666 ) ) ;
#6269=EDGE_CURVE ( 'NONE', #16151, #22139, #14432, .T. ) ;
#6271=CARTESIAN_POINT ( 'NONE',  ( 56.73072851771979686, -50.34974087631989903, -52.75329813171639870 ) ) ;
#6275=EDGE_LOOP ( 'NONE', ( #2573, #30372, #1834, #9532 ) ) ;
#6276=CARTESIAN_POINT ( 'NONE',  ( 46.40342216745409587, 21.74594192202859944, -76.14871748185780120 ) ) ;
#6278=CARTESIAN_POINT ( 'NONE',  ( 75.28824676885817269, -36.05057910978030122, -12.47240171960510580 ) ) ;
#6279=CARTESIAN_POINT ( 'NONE',  ( 12.58400818661273668, -65.44616333973714006, -23.49836544046852893 ) ) ;
#6281=ADVANCED_FACE ( 'NONE', ( #46424 ), #13922, .T. ) ;
#6283=CARTESIAN_POINT ( 'NONE',  ( 82.13853704237929776, 14.41952981576026005, -47.73442046593409316 ) ) ;
#6285=DIRECTION ( 'NONE',  ( -1.000000000000000000, 6.785502314117012559E-28, 1.822422554782380175E-11 ) ) ;
#6289=CARTESIAN_POINT ( 'NONE',  ( -18.46512919571819822, 21.18267207168980093, -54.23003070569360062 ) ) ;
#6290=ORIENTED_EDGE ( 'NONE', *, *, #3756, .F. ) ;
#6291=CARTESIAN_POINT ( 'NONE',  ( 52.65923618566689868, -49.77350477033189691, -48.49072211711909830 ) ) ;
#6293=DIRECTION ( 'NONE',  ( 0.6911981449639417185, -0.7226652920947607139, 0.000000000000000000 ) ) ;
#6295=CARTESIAN_POINT ( 'NONE',  ( 13.50106276864140042, 20.05783398961539632, -22.28116795780599801 ) ) ;
#6296=CARTESIAN_POINT ( 'NONE',  ( 57.59065840064920394, 13.88420960100420132, -25.33983012720019801 ) ) ;
#6299=CARTESIAN_POINT ( 'NONE',  ( 52.65272527767510269, 18.55395787694629917, -48.66231656572949760 ) ) ;
#6302=ORIENTED_EDGE ( 'NONE', *, *, #26165, .F. ) ;
#6304=B_SPLINE_CURVE_WITH_KNOTS ( 'NONE', 3,
 ( #19091, #51072, #15172, #7309, #39276, #3896, #19860, #717 ),
 .UNSPECIFIED., .F., .F.,
 ( 4, 2, 2, 4 ),
 ( 0.000000000000000000, 0.1753589473978111879, 0.6151675087881982584, 1.000000000000000000 ),
 .UNSPECIFIED. ) ;
#6306=DIRECTION ( 'NONE',  ( -0.4640893551880601597, -0.8857883891771953788, 0.000000000000000000 ) ) ;
#6308=CARTESIAN_POINT ( 'NONE',  ( 11.78673863892869988, -65.42703615493769576, -17.91922926161289809 ) ) ;
#6317=CARTESIAN_POINT ( 'NONE',  ( 10.77067511104800168, -63.19718398965360251, -45.20499083143030106 ) ) ;
#6318=PLANE ( 'NONE',  #35249 ) ;
#6321=CARTESIAN_POINT ( 'NONE',  ( 57.12444641451660488, 19.38683328975340103, -53.89324253205270310 ) ) ;
#6322=CARTESIAN_POINT ( 'NONE',  ( 53.11717555236790389, 19.14142822879220063, -77.21703359850030779 ) ) ;
#6325=DIRECTION ( 'NONE',  ( -0.4439767838697923907, -0.8960382890170686121, 0.000000000000000000 ) ) ;
#6333=CARTESIAN_POINT ( 'NONE',  ( 56.64397300593279994, -46.12966333012919762, -26.25586768246660085 ) ) ;
#6338=CARTESIAN_POINT ( 'NONE',  ( 13.39997048867730101, 20.55443781750869903, -74.14994299942661371 ) ) ;
#6341=CARTESIAN_POINT ( 'NONE',  ( 44.70608228162969766, -45.11482979815730232, -7.106782871617689956 ) ) ;
#6343=CIRCLE ( 'NONE', #41456, 40.00000000000000711 ) ;
#6346=CARTESIAN_POINT ( 'NONE',  ( 53.72142583261089754, -48.59959933175579749, -26.50701750644289945 ) ) ;
#6347=AXIS2_PLACEMENT_3D ( 'NONE', #38247, #38509, #2340 ) ;
#6348=CARTESIAN_POINT ( 'NONE',  ( 55.25034777390520446, -50.83736373112089524, -75.46481584694240041 ) ) ;
#6349=CARTESIAN_POINT ( 'NONE',  ( 3.293849930124880032, 24.23711703498809911, -8.836877851435611220 ) ) ;
#6353=EDGE_LOOP ( 'NONE', ( #16666, #46938, #49691, #41600, #25301, #41039, #39290 ) ) ;
#6355=CARTESIAN_POINT ( 'NONE',  ( 47.40902048891640419, 23.41821873921709951, -54.79940014147959459 ) ) ;
#6356=DIRECTION ( 'NONE',  ( -1.649757730820868427E-30, -1.000000000000000000, -1.919972818367709724E-16 ) ) ;
#6358=DIRECTION ( 'NONE',  ( 0.3294064756441338893, 0.9441882088883076785, 0.000000000000000000 ) ) ;
#6359=CARTESIAN_POINT ( 'NONE',  ( 11.16919178478540076, 33.86141759158169862, -17.21576959522939987 ) ) ;
#6361=CARTESIAN_POINT ( 'NONE',  ( 53.05172804014560484, 18.31224535922569885, -48.80720635444740196 ) ) ;
#6362=CARTESIAN_POINT ( 'NONE',  ( 19.16183572673343960, 24.26821873444684741, -75.85379901496348509 ) ) ;
#6363=CARTESIAN_POINT ( 'NONE',  ( 59.94009989542160355, -46.08106328245670369, -47.78644945012640477 ) ) ;
#6364=CARTESIAN_POINT ( 'NONE',  ( 53.32548350150899807, 17.93821637278129799, -27.25266754418050041 ) ) ;
#6366=CARTESIAN_POINT ( 'NONE',  ( 53.16274087092459411, 18.32513333159890223, -49.15255084583340306 ) ) ;
#6367=FACE_OUTER_BOUND ( 'NONE', #50811, .T. ) ;
#6369=CARTESIAN_POINT ( 'NONE',  ( 10.97944215675429902, 32.11615974706089816, -44.74438178823580614 ) ) ;
#6372=FACE_OUTER_BOUND ( 'NONE', #25230, .T. ) ;
#6378=CARTESIAN_POINT ( 'NONE',  ( 56.46340970881719556, 19.25363520061540257, -52.83593731267799143 ) ) ;
#6379=CARTESIAN_POINT ( 'NONE',  ( 76.51288141920070984, -2.167259785322154908, -13.28292618809263992 ) ) ;
#6381=CARTESIAN_POINT ( 'NONE',  ( 11.21372797129970067, -64.10201777544770607, -44.24198874234829759 ) ) ;
#6382=CARTESIAN_POINT ( 'NONE',  ( 57.66457883666589623, -45.12239002789189612, -25.34735987882629971 ) ) ;
#6387=DIRECTION ( 'NONE',  ( 0.000000000000000000, 1.000000000000000000, 0.000000000000000000 ) ) ;
#6388=ORIENTED_EDGE ( 'NONE', *, *, #45322, .F. ) ;
#6391=CIRCLE ( 'NONE', #4686, 2.000000000000001776 ) ;
#6393=ORIENTED_EDGE ( 'NONE', *, *, #33775, .F. ) ;
#6394=CARTESIAN_POINT ( 'NONE',  ( 53.45824824194160385, -46.01483040506809630, -14.86313069892749894 ) ) ;
#6397=CARTESIAN_POINT ( 'NONE',  ( 15.85308752007499855, 19.88381105299019680, -21.66365682949070148 ) ) ;
#6401=CARTESIAN_POINT ( 'NONE',  ( 47.18937032989539659, -54.36132375060520161, -75.29143818916560349 ) ) ;
#6402=CARTESIAN_POINT ( 'NONE',  ( 61.35257612535340144, 13.88381105527380122, -11.49664314637620066 ) ) ;
#6404=CYLINDRICAL_SURFACE ( 'NONE', #51856, 2.000000000000070610 ) ;
#6405=CARTESIAN_POINT ( 'NONE',  ( 52.20740535868720400, 20.17246182719640046, -75.93239680710080108 ) ) ;
#6407=CARTESIAN_POINT ( 'NONE',  ( 58.63648023476770277, 14.01916632703320076, -26.11532393003080088 ) ) ;
#6410=AXIS2_PLACEMENT_3D ( 'NONE', #33405, #13518, #42327 ) ;
#6411=CARTESIAN_POINT ( 'NONE',  ( 13.00893747662790112, -65.51843693869379592, -23.32157303180050079 ) ) ;
#6412=CARTESIAN_POINT ( 'NONE',  ( -8.213039659533700743, -43.95837968899080295, -4.510005153980579884 ) ) ;
#6413=CARTESIAN_POINT ( 'NONE',  ( 76.50235723590930093, 0.4624019994698309599, -13.23610440576140057 ) ) ;
#6414=CARTESIAN_POINT ( 'NONE',  ( 75.10386764943962135, 13.78341926604215750, -14.70942033535232873 ) ) ;
#6415=CARTESIAN_POINT ( 'NONE',  ( 75.47966807050509885, -43.37310274687460065, -13.40512917118210012 ) ) ;
#6416=CARTESIAN_POINT ( 'NONE',  ( 13.10603906833544485, -55.50059662380513004, -75.85379901477443809 ) ) ;
#6419=CARTESIAN_POINT ( 'NONE',  ( 82.54642784563390023, -45.59022060583280478, -47.66712544853100297 ) ) ;
#6420=DIRECTION ( 'NONE',  ( 0.5721078732755749963, -0.8201783838507928914, 0.000000000000000000 ) ) ;
#6421=CARTESIAN_POINT ( 'NONE',  ( 42.98728576789530109, 11.64384254154439979, -4.202726304293560311 ) ) ;
#6425=CARTESIAN_POINT ( 'NONE',  ( 68.13393739769790614, -49.95860450174320277, -71.35146707679190570 ) ) ;
#6427=FACE_OUTER_BOUND ( 'NONE', #20760, .T. ) ;
#6428=EDGE_LOOP ( 'NONE', ( #22399, #3553, #6431, #13915 ) ) ;
#6431=ORIENTED_EDGE ( 'NONE', *, *, #23738, .F. ) ;
#6433=DIRECTION ( 'NONE',  ( 1.000000000000000000, 0.000000000000000000, 0.000000000000000000 ) ) ;
#6438=DIRECTION ( 'NONE',  ( -9.834501533011740460E-16, -2.054487543405499690E-16, -1.000000000000000000 ) ) ;
#6439=VERTEX_POINT ( 'NONE', #42746 ) ;
#6442=CIRCLE ( 'NONE', #8076, 1.000000000000000888 ) ;
#6444=FACE_OUTER_BOUND ( 'NONE', #20375, .T. ) ;
#6445=CARTESIAN_POINT ( 'NONE',  ( 61.27924359309639613, -45.29619558891289444, -47.09340982550319410 ) ) ;
#6455=CARTESIAN_POINT ( 'NONE',  ( 51.62681347090829576, -50.36479533742150494, -76.35210449998979243 ) ) ;
#6456=CARTESIAN_POINT ( 'NONE',  ( 60.60289840739719835, 14.37099682994570138, -47.31448087610870346 ) ) ;
#6461=CARTESIAN_POINT ( 'NONE',  ( 43.02889804305800681, 14.13343854988660020, -6.968343944726750117 ) ) ;
#6462=EDGE_CURVE ( 'NONE', #45513, #30141, #33697, .T. ) ;
#6463=CARTESIAN_POINT ( 'NONE',  ( 40.87457736023439736, -44.61120891011739786, -4.704571543260979816 ) ) ;
#6464=DIRECTION ( 'NONE',  ( 1.000000000000000000, 0.000000000000000000, 0.000000000000000000 ) ) ;
#6465=CARTESIAN_POINT ( 'NONE',  ( 66.28198996516779573, 1.842642050337383264, -19.91063246777952855 ) ) ;
#6468=CARTESIAN_POINT ( 'NONE',  ( 17.87263216484612727, -51.26000751223833163, -74.91995119714192697 ) ) ;
#6470=ORIENTED_EDGE ( 'NONE', *, *, #4848, .F. ) ;
#6471=CARTESIAN_POINT ( 'NONE',  ( 57.55751162087899786, 18.85811933572209753, -52.57651812407429759 ) ) ;
#6474=CARTESIAN_POINT ( 'NONE',  ( 46.77994874552049254, -53.89178638932320098, -75.86501933388160523 ) ) ;
#6477=CARTESIAN_POINT ( 'NONE',  ( 13.13393739769619906, -63.52234721269329754, -46.39999999999999858 ) ) ;
#6480=CARTESIAN_POINT ( 'NONE',  ( 48.25999128426249740, 23.03781136496079895, -55.22775327136439927 ) ) ;
#6483=EDGE_LOOP ( 'NONE', ( #29569, #39127, #11789, #48336, #5565 ) ) ;
#6486=AXIS2_PLACEMENT_3D ( 'NONE', #9350, #25295, #21368 ) ;
#6487=CARTESIAN_POINT ( 'NONE',  ( 57.34776335324270491, 14.57942837581910034, -26.27178905609630277 ) ) ;
#6490=CARTESIAN_POINT ( 'NONE',  ( 54.12395466776580122, 16.89186266783300283, -26.13497438140159801 ) ) ;
#6492=DIRECTION ( 'NONE',  ( -0.3294064756440908681, 0.9441882088883227775, 0.000000000000000000 ) ) ;
#6495=ORIENTED_EDGE ( 'NONE', *, *, #16968, .T. ) ;
#6497=ORIENTED_EDGE ( 'NONE', *, *, #11152, .T. ) ;
#6498=EDGE_CURVE ( 'NONE', #2490, #36299, #19160, .T. ) ;
#6501=CARTESIAN_POINT ( 'NONE',  ( 54.53727200435603351, 14.79464053051451700, -15.67785519347521550 ) ) ;
#6503=DIRECTION ( 'NONE',  ( 0.9200120562340476926, 0.3918900565005438708, 0.000000000000000000 ) ) ;
#6504=ORIENTED_EDGE ( 'NONE', *, *, #10284, .F. ) ;
#6506=CARTESIAN_POINT ( 'NONE',  ( 49.72648160330989953, 22.41435850158119791, -55.11972614036179863 ) ) ;
#6508=CARTESIAN_POINT ( 'NONE',  ( 53.46099711234219143, 18.11456714212909702, -49.02220847068660703 ) ) ;
#6509=CARTESIAN_POINT ( 'NONE',  ( 65.46589392415390307, -1.325377498103930130, -16.55434372537479959 ) ) ;
#6510=CARTESIAN_POINT ( 'NONE',  ( 51.59667043160109756, -49.96101828097980047, -76.48753601724520479 ) ) ;
#6511=CARTESIAN_POINT ( 'NONE',  ( 57.25062957476220049, -50.11783017573850429, -52.59164223185749876 ) ) ;
#6512=ORIENTED_EDGE ( 'NONE', *, *, #44916, .T. ) ;
#6514=CARTESIAN_POINT ( 'NONE',  ( 69.22748654599826068, 19.47158195952029303, -72.59354914830210248 ) ) ;
#6515=VERTEX_POINT ( 'NONE', #35111 ) ;
#6519=CARTESIAN_POINT ( 'NONE',  ( 12.99344367413189971, -50.62396699225990204, -21.36723036234760187 ) ) ;
#6520=CARTESIAN_POINT ( 'NONE',  ( 54.17122153902240456, 19.43792079591710120, -76.49428706740339123 ) ) ;
#6522=CARTESIAN_POINT ( 'NONE',  ( 47.47118984295180155, -54.42867273149169449, -74.94873378728740931 ) ) ;
#6523=CARTESIAN_POINT ( 'NONE',  ( 55.61922199844690340, 13.90021221559030096, -14.76093055395720022 ) ) ;
#6524=CARTESIAN_POINT ( 'NONE',  ( 8.815605938792600682, 32.05029769220720226, -46.67186391141279955 ) ) ;
#6525=CARTESIAN_POINT ( 'NONE',  ( 56.77163879080330133, -50.67344205490699949, -53.71547587233740018 ) ) ;
#6528=VERTEX_POINT ( 'NONE', #40086 ) ;
#6529=CARTESIAN_POINT ( 'NONE',  ( 46.35275103504439898, 21.67755452994670406, -76.14999999999999147 ) ) ;
#6531=CARTESIAN_POINT ( 'NONE',  ( -12.18284927255036543, -15.61618894467929763, 6.072546842075589701 ) ) ;
#6535=CARTESIAN_POINT ( 'NONE',  ( 82.32429372338799567, 14.20864740965710027, -47.46868296552500510 ) ) ;
#6541=CARTESIAN_POINT ( 'NONE',  ( -33.78933650424870194, -10.75740117049570088, -57.07866011716559740 ) ) ;
#6543=CARTESIAN_POINT ( 'NONE',  ( 53.23189944373280014, -49.47193143504960489, -48.99600315007679541 ) ) ;
#6544=ORIENTED_EDGE ( 'NONE', *, *, #47166, .T. ) ;
#6547=CARTESIAN_POINT ( 'NONE',  ( 14.30978967243790123, 19.88381105581349573, -22.40422843537270126 ) ) ;
#6548=CARTESIAN_POINT ( 'NONE',  ( 55.97700001955439575, 14.61467643665769955, -25.52897050747419883 ) ) ;
#6551=CARTESIAN_POINT ( 'NONE',  ( 52.95534730618609842, 18.39748524797530038, -49.01774095212640248 ) ) ;
#6552=CARTESIAN_POINT ( 'NONE',  ( 55.36019775732630421, -46.03750363997700390, -16.50346971581090116 ) ) ;
#6555=EDGE_CURVE ( 'NONE', #14404, #260, #47703, .T. ) ;
#6558=CARTESIAN_POINT ( 'NONE',  ( 59.77423841227909662, 14.93359823389899788, -47.80915357183090464 ) ) ;
#6559=CARTESIAN_POINT ( 'NONE',  ( 9.469557471980332153, 33.05699343178789462, -46.83899467929160210 ) ) ;
#6561=CARTESIAN_POINT ( 'NONE',  ( 10.64977475910500004, -64.85626261263139725, -18.05902683592860214 ) ) ;
#6562=CARTESIAN_POINT ( 'NONE',  ( 52.60295254337715676, -49.82768164818063639, -48.60889610034470110 ) ) ;
#6564=DIRECTION ( 'NONE',  ( 0.8229030450105319083, 0.000000000000000000, 0.5681818181818162339 ) ) ;
#6572=CARTESIAN_POINT ( 'NONE',  ( 10.77295366634669804, -63.31447053344770381, -45.20535261670850247 ) ) ;
#6576=CARTESIAN_POINT ( 'NONE',  ( 57.28774565042520095, 19.34651099262390161, -53.44461253008790180 ) ) ;
#6577=CARTESIAN_POINT ( 'NONE',  ( 52.98832975904100095, 19.18558910406980189, -76.96373677364138643 ) ) ;
#6580=CARTESIAN_POINT ( 'NONE',  ( 60.14150383576895109, 15.95610133017432908, -49.41068029984030119 ) ) ;
#6582=EDGE_CURVE ( 'NONE', #12303, #18612, #48996, .T. ) ;
#6589=CARTESIAN_POINT ( 'NONE',  ( 74.93037295002240228, -43.11618894467930119, -15.31098073120859837 ) ) ;
#6592=CARTESIAN_POINT ( 'NONE',  ( 50.95182575631829991, 19.71852405838109945, -76.14999999999999147 ) ) ;
#6593=CARTESIAN_POINT ( 'NONE',  ( 13.78212824785540036, 20.09246212084070038, -74.56515407679870577 ) ) ;
#6594=CARTESIAN_POINT ( 'NONE',  ( 57.24929578595760660, 21.38381105532069881, -63.99406948319570887 ) ) ;
#6595=CARTESIAN_POINT ( 'NONE',  ( 41.35125392209459960, -44.98027078473889873, -5.668951409370400540 ) ) ;
#6602=CARTESIAN_POINT ( 'NONE',  ( 52.67941827447170056, -49.73994065207369886, -27.56303321415330032 ) ) ;
#6603=CARTESIAN_POINT ( 'NONE',  ( 54.78812434636329698, -50.98684819909150434, -75.45670350304489205 ) ) ;
#6604=CARTESIAN_POINT ( 'NONE',  ( 10.28185505973059932, 33.24230909050100280, -17.86151643087199758 ) ) ;
#6607=CARTESIAN_POINT ( 'NONE',  ( 6.187261889072820154, -46.71083452957879700, -20.15000000000000213 ) ) ;
#6609=CARTESIAN_POINT ( 'NONE',  ( -10.89082349597999944, -42.33811146364660516, -6.201050197583099610 ) ) ;
#6610=CARTESIAN_POINT ( 'NONE',  ( 47.48653415169840031, 23.37519123828230150, -54.89669719852860652 ) ) ;
#6612=LINE ( 'NONE', #7389, #19300 ) ;
#6614=CARTESIAN_POINT ( 'NONE',  ( 11.91426296011000119, 33.88532756217980335, -16.60966417100599912 ) ) ;
#6615=CARTESIAN_POINT ( 'NONE',  ( 7.853097003783789276, 29.28805065900050053, -20.86915960608759946 ) ) ;
#6616=CARTESIAN_POINT ( 'NONE',  ( 52.83464909576289159, 18.42637314819869943, -48.65907448191860141 ) ) ;
#6617=LINE ( 'NONE', #45421, #48424 ) ;
#6619=CARTESIAN_POINT ( 'NONE',  ( 53.37647868240819804, 17.93233224264670156, -27.30365310598189765 ) ) ;
#6622=CARTESIAN_POINT ( 'NONE',  ( 11.10574934303680017, -63.48107579820671020, -44.26157399421149563 ) ) ;
#6623=CARTESIAN_POINT ( 'NONE',  ( 52.77399500191609860, 18.49248106158579930, -48.90117827005099826 ) ) ;
#6626=CARTESIAN_POINT ( 'NONE',  ( 11.10574934303680017, 32.24869790884810072, -44.26157399421149563 ) ) ;
#6629=CARTESIAN_POINT ( 'NONE',  ( 65.13922429466639130, -32.18685348281329794, -17.74407301686150262 ) ) ;
#6631=CARTESIAN_POINT ( 'NONE',  ( 12.18502445233735187, 24.18831204814821945, -74.66535148663518839 ) ) ;
#6634=FACE_OUTER_BOUND ( 'NONE', #44763, .T. ) ;
#6635=CARTESIAN_POINT ( 'NONE',  ( 48.94724833445295076, -2.939553391498948898, -15.65000000114250334 ) ) ;
#6637=CARTESIAN_POINT ( 'NONE',  ( 11.39881522676340175, -64.71865303079098908, -45.74527777199200784 ) ) ;
#6638=CARTESIAN_POINT ( 'NONE',  ( 56.54952170946580736, -45.45011454905849746, -25.70425748956289880 ) ) ;
#6639=PLANE ( 'NONE',  #29466 ) ;
#6640=CIRCLE ( 'NONE', #29203, 2.000000000000001332 ) ;
#6642=ORIENTED_EDGE ( 'NONE', *, *, #45969, .F. ) ;
#6647=CARTESIAN_POINT ( 'NONE',  ( 12.26871351663039889, 34.23561203028980060, -22.61095353172289890 ) ) ;
#6648=ORIENTED_EDGE ( 'NONE', *, *, #12738, .F. ) ;
#6649=CARTESIAN_POINT ( 'NONE',  ( 48.26658354509820725, -45.11618894467940066, -9.084211283098401424 ) ) ;
#6651=AXIS2_PLACEMENT_3D ( 'NONE', #39876, #2945, #31718 ) ;
#6652=CARTESIAN_POINT ( 'NONE',  ( 16.65429250104310199, 19.88381105411679783, -20.30769847209329981 ) ) ;
#6657=CARTESIAN_POINT ( 'NONE',  ( 46.61365481427139912, -53.40542986336679832, -76.07618347743780873 ) ) ;
#6658=CARTESIAN_POINT ( 'NONE',  ( 60.84977283502919931, 12.51329875045430029, -9.366796605703170187 ) ) ;
#6659=FACE_OUTER_BOUND ( 'NONE', #45429, .T. ) ;
#6660=CARTESIAN_POINT ( 'NONE',  ( 53.38272065464079930, 20.08420318064650090, -75.68264751698761472 ) ) ;
#6662=EDGE_CURVE ( 'NONE', #2811, #17149, #14640, .T. ) ;
#6667=CARTESIAN_POINT ( 'NONE',  ( 4.986282691042689841, -58.88488589497760728, -12.65546072889769924 ) ) ;
#6668=CARTESIAN_POINT ( 'NONE',  ( 75.73654537959819777, -5.923657072368180287, -11.84124065471690024 ) ) ;
#6669=CARTESIAN_POINT ( 'NONE',  ( 75.07825548516527192, 13.81215145325568550, -14.79904531683525626 ) ) ;
#6670=CARTESIAN_POINT ( 'NONE',  ( 75.19651472130358627, -44.95919067516332035, -14.38756988197933495 ) ) ;
#6671=VECTOR ( 'NONE', #469, 1000.000000000000000 ) ;
#6673=CARTESIAN_POINT ( 'NONE',  ( 12.75813532167091324, -55.47348756089835575, -75.58682750841406062 ) ) ;
#6674=AXIS2_PLACEMENT_3D ( 'NONE', #39344, #14712, #3445 ) ;
#6679=CARTESIAN_POINT ( 'NONE',  ( 40.36721523011259904, 13.65407319109449880, -4.296538310234210734 ) ) ;
#6680=DIRECTION ( 'NONE',  ( 0.000000000000000000, -1.000000000000000000, 0.000000000000000000 ) ) ;
#6685=CARTESIAN_POINT ( 'NONE',  ( 17.83683460335419824, -52.03647206054819918, -75.81086730487160708 ) ) ;
#6686=CARTESIAN_POINT ( 'NONE',  ( 58.84619698805219912, -43.44629174156790441, -8.775524122719259523 ) ) ;
#6687=ORIENTED_EDGE ( 'NONE', *, *, #37574, .T. ) ;
#6692=VERTEX_POINT ( 'NONE', #14625 ) ;
#6694=CARTESIAN_POINT ( 'NONE',  ( 60.41799884498819750, -45.84359652593190049, -47.74079192425810447 ) ) ;
#6695=CARTESIAN_POINT ( 'NONE',  ( 56.17779366879769753, 14.41653637947479893, -28.15000000000000213 ) ) ;
#6698=CARTESIAN_POINT ( 'NONE',  ( 41.19621318014409894, -45.49641962229259917, -6.107574381499630611 ) ) ;
#6699=EDGE_CURVE ( 'NONE', #40057, #15227, #26666, .T. ) ;
#6700=ORIENTED_EDGE ( 'NONE', *, *, #48595, .F. ) ;
#6702=ORIENTED_EDGE ( 'NONE', *, *, #26777, .T. ) ;
#6703=CARTESIAN_POINT ( 'NONE',  ( 55.55365133010059964, -45.11618894467940066, -14.32025150907159983 ) ) ;
#6704=CARTESIAN_POINT ( 'NONE',  ( 61.39588726022179799, -45.18041116279739811, -46.45920956806440216 ) ) ;
#6705=CARTESIAN_POINT ( 'NONE',  ( 82.46534343335889616, -45.09316689051424731, -46.44242255414575737 ) ) ;
#6708=ORIENTED_EDGE ( 'NONE', *, *, #13673, .T. ) ;
#6713=AXIS2_PLACEMENT_3D ( 'NONE', #15930, #23766, #27453 ) ;
#6714=ORIENTED_EDGE ( 'NONE', *, *, #31813, .F. ) ;
#6716=CARTESIAN_POINT ( 'NONE',  ( 51.15928635398449842, -50.96517669477629653, -76.15045079391039451 ) ) ;
#6717=VECTOR ( 'NONE', #30262, 1000.000000000000000 ) ;
#6718=CARTESIAN_POINT ( 'NONE',  ( 60.32710813244079873, 14.50229188127310032, -47.29630948315320182 ) ) ;
#6720=CARTESIAN_POINT ( 'NONE',  ( 61.75019796695539753, 14.88381105532069881, -37.26101630944549470 ) ) ;
#6721=CARTESIAN_POINT ( 'NONE',  ( 40.73531874280419629, -44.64268826760660147, -4.523453480819620509 ) ) ;
#6724=CARTESIAN_POINT ( 'NONE',  ( -3.308601418378690262, 17.32579908435650040, -5.270794404415338974 ) ) ;
#6729=ORIENTED_EDGE ( 'NONE', *, *, #26096, .F. ) ;
#6730=CARTESIAN_POINT ( 'NONE',  ( 14.53574929604680044, -52.38593004734789815, -75.99067819366339904 ) ) ;
#6731=ADVANCED_FACE ( 'NONE', ( #34258 ), #40379, .T. ) ;
#6733=CARTESIAN_POINT ( 'NONE',  ( 11.89321892218980103, -65.43602743108449715, -22.25048313876769868 ) ) ;
#6740=CARTESIAN_POINT ( 'NONE',  ( 47.86038305415719663, -54.40158572345529819, -54.84188222968870008 ) ) ;
#6743=CARTESIAN_POINT ( 'NONE',  ( 47.79491795492819506, 23.18827802853950004, -54.76904050233790144 ) ) ;
#6744=CIRCLE ( 'NONE', #51113, 14.50000000000000178 ) ;
#6747=ORIENTED_EDGE ( 'NONE', *, *, #16591, .F. ) ;
#6751=DIRECTION ( 'NONE',  ( 0.000000000000000000, 0.000000000000000000, -1.000000000000000000 ) ) ;
#6752=CARTESIAN_POINT ( 'NONE',  ( 84.44784216359251161, 11.88381105532070059, -47.47585302082339354 ) ) ;
#6753=DIRECTION ( 'NONE',  ( 0.000000000000000000, 0.000000000000000000, -1.000000000000000000 ) ) ;
#6756=DIRECTION ( 'NONE',  ( 0.000000000000000000, 0.000000000000000000, 1.000000000000000000 ) ) ;
#6760=B_SPLINE_SURFACE_WITH_KNOTS ( 'NONE', 3, 3, ( 
 ( #9613, #32914, #25046, #49201, #33440, #13549, #5426, #45516, #45773, #9865, #44733, #4900, #13293, #41063, #24789, #25819 ),
 ( #21896, #41831, #16691, #5175, #48673, #32648, #12777, #8838, #45259, #41571, #40797, #21130, #25313, #38419, #22928, #46559 ),
 ( #30280, #38162, #10910, #42620, #14311, #38948, #50731, #10649, #18753, #6976, #26872, #46038, #2518, #6718, #14830, #50481 ),
 ( #50989, #22673, #30536, #26604, #26087, #3038, #42879, #46300, #6456, #10387, #19012, #34988, #47078, #15089, #10129, #38693 ),
 ( #43140, #2260, #34200, #2782, #34729, #30794, #7232, #26343, #42355, #22416, #46820, #31055, #14054, #18500, #11166, #33947 ),
 ( #27134, #30015, #42095, #34471, #6198, #18235, #37907, #2000, #17980, #49964, #22153, #50222, #14571, #36025, #20029, #39462 ),
 ( #24201, #16111, #31821, #43392, #7487, #16372, #136, #28408, #40227, #23182, #44416, #23439, #47585, #19532, #39199, #3559 ),
 ( #43901, #11941, #3294, #7996, #4316, #23948, #7751, #39968, #32327, #35520, #32073, #51510, #15610, #23698, #4063, #48091 ),
 ( #27647, #48348, #31564, #27898, #28150, #19273, #35258, #12443, #44154, #11680, #39713, #20285, #43650, #3817, #51258, #15353 ),
 ( #19786, #35778, #31305, #36278, #12190, #8250, #386, #47334, #27390, #47838, #51761, #11426, #15861, #49658, #13497, #907 ),
 ( #32581, #25509, #16901, #9558, #21323, #13749, #24465, #44672, #17413, #8518, #8775, #13239, #5115, #28932, #41257, #45195 ) ),
 .UNSPECIFIED., .F., .F., .F.,
 ( 4, 1, 1, 1, 1, 1, 1, 1, 4 ),
 ( 4, 2, 2, 2, 2, 2, 2, 4 ),
 ( 0.000000000000000000, 0.1250000000000000000, 0.2500000000000000000, 0.3750000000000000000, 0.5000000000000000000, 0.6250000000000000000, 0.7500000000000000000, 0.8750000000000000000, 1.000000000000000000 ),
 ( 0.000000000000000000, 0.1402455969909039979, 0.3005262792662219962, 0.4007017056882959949, 0.4507894188993329943, 0.5309297600369919934, 0.6591543058572471026, 0.8014034113765919898 ),
 .UNSPECIFIED. ) ;
#6762=CARTESIAN_POINT ( 'NONE',  ( 11.51160566532330165, 19.89559162839070083, -21.14999999999999858 ) ) ;
#6763=ORIENTED_EDGE ( 'NONE', *, *, #1106, .T. ) ;
#6765=CARTESIAN_POINT ( 'NONE',  ( 12.24533245415720017, -64.90027884028160088, -16.17634614696339668 ) ) ;
#6767=CARTESIAN_POINT ( 'NONE',  ( 76.46365438545950610, -25.95764364605460983, -13.07079957363982814 ) ) ;
#6768=CARTESIAN_POINT ( 'NONE',  ( 12.89950475509210115, -65.51158420262359527, -47.71261340485989422 ) ) ;
#6770=EDGE_LOOP ( 'NONE', ( #25594, #32626, #41467, #33041 ) ) ;
#6773=CARTESIAN_POINT ( 'NONE',  ( 47.68692968653899555, 23.40598529524750049, -55.28501249849080068 ) ) ;
#6774=CARTESIAN_POINT ( 'NONE',  ( 64.67926456151019465, 0.3460283776947450374, -17.08790319438210048 ) ) ;
#6775=CARTESIAN_POINT ( 'NONE',  ( 51.86152422305890042, -49.39855420986879864, -77.00280416433220410 ) ) ;
#6776=CARTESIAN_POINT ( 'NONE',  ( 56.78254564749959599, -50.61158444988599570, -53.13069165659919690 ) ) ;
#6780=ORIENTED_EDGE ( 'NONE', *, *, #42246, .F. ) ;
#6784=CARTESIAN_POINT ( 'NONE',  ( 13.79398456934750072, -51.11484069242550277, -22.16948675641290123 ) ) ;
#6785=B_SPLINE_CURVE_WITH_KNOTS ( 'NONE', 3,
 ( #49421, #25533, #13517, #28690, #17183, #5134, #20828, #36825, #21090, #5652, #6947, #14283, #30507, #17946, #29725, #33914, #18721, #46004, #38388, #10877, #42850, #41796, #46530, #22899, #18466, #34171, #34439, #38916, #22384, #10619, #49932, #50449, #18205, #50189, #50700, #45739, #3007, #21865, #10356, #6164, #26573, #26840 ),
 .UNSPECIFIED., .F., .F.,
 ( 4, 2, 2, 1, 1, 2, 2, 2, 2, 1, 1, 2, 2, 2, 2, 1, 1, 2, 2, 2, 1, 1, 2, 2, 4 ),
 ( 0.000000000000000000, 0.1250000000000936196, 0.1875000000001387224, 0.2187500000001632583, 0.2343750000001697253, 0.2421875000001709188, 0.2500000000001720846, 0.3750000000001643685, 0.4375000000001614819, 0.4687500000001668110, 0.4843750000001631473, 0.4921875000001623701, 0.5000000000001615375, 0.6250000000001039169, 0.6875000000000743849, 0.7187500000000507372, 0.7343750000000396350, 0.7421875000000440759, 0.7500000000000484057, 0.8125000000000045519, 0.8437499999999744649, 0.8593749999999678035, 0.8671874999999650280, 0.8749999999999622524, 1.000000000000000000 ),
 .UNSPECIFIED. ) ;
#6786=CARTESIAN_POINT ( 'NONE',  ( 54.67587076525569501, 19.38381105532069881, -76.72550994220580378 ) ) ;
#6787=CARTESIAN_POINT ( 'NONE',  ( 46.70520323956110076, -53.35084480228680093, -76.07728942632040514 ) ) ;
#6788=CARTESIAN_POINT ( 'NONE',  ( 57.24436406277250455, 13.89534489142819851, -17.69598351972189931 ) ) ;
#6790=CARTESIAN_POINT ( 'NONE',  ( 56.56050783365309798, -50.71580908316560254, -53.48830978476309639 ) ) ;
#6795=ORIENTED_EDGE ( 'NONE', *, *, #21797, .T. ) ;
#6796=CARTESIAN_POINT ( 'NONE',  ( 47.42018403062719756, 23.12668429572390139, -75.11910893338719575 ) ) ;
#6797=ADVANCED_FACE ( 'NONE', ( #20598 ), #9183, .T. ) ;
#6800=CARTESIAN_POINT ( 'NONE',  ( 44.45072406794265163, -15.61618894467929408, 6.072546842075589701 ) ) ;
#6805=CARTESIAN_POINT ( 'NONE',  ( 53.82997852138471018, 19.36722236602833291, -77.06221308720526508 ) ) ;
#6808=DIRECTION ( 'NONE',  ( 0.000000000000000000, 0.000000000000000000, 1.000000000000000000 ) ) ;
#6809=CARTESIAN_POINT ( 'NONE',  ( -32.94143001319760344, -10.86309130919419985, -56.02216466475820056 ) ) ;
#6811=CARTESIAN_POINT ( 'NONE',  ( 52.83452152375440392, -49.66311762893110426, -48.76554745825549730 ) ) ;
#6812=ORIENTED_EDGE ( 'NONE', *, *, #27902, .T. ) ;
#6813=CARTESIAN_POINT ( 'NONE',  ( 17.47784055284634164, 21.13935400224278283, -76.01806011802844409 ) ) ;
#6815=CARTESIAN_POINT ( 'NONE',  ( 13.56093559663669978, 20.01022379959449893, -22.27875244362760299 ) ) ;
#6816=CARTESIAN_POINT ( 'NONE',  ( 83.70899958829821230, 13.23037409732310010, -46.59258846095900708 ) ) ;
#6818=CARTESIAN_POINT ( 'NONE',  ( 52.68346203708500042, 18.53457133105899857, -48.72605036086640240 ) ) ;
#6819=CARTESIAN_POINT ( 'NONE',  ( 56.08437071186119738, -45.70248805069130071, -17.77137460264779989 ) ) ;
#6821=CYLINDRICAL_SURFACE ( 'NONE', #38100, 2.000000000000170530 ) ;
#6822=ORIENTED_EDGE ( 'NONE', *, *, #34531, .F. ) ;
#6826=DIRECTION ( 'NONE',  ( -0.4640893551880381218, 0.8857883891772070362, 0.000000000000000000 ) ) ;
#6827=CARTESIAN_POINT ( 'NONE',  ( 10.42914237359489960, 33.65646982241409546, -47.08729022436619971 ) ) ;
#6830=CARTESIAN_POINT ( 'NONE',  ( 55.91595722987329964, -45.90465052577939531, -25.32543029193989881 ) ) ;
#6831=CARTESIAN_POINT ( 'NONE',  ( 52.57435367313225782, -49.85246693219066572, -48.51308846454130475 ) ) ;
#6837=VERTEX_POINT ( 'NONE', #14280 ) ;
#6839=ORIENTED_EDGE ( 'NONE', *, *, #18392, .T. ) ;
#6840=CARTESIAN_POINT ( 'NONE',  ( 10.48523087532100107, -63.11543068638779630, -45.62962604688630108 ) ) ;
#6842=ORIENTED_EDGE ( 'NONE', *, *, #41294, .T. ) ;
#6844=CARTESIAN_POINT ( 'NONE',  ( 57.28991729228510366, 19.34649676830889931, -53.44461810997239581 ) ) ;
#6845=CARTESIAN_POINT ( 'NONE',  ( 53.79479188179159621, 19.37048951312020151, -76.98386108904900027 ) ) ;
#6847=CARTESIAN_POINT ( 'NONE',  ( 8.875293496618541056, -63.51482374781645746, -46.68678634667735139 ) ) ;
#6849=CARTESIAN_POINT ( 'NONE',  ( 15.05440318628110141, 21.88381105532300097, -76.14999999999999147 ) ) ;
#6859=CARTESIAN_POINT ( 'NONE',  ( 52.56445806708630641, -49.86260722447150329, -48.47378032971909789 ) ) ;
#6863=DIRECTION ( 'NONE',  ( 7.935614746461580696E-16, 6.060292087350920604E-16, -1.000000000000000000 ) ) ;
#6866=CARTESIAN_POINT ( 'NONE',  ( 41.23778026548699671, -45.08170077868949477, -5.742147589652049966 ) ) ;
#6867=AXIS2_PLACEMENT_3D ( 'NONE', #39707, #46814, #19263 ) ;
#6870=CARTESIAN_POINT ( 'NONE',  ( 54.18928026078430094, -48.04840664809780293, -26.03349461057250025 ) ) ;
#6871=CARTESIAN_POINT ( 'NONE',  ( 56.50083622498900127, -50.76116396499730143, -74.29147146558989334 ) ) ;
#6872=CARTESIAN_POINT ( 'NONE',  ( -8.804542933903709567, 12.11215359422420157, -4.447949915414280753 ) ) ;
#6873=CARTESIAN_POINT ( 'NONE',  ( 16.13393739769620083, -15.61618894467929941, -19.14999999999999858 ) ) ;
#6874=CARTESIAN_POINT ( 'NONE',  ( 47.18324681005260146, -54.80726426785999905, -54.61059023070370699 ) ) ;
#6875=CARTESIAN_POINT ( 'NONE',  ( 47.18325654339099628, 23.57487866773040253, -54.61058579560449289 ) ) ;
#6877=CARTESIAN_POINT ( 'NONE',  ( -8.116933555837720249, -44.87420182772909527, -5.094470740012030596 ) ) ;
#6878=CARTESIAN_POINT ( 'NONE',  ( 47.80451765783929829, 23.19120698434290162, -54.80734825992600179 ) ) ;
#6879=CARTESIAN_POINT ( 'NONE',  ( 56.17779366879769753, -45.64891426883350078, -28.15000000000000213 ) ) ;
#6881=CARTESIAN_POINT ( 'NONE',  ( 61.12568535967459837, 14.12366961404920040, -47.15003794073030008 ) ) ;
#6882=CARTESIAN_POINT ( 'NONE',  ( 12.04669083382830053, 34.10719181568249780, -17.12210558019860329 ) ) ;
#6883=CARTESIAN_POINT ( 'NONE',  ( 51.75950492042200324, 18.21739703323269666, -76.84761919141568853 ) ) ;
#6884=CARTESIAN_POINT ( 'NONE',  ( 53.18776295313059421, 18.24184040730330025, -48.84930895489249991 ) ) ;
#6887=CARTESIAN_POINT ( 'NONE',  ( 55.96589641171290452, 15.46583100414529888, -26.32679269575499958 ) ) ;
#6888=CARTESIAN_POINT ( 'NONE',  ( 50.58453602478152789, 4.710080170683036194, -76.22811488052452944 ) ) ;
#6890=CARTESIAN_POINT ( 'NONE',  ( 9.746758075853771075, -63.31345910889199757, -46.29788637164419640 ) ) ;
#6892=DIRECTION ( 'NONE',  ( 0.4042525045258802963, 0.000000000000000000, -0.9146474252872268673 ) ) ;
#6894=CARTESIAN_POINT ( 'NONE',  ( 10.77457706359389888, 32.17075419748780263, -45.20848294960729419 ) ) ;
#6896=DIRECTION ( 'NONE',  ( 0.3294064756440934771, -0.9441882088883220003, -3.885780586188049864E-16 ) ) ;
#6900=CARTESIAN_POINT ( 'NONE',  ( 40.50275707922880031, 13.54185611314979987, -4.148922232357650230 ) ) ;
#6901=CARTESIAN_POINT ( 'NONE',  ( 76.55750383288518890, 0.1397330900750557992, -13.47521080995300480 ) ) ;
#6903=CARTESIAN_POINT ( 'NONE',  ( 56.51428737249189993, -45.39462441605950005, -25.50343997284580055 ) ) ;
#6912=CARTESIAN_POINT ( 'NONE',  ( 11.73992142287220197, 32.72645697550250077, -24.71095559905290173 ) ) ;
#6916=CARTESIAN_POINT ( 'NONE',  ( 16.05893884862259924, 19.85742967422829608, -20.93640534643579798 ) ) ;
#6918=CARTESIAN_POINT ( 'NONE',  ( 60.96203672470600310, -29.75511121401200043, -15.98584738528380278 ) ) ;
#6919=CARTESIAN_POINT ( 'NONE',  ( 16.13393739769620083, -15.61618894467929941, -6.649999999999999467 ) ) ;
#6920=CARTESIAN_POINT ( 'NONE',  ( 47.07006461603570102, -54.26997103497729569, -75.46887108633241326 ) ) ;
#6921=CARTESIAN_POINT ( 'NONE',  ( 49.81260523996059675, 12.27001346555440087, -6.460395669183189860 ) ) ;
#6922=EDGE_CURVE ( 'NONE', #46486, #29806, #17712, .T. ) ;
#6926=DIRECTION ( 'NONE',  ( 0.000000000000000000, 0.000000000000000000, 1.000000000000000000 ) ) ;
#6929=ORIENTED_EDGE ( 'NONE', *, *, #10533, .F. ) ;
#6930=CARTESIAN_POINT ( 'NONE',  ( 54.23650158716049674, -48.37337528119039831, -26.83965679272169780 ) ) ;
#6931=CARTESIAN_POINT ( 'NONE',  ( 9.468372918422769402, -62.32709119060739766, -13.97902442704289960 ) ) ;
#6932=CARTESIAN_POINT ( 'NONE',  ( 75.70026563160030264, -21.87202185586589565, -11.67482764317330002 ) ) ;
#6933=CARTESIAN_POINT ( 'NONE',  ( 75.35176292259957620, 13.18942012435235078, -13.85075860070319287 ) ) ;
#6935=AXIS2_PLACEMENT_3D ( 'NONE', #24259, #3612, #27945 ) ;
#6936=DIRECTION ( 'NONE',  ( 0.000000000000000000, -1.000000000000000000, 0.000000000000000000 ) ) ;
#6939=EDGE_CURVE ( 'NONE', #28860, #11300, #20871, .T. ) ;
#6940=DIRECTION ( 'NONE',  ( 0.000000000000000000, -1.000000000000000000, 0.000000000000000000 ) ) ;
#6942=CARTESIAN_POINT ( 'NONE',  ( 42.30536707493200055, 11.93584660880990000, -3.349718967436809525 ) ) ;
#6944=CARTESIAN_POINT ( 'NONE',  ( 65.36732126366399598, -45.11618894467940066, -12.60113342886489995 ) ) ;
#6945=CARTESIAN_POINT ( 'NONE',  ( 19.53299984191638927, 24.23912880602019726, -75.56421462368636810 ) ) ;
#6947=CARTESIAN_POINT ( 'NONE',  ( 76.69488533474444125, -43.19260729310870062, -14.37252596537610394 ) ) ;
#6948=CARTESIAN_POINT ( 'NONE',  ( 17.63527260060340041, -51.92834279550939414, -75.76244777734170555 ) ) ;
#6949=CARTESIAN_POINT ( 'NONE',  ( 43.06099782924809460, -45.11618894467940066, -6.588391211254950086 ) ) ;
#6953=ORIENTED_EDGE ( 'NONE', *, *, #30300, .F. ) ;
#6955=DIRECTION ( 'NONE',  ( -0.2260571801428090388, -1.168509733417976470E-14, 0.9741140340359961680 ) ) ;
#6958=CARTESIAN_POINT ( 'NONE',  ( 41.40015264295030306, -45.44364689039419858, -6.186196351018840467 ) ) ;
#6960=ORIENTED_EDGE ( 'NONE', *, *, #43477, .T. ) ;
#6966=ORIENTED_EDGE ( 'NONE', *, *, #14618, .F. ) ;
#6967=CARTESIAN_POINT ( 'NONE',  ( -5.366062602303798279, -15.61618894467929586, -11.65000000000000036 ) ) ;
#6968=ORIENTED_EDGE ( 'NONE', *, *, #9854, .T. ) ;
#6969=FACE_OUTER_BOUND ( 'NONE', #50521, .T. ) ;
#6971=AXIS2_PLACEMENT_3D ( 'NONE', #38850, #6356, #34629 ) ;
#6975=CARTESIAN_POINT ( 'NONE',  ( 53.64468172317890549, -51.26703106273480159, -75.63087525034551106 ) ) ;
#6976=CARTESIAN_POINT ( 'NONE',  ( 60.53471020050410090, 14.39428645268190010, -47.24686264531659674 ) ) ;
#6978=CARTESIAN_POINT ( 'NONE',  ( 40.87221823369649343, -44.53072057087500468, -4.420649961794050675 ) ) ;
#6980=CARTESIAN_POINT ( 'NONE',  ( -6.895430101768229569, 14.71875163426810040, -5.354287734213469818 ) ) ;
#6983=LINE ( 'NONE', #11688, #21374 ) ;
#6984=CARTESIAN_POINT ( 'NONE',  ( 17.77818319944547909, -51.52597369355607526, -75.36997958382859508 ) ) ;
#6985=EDGE_CURVE ( 'NONE', #51033, #26368, #51406, .T. ) ;
#6988=CARTESIAN_POINT ( 'NONE',  ( -1.365754458141149819, 11.26366790782569893, -20.15000000000000213 ) ) ;
#6990=CARTESIAN_POINT ( 'NONE',  ( 57.55751162087899786, 19.35892401864479950, -53.59933301304759823 ) ) ;
#6993=CARTESIAN_POINT ( 'NONE',  ( 15.66736729374060211, 19.66432312694319862, -20.45701610577899743 ) ) ;
#6994=( BOUNDED_CURVE ( )  B_SPLINE_CURVE ( 3, ( #51129, #7361, #39330, #3433 ),
 .UNSPECIFIED., .F., .T. ) 
 B_SPLINE_CURVE_WITH_KNOTS ( ( 4, 4 ),
 ( 0.000000000000000000, 0.5134355670272889860 ),
 .UNSPECIFIED. ) 
 CURVE ( )  GEOMETRIC_REPRESENTATION_ITEM ( )  RATIONAL_B_SPLINE_CURVE ( ( 1.000000000000000000, 0.9781523768112215800, 0.9781523768112215800, 1.000000000000000000 ) ) 
 REPRESENTATION_ITEM ( '' )  );
#6995=B_SPLINE_CURVE_WITH_KNOTS ( 'NONE', 3,
 ( #12590, #44551, #8651, #40620, #17300, #6018, #34285, #45856, #9688, #9942, #50306, #9441, #34029, #45337, #25390, #45592, #25648, #26168, #21204, #30355, #49278, #13627, #21975, #30098, #6278, #10207, #33776, #42178, #29587, #41917, #41652, #17802, #37987 ),
 .UNSPECIFIED., .F., .F.,
 ( 4, 2, 2, 2, 1, 1, 1, 1, 1, 1, 1, 2, 2, 2, 2, 1, 1, 1, 1, 2, 2, 4 ),
 ( 0.000000000000000000, 0.2500000000003731460, 0.3750000000005595524, 0.4375000000006527001, 0.4687500000006993850, 0.4843750000007223111, 0.4921875000007341350, 0.4960937500007400192, 0.4980468750007425172, 0.4990234375007434053, 0.4995117187507441825, 0.4997558593757441270, 0.5000000000007440715, 0.6250000000005758727, 0.6875000000004914957, 0.7187500000004496403, 0.7343750000004286571, 0.7421875000004182210, 0.7460937500004128919, 0.7480468750004098943, 0.7500000000004067857, 1.000000000000000000 ),
 .UNSPECIFIED. ) ;
#6997=DIRECTION ( 'NONE',  ( -0.000000000000000000, -1.000000000000000000, -0.000000000000000000 ) ) ;
#6998=CARTESIAN_POINT ( 'NONE',  ( 48.08635818190299460, -54.25091888102380011, -54.70531615945079551 ) ) ;
#7002=CARTESIAN_POINT ( 'NONE',  ( 47.68999173674550462, 23.28182553471719984, -55.17369749140770097 ) ) ;
#7004=CIRCLE ( 'NONE', #32894, 2.000000000000004441 ) ;
#7006=AXIS2_PLACEMENT_3D ( 'NONE', #46745, #35438, #3220 ) ;
#7014=DIRECTION ( 'NONE',  ( 1.000000000000000000, -4.005157696510369650E-32, -3.556943099846429769E-14 ) ) ;
#7019=ORIENTED_EDGE ( 'NONE', *, *, #21105, .T. ) ;
#7020=ORIENTED_EDGE ( 'NONE', *, *, #24991, .T. ) ;
#7021=CARTESIAN_POINT ( 'NONE',  ( 12.36320305068320025, -64.54682834576858852, -15.76422791927960176 ) ) ;
#7023=CARTESIAN_POINT ( 'NONE',  ( 76.42505012355316296, -22.70526211292518326, -12.90445136872428655 ) ) ;
#7024=CARTESIAN_POINT ( 'NONE',  ( 11.26003149166710138, -65.11465353321858629, -47.09181534538819847 ) ) ;
#7025=ORIENTED_EDGE ( 'NONE', *, *, #24143, .F. ) ;
#7029=CARTESIAN_POINT ( 'NONE',  ( 56.79275862933049979, 14.79020353670410159, -26.24735317389830058 ) ) ;
#7030=EDGE_CURVE ( 'NONE', #43570, #14404, #18620, .T. ) ;
#7031=AXIS2_PLACEMENT_3D ( 'NONE', #3872, #39769, #7288 ) ;
#7033=CARTESIAN_POINT ( 'NONE',  ( 59.64872764346009859, -1.856411653216130109, -15.80443724322539900 ) ) ;
#7040=CARTESIAN_POINT ( 'NONE',  ( 55.55365133010059964, -45.11618894467940066, -14.32025150907159983 ) ) ;
#7042=CARTESIAN_POINT ( 'NONE',  ( 13.55383807960289921, -51.02647431419499924, -21.89020893026379611 ) ) ;
#7043=CARTESIAN_POINT ( 'NONE',  ( 57.24950193371399365, 19.38381105532069881, -74.41700251245109143 ) ) ;
#7045=CARTESIAN_POINT ( 'NONE',  ( 57.13451053105050192, 13.89565872282230075, -17.02117289981309867 ) ) ;
#7046=CARTESIAN_POINT ( 'NONE',  ( 61.00296193527120181, -45.42954057104920196, -47.27669373200819791 ) ) ;
#7047=AXIS2_PLACEMENT_3D ( 'NONE', #4083, #48113, #8275 ) ;
#7048=B_SPLINE_CURVE_WITH_KNOTS ( 'NONE', 3,
 ( #50975, #46549, #23425, #31292, #34716, #26858, #14818, #11413, #27375, #15598, #19517, #14557, #47067, #26590, #11668, #6703 ),
 .UNSPECIFIED., .F., .F.,
 ( 4, 2, 2, 2, 2, 2, 2, 4 ),
 ( -4.238728269404560045, -3.496950822258759750, -2.649205168377850139, -2.119364134702280023, -1.854443617864499849, -1.430570790924039937, -0.7523742678193099387, -8.881784197001252323E-16 ),
 .UNSPECIFIED. ) ;
#7049=CARTESIAN_POINT ( 'NONE',  ( 56.62412426209190386, -50.71562078093869985, -53.71767670194419964 ) ) ;
#7052=EDGE_CURVE ( 'NONE', #13860, #1516, #5820, .T. ) ;
#7053=VERTEX_POINT ( 'NONE', #47300 ) ;
#7054=CARTESIAN_POINT ( 'NONE',  ( 47.18716110640669825, 22.75249779235520009, -75.65750133416010215 ) ) ;
#7057=CARTESIAN_POINT ( 'NONE',  ( 17.87990108355959862, 20.00716050925151990, -74.86151687916520814 ) ) ;
#7059=CARTESIAN_POINT ( 'NONE',  ( 60.34784566561199881, 13.88381105532070059, -11.22422230768829898 ) ) ;
#7061=CARTESIAN_POINT ( 'NONE',  ( 82.13853704237929776, 14.20578202076580077, -47.46441090728419709 ) ) ;
#7065=DIRECTION ( 'NONE',  ( -1.000000000000000000, 0.000000000000000000, 0.000000000000000000 ) ) ;
#7068=CARTESIAN_POINT ( 'NONE',  ( 49.44022876851060033, 22.43072660820480024, -54.54742833745199704 ) ) ;
#7070=CARTESIAN_POINT ( 'NONE',  ( 53.42698669076009566, -49.38007291881159944, -49.00234524114569723 ) ) ;
#7074=CARTESIAN_POINT ( 'NONE',  ( 13.69515105064549942, 20.07945732920870086, -22.67923001873320032 ) ) ;
#7075=CARTESIAN_POINT ( 'NONE',  ( 51.67587649748560352, -48.61618894467930119, -77.01363636363639387 ) ) ;
#7077=CARTESIAN_POINT ( 'NONE',  ( 53.52649861393759778, 18.16770936907249734, -49.17036649158689698 ) ) ;
#7078=CARTESIAN_POINT ( 'NONE',  ( 56.11585462898960230, -45.54751570299690400, -17.03826781972080084 ) ) ;
#7080=ORIENTED_EDGE ( 'NONE', *, *, #47600, .F. ) ;
#7081=CIRCLE ( 'NONE', #19597, 25.10000000000000142 ) ;
#7086=CARTESIAN_POINT ( 'NONE',  ( 9.643247817651371179, 32.68959971546669863, -46.55912598233139477 ) ) ;
#7088=CARTESIAN_POINT ( 'NONE',  ( 52.88442569144270067, -50.11009285736640351, -50.03528398879910100 ) ) ;
#7089=CARTESIAN_POINT ( 'NONE',  ( 52.59026075507055964, -49.83798095265304084, -48.57069100191421995 ) ) ;
#7091=FACE_OUTER_BOUND ( 'NONE', #10951, .T. ) ;
#7092=ORIENTED_EDGE ( 'NONE', *, *, #27565, .T. ) ;
#7093=CARTESIAN_POINT ( 'NONE',  ( 61.28398356453099893, 14.37233669519349988, -47.68178229854910199 ) ) ;
#7095=CARTESIAN_POINT ( 'NONE',  ( 10.14913760601130122, -63.33847347462889843, -45.99399621147029649 ) ) ;
#7096=EDGE_CURVE ( 'NONE', #41037, #10101, #11131, .T. ) ;
#7097=CARTESIAN_POINT ( 'NONE',  ( 70.03247032090601465, 18.72622661238169783, -73.39853292320987066 ) ) ;
#7099=CARTESIAN_POINT ( 'NONE',  ( 11.23030387052107315, -64.15300031985499629, -44.07782004882023585 ) ) ;
#7100=CARTESIAN_POINT ( 'NONE',  ( 57.13721803582939884, 19.38601056229089892, -53.74365126442869922 ) ) ;
#7103=CARTESIAN_POINT ( 'NONE',  ( 53.53698247381380781, 19.31898572816820092, -77.03764896304019771 ) ) ;
#7105=CARTESIAN_POINT ( 'NONE',  ( 71.71126032029680175, -47.11618894467930119, -46.37203261889099792 ) ) ;
#7107=DIRECTION ( 'NONE',  ( 0.000000000000000000, 0.000000000000000000, 1.000000000000000000 ) ) ;
#7110=AXIS2_PLACEMENT_3D ( 'NONE', #2915, #22030, #43014 ) ;
#7114=ORIENTED_EDGE ( 'NONE', *, *, #51717, .T. ) ;
#7116=CARTESIAN_POINT ( 'NONE',  ( 53.24445252169859799, 13.88381105524720027, -12.91583287338970010 ) ) ;
#7121=ADVANCED_FACE ( 'NONE', ( #23911 ), #26701, .T. ) ;
#7124=CARTESIAN_POINT ( 'NONE',  ( 12.13449217322260054, 33.70756578350810173, -16.24910028838000287 ) ) ;
#7126=CARTESIAN_POINT ( 'NONE',  ( 52.69455864859469330, -49.72372575057979560, -27.57640321585610010 ) ) ;
#7127=CARTESIAN_POINT ( 'NONE',  ( 53.93843392091529410, -50.96933828858919924, -75.87693567902510949 ) ) ;
#7128=CARTESIAN_POINT ( 'NONE',  ( -3.436548605939819812, 18.89937065357259982, -7.972479206788761097 ) ) ;
#7131=CARTESIAN_POINT ( 'NONE',  ( 16.13393739769620083, -15.61618894467929941, -46.39999999999999858 ) ) ;
#7133=CARTESIAN_POINT ( 'NONE',  ( -5.673894891273640440, -46.74181062945210385, -4.529014137033779974 ) ) ;
#7134=CARTESIAN_POINT ( 'NONE',  ( 47.54393415417700197, 23.34658024450819980, -54.99317590619320129 ) ) ;
#7137=CARTESIAN_POINT ( 'NONE',  ( 60.85471687133040319, 14.24866023781859958, -47.26085515436560058 ) ) ;
#7139=CARTESIAN_POINT ( 'NONE',  ( 51.51980099933500412, 18.20712782104119754, -76.63338017729078899 ) ) ;
#7140=CARTESIAN_POINT ( 'NONE',  ( 52.81767038776369816, 18.43487472115680248, -48.48655862607250100 ) ) ;
#7142=CARTESIAN_POINT ( 'NONE',  ( 52.87019085405700025, -49.63973566670129856, -48.66536726492419263 ) ) ;
#7143=CARTESIAN_POINT ( 'NONE',  ( 54.72133342176110204, 16.56637610245050141, -26.54825754140699701 ) ) ;
#7144=VECTOR ( 'NONE', #19665, 1000.000000000000000 ) ;
#7145=CARTESIAN_POINT ( 'NONE',  ( 50.12648257197400170, 22.24397334070440380, -55.01261709213260076 ) ) ;
#7146=CARTESIAN_POINT ( 'NONE',  ( 9.299128317299539148, -63.29430534918720497, -46.53057822423220102 ) ) ;
#7147=CARTESIAN_POINT ( 'NONE',  ( 52.88388581274700329, 18.44024018630440409, -49.00306432449180249 ) ) ;
#7148=CARTESIAN_POINT ( 'NONE',  ( 63.72329982364428957, -31.81072269598050184, -17.26606606354560114 ) ) ;
#7150=CARTESIAN_POINT ( 'NONE',  ( 11.13393739769619906, 32.28996932333459569, -43.76018303787720498 ) ) ;
#7156=EDGE_LOOP ( 'NONE', ( #1728, #36853, #574, #43247 ) ) ;
#7157=CARTESIAN_POINT ( 'NONE',  ( 41.72053738002269796, 12.47914145849200018, -3.400228433360679592 ) ) ;
#7159=AXIS2_PLACEMENT_3D ( 'NONE', #38901, #39153, #43346 ) ;
#7160=CARTESIAN_POINT ( 'NONE',  ( 76.49475639570208330, -3.230431607988094811, -13.20482276423291879 ) ) ;
#7162=CARTESIAN_POINT ( 'NONE',  ( 57.13573030296199562, -45.16451340659830294, -25.51734512155490364 ) ) ;
#7166=CARTESIAN_POINT ( 'NONE',  ( 41.34377498613339696, -44.75585903957070144, -5.356936576703770214 ) ) ;
#7168=CARTESIAN_POINT ( 'NONE',  ( 47.18077207768379822, -45.11618894467940066, -8.347044623099190375 ) ) ;
#7171=CARTESIAN_POINT ( 'NONE',  ( 61.08036406955709907, -29.31821407486409825, -15.93372933320830143 ) ) ;
#7172=DIRECTION ( 'NONE',  ( 1.000000000000000000, 0.000000000000000000, 0.000000000000000000 ) ) ;
#7173=CARTESIAN_POINT ( 'NONE',  ( 46.63190898996919742, -53.39441561763939603, -76.07596939981860373 ) ) ;
#7177=FACE_OUTER_BOUND ( 'NONE', #4042, .T. ) ;
#7178=CARTESIAN_POINT ( 'NONE',  ( 83.94975121583560451, -44.29606033358990658, -46.94103493214879563 ) ) ;
#7179=CARTESIAN_POINT ( 'NONE',  ( 61.50012592447659898, 13.88381109315920092, -27.25296643813030073 ) ) ;
#7183=CARTESIAN_POINT ( 'NONE',  ( 52.83769228248530681, -49.65410697577470245, -28.03887768922920287 ) ) ;
#7184=CARTESIAN_POINT ( 'NONE',  ( 6.339668291764630759, -58.73921203693550552, -11.09392847882710065 ) ) ;
#7185=CARTESIAN_POINT ( 'NONE',  ( 75.18881547038029112, 0.6024962871804371289, -12.00534390646789973 ) ) ;
#7186=CARTESIAN_POINT ( 'NONE',  ( 75.41655381601106001, 12.84207971899083489, -13.62414596433559311 ) ) ;
#7187=CARTESIAN_POINT ( 'NONE',  ( 19.71407736822502699, -55.45560309152967449, -75.36448431255345781 ) ) ;
#7188=FACE_OUTER_BOUND ( 'NONE', #22276, .T. ) ;
#7192=CARTESIAN_POINT ( 'NONE',  ( 57.43388575162559562, -50.22061705833820611, -52.72793123370430379 ) ) ;
#7193=CARTESIAN_POINT ( 'NONE',  ( 40.68015366847210146, 13.39283706869419888, -4.085852594949460403 ) ) ;
#7194=DIRECTION ( 'NONE',  ( -0.8732394366197193669, -0.4872913772396092469, 0.000000000000000000 ) ) ;
#7196=CARTESIAN_POINT ( 'NONE',  ( 57.46792114364419746, -47.23085594836910417, -47.80306618055729473 ) ) ;
#7197=VECTOR ( 'NONE', #43292, 1000.000000000000227 ) ;
#7199=CARTESIAN_POINT ( 'NONE',  ( 66.69979047892330470, -1.463808326225739975, -17.02723538977290119 ) ) ;
#7200=CARTESIAN_POINT ( 'NONE',  ( 18.34505658028029984, -52.20693806470120535, -75.61048537065330777 ) ) ;
#7204=CARTESIAN_POINT ( 'NONE',  ( 10.81033552764298555, -63.45699809194467633, -23.82639812994678863 ) ) ;
#7210=CARTESIAN_POINT ( 'NONE',  ( 40.80913783761709368, -45.21803053746209855, -5.659197024988120717 ) ) ;
#7211=EDGE_LOOP ( 'NONE', ( #43647, #21885, #40840, #12238, #8232 ) ) ;
#7212=CARTESIAN_POINT ( 'NONE',  ( 17.68279279595209985, 20.56214955651219967, -75.65676662446099954 ) ) ;
#7216=EDGE_LOOP ( 'NONE', ( #45237, #41810, #8607, #2793 ) ) ;
#7220=LINE ( 'NONE', #51248, #38556 ) ;
#7222=VERTEX_POINT ( 'NONE', #16861 ) ;
#7226=DIRECTION ( 'NONE',  ( 0.000000000000000000, -1.000000000000000000, 0.000000000000000000 ) ) ;
#7230=CARTESIAN_POINT ( 'NONE',  ( 13.39998208309999939, 20.55440457967890211, -74.14999999999999147 ) ) ;
#7231=CARTESIAN_POINT ( 'NONE',  ( 51.04849420485089695, -50.89596744187040400, -76.15025768116009885 ) ) ;
#7232=CARTESIAN_POINT ( 'NONE',  ( 60.70121379090529956, 14.34289773273770052, -47.37813858017759827 ) ) ;
#7235=DIRECTION ( 'NONE',  ( 0.5547001962252301466, -1.445602896647336944E-16, 0.8320502943378429439 ) ) ;
#7236=EDGE_CURVE ( 'NONE', #6837, #51855, #29326, .T. ) ;
#7237=CARTESIAN_POINT ( 'NONE',  ( 42.29536634146689522, -43.17774985521609921, -3.241362036132330093 ) ) ;
#7238=CARTESIAN_POINT ( 'NONE',  ( -3.853615750487999758, 16.96449338327530043, -5.240522787413070205 ) ) ;
#7239=CARTESIAN_POINT ( 'NONE',  ( 46.91750639651494481, 22.97282010492738280, -75.61476957852809733 ) ) ;
#7240=DIRECTION ( 'NONE',  ( 0.000000000000000000, -4.336808689941963009E-16, 1.000000000000000000 ) ) ;
#7243=CIRCLE ( 'NONE', #44913, 2.000000000000002665 ) ;
#7245=CARTESIAN_POINT ( 'NONE',  ( 57.46598710300569479, 19.38381105532060289, -53.87378585246109708 ) ) ;
#7248=CARTESIAN_POINT ( 'NONE',  ( 14.17150143965160147, 19.18236913456970072, -20.90975112687780069 ) ) ;
#7249=EDGE_CURVE ( 'NONE', #12485, #22335, #11690, .T. ) ;
#7252=CARTESIAN_POINT ( 'NONE',  ( 48.49909158994660174, -54.16138566422429790, -55.13510240093949477 ) ) ;
#7254=VECTOR ( 'NONE', #29720, 999.9999999999998863 ) ;
#7255=DIRECTION ( 'NONE',  ( 0.000000000000000000, 0.000000000000000000, 1.000000000000000000 ) ) ;
#7264=LINE ( 'NONE', #43423, #47853 ) ;
#7268=CARTESIAN_POINT ( 'NONE',  ( -5.866062602303799167, -15.61618894467929586, -14.65000000000000036 ) ) ;
#7270=CARTESIAN_POINT ( 'NONE',  ( 84.44784216359251161, -43.11618894467930119, -47.47585302082339354 ) ) ;
#7272=ORIENTED_EDGE ( 'NONE', *, *, #51064, .F. ) ;
#7274=CARTESIAN_POINT ( 'NONE',  ( 56.50022374573209305, 14.94172953599193754, -26.24581867127661639 ) ) ;
#7276=CARTESIAN_POINT ( 'NONE',  ( 10.49965938277759925, -64.70776751887689215, -46.82084276604349071 ) ) ;
#7283=CARTESIAN_POINT ( 'NONE',  ( 50.95182575631829991, -50.95090194773979420, -76.14999999999999147 ) ) ;
#7284=CARTESIAN_POINT ( 'NONE',  ( 56.36079422399649985, -50.55996778040380235, -52.89779376298050551 ) ) ;
#7286=CARTESIAN_POINT ( 'NONE',  ( 64.11742790134928782, 0.5060918581745209588, -17.20042942902649941 ) ) ;
#7287=CARTESIAN_POINT ( 'NONE',  ( 51.94902347081840333, -49.52373935748639866, -77.02691575752830033 ) ) ;
#7288=DIRECTION ( 'NONE',  ( 1.000000000000000000, 0.000000000000000000, 0.000000000000000000 ) ) ;
#7295=CARTESIAN_POINT ( 'NONE',  ( 13.04440776331039942, -50.02432106228609854, -21.04429563615369858 ) ) ;
#7297=LINE ( 'NONE', #47144, #43524 ) ;
#7298=CARTESIAN_POINT ( 'NONE',  ( 56.32680328304889628, 14.04817129808600029, -16.42293331861320027 ) ) ;
#7299=CARTESIAN_POINT ( 'NONE',  ( 60.99063479934959275, -45.64856812161170296, -47.70729053994229929 ) ) ;
#7301=CARTESIAN_POINT ( 'NONE',  ( 56.55337564821359564, -50.50557100886170048, -52.91477395665069849 ) ) ;
#7304=EDGE_LOOP ( 'NONE', ( #43256, #25738, #37367, #18652, #5348 ) ) ;
#7305=CARTESIAN_POINT ( 'NONE',  ( 46.52565835080890366, 21.89345249355760004, -76.13734531346200640 ) ) ;
#7309=CARTESIAN_POINT ( 'NONE',  ( 55.25526344926753808, -47.47676247021213669, -26.53762684301318231 ) ) ;
#7312=ADVANCED_FACE ( 'NONE', ( #5074 ), #45154, .F. ) ;
#7313=CARTESIAN_POINT ( 'NONE',  ( 47.26413010207565435, -54.05555214137573472, -75.56727778750388325 ) ) ;
#7314=CARTESIAN_POINT ( 'NONE',  ( 82.74207635200149014, 14.32739582876689965, -47.63391066194130019 ) ) ;
#7316=DIRECTION ( 'NONE',  ( 0.000000000000000000, 0.000000000000000000, -1.000000000000000000 ) ) ;
#7318=CARTESIAN_POINT ( 'NONE',  ( 11.41017075758820809, 33.30599513501292819, -24.00668485612997216 ) ) ;
#7320=CARTESIAN_POINT ( 'NONE',  ( 49.25538189185729721, 22.42010655522559759, -54.36832621985269753 ) ) ;
#7322=ORIENTED_EDGE ( 'NONE', *, *, #42556, .T. ) ;
#7323=CARTESIAN_POINT ( 'NONE',  ( 52.59812909015290217, -49.82798299618050208, -48.49246230761499277 ) ) ;
#7324=EDGE_LOOP ( 'NONE', ( #40284, #3652, #41899, #2712, #33735 ) ) ;
#7327=CARTESIAN_POINT ( 'NONE',  ( 13.63913721475599949, 20.12796159149439745, -22.70105333191040131 ) ) ;
#7328=CARTESIAN_POINT ( 'NONE',  ( 12.73487912048826232, 24.23912916116268690, -75.56421958049274679 ) ) ;
#7330=CARTESIAN_POINT ( 'NONE',  ( 52.71454275216699870, 18.51637985033769951, -48.77935984480249942 ) ) ;
#7333=ORIENTED_EDGE ( 'NONE', *, *, #9370, .T. ) ;
#7336=CARTESIAN_POINT ( 'NONE',  ( 11.37397765035290043, -65.29604510817189578, -17.68262795671300225 ) ) ;
#7341=CARTESIAN_POINT ( 'NONE',  ( 53.59003930803689997, -49.40628012469949937, -49.22510501142529904 ) ) ;
#7342=DIRECTION ( 'NONE',  ( 0.3294064756441054120, -0.9441882088883177815, 9.436895709313929201E-16 ) ) ;
#7346=CARTESIAN_POINT ( 'NONE',  ( 9.726666662871039648, -63.11543068638779630, -46.30264950036470140 ) ) ;
#7347=CARTESIAN_POINT ( 'NONE',  ( 68.13393739769630031, 16.88381105531719939, -74.20000000000000284 ) ) ;
#7354=CARTESIAN_POINT ( 'NONE',  ( 52.32303876295807754, 20.18503163261358679, -75.90202713928304945 ) ) ;
#7356=VECTOR ( 'NONE', #51251, 1000.000000000000000 ) ;
#7359=CARTESIAN_POINT ( 'NONE',  ( 52.75108815572690446, -49.73378124990440341, -48.86094483346149531 ) ) ;
#7361=CARTESIAN_POINT ( 'NONE',  ( 61.28610861176740343, -45.23040055550220018, -46.54508491471730025 ) ) ;
#7365=SPHERICAL_SURFACE ( 'NONE', #12507, 2.000000000000000000 ) ;
#7367=CARTESIAN_POINT ( 'NONE',  ( 53.59007319633400357, -49.40623578145169859, -49.22505640094960455 ) ) ;
#7368=CARTESIAN_POINT ( 'NONE',  ( 50.31596467094429670, -49.96707859667039742, -76.14999999999999147 ) ) ;
#7370=CARTESIAN_POINT ( 'NONE',  ( 46.38946308792309736, 21.75434083481459879, -76.14871748201410639 ) ) ;
#7373=CARTESIAN_POINT ( 'NONE',  ( 12.17975455548389974, 33.45308329381320078, -15.92303081429079903 ) ) ;
#7377=CARTESIAN_POINT ( 'NONE',  ( 57.01978172671810086, -50.62831244894230309, -74.38112120481839895 ) ) ;
#7378=CARTESIAN_POINT ( 'NONE',  ( -9.451250797512591006, 12.57291231543609911, -6.018481141893100350 ) ) ;
#7380=CARTESIAN_POINT ( 'NONE',  ( 1.027904703268279984, -42.68661147989060112, -20.15000000000000213 ) ) ;
#7383=ADVANCED_FACE ( 'NONE', ( #30192 ), #24456, .T. ) ;
#7386=CARTESIAN_POINT ( 'NONE',  ( 47.60612636963649891, 23.31708596581999871, -55.05355304419519769 ) ) ;
#7388=CARTESIAN_POINT ( 'NONE',  ( 59.11255455559349770, -45.23257961995879839, -26.22557274275510153 ) ) ;
#7389=CARTESIAN_POINT ( 'NONE',  ( 36.93393739769619799, -15.61618894467929941, -11.54999999999999893 ) ) ;
#7390=CARTESIAN_POINT ( 'NONE',  ( 60.94773661516500596, 14.19689157201089991, -47.19004457261220153 ) ) ;
#7392=CARTESIAN_POINT ( 'NONE',  ( 51.55656746335520779, 18.27266258789200037, -76.63870291393729417 ) ) ;
#7393=CARTESIAN_POINT ( 'NONE',  ( 53.10940561484209610, 18.28271463908539829, -48.84491345906369730 ) ) ;
#7395=CARTESIAN_POINT ( 'NONE',  ( 52.94585587482559674, -49.60009264233129755, -48.75076953771959865 ) ) ;
#7397=CARTESIAN_POINT ( 'NONE',  ( 51.49137293625199874, 21.54576438608010136, -53.98331227670009724 ) ) ;
#7401=CARTESIAN_POINT ( 'NONE',  ( 59.22067766047359783, -28.67256876376159980, -15.68016428579549881 ) ) ;
#7405=CARTESIAN_POINT ( 'NONE',  ( 51.58134242171076522, -34.14973535910032609, -76.88488821125437767 ) ) ;
#7411=EDGE_CURVE ( 'NONE', #24770, #40057, #3304, .T. ) ;
#7413=EDGE_LOOP ( 'NONE', ( #11139, #49693 ) ) ;
#7414=CARTESIAN_POINT ( 'NONE',  ( 57.33727144475490434, -45.20148317274580307, -25.72981098958030088 ) ) ;
#7418=DIRECTION ( 'NONE',  ( 0.000000000000000000, -1.000000000000000000, 0.000000000000000000 ) ) ;
#7420=CARTESIAN_POINT ( 'NONE',  ( 12.54247866899070019, 34.25618301002470645, -23.07435593645569938 ) ) ;
#7421=EDGE_LOOP ( 'NONE', ( #12381, #37190, #18931, #798, #37275 ) ) ;
#7425=CARTESIAN_POINT ( 'NONE',  ( 64.68287081661640059, -30.48142292270370035, -16.53828615335140029 ) ) ;
#7427=CARTESIAN_POINT ( 'NONE',  ( 46.35275103504449845, -52.90993241930539881, -76.14999999999999147 ) ) ;
#7431=CARTESIAN_POINT ( 'NONE',  ( 41.48254013806749896, 13.91499593496540044, -5.927804853516350114 ) ) ;
#7434=CARTESIAN_POINT ( 'NONE',  ( 87.04559528857579664, 18.79802461769378397, -61.26127762739950811 ) ) ;
#7435=CARTESIAN_POINT ( 'NONE',  ( 84.24534987432259925, -43.83635652924289872, -47.12743895163409746 ) ) ;
#7438=ORIENTED_EDGE ( 'NONE', *, *, #27312, .T. ) ;
#7439=DIRECTION ( 'NONE',  ( 0.3294064756441278941, 0.9441882088883097879, 0.000000000000000000 ) ) ;
#7440=ADVANCED_FACE ( 'NONE', ( #11525 ), #779, .T. ) ;
#7441=CARTESIAN_POINT ( 'NONE',  ( 9.945332009489360914, -62.12608445570190696, -13.67195039459510042 ) ) ;
#7442=CARTESIAN_POINT ( 'NONE',  ( 75.68634210793200623, -12.48868729177629966, -11.61082697430510002 ) ) ;
#7443=CARTESIAN_POINT ( 'NONE',  ( 18.06932202639800167, 24.33696219936669891, -76.14999999999999147 ) ) ;
#7444=DIRECTION ( 'NONE',  ( 0.6415444970810866288, 0.4854844151940982400, 0.5939070136550167467 ) ) ;
#7445=CARTESIAN_POINT ( 'NONE',  ( 48.93887227096879400, -45.11618894467940066, -44.18916148508130703 ) ) ;
#7449=CARTESIAN_POINT ( 'NONE',  ( 57.35498654301330390, -50.32030778642509716, -52.86924993879389945 ) ) ;
#7450=CARTESIAN_POINT ( 'NONE',  ( 42.15277068879080247, 12.54031964892660156, -4.489091469251048849 ) ) ;
#7453=CARTESIAN_POINT ( 'NONE',  ( 55.49599478882970516, -48.26400341526499460, -48.16694294531140486 ) ) ;
#7456=CARTESIAN_POINT ( 'NONE',  ( 17.69922415165360263, -51.74824662968959643, -75.61048537065330777 ) ) ;
#7457=CARTESIAN_POINT ( 'NONE',  ( 63.44426004651669615, -45.11618894467940066, -11.74199176319659976 ) ) ;
#7459=CARTESIAN_POINT ( 'NONE',  ( 15.54400253304468116, 19.58458200056557530, -20.39351677730839185 ) ) ;
#7460=DIRECTION ( 'NONE',  ( 1.000000000000000000, 0.000000000000000000, 0.000000000000000000 ) ) ;
#7462=CARTESIAN_POINT ( 'NONE',  ( 45.31003520305578292, 14.31855968887177255, -8.676032565373851924 ) ) ;
#7471=CARTESIAN_POINT ( 'NONE',  ( 17.21347160910339724, 21.88381105532300097, -76.14999999999999147 ) ) ;
#7474=EDGE_CURVE ( 'NONE', #51185, #12580, #4673, .T. ) ;
#7478=CARTESIAN_POINT ( 'NONE',  ( 61.73062563639849998, 13.90432078297569873, -46.66292371669469929 ) ) ;
#7482=CARTESIAN_POINT ( 'NONE',  ( 41.13393739769620083, -15.61618894467929941, 4.450000000000000178 ) ) ;
#7483=CARTESIAN_POINT ( 'NONE',  ( 56.16732778801245018, 19.38381105532069881, -76.24890161727635984 ) ) ;
#7486=CARTESIAN_POINT ( 'NONE',  ( 53.09964378157899745, -51.41544001692909660, -75.69941956541140371 ) ) ;
#7487=CARTESIAN_POINT ( 'NONE',  ( 60.91162229252049798, 14.31804145399359918, -47.50905935143390479 ) ) ;
#7489=CARTESIAN_POINT ( 'NONE',  ( 42.62644315484929791, -42.85940974227979439, -3.197525305375130245 ) ) ;
#7490=CARTESIAN_POINT ( 'NONE',  ( -6.454950692847609695, 15.20115021654400067, -5.551883511487449852 ) ) ;
#7492=CIRCLE ( 'NONE', #14192, 38.00000000000000000 ) ;
#7501=CARTESIAN_POINT ( 'NONE',  ( 44.20345041334109482, 14.84825193712300084, -8.431702830100249457 ) ) ;
#7504=EDGE_CURVE ( 'NONE', #47622, #19762, #802, .T. ) ;
#7505=CARTESIAN_POINT ( 'NONE',  ( 14.79307399754019947, 19.45299727194570139, -20.88395191203290224 ) ) ;
#7508=CARTESIAN_POINT ( 'NONE',  ( 12.76110939629680097, 18.75367528263859995, -21.08964675879520101 ) ) ;
#7509=EDGE_CURVE ( 'NONE', #39070, #6528, #16625, .T. ) ;
#7511=CARTESIAN_POINT ( 'NONE',  ( 48.78510665982869909, -53.94511784475069760, -54.68190458609500126 ) ) ;
#7512=CARTESIAN_POINT ( 'NONE',  ( -33.14629235451243972, -25.37746373560590740, -57.60079496986296732 ) ) ;
#7515=CARTESIAN_POINT ( 'NONE',  ( 47.81335647231740182, 23.16511464034180179, -54.71582838609170096 ) ) ;
#7521=CARTESIAN_POINT ( 'NONE',  ( 60.27360767123050067, -45.79670854958099824, -47.49318409392839868 ) ) ;
#7522=CARTESIAN_POINT ( 'NONE',  ( 59.41577471975829638, -46.21032088470760613, -47.36236646002819839 ) ) ;
#7523=CARTESIAN_POINT ( 'NONE',  ( 83.45566975104344465, 13.44200870639070722, -46.48562894763595921 ) ) ;
#7524=CARTESIAN_POINT ( 'NONE',  ( 84.25371145582080601, 12.95080643885139970, -47.43624648648039965 ) ) ;
#7526=CARTESIAN_POINT ( 'NONE',  ( 59.52869175205803032, 14.25746298374641441, -26.73578769780420572 ) ) ;
#7537=CARTESIAN_POINT ( 'NONE',  ( 76.47144082675787047, -26.50245961684229101, -13.10435250752327718 ) ) ;
#7538=CARTESIAN_POINT ( 'NONE',  ( 11.29861653319979986, -65.19153529705319272, -47.24805190295079882 ) ) ;
#7539=ORIENTED_EDGE ( 'NONE', *, *, #28960, .T. ) ;
#7541=ORIENTED_EDGE ( 'NONE', *, *, #29086, .F. ) ;
#7544=CARTESIAN_POINT ( 'NONE',  ( 56.38980056118450079, -50.68245470039340006, -53.17791771570339421 ) ) ;
#7546=CARTESIAN_POINT ( 'NONE',  ( 65.26361326256220252, 0.1311058356091460153, -16.98102554325449987 ) ) ;
#7547=CARTESIAN_POINT ( 'NONE',  ( 51.70989473440189954, -48.92491810616539993, -77.02394377353789423 ) ) ;
#7549=ORIENTED_EDGE ( 'NONE', *, *, #19285, .T. ) ;
#7553=CARTESIAN_POINT ( 'NONE',  ( 16.13393739769620083, -15.61618894467929941, -20.15000000000000213 ) ) ;
#7556=CARTESIAN_POINT ( 'NONE',  ( 57.18064182625810332, 19.38381105532069881, -74.68520933546099627 ) ) ;
#7557=DIRECTION ( 'NONE',  ( 0.8732394366197157032, 0.4872913772396159082, 0.000000000000000000 ) ) ;
#7558=CARTESIAN_POINT ( 'NONE',  ( 56.73667420260279926, 14.03196537716829972, -17.93020592428829829 ) ) ;
#7559=CARTESIAN_POINT ( 'NONE',  ( 60.98488730395339985, -45.38821883831149506, -46.95029822698879940 ) ) ;
#7564=CARTESIAN_POINT ( 'NONE',  ( 46.35275103504439898, 21.67755452994670406, -76.14999999999999147 ) ) ;
#7567=CARTESIAN_POINT ( 'NONE',  ( 41.89773878495709880, -45.76711833347420111, -6.740064978679530583 ) ) ;
#7568=ADVANCED_FACE ( 'NONE', ( #36905 ), #32952, .F. ) ;
#7569=CARTESIAN_POINT ( 'NONE',  ( 17.92370450339628007, 19.88381105532280202, -74.33587756533624713 ) ) ;
#7574=CARTESIAN_POINT ( 'NONE',  ( 47.13794097070190503, -53.89583813975270488, -75.74423906255060501 ) ) ;
#7575=AXIS2_PLACEMENT_3D ( 'NONE', #21057, #36787, #37057 ) ;
#7577=CARTESIAN_POINT ( 'NONE',  ( 11.43201365337999853, 34.12765256329690544, -18.10223070852750027 ) ) ;
#7581=CARTESIAN_POINT ( 'NONE',  ( -11.21082239979770101, -42.00354444696370138, -6.430205136515479758 ) ) ;
#7582=CARTESIAN_POINT ( 'NONE',  ( 49.01754034824669759, 22.51163454169229894, -54.40023370205440045 ) ) ;
#7584=CARTESIAN_POINT ( 'NONE',  ( 53.36579634005869366, -49.42372989600390554, -49.05761866421319439 ) ) ;
#7589=CARTESIAN_POINT ( 'NONE',  ( 51.73306225781979606, -49.00921943299249506, -77.03096025453059781 ) ) ;
#7592=CARTESIAN_POINT ( 'NONE',  ( 55.35937001036280236, -45.20692410961479624, -14.95305198190059848 ) ) ;
#7593=CARTESIAN_POINT ( 'NONE',  ( 52.57331737020290063, 18.62080981822910175, -27.97395075092120109 ) ) ;
#7594=ORIENTED_EDGE ( 'NONE', *, *, #38044, .F. ) ;
#7596=EDGE_CURVE ( 'NONE', #30791, #44451, #26207, .T. ) ;
#7597=B_SPLINE_CURVE_WITH_KNOTS ( 'NONE', 3,
 ( #38649, #35211, #26830, #47037, #6669, #22887, #6414, #51213, #22634, #42838, #39158, #22372, #38378, #50688, #34686, #18711, #14784, #27090, #27345, #34426, #30754, #47292, #2737, #43350, #3252, #6933, #38905, #15306, #15040, #2995, #18965, #7186, #3516, #11121, #19483, #31010, #43094, #35475, #48558, #36486, #43605, #19983, #40176, #24156, #24677, #28360, #36745 ),
 .UNSPECIFIED., .F., .F.,
 ( 4, 2, 2, 2, 1, 1, 2, 2, 2, 2, 1, 1, 1, 2, 2, 2, 2, 1, 1, 1, 2, 2, 2, 2, 1, 2, 2, 4 ),
 ( 0.000000000000000000, 0.1250000000000352496, 0.1875000000000550116, 0.2187500000000639211, 0.2343750000000658085, 0.2421875000000672240, 0.2460937500000678901, 0.2500000000000685563, 0.3750000000000802136, 0.4375000000000867084, 0.4687500000000899836, 0.4843750000000934808, 0.4921875000000958678, 0.4960937500000944245, 0.5000000000000929257, 0.6250000000000990319, 0.6875000000001015854, 0.7187500000001020295, 0.7343750000001014744, 0.7421875000001018075, 0.7460937500001014744, 0.7500000000001011413, 0.8125000000000764944, 0.8437500000000640599, 0.8593750000000591749, 0.8671875000000557332, 0.8750000000000521805, 1.000000000000000000 ),
 .UNSPECIFIED. ) ;
#7599=CARTESIAN_POINT ( 'NONE',  ( 11.46543046584420011, -65.12255705699759289, -16.91315247372250141 ) ) ;
#7600=CARTESIAN_POINT ( 'NONE',  ( 9.603216745788369479, 33.01762841516160307, -46.77201822708810397 ) ) ;
#7602=CARTESIAN_POINT ( 'NONE',  ( 68.13393739769620083, -15.61618894467929941, -65.65000000000000568 ) ) ;
#7603=CARTESIAN_POINT ( 'NONE',  ( 10.76627208480596387, -64.36776573450144667, -23.46779268753286019 ) ) ;
#7605=ORIENTED_EDGE ( 'NONE', *, *, #49696, .F. ) ;
#7607=CARTESIAN_POINT ( 'NONE',  ( 11.13393739769619906, -63.13952684277840177, -43.74348518090240390 ) ) ;
#7608=CARTESIAN_POINT ( 'NONE',  ( 68.13393739769630031, 16.88381105531719939, -74.20000000000000284 ) ) ;
#7609=VERTEX_POINT ( 'NONE', #22964 ) ;
#7612=CARTESIAN_POINT ( 'NONE',  ( 11.37537782909544504, -65.24381549433910266, -22.78468322869543172 ) ) ;
#7613=LINE ( 'NONE', #15473, #2839 ) ;
#7615=EDGE_LOOP ( 'NONE', ( #32559, #16430, #15455, #428 ) ) ;
#7617=LINE ( 'NONE', #23563, #47673 ) ;
#7619=LINE ( 'NONE', #20670, #5251 ) ;
#7624=FACE_OUTER_BOUND ( 'NONE', #29461, .T. ) ;
#7631=CARTESIAN_POINT ( 'NONE',  ( 47.08376783210989913, 23.19752807116610072, -75.29485540125669729 ) ) ;
#7632=DIRECTION ( 'NONE',  ( -1.000000000000000000, 1.127159607568241538E-32, -7.935614746461580696E-16 ) ) ;
#7634=ADVANCED_FACE ( 'NONE', ( #22190 ), #21931, .T. ) ;
#7635=CARTESIAN_POINT ( 'NONE',  ( 11.62560706826469925, 33.71532168021870035, -16.46999247996680182 ) ) ;
#7639=CARTESIAN_POINT ( 'NONE',  ( 55.44147505427400091, -50.69485088026120678, -75.76380498141109854 ) ) ;
#7640=CARTESIAN_POINT ( 'NONE',  ( -11.32741028376500125, 10.64927095071240082, -6.431200827838360112 ) ) ;
#7641=CARTESIAN_POINT ( 'NONE',  ( 74.93037295002240228, 11.88381105532070059, -15.31098073120859837 ) ) ;
#7643=CARTESIAN_POINT ( 'NONE',  ( 61.33698243797909555, 13.98069162214219929, -46.67936773079180313 ) ) ;
#7646=VERTEX_POINT ( 'NONE', #18534 ) ;
#7648=CARTESIAN_POINT ( 'NONE',  ( 52.86806099848610074, -49.64085155770939650, -48.68114582883949737 ) ) ;
#7649=CARTESIAN_POINT ( 'NONE',  ( 47.59379709645970280, 23.30360333313180021, -54.77931482373369931 ) ) ;
#7652=CARTESIAN_POINT ( 'NONE',  ( 61.60324134049525924, -45.27018021557786653, -47.14317994272850143 ) ) ;
#7655=CARTESIAN_POINT ( 'NONE',  ( 50.83757470097779674, 17.49618323911590068, -76.31330844465840357 ) ) ;
#7656=CARTESIAN_POINT ( 'NONE',  ( 53.05831033682530062, 18.31656324100610078, -48.91556381798330477 ) ) ;
#7658=CARTESIAN_POINT ( 'NONE',  ( 52.93498292564289187, -49.60578928504740048, -48.74287988808979577 ) ) ;
#7661=CARTESIAN_POINT ( 'NONE',  ( 47.56676769225379786, -54.56411824221549978, -54.92148441692940253 ) ) ;
#7662=DIRECTION ( 'NONE',  ( 0.6888026391158329487, -0.7071067811865494601, 0.1598465650148944150 ) ) ;
#7663=CYLINDRICAL_SURFACE ( 'NONE', #32737, 2.000000000000001776 ) ;
#7664=CARTESIAN_POINT ( 'NONE',  ( 59.60922403236150302, -29.31984253203929569, -15.79452132106010076 ) ) ;
#7668=CARTESIAN_POINT ( 'NONE',  ( 56.46551566992090443, -50.77616483350429633, -53.85225086718720178 ) ) ;
#7671=ORIENTED_EDGE ( 'NONE', *, *, #41923, .T. ) ;
#7675=CYLINDRICAL_SURFACE ( 'NONE', #46156, 1.999999999999996225 ) ;
#7678=ORIENTED_EDGE ( 'NONE', *, *, #19768, .F. ) ;
#7679=CARTESIAN_POINT ( 'NONE',  ( 10.98599679800559770, 33.59687660070252946, -23.20934807910649766 ) ) ;
#7681=CARTESIAN_POINT ( 'NONE',  ( 12.71511855601199947, 34.23582645008529823, -23.64159478333349895 ) ) ;
#7682=EDGE_CURVE ( 'NONE', #33030, #34403, #50502, .T. ) ;
#7686=CARTESIAN_POINT ( 'NONE',  ( 10.66246720353709954, 33.63422984119760173, -18.01843150758180201 ) ) ;
#7689=CARTESIAN_POINT ( 'NONE',  ( 59.28323976345399871, -28.29587047411439826, -15.67173192143519955 ) ) ;
#7692=CARTESIAN_POINT ( 'NONE',  ( 46.42028843557609719, -53.00875148048739760, -76.14999999999999147 ) ) ;
#7695=CARTESIAN_POINT ( 'NONE',  ( 55.12912832402329144, 14.86073885494939972, -16.25649608933859724 ) ) ;
#7696=AXIS2_PLACEMENT_3D ( 'NONE', #25214, #17376, #21285 ) ;
#7697=CARTESIAN_POINT ( 'NONE',  ( 41.40014251418400448, 14.21126602188850008, -6.186187947539579568 ) ) ;
#7698=CARTESIAN_POINT ( 'NONE',  ( 15.05440318628110141, 21.88381105532300097, -76.14999999999999147 ) ) ;
#7699=CARTESIAN_POINT ( 'NONE',  ( 83.73251846585449698, -44.53015045067650135, -46.86010343433790126 ) ) ;
#7703=VERTEX_POINT ( 'NONE', #10685 ) ;
#7705=CARTESIAN_POINT ( 'NONE',  ( 15.41374403315040098, -50.77302816826519916, -20.47798662115089741 ) ) ;
#7706=CARTESIAN_POINT ( 'NONE',  ( 50.26043905619395247, -36.48157363899628791, -76.16290606360576021 ) ) ;
#7711=CARTESIAN_POINT ( 'NONE',  ( -11.32734370190460105, -41.88171845330919751, -6.430192534648670133 ) ) ;
#7715=CARTESIAN_POINT ( 'NONE',  ( 57.55751162055879888, -50.51057731619299318, -53.27961218324600168 ) ) ;
#7716=CARTESIAN_POINT ( 'NONE',  ( 42.31976157503279978, 12.63773038262479886, -4.715714940419609924 ) ) ;
#7717=CARTESIAN_POINT ( 'NONE',  ( 61.47028729602050845, -45.40949600205838976, -47.41717745499089887 ) ) ;
#7719=CARTESIAN_POINT ( 'NONE',  ( 56.53085617112640193, -47.72181054224110142, -48.00558725693349515 ) ) ;
#7722=CARTESIAN_POINT ( 'NONE',  ( 18.26290488187510164, -51.89834789502650381, -75.53980707817230211 ) ) ;
#7726=CARTESIAN_POINT ( 'NONE',  ( 50.89343982362250074, -52.15145316057449776, -52.52829244528589925 ) ) ;
#7727=ORIENTED_EDGE ( 'NONE', *, *, #14061, .T. ) ;
#7732=DIRECTION ( 'NONE',  ( 0.3805321250008311118, 0.000000000000000000, -0.9247677015566405645 ) ) ;
#7735=CARTESIAN_POINT ( 'NONE',  ( 17.43015572509100153, 21.57872223484060115, -76.12922349804929922 ) ) ;
#7736=ORIENTED_EDGE ( 'NONE', *, *, #31576, .T. ) ;
#7738=CARTESIAN_POINT ( 'NONE',  ( 57.18178511478169668, -45.84706250231700153, -26.25564504989590020 ) ) ;
#7745=EDGE_CURVE ( 'NONE', #38464, #13785, #10163, .T. ) ;
#7748=ORIENTED_EDGE ( 'NONE', *, *, #47447, .F. ) ;
#7749=LINE ( 'NONE', #19784, #42599 ) ;
#7751=CARTESIAN_POINT ( 'NONE',  ( 60.82616199806800239, 14.39437461288099840, -47.60746935378129763 ) ) ;
#7753=CARTESIAN_POINT ( 'NONE',  ( 84.44784216359251161, -43.11618894467930119, -47.47585302082339354 ) ) ;
#7754=CARTESIAN_POINT ( 'NONE',  ( -7.968642834068480951, 13.86896153487260008, -5.614579153141090018 ) ) ;
#7756=CARTESIAN_POINT ( 'NONE',  ( 47.01289945827778638, 23.18945904231436117, -75.36289877398526471 ) ) ;
#7759=EDGE_CURVE ( 'NONE', #9610, #42606, #26123, .T. ) ;
#7760=ORIENTED_EDGE ( 'NONE', *, *, #41352, .T. ) ;
#7761=CARTESIAN_POINT ( 'NONE',  ( 56.52536539877740296, -50.75180572374080157, -53.84278118897309895 ) ) ;
#7766=CYLINDRICAL_SURFACE ( 'NONE', #43975, 2.000000000000003553 ) ;
#7767=FACE_OUTER_BOUND ( 'NONE', #14921, .T. ) ;
#7768=CARTESIAN_POINT ( 'NONE',  ( 61.14297911010989850, 14.08836397059769574, -46.99578574395629715 ) ) ;
#7769=CARTESIAN_POINT ( 'NONE',  ( 48.87989277424459544, -54.00735095224600002, -55.25437946346490037 ) ) ;
#7770=CARTESIAN_POINT ( 'NONE',  ( 72.38393739769620083, 4.883811055320659733, -61.44999999999999574 ) ) ;
#7771=DIRECTION ( 'NONE',  ( 0.000000000000000000, 0.000000000000000000, -1.000000000000000000 ) ) ;
#7772=CARTESIAN_POINT ( 'NONE',  ( 47.81203533955039831, 23.17981727675569914, -54.77279602202729336 ) ) ;
#7777=CARTESIAN_POINT ( 'NONE',  ( 17.51664573667515157, 21.64019614504773870, -76.12465453343314437 ) ) ;
#7778=CARTESIAN_POINT ( 'NONE',  ( 60.96180853276540290, -45.45167203910889242, -47.29837554833880375 ) ) ;
#7779=CARTESIAN_POINT ( 'NONE',  ( 13.39998208310050032, -51.78678246903520233, -23.15000000000000213 ) ) ;
#7780=CARTESIAN_POINT ( 'NONE',  ( 83.53665348990875827, 13.38079070459579967, -46.51478504176231610 ) ) ;
#7784=CARTESIAN_POINT ( 'NONE',  ( 75.13393739769618662, 4.883811055320659733, -84.38499399519520239 ) ) ;
#7791=AXIS2_PLACEMENT_3D ( 'NONE', #9773, #33601, #40696 ) ;
#7793=CARTESIAN_POINT ( 'NONE',  ( 10.75428388279330072, -64.86834293686459318, -46.90868476786780406 ) ) ;
#7798=CARTESIAN_POINT ( 'NONE',  ( 56.35668519540149646, -50.69685899399890161, -53.18239453017169893 ) ) ;
#7801=CARTESIAN_POINT ( 'NONE',  ( 59.71002301575170179, -1.985703112241369972, -15.78375127595690230 ) ) ;
#7802=CARTESIAN_POINT ( 'NONE',  ( 51.67727694508769787, -49.68733520360949996, -76.65630996370649086 ) ) ;
#7803=CARTESIAN_POINT ( 'NONE',  ( 57.64403164091130094, -49.99897929508820482, -52.47668038226420606 ) ) ;
#7804=ORIENTED_EDGE ( 'NONE', *, *, #46751, .F. ) ;
#7806=CARTESIAN_POINT ( 'NONE',  ( 82.81464131963001307, -43.11618894467930119, -49.28546657628889704 ) ) ;
#7807=DIRECTION ( 'NONE',  ( 0.000000000000000000, 0.000000000000000000, 1.000000000000000000 ) ) ;
#7810=CARTESIAN_POINT ( 'NONE',  ( 12.28937801554179821, -50.00765209207849438, -21.14656546066629872 ) ) ;
#7811=AXIS2_PLACEMENT_3D ( 'NONE', #44546, #8648, #40614 ) ;
#7812=CARTESIAN_POINT ( 'NONE',  ( 55.48172515062150012, 19.38381105532069881, -76.40185937632740831 ) ) ;
#7814=CARTESIAN_POINT ( 'NONE',  ( 57.48325051288529863, 13.88381105532070059, -17.42702951318920057 ) ) ;
#7815=CARTESIAN_POINT ( 'NONE',  ( 61.12227989346150281, -45.45881623026480156, -47.44113852007230037 ) ) ;
#7816=LINE ( 'NONE', #12010, #15380 ) ;
#7820=CARTESIAN_POINT ( 'NONE',  ( 13.42425491221250056, -51.80633386256230466, -74.54427505470819426 ) ) ;
#7822=CARTESIAN_POINT ( 'NONE',  ( 47.24973492052809831, -54.75565816223589621, -54.63348945589360284 ) ) ;
#7823=ADVANCED_FACE ( 'NONE', ( #18269 ), #48821, .F. ) ;
#7824=CARTESIAN_POINT ( 'NONE',  ( 11.71414166050488248, 34.09778695713147556, -47.42034454217008488 ) ) ;
#7825=CIRCLE ( 'NONE', #12883, 29.70020322226740106 ) ;
#7826=DIRECTION ( 'NONE',  ( 0.000000000000000000, 0.000000000000000000, 1.000000000000000000 ) ) ;
#7827=CARTESIAN_POINT ( 'NONE',  ( 15.67961772667648290, -50.86266697332435172, -20.20261269004708993 ) ) ;
#7832=DIRECTION ( 'NONE',  ( 0.000000000000000000, 0.000000000000000000, -1.000000000000000000 ) ) ;
#7833=DIRECTION ( 'NONE',  ( -0.2260571801428149508, -1.665334536937734318E-16, 0.9741140340359947247 ) ) ;
#7834=FACE_OUTER_BOUND ( 'NONE', #2183, .T. ) ;
#7835=CARTESIAN_POINT ( 'NONE',  ( 49.16018969832690289, 22.62491742194789879, -54.90022772030559395 ) ) ;
#7837=CARTESIAN_POINT ( 'NONE',  ( 52.96080973490879984, -49.61775551211789548, -48.98458849178360452 ) ) ;
#7841=CARTESIAN_POINT ( 'NONE',  ( 14.29774505810699914, 19.88381105514569924, -22.54670832509589928 ) ) ;
#7844=CARTESIAN_POINT ( 'NONE',  ( 53.36465014982429977, 18.25085194934079880, -49.20420490330940311 ) ) ;
#7845=CARTESIAN_POINT ( 'NONE',  ( 55.59033526946949877, -45.44877594268120191, -15.86859551517999911 ) ) ;
#7846=CARTESIAN_POINT ( 'NONE',  ( 53.37088539291629985, 17.75190881940810073, -26.62991259020409984 ) ) ;
#7851=CARTESIAN_POINT ( 'NONE',  ( 11.64437505592259825, -65.39202089365400639, -17.80448344477410316 ) ) ;
#7852=CARTESIAN_POINT ( 'NONE',  ( 11.80354816905300019, 33.97835162598539682, -46.90015655923220095 ) ) ;
#7855=CARTESIAN_POINT ( 'NONE',  ( 11.34809686822852726, -65.22440864330458510, -22.81359155188068044 ) ) ;
#7856=DIRECTION ( 'NONE',  ( 0.000000000000000000, 1.000000000000000000, 0.000000000000000000 ) ) ;
#7857=ORIENTED_EDGE ( 'NONE', *, *, #13740, .T. ) ;
#7859=CARTESIAN_POINT ( 'NONE',  ( 11.10551638025419940, -63.28312641050290210, -44.25178297920150072 ) ) ;
#7860=EDGE_CURVE ( 'NONE', #26641, #33083, #26909, .T. ) ;
#7861=CARTESIAN_POINT ( 'NONE',  ( 70.83745409581385388, 17.98087126524510637, -71.50000000000081002 ) ) ;
#7862=EDGE_LOOP ( 'NONE', ( #48210, #37435 ) ) ;
#7865=CARTESIAN_POINT ( 'NONE',  ( 12.13393739769649926, 24.18330853958550364, -23.15000000000000213 ) ) ;
#7868=VERTEX_POINT ( 'NONE', #4811 ) ;
#7873=CARTESIAN_POINT ( 'NONE',  ( 56.37610586342359653, 14.84999283348500043, -45.22263387109850186 ) ) ;
#7879=ORIENTED_EDGE ( 'NONE', *, *, #45381, .F. ) ;
#7883=AXIS2_PLACEMENT_3D ( 'NONE', #31826, #36281, #39467 ) ;
#7884=CARTESIAN_POINT ( 'NONE',  ( 47.30620419303679824, 23.48429292510279609, -74.17369128426381053 ) ) ;
#7886=DIRECTION ( 'NONE',  ( 0.6911981449639433839, -0.7226652920947592706, -1.665334536937735550E-16 ) ) ;
#7887=CARTESIAN_POINT ( 'NONE',  ( 11.96713421144920098, 33.63456231549939446, -16.19173486065400169 ) ) ;
#7890=CARTESIAN_POINT ( 'NONE',  ( 56.90565798765720729, -50.64481172289290356, -74.14903650335379837 ) ) ;
#7891=CARTESIAN_POINT ( 'NONE',  ( 10.83485780772508988, -55.26361012050001165, -45.05995334480344638 ) ) ;
#7894=CARTESIAN_POINT ( 'NONE',  ( 61.56738629693729337, 13.90151360212160014, -46.47169905912059562 ) ) ;
#7897=CARTESIAN_POINT ( 'NONE',  ( 52.84731369148340008, -49.65172165314799457, -48.60966827451729699 ) ) ;
#7899=CARTESIAN_POINT ( 'NONE',  ( 58.54882648235869880, -45.58368087071139740, -26.43241409811030351 ) ) ;
#7901=CARTESIAN_POINT ( 'NONE',  ( 61.16408118782140946, 14.10070246553319961, -47.10588363253890520 ) ) ;
#7903=CARTESIAN_POINT ( 'NONE',  ( 51.67727282663010158, 18.45495170809379815, -76.65630935983880079 ) ) ;
#7904=CARTESIAN_POINT ( 'NONE',  ( 52.72459105117300737, 18.49182676863240005, -48.48894656618049481 ) ) ;
#7908=DIRECTION ( 'NONE',  ( 0.000000000000000000, 0.000000000000000000, 1.000000000000000000 ) ) ;
#7909=CARTESIAN_POINT ( 'NONE',  ( 47.58993135570310073, -54.55740034306059982, -55.07469421153570721 ) ) ;
#7912=CARTESIAN_POINT ( 'NONE',  ( -15.86606260230380094, -15.61618894467929941, -21.15000000000000213 ) ) ;
#7913=CARTESIAN_POINT ( 'NONE',  ( 58.98156044741060100, -28.10868613328409893, -15.65041641687770024 ) ) ;
#7915=CARTESIAN_POINT ( 'NONE',  ( 68.13393739769620083, 6.883811055320649963, -71.50000000000000000 ) ) ;
#7919=ORIENTED_EDGE ( 'NONE', *, *, #30689, .F. ) ;
#7921=CIRCLE ( 'NONE', #36327, 23.00000000000000000 ) ;
#7923=CARTESIAN_POINT ( 'NONE',  ( 50.02500898439532762, -29.89093149159158713, -15.97526755063678117 ) ) ;
#7928=B_SPLINE_CURVE_WITH_KNOTS ( 'NONE', 3,
 ( #46514, #17425, #13507, #26559, #41525, #18454, #26300, #29714 ),
 .UNSPECIFIED., .F., .F.,
 ( 4, 2, 2, 4 ),
 ( 0.000000000000000000, 0.006927380359722845604, 0.5031982232999553384, 1.000000000000000000 ),
 .UNSPECIFIED. ) ;
#7939=CARTESIAN_POINT ( 'NONE',  ( 62.45731387899189713, -29.68130429890049982, -16.13463557047360197 ) ) ;
#7942=CARTESIAN_POINT ( 'NONE',  ( 40.73312621558000046, 14.05717019330969819, -5.671158935740639784 ) ) ;
#7943=DIRECTION ( 'NONE',  ( -0.6911981449639438280, -0.7226652920947587155, -3.885780586188047891E-16 ) ) ;
#7944=CARTESIAN_POINT ( 'NONE',  ( 83.93595989616819963, -44.26186973806559877, -46.83273212233100224 ) ) ;
#7947=ORIENTED_EDGE ( 'NONE', *, *, #40761, .T. ) ;
#7948=CARTESIAN_POINT ( 'NONE',  ( 56.00515889221910015, -46.65902915747689406, -26.31855334364909993 ) ) ;
#7949=CARTESIAN_POINT ( 'NONE',  ( 15.67956920600099835, -50.86263546383059975, -20.20255632743579710 ) ) ;
#7950=CARTESIAN_POINT ( 'NONE',  ( 76.63910079429579980, 12.04342629570849965, -14.20152708415839982 ) ) ;
#7952=DIRECTION ( 'NONE',  ( 1.000000000000000000, 0.000000000000000000, 0.000000000000000000 ) ) ;
#7953=CARTESIAN_POINT ( 'NONE',  ( 12.53567563011250030, -49.97757164388899298, -21.12174283345060388 ) ) ;
#7955=CARTESIAN_POINT ( 'NONE',  ( -6.906523692131460557, -46.00570557808070049, -5.490002812737249549 ) ) ;
#7958=CARTESIAN_POINT ( 'NONE',  ( 16.13393739769620083, -15.61618894467929941, 7.944363289481099599 ) ) ;
#7960=CARTESIAN_POINT ( 'NONE',  ( 57.37407586127599757, -50.61618894467930119, -53.92464312453480346 ) ) ;
#7961=CARTESIAN_POINT ( 'NONE',  ( 41.98453335044129631, 12.86081823404789937, -4.765379570853959912 ) ) ;
#7967=CARTESIAN_POINT ( 'NONE',  ( 66.65424812453399284, -1.319067908241720044, -16.99686718764349891 ) ) ;
#7968=CARTESIAN_POINT ( 'NONE',  ( 17.30873035729209874, -52.95108609461500748, -76.14999999999999147 ) ) ;
#7978=CARTESIAN_POINT ( 'NONE',  ( 17.47783027489900221, 21.13934752900200209, -76.01805773991210913 ) ) ;
#7980=B_SPLINE_CURVE_WITH_KNOTS ( 'NONE', 3,
 ( #4860, #16647, #16132, #8541, #48633, #8794, #12734, #36295, #44690, #32091, #44433, #48111, #20304, #24484, #12210, #27919 ),
 .UNSPECIFIED., .F., .F.,
 ( 4, 2, 2, 2, 2, 2, 2, 4 ),
 ( 0.000000000000000000, 0.1775000002334429783, 0.3375000001880322786, 0.4375000001596504040, 0.5000000001419118156, 0.6250000001064347499, 0.8250000000496718888, 1.000000000000000000 ),
 .UNSPECIFIED. ) ;
#7981=EDGE_LOOP ( 'NONE', ( #8489, #37777, #51281, #13973, #31288 ) ) ;
#7985=VERTEX_POINT ( 'NONE', #44131 ) ;
#7990=AXIS2_PLACEMENT_3D ( 'NONE', #10131, #6200, #14572 ) ;
#7993=VERTEX_POINT ( 'NONE', #4289 ) ;
#7995=CARTESIAN_POINT ( 'NONE',  ( 50.95179065782230055, -50.95087911780539969, -76.14999999969799660 ) ) ;
#7996=CARTESIAN_POINT ( 'NONE',  ( 61.02187414602389737, 14.32404985249469931, -47.57273269190739740 ) ) ;
#7999=CARTESIAN_POINT ( 'NONE',  ( -10.45107869171170023, 11.54332210424730043, -5.993506745208079245 ) ) ;
#8001=VECTOR ( 'NONE', #8358, 1000.000000000000114 ) ;
#8002=CARTESIAN_POINT ( 'NONE',  ( 58.55928041488670033, 14.25308721433460057, -26.37445203316179843 ) ) ;
#8006=CARTESIAN_POINT ( 'NONE',  ( 42.86745194688189997, 14.71797365073330077, -7.481799581053440562 ) ) ;
#8007=CARTESIAN_POINT ( 'NONE',  ( 53.68563787866792580, -51.14635906356087958, -75.73808238357163702 ) ) ;
#8012=CIRCLE ( 'NONE', #37317, 2.000000000000001332 ) ;
#8013=CARTESIAN_POINT ( 'NONE',  ( 46.46257346985409953, 21.93137764140289647, -76.13734532152261636 ) ) ;
#8014=CARTESIAN_POINT ( 'NONE',  ( 48.72323709853730378, -54.03203391146720236, -54.90603619288649639 ) ) ;
#8015=AXIS2_PLACEMENT_3D ( 'NONE', #34431, #14528, #15309 ) ;
#8018=CARTESIAN_POINT ( 'NONE',  ( 16.15069188244332210, 19.81939201856824795, -15.66900176635303232 ) ) ;
#8019=CARTESIAN_POINT ( 'NONE',  ( 66.28197446254964120, -33.07501703851021091, -19.91060653315744489 ) ) ;
#8020=CARTESIAN_POINT ( 'NONE',  ( 75.13393739769618662, -43.11618894467930119, -84.38499399519520239 ) ) ;
#8021=EDGE_CURVE ( 'NONE', #21139, #17894, #27632, .T. ) ;
#8026=CYLINDRICAL_SURFACE ( 'NONE', #21689, 2.000000000000040856 ) ;
#8027=CARTESIAN_POINT ( 'NONE',  ( 60.95366616844789576, -45.42739688593400160, -47.19077871656730139 ) ) ;
#8028=CARTESIAN_POINT ( 'NONE',  ( 56.51601257069349771, -47.72958752039729546, -47.92267345016619373 ) ) ;
#8029=CARTESIAN_POINT ( 'NONE',  ( 47.40322300430459990, 23.42336669154519768, -54.88279555090589668 ) ) ;
#8033=DIRECTION ( 'NONE',  ( 1.000000000000000000, 0.000000000000000000, 0.000000000000000000 ) ) ;
#8035=CARTESIAN_POINT ( 'NONE',  ( 48.82567944625920120, -28.11618896394480061, -15.64999999241030082 ) ) ;
#8036=ORIENTED_EDGE ( 'NONE', *, *, #15517, .T. ) ;
#8037=B_SPLINE_CURVE_WITH_KNOTS ( 'NONE', 3,
 ( #5254, #1314, #9694, #29592, #8656 ),
 .UNSPECIFIED., .F., .F.,
 ( 4, 1, 4 ),
 ( 0.000000000000000000, 0.5000000000000000000, 1.000000000000000000 ),
 .UNSPECIFIED. ) ;
#8041=CARTESIAN_POINT ( 'NONE',  ( 76.39902651674920264, -19.28652455383290132, -12.79235177570935456 ) ) ;
#8042=CARTESIAN_POINT ( 'NONE',  ( 52.50031725165329988, -52.44384906523560375, -54.11907245731389793 ) ) ;
#8044=ORIENTED_EDGE ( 'NONE', *, *, #31202, .T. ) ;
#8045=ORIENTED_EDGE ( 'NONE', *, *, #31199, .F. ) ;
#8051=CARTESIAN_POINT ( 'NONE',  ( 56.48750829591079992, -50.75384514585400098, -53.61740582762440255 ) ) ;
#8052=CARTESIAN_POINT ( 'NONE',  ( 52.67900408153330005, -49.77440099653090044, -48.75317613627849767 ) ) ;
#8054=EDGE_CURVE ( 'NONE', #12711, #1664, #43846, .T. ) ;
#8055=CARTESIAN_POINT ( 'NONE',  ( 59.03458116493130348, -2.378454724218949767, -15.69068937066560032 ) ) ;
#8060=CARTESIAN_POINT ( 'NONE',  ( 53.27342897376659892, -50.46946016740059804, -77.09451958621460221 ) ) ;
#8062=FACE_OUTER_BOUND ( 'NONE', #51432, .T. ) ;
#8065=CIRCLE ( 'NONE', #41534, 15.24604989415149703 ) ;
#8066=CARTESIAN_POINT ( 'NONE',  ( 13.68260753953069830, -50.61260876938109732, -21.30691141874990180 ) ) ;
#8069=CARTESIAN_POINT ( 'NONE',  ( 56.78179639309170312, 13.88381105532070059, -15.59568127148789962 ) ) ;
#8070=CARTESIAN_POINT ( 'NONE',  ( 60.75158972514669387, -45.53853088870819477, -47.32592394361339672 ) ) ;
#8075=CARTESIAN_POINT ( 'NONE',  ( 47.06135413716880578, 22.56673458592310055, -75.82639806884090206 ) ) ;
#8076=AXIS2_PLACEMENT_3D ( 'NONE', #26833, #15046, #19488 ) ;
#8077=CARTESIAN_POINT ( 'NONE',  ( 47.34394088935550116, -54.69230464071289788, -54.81224997073749705 ) ) ;
#8078=CARTESIAN_POINT ( 'NONE',  ( -4.666062602303798990, -15.61618894467930119, -12.65000000000000036 ) ) ;
#8081=CARTESIAN_POINT ( 'NONE',  ( 60.91226570742461632, -45.44496133806553217, -47.18149654191857678 ) ) ;
#8082=AXIS2_PLACEMENT_3D ( 'NONE', #14393, #15943, #42963 ) ;
#8083=CARTESIAN_POINT ( 'NONE',  ( 47.26511662130825897, -54.05680164242729546, -75.56574662652583640 ) ) ;
#8084=CARTESIAN_POINT ( 'NONE',  ( 10.72320681404810117, 33.67578529855150293, -17.84617904793899967 ) ) ;
#8086=CARTESIAN_POINT ( 'NONE',  ( 16.13393739769620083, -15.61618894467929941, 1.600000000000000089 ) ) ;
#8090=CYLINDRICAL_SURFACE ( 'NONE', #19601, 2.000000000000001776 ) ;
#8091=CARTESIAN_POINT ( 'NONE',  ( 49.30929069640199458, 22.32182524534569978, -54.21028152426279689 ) ) ;
#8093=CARTESIAN_POINT ( 'NONE',  ( 52.90147003455390262, -49.64573303326979214, -48.94440827424179474 ) ) ;
#8096=AXIS2_PLACEMENT_3D ( 'NONE', #22893, #14531, #46264 ) ;
#8098=DIRECTION ( 'NONE',  ( 0.000000000000000000, 0.000000000000000000, -1.000000000000000000 ) ) ;
#8099=CARTESIAN_POINT ( 'NONE',  ( 83.86651039750330483, 13.16223578792310001, -46.90523421348220268 ) ) ;
#8100=CARTESIAN_POINT ( 'NONE',  ( 52.95630170018949912, 18.21339351390729888, -27.21371790733410023 ) ) ;
#8102=CARTESIAN_POINT ( 'NONE',  ( 52.84346299185870066, 18.45884386080550144, -48.96941050064629763 ) ) ;
#8103=CARTESIAN_POINT ( 'NONE',  ( 56.87281233921919466, -45.18115549338420323, -17.04514278619280176 ) ) ;
#8104=CARTESIAN_POINT ( 'NONE',  ( 54.52192486798780635, 16.42131495964800436, -25.85211914981980286 ) ) ;
#8107=ORIENTED_EDGE ( 'NONE', *, *, #36141, .F. ) ;
#8108=CARTESIAN_POINT ( 'NONE',  ( 10.91696776951759951, -65.00855143979499928, -17.52451585372379839 ) ) ;
#8109=CARTESIAN_POINT ( 'NONE',  ( 11.15097258569349847, 33.37846234896409925, -45.98097165681439691 ) ) ;
#8111=CARTESIAN_POINT ( 'NONE',  ( 53.08619397177870525, -49.46320494400659840, -48.78329442807490324 ) ) ;
#8112=CARTESIAN_POINT ( 'NONE',  ( 11.42100611455456871, -65.27489793864438639, -22.73641203297022884 ) ) ;
#8113=DIRECTION ( 'NONE',  ( 0.05023550054956202326, 0.000000000000000000, -0.9987374001630934250 ) ) ;
#8116=CARTESIAN_POINT ( 'NONE',  ( 11.13393739769619906, -63.28004284733241036, -43.74619111847169961 ) ) ;
#8117=CARTESIAN_POINT ( 'NONE',  ( 68.13393739769814772, 19.38381105532029736, -71.50000000000200373 ) ) ;
#8118=ORIENTED_EDGE ( 'NONE', *, *, #32660, .F. ) ;
#8119=EDGE_CURVE ( 'NONE', #35503, #34565, #41487, .T. ) ;
#8120=DIRECTION ( 'NONE',  ( 0.000000000000000000, 0.000000000000000000, -1.000000000000000000 ) ) ;
#8121=CARTESIAN_POINT ( 'NONE',  ( 56.50450790981899729, 19.50659178549170036, -53.50133212754479928 ) ) ;
#8128=CARTESIAN_POINT ( 'NONE',  ( 56.95883376355960337, -50.25507440355580258, -52.69722347720740174 ) ) ;
#8131=DIRECTION ( 'NONE',  ( -0.000000000000000000, 1.000000000000000000, 0.000000000000000000 ) ) ;
#8138=CARTESIAN_POINT ( 'NONE',  ( 46.53489442956319522, 22.05800845228959872, -76.11277936651509890 ) ) ;
#8143=CARTESIAN_POINT ( 'NONE',  ( 12.10858429747900011, 33.61313455612010159, -16.12611387918660100 ) ) ;
#8145=CARTESIAN_POINT ( 'NONE',  ( 54.27570680556749494, -50.62601669679319372, -76.71275195964710747 ) ) ;
#8150=CARTESIAN_POINT ( 'NONE',  ( 61.27465791697959929, 14.01526204812190102, -46.81188391966050233 ) ) ;
#8151=CARTESIAN_POINT ( 'NONE',  ( 72.38393739883420608, 4.883811055320659733, -61.44999999999999574 ) ) ;
#8154=CARTESIAN_POINT ( 'NONE',  ( 53.01963658129270129, -49.56143686301879825, -48.79855610848599667 ) ) ;
#8156=CARTESIAN_POINT ( 'NONE',  ( 57.62794015340739406, -45.42613097097460439, -26.09739812807309889 ) ) ;
#8158=CARTESIAN_POINT ( 'NONE',  ( 57.07496343321250265, 14.26128913866610048, -26.05062655201860267 ) ) ;
#8161=CARTESIAN_POINT ( 'NONE',  ( 50.55764111442330488, 18.57534966417999911, -76.16355215269059897 ) ) ;
#8162=CARTESIAN_POINT ( 'NONE',  ( 53.04305184480200097, 18.31989923538939991, -48.87083722090200411 ) ) ;
#8164=FACE_OUTER_BOUND ( 'NONE', #41040, .T. ) ;
#8167=CARTESIAN_POINT ( 'NONE',  ( 47.69978268171949765, -54.49413833317590417, -54.91276148295600734 ) ) ;
#8168=CARTESIAN_POINT ( 'NONE',  ( -9.468778083922810396, 12.47338336450459906, -5.557361636894910362 ) ) ;
#8169=CARTESIAN_POINT ( 'NONE',  ( 36.93393739717168245, -15.61618894541809688, -10.44999999999999929 ) ) ;
#8170=CARTESIAN_POINT ( 'NONE',  ( 65.26406672541840237, -31.36357188815229335, -16.98112372788800073 ) ) ;
#8175=DIRECTION ( 'NONE',  ( 1.590235242698480059E-09, 2.885242803146169796E-09, 1.000000000000000000 ) ) ;
#8177=ORIENTED_EDGE ( 'NONE', *, *, #15915, .T. ) ;
#8178=EDGE_LOOP ( 'NONE', ( #9330, #134, #20217, #30529 ) ) ;
#8184=CARTESIAN_POINT ( 'NONE',  ( 56.18863030598410546, -45.60033839361480545, -25.30081866445960159 ) ) ;
#8194=B_SPLINE_CURVE_WITH_KNOTS ( 'NONE', 3,
 ( #4716, #4202, #28552, #40878, #48231, #4982 ),
 .UNSPECIFIED., .F., .F.,
 ( 4, 2, 4 ),
 ( 0.1924323111301881328, 0.5962161555650941080, 1.000000000000000000 ),
 .UNSPECIFIED. ) ;
#8195=CARTESIAN_POINT ( 'NONE',  ( 11.82388200435210024, -65.03973971535801013, -23.85088417817880213 ) ) ;
#8198=CARTESIAN_POINT ( 'NONE',  ( 45.22532672935899711, 14.34554167113489953, -8.601054614529550335 ) ) ;
#8199=CARTESIAN_POINT ( 'NONE',  ( 14.49215175659190002, 20.43782862716600235, -75.53341961486970035 ) ) ;
#8201=CARTESIAN_POINT ( 'NONE',  ( 83.91322170983950457, -44.47913769101550230, -47.13452068490819613 ) ) ;
#8202=TOROIDAL_SURFACE ( 'NONE', #48379, 17.39999999955150045, 3.400000000022779911 ) ;
#8203=DIRECTION ( 'NONE',  ( 0.000000000000000000, 0.000000000000000000, -1.000000000000000000 ) ) ;
#8205=VERTEX_POINT ( 'NONE', #1341 ) ;
#8206=CARTESIAN_POINT ( 'NONE',  ( 52.75143703161269571, -49.69438780581380399, -27.88778421337200442 ) ) ;
#8207=CARTESIAN_POINT ( 'NONE',  ( 15.65801254756290106, -50.85536889816550143, -20.25518593351960206 ) ) ;
#8208=CARTESIAN_POINT ( 'NONE',  ( 50.91918776801460922, -35.36424194159308598, -76.35849960748986121 ) ) ;
#8211=LINE ( 'NONE', #17115, #9771 ) ;
#8212=EDGE_CURVE ( 'NONE', #51131, #51304, #17331, .T. ) ;
#8215=CARTESIAN_POINT ( 'NONE',  ( 47.31231821074380406, 23.47848045659210214, -54.67852925653989615 ) ) ;
#8218=CARTESIAN_POINT ( 'NONE',  ( 57.47389180249940921, -50.59199526962510163, -53.60388562653090361 ) ) ;
#8219=CARTESIAN_POINT ( 'NONE',  ( 42.47447998727660234, 12.94812977345070060, -5.039225366711079346 ) ) ;
#8220=EDGE_CURVE ( 'NONE', #13785, #36880, #37008, .T. ) ;
#8224=CARTESIAN_POINT ( 'NONE',  ( 17.80205609966759894, -52.64324949044360125, -76.02664804518839503 ) ) ;
#8226=CARTESIAN_POINT ( 'NONE',  ( 50.15655331733719891, -52.83076837965879946, -53.34591643228289826 ) ) ;
#8227=ORIENTED_EDGE ( 'NONE', *, *, #28727, .T. ) ;
#8230=FACE_OUTER_BOUND ( 'NONE', #46324, .T. ) ;
#8232=ORIENTED_EDGE ( 'NONE', *, *, #15458, .T. ) ;
#8233=CARTESIAN_POINT ( 'NONE',  ( 18.12471141111990036, 20.82672717200830093, -75.71427953954510315 ) ) ;
#8237=CARTESIAN_POINT ( 'NONE',  ( 56.94969803572780620, -45.93464612349889364, -26.24572192374850133 ) ) ;
#8239=CARTESIAN_POINT ( 'NONE',  ( 61.60836755608340098, 14.03242982913499937, -47.13168653318339807 ) ) ;
#8241=CARTESIAN_POINT ( 'NONE',  ( 66.63393739769620083, -43.11618894467930119, -73.25000000000000000 ) ) ;
#8242=CARTESIAN_POINT ( 'NONE',  ( 8.815605938724019097, -63.28267558148569094, -46.67186391142220003 ) ) ;
#8249=CARTESIAN_POINT ( 'NONE',  ( 11.63826681151173226, -65.39198021151038631, -17.83149674230410398 ) ) ;
#8250=CARTESIAN_POINT ( 'NONE',  ( 60.94487250823569724, 14.43811055919129949, -47.71586022308749619 ) ) ;
#8252=EDGE_CURVE ( 'NONE', #48088, #5276, #43075, .T. ) ;
#8253=CARTESIAN_POINT ( 'NONE',  ( 46.19336502865940020, 14.89804580897780006, -9.780208910710129544 ) ) ;
#8254=CARTESIAN_POINT ( 'NONE',  ( 40.36721523011259904, -44.88645108045319887, -4.296538310234230273 ) ) ;
#8255=CARTESIAN_POINT ( 'NONE',  ( -6.415768085208600091, 15.00222229924320061, -4.992725166975239937 ) ) ;
#8257=CARTESIAN_POINT ( 'NONE',  ( 60.21275759892589718, 14.07912474133270031, -26.88233855053889698 ) ) ;
#8262=CARTESIAN_POINT ( 'NONE',  ( 53.83033730549027496, -50.85522578410522243, -76.11623740298810503 ) ) ;
#8265=ADVANCED_FACE ( 'NONE', ( #27495 ), #17102, .F. ) ;
#8266=AXIS2_PLACEMENT_3D ( 'NONE', #16370, #32070, #1163 ) ;
#8267=CARTESIAN_POINT ( 'NONE',  ( 12.06284766121009966, -63.44323389162830296, -46.39999999999999858 ) ) ;
#8269=EDGE_CURVE ( 'NONE', #44411, #14960, #5388, .T. ) ;
#8270=CARTESIAN_POINT ( 'NONE',  ( 46.81801046767949970, 22.71153819036710075, -75.82551469934900013 ) ) ;
#8271=CARTESIAN_POINT ( 'NONE',  ( 48.70825858349740400, -54.07088363299979505, -55.10877340735739693 ) ) ;
#8272=CARTESIAN_POINT ( 'NONE',  ( 51.68175210104495676, -32.44720899933275149, -18.13119989886391537 ) ) ;
#8274=CARTESIAN_POINT ( 'NONE',  ( 57.50723796702470025, -47.11618894467930119, -17.93019253464870033 ) ) ;
#8275=DIRECTION ( 'NONE',  ( -1.000000000000000000, 5.464378949326942347E-15, 0.000000000000000000 ) ) ;
#8277=EDGE_LOOP ( 'NONE', ( #19873, #43462, #26010, #36347, #44255 ) ) ;
#8283=CARTESIAN_POINT ( 'NONE',  ( 61.01538930092709734, -45.46451225926809769, -47.38536193545689912 ) ) ;
#8290=VERTEX_POINT ( 'NONE', #42473 ) ;
#8291=CARTESIAN_POINT ( 'NONE',  ( 84.44303304399450383, -43.32157562320250577, -47.45512980871949793 ) ) ;
#8292=ORIENTED_EDGE ( 'NONE', *, *, #29071, .F. ) ;
#8296=CARTESIAN_POINT ( 'NONE',  ( 54.17308945005400034, -50.61618894467930119, -77.01198594373980200 ) ) ;
#8297=CARTESIAN_POINT ( 'NONE',  ( 76.41350034479297904, -9.865538814804375889, -12.85467835030281414 ) ) ;
#8298=CARTESIAN_POINT ( 'NONE',  ( 53.65725511832430072, -51.85618790261810318, -53.56195944851729962 ) ) ;
#8300=ORIENTED_EDGE ( 'NONE', *, *, #43962, .T. ) ;
#8301=CARTESIAN_POINT ( 'NONE',  ( 48.51124500827120301, 22.78135976125399864, -54.58137771766570268 ) ) ;
#8302=CARTESIAN_POINT ( 'NONE',  ( 57.32036346896229873, -45.12488344740960144, -25.31853672637360120 ) ) ;
#8303=CARTESIAN_POINT ( 'NONE',  ( 56.40269203625919658, -50.74743185910909915, -53.40076008979360012 ) ) ;
#8304=LINE ( 'NONE', #12498, #978 ) ;
#8309=CARTESIAN_POINT ( 'NONE',  ( 53.03699916977929973, -50.36565223154730120, -77.13749947632319959 ) ) ;
#8310=CARTESIAN_POINT ( 'NONE',  ( 60.34379259250669492, 14.63564649040839960, -47.72732609510669732 ) ) ;
#8311=VECTOR ( 'NONE', #25256, 1000.000000000000227 ) ;
#8312=LINE ( 'NONE', #196, #46298 ) ;
#8313=AXIS2_PLACEMENT_3D ( 'NONE', #29194, #26749, #13501 ) ;
#8314=AXIS2_PLACEMENT_3D ( 'NONE', #51221, #7194, #15051 ) ;
#8316=EDGE_CURVE ( 'NONE', #49564, #19884, #10096, .T. ) ;
#8317=CARTESIAN_POINT ( 'NONE',  ( 12.49509346338360061, -50.35846906381240018, -21.18371118359339889 ) ) ;
#8318=CARTESIAN_POINT ( 'NONE',  ( 59.49262858449159808, -48.61618894467930119, -53.92796738110899923 ) ) ;
#8322=CARTESIAN_POINT ( 'NONE',  ( 70.83745409581581498, -49.21324915460289162, -70.54648330188271643 ) ) ;
#8323=CARTESIAN_POINT ( 'NONE',  ( 61.10200083216010114, -45.74837858088729803, -47.83148726571160125 ) ) ;
#8327=ORIENTED_EDGE ( 'NONE', *, *, #48033, .F. ) ;
#8328=CARTESIAN_POINT ( 'NONE',  ( 14.25534935311820028, -51.38128844478910651, -75.14498753492070193 ) ) ;
#8329=CARTESIAN_POINT ( 'NONE',  ( 47.35085381701830443, -54.68778914017550363, -54.79599060749220030 ) ) ;
#8330=FACE_OUTER_BOUND ( 'NONE', #49702, .T. ) ;
#8333=B_SPLINE_CURVE_WITH_KNOTS ( 'NONE', 3,
 ( #2576, #48139, #47888, #39510, #12496, #8302, #51810, #43950, #24257, #23233, #15917, #184, #40278, #12240, #3352, #28203, #19326, #44204, #19836, #27696, #43694, #4368, #43188, #31871, #11737 ),
 .UNSPECIFIED., .F., .F.,
 ( 4, 3, 3, 3, 3, 3, 3, 3, 4 ),
 ( -0.9179866157961039663, -0.8390154556610909253, -0.8167403651645870344, -0.7424182710533929752, -0.7016502394034429546, -0.6210824869669100412, -0.5865601136422979867, -0.5066596203617099725, -0.4589335890893689873 ),
 .UNSPECIFIED. ) ;
#8334=CARTESIAN_POINT ( 'NONE',  ( 60.91744553903900083, -45.44454046914316336, -47.19084313326123237 ) ) ;
#8335=CARTESIAN_POINT ( 'NONE',  ( 46.81978912889830013, -53.49478526707780190, -76.01748491306379663 ) ) ;
#8336=ADVANCED_FACE ( 'NONE', ( #47442 ), #11537, .F. ) ;
#8337=CARTESIAN_POINT ( 'NONE',  ( 10.62398834547849980, 33.60001816844019373, -18.14938726548519909 ) ) ;
#8338=CARTESIAN_POINT ( 'NONE',  ( 61.04001029137710077, 14.12696047140060074, -46.86320535112459851 ) ) ;
#8339=CARTESIAN_POINT ( 'NONE',  ( -7.450541063502280181, -45.60837410880110099, -5.667773980459688943 ) ) ;
#8340=CARTESIAN_POINT ( 'NONE',  ( 1.775259308235590083, -55.58082413018939860, -10.96133985404039990 ) ) ;
#8341=CARTESIAN_POINT ( 'NONE',  ( 43.91474985151640453, 12.31375205243809923, -5.093415854581109237 ) ) ;
#8342=CARTESIAN_POINT ( 'NONE',  ( 48.47704942716229937, 22.94511149931419780, -55.22628212196720199 ) ) ;
#8344=CIRCLE ( 'NONE', #27601, 2.000000000000001776 ) ;
#8345=CARTESIAN_POINT ( 'NONE',  ( 53.25070616645550103, -49.48958487454920174, -49.09190788158600327 ) ) ;
#8346=ORIENTED_EDGE ( 'NONE', *, *, #27688, .T. ) ;
#8348=DIRECTION ( 'NONE',  ( 0.6888026391158329487, 0.7071067811865494601, 0.1598465650148944150 ) ) ;
#8349=DIRECTION ( 'NONE',  ( -0.5109955813515499878, 0.8595833385072046973, 0.000000000000000000 ) ) ;
#8350=FACE_OUTER_BOUND ( 'NONE', #31605, .T. ) ;
#8351=CARTESIAN_POINT ( 'NONE',  ( 83.67009235204480433, 13.30315351291969961, -46.70940576878270178 ) ) ;
#8352=CARTESIAN_POINT ( 'NONE',  ( 53.83139499286720309, 17.29048075286380026, -26.60275948463279860 ) ) ;
#8353=AXIS2_PLACEMENT_3D ( 'NONE', #44058, #28313, #796 ) ;
#8356=CARTESIAN_POINT ( 'NONE',  ( 52.70698220066480388, 18.52838197885590077, -48.81385519956149466 ) ) ;
#8357=CARTESIAN_POINT ( 'NONE',  ( 55.78374828174529654, -45.43414358645100037, -16.08112280697800145 ) ) ;
#8358=DIRECTION ( 'NONE',  ( 0.3294064756440929220, 0.9441882088883218893, 0.000000000000000000 ) ) ;
#8359=ORIENTED_EDGE ( 'NONE', *, *, #43436, .F. ) ;
#8362=ORIENTED_EDGE ( 'NONE', *, *, #42131, .T. ) ;
#8363=CARTESIAN_POINT ( 'NONE',  ( 11.65337902053890140, -65.21696613297268641, -16.97470852089599802 ) ) ;
#8364=CARTESIAN_POINT ( 'NONE',  ( 12.56561337444859916, 34.23963782672920075, -47.52000344619509775 ) ) ;
#8365=CARTESIAN_POINT ( 'NONE',  ( 17.92370450342619748, 19.88381105532299742, -15.67980087199299888 ) ) ;
#8366=( BOUNDED_CURVE ( )  B_SPLINE_CURVE ( 3, ( #19924, #35917, #12085, #20432 ),
 .UNSPECIFIED., .F., .T. ) 
 B_SPLINE_CURVE_WITH_KNOTS ( ( 4, 4 ),
 ( 2.702343591312255100, 2.767378142270199959 ),
 .UNSPECIFIED. ) 
 CURVE ( )  GEOMETRIC_REPRESENTATION_ITEM ( )  RATIONAL_B_SPLINE_CURVE ( ( 1.000000000000000000, 0.9996475733206606762, 0.9996475733206606762, 1.000000000000000000 ) ) 
 REPRESENTATION_ITEM ( '' )  );
#8367=CARTESIAN_POINT ( 'NONE',  ( 53.24273501492499605, -49.42207489150700184, -48.94011550641359776 ) ) ;
#8368=CARTESIAN_POINT ( 'NONE',  ( 10.64863409883700029, -63.44323389162830296, -23.66469670114080159 ) ) ;
#8370=ORIENTED_EDGE ( 'NONE', *, *, #29964, .T. ) ;
#8371=CARTESIAN_POINT ( 'NONE',  ( 13.32898876123410403, 19.91878638302433657, -21.92090654609880218 ) ) ;
#8372=CARTESIAN_POINT ( 'NONE',  ( 10.97902946416030012, -63.29183189191540748, -44.74276748639299939 ) ) ;
#8373=FACE_OUTER_BOUND ( 'NONE', #17015, .T. ) ;
#8374=ORIENTED_EDGE ( 'NONE', *, *, #5622, .T. ) ;
#8380=DIRECTION ( 'NONE',  ( 0.000000000000000000, 0.000000000000000000, 1.000000000000000000 ) ) ;
#8381=CARTESIAN_POINT ( 'NONE',  ( 57.36123081458359962, -50.13537923174280309, -52.61896056486340001 ) ) ;
#8382=CARTESIAN_POINT ( 'NONE',  ( 49.38980915263670113, 22.26227279580249885, -54.14433698582279675 ) ) ;
#8384=EDGE_CURVE ( 'NONE', #9438, #4297, #3884, .T. ) ;
#8385=CARTESIAN_POINT ( 'NONE',  ( 10.10517893431049963, -55.15925497894330931, -21.14999999999999858 ) ) ;
#8394=VECTOR ( 'NONE', #49632, 1000.000000000000000 ) ;
#8396=CARTESIAN_POINT ( 'NONE',  ( 47.24370953076470414, 23.52822497215869646, -74.17376148375639389 ) ) ;
#8398=EDGE_CURVE ( 'NONE', #51191, #17738, #34491, .T. ) ;
#8400=CARTESIAN_POINT ( 'NONE',  ( 12.28024544113380045, 33.39054034926959957, -15.84304030212500081 ) ) ;
#8403=CARTESIAN_POINT ( 'NONE',  ( 56.17731397218030054, -50.61618894601519969, -75.94110601102539704 ) ) ;
#8409=CARTESIAN_POINT ( 'NONE',  ( 61.39588016577010166, 13.94803720521050039, -46.37201980406299384 ) ) ;
#8410=CARTESIAN_POINT ( 'NONE',  ( -0.3068767133167060179, -63.31736862303570490, -50.59628790670890197 ) ) ;
#8413=CARTESIAN_POINT ( 'NONE',  ( 52.84340795157500281, -49.65376797971740075, -48.59551871909959431 ) ) ;
#8414=CARTESIAN_POINT ( 'NONE',  ( 61.34256095932860120, -45.15002362613940079, -27.50959865473700106 ) ) ;
#8416=CARTESIAN_POINT ( 'NONE',  ( 57.10264026197389597, 14.43158848240689984, -26.17393976174119885 ) ) ;
#8418=CARTESIAN_POINT ( 'NONE',  ( 50.30621290460380379, 17.52022015291559853, -76.16272939178270462 ) ) ;
#8419=CARTESIAN_POINT ( 'NONE',  ( 52.76045202141140322, 18.46818829728630007, -48.50240600070850405 ) ) ;
#8421=CARTESIAN_POINT ( 'NONE',  ( 42.62644315484929791, -42.85940974227979439, -3.197525305375130245 ) ) ;
#8422=CARTESIAN_POINT ( 'NONE',  ( 53.78771641980449658, -51.63629534268280707, -53.21849989078970111 ) ) ;
#8425=VECTOR ( 'NONE', #16106, 1000.000000000000000 ) ;
#8426=CARTESIAN_POINT ( 'NONE',  ( 47.73397142286539463, -54.47958293233019589, -54.93080396559629719 ) ) ;
#8427=CARTESIAN_POINT ( 'NONE',  ( -8.011283399303589903, 13.73034950232750084, -5.061381375665199300 ) ) ;
#8428=AXIS2_PLACEMENT_3D ( 'NONE', #34950, #10612, #6940 ) ;
#8429=CARTESIAN_POINT ( 'NONE',  ( 42.93197233849420513, 11.32569894967160096, -3.187564294433600232 ) ) ;
#8430=CARTESIAN_POINT ( 'NONE',  ( 56.91683567916710018, 19.43129369009569984, -53.20179923793649834 ) ) ;
#8432=CARTESIAN_POINT ( 'NONE',  ( 41.13393739769620083, -15.61618894467929941, 4.450000000000000178 ) ) ;
#8441=CYLINDRICAL_SURFACE ( 'NONE', #27717, 5.000000000000000000 ) ;
#8455=CARTESIAN_POINT ( 'NONE',  ( 11.75056615120120185, -63.52426806926749236, -24.76662875350499959 ) ) ;
#8457=CARTESIAN_POINT ( 'NONE',  ( 41.71810510585039822, 14.49570306633170169, -6.599646603091770203 ) ) ;
#8458=CARTESIAN_POINT ( 'NONE',  ( 14.41909000996080081, 21.14718688187949880, -75.96082109999758814 ) ) ;
#8459=CARTESIAN_POINT ( 'NONE',  ( 51.73306225501220013, 17.77684153297740011, -77.03096025368019184 ) ) ;
#8461=EDGE_CURVE ( 'NONE', #33975, #31547, #3708, .T. ) ;
#8463=AXIS2_PLACEMENT_3D ( 'NONE', #29052, #9151, #17275 ) ;
#8465=ORIENTED_EDGE ( 'NONE', *, *, #42246, .T. ) ;
#8466=CARTESIAN_POINT ( 'NONE',  ( 53.86231929347299996, -48.56206393835490331, -26.75416873081589841 ) ) ;
#8467=CARTESIAN_POINT ( 'NONE',  ( 15.94236692260130006, -50.98710977590300075, -20.14988694616399911 ) ) ;
#8468=CARTESIAN_POINT ( 'NONE',  ( 76.84075427690970628, 10.73731228644500035, -14.69578844725669953 ) ) ;
#8472=DIRECTION ( 'NONE',  ( 0.1686178020941689892, 0.6660492713794449182, -0.7265992051412129005 ) ) ;
#8473=VERTEX_POINT ( 'NONE', #7443 ) ;
#8474=CARTESIAN_POINT ( 'NONE',  ( -4.044075683915660413, -48.07007205289909990, -5.230652478517891169 ) ) ;
#8475=CARTESIAN_POINT ( 'NONE',  ( 47.36954728576590412, 23.43543924705889836, -54.64415512175509804 ) ) ;
#8479=CARTESIAN_POINT ( 'NONE',  ( 43.02291017071019752, 12.66373381907540008, -5.004961222460109660 ) ) ;
#8482=DIRECTION ( 'NONE',  ( 0.4042525045258790750, 0.000000000000000000, -0.9146474252872273114 ) ) ;
#8483=CARTESIAN_POINT ( 'NONE',  ( 59.50642288013500547, -46.25939025630010093, -47.77182982531389399 ) ) ;
#8486=CARTESIAN_POINT ( 'NONE',  ( 56.45472350107259984, 19.54838399657660020, -53.73843559234909861 ) ) ;
#8487=DIRECTION ( 'NONE',  ( 0.000000000000000000, 0.000000000000000000, -1.000000000000000000 ) ) ;
#8488=CARTESIAN_POINT ( 'NONE',  ( 50.44542158113339525, 13.88381105532070059, -10.59990841363550018 ) ) ;
#8489=ORIENTED_EDGE ( 'NONE', *, *, #41754, .F. ) ;
#8491=CARTESIAN_POINT ( 'NONE',  ( 9.736267853041370657, 31.97384013447830142, -46.29821234986540190 ) ) ;
#8492=CARTESIAN_POINT ( 'NONE',  ( 41.60144942313346661, 13.58288154834297501, -5.503716546408811361 ) ) ;
#8495=CARTESIAN_POINT ( 'NONE',  ( 18.36003180639029964, 20.26946707534090208, -75.09610479291009710 ) ) ;
#8499=FACE_OUTER_BOUND ( 'NONE', #21799, .T. ) ;
#8501=AXIS2_PLACEMENT_3D ( 'NONE', #4413, #35349, #8349 ) ;
#8505=CARTESIAN_POINT ( 'NONE',  ( 14.34417029198830029, 19.88381105532299742, -74.14999999999999147 ) ) ;
#8507=FACE_OUTER_BOUND ( 'NONE', #32319, .T. ) ;
#8508=ORIENTED_EDGE ( 'NONE', *, *, #39766, .F. ) ;
#8511=CARTESIAN_POINT ( 'NONE',  ( 51.81838375203209779, 2.459119445085170330, -77.22003095415269058 ) ) ;
#8512=ORIENTED_EDGE ( 'NONE', *, *, #20425, .T. ) ;
#8516=FACE_OUTER_BOUND ( 'NONE', #39444, .T. ) ;
#8518=CARTESIAN_POINT ( 'NONE',  ( 60.77958717670829714, 14.50249311732349966, -47.75277892092170617 ) ) ;
#8519=ADVANCED_FACE ( 'NONE', ( #46518 ), #19225, .T. ) ;
#8520=CARTESIAN_POINT ( 'NONE',  ( 45.70140901369219932, 14.68666752987680013, -9.304972802417179167 ) ) ;
#8522=CARTESIAN_POINT ( 'NONE',  ( -7.088889386270000870, 14.46722970464960056, -4.961773261597420159 ) ) ;
#8524=CARTESIAN_POINT ( 'NONE',  ( 54.47259832750690123, 15.01994964729280113, -15.76422791930239953 ) ) ;
#8527=DIRECTION ( 'NONE',  ( -1.000000000000000000, 0.000000000000000000, 0.000000000000000000 ) ) ;
#8528=B_SPLINE_CURVE_WITH_KNOTS ( 'NONE', 3,
 ( #39222, #35279, #7512, #43160, #47354, #11450, #27408, #35010, #2806, #42381 ),
 .UNSPECIFIED., .F., .F.,
 ( 4, 2, 2, 2, 4 ),
 ( 0.4999999999999911737, 0.5970844297732782469, 0.7236511483078821305, 0.8661472597497344994, 1.000000000000000000 ),
 .UNSPECIFIED. ) ;
#8529=CARTESIAN_POINT ( 'NONE',  ( 40.84819594366380358, 14.17549957042029973, -5.828853726967939686 ) ) ;
#8530=CARTESIAN_POINT ( 'NONE',  ( 12.21949317767530019, 34.07078414252080023, -46.32488671064290031 ) ) ;
#8533=EDGE_CURVE ( 'NONE', #10891, #3359, #7597, .T. ) ;
#8536=CIRCLE ( 'NONE', #21051, 22.00000000000000000 ) ;
#8537=TOROIDAL_SURFACE ( 'NONE', #11922, 18.00000000000000000, 2.000000000000000000 ) ;
#8538=CARTESIAN_POINT ( 'NONE',  ( 11.68991505667689879, -64.90566085822540288, -16.36861125146140239 ) ) ;
#8539=CARTESIAN_POINT ( 'NONE',  ( 46.38760183179699936, 21.75546072051859881, -76.14872548137130082 ) ) ;
#8540=CARTESIAN_POINT ( 'NONE',  ( 49.05314114107740409, -53.88090997908469859, -54.81529494278139936 ) ) ;
#8541=CARTESIAN_POINT ( 'NONE',  ( -4.967261132674519963, 16.44508974743529706, -5.583919853821729617 ) ) ;
#8548=ORIENTED_EDGE ( 'NONE', *, *, #48493, .T. ) ;
#8549=DIRECTION ( 'NONE',  ( 0.000000000000000000, 0.000000000000000000, -1.000000000000000000 ) ) ;
#8550=CARTESIAN_POINT ( 'NONE',  ( 60.52205090682910082, -45.66102862280700236, -47.41488707632970545 ) ) ;
#8551=CARTESIAN_POINT ( 'NONE',  ( 68.13393739769620083, -48.61618894467930119, -65.65000000000000568 ) ) ;
#8552=CARTESIAN_POINT ( 'NONE',  ( 64.89113374320363903, -43.41649467415835772, -10.41665185867834964 ) ) ;
#8559=CARTESIAN_POINT ( 'NONE',  ( 83.49396592876078671, -45.25227995425159833, -47.52773119087509457 ) ) ;
#8563=CARTESIAN_POINT ( 'NONE',  ( 61.54545584751650011, -45.33073283442580248, -47.27437412891610080 ) ) ;
#8564=CARTESIAN_POINT ( 'NONE',  ( 52.97776617209801486, -50.30125835459202932, -77.23905649395202033 ) ) ;
#8565=CARTESIAN_POINT ( 'NONE',  ( 76.39547088046599299, -13.14241137819745653, -12.77698718076613815 ) ) ;
#8566=CARTESIAN_POINT ( 'NONE',  ( 52.30020358789180079, -52.26933069182599212, -53.48872967491809760 ) ) ;
#8569=CARTESIAN_POINT ( 'NONE',  ( 47.82941845642289991, 23.15673897679920046, -54.71834399002119653 ) ) ;
#8572=CARTESIAN_POINT ( 'NONE',  ( 8.788636732660460638, -63.13527780971870129, -46.67124789091300130 ) ) ;
#8573=CARTESIAN_POINT ( 'NONE',  ( 63.14276237176480322, 0.4687350093257069972, -17.15814307286319718 ) ) ;
#8576=CIRCLE ( 'NONE', #190, 1.999999999999998224 ) ;
#8578=CARTESIAN_POINT ( 'NONE',  ( -1.549418844231527537, 19.36423916373297160, -6.286238266776149608 ) ) ;
#8579=CIRCLE ( 'NONE', #2741, 2.000000000000001332 ) ;
#8580=CARTESIAN_POINT ( 'NONE',  ( 54.17317666706389900, -50.61618894916709621, -77.01210126949929702 ) ) ;
#8582=LINE ( 'NONE', #31881, #221 ) ;
#8583=EDGE_CURVE ( 'NONE', #31649, #7985, #2014, .T. ) ;
#8586=CARTESIAN_POINT ( 'NONE',  ( 41.32046296083159831, -44.52894084121439988, -4.975097116197259695 ) ) ;
#8588=CARTESIAN_POINT ( 'NONE',  ( 57.04834586696819798, 13.88381105532070059, -16.05449549621770089 ) ) ;
#8589=CARTESIAN_POINT ( 'NONE',  ( 61.29293631677610676, -45.55587099302650955, -47.63113523840529950 ) ) ;
#8593=CARTESIAN_POINT ( 'NONE',  ( 14.38326576340259955, -51.65751396603660339, -75.51495726157199329 ) ) ;
#8594=CARTESIAN_POINT ( 'NONE',  ( 47.34625512861649810, -54.69081487665980035, -54.80683018298890374 ) ) ;
#8595=CARTESIAN_POINT ( 'NONE',  ( 10.53031889351280981, 33.70290473897190964, -47.11352251473290664 ) ) ;
#8597=CARTESIAN_POINT ( 'NONE',  ( 60.89412992731197249, -45.44744514121628498, -47.14788752398113303 ) ) ;
#8598=CARTESIAN_POINT ( 'NONE',  ( 57.40776171064106137, 14.07025572946862368, -25.91845855463345671 ) ) ;
#8599=FACE_OUTER_BOUND ( 'NONE', #2584, .T. ) ;
#8600=DIRECTION ( 'NONE',  ( 0.000000000000000000, 0.000000000000000000, 1.000000000000000000 ) ) ;
#8602=CARTESIAN_POINT ( 'NONE',  ( 14.98839500567465599, -52.93031137934188024, -76.14999999999994884 ) ) ;
#8603=CARTESIAN_POINT ( 'NONE',  ( 48.45558241519640319, 22.90200554677129929, -54.87093290419399949 ) ) ;
#8607=ORIENTED_EDGE ( 'NONE', *, *, #2540, .F. ) ;
#8611=CARTESIAN_POINT ( 'NONE',  ( 82.65203287802668797, 13.84520072205750019, -46.57208626984800048 ) ) ;
#8612=CARTESIAN_POINT ( 'NONE',  ( 55.08137342987989626, 16.01549851114500100, -26.24734268074100285 ) ) ;
#8615=CARTESIAN_POINT ( 'NONE',  ( 52.57435089425080577, 18.62009177781090230, -48.51307714252150305 ) ) ;
#8616=CARTESIAN_POINT ( 'NONE',  ( 54.83244778698070121, -45.50794643880949764, -15.28355693140960092 ) ) ;
#8617=DIRECTION ( 'NONE',  ( 0.000000000000000000, -1.000000000000000000, 0.000000000000000000 ) ) ;
#8621=EDGE_CURVE ( 'NONE', #25343, #38938, #10752, .T. ) ;
#8622=CARTESIAN_POINT ( 'NONE',  ( 11.80495200724810090, -64.96876320708929597, -16.40176568415489911 ) ) ;
#8623=CARTESIAN_POINT ( 'NONE',  ( 11.11335566852529944, 33.52968406517779698, -46.40488835177220039 ) ) ;
#8624=CARTESIAN_POINT ( 'NONE',  ( 51.17461318815491467, 0.4193470954621815738, -17.11446460828111427 ) ) ;
#8625=CARTESIAN_POINT ( 'NONE',  ( 16.13393739769620083, -15.61618894467929941, -6.649999999999999467 ) ) ;
#8629=CARTESIAN_POINT ( 'NONE',  ( 11.13393739769619906, -63.35298109097990960, -43.74913429451299862 ) ) ;
#8630=CARTESIAN_POINT ( 'NONE',  ( 53.58906601315669604, 18.17498435715450000, -49.22641449468370212 ) ) ;
#8631=CARTESIAN_POINT ( 'NONE',  ( 47.64143405402000297, 23.30250925608569901, -55.14905519569659731 ) ) ;
#8632=CARTESIAN_POINT ( 'NONE',  ( 50.40317164625179913, -49.92886143348300720, -76.14999999999999147 ) ) ;
#8634=ORIENTED_EDGE ( 'NONE', *, *, #40471, .T. ) ;
#8636=CARTESIAN_POINT ( 'NONE',  ( 57.03107162669589769, -50.22865659835970575, -52.68131389647400198 ) ) ;
#8637=CARTESIAN_POINT ( 'NONE',  ( 52.56662653895409676, 22.94659662340869843, -56.87452811520210361 ) ) ;
#8640=CARTESIAN_POINT ( 'NONE',  ( 14.12233147869610050, -51.14020415306820411, -22.75736351947179870 ) ) ;
#8641=CARTESIAN_POINT ( 'NONE',  ( 53.72798125810859915, 20.02004718435770059, -75.61331206641780511 ) ) ;
#8642=CARTESIAN_POINT ( 'NONE',  ( 46.48018481170299765, -53.11273823506989800, -76.13961530627510399 ) ) ;
#8648=DIRECTION ( 'NONE',  ( -0.9339609686412669864, 0.000000000000000000, -0.3573750257847720380 ) ) ;
#8649=CARTESIAN_POINT ( 'NONE',  ( 47.43599257781200151, 23.40374490022220044, -74.17365615959539582 ) ) ;
#8650=CARTESIAN_POINT ( 'NONE',  ( 19.71324513114140231, -54.20984286782871919, -17.35305593079180042 ) ) ;
#8651=CARTESIAN_POINT ( 'NONE',  ( 75.07156378438740774, -22.19556467665293553, -11.41441923602980602 ) ) ;
#8652=CARTESIAN_POINT ( 'NONE',  ( 41.31714037750759871, -44.78197124420869812, -5.389672071857970259 ) ) ;
#8656=CARTESIAN_POINT ( 'NONE',  ( 60.23130391296999875, -45.78304229081430066, -47.24246919202539630 ) ) ;
#8660=CARTESIAN_POINT ( 'NONE',  ( 61.45294174464890347, 13.92837788602000160, -46.37201849592059943 ) ) ;
#8662=DIRECTION ( 'NONE',  ( 0.000000000000000000, 1.000000000000000000, 0.000000000000000000 ) ) ;
#8664=( BOUNDED_CURVE ( )  B_SPLINE_CURVE ( 2, ( #25117, #33761, #29573, #36935, #40604 ),
 .UNSPECIFIED., .F., .T. ) 
 B_SPLINE_CURVE_WITH_KNOTS ( ( 3, 2, 3 ),
 ( -0.003205554297748039981, 0.8238407534185530068, 1.650887061134849843 ),
 .UNSPECIFIED. ) 
 CURVE ( )  GEOMETRIC_REPRESENTATION_ITEM ( )  RATIONAL_B_SPLINE_CURVE ( ( 1.000000000000000000, 0.9157107718030679244, 1.000000000000000000, 0.9157107718030469412, 1.000000000000000000 ) ) 
 REPRESENTATION_ITEM ( '' )  );
#8665=CARTESIAN_POINT ( 'NONE',  ( 52.86217718811949595, -49.64393425081360789, -48.67083959267399962 ) ) ;
#8666=CARTESIAN_POINT ( 'NONE',  ( 60.50740924954109801, -45.14437743309510154, -26.64919274788590187 ) ) ;
#8668=CARTESIAN_POINT ( 'NONE',  ( 56.62419727214309262, 14.29741701462000059, -25.88689047256800180 ) ) ;
#8670=CARTESIAN_POINT ( 'NONE',  ( 50.21099649534220077, 18.14781963348989891, -76.14999999999999147 ) ) ;
#8671=CARTESIAN_POINT ( 'NONE',  ( 53.22412257189229479, 18.23394763870219748, -48.94726806477149950 ) ) ;
#8673=CARTESIAN_POINT ( 'NONE',  ( 11.13393739769619906, -55.30245861064819479, -24.15000000000000213 ) ) ;
#8674=CARTESIAN_POINT ( 'NONE',  ( 66.97218591609239979, -45.11618894467940066, -13.04694144512030007 ) ) ;
#8678=EDGE_CURVE ( 'NONE', #11745, #27748, #41994, .T. ) ;
#8681=CARTESIAN_POINT ( 'NONE',  ( 47.64143405402000297, -54.53488714544450033, -55.14905519569939685 ) ) ;
#8682=CARTESIAN_POINT ( 'NONE',  ( 11.89321892217540011, -65.43602743108330344, -18.17421237901570308 ) ) ;
#8684=CARTESIAN_POINT ( 'NONE',  ( 41.06001733956060207, 13.06695014755839956, -3.719605790254209676 ) ) ;
#8685=CARTESIAN_POINT ( 'NONE',  ( 57.18156601109950543, 18.52541442572180230, -52.05824807082350247 ) ) ;
#8693=VERTEX_POINT ( 'NONE', #9513 ) ;
#8694=EDGE_LOOP ( 'NONE', ( #23165, #14632, #16735, #39242, #37454 ) ) ;
#8696=CARTESIAN_POINT ( 'NONE',  ( 16.13232929059349985, -51.04699384658444217, -15.66849738685780657 ) ) ;
#8698=CARTESIAN_POINT ( 'NONE',  ( 16.13393739769620083, -15.61618894467929941, -11.23251175440650051 ) ) ;
#8700=CARTESIAN_POINT ( 'NONE',  ( 54.11862986506081796, 20.00205326672937645, -75.47294485644663098 ) ) ;
#8701=CARTESIAN_POINT ( 'NONE',  ( 51.62918027504110086, 19.74959736141559929, -76.14997290609490221 ) ) ;
#8702=EDGE_LOOP ( 'NONE', ( #5676, #3248, #30510, #48460, #4663 ) ) ;
#8703=DIRECTION ( 'NONE',  ( 0.2956364143885911178, -0.8200397212266696823, 0.4900346580579206246 ) ) ;
#8705=CARTESIAN_POINT ( 'NONE',  ( 61.28085239525059791, 14.36939662108470017, -47.67834120296360112 ) ) ;
#8706=EDGE_CURVE ( 'NONE', #31690, #32099, #7081, .T. ) ;
#8710=EDGE_CURVE ( 'NONE', #18800, #20534, #31289, .T. ) ;
#8711=B_SPLINE_CURVE_WITH_KNOTS ( 'NONE', 3,
 ( #35161, #38603, #2693, #18666, #43050, #34640, #15519, #46733, #31472, #34904, #26778, #22840 ),
 .UNSPECIFIED., .F., .F.,
 ( 4, 2, 2, 2, 2, 4 ),
 ( 0.000000000000000000, 0.1250000000000000000, 0.2500000000000000000, 0.5000000000000000000, 0.7500000000000000000, 1.000000000000000000 ),
 .UNSPECIFIED. ) ;
#8717=CARTESIAN_POINT ( 'NONE',  ( 13.83803551327370229, 20.84559406376729740, -75.48537863783369062 ) ) ;
#8719=CARTESIAN_POINT ( 'NONE',  ( 83.10006388208900319, -44.89976216378850182, -46.45756164887509954 ) ) ;
#8723=CARTESIAN_POINT ( 'NONE',  ( 53.52135793756909976, -48.91598921442630399, -26.96728785596230082 ) ) ;
#8724=CARTESIAN_POINT ( 'NONE',  ( 14.79734571143089994, -51.11619430643680317, -22.20703854455320325 ) ) ;
#8725=CARTESIAN_POINT ( 'NONE',  ( 76.59936668305130070, 10.83832045962729929, -14.02863287010100102 ) ) ;
#8726=CARTESIAN_POINT ( 'NONE',  ( 57.24929578234380045, 19.38381105828390361, -53.91492796160409284 ) ) ;
#8727=DIRECTION ( 'NONE',  ( 0.000000000000000000, 0.000000000000000000, -1.000000000000000000 ) ) ;
#8730=CARTESIAN_POINT ( 'NONE',  ( -11.32734370190460105, -41.88171845330919751, -6.430192534648670133 ) ) ;
#8731=CARTESIAN_POINT ( 'NONE',  ( 47.35435173871399428, 23.44893959130619976, -54.68374326288559928 ) ) ;
#8735=CARTESIAN_POINT ( 'NONE',  ( 41.40756461421400303, 13.53921217941219979, -5.393981499654319833 ) ) ;
#8739=CARTESIAN_POINT ( 'NONE',  ( 59.91112534698100234, -46.04755292983879400, -47.70997890928379803 ) ) ;
#8741=CIRCLE ( 'NONE', #26301, 21.50000000000000000 ) ;
#8744=CARTESIAN_POINT ( 'NONE',  ( 17.86672151352269822, -52.48721817738829287, -75.97756937697440094 ) ) ;
#8745=CYLINDRICAL_SURFACE ( 'NONE', #14536, 1.999999999999999778 ) ;
#8749=CARTESIAN_POINT ( 'NONE',  ( 8.975705354591740459, 32.03333151996960027, -46.63325874977040542 ) ) ;
#8751=CARTESIAN_POINT ( 'NONE',  ( 67.98302783225990709, -31.38011479710340623, -18.18687859448679944 ) ) ;
#8753=CARTESIAN_POINT ( 'NONE',  ( 18.54732536477180105, 20.81202934652590031, -75.33782839756391070 ) ) ;
#8756=EDGE_LOOP ( 'NONE', ( #29173, #16800, #19117, #28911 ) ) ;
#8759=CARTESIAN_POINT ( 'NONE',  ( 10.80918145290640098, -64.05807750357701025, -45.60126697491269709 ) ) ;
#8760=PLANE ( 'NONE',  #49477 ) ;
#8762=CARTESIAN_POINT ( 'NONE',  ( 61.49527322741659674, 13.95390136402409986, -46.82383681851589330 ) ) ;
#8763=EDGE_LOOP ( 'NONE', ( #11606, #46092, #45528, #44777, #5202 ) ) ;
#8764=CARTESIAN_POINT ( 'NONE',  ( 75.24686161380772376, 2.959163858433984551, -12.27461306487479042 ) ) ;
#8766=ORIENTED_EDGE ( 'NONE', *, *, #11824, .T. ) ;
#8767=CARTESIAN_POINT ( 'NONE',  ( 50.59865144046819552, -46.19777500518519986, -12.88937842738419981 ) ) ;
#8768=CARTESIAN_POINT ( 'NONE',  ( 14.90064330294591954, -52.99263552515018461, -76.14999999999999147 ) ) ;
#8769=EDGE_CURVE ( 'NONE', #19, #34516, #17366, .T. ) ;
#8770=CARTESIAN_POINT ( 'NONE',  ( 10.47385409520754784, -55.21366976880749888, -45.62050209441289894 ) ) ;
#8775=CARTESIAN_POINT ( 'NONE',  ( 60.74502025776879321, 14.51238070346370002, -47.75426036517409756 ) ) ;
#8776=FACE_OUTER_BOUND ( 'NONE', #31817, .T. ) ;
#8777=AXIS2_PLACEMENT_3D ( 'NONE', #11555, #3948, #23567 ) ;
#8778=DIRECTION ( 'NONE',  ( 0.000000000000000000, 0.000000000000000000, 1.000000000000000000 ) ) ;
#8779=CARTESIAN_POINT ( 'NONE',  ( -5.332450679183510012, 15.75303166516230036, -4.673630178135430135 ) ) ;
#8781=CARTESIAN_POINT ( 'NONE',  ( 61.28115109886760337, 13.99884544370929973, -28.05810216926879974 ) ) ;
#8783=B_SPLINE_SURFACE_WITH_KNOTS ( 'NONE', 3, 3, ( 
 ( #15576, #24168, #31532, #11910, #7453, #31270, #15053, #39426, #39678, #35486, #23913, #16080, #43104, #50955, #23405, #19995 ),
 ( #108, #3526, #32039, #48061, #12161, #44123, #7719, #23664, #19238, #7196, #40192, #3784, #31020, #15317, #19753, #47045 ),
 ( #3262, #35745, #15822, #35220, #51223, #47302, #11392, #27354, #36245, #32292, #17379, #16863, #37033, #13463, #32542, #13207 ),
 ( #21288, #44898, #48578, #28633, #33078, #32811, #25474, #41222, #12940, #37294, #12679, #354, #9527, #8483, #8739, #16337 ),
 ( #29418, #44634, #24689, #45422, #48314, #12410, #41479, #24429, #1392, #9270, #40704, #28374, #25217, #4803, #5337, #36758 ),
 ( #36500, #28896, #5594, #33346, #604, #48837, #29157, #44381, #40443, #20770, #870, #9005, #45156, #24948, #40959, #5076 ),
 ( #49106, #4534, #49362, #20508, #16589, #21032, #1130, #17125, #5844, #25996, #21810, #6107, #10295, #21548, #6363, #2690 ),
 ( #22063, #42264, #30708, #37817, #30448, #41739, #1910, #38073, #22323, #38329, #26259, #2419, #14738, #18662, #49622, #25731 ) ),
 .UNSPECIFIED., .F., .F., .F.,
 ( 4, 1, 3, 4 ),
 ( 4, 2, 2, 2, 2, 2, 2, 4 ),
 ( 0.000000000000000000, 0.5000000000000000000, 1.000000000000000000, 1.010000000000000009 ),
 ( 0.000000000000000000, 1.372899869568840137, 2.941928291933239681, 3.922571055910980320, 4.412892437899860631, 5.197406649082060071, 6.452629386973570469, 7.845142111821970410 ),
 .UNSPECIFIED. ) ;
#8785=CARTESIAN_POINT ( 'NONE',  ( 59.77423841227909662, 14.93359823389899788, -47.80915357183090464 ) ) ;
#8791=CARTESIAN_POINT ( 'NONE',  ( 11.22384634879449905, -65.01277928531338546, -16.94931743789749845 ) ) ;
#8793=CARTESIAN_POINT ( 'NONE',  ( 49.66352655669079752, -53.65682907869459939, -54.86856413023180323 ) ) ;
#8794=CARTESIAN_POINT ( 'NONE',  ( -6.178851728588689696, 15.46435443030710033, -5.588668033364348808 ) ) ;
#8795=EDGE_CURVE ( 'NONE', #10642, #15006, #33834, .T. ) ;
#8799=ORIENTED_EDGE ( 'NONE', *, *, #41882, .F. ) ;
#8806=CARTESIAN_POINT ( 'NONE',  ( 61.18220403599099910, -45.50035139021139940, -47.53341915241229998 ) ) ;
#8807=CARTESIAN_POINT ( 'NONE',  ( 57.24507233897389824, 19.38381439978470056, -53.91419826472959898 ) ) ;
#8808=CARTESIAN_POINT ( 'NONE',  ( 13.61804212000129866, 18.93546666416320079, -20.94890277169909965 ) ) ;
#8810=PLANE ( 'NONE',  #34875 ) ;
#8815=CARTESIAN_POINT ( 'NONE',  ( 83.82017571155999747, -44.67807987934809688, -47.23783155238629661 ) ) ;
#8817=ORIENTED_EDGE ( 'NONE', *, *, #27750, .F. ) ;
#8820=CARTESIAN_POINT ( 'NONE',  ( 61.60870436204309897, -45.23813693204910180, -47.07717016886380179 ) ) ;
#8821=DIRECTION ( 'NONE',  ( 0.06672502100504951184, 0.04847856544221944286, 0.9965929962951476373 ) ) ;
#8822=CARTESIAN_POINT ( 'NONE',  ( 76.40019456172100831, -19.50358666587276346, -12.79738190608483883 ) ) ;
#8823=CARTESIAN_POINT ( 'NONE',  ( 54.77086636619779370, -51.21734551792319223, -53.06498560372880746 ) ) ;
#8824=EDGE_CURVE ( 'NONE', #9855, #20898, #49610, .T. ) ;
#8825=EDGE_LOOP ( 'NONE', ( #14284, #42572, #14942, #24444, #4212, #20668, #37315, #43274, #13344, #43244 ) ) ;
#8830=DIRECTION ( 'NONE',  ( -1.000000000000000000, 0.000000000000000000, 0.000000000000000000 ) ) ;
#8835=CARTESIAN_POINT ( 'NONE',  ( 7.542479837843401924, 28.49039248266597824, -11.77476003560691176 ) ) ;
#8836=DIRECTION ( 'NONE',  ( 0.6888026391158329487, -0.7071067811865494601, 0.1598465650148944150 ) ) ;
#8838=CARTESIAN_POINT ( 'NONE',  ( 60.56956494586819417, 14.37343996889240039, -47.17558661336109793 ) ) ;
#8842=CARTESIAN_POINT ( 'NONE',  ( 42.31976156911279929, -43.87010827594590268, -4.715714940980549663 ) ) ;
#8843=CARTESIAN_POINT ( 'NONE',  ( 66.63393739769620083, 11.88381105532070059, -71.50000000000000000 ) ) ;
#8844=CARTESIAN_POINT ( 'NONE',  ( 68.13393739769745139, -49.21324915460109395, -75.95351669811962836 ) ) ;
#8845=CARTESIAN_POINT ( 'NONE',  ( 68.38971107296249841, -1.116188944679350037, -18.15384911730639672 ) ) ;
#8846=EDGE_CURVE ( 'NONE', #21618, #28130, #17945, .T. ) ;
#8848=CIRCLE ( 'NONE', #44830, 1.500000000000001332 ) ;
#8850=CARTESIAN_POINT ( 'NONE',  ( 67.20513489140449792, 1.550091694609170068, -19.24943083180730241 ) ) ;
#8853=CARTESIAN_POINT ( 'NONE',  ( 13.83004271473379987, -51.93606027628250388, -75.41551559479479749 ) ) ;
#8854=CARTESIAN_POINT ( 'NONE',  ( 47.32093757237190346, -54.70280804132740116, -54.63841117994249430 ) ) ;
#8859=CARTESIAN_POINT ( 'NONE',  ( 55.13250725764758187, -46.09227360768333170, -16.25833532637385304 ) ) ;
#8861=CARTESIAN_POINT ( 'NONE',  ( 47.78697217749750337, -54.43650991200640021, -54.82585106944300435 ) ) ;
#8862=CARTESIAN_POINT ( 'NONE',  ( 47.46022127273401026, 23.07192594333263358, -75.17786410066094049 ) ) ;
#8863=CARTESIAN_POINT ( 'NONE',  ( -7.625187662226220020, -45.45404276017920608, -5.684751090845729493 ) ) ;
#8864=CARTESIAN_POINT ( 'NONE',  ( 56.28151124241350800, 19.36078090757409953, -52.90566144362949785 ) ) ;
#8865=CARTESIAN_POINT ( 'NONE',  ( 48.54525988008339255, 22.76209179570290075, -54.56845936111729856 ) ) ;
#8866=ORIENTED_EDGE ( 'NONE', *, *, #34767, .F. ) ;
#8872=DIRECTION ( 'NONE',  ( 0.6566103562584382214, -0.5836782507651213647, 0.4776845608117712971 ) ) ;
#8873=CARTESIAN_POINT ( 'NONE',  ( 83.71674455129429759, 13.26039317643239990, -46.72760658838089398 ) ) ;
#8874=CARTESIAN_POINT ( 'NONE',  ( 52.62011612078570266, 18.57322221019510167, -27.98591982627220176 ) ) ;
#8878=CARTESIAN_POINT ( 'NONE',  ( 56.83984272715319719, -45.11618894467940066, -15.86913725221539906 ) ) ;
#8880=AXIS2_PLACEMENT_3D ( 'NONE', #49863, #17876, #29911 ) ;
#8881=ORIENTED_EDGE ( 'NONE', *, *, #4594, .F. ) ;
#8883=CARTESIAN_POINT ( 'NONE',  ( 12.01222358505219923, -65.01572836191429872, -16.39655052253609924 ) ) ;
#8884=CARTESIAN_POINT ( 'NONE',  ( 12.30426158441329854, 34.20084824820960279, -47.48507929029160124 ) ) ;
#8885=CARTESIAN_POINT ( 'NONE',  ( 61.04001029137710077, -45.35933836075930259, -46.86320535112459851 ) ) ;
#8886=DIRECTION ( 'NONE',  ( 1.000000000000000000, 0.000000000000000000, 0.000000000000000000 ) ) ;
#8888=VECTOR ( 'NONE', #29275, 1000.000000000000114 ) ;
#8890=CARTESIAN_POINT ( 'NONE',  ( 12.54923789920940180, 19.17756050559142267, -21.20205464577261267 ) ) ;
#8894=CARTESIAN_POINT ( 'NONE',  ( 57.50723796702470025, 13.88381105532070059, -17.93019253464870033 ) ) ;
#8895=EDGE_CURVE ( 'NONE', #24585, #17738, #22093, .T. ) ;
#8896=CARTESIAN_POINT ( 'NONE',  ( 50.36549737501839985, -50.07561419642740219, -76.14999999999999147 ) ) ;
#8899=CARTESIAN_POINT ( 'NONE',  ( 54.18928026078430094, -48.04840664809780293, -26.03349461057250025 ) ) ;
#8903=CARTESIAN_POINT ( 'NONE',  ( 51.61135292554669718, -46.21249342017139838, -13.62812988203759801 ) ) ;
#8905=CARTESIAN_POINT ( 'NONE',  ( 14.34417029580689906, -51.11618894467930119, -22.49240189290920000 ) ) ;
#8907=CARTESIAN_POINT ( 'NONE',  ( 16.13393739769620083, -15.61618894467929941, -13.15000000000000036 ) ) ;
#8908=CARTESIAN_POINT ( 'NONE',  ( 47.43257551170959374, -54.63067240927929902, -74.36142533359220863 ) ) ;
#8910=FACE_OUTER_BOUND ( 'NONE', #25008, .T. ) ;
#8913=EDGE_CURVE ( 'NONE', #34714, #3421, #30695, .T. ) ;
#8916=AXIS2_PLACEMENT_3D ( 'NONE', #27615, #11650, #39172 ) ;
#8918=CARTESIAN_POINT ( 'NONE',  ( 47.09511218098770513, 22.86011577770599956, -75.60848552117779775 ) ) ;
#8919=CARTESIAN_POINT ( 'NONE',  ( 19.84371743758253714, -54.58381977003536178, -17.84615285344403546 ) ) ;
#8920=EDGE_CURVE ( 'NONE', #23175, #48985, #28506, .T. ) ;
#8921=CARTESIAN_POINT ( 'NONE',  ( 55.91595717589669334, 14.67227259378219983, -17.93019253464870033 ) ) ;
#8925=VECTOR ( 'NONE', #49178, 1000.000000000000000 ) ;
#8931=CARTESIAN_POINT ( 'NONE',  ( 13.10176660314340147, -65.52395148895190857, -47.73582792185870005 ) ) ;
#8932=VERTEX_POINT ( 'NONE', #30433 ) ;
#8934=CARTESIAN_POINT ( 'NONE',  ( 52.76444823262289674, -49.70074108386170053, -48.64234372005410023 ) ) ;
#8935=CARTESIAN_POINT ( 'NONE',  ( 57.94110753308110162, -45.18729252235269911, -25.80829669411419758 ) ) ;
#8937=CARTESIAN_POINT ( 'NONE',  ( 13.21390947859770115, 19.65074986685339908, -21.61005117736269909 ) ) ;
#8938=CARTESIAN_POINT ( 'NONE',  ( 56.21969265526590220, 14.80816776983419913, -26.07003510870140062 ) ) ;
#8940=CARTESIAN_POINT ( 'NONE',  ( 51.07962909496099968, 18.40003410206369949, -76.32455169463339928 ) ) ;
#8941=CARTESIAN_POINT ( 'NONE',  ( 52.73800103340319367, 18.49116459405509971, -48.71589999865829412 ) ) ;
#8944=CARTESIAN_POINT ( 'NONE',  ( 8.133937397696209715, -59.33545798990849818, -21.14999999999999858 ) ) ;
#8945=CARTESIAN_POINT ( 'NONE',  ( 72.29879703195499019, -43.70058892286719754, -12.53766171548880060 ) ) ;
#8949=CARTESIAN_POINT ( 'NONE',  ( 47.42745323055219586, -54.62870758109379921, -54.65928341309859917 ) ) ;
#8952=CARTESIAN_POINT ( 'NONE',  ( 57.29122018273359629, 19.04244741251779871, -52.77760329876059586 ) ) ;
#8958=EDGE_LOOP ( 'NONE', ( #22452, #21303, #16880, #23682, #21954 ) ) ;
#8960=CARTESIAN_POINT ( 'NONE',  ( 8.800117217589539464, -63.19572640051600132, -46.67015592357310538 ) ) ;
#8961=CARTESIAN_POINT ( 'NONE',  ( 48.82567944625920120, -28.11618896394480061, -15.64999999241030082 ) ) ;
#8963=CARTESIAN_POINT ( 'NONE',  ( 11.14351463905549977, -63.74727278248460038, -43.82532547204769457 ) ) ;
#8966=CARTESIAN_POINT ( 'NONE',  ( 53.10072982268869879, 19.49376234953830078, -76.45474630841620467 ) ) ;
#8971=CARTESIAN_POINT ( 'NONE',  ( 16.13393739769620083, -15.61618894467929941, -7.225658350974740074 ) ) ;
#8973=DIRECTION ( 'NONE',  ( 1.000000000000000000, 0.000000000000000000, 0.000000000000000000 ) ) ;
#8978=CARTESIAN_POINT ( 'NONE',  ( 43.88918661166069768, 14.83350785940550054, -8.216749244412550723 ) ) ;
#8980=CARTESIAN_POINT ( 'NONE',  ( 14.41339629623599983, 20.77357945327109690, -75.79069550273320033 ) ) ;
#8981=EDGE_CURVE ( 'NONE', #2493, #19930, #33003, .T. ) ;
#8983=( BOUNDED_CURVE ( )  B_SPLINE_CURVE ( 3, ( #28742, #3627, #23767, #48414 ),
 .UNSPECIFIED., .F., .T. ) 
 B_SPLINE_CURVE_WITH_KNOTS ( ( 4, 4 ),
 ( 0.5134355670272889860, 0.7048181067645971076 ),
 .UNSPECIFIED. ) 
 CURVE ( )  GEOMETRIC_REPRESENTATION_ITEM ( )  RATIONAL_B_SPLINE_CURVE ( ( 1.000000000000000000, 0.9969500553388705999, 0.9969500553388705999, 1.000000000000000000 ) ) 
 REPRESENTATION_ITEM ( '' )  );
#8984=CARTESIAN_POINT ( 'NONE',  ( 83.84453551654038961, -44.32823745891949585, -46.66649649553739465 ) ) ;
#8986=EDGE_LOOP ( 'NONE', ( #32532, #24712, #19269, #37119 ) ) ;
#8987=CARTESIAN_POINT ( 'NONE',  ( 53.59970586858850083, -48.90735548451660009, -27.06398614015060033 ) ) ;
#8991=CARTESIAN_POINT ( 'NONE',  ( 74.93037295002240228, -43.11618894467930119, -15.31098073120859837 ) ) ;
#8993=VERTEX_POINT ( 'NONE', #26501 ) ;
#8994=CARTESIAN_POINT ( 'NONE',  ( -3.355680836222830088, -48.40293006637049444, -5.033607157952709521 ) ) ;
#8995=CARTESIAN_POINT ( 'NONE',  ( 47.44871638918419876, 23.38584436733959748, -54.69912089980569903 ) ) ;
#9000=CARTESIAN_POINT ( 'NONE',  ( 11.36506040363580006, 34.06329960752539421, -17.70888297486289886 ) ) ;
#9005=CARTESIAN_POINT ( 'NONE',  ( 58.40527474631630156, -46.88335097056240386, -48.04018388860429667 ) ) ;
#9006=CARTESIAN_POINT ( 'NONE',  ( 52.95539585931859961, 18.32046256209179802, -27.75247797855960030 ) ) ;
#9007=CARTESIAN_POINT ( 'NONE',  ( 17.52353788780599686, -52.44145270522049884, -76.03823174343609992 ) ) ;
#9013=CARTESIAN_POINT ( 'NONE',  ( 8.957196496706650635, 31.92430757304470035, -46.63362000866580104 ) ) ;
#9014=CARTESIAN_POINT ( 'NONE',  ( 57.77564497937559906, 0.4193449612534105309, -17.11446609406728570 ) ) ;
#9015=ORIENTED_EDGE ( 'NONE', *, *, #19161, .T. ) ;
#9016=CARTESIAN_POINT ( 'NONE',  ( 18.34433777603829796, 20.57110240350969832, -75.40982873507010709 ) ) ;
#9018=ORIENTED_EDGE ( 'NONE', *, *, #8846, .T. ) ;
#9019=ORIENTED_EDGE ( 'NONE', *, *, #34752, .F. ) ;
#9020=CARTESIAN_POINT ( 'NONE',  ( 12.82504919487779915, -65.50308766827649265, -47.62518768686640414 ) ) ;
#9021=CARTESIAN_POINT ( 'NONE',  ( 57.03244692032389906, -45.51060902889650350, -26.04968356573699850 ) ) ;
#9023=CARTESIAN_POINT ( 'NONE',  ( 61.71737073286530517, 13.89658578540509914, -46.60406873706940445 ) ) ;
#9025=ORIENTED_EDGE ( 'NONE', *, *, #10474, .F. ) ;
#9027=CARTESIAN_POINT ( 'NONE',  ( 11.93810440114173055, 34.20707662183112774, -17.87564879217053004 ) ) ;
#9029=CARTESIAN_POINT ( 'NONE',  ( 46.20925947970359715, -46.13067797581490481, -9.791027853733639930 ) ) ;
#9035=CARTESIAN_POINT ( 'NONE',  ( 46.58330506947539362, -53.42389239804139578, -76.07703971530399656 ) ) ;
#9037=CARTESIAN_POINT ( 'NONE',  ( 50.71554509951779721, 14.96710075306869925, -12.97454429901910089 ) ) ;
#9041=CARTESIAN_POINT ( 'NONE',  ( -8.004967211730480869, 13.73555245088170018, -5.098737574129920347 ) ) ;
#9046=CARTESIAN_POINT ( 'NONE',  ( 58.58074692517319448, 15.55817703255979900, -48.00570932831679727 ) ) ;
#9047=CARTESIAN_POINT ( 'NONE',  ( -8.770054618657720624, -44.34737232867720280, -5.608366899511570303 ) ) ;
#9048=CARTESIAN_POINT ( 'NONE',  ( 11.13393739769619906, 32.28996932331859426, -43.76018303691880362 ) ) ;
#9050=CARTESIAN_POINT ( 'NONE',  ( 11.97330428934050062, -64.78167623425329680, -16.08313759591939984 ) ) ;
#9052=CARTESIAN_POINT ( 'NONE',  ( 46.36969429687169963, 21.71676565170959705, -76.14999999999999147 ) ) ;
#9054=CARTESIAN_POINT ( 'NONE',  ( 49.43871793799859660, -53.66383539453889284, -54.54809130707169373 ) ) ;
#9055=CARTESIAN_POINT ( 'NONE',  ( 41.40756764072759921, -44.77159127043780273, -5.393983506378570603 ) ) ;
#9060=VERTEX_POINT ( 'NONE', #23200 ) ;
#9064=CARTESIAN_POINT ( 'NONE',  ( 83.71507600481126588, -44.45672478866849531, -46.59591550923387615 ) ) ;
#9065=CARTESIAN_POINT ( 'NONE',  ( 60.34379256561119576, -45.86802437250690190, -47.72732608210890248 ) ) ;
#9066=LINE ( 'NONE', #20317, #36273 ) ;
#9067=AXIS2_PLACEMENT_3D ( 'NONE', #3874, #12248, #24007 ) ;
#9068=CARTESIAN_POINT ( 'NONE',  ( 61.70641836169023264, 13.92968577895933535, -46.86525494990149099 ) ) ;
#9074=CARTESIAN_POINT ( 'NONE',  ( 84.22529662124048855, -44.14854820750499442, -47.36165834067109870 ) ) ;
#9077=ORIENTED_EDGE ( 'NONE', *, *, #11428, .F. ) ;
#9078=CARTESIAN_POINT ( 'NONE',  ( 61.52539987384010089, -45.35174871025959931, -47.31480267961979536 ) ) ;
#9079=CARTESIAN_POINT ( 'NONE',  ( 52.62660330590350100, -49.81109310332840323, -48.67237100752149814 ) ) ;
#9080=CARTESIAN_POINT ( 'NONE',  ( 52.66500433930978176, -50.10310259146618961, -77.26040935214849981 ) ) ;
#9081=CARTESIAN_POINT ( 'NONE',  ( 76.39890521214071839, -19.26305209071983526, -12.79182930615482050 ) ) ;
#9082=CARTESIAN_POINT ( 'NONE',  ( 56.55536805559270164, -50.73789114322060101, -53.84226117436379866 ) ) ;
#9083=ORIENTED_EDGE ( 'NONE', *, *, #4655, .T. ) ;
#9085=CARTESIAN_POINT ( 'NONE',  ( 11.64494012201000039, 34.15031286627577600, -22.50329527685726561 ) ) ;
#9086=CARTESIAN_POINT ( 'NONE',  ( 56.55337564908950299, 19.27319311912070177, -52.91477395641850734 ) ) ;
#9088=CARTESIAN_POINT ( 'NONE',  ( 14.02678725144039973, -50.30560580096022960, -20.88317649143804644 ) ) ;
#9089=CARTESIAN_POINT ( 'NONE',  ( 8.799470649396189614, -63.19223985362448559, -46.67016919464409597 ) ) ;
#9090=CARTESIAN_POINT ( 'NONE',  ( 51.84382619997980157, -49.26715712592199736, -77.06468978676770121 ) ) ;
#9091=ORIENTED_EDGE ( 'NONE', *, *, #27469, .T. ) ;
#9096=CARTESIAN_POINT ( 'NONE',  ( 13.39998208309999939, 20.55440457967890211, -76.14999999999999147 ) ) ;
#9098=CYLINDRICAL_SURFACE ( 'NONE', #4572, 3.500000000000003109 ) ;
#9099=EDGE_CURVE ( 'NONE', #23745, #19697, #27406, .T. ) ;
#9100=CARTESIAN_POINT ( 'NONE',  ( 42.52205267802430200, -43.49267883201609664, -4.456987777804809703 ) ) ;
#9104=EDGE_CURVE ( 'NONE', #34463, #47835, #41599, .T. ) ;
#9107=FACE_OUTER_BOUND ( 'NONE', #5101, .T. ) ;
#9108=CARTESIAN_POINT ( 'NONE',  ( 67.25971769855989635, -0.6780106752988179775, -17.44087497863319669 ) ) ;
#9109=ORIENTED_EDGE ( 'NONE', *, *, #23738, .T. ) ;
#9110=CARTESIAN_POINT ( 'NONE',  ( 13.79823471886849973, -51.65733818268109445, -75.17186369577468952 ) ) ;
#9111=CARTESIAN_POINT ( 'NONE',  ( 47.21517444068279445, -54.78196946262829670, -54.62462293534060365 ) ) ;
#9116=LINE ( 'NONE', #12530, #11371 ) ;
#9117=CARTESIAN_POINT ( 'NONE',  ( 10.81643727141089961, 33.72113552640900025, -17.63284883033089656 ) ) ;
#9118=CARTESIAN_POINT ( 'NONE',  ( 13.97461707263510178, 19.95444906609850122, -22.92155396671540046 ) ) ;
#9120=CARTESIAN_POINT ( 'NONE',  ( 56.42218940953110007, 19.53148004655350078, -53.51231675409619726 ) ) ;
#9122=CARTESIAN_POINT ( 'NONE',  ( 48.46328056021759778, 22.91827103051950232, -54.95887287608610450 ) ) ;
#9123=ORIENTED_EDGE ( 'NONE', *, *, #20614, .F. ) ;
#9126=AXIS2_PLACEMENT_3D ( 'NONE', #15733, #11038, #43015 ) ;
#9130=CARTESIAN_POINT ( 'NONE',  ( 84.37646258656080533, 12.22652691366610078, -47.26568110888489826 ) ) ;
#9131=CARTESIAN_POINT ( 'NONE',  ( 53.25483989353620018, 17.95639845396440393, -27.17232069770570035 ) ) ;
#9133=CARTESIAN_POINT ( 'NONE',  ( 12.36320305029179956, 33.31445045633500257, -15.76422791923680045 ) ) ;
#9135=CARTESIAN_POINT ( 'NONE',  ( 16.15069456443260520, -51.05177125324679110, -17.90311212357429937 ) ) ;
#9138=CARTESIAN_POINT ( 'NONE',  ( 11.41271396217149992, -64.98654470182599141, -16.69425700586020156 ) ) ;
#9139=CARTESIAN_POINT ( 'NONE',  ( 11.31321705866109895, 33.19720110168429272, -44.95199481682620046 ) ) ;
#9140=CARTESIAN_POINT ( 'NONE',  ( 61.25724218321475689, -45.31063123919039981, -47.12446599951652360 ) ) ;
#9142=CARTESIAN_POINT ( 'NONE',  ( 50.13069710666830048, -52.30340857919710373, -51.78329334912879744 ) ) ;
#9143=CARTESIAN_POINT ( 'NONE',  ( 51.58134972076286573, 2.917345700074899462, -76.88489686019924818 ) ) ;
#9144=CIRCLE ( 'NONE', #51821, 32.00000000000000000 ) ;
#9149=CARTESIAN_POINT ( 'NONE',  ( 57.16896213477740218, 14.61892080237120162, -26.25490629759670114 ) ) ;
#9151=DIRECTION ( 'NONE',  ( 0.000000000000000000, 0.000000000000000000, 1.000000000000000000 ) ) ;
#9153=CARTESIAN_POINT ( 'NONE',  ( 50.95182855010879308, -50.95090509061829209, -76.14999999999999147 ) ) ;
#9154=DIRECTION ( 'NONE',  ( 0.000000000000000000, 0.000000000000000000, 1.000000000000000000 ) ) ;
#9155=EDGE_LOOP ( 'NONE', ( #4134, #35873, #17709, #5024 ) ) ;
#9158=CARTESIAN_POINT ( 'NONE',  ( 12.68691374172937003, -55.46739277041032068, -75.51638835765626823 ) ) ;
#9159=CARTESIAN_POINT ( 'NONE',  ( 16.13393739769620083, -15.61618894467929941, -11.05000000000000071 ) ) ;
#9162=CARTESIAN_POINT ( 'NONE',  ( 56.13201255944740353, 19.60900434519550117, -74.69880780947919163 ) ) ;
#9164=CARTESIAN_POINT ( 'NONE',  ( 46.91625109622430045, -53.80736403542660184, -75.86076060431129520 ) ) ;
#9165=ORIENTED_EDGE ( 'NONE', *, *, #30558, .F. ) ;
#9166=CARTESIAN_POINT ( 'NONE',  ( 55.11318621343720281, 14.43546311050189956, -15.75535627857289889 ) ) ;
#9167=ADVANCED_FACE ( 'NONE', ( #44952 ), #13837, .T. ) ;
#9169=CARTESIAN_POINT ( 'NONE',  ( 52.56799448115409490, -49.85882480688869833, -48.49336018736870102 ) ) ;
#9171=CARTESIAN_POINT ( 'NONE',  ( 12.29386161020425838, 34.10498507263372403, -23.62058203229901210 ) ) ;
#9173=ORIENTED_EDGE ( 'NONE', *, *, #11027, .F. ) ;
#9174=CARTESIAN_POINT ( 'NONE',  ( 47.40872200122030478, 23.22827899685340114, -74.94663380581118872 ) ) ;
#9177=CARTESIAN_POINT ( 'NONE',  ( 60.23130391297029718, 14.55066440145539985, -47.24246919202519734 ) ) ;
#9179=CARTESIAN_POINT ( 'NONE',  ( 12.28455908802819962, 33.49872389401299699, -15.95890976725140220 ) ) ;
#9183=TOROIDAL_SURFACE ( 'NONE', #37594, 17.39999999999999858, 3.799999999999999822 ) ;
#9187=CARTESIAN_POINT ( 'NONE',  ( 66.63393739769620083, 6.883811055320649963, -71.50000000000000000 ) ) ;
#9189=CARTESIAN_POINT ( 'NONE',  ( 61.20155191191109623, 14.04232429033380036, -46.66714648058599835 ) ) ;
#9191=CARTESIAN_POINT ( 'NONE',  ( 6.188526101445139815, -63.88644423068799938, -47.34841622259269656 ) ) ;
#9193=CARTESIAN_POINT ( 'NONE',  ( 52.90392158692600333, -49.62416384515039880, -48.79551526944879924 ) ) ;
#9194=CARTESIAN_POINT ( 'NONE',  ( 57.72833049119049775, -45.13003903922449211, -25.57691600686959887 ) ) ;
#9196=CARTESIAN_POINT ( 'NONE',  ( 57.40895152886420050, 14.37846127530180063, -26.19991503117499931 ) ) ;
#9198=CARTESIAN_POINT ( 'NONE',  ( 50.57758487413249782, 18.62004947392870235, -76.16361833584198848 ) ) ;
#9199=CARTESIAN_POINT ( 'NONE',  ( 52.81564606049040123, 18.44441551310690031, -48.78617137558140371 ) ) ;
#9201=DIRECTION ( 'NONE',  ( 0.000000000000000000, 0.000000000000000000, -1.000000000000000000 ) ) ;
#9203=VERTEX_POINT ( 'NONE', #23514 ) ;
#9207=CARTESIAN_POINT ( 'NONE',  ( 47.39224450036900294, -54.66215068426350143, -54.83956910525469652 ) ) ;
#9210=CARTESIAN_POINT ( 'NONE',  ( 60.71152220950099831, -30.57213475406030057, -16.28960219260079967 ) ) ;
#9211=CARTESIAN_POINT ( 'NONE',  ( 53.18486760013709613, 18.24248981343010101, -48.80133335483819934 ) ) ;
#9214=EDGE_CURVE ( 'NONE', #9489, #45513, #35848, .T. ) ;
#9215=CARTESIAN_POINT ( 'NONE',  ( 78.22251691734010137, 1.883811055320649963, -20.65000000000000213 ) ) ;
#9217=ORIENTED_EDGE ( 'NONE', *, *, #25699, .F. ) ;
#9218=EDGE_CURVE ( 'NONE', #18453, #51359, #1609, .T. ) ;
#9219=ORIENTED_EDGE ( 'NONE', *, *, #4580, .F. ) ;
#9220=CARTESIAN_POINT ( 'NONE',  ( 9.287874463674199887, -63.21240253717019897, -46.53018408198249745 ) ) ;
#9222=ORIENTED_EDGE ( 'NONE', *, *, #35321, .T. ) ;
#9227=CARTESIAN_POINT ( 'NONE',  ( 52.51047226760390174, 19.75004459190430239, -76.15156771798700674 ) ) ;
#9230=LINE ( 'NONE', #32772, #5069 ) ;
#9235=B_SPLINE_SURFACE_WITH_KNOTS ( 'NONE', 3, 3, ( 
 ( #9680, #25640, #14125, #45065, #49528, #21197 ),
 ( #25383, #30090, #45848, #33253, #36940, #13118 ),
 ( #49269, #41909, #1814, #46116, #4973, #25124 ),
 ( #40871, #41133, #45586, #37456, #9434, #21707 ),
 ( #29069, #13364, #5244, #1555, #13619, #1041 ),
 ( #37716, #10201, #18056, #2077, #29582, #21457 ),
 ( #9934, #20943, #17035, #37203, #1302, #41642 ),
 ( #33515, #17292, #25896, #37980, #6009, #29328 ),
 ( #41384, #32987, #5751, #5501, #17795, #17543 ),
 ( #33768, #49779, #13872, #29828, #46375, #10717 ),
 ( #10980, #14897, #26945, #19343, #23251, #2329 ),
 ( #6271, #31376, #35327, #31122, #6525, #26673 ),
 ( #34546, #22487, #51326, #47403, #14385, #42695 ),
 ( #38237, #7301, #42951, #46892, #7049, #15424 ),
 ( #34804, #38493, #22228, #6790, #26160, #47147 ),
 ( #18304, #50297, #43210, #50550, #27197, #39020 ) ),
 .UNSPECIFIED., .F., .F., .F.,
 ( 4, 2, 2, 2, 2, 2, 2, 4 ),
 ( 4, 1, 1, 4 ),
 ( -1.480557284018800157, -1.467872963798670050, -1.112024972574749970, -0.8896199780598010864, -0.7784174808023259784, -0.6004934851903659387, -0.3158150922112299974, 0.000000000000000000 ),
 ( 0.000000000000000000, 0.3333333333333329818, 0.6666666666666670737, 1.000000000000000000 ),
 .UNSPECIFIED. ) ;
#9237=DIRECTION ( 'NONE',  ( 0.000000000000000000, 0.000000000000000000, -1.000000000000000000 ) ) ;
#9238=CARTESIAN_POINT ( 'NONE',  ( 53.70553476669380188, 20.08271752784780162, -75.56421356237311215 ) ) ;
#9240=ADVANCED_FACE ( 'NONE', ( #51068 ), #22193, .T. ) ;
#9241=CARTESIAN_POINT ( 'NONE',  ( 60.34379258661509482, -45.86802437805019395, -47.72732609191810127 ) ) ;
#9243=CARTESIAN_POINT ( 'NONE',  ( 52.60295254337719939, -49.82768164818060086, -48.60889610034470110 ) ) ;
#9245=EDGE_CURVE ( 'NONE', #9812, #43378, #35533, .T. ) ;
#9247=CARTESIAN_POINT ( 'NONE',  ( 14.91464035002509902, 21.52412519331699770, -76.12563501418100032 ) ) ;
#9252=CARTESIAN_POINT ( 'NONE',  ( 52.83716997623850631, -49.57025241744720745, -27.30068420219360092 ) ) ;
#9253=CARTESIAN_POINT ( 'NONE',  ( 53.97741451551910075, -51.26237320098420014, -75.50474183165199804 ) ) ;
#9259=CARTESIAN_POINT ( 'NONE',  ( -3.304781330980080423, -48.28933272873660343, -4.547377290988400489 ) ) ;
#9260=AXIS2_PLACEMENT_3D ( 'NONE', #41686, #42214, #18095 ) ;
#9261=CARTESIAN_POINT ( 'NONE',  ( 47.34367498752779824, 23.45770001724940101, -54.71075737435550224 ) ) ;
#9262=CARTESIAN_POINT ( 'NONE',  ( 56.61928470354429521, -45.32411298099489727, -25.29356197036729981 ) ) ;
#9266=CARTESIAN_POINT ( 'NONE',  ( 43.60412366959330654, 12.47234831688600210, -5.064848484392650008 ) ) ;
#9268=CARTESIAN_POINT ( 'NONE',  ( 53.02240706027900075, 18.32760744209570092, -48.78672998508179859 ) ) ;
#9270=CARTESIAN_POINT ( 'NONE',  ( 57.59002137063620097, -47.30929821719110606, -48.19818069499370239 ) ) ;
#9272=CARTESIAN_POINT ( 'NONE',  ( 56.27101956176600339, 19.34483571430840243, -52.87263781881699032 ) ) ;
#9275=VERTEX_POINT ( 'NONE', #47344 ) ;
#9277=CARTESIAN_POINT ( 'NONE',  ( 9.287340138010449664, 31.97629639357099762, -46.53025760029479585 ) ) ;
#9280=FACE_OUTER_BOUND ( 'NONE', #49974, .T. ) ;
#9281=ORIENTED_EDGE ( 'NONE', *, *, #43243, .T. ) ;
#9282=CARTESIAN_POINT ( 'NONE',  ( 18.36813433944570306, 20.77108261440790216, -75.51240970683930698 ) ) ;
#9285=EDGE_LOOP ( 'NONE', ( #1143, #21624, #17456, #48372, #11063, #22089, #9025, #42191, #27998, #3396, #29930, #38102, #10186 ) ) ;
#9286=DIRECTION ( 'NONE',  ( -0.6209860917175333839, 0.7838215829468996310, 0.000000000000000000 ) ) ;
#9288=CARTESIAN_POINT ( 'NONE',  ( 10.66720212314140070, -63.45534415236151204, -45.40081149022140039 ) ) ;
#9289=CARTESIAN_POINT ( 'NONE',  ( 57.13718842672530229, -45.48243698324539253, -26.05465429760539919 ) ) ;
#9293=CARTESIAN_POINT ( 'NONE',  ( 61.53499251318310570, 13.92503479677660039, -46.68296636261909782 ) ) ;
#9296=CARTESIAN_POINT ( 'NONE',  ( 13.61938558678000000, 20.19483563406610216, -23.15000000000000213 ) ) ;
#9297=EDGE_LOOP ( 'NONE', ( #45236, #3793, #42542, #39459 ) ) ;
#9298=CARTESIAN_POINT ( 'NONE',  ( 46.44332427445870337, -45.55948807132040201, -9.443144690562260024 ) ) ;
#9302=AXIS2_PLACEMENT_3D ( 'NONE', #19433, #47487, #3970 ) ;
#9306=CARTESIAN_POINT ( 'NONE',  ( 47.12094126571430763, -54.61101435440190244, -75.00840848463889188 ) ) ;
#9307=TOROIDAL_SURFACE ( 'NONE', #40962, 24.89999999999999858, 4.000000000000059508 ) ;
#9310=EDGE_CURVE ( 'NONE', #26977, #20243, #35389, .T. ) ;
#9311=CARTESIAN_POINT ( 'NONE',  ( 49.09894036100649828, 14.73025699061659921, -11.67146733142279835 ) ) ;
#9313=CYLINDRICAL_SURFACE ( 'NONE', #39915, 1.999999999999995559 ) ;
#9314=CARTESIAN_POINT ( 'NONE',  ( 10.61751707702059910, 33.59325229219749787, -22.25048313876769868 ) ) ;
#9315=CARTESIAN_POINT ( 'NONE',  ( 61.52376219282579939, 13.89663229014939994, -27.65962565353160230 ) ) ;
#9318=CARTESIAN_POINT ( 'NONE',  ( 59.03492131492150463, 15.32045715074029957, -47.92638814198690511 ) ) ;
#9319=CARTESIAN_POINT ( 'NONE',  ( -11.19057721206939959, -41.98697526176020034, -5.946211766447980551 ) ) ;
#9320=CARTESIAN_POINT ( 'NONE',  ( 76.84281711086150324, -42.03110714784109803, -14.70467750791790174 ) ) ;
#9322=CARTESIAN_POINT ( 'NONE',  ( 11.57186432615189986, -64.94495217133389531, -16.50172565924879819 ) ) ;
#9323=CARTESIAN_POINT ( 'NONE',  ( 57.24929578595760660, -50.61618894467930119, -74.14999999999999147 ) ) ;
#9325=CARTESIAN_POINT ( 'NONE',  ( 49.11893593088550602, -53.90327866102659726, -55.14224250079890055 ) ) ;
#9326=CARTESIAN_POINT ( 'NONE',  ( 51.30165636469427426, -31.84994407807069905, -17.32271793605100285 ) ) ;
#9328=CARTESIAN_POINT ( 'NONE',  ( 18.84361988317459691, -51.80633386256119621, -74.54427505469620030 ) ) ;
#9330=ORIENTED_EDGE ( 'NONE', *, *, #29862, .T. ) ;
#9331=AXIS2_PLACEMENT_3D ( 'NONE', #21992, #38002, #2100 ) ;
#9335=CARTESIAN_POINT ( 'NONE',  ( 83.92831069520973131, -44.23173704228813108, -46.72265495406260527 ) ) ;
#9336=CARTESIAN_POINT ( 'NONE',  ( 60.33694438359599843, -45.85988071783310716, -47.70890968787160347 ) ) ;
#9337=CARTESIAN_POINT ( 'NONE',  ( 57.02861369189989915, 19.39567887795939782, -53.87746547145160037 ) ) ;
#9338=CARTESIAN_POINT ( 'NONE',  ( 50.67689124139599244, 19.37866773268720166, -76.14999999999999147 ) ) ;
#9341=AXIS2_PLACEMENT_3D ( 'NONE', #4435, #4691, #20402 ) ;
#9344=VERTEX_POINT ( 'NONE', #23709 ) ;
#9349=CARTESIAN_POINT ( 'NONE',  ( 61.62977292002289431, -45.12285047192839471, -46.49409185169140102 ) ) ;
#9350=CARTESIAN_POINT ( 'NONE',  ( 53.29384558423090112, 19.31433099946569953, -38.31189016485890875 ) ) ;
#9351=CARTESIAN_POINT ( 'NONE',  ( 53.78771641980449658, -51.63629534268280707, -53.21849989078959453 ) ) ;
#9352=ORIENTED_EDGE ( 'NONE', *, *, #17160, .T. ) ;
#9358=CARTESIAN_POINT ( 'NONE',  ( 54.62261979470819995, -51.56116820793610600, -54.09401641884280565 ) ) ;
#9359=FACE_OUTER_BOUND ( 'NONE', #45226, .T. ) ;
#9361=CARTESIAN_POINT ( 'NONE',  ( 20.44965901189399204, -33.35837913196784399, -75.56421356237308373 ) ) ;
#9362=CARTESIAN_POINT ( 'NONE',  ( 52.53869631642899662, -50.56896709113740229, -76.53474691443801703 ) ) ;
#9366=ADVANCED_FACE ( 'NONE', ( #39980 ), #28819, .T. ) ;
#9369=CARTESIAN_POINT ( 'NONE',  ( 45.55533282443069965, 13.99868975454399944, -8.104371290795420180 ) ) ;
#9370=EDGE_CURVE ( 'NONE', #35625, #12521, #24660, .T. ) ;
#9371=CARTESIAN_POINT ( 'NONE',  ( 43.02291016728809581, -43.89611171023040015, -5.004961222441979274 ) ) ;
#9372=DIRECTION ( 'NONE',  ( 0.000000000000000000, 0.000000000000000000, -1.000000000000000000 ) ) ;
#9373=CARTESIAN_POINT ( 'NONE',  ( 68.38971107296249841, -1.116188944679350037, -18.15384911730639672 ) ) ;
#9379=CARTESIAN_POINT ( 'NONE',  ( 66.62841617083020651, 1.722393603085859981, -19.40721067926959975 ) ) ;
#9381=CARTESIAN_POINT ( 'NONE',  ( 14.03647079426650102, -51.35642126254130346, -74.98719232987430416 ) ) ;
#9382=CARTESIAN_POINT ( 'NONE',  ( 57.34629640291740316, 19.08899856727470379, -52.87029358442639904 ) ) ;
#9386=CARTESIAN_POINT ( 'NONE',  ( 57.50723798014340105, 13.88381064843590096, -25.33268340738889890 ) ) ;
#9387=CARTESIAN_POINT ( 'NONE',  ( 11.80006687032470047, 34.19580789139209998, -17.88619248980069898 ) ) ;
#9388=CARTESIAN_POINT ( 'NONE',  ( 13.92801754073780174, 19.97389345277590067, -22.96894028473249705 ) ) ;
#9389=CARTESIAN_POINT ( 'NONE',  ( 15.82997274079101224, 19.88381105532299387, -21.91305730704999988 ) ) ;
#9391=CARTESIAN_POINT ( 'NONE',  ( 48.57851549001960478, 22.81624679364150055, -54.74774495437689836 ) ) ;
#9394=ORIENTED_EDGE ( 'NONE', *, *, #28430, .T. ) ;
#9395=CARTESIAN_POINT ( 'NONE',  ( 16.13393739769620083, -15.61618894467929941, 7.849999999999999645 ) ) ;
#9397=CYLINDRICAL_SURFACE ( 'NONE', #42985, 1.000000000000001110 ) ;
#9398=CARTESIAN_POINT ( 'NONE',  ( 84.44784216359251161, 11.88381105532070059, -47.47585302082339354 ) ) ;
#9399=CARTESIAN_POINT ( 'NONE',  ( 55.68001326603900480, 15.01258945603300177, -25.63522347839200322 ) ) ;
#9402=CARTESIAN_POINT ( 'NONE',  ( 56.29021670269609956, -45.11618894467940066, -14.97294918829250143 ) ) ;
#9406=EDGE_LOOP ( 'NONE', ( #44022, #21565, #31894, #49331 ) ) ;
#9407=CARTESIAN_POINT ( 'NONE',  ( 11.50001307143430118, -64.98824575801700121, -16.62227806134499986 ) ) ;
#9408=CARTESIAN_POINT ( 'NONE',  ( 12.95715363918909979, 34.28281642642240001, -47.67656520517239471 ) ) ;
#9414=ORIENTED_EDGE ( 'NONE', *, *, #26096, .T. ) ;
#9417=CARTESIAN_POINT ( 'NONE',  ( 47.94498215251270068, 23.43361079511839762, -55.53475709714179942 ) ) ;
#9419=CARTESIAN_POINT ( 'NONE',  ( 50.47459759387780309, -50.28724450852030259, -76.14999999999999147 ) ) ;
#9421=ORIENTED_EDGE ( 'NONE', *, *, #48044, .F. ) ;
#9423=CARTESIAN_POINT ( 'NONE',  ( 65.43042069958036677, 17.98087126524680102, -74.20351669811765305 ) ) ;
#9424=VERTEX_POINT ( 'NONE', #47089 ) ;
#9426=CARTESIAN_POINT ( 'NONE',  ( 45.64502415131030233, -46.12165179014160543, -9.406922201967550023 ) ) ;
#9428=CARTESIAN_POINT ( 'NONE',  ( 13.72898021142920122, -51.28551575856799616, -22.65893573105330105 ) ) ;
#9429=CARTESIAN_POINT ( 'NONE',  ( 54.00166005263069735, 19.61159079012060147, -76.07248000621819983 ) ) ;
#9430=ADVANCED_FACE ( 'NONE', ( #42894 ), #39207, .T. ) ;
#9431=CARTESIAN_POINT ( 'NONE',  ( 47.43599255125010217, -54.63612274721339901, -74.14999999999999147 ) ) ;
#9433=CARTESIAN_POINT ( 'NONE',  ( 54.90608630352579667, 14.46110100129650000, -15.60660465066449909 ) ) ;
#9434=CARTESIAN_POINT ( 'NONE',  ( 57.19702055511909577, -50.61594403054400004, -53.75054411264890319 ) ) ;
#9435=CARTESIAN_POINT ( 'NONE',  ( 52.57286858291280396, -49.85400817756870140, -48.51318051594920178 ) ) ;
#9438=VERTEX_POINT ( 'NONE', #38960 ) ;
#9439=CARTESIAN_POINT ( 'NONE',  ( 46.39504675003949785, 21.75098124655080056, -76.14870548336060097 ) ) ;
#9441=CARTESIAN_POINT ( 'NONE',  ( 75.16123461437827302, -29.48656911042399287, -11.85229885355600565 ) ) ;
#9443=CIRCLE ( 'NONE', #21942, 48.00000000000000000 ) ;
#9444=CARTESIAN_POINT ( 'NONE',  ( 12.36320305067610015, 33.31445045643330616, -15.76422791930239953 ) ) ;
#9449=CARTESIAN_POINT ( 'NONE',  ( 61.16806598196220079, 14.05986850724769965, -46.71992872349159853 ) ) ;
#9450=CARTESIAN_POINT ( 'NONE',  ( -12.74467463197679962, -57.05710031237479996, -53.24963421316559931 ) ) ;
#9452=B_SPLINE_CURVE_WITH_KNOTS ( 'NONE', 3,
 ( #18153, #14996, #34119, #46215, #2423, #34641, #42269, #6366, #38604, #22328, #30964, #27047, #46994, #38334, #7147, #22841, #18408, #6623, #23099, #50646, #34383, #2951, #18921, #30712, #50395, #46734, #39117, #3211, #30452, #10561 ),
 .UNSPECIFIED., .F., .F.,
 ( 4, 2, 2, 2, 2, 2, 2, 2, 2, 2, 2, 2, 2, 2, 4 ),
 ( -1.979714999999999961E-13, 0.09067111850398298922, 0.2140247704412500118, 0.2911208029020420085, 0.3773788185767790737, 0.4312900783734900378, 0.4852013381702010020, 0.5283303460075698954, 0.5714593538449389554, 0.6404657663847290738, 0.6753592001671930856, 0.7102526339496559871, 0.7544412783218740204, 0.8251431093174219633, 0.8625801567471780285 ),
 .UNSPECIFIED. ) ;
#9453=CARTESIAN_POINT ( 'NONE',  ( 53.37783364382759999, -49.37513790283500015, -48.82822306731589634 ) ) ;
#9455=CARTESIAN_POINT ( 'NONE',  ( 57.46922327009529852, -45.13092459265400436, -25.53935936133710172 ) ) ;
#9456=CARTESIAN_POINT ( 'NONE',  ( 47.65668213871590098, -54.52839204276340013, -55.15716614278580465 ) ) ;
#9457=CARTESIAN_POINT ( 'NONE',  ( 56.70381597338830204, 14.06601603320560123, -25.50387274212789634 ) ) ;
#9459=CARTESIAN_POINT ( 'NONE',  ( 50.39461195648269864, 18.90258328430419965, -76.14999999999999147 ) ) ;
#9460=CARTESIAN_POINT ( 'NONE',  ( 53.03535125111080362, 18.33408603822369898, -48.94674794257169737 ) ) ;
#9462=CARTESIAN_POINT ( 'NONE',  ( 60.28107860282390362, -45.75696393620810198, -47.25802466845119909 ) ) ;
#9463=CARTESIAN_POINT ( 'NONE',  ( 71.85433366084710372, -45.11618894467940066, -14.09557305447640019 ) ) ;
#9466=ADVANCED_FACE ( 'NONE', ( #19022 ), #41011, .T. ) ;
#9469=CARTESIAN_POINT ( 'NONE',  ( 47.51629483024640166, -54.56948809585979632, -54.66793506916069845 ) ) ;
#9470=CARTESIAN_POINT ( 'NONE',  ( 61.75019796695539753, 14.88381105532069881, -28.15000000000000213 ) ) ;
#9472=CARTESIAN_POINT ( 'NONE',  ( 60.69770788394099981, 14.26247553725569972, -47.37008640455089648 ) ) ;
#9478=ADVANCED_FACE ( 'NONE', ( #12724 ), #34698, .T. ) ;
#9480=ORIENTED_EDGE ( 'NONE', *, *, #40847, .T. ) ;
#9481=CARTESIAN_POINT ( 'NONE',  ( 9.744582219142259305, -63.29038400323761238, -46.29748084500919703 ) ) ;
#9482=DIRECTION ( 'NONE',  ( 1.000000000000000000, 0.000000000000000000, 0.000000000000000000 ) ) ;
#9483=ORIENTED_EDGE ( 'NONE', *, *, #24609, .T. ) ;
#9484=CARTESIAN_POINT ( 'NONE',  ( 11.13393739769479929, -63.52234716422830729, -43.76018014099159359 ) ) ;
#9485=DIRECTION ( 'NONE',  ( 0.8320502943378423888, -5.155044000000003308E-14, -0.5547001962252312568 ) ) ;
#9487=CARTESIAN_POINT ( 'NONE',  ( 52.81902780364940497, 19.43027145643710085, -76.50043241533330729 ) ) ;
#9488=CIRCLE ( 'NONE', #35423, 1.999999999999998224 ) ;
#9489=VERTEX_POINT ( 'NONE', #24993 ) ;
#9490=AXIS2_PLACEMENT_3D ( 'NONE', #50736, #6205, #31057 ) ;
#9495=CARTESIAN_POINT ( 'NONE',  ( -23.86606260230380272, -15.61618894467908092, -48.64999999999999858 ) ) ;
#9498=VERTEX_POINT ( 'NONE', #16381 ) ;
#9499=CARTESIAN_POINT ( 'NONE',  ( 57.34776334542480214, -45.81180625069929846, -26.27178910182970029 ) ) ;
#9503=CARTESIAN_POINT ( 'NONE',  ( 13.42153893133809994, 20.57176844745109889, -74.52171359303420672 ) ) ;
#9505=CARTESIAN_POINT ( 'NONE',  ( 82.46791274550251671, -45.09332969728169616, -46.45744338702549925 ) ) ;
#9508=ORIENTED_EDGE ( 'NONE', *, *, #20873, .T. ) ;
#9509=CARTESIAN_POINT ( 'NONE',  ( 54.36039143410459928, -47.84659789142740038, -25.99973999818690018 ) ) ;
#9511=CARTESIAN_POINT ( 'NONE',  ( 7.094823580868710344, 28.68663061054669683, -12.04540313013450081 ) ) ;
#9513=CARTESIAN_POINT ( 'NONE',  ( 10.61751707702059910, -64.82563018155620682, -22.25048313876769868 ) ) ;
#9517=CARTESIAN_POINT ( 'NONE',  ( -7.614741595775099903, -45.32579099379800169, -5.329995886356219792 ) ) ;
#9519=CARTESIAN_POINT ( 'NONE',  ( 47.45990050842959818, 23.38532434082769740, -54.77936059081219611 ) ) ;
#9522=FACE_OUTER_BOUND ( 'NONE', #20569, .T. ) ;
#9523=CARTESIAN_POINT ( 'NONE',  ( 11.10018436985160051, 33.80960200586510211, -17.19464589430749868 ) ) ;
#9525=CARTESIAN_POINT ( 'NONE',  ( 52.94585586128479093, 18.36771476006709847, -48.75076952771310346 ) ) ;
#9527=CARTESIAN_POINT ( 'NONE',  ( 58.73840381835399427, -46.66147107097890512, -47.90022353259229249 ) ) ;
#9529=CARTESIAN_POINT ( 'NONE',  ( 52.59105628395929699, 20.91324755812640035, -53.43271834460720271 ) ) ;
#9532=ORIENTED_EDGE ( 'NONE', *, *, #11168, .T. ) ;
#9534=CARTESIAN_POINT ( 'NONE',  ( 8.959210788195541397, 31.93568363525710296, -46.63329613156509623 ) ) ;
#9536=CARTESIAN_POINT ( 'NONE',  ( 67.94623181482140239, -30.09959995773170149, -17.85819628216900057 ) ) ;
#9538=CARTESIAN_POINT ( 'NONE',  ( 17.93516875359370388, 20.31584378320569684, -75.38352342698830455 ) ) ;
#9540=VERTEX_POINT ( 'NONE', #50434 ) ;
#9543=CARTESIAN_POINT ( 'NONE',  ( 10.41833236504899851, -64.35094718373520095, -46.41941406982350316 ) ) ;
#9544=CARTESIAN_POINT ( 'NONE',  ( 56.67773033073410005, -45.66254785057299870, -26.04367575654990219 ) ) ;
#9547=CARTESIAN_POINT ( 'NONE',  ( 61.40746854249709941, 14.07231923713010069, -47.19815667451499763 ) ) ;
#9551=EDGE_LOOP ( 'NONE', ( #7594, #18130, #24053, #5523, #32250, #25099 ) ) ;
#9552=CARTESIAN_POINT ( 'NONE',  ( 50.44925730351350524, -45.58854146516910077, -12.26883546960940130 ) ) ;
#9554=FACE_OUTER_BOUND ( 'NONE', #1362, .T. ) ;
#9555=ORIENTED_EDGE ( 'NONE', *, *, #51762, .T. ) ;
#9557=CARTESIAN_POINT ( 'NONE',  ( 46.57724752952230318, -53.42760099267549379, -76.07728942632040514 ) ) ;
#9558=CARTESIAN_POINT ( 'NONE',  ( 61.13405154998650204, 14.40638383414069956, -47.71032547765840093 ) ) ;
#9559=CARTESIAN_POINT ( 'NONE',  ( 48.87615309687829779, 13.88381105525199999, -9.792211629500439329 ) ) ;
#9560=CARTESIAN_POINT ( 'NONE',  ( 20.13393739768869750, 24.18330853958710236, -76.14999999999999147 ) ) ;
#9561=CARTESIAN_POINT ( 'NONE',  ( -1.733483264138872437, -50.41034150931718472, -6.209623304567350566 ) ) ;
#9562=CARTESIAN_POINT ( 'NONE',  ( 58.48388423183219942, 13.89519089340790181, -25.73063636213230154 ) ) ;
#9563=EDGE_CURVE ( 'NONE', #22762, #16412, #7928, .T. ) ;
#9569=CARTESIAN_POINT ( 'NONE',  ( 76.80638706214371325, -40.88990971753789694, -14.54769496735189982 ) ) ;
#9571=EDGE_CURVE ( 'NONE', #38625, #26843, #46253, .T. ) ;
#9572=CARTESIAN_POINT ( 'NONE',  ( 10.85466640530910176, -64.96697012893029921, -17.55961383758990024 ) ) ;
#9575=CARTESIAN_POINT ( 'NONE',  ( 49.07734691198550081, -53.89406825560470082, -54.92337139623040088 ) ) ;
#9576=CARTESIAN_POINT ( 'NONE',  ( 42.35079386031210191, -44.32234244509449894, -5.113119501825009294 ) ) ;
#9577=AXIS2_PLACEMENT_3D ( 'NONE', #14937, #30391, #43253 ) ;
#9579=CARTESIAN_POINT ( 'NONE',  ( 18.78671361505629633, -51.59709463796549755, -74.36013246830410139 ) ) ;
#9580=CARTESIAN_POINT ( 'NONE',  ( 13.89790909569722643, -39.31946990788019747, -75.56421356237308373 ) ) ;
#9581=VERTEX_POINT ( 'NONE', #5642 ) ;
#9586=CARTESIAN_POINT ( 'NONE',  ( 60.59128431671459936, -45.75012338594650174, -47.69436703140129907 ) ) ;
#9591=CARTESIAN_POINT ( 'NONE',  ( 51.19516171219699885, -51.09621740586149485, -76.13919816896859061 ) ) ;
#9592=FACE_OUTER_BOUND ( 'NONE', #34127, .T. ) ;
#9594=ORIENTED_EDGE ( 'NONE', *, *, #359, .T. ) ;
#9596=VERTEX_POINT ( 'NONE', #6411 ) ;
#9598=CARTESIAN_POINT ( 'NONE',  ( 61.05611720366390216, -45.35089833204299481, -46.88541463101370255 ) ) ;
#9599=CARTESIAN_POINT ( 'NONE',  ( 52.95029351598290646, -49.64428300453829479, -49.05315204363950699 ) ) ;
#9600=CARTESIAN_POINT ( 'NONE',  ( 66.70013194292150160, -29.76883965895079953, -17.02746303015019791 ) ) ;
#9602=CARTESIAN_POINT ( 'NONE',  ( 53.88967637140569877, -51.75719455529880264, -53.52284543613809831 ) ) ;
#9603=VERTEX_POINT ( 'NONE', #29970 ) ;
#9610=VERTEX_POINT ( 'NONE', #33904 ) ;
#9611=CARTESIAN_POINT ( 'NONE',  ( 15.82777515116789679, 19.71296418728957889, -15.66098702019284516 ) ) ;
#9612=CARTESIAN_POINT ( 'NONE',  ( 52.30891884663609659, -50.47057820349319712, -76.54990093660988748 ) ) ;
#9613=CARTESIAN_POINT ( 'NONE',  ( 60.89998638923590590, 14.20032291693460103, -46.98170749212670216 ) ) ;
#9615=DIRECTION ( 'NONE',  ( 0.3294064756440921449, -0.9441882088883224444, 0.000000000000000000 ) ) ;
#9616=CARTESIAN_POINT ( 'NONE',  ( 42.44160469162459748, 13.71702471974399984, -5.942261413879579734 ) ) ;
#9617=CARTESIAN_POINT ( 'NONE',  ( 41.87064575245250353, -44.48858809718330320, -5.149961107190939913 ) ) ;
#9622=CARTESIAN_POINT ( 'NONE',  ( 66.37093321642988997, -0.5958227600134150537, -16.96665182656099802 ) ) ;
#9624=CARTESIAN_POINT ( 'NONE',  ( 14.98352178517470001, -52.93377250084219554, -76.14999999999999147 ) ) ;
#9631=DIRECTION ( 'NONE',  ( -0.6653150774946530177, -0.7465626883646704348, 0.000000000000000000 ) ) ;
#9632=VECTOR ( 'NONE', #44736, 1000.000000000000000 ) ;
#9635=CARTESIAN_POINT ( 'NONE',  ( 48.19073678848020137, 23.05382179323920155, -55.06660192028969902 ) ) ;
#9636=ORIENTED_EDGE ( 'NONE', *, *, #36590, .T. ) ;
#9638=ORIENTED_EDGE ( 'NONE', *, *, #10592, .T. ) ;
#9639=CARTESIAN_POINT ( 'NONE',  ( 82.75389768041466709, 14.36255265567944406, -47.67226356402779430 ) ) ;
#9640=CARTESIAN_POINT ( 'NONE',  ( 60.14148612135956284, -47.18849741077894322, -49.41070014483602080 ) ) ;
#9642=CARTESIAN_POINT ( 'NONE',  ( 82.57306898050261168, 13.95576942188810143, -46.98632580443239704 ) ) ;
#9643=CARTESIAN_POINT ( 'NONE',  ( 55.48825172393549821, 15.25629303179229979, -25.68709965441729892 ) ) ;
#9645=CARTESIAN_POINT ( 'NONE',  ( 11.57186432615972471, 33.71257428197281314, -16.50172565923971035 ) ) ;
#9649=B_SPLINE_SURFACE_WITH_KNOTS ( 'NONE', 3, 3, ( 
 ( #393, #39977, #32079, #48621, #31827, #24732, #15870, #32335, #36033, #20549, #12720, #8781, #48097, #47843 ),
 ( #20813, #24472, #12196, #28157, #44942, #912, #5121, #16908, #51768, #40484, #36282, #48355, #12448, #21073 ),
 ( #11949, #36544, #27904, #43908, #8002, #44160, #28418, #8257, #24208, #23954, #4576, #650, #16633, #37583 ),
 ( #5884, #49912, #33901, #1437, #17169, #38115, #29966, #45721, #5374, #21329, #30233, #14007, #42307, #2211 ),
 ( #9821, #5639, #25515, #49665, #6407, #17422, #33121, #21850, #37077, #29196, #17930, #46250, #37857, #21585 ),
 ( #10339, #37336, #45985, #33388, #49406, #22104, #10077, #13503, #41520, #1173, #9315, #13753, #45464, #41264 ),
 ( #29459, #25259, #18188, #9562, #49150, #14265, #13246, #1692, #45203, #17678, #33646, #34154, #29709, #1953 ),
 ( #42046, #25773, #50168, #26036, #26297, #41780, #6149, #22625, #47284, #27083, #50680, #23384, #35203, #47029 ),
 ( #43343, #11375, #30488, #38898, #43087, #51206, #34939, #34679, #35467, #7179, #15034, #31002, #34420, #2462 ) ),
 .UNSPECIFIED., .F., .F., .F.,
 ( 4, 1, 1, 1, 1, 1, 4 ),
 ( 4, 2, 2, 2, 2, 2, 4 ),
 ( -0.0005599991503559129851, 0.1666666666666670182, 0.3333333333333329818, 0.5000000000000000000, 0.6666666666666670737, 0.8333333333333330373, 1.000498765355949837 ),
 ( -1.222991916297710091, -1.090716821865840069, -0.9543772191326050924, -0.7362338547594379223, -0.4169048829278029777, -0.06920342394185401147, 0.0005257736236440000441 ),
 .UNSPECIFIED. ) ;
#9651=ORIENTED_EDGE ( 'NONE', *, *, #38361, .F. ) ;
#9653=VERTEX_POINT ( 'NONE', #45988 ) ;
#9654=CARTESIAN_POINT ( 'NONE',  ( 12.05299951489469912, -65.27260376066310243, -16.91217736885799994 ) ) ;
#9655=CARTESIAN_POINT ( 'NONE',  ( 12.47552258722870100, 34.20483690453190206, -47.26471363895340261 ) ) ;
#9657=CARTESIAN_POINT ( 'NONE',  ( 17.92370450339619836, 19.88381105532299742, -74.14999999999999147 ) ) ;
#9658=CARTESIAN_POINT ( 'NONE',  ( 50.97614579714448979, 4.031109038251211807, -76.38790111114094827 ) ) ;
#9661=CARTESIAN_POINT ( 'NONE',  ( 49.10028735341099804, 22.39587775051610308, -54.20564384830549898 ) ) ;
#9662=CARTESIAN_POINT ( 'NONE',  ( 59.33862398020649920, -2.694272193572899710, -15.68334875206189949 ) ) ;
#9663=CARTESIAN_POINT ( 'NONE',  ( 51.38507923684370127, -50.52849113110060131, -76.23533798706770881 ) ) ;
#9665=ORIENTED_EDGE ( 'NONE', *, *, #9685, .T. ) ;
#9666=DIRECTION ( 'NONE',  ( 0.000000000000000000, 0.000000000000000000, 1.000000000000000000 ) ) ;
#9667=CARTESIAN_POINT ( 'NONE',  ( 70.03247032090601465, 18.72622661238169783, -73.39853292320987066 ) ) ;
#9670=DIRECTION ( 'NONE',  ( 0.000000000000000000, 0.000000000000000000, 1.000000000000000000 ) ) ;
#9673=VECTOR ( 'NONE', #266, 1000.000000000000000 ) ;
#9674=CARTESIAN_POINT ( 'NONE',  ( 13.81676756077919954, -51.22923098943019937, -22.59431933179259744 ) ) ;
#9675=CARTESIAN_POINT ( 'NONE',  ( 55.47166349443130429, 19.51716785246549790, -75.55743771978688983 ) ) ;
#9676=CARTESIAN_POINT ( 'NONE',  ( 47.62441105329040170, -54.51319350303420208, -74.50474471063260751 ) ) ;
#9677=EDGE_LOOP ( 'NONE', ( #50660, #4391, #47407, #37236, #2350, #5404, #31482, #6795, #17655, #10276, #25627, #18586 ) ) ;
#9678=CARTESIAN_POINT ( 'NONE',  ( 56.40317685213560139, 14.15597851795049955, -17.20359917593829735 ) ) ;
#9680=CARTESIAN_POINT ( 'NONE',  ( 57.36123083241410114, -50.13537925600150658, -52.61896061011599812 ) ) ;
#9681=CARTESIAN_POINT ( 'NONE',  ( 52.62724176572390178, -49.81047453036210015, -48.67212384193049957 ) ) ;
#9684=CARTESIAN_POINT ( 'NONE',  ( 46.56240039978320056, 22.04143744298989915, -76.11243514202939764 ) ) ;
#9685=EDGE_CURVE ( 'NONE', #43315, #5274, #17681, .T. ) ;
#9688=CARTESIAN_POINT ( 'NONE',  ( 75.15439417744582329, -29.05685264498805864, -11.81924130454197552 ) ) ;
#9690=DIRECTION ( 'NONE',  ( 0.000000000000000000, -1.000000000000000000, 0.000000000000000000 ) ) ;
#9692=AXIS2_PLACEMENT_3D ( 'NONE', #38061, #50888, #11061 ) ;
#9694=CARTESIAN_POINT ( 'NONE',  ( 60.26929283095191892, -45.78778679473056457, -47.49574889169480940 ) ) ;
#9697=CARTESIAN_POINT ( 'NONE',  ( 61.29115875527060098, 13.99537663710240132, -46.49544470360039838 ) ) ;
#9698=CARTESIAN_POINT ( 'NONE',  ( -26.88697088543599989, 10.64579088486830116, -56.26659592162459944 ) ) ;
#9700=CARTESIAN_POINT ( 'NONE',  ( 52.94386163188770666, -49.60344564807929402, -48.82486940075439463 ) ) ;
#9702=CARTESIAN_POINT ( 'NONE',  ( 58.77552830958769903, -45.11615816423340419, -25.67179826716159852 ) ) ;
#9703=VECTOR ( 'NONE', #26050, 1000.000000000000114 ) ;
#9705=CARTESIAN_POINT ( 'NONE',  ( 13.57018851586839858, 19.78829187941649792, -21.88591218289379725 ) ) ;
#9706=CARTESIAN_POINT ( 'NONE',  ( 56.49550580218529916, 14.24991461377820023, -25.70480935931119859 ) ) ;
#9708=CARTESIAN_POINT ( 'NONE',  ( 50.95182855010829570, 19.71852720125919944, -76.14999999999999147 ) ) ;
#9709=CARTESIAN_POINT ( 'NONE',  ( 52.86125337422269865, 18.42614690627490148, -48.87400159313619952 ) ) ;
#9711=CARTESIAN_POINT ( 'NONE',  ( 60.66054148094019638, -45.55815270253820159, -47.10566629212190293 ) ) ;
#9712=CARTESIAN_POINT ( 'NONE',  ( 46.37947015900544301, 21.71088129867535699, -76.14999999999999147 ) ) ;
#9713=ORIENTED_EDGE ( 'NONE', *, *, #41817, .F. ) ;
#9715=EDGE_CURVE ( 'NONE', #38484, #15061, #23016, .T. ) ;
#9717=CARTESIAN_POINT ( 'NONE',  ( 47.41728684029249763, -54.64464118299699891, -54.77930846233410023 ) ) ;
#9718=CARTESIAN_POINT ( 'NONE',  ( -3.204518369755029905, 17.10185219583640048, -4.296538310232840274 ) ) ;
#9720=CARTESIAN_POINT ( 'NONE',  ( 11.14146392936840080, -65.20891899316059437, -17.73105615079460051 ) ) ;
#9727=FACE_OUTER_BOUND ( 'NONE', #42343, .T. ) ;
#9729=ORIENTED_EDGE ( 'NONE', *, *, #1007, .F. ) ;
#9731=LINE ( 'NONE', #17845, #36098 ) ;
#9733=CARTESIAN_POINT ( 'NONE',  ( 52.12745817633830114, 19.40061496106389782, -76.37383754635089872 ) ) ;
#9736=AXIS2_PLACEMENT_3D ( 'NONE', #45919, #45655, #30687 ) ;
#9740=CIRCLE ( 'NONE', #28985, 1.999999999999998446 ) ;
#9744=( BOUNDED_CURVE ( )  B_SPLINE_CURVE ( 3, ( #13040, #24786, #21126, #32384 ),
 .UNSPECIFIED., .F., .T. ) 
 B_SPLINE_CURVE_WITH_KNOTS ( ( 4, 4 ),
 ( 4.856961825214290762, 7.709408789144880814 ),
 .UNSPECIFIED. ) 
 CURVE ( )  GEOMETRIC_REPRESENTATION_ITEM ( )  RATIONAL_B_SPLINE_CURVE ( ( 1.000000000000000000, 0.4293798293182609638, 0.4293798293182609638, 1.000000000000000000 ) ) 
 REPRESENTATION_ITEM ( '' )  );
#9746=CARTESIAN_POINT ( 'NONE',  ( 56.74295248199899788, -46.05519997842870339, -26.24922959646229970 ) ) ;
#9751=ADVANCED_FACE ( 'NONE', ( #49917 ), #18192, .F. ) ;
#9752=CARTESIAN_POINT ( 'NONE',  ( 13.94115953390780049, 19.96087670211870346, -74.14993703734479880 ) ) ;
#9755=EDGE_CURVE ( 'NONE', #30578, #679, #21335, .T. ) ;
#9756=CARTESIAN_POINT ( 'NONE',  ( 45.86654133577830095, -45.11728007697210785, -7.634490596206400248 ) ) ;
#9757=CARTESIAN_POINT ( 'NONE',  ( 82.13853704237929776, 15.88381105532069704, -46.37203261889099792 ) ) ;
#9761=CARTESIAN_POINT ( 'NONE',  ( 52.92251006689210158, -49.49947021432900129, -27.40003960897890067 ) ) ;
#9762=CIRCLE ( 'NONE', #44929, 15.11955878774480233 ) ;
#9763=CARTESIAN_POINT ( 'NONE',  ( 14.13974949994079999, -51.04257351792690400, -21.96874462324809940 ) ) ;
#9764=CARTESIAN_POINT ( 'NONE',  ( 2.967561434627600025, 25.54483905069779937, -11.19253359192279973 ) ) ;
#9767=CARTESIAN_POINT ( 'NONE',  ( -23.86606260230395904, -35.74824341182122822, -53.92777777777786952 ) ) ;
#9769=CARTESIAN_POINT ( 'NONE',  ( -10.43357540151349916, -42.79329260199609308, -6.008434035834979703 ) ) ;
#9770=CARTESIAN_POINT ( 'NONE',  ( 47.63214245887139953, 23.26321908959739915, -54.67389918656080283 ) ) ;
#9771=VECTOR ( 'NONE', #4524, 1000.000000000000000 ) ;
#9772=EDGE_CURVE ( 'NONE', #36840, #39487, #32208, .T. ) ;
#9773=CARTESIAN_POINT ( 'NONE',  ( 16.13393739769620083, -15.61618894467929941, 7.349999999999999645 ) ) ;
#9776=CARTESIAN_POINT ( 'NONE',  ( 41.66707738397720107, 13.41595190872300059, -5.278831649207059939 ) ) ;
#9777=CARTESIAN_POINT ( 'NONE',  ( 51.84382618163579792, 18.03477920213529728, -77.06468978116740232 ) ) ;
#9778=CARTESIAN_POINT ( 'NONE',  ( 16.13393739769620083, -15.61618894467929941, -11.05000000000000071 ) ) ;
#9782=CARTESIAN_POINT ( 'NONE',  ( 52.45962341386800176, 21.25014430318469749, -54.36149425316440187 ) ) ;
#9785=DIRECTION ( 'NONE',  ( 0.000000000000000000, -1.000000000000000000, 0.000000000000000000 ) ) ;
#9786=VERTEX_POINT ( 'NONE', #39663 ) ;
#9788=CARTESIAN_POINT ( 'NONE',  ( 10.97845908955850014, 31.98345705163180241, -44.74187252678620297 ) ) ;
#9789=CYLINDRICAL_SURFACE ( 'NONE', #17604, 2.999999999999999112 ) ;
#9790=AXIS2_PLACEMENT_3D ( 'NONE', #19369, #51089, #30889 ) ;
#9791=CARTESIAN_POINT ( 'NONE',  ( 66.95998268897230332, -32.69201298692910029, -18.94774364808279898 ) ) ;
#9795=ORIENTED_EDGE ( 'NONE', *, *, #31917, .T. ) ;
#9798=CARTESIAN_POINT ( 'NONE',  ( 9.965595104546959959, -63.68164282303038704, -46.24046655278920070 ) ) ;
#9799=CARTESIAN_POINT ( 'NONE',  ( 57.29432520663860373, -45.62414914554469902, -26.18807222717889971 ) ) ;
#9801=CARTESIAN_POINT ( 'NONE',  ( 16.65420337941489848, 19.88381105532299742, -20.15000000000000213 ) ) ;
#9807=CARTESIAN_POINT ( 'NONE',  ( 54.71777093172589446, -45.61739902857990359, -15.43676083049879999 ) ) ;
#9808=VECTOR ( 'NONE', #27962, 1000.000000000000000 ) ;
#9810=CARTESIAN_POINT ( 'NONE',  ( 16.65427257814469897, 19.88381105411679783, -20.14977964541809996 ) ) ;
#9812=VERTEX_POINT ( 'NONE', #51463 ) ;
#9814=CARTESIAN_POINT ( 'NONE',  ( 46.77994874552049254, -53.89178638932320098, -75.86501933388160523 ) ) ;
#9815=CARTESIAN_POINT ( 'NONE',  ( 41.23501606932020280, 13.88381301678689894, -6.199056208102949661 ) ) ;
#9816=CARTESIAN_POINT ( 'NONE',  ( 51.00410689780089513, 21.58760788935499875, -53.76372497442359588 ) ) ;
#9817=ADVANCED_FACE ( 'NONE', ( #34682 ), #43090, .T. ) ;
#9820=CARTESIAN_POINT ( 'NONE',  ( 51.15928693312330466, 19.73279912208279896, -76.15045075665069874 ) ) ;
#9821=CARTESIAN_POINT ( 'NONE',  ( 57.39038370734829897, 14.07100446516539982, -25.91661231449569769 ) ) ;
#9822=ADVANCED_FACE ( 'NONE', ( #15563 ), #41875, .T. ) ;
#9826=CARTESIAN_POINT ( 'NONE',  ( -11.30871548113529990, -41.86345860935140450, -5.946230549336929627 ) ) ;
#9833=CARTESIAN_POINT ( 'NONE',  ( 43.27084646103560317, -43.87227363443550132, -5.051381114840269859 ) ) ;
#9834=LINE ( 'NONE', #38131, #18364 ) ;
#9842=CARTESIAN_POINT ( 'NONE',  ( 61.23205860893720143, -45.59110651710669515, -47.66442491677190674 ) ) ;
#9847=CARTESIAN_POINT ( 'NONE',  ( 40.70150336865399510, -45.32906768026739996, -5.681035058216649780 ) ) ;
#9850=ORIENTED_EDGE ( 'NONE', *, *, #1473, .T. ) ;
#9853=CARTESIAN_POINT ( 'NONE',  ( 56.39371274214659735, -50.58610758163149512, -52.96141008474040035 ) ) ;
#9854=EDGE_CURVE ( 'NONE', #25744, #9892, #27214, .T. ) ;
#9855=VERTEX_POINT ( 'NONE', #22693 ) ;
#9859=VECTOR ( 'NONE', #4345, 1000.000000000000000 ) ;
#9861=DIRECTION ( 'NONE',  ( 0.04251717301921900671, 0.000000000000000000, 0.9990957361526741076 ) ) ;
#9863=CARTESIAN_POINT ( 'NONE',  ( 11.67619942398489918, -64.89165360645620240, -45.08494251881790404 ) ) ;
#9864=CARTESIAN_POINT ( 'NONE',  ( 52.84397959254010146, -50.50345798787359541, -76.72969847629740059 ) ) ;
#9865=CARTESIAN_POINT ( 'NONE',  ( 60.51067680394970694, 14.40429311637669940, -47.16814695452289641 ) ) ;
#9867=CARTESIAN_POINT ( 'NONE',  ( 68.13393739769620083, -50.61618894467930119, -69.74999999999998579 ) ) ;
#9868=CARTESIAN_POINT ( 'NONE',  ( 44.89324673519139708, 14.02190024633609866, -7.755622268330540692 ) ) ;
#9869=CARTESIAN_POINT ( 'NONE',  ( 42.94731284509200009, -42.57349969409850132, -3.548345704167709780 ) ) ;
#9871=CARTESIAN_POINT ( 'NONE',  ( 65.36113773965780638, 1.378962859947149955, -18.37587875859610165 ) ) ;
#9872=EDGE_CURVE ( 'NONE', #41037, #4059, #13816, .T. ) ;
#9875=CARTESIAN_POINT ( 'NONE',  ( 68.36214382535489165, -0.4430383702800620438, -18.19623533484779898 ) ) ;
#9878=CARTESIAN_POINT ( 'NONE',  ( 15.05440318628160057, -53.11618894467930119, -76.14999999999999147 ) ) ;
#9879=CARTESIAN_POINT ( 'NONE',  ( 47.18324198357289845, -54.80726809202429450, -54.61058319554170026 ) ) ;
#9881=CARTESIAN_POINT ( 'NONE',  ( 10.61754762155600140, 33.59328422689429772, -18.17417937929459981 ) ) ;
#9883=CARTESIAN_POINT ( 'NONE',  ( 47.01289497786039817, -54.42182676496869931, -75.36291177546809195 ) ) ;
#9885=CARTESIAN_POINT ( 'NONE',  ( 47.81335647231750130, -54.39749252970050009, -54.71582838609450050 ) ) ;
#9887=CARTESIAN_POINT ( 'NONE',  ( 56.35668072086730263, 19.46447099969040195, -53.18237273277000554 ) ) ;
#9889=CARTESIAN_POINT ( 'NONE',  ( 47.93812309775100289, 23.11656297732089627, -54.78467533403669876 ) ) ;
#9890=ORIENTED_EDGE ( 'NONE', *, *, #4974, .F. ) ;
#9892=VERTEX_POINT ( 'NONE', #22431 ) ;
#9894=CARTESIAN_POINT ( 'NONE',  ( 83.07525789736615707, 14.27201180209920217, -47.60488146747717053 ) ) ;
#9896=CARTESIAN_POINT ( 'NONE',  ( 84.32109122769391263, 12.72058013282260092, -47.41657241682830204 ) ) ;
#9897=CARTESIAN_POINT ( 'NONE',  ( 65.03603135424580728, -29.76883965895079953, -19.52361391316370032 ) ) ;
#9904=B_SPLINE_CURVE_WITH_KNOTS ( 'NONE', 3,
 ( #5015, #3982, #16029, #8168, #20452, #8427, #24112, #40132, #4226, #36442, #16534, #32486, #48514, #12618, #9718, #41167 ),
 .UNSPECIFIED., .F., .F.,
 ( 4, 2, 2, 2, 2, 2, 2, 4 ),
 ( -11.88254149278500016, -9.803096731538550657, -7.426588432971120035, -5.941270746366480004, -5.198611903064159989, -4.010357753780449563, -2.109151114926509862, 5.208278253121534362E-11 ),
 .UNSPECIFIED. ) ;
#9907=CARTESIAN_POINT ( 'NONE',  ( 11.54602910941480154, 33.64475169218199824, -45.95025651893509888 ) ) ;
#9909=DIRECTION ( 'NONE',  ( 0.000000000000000000, 0.000000000000000000, -1.000000000000000000 ) ) ;
#9913=EDGE_CURVE ( 'NONE', #14240, #18792, #14787, .T. ) ;
#9914=CARTESIAN_POINT ( 'NONE',  ( 53.26712897989530404, 18.16301094328009924, -48.90765490644029967 ) ) ;
#9915=CARTESIAN_POINT ( 'NONE',  ( 64.47274453872979905, -1.570850956254630004, -16.41268983226810008 ) ) ;
#9916=CARTESIAN_POINT ( 'NONE',  ( 51.67725368488709847, -50.05092317807059743, -76.49491248771630580 ) ) ;
#9917=ADVANCED_FACE ( 'NONE', ( #4078 ), #43664, .F. ) ;
#9918=CARTESIAN_POINT ( 'NONE',  ( 56.87642604909630251, -50.51355556899029864, -53.02367019345480514 ) ) ;
#9925=CARTESIAN_POINT ( 'NONE',  ( 57.50723796702470025, -47.11618894467930119, -17.93019253464870033 ) ) ;
#9928=CARTESIAN_POINT ( 'NONE',  ( 13.32539517089530001, -51.13125742665909712, -21.90065997771110418 ) ) ;
#9929=CARTESIAN_POINT ( 'NONE',  ( 56.72660940836590271, 19.43947700957160052, -74.52937665603549533 ) ) ;
#9930=CARTESIAN_POINT ( 'NONE',  ( 47.20372080753160304, -53.97904105312669287, -75.66073271794819277 ) ) ;
#9931=ORIENTED_EDGE ( 'NONE', *, *, #40499, .T. ) ;
#9932=CARTESIAN_POINT ( 'NONE',  ( 56.03489956542599515, 14.32464527057259929, -16.86885345059799945 ) ) ;
#9933=CARTESIAN_POINT ( 'NONE',  ( 47.75363926615540322, 23.23893620800870252, -54.94115012086979988 ) ) ;
#9934=CARTESIAN_POINT ( 'NONE',  ( 57.03107162669589769, -50.22865659835970575, -52.68131389647400198 ) ) ;
#9939=EDGE_LOOP ( 'NONE', ( #48938, #49011, #682, #22348 ) ) ;
#9940=CARTESIAN_POINT ( 'NONE',  ( 47.50503096094819711, 23.24249282884580126, -74.80880243014959774 ) ) ;
#9942=CARTESIAN_POINT ( 'NONE',  ( 75.15838486831707144, -29.30899119363491678, -11.83853932060654657 ) ) ;
#9949=CARTESIAN_POINT ( 'NONE',  ( 61.24542922434319792, 14.01933573698959989, -46.57808965542819379 ) ) ;
#9951=CARTESIAN_POINT ( 'NONE',  ( -18.43754721997740020, 21.20956224061950124, -54.46408928706180319 ) ) ;
#9953=CARTESIAN_POINT ( 'NONE',  ( 52.79145514622300084, -49.68335952808720180, -48.63147282162839957 ) ) ;
#9955=AXIS2_PLACEMENT_3D ( 'NONE', #48346, #4838, #16109 ) ;
#9958=CARTESIAN_POINT ( 'NONE',  ( 13.86896207300669914, 19.56934397777870061, -21.50766788832570242 ) ) ;
#9962=VECTOR ( 'NONE', #25613, 999.9999999999998863 ) ;
#9963=CARTESIAN_POINT ( 'NONE',  ( 50.03007021624649298, 17.53271186393800107, -76.14999999999999147 ) ) ;
#9964=CARTESIAN_POINT ( 'NONE',  ( 52.97367359308089618, 18.36436387382549995, -48.91755406990360200 ) ) ;
#9966=CARTESIAN_POINT ( 'NONE',  ( 60.58881092996779927, -45.59573434794560143, -47.13710661926510426 ) ) ;
#9973=CARTESIAN_POINT ( 'NONE',  ( 11.89433743671910015, -65.43612263100310145, -18.12680249715119984 ) ) ;
#9974=CARTESIAN_POINT ( 'NONE',  ( 52.85589143289909941, 18.41484964472969921, -48.63420543068689739 ) ) ;
#9975=DIRECTION ( 'NONE',  ( 0.000000000000000000, -1.000000000000000000, 0.000000000000000000 ) ) ;
#9980=CARTESIAN_POINT ( 'NONE',  ( 13.97463716302289960, -51.18681913639190384, -22.92153292251790120 ) ) ;
#9981=ADVANCED_FACE ( 'NONE', ( #7767 ), #31579, .F. ) ;
#9983=VERTEX_POINT ( 'NONE', #51528 ) ;
#9984=DIRECTION ( 'NONE',  ( 0.000000000000000000, 0.000000000000000000, 1.000000000000000000 ) ) ;
#9985=CARTESIAN_POINT ( 'NONE',  ( 57.24929578232330130, -50.61618894764249887, -53.91492796143979405 ) ) ;
#9987=CARTESIAN_POINT ( 'NONE',  ( 52.01032270792030232, 18.80640155979590133, -76.70782231553221209 ) ) ;
#9994=FACE_OUTER_BOUND ( 'NONE', #4056, .T. ) ;
#9997=CIRCLE ( 'NONE', #16686, 50.00000000000000000 ) ;
#10000=CIRCLE ( 'NONE', #24998, 40.00000000000000711 ) ;
#10001=AXIS2_PLACEMENT_3D ( 'NONE', #10886, #34178, #50197 ) ;
#10005=CIRCLE ( 'NONE', #31753, 38.00000000000000711 ) ;
#10008=CARTESIAN_POINT ( 'NONE',  ( 13.39996607787550076, 20.55443427335040241, -74.33583724502659607 ) ) ;
#10009=CARTESIAN_POINT ( 'NONE',  ( 17.21347160910390173, -53.11618894467930119, -76.14999999999999147 ) ) ;
#10010=CARTESIAN_POINT ( 'NONE',  ( 41.01790532569319225, -45.00796875502680194, -5.564953489975700052 ) ) ;
#10014=CARTESIAN_POINT ( 'NONE',  ( 53.56631670864459949, -48.76508776475549922, -26.51357180580690098 ) ) ;
#10015=CARTESIAN_POINT ( 'NONE',  ( 54.09921394265249717, -50.74273564420649762, -76.27543683137730568 ) ) ;
#10016=CARTESIAN_POINT ( 'NONE',  ( 5.772816392169699995, 28.52799414409169643, -13.89632254613010076 ) ) ;
#10019=FACE_OUTER_BOUND ( 'NONE', #2121, .T. ) ;
#10021=CARTESIAN_POINT ( 'NONE',  ( -7.453150335675089444, -45.41421344120890069, -5.042286980664930418 ) ) ;
#10022=CARTESIAN_POINT ( 'NONE',  ( 47.42530979538980063, 23.40590081362070052, -54.75924875434800043 ) ) ;
#10026=CARTESIAN_POINT ( 'NONE',  ( 11.93872965651339868, 33.96647849370500438, -16.76612700402739975 ) ) ;
#10029=DIRECTION ( 'NONE',  ( 0.000000000000000000, 0.000000000000000000, -1.000000000000000000 ) ) ;
#10032=CARTESIAN_POINT ( 'NONE',  ( 54.69511575210409404, 20.01728140309300130, -53.07518616905519337 ) ) ;
#10035=AXIS2_PLACEMENT_3D ( 'NONE', #25043, #36086, #8836 ) ;
#10036=CARTESIAN_POINT ( 'NONE',  ( 12.17742765526699955, -65.07456428805339499, -16.46016921340210004 ) ) ;
#10037=DIRECTION ( 'NONE',  ( 0.2169304578186566079, 0.000000000000000000, -0.9761870601839527373 ) ) ;
#10039=CARTESIAN_POINT ( 'NONE',  ( 19.65221995360836260, 22.80254658028719206, -17.14827763294746532 ) ) ;
#10040=CARTESIAN_POINT ( 'NONE',  ( 10.97923803353369898, 32.08794574957100565, -44.74348915807490101 ) ) ;
#10043=CARTESIAN_POINT ( 'NONE',  ( 67.20512611029329264, -32.78246747541099637, -19.24941993779820137 ) ) ;
#10044=CARTESIAN_POINT ( 'NONE',  ( 68.13393739769620083, -48.11618894467930119, -69.74999999999998579 ) ) ;
#10050=CARTESIAN_POINT ( 'NONE',  ( 50.51115622925506443, -0.6041507554334789587, -16.31432736417265161 ) ) ;
#10052=CARTESIAN_POINT ( 'NONE',  ( 12.52502643766059975, -65.43529974157461027, -47.02089506534060348 ) ) ;
#10053=CARTESIAN_POINT ( 'NONE',  ( 57.19937016862409962, -45.64255992831129305, -26.18060017548449991 ) ) ;
#10058=ORIENTED_EDGE ( 'NONE', *, *, #51717, .F. ) ;
#10061=CARTESIAN_POINT ( 'NONE',  ( 50.50428634387549920, -45.11618894460880114, -10.93747568071940002 ) ) ;
#10064=CARTESIAN_POINT ( 'NONE',  ( 16.50880182599389912, 19.88028731614700106, -20.14980157100500335 ) ) ;
#10065=CARTESIAN_POINT ( 'NONE',  ( 57.55751162049570269, -50.61618894467930119, -53.92796738110899923 ) ) ;
#10067=CARTESIAN_POINT ( 'NONE',  ( 82.13853704237929776, 14.40950277491920062, -47.72348187592560009 ) ) ;
#10068=CARTESIAN_POINT ( 'NONE',  ( 46.79115157945750525, -53.88453574729260254, -75.86421395400510903 ) ) ;
#10069=CARTESIAN_POINT ( 'NONE',  ( 51.93064259432500052, 13.88381105527570014, -9.012790087523750771 ) ) ;
#10070=CARTESIAN_POINT ( 'NONE',  ( 51.23808412325809769, 13.88381105532070059, -11.16296171910600066 ) ) ;
#10071=ADVANCED_FACE ( 'NONE', ( #3315 ), #47599, .T. ) ;
#10074=AXIS2_PLACEMENT_3D ( 'NONE', #3418, #11279, #43257 ) ;
#10076=CARTESIAN_POINT ( 'NONE',  ( 52.14830235930340052, 19.90969062716179749, -76.06502807877821226 ) ) ;
#10077=CARTESIAN_POINT ( 'NONE',  ( 59.63820723955320346, 13.92583137105579993, -26.24900372433129903 ) ) ;
#10079=B_SPLINE_SURFACE_WITH_KNOTS ( 'NONE', 3, 3, ( 
 ( #8580, #20866, #32912, #28994, #40795, #4378, #13041, #194, #31879, #24266, #41061, #21128, #44994, #16965, #24522, #5173, #40028, #51819 ),
 ( #48406, #44731, #20346, #48671, #36596, #8060, #28211, #16689, #8309, #15923, #12775, #40286, #4630, #32385, #47898, #27953, #16432, #28730 ),
 ( #44212, #24787, #43956, #16171, #4120, #40540, #36332, #20601, #20096, #32129, #48148, #12249, #442, #12505, #28474, #13548, #13799, #42094 ),
 ( #6197, #22152, #33946, #17979, #37906, #18234, #17217, #9864, #46036, #2259, #38161, #49199, #21381, #49963, #33438, #34199, #21632, #37639 ),
 ( #21895, #25818, #1999, #30279, #50220, #13291, #41313, #49709, #17472, #9362, #41830, #9612, #29755, #45772, #37129, #49456, #33177, #1228 ),
 ( #14310, #17723, #14053, #46299, #29510, #30014, #1742, #10386, #5937, #45515, #25564, #10128, #33694, #26342, #42354, #26086, #6455, #41570 ),
 ( #29248, #25311, #5684, #45257, #5424, #37384, #1487, #30793, #15609, #38418, #34470, #47584, #10648, #39461, #47333, #50730, #43139, #34987 ),
 ( #11679, #22927, #23181, #22672, #50987, #43649, #11425, #38692, #3037, #15352, #2516, #14570, #26871, #10908, #46818, #42878, #3293, #3558 ),
 ( #6975, #35257, #18499, #51257, #50480, #26603, #38947, #42619, #2781, #19271, #31304, #19011, #27645, #15087, #6716, #7231, #27389, #43391 ),
 ( #30535, #23437, #7486, #31054, #47077, #11165, #31563, #19531, #22415, #35519, #46558, #51509, #27133, #39198, #18752, #34728, #14829, #7995 ) ),
 .UNSPECIFIED., .F., .F., .F.,
 ( 4, 1, 1, 1, 1, 1, 1, 4 ),
 ( 4, 2, 2, 2, 2, 2, 2, 2, 4 ),
 ( -7.333206230300000740E-05, 0.1428571428571430157, 0.2857142857142860315, 0.4285714285714289917, 0.5714285714285709528, 0.7142857142857139685, 0.8571428571428569843, 1.000000000000000000 ),
 ( -3.925943193499569883, -2.996312950063570124, -2.453668663398290040, -1.962934930718630122, -1.717568064378800052, -1.324981078235079934, -0.6968419004051140675, -0.06459440906511799974, 7.333206230300000740E-05 ),
 .UNSPECIFIED. ) ;
#10082=CARTESIAN_POINT ( 'NONE',  ( -10.65432657557460061, -41.72751226988879836, -4.619077395148970311 ) ) ;
#10083=DIRECTION ( 'NONE',  ( -1.000000000000000000, 1.127159607568241538E-32, -7.935614746461580696E-16 ) ) ;
#10085=CARTESIAN_POINT ( 'NONE',  ( 17.92370450347650035, -51.11618894467930119, -15.67980085856620143 ) ) ;
#10086=DIRECTION ( 'NONE',  ( 0.000000000000000000, 0.7371541402007432131, -0.6757246285173443834 ) ) ;
#10088=CARTESIAN_POINT ( 'NONE',  ( 41.73867463177359838, 12.46261384428329855, -3.496169909523889618 ) ) ;
#10091=CARTESIAN_POINT ( 'NONE',  ( 31.00696234477200264, -15.61618894467929941, -7.225658350974740074 ) ) ;
#10094=CARTESIAN_POINT ( 'NONE',  ( 18.63644253395800021, -51.46210362308070074, -74.58518005234699899 ) ) ;
#10096=B_SPLINE_CURVE_WITH_KNOTS ( 'NONE', 3,
 ( #46672, #31160, #6831, #7089, #6562, #11016, #22267, #47188, #22527, #38802, #51102, #38276, #50334, #2896, #18861, #26987, #42993, #39061, #3414, #14422, #23040, #2366, #35102, #46414, #38539, #19122, #18607, #15202, #11275, #7341 ),
 .UNSPECIFIED., .F., .F.,
 ( 4, 2, 2, 2, 2, 2, 2, 2, 2, 2, 2, 2, 2, 2, 4 ),
 ( 0.000000000000000000, 0.04341623943293104748, 0.1253847836472181121, 0.1766151237811480201, 0.2170652101236044962, 0.2575152964660598065, 0.3375200487661945692, 0.3875230189537799963, 0.4375259891413642577, 0.5000297018758445011, 0.5625334146103245780, 0.6625393549854932118, 0.7519024652212540349, 0.8948834415984711077, 1.000000000000000000 ),
 .UNSPECIFIED. ) ;
#10097=ORIENTED_EDGE ( 'NONE', *, *, #20873, .F. ) ;
#10101=VERTEX_POINT ( 'NONE', #32862 ) ;
#10102=CARTESIAN_POINT ( 'NONE',  ( 1.761217661586780059, 24.33376534107589961, -11.00321056186240121 ) ) ;
#10108=LINE ( 'NONE', #38676, #6717 ) ;
#10109=CARTESIAN_POINT ( 'NONE',  ( 60.23130391296999875, -45.78304229081430066, -47.24246919202539630 ) ) ;
#10111=VERTEX_POINT ( 'NONE', #45214 ) ;
#10114=CARTESIAN_POINT ( 'NONE',  ( 61.32175331331019663, -45.22151323983460003, -46.73009288909239700 ) ) ;
#10119=CIRCLE ( 'NONE', #20116, 6.049999999999999822 ) ;
#10120=ORIENTED_EDGE ( 'NONE', *, *, #18442, .F. ) ;
#10126=ORIENTED_EDGE ( 'NONE', *, *, #16820, .T. ) ;
#10128=CARTESIAN_POINT ( 'NONE',  ( 52.12745821273779256, -50.63299286582169856, -76.37383754424429583 ) ) ;
#10129=CARTESIAN_POINT ( 'NONE',  ( 60.29580587845369877, 14.52606445528390111, -47.36817177740100249 ) ) ;
#10131=CARTESIAN_POINT ( 'NONE',  ( 51.63351621991599671, 19.38381105532069881, -66.86356675664690385 ) ) ;
#10132=CARTESIAN_POINT ( 'NONE',  ( 46.03123730839019601, 13.88381105531820126, -7.582885970392889696 ) ) ;
#10133=EDGE_CURVE ( 'NONE', #14240, #15334, #39879, .T. ) ;
#10134=CARTESIAN_POINT ( 'NONE',  ( 41.54582571382449174, -43.96466023683059632, -4.072799765277079764 ) ) ;
#10135=CARTESIAN_POINT ( 'NONE',  ( 56.44408186407410000, 14.18700613804810118, -25.29404973353000230 ) ) ;
#10138=CARTESIAN_POINT ( 'NONE',  ( 57.24929578595760660, -50.61618894467930119, -74.14999999999999147 ) ) ;
#10140=CARTESIAN_POINT ( 'NONE',  ( 14.78260632833550048, -52.41676442117930179, -76.03098605356829864 ) ) ;
#10141=CARTESIAN_POINT ( 'NONE',  ( 47.20997691013830178, -54.78608722903020123, -54.63758431345319622 ) ) ;
#10142=CARTESIAN_POINT ( 'NONE',  ( 9.949440222648611609, 33.40288359691523112, -46.96299386723978131 ) ) ;
#10143=CARTESIAN_POINT ( 'NONE',  ( 11.43204200623334188, 33.34744811472585013, -44.55415195547232088 ) ) ;
#10144=AXIS2_PLACEMENT_3D ( 'NONE', #3912, #32418, #40061 ) ;
#10146=CARTESIAN_POINT ( 'NONE',  ( 47.18324198357279897, -54.80726809202429450, -74.17417149933299925 ) ) ;
#10147=EDGE_CURVE ( 'NONE', #13586, #19842, #17849, .T. ) ;
#10150=CARTESIAN_POINT ( 'NONE',  ( 47.93286353489659746, -54.34025906026520403, -54.74353221703739791 ) ) ;
#10152=CARTESIAN_POINT ( 'NONE',  ( 56.52536539877749533, 19.51942783438209972, -53.84278118897309895 ) ) ;
#10153=CARTESIAN_POINT ( 'NONE',  ( 47.96474501199910634, 23.16479111562100002, -55.26734477448599847 ) ) ;
#10156=ORIENTED_EDGE ( 'NONE', *, *, #48882, .F. ) ;
#10157=CARTESIAN_POINT ( 'NONE',  ( 82.51390001523527928, 13.88631490708104366, -46.70336726651584769 ) ) ;
#10158=CARTESIAN_POINT ( 'NONE',  ( 68.13393739769620083, -48.61618894467930119, -65.65000000000000568 ) ) ;
#10160=CARTESIAN_POINT ( 'NONE',  ( 83.89463082533569604, 13.54987550622989900, -47.42987625071230440 ) ) ;
#10161=CARTESIAN_POINT ( 'NONE',  ( 52.58045495532469715, 18.61321147008669996, -28.06440927671260255 ) ) ;
#10163=LINE ( 'NONE', #14606, #10334 ) ;
#10164=CARTESIAN_POINT ( 'NONE',  ( 56.84932592767829362, -50.65659099804129539, -74.14999999999999147 ) ) ;
#10166=ORIENTED_EDGE ( 'NONE', *, *, #10213, .T. ) ;
#10167=DIRECTION ( 'NONE',  ( -0.3294064756440938657, 0.9441882088883216673, 2.329877999999999163E-14 ) ) ;
#10172=ADVANCED_FACE ( 'NONE', ( #1182 ), #40243, .F. ) ;
#10173=CARTESIAN_POINT ( 'NONE',  ( 0.8851803632885170137, 11.70999949991828259, -20.85710678118654471 ) ) ;
#10180=CARTESIAN_POINT ( 'NONE',  ( 52.66874163714970081, -49.78066393629400466, -48.73461952183779999 ) ) ;
#10181=CARTESIAN_POINT ( 'NONE',  ( 47.41023719977609829, 23.44958313673180328, -54.95588507597090455 ) ) ;
#10182=CARTESIAN_POINT ( 'NONE',  ( 62.18049626896419824, -1.322404863900719985, -16.13653024010810100 ) ) ;
#10183=CARTESIAN_POINT ( 'NONE',  ( 51.47836095788819932, -49.80706049537930369, -76.47682165003159582 ) ) ;
#10184=CARTESIAN_POINT ( 'NONE',  ( 57.91488495618810362, -49.39618335747870503, -51.80378965555370030 ) ) ;
#10186=ORIENTED_EDGE ( 'NONE', *, *, #37866, .F. ) ;
#10189=CARTESIAN_POINT ( 'NONE',  ( 68.13393739769630031, 16.88381105531719939, -74.20000000000000284 ) ) ;
#10195=CARTESIAN_POINT ( 'NONE',  ( 13.78851007908129844, -50.80050206934620149, -21.52764351545879862 ) ) ;
#10196=CARTESIAN_POINT ( 'NONE',  ( 56.33747328523660514, 19.49822906174120263, -74.84828165003129641 ) ) ;
#10197=CARTESIAN_POINT ( 'NONE',  ( 47.64143405400680109, -54.53488714545009941, -74.17417149933299925 ) ) ;
#10199=CARTESIAN_POINT ( 'NONE',  ( 55.59517693494780133, 14.55448978459209997, -16.53159430204590308 ) ) ;
#10201=CARTESIAN_POINT ( 'NONE',  ( 57.07954902837180100, -50.30027628258600458, -52.78599242821820070 ) ) ;
#10203=CARTESIAN_POINT ( 'NONE',  ( 16.65420337942459739, 19.88381105532299742, -15.67544741556190324 ) ) ;
#10205=CARTESIAN_POINT ( 'NONE',  ( 47.47121842882930309, 23.19633386185850199, -74.94862672502200951 ) ) ;
#10207=CARTESIAN_POINT ( 'NONE',  ( 75.29303414918550175, -36.26344722174416546, -12.49608819919907354 ) ) ;
#10208=CARTESIAN_POINT ( 'NONE',  ( 12.66989959080678574, -65.46799403849351506, -23.46212470398215544 ) ) ;
#10210=ADVANCED_FACE ( 'NONE', ( #33657 ), #18460, .T. ) ;
#10212=CARTESIAN_POINT ( 'NONE',  ( 82.27845167518849223, 13.94631328714430119, -46.87713584290389690 ) ) ;
#10213=EDGE_CURVE ( 'NONE', #23799, #49749, #49924, .T. ) ;
#10219=CARTESIAN_POINT ( 'NONE',  ( 12.78938691692309959, 32.28743192295770115, -45.78213823142860406 ) ) ;
#10221=EDGE_LOOP ( 'NONE', ( #2106, #44075, #34839, #45438 ) ) ;
#10222=VECTOR ( 'NONE', #26279, 1000.000000000000000 ) ;
#10223=CARTESIAN_POINT ( 'NONE',  ( 53.03535128242899788, -49.56646391233060456, -48.94674795462399430 ) ) ;
#10224=VECTOR ( 'NONE', #20842, 1000.000000000000000 ) ;
#10228=CARTESIAN_POINT ( 'NONE',  ( 13.72477621988739926, 19.74414037213060169, -21.83795113765379980 ) ) ;
#10229=CARTESIAN_POINT ( 'NONE',  ( 56.23669252666629603, 14.33142556199779882, -25.29918085107650327 ) ) ;
#10232=CARTESIAN_POINT ( 'NONE',  ( 53.15063587404129919, 18.30021473852120195, -49.06766776400879593 ) ) ;
#10234=DIRECTION ( 'NONE',  ( 0.000000000000000000, 0.000000000000000000, 1.000000000000000000 ) ) ;
#10237=DIRECTION ( 'NONE',  ( 0.000000000000000000, 0.000000000000000000, 1.000000000000000000 ) ) ;
#10240=CARTESIAN_POINT ( 'NONE',  ( 11.04564840984290086, -65.17882761888340326, -17.95839446281759777 ) ) ;
#10247=ORIENTED_EDGE ( 'NONE', *, *, #22619, .F. ) ;
#10248=CARTESIAN_POINT ( 'NONE',  ( 10.49110564618760044, -63.26315525827371289, -45.62557459999030129 ) ) ;
#10250=ORIENTED_EDGE ( 'NONE', *, *, #15517, .F. ) ;
#10252=CARTESIAN_POINT ( 'NONE',  ( 57.36123083241199794, 18.90300136664210129, -52.61896061011540127 ) ) ;
#10253=CARTESIAN_POINT ( 'NONE',  ( 46.35275103504449845, -52.90993241930539881, -76.14999999999999147 ) ) ;
#10254=CARTESIAN_POINT ( 'NONE',  ( 52.34620960925839483, 18.68177451820979940, -77.13858428499739261 ) ) ;
#10256=CARTESIAN_POINT ( 'NONE',  ( 11.71633470187599180, -65.33094175621533850, -47.42091646568417929 ) ) ;
#10258=CARTESIAN_POINT ( 'NONE',  ( 57.55751162087899786, 18.85811933572220056, -52.57651812407429759 ) ) ;
#10259=DIRECTION ( 'NONE',  ( 0.000000000000000000, 0.000000000000000000, -1.000000000000000000 ) ) ;
#10264=ORIENTED_EDGE ( 'NONE', *, *, #44465, .F. ) ;
#10265=CARTESIAN_POINT ( 'NONE',  ( 57.07405361051419845, -45.88223445567830083, -26.24937779502229773 ) ) ;
#10267=TOROIDAL_SURFACE ( 'NONE', #28642, 18.00000000000000000, 2.000000000000000000 ) ;
#10268=CARTESIAN_POINT ( 'NONE',  ( 53.23493483693680162, -49.52411911180049486, -49.16095918439189916 ) ) ;
#10271=CARTESIAN_POINT ( 'NONE',  ( 14.20218124254490100, 20.03470611338460472, -74.90176971618339508 ) ) ;
#10273=CARTESIAN_POINT ( 'NONE',  ( 45.18655670870639796, -45.12046577740490250, -7.327032537671530399 ) ) ;
#10276=ORIENTED_EDGE ( 'NONE', *, *, #36418, .T. ) ;
#10277=CARTESIAN_POINT ( 'NONE',  ( 54.20225837649419987, -48.03317578680400146, -26.08669670602439794 ) ) ;
#10278=EDGE_CURVE ( 'NONE', #47824, #20725, #46522, .T. ) ;
#10279=CARTESIAN_POINT ( 'NONE',  ( 55.75888635692119522, -50.73156338577249613, -75.40713992321559545 ) ) ;
#10280=CARTESIAN_POINT ( 'NONE',  ( 3.573464422544550434, 25.59147421693169733, -10.25614976361119979 ) ) ;
#10282=DIRECTION ( 'NONE',  ( -0.3044500358626250902, -0.5455827667248117629, 0.7808006277636730941 ) ) ;
#10283=DIRECTION ( 'NONE',  ( -1.000000000000000000, 0.000000000000000000, 0.000000000000000000 ) ) ;
#10284=EDGE_CURVE ( 'NONE', #39070, #33614, #27333, .T. ) ;
#10286=CARTESIAN_POINT ( 'NONE',  ( 14.75122905864259160, 21.64019614509532730, -76.12465453342632316 ) ) ;
#10287=CARTESIAN_POINT ( 'NONE',  ( 47.42217282182370752, 23.41203903866150071, -54.87062249528260338 ) ) ;
#10290=CARTESIAN_POINT ( 'NONE',  ( 61.00623573019170465, 14.14465591030429970, -46.89457832669390314 ) ) ;
#10291=CARTESIAN_POINT ( 'NONE',  ( 11.74995128003140010, 34.02380396729650158, -17.00864127458340036 ) ) ;
#10292=CARTESIAN_POINT ( 'NONE',  ( 51.68242196497799767, 17.78920151642020286, -76.95384497402039869 ) ) ;
#10293=CARTESIAN_POINT ( 'NONE',  ( 53.26662649590710430, 18.19965403720820163, -48.79175420715170475 ) ) ;
#10295=CARTESIAN_POINT ( 'NONE',  ( 58.76885703184290577, -46.69396177055759978, -47.97628940940079900 ) ) ;
#10296=CARTESIAN_POINT ( 'NONE',  ( 52.71556874917159519, 18.49758023621189906, -28.15002987606190032 ) ) ;
#10297=CARTESIAN_POINT ( 'NONE',  ( 55.62530649940679695, 19.78524991857049997, -53.26680650779459825 ) ) ;
#10302=CARTESIAN_POINT ( 'NONE',  ( 56.32402052750479982, -45.11618894467940066, -10.15270052037220161 ) ) ;
#10303=CARTESIAN_POINT ( 'NONE',  ( 19.51692496783413944, 22.41474627964059962, -16.78241351213016586 ) ) ;
#10304=CARTESIAN_POINT ( 'NONE',  ( 10.49444742495719929, 32.12130227714850150, -45.62689257694430012 ) ) ;
#10305=VECTOR ( 'NONE', #50139, 999.9999999999998863 ) ;
#10312=CARTESIAN_POINT ( 'NONE',  ( 48.02894741700589520, 23.13744333908360318, -55.28037973459740329 ) ) ;
#10313=EDGE_CURVE ( 'NONE', #11745, #19040, #41422, .T. ) ;
#10314=CARTESIAN_POINT ( 'NONE',  ( 76.55694930642907536, 0.1129182662885630517, -13.47282127292171516 ) ) ;
#10315=ORIENTED_EDGE ( 'NONE', *, *, #9099, .F. ) ;
#10316=CARTESIAN_POINT ( 'NONE',  ( 12.94329929307280125, -65.51432672297359261, -47.65575625725580267 ) ) ;
#10317=CARTESIAN_POINT ( 'NONE',  ( 56.04095368967779933, -46.04400048969489490, -25.92328318301699852 ) ) ;
#10318=CARTESIAN_POINT ( 'NONE',  ( 57.77564497937559906, -31.65172285061208868, -17.11446609406731767 ) ) ;
#10321=CARTESIAN_POINT ( 'NONE',  ( 11.89321892218980103, 34.20364954172580241, -22.25048313876769868 ) ) ;
#10325=CARTESIAN_POINT ( 'NONE',  ( 45.64501526700150436, -46.12166612246060282, -9.406926139117178565 ) ) ;
#10327=CARTESIAN_POINT ( 'NONE',  ( 52.08182673490480141, 1.850722219266808910, -19.98516726105009411 ) ) ;
#10328=CARTESIAN_POINT ( 'NONE',  ( 16.19818216288450330, 19.87900877640220187, -21.03492549853969962 ) ) ;
#10332=CARTESIAN_POINT ( 'NONE',  ( 47.23192694729809915, -54.73625513866609538, -74.50311761397450994 ) ) ;
#10333=CARTESIAN_POINT ( 'NONE',  ( 45.26119862906019620, 13.15965671286969929, -5.724999702673090773 ) ) ;
#10334=VECTOR ( 'NONE', #50516, 1000.000000000000000 ) ;
#10335=CARTESIAN_POINT ( 'NONE',  ( 51.37525108058719070, 21.43002075209610169, -53.68096604571569941 ) ) ;
#10338=CARTESIAN_POINT ( 'NONE',  ( 53.68570370402219538, 19.91397335543889824, -75.73808979149589504 ) ) ;
#10339=CARTESIAN_POINT ( 'NONE',  ( 57.42077085024149596, 13.96450533941020034, -25.73600857157110156 ) ) ;
#10342=DIRECTION ( 'NONE',  ( -0.4439767838698117641, 0.8960382890170590642, 0.000000000000000000 ) ) ;
#10344=CARTESIAN_POINT ( 'NONE',  ( -4.193175284732109986, -49.34067351630189791, -7.780658117633309168 ) ) ;
#10345=DIRECTION ( 'NONE',  ( 7.935614746461580696E-16, 6.060292087350920604E-16, -1.000000000000000000 ) ) ;
#10349=CARTESIAN_POINT ( 'NONE',  ( 82.25807818787700398, -45.12248685479210053, -46.55740799543180231 ) ) ;
#10350=CARTESIAN_POINT ( 'NONE',  ( 16.13393739769620083, -15.61618894467929941, 5.856814007409659517 ) ) ;
#10351=CARTESIAN_POINT ( 'NONE',  ( 42.84544925580660646, 11.76657522153120183, -4.190148907829390090 ) ) ;
#10356=CARTESIAN_POINT ( 'NONE',  ( 75.73620089847491954, -43.35142246084668471, -13.49567144614401748 ) ) ;
#10365=DIRECTION ( 'NONE',  ( 0.8857883891771956009, -0.4640893551880597712, 2.775557561562888578E-17 ) ) ;
#10366=CARTESIAN_POINT ( 'NONE',  ( 47.79865291297670638, -54.41610742667179323, -54.75837665837189405 ) ) ;
#10369=CARTESIAN_POINT ( 'NONE',  ( 44.88826907266649613, -46.10884305417119577, -8.898922653467518984 ) ) ;
#10370=ORIENTED_EDGE ( 'NONE', *, *, #19521, .T. ) ;
#10372=EDGE_CURVE ( 'NONE', #34590, #14522, #9762, .T. ) ;
#10376=CIRCLE ( 'NONE', #1991, 1.500000000000001332 ) ;
#10386=CARTESIAN_POINT ( 'NONE',  ( 52.52866731283389612, -50.77248804783529579, -76.33211553913280056 ) ) ;
#10387=CARTESIAN_POINT ( 'NONE',  ( 60.56229479663769411, 14.39144051458180051, -47.32503848654899770 ) ) ;
#10390=VECTOR ( 'NONE', #19069, 1000.000000000000000 ) ;
#10391=CARTESIAN_POINT ( 'NONE',  ( 41.33192651172240062, 13.52043771225929980, -5.349971584196499208 ) ) ;
#10392=CARTESIAN_POINT ( 'NONE',  ( 41.74201990413180141, -44.07933325136760061, -4.572451439087529934 ) ) ;
#10394=CARTESIAN_POINT ( 'NONE',  ( 65.04849531401515605, 1.029538923565187059, -17.85480804919157194 ) ) ;
#10395=B_SPLINE_CURVE_WITH_KNOTS ( 'NONE', 3,
 ( #10816, #26775, #51422, #42793, #11333, #50644, #6888, #18403, #27297, #38601, #14994, #31470, #43305, #14478 ),
 .UNSPECIFIED., .F., .F.,
 ( 4, 2, 2, 1, 1, 2, 2, 4 ),
 ( 0.4756219748450489226, 0.6067164811337820707, 0.6722637342781461189, 0.7050373608503291978, 0.7214241741364214588, 0.7296175807794663681, 0.7378109874225112774, 1.000000000000000000 ),
 .UNSPECIFIED. ) ;
#10398=LINE ( 'NONE', #2791, #45158 ) ;
#10400=ORIENTED_EDGE ( 'NONE', *, *, #50166, .F. ) ;
#10401=CARTESIAN_POINT ( 'NONE',  ( 14.57450527953789887, -52.55982454884319566, -76.04476946176040997 ) ) ;
#10403=VECTOR ( 'NONE', #13910, 1000.000000000000000 ) ;
#10404=CARTESIAN_POINT ( 'NONE',  ( 57.55751162087899786, 19.37927774188059971, -53.76309025933280594 ) ) ;
#10409=CARTESIAN_POINT ( 'NONE',  ( 46.89823403300989924, -54.16139584019150277, -75.66073271794819277 ) ) ;
#10414=CARTESIAN_POINT ( 'NONE',  ( 48.19306574706310897, 22.95973674188289948, -54.68274065309989851 ) ) ;
#10415=ORIENTED_EDGE ( 'NONE', *, *, #49170, .F. ) ;
#10420=DIRECTION ( 'NONE',  ( -1.000000000000000000, 0.000000000000000000, 0.000000000000000000 ) ) ;
#10422=ADVANCED_FACE ( 'NONE', ( #47543 ), #23905, .F. ) ;
#10423=FACE_OUTER_BOUND ( 'NONE', #47002, .T. ) ;
#10424=CARTESIAN_POINT ( 'NONE',  ( 53.18037562183940281, 17.96329376868539995, -26.81634874583109962 ) ) ;
#10431=AXIS2_PLACEMENT_3D ( 'NONE', #33576, #9237, #8973 ) ;
#10434=CARTESIAN_POINT ( 'NONE',  ( 11.92574115021280079, -64.84651890715629463, -16.17905523991749916 ) ) ;
#10435=DIRECTION ( 'NONE',  ( 0.5685928097855380559, -0.5944782866685500711, -0.5685928097855370567 ) ) ;
#10439=ORIENTED_EDGE ( 'NONE', *, *, #30870, .T. ) ;
#10442=AXIS2_PLACEMENT_3D ( 'NONE', #30178, #46198, #10282 ) ;
#10443=CARTESIAN_POINT ( 'NONE',  ( 52.94229166988520063, 18.29346755790560053, -48.62158860753390144 ) ) ;
#10444=CARTESIAN_POINT ( 'NONE',  ( 63.51857099600739787, -1.340451266368759775, -16.28959496159560061 ) ) ;
#10445=CARTESIAN_POINT ( 'NONE',  ( 50.72813273197049710, -50.14449156618339742, -76.16412224154011312 ) ) ;
#10446=CARTESIAN_POINT ( 'NONE',  ( 56.85281608942280229, -50.03689262213919875, -52.32211952640530228 ) ) ;
#10447=AXIS2_PLACEMENT_3D ( 'NONE', #14348, #15129, #11203 ) ;
#10448=ORIENTED_EDGE ( 'NONE', *, *, #10867, .T. ) ;
#10450=CARTESIAN_POINT ( 'NONE',  ( 68.13393739769706769, 17.98087126524489321, -74.20351669811762463 ) ) ;
#10451=ORIENTED_EDGE ( 'NONE', *, *, #8533, .F. ) ;
#10456=CARTESIAN_POINT ( 'NONE',  ( 12.94104881845139943, -50.63124966762359946, -21.36191658295230411 ) ) ;
#10457=CARTESIAN_POINT ( 'NONE',  ( 55.79982945748940182, 19.45001043779030070, -75.57654528039118702 ) ) ;
#10459=CARTESIAN_POINT ( 'NONE',  ( 47.51349502337109953, -54.40873673668700405, -74.95072482230889932 ) ) ;
#10460=CARTESIAN_POINT ( 'NONE',  ( 56.63496331945069784, 14.03594713436370078, -17.14577433238509840 ) ) ;
#10462=CARTESIAN_POINT ( 'NONE',  ( 82.24885268122095283, 13.88381105532070059, -46.39515304430425147 ) ) ;
#10465=VERTEX_POINT ( 'NONE', #27093 ) ;
#10467=CARTESIAN_POINT ( 'NONE',  ( 46.52265252981779753, 21.89525509478169951, -76.13729948142909620 ) ) ;
#10474=EDGE_CURVE ( 'NONE', #33592, #51185, #34678, .T. ) ;
#10475=CARTESIAN_POINT ( 'NONE',  ( 82.13853704237929776, 14.41618746881323965, -47.73077426926469968 ) ) ;
#10477=CARTESIAN_POINT ( 'NONE',  ( 52.66500432174891699, 18.87072468935784642, -77.26040935145131527 ) ) ;
#10482=CARTESIAN_POINT ( 'NONE',  ( -17.94291051752509958, 20.26287486693599860, -52.69725456403749320 ) ) ;
#10484=CARTESIAN_POINT ( 'NONE',  ( 52.94725100682300223, -49.60502802665939726, -48.86448480421770313 ) ) ;
#10488=CARTESIAN_POINT ( 'NONE',  ( 13.95360802883759987, 19.96225614441449991, -22.78639309220759657 ) ) ;
#10489=CARTESIAN_POINT ( 'NONE',  ( 56.78892056362640517, 14.01480988326609811, -25.36526022269899983 ) ) ;
#10492=CARTESIAN_POINT ( 'NONE',  ( 53.58092488844219758, 18.16693936222939953, -49.20716744093490291 ) ) ;
#10493=CARTESIAN_POINT ( 'NONE',  ( 55.62883302160090437, -45.78101872142640616, -16.58062561592149819 ) ) ;
#10494=CYLINDRICAL_SURFACE ( 'NONE', #2099, 2.999999999999942712 ) ;
#10499=CARTESIAN_POINT ( 'NONE',  ( 9.984444803807511093, 33.07180274346050197, -46.65389492738129462 ) ) ;
#10509=CARTESIAN_POINT ( 'NONE',  ( 10.49276773230469928, -63.30748148486130589, -45.62583636195460457 ) ) ;
#10513=FACE_OUTER_BOUND ( 'NONE', #44871, .T. ) ;
#10514=CARTESIAN_POINT ( 'NONE',  ( 52.78679726808729811, 19.08802767016269897, -76.98734330701118722 ) ) ;
#10515=ORIENTED_EDGE ( 'NONE', *, *, #28540, .T. ) ;
#10520=EDGE_CURVE ( 'NONE', #28130, #42929, #6442, .T. ) ;
#10521=B_SPLINE_SURFACE_WITH_KNOTS ( 'NONE', 3, 3, ( 
 ( #34331, #35112, #6844, #30660, #46684, #10252 ),
 ( #46943, #50348, #6576, #30403, #26997, #43003 ),
 ( #51112, #46165, #10771, #22539, #22793, #38813 ),
 ( #18874, #31170, #19133, #50080, #26211, #34596 ),
 ( #6321, #7100, #14433, #27246, #47197, #22018 ),
 ( #18104, #38030, #34071, #11284, #2649, #34857 ),
 ( #18353, #50856, #38550, #23051, #26729, #46425 ),
 ( #22278, #11029, #42747, #26470, #39072, #14949 ),
 ( #43262, #2123, #14175, #38288, #18618, #2378 ),
 ( #50601, #19650, #21121, #44019, #6, #15983 ),
 ( #25034, #32902, #35643, #27767, #15722, #13033 ),
 ( #51628, #4178, #49192, #37123, #1219, #47958 ),
 ( #15472, #28986, #23298, #39319, #43509, #11545 ),
 ( #31937, #31423, #44985, #5165, #9086, #31679 ),
 ( #36858, #47702, #35891, #41053, #12061, #3680 ),
 ( #17210, #28012, #8121, #33170, #3423, #24066 ) ),
 .UNSPECIFIED., .F., .F., .F.,
 ( 4, 2, 2, 2, 2, 2, 2, 4 ),
 ( 4, 1, 1, 4 ),
 ( 0.2986826642956370015, 0.3113669960630360278, 0.6672149915636490514, 0.8896199887515309213, 1.000822487345470080, 1.178746485095780061, 1.463424881496269814, 1.779239977503060066 ),
 ( 0.000000000000000000, 0.3333333333333329818, 0.6666666666666670737, 1.000000000000000000 ),
 .UNSPECIFIED. ) ;
#10523=ADVANCED_FACE ( 'NONE', ( #38908 ), #18020, .T. ) ;
#10531=CARTESIAN_POINT ( 'NONE',  ( 13.50448204009659925, 20.38750180725810068, -74.54610039094001195 ) ) ;
#10532=CYLINDRICAL_SURFACE ( 'NONE', #2227, 2.000000000000040856 ) ;
#10533=EDGE_CURVE ( 'NONE', #9855, #9438, #47893, .T. ) ;
#10534=CARTESIAN_POINT ( 'NONE',  ( 41.12837288530710111, -45.19325662561399781, -5.806229973785479892 ) ) ;
#10540=CARTESIAN_POINT ( 'NONE',  ( 53.34500566076300032, -49.01310193610019894, -26.65466145037910195 ) ) ;
#10541=AXIS2_PLACEMENT_3D ( 'NONE', #33202, #32668, #49220 ) ;
#10542=CARTESIAN_POINT ( 'NONE',  ( 55.66015518744840307, -50.79683962258500429, -75.28107449616210545 ) ) ;
#10543=CARTESIAN_POINT ( 'NONE',  ( 12.28762636745939929, 33.23782178623170580, -15.69519614581730060 ) ) ;
#10546=PLANE ( 'NONE',  #26506 ) ;
#10548=CARTESIAN_POINT ( 'NONE',  ( -6.924872749838059782, -45.82389030641969896, -4.775471299587530360 ) ) ;
#10549=CARTESIAN_POINT ( 'NONE',  ( 47.50940371821619834, 23.35937273273760084, -54.84160031900390209 ) ) ;
#10550=CYLINDRICAL_SURFACE ( 'NONE', #44622, 1.999999999999997335 ) ;
#10552=CARTESIAN_POINT ( 'NONE',  ( 57.48608977619462479, 13.88381019371527358, -25.33088771662052352 ) ) ;
#10553=CARTESIAN_POINT ( 'NONE',  ( 11.63839622733459933, 33.75269855431290011, -16.51998659929800084 ) ) ;
#10554=CARTESIAN_POINT ( 'NONE',  ( 51.79630865696839948, 18.05475250901589845, -76.98491570867250289 ) ) ;
#10555=CARTESIAN_POINT ( 'NONE',  ( 52.86217581337979965, 18.41155708171960015, -48.67083718181420693 ) ) ;
#10556=CARTESIAN_POINT ( 'NONE',  ( 19.36032775985367138, 24.25318110953120510, -75.71503644620106854 ) ) ;
#10557=CARTESIAN_POINT ( 'NONE',  ( 16.13393739769620083, -15.61618894467929941, -15.76422791930239953 ) ) ;
#10558=CARTESIAN_POINT ( 'NONE',  ( 56.55526382498660354, 14.97959948432539967, -26.26696731187869815 ) ) ;
#10559=CARTESIAN_POINT ( 'NONE',  ( 49.93953522581040261, 22.20567224523410133, -54.35118285553540574 ) ) ;
#10561=CARTESIAN_POINT ( 'NONE',  ( 52.56521937542130019, 18.62941943741099848, -48.47378147059570352 ) ) ;
#10562=CARTESIAN_POINT ( 'NONE',  ( 60.34831028877889736, -45.11618894467940066, -11.22201639935360085 ) ) ;
#10564=CARTESIAN_POINT ( 'NONE',  ( 10.97767197991529997, 31.88305279702909800, -44.74312619248830458 ) ) ;
#10567=CARTESIAN_POINT ( 'NONE',  ( 16.13393739769620083, -15.61618894467929941, -10.44999999999999929 ) ) ;
#10569=VECTOR ( 'NONE', #23462, 1000.000000000000000 ) ;
#10570=CARTESIAN_POINT ( 'NONE',  ( 12.65210637300620533, 24.23198390231812027, -75.47957398526430950 ) ) ;
#10571=ORIENTED_EDGE ( 'NONE', *, *, #40387, .T. ) ;
#10574=CARTESIAN_POINT ( 'NONE',  ( 76.80229243761525026, 9.607667892824617084, -14.53004134039231054 ) ) ;
#10577=CARTESIAN_POINT ( 'NONE',  ( 12.87764532066540113, -65.50708823514179358, -47.55684977079440046 ) ) ;
#10578=CARTESIAN_POINT ( 'NONE',  ( 57.19388132582110273, -45.22028251464379878, -25.72059501569479778 ) ) ;
#10581=EDGE_LOOP ( 'NONE', ( #23735, #51053, #1152 ) ) ;
#10582=DIRECTION ( 'NONE',  ( 0.006865953067580490843, 0.7399621225138561798, -0.6726134966927608261 ) ) ;
#10584=AXIS2_PLACEMENT_3D ( 'NONE', #30877, #27212, #51340 ) ;
#10585=CARTESIAN_POINT ( 'NONE',  ( 10.64863409883700029, 32.21085600226960111, -23.66469670114080159 ) ) ;
#10590=CARTESIAN_POINT ( 'NONE',  ( 14.24082757525529885, 19.87036215778640269, -22.22799665057820206 ) ) ;
#10592=EDGE_CURVE ( 'NONE', #30733, #2407, #2594, .T. ) ;
#10595=CARTESIAN_POINT ( 'NONE',  ( 47.35703446467029210, -54.65209995708080015, -74.50157339271500234 ) ) ;
#10596=CARTESIAN_POINT ( 'NONE',  ( 83.63329919740728258, -44.53040215208500996, -46.55718455497714103 ) ) ;
#10597=DIRECTION ( 'NONE',  ( 0.000000000000000000, 0.000000000000000000, -1.000000000000000000 ) ) ;
#10598=CARTESIAN_POINT ( 'NONE',  ( 51.98443725223810219, 20.13520455629999972, -75.98853295767520422 ) ) ;
#10599=VECTOR ( 'NONE', #43606, 1000.000000000000000 ) ;
#10600=CARTESIAN_POINT ( 'NONE',  ( 65.30823856897173130, -30.98971297456273177, -16.78605249253913811 ) ) ;
#10605=CARTESIAN_POINT ( 'NONE',  ( -4.080334501795739754, -49.41737491467630150, -7.291472505024230166 ) ) ;
#10606=CARTESIAN_POINT ( 'NONE',  ( 76.51282310243020390, -29.88146092617099825, -13.28268384058759999 ) ) ;
#10607=DIRECTION ( 'NONE',  ( 0.000000000000000000, 3.054848041326975067E-12, -1.000000000000000000 ) ) ;
#10609=CARTESIAN_POINT ( 'NONE',  ( 19.93042841486727923, -55.43540767232475730, -75.02878472486347050 ) ) ;
#10612=DIRECTION ( 'NONE',  ( 0.000000000000000000, 0.000000000000000000, -1.000000000000000000 ) ) ;
#10614=CARTESIAN_POINT ( 'NONE',  ( 41.85352073560179775, 12.59900291848219922, -4.272019243654880505 ) ) ;
#10615=CARTESIAN_POINT ( 'NONE',  ( 47.64143404728118014, -54.53488714831495798, -74.17417149932109055 ) ) ;
#10618=CARTESIAN_POINT ( 'NONE',  ( 57.55751162087899786, 18.85811933572220056, -52.57651812407429759 ) ) ;
#10619=CARTESIAN_POINT ( 'NONE',  ( 75.97446932798683861, -43.32575349481732019, -13.61806422801180005 ) ) ;
#10620=CARTESIAN_POINT ( 'NONE',  ( 18.02758775305530037, -52.17195122215589720, -75.81086730487160708 ) ) ;
#10621=CARTESIAN_POINT ( 'NONE',  ( 52.30020358789180079, -52.26933069182599212, -53.48872967491809760 ) ) ;
#10627=FACE_OUTER_BOUND ( 'NONE', #6353, .T. ) ;
#10631=CARTESIAN_POINT ( 'NONE',  ( 41.30043219516269914, -45.59471617425819545, -6.243955610188449690 ) ) ;
#10632=ORIENTED_EDGE ( 'NONE', *, *, #37930, .T. ) ;
#10633=EDGE_LOOP ( 'NONE', ( #38717, #12669, #42907, #35563, #5110 ) ) ;
#10635=ORIENTED_EDGE ( 'NONE', *, *, #2069, .T. ) ;
#10637=CARTESIAN_POINT ( 'NONE',  ( 61.24171035206370561, -45.28669213153539630, -47.00360896229330621 ) ) ;
#10639=CARTESIAN_POINT ( 'NONE',  ( 82.71777775636080321, -45.49271782872658321, -47.55444199374405656 ) ) ;
#10642=VERTEX_POINT ( 'NONE', #5750 ) ;
#10648=CARTESIAN_POINT ( 'NONE',  ( 51.83018430297099854, -50.77522728973830368, -76.24313691376478630 ) ) ;
#10649=CARTESIAN_POINT ( 'NONE',  ( 60.58781920018089551, 14.36667126140370065, -47.22968683208149088 ) ) ;
#10652=CARTESIAN_POINT ( 'NONE',  ( 42.87450601165679842, -42.77519057968400062, -3.882344406266829751 ) ) ;
#10653=CARTESIAN_POINT ( 'NONE',  ( 65.17764324051411506, 0.4654656955129265472, -17.21758742400660580 ) ) ;
#10661=CARTESIAN_POINT ( 'NONE',  ( 14.95914443809330052, -52.95108609461500748, -76.14999999999999147 ) ) ;
#10662=CARTESIAN_POINT ( 'NONE',  ( 57.48430709216129486, 19.22299575600860067, -53.13654412953230377 ) ) ;
#10666=CARTESIAN_POINT ( 'NONE',  ( 11.67619942398430055, 33.65927571709689659, -45.08494251881550241 ) ) ;
#10668=DIRECTION ( 'NONE',  ( 0.3294064756440788777, -0.9441882088883267743, 0.000000000000000000 ) ) ;
#10670=CARTESIAN_POINT ( 'NONE',  ( 47.75973331525239729, -54.48449617083259966, -55.18290192981469744 ) ) ;
#10672=CARTESIAN_POINT ( 'NONE',  ( -5.673894890943248726, -46.74181062968316525, -4.529014140242093589 ) ) ;
#10673=CARTESIAN_POINT ( 'NONE',  ( 48.07327434400980337, 23.08200056603829964, -54.91761349180919893 ) ) ;
#10674=EDGE_LOOP ( 'NONE', ( #21833, #6180 ) ) ;
#10677=B_SPLINE_SURFACE_WITH_KNOTS ( 'NONE', 3, 3, ( 
 ( #15761, #31714, #43801, #23848, #4473, #32740, #36430, #48768, #538, #28567, #12342, #12095, #16524, #21218 ),
 ( #24363, #28050, #4216, #20190, #32473, #25148, #40123, #37229, #47995, #16272, #40892, #28828, #41152, #36180 ),
 ( #28306, #36690, #4733, #32225, #24102, #5003, #40634, #1326, #44053, #8416, #44833, #31975, #9196, #45088 ),
 ( #12605, #8938, #287, #40376, #44567, #5266, #20700, #48248, #20442, #8158, #12872, #44307, #791, #33010 ),
 ( #49033, #24881, #13141, #16792, #48503, #29090, #8668, #20963, #24623, #36963, #1061, #17057, #37743, #42461 ),
 ( #34309, #22254, #29349, #6036, #5773, #9706, #49557, #1841, #17819, #26445, #33793, #50055, #37481, #49293 ),
 ( #38261, #41409, #6548, #13644, #21993, #41936, #17570, #9457, #42198, #25921, #38524, #45354, #45607, #14150 ),
 ( #46401, #30376, #38003, #49802, #46138, #5527, #25666, #29853, #10489, #2101, #1581, #21736, #22513, #34045 ),
 ( #18077, #18328, #41668, #50322, #10229, #14408, #30119, #33539, #17314, #33278, #26187, #13391, #6296, #13895 ) ),
 .UNSPECIFIED., .F., .F., .F.,
 ( 4, 1, 1, 1, 1, 1, 4 ),
 ( 4, 2, 2, 2, 2, 2, 4 ),
 ( -1.457552082500000009E-05, 0.1666666666666670182, 0.3333333333333329818, 0.5000000000000000000, 0.6666666666666670737, 0.8333333333333330373, 1.000000000000000000 ),
 ( -0.9973649408979550213, -0.8379246112468560215, -0.6064737235837710516, -0.4618169187943430010, -0.3171601140049140066, -0.03213823312263499460, 0.07935366520894500397 ),
 .UNSPECIFIED. ) ;
#10681=CARTESIAN_POINT ( 'NONE',  ( 61.13393739769620083, -43.11618894467930119, -84.38499399519520239 ) ) ;
#10685=CARTESIAN_POINT ( 'NONE',  ( 37.33393739769619657, -15.61618894467929941, -10.44999999999999929 ) ) ;
#10691=CARTESIAN_POINT ( 'NONE',  ( 12.26572565712860019, -64.61660037486478814, -15.83807272483589834 ) ) ;
#10694=CARTESIAN_POINT ( 'NONE',  ( 10.68300311294020055, -64.60342289521591397, -46.54418054629820034 ) ) ;
#10696=VERTEX_POINT ( 'NONE', #19852 ) ;
#10698=CARTESIAN_POINT ( 'NONE',  ( 82.35517546691707480, -45.10830561011249529, -46.40108830999478329 ) ) ;
#10699=CARTESIAN_POINT ( 'NONE',  ( 52.57890812028310279, -49.84736177554090375, -48.49303208760839823 ) ) ;
#10700=EDGE_CURVE ( 'NONE', #50146, #24819, #15932, .T. ) ;
#10701=CARTESIAN_POINT ( 'NONE',  ( 52.74869365736800120, 18.89386278705310218, -49.96575957230339782 ) ) ;
#10703=CARTESIAN_POINT ( 'NONE',  ( 50.84617524815230638, -48.84160893671730008, -76.31370213948670767 ) ) ;
#10704=ADVANCED_FACE ( 'NONE', ( #24015 ), #14268, .T. ) ;
#10705=CARTESIAN_POINT ( 'NONE',  ( 59.87419911194779587, -46.57917323255409769, -48.56273897241279514 ) ) ;
#10708=DIRECTION ( 'NONE',  ( 0.1686178020941689892, 0.6660492713794449182, -0.7265992051412129005 ) ) ;
#10710=FACE_OUTER_BOUND ( 'NONE', #24595, .T. ) ;
#10713=CARTESIAN_POINT ( 'NONE',  ( 13.58983010028589966, -51.22113851962519959, -22.27008681093980158 ) ) ;
#10714=CARTESIAN_POINT ( 'NONE',  ( 47.46038822159390236, -54.33963646450610696, -75.12137911381070410 ) ) ;
#10715=CARTESIAN_POINT ( 'NONE',  ( 56.29010337146409881, 14.04964247742699968, -16.36031652423400118 ) ) ;
#10716=CARTESIAN_POINT ( 'NONE',  ( 10.14913760601130122, 32.10609558527020369, -45.99399621147029649 ) ) ;
#10717=CARTESIAN_POINT ( 'NONE',  ( 56.87125376272950206, -50.65201878316320006, -53.85479923535680058 ) ) ;
#10722=CARTESIAN_POINT ( 'NONE',  ( 46.88052044270690288, 22.39196474760659683, -75.96172452672209374 ) ) ;
#10725=EDGE_CURVE ( 'NONE', #6259, #10739, #14757, .T. ) ;
#10726=CARTESIAN_POINT ( 'NONE',  ( 43.24976358433020351, -46.00069318273389740, -7.760792318163260539 ) ) ;
#10728=CARTESIAN_POINT ( 'NONE',  ( 74.93037820153030282, 13.88381105528979909, -15.31096251095349992 ) ) ;
#10730=DIRECTION ( 'NONE',  ( 0.9200120562340469155, 0.3918900565005459247, 8.326672684688669123E-17 ) ) ;
#10731=LINE ( 'NONE', #26685, #28457 ) ;
#10732=CARTESIAN_POINT ( 'NONE',  ( 52.75990468010462564, 18.93640155443588213, -77.25922080063452313 ) ) ;
#10733=DIRECTION ( 'NONE',  ( 1.000000000000000000, 0.000000000000000000, 0.000000000000000000 ) ) ;
#10736=CARTESIAN_POINT ( 'NONE',  ( -0.08095109960242620473, 30.16966275033259848, -48.64221216126279757 ) ) ;
#10738=CARTESIAN_POINT ( 'NONE',  ( 52.75620357935920168, -49.71340975552000430, -48.74712242243199967 ) ) ;
#10739=VERTEX_POINT ( 'NONE', #8845 ) ;
#10742=CARTESIAN_POINT ( 'NONE',  ( 13.61605761131730041, 20.15014681539719987, -22.70458626188970186 ) ) ;
#10745=DIRECTION ( 'NONE',  ( 0.000000000000000000, 0.000000000000000000, -1.000000000000000000 ) ) ;
#10746=CARTESIAN_POINT ( 'NONE',  ( 53.41300596567459280, 18.22585793593439618, -49.19565812895479695 ) ) ;
#10747=CARTESIAN_POINT ( 'NONE',  ( 55.40266554404109911, -45.95720592209579536, -16.47441024969080203 ) ) ;
#10751=B_SPLINE_CURVE_WITH_KNOTS ( 'NONE', 3,
 ( #32184, #29050, #41112, #4172, #36387, #48200, #31932, #17016 ),
 .UNSPECIFIED., .F., .F.,
 ( 4, 2, 2, 4 ),
 ( 0.5031119562093512299, 0.6273339671570132836, 0.7515559781046754484, 1.000000000000000000 ),
 .UNSPECIFIED. ) ;
#10752=B_SPLINE_CURVE_WITH_KNOTS ( 'NONE', 3,
 ( #39666, #3774, #36231, #19740, #35733, #51716 ),
 .UNSPECIFIED., .F., .F.,
 ( 4, 2, 4 ),
 ( 0.2774707949478909530, 0.5953712600656003717, 1.000000000000000000 ),
 .UNSPECIFIED. ) ;
#10754=CARTESIAN_POINT ( 'NONE',  ( 10.75750387234210059, 33.63386303445160053, -46.91033328174970052 ) ) ;
#10756=B_SPLINE_CURVE_WITH_KNOTS ( 'NONE', 3,
 ( #564, #12369, #40146, #32251, #12635, #24389, #23620, #51690, #11871, #44080, #48273, #44333, #51439, #39900 ),
 .UNSPECIFIED., .F., .F.,
 ( 4, 2, 2, 2, 2, 2, 4 ),
 ( -8.605215961916560019, -8.065295816869170409, -6.871057665605490250, -6.124658821065700032, -5.378259976525890274, -4.302607981395680348, -4.009099514081210458 ),
 .UNSPECIFIED. ) ;
#10757=CARTESIAN_POINT ( 'NONE',  ( 11.92216765568469761, -65.43848403456330232, -17.95790456665970325 ) ) ;
#10758=CARTESIAN_POINT ( 'NONE',  ( 53.36496928958640495, 18.14812949222240235, -48.76946463831470169 ) ) ;
#10762=CARTESIAN_POINT ( 'NONE',  ( 47.18324681005260146, -54.80726426785999905, -54.61059023070370699 ) ) ;
#10766=CARTESIAN_POINT ( 'NONE',  ( 10.13805148651129961, -63.16689821662900783, -45.99545731505420321 ) ) ;
#10769=ORIENTED_EDGE ( 'NONE', *, *, #14598, .F. ) ;
#10771=CARTESIAN_POINT ( 'NONE',  ( 57.28557293208299939, 19.34652869517200102, -53.44460714490739406 ) ) ;
#10772=CARTESIAN_POINT ( 'NONE',  ( 52.38320845594909514, 19.05065453847920054, -76.75839862161949156 ) ) ;
#10773=ORIENTED_EDGE ( 'NONE', *, *, #49, .F. ) ;
#10774=EDGE_CURVE ( 'NONE', #44502, #9603, #49136, .T. ) ;
#10777=CARTESIAN_POINT ( 'NONE',  ( 83.62685953798910532, -44.53601850760680492, -46.55427990986279241 ) ) ;
#10778=PLANE ( 'NONE',  #49631 ) ;
#10785=CARTESIAN_POINT ( 'NONE',  ( 59.34499803081114777, -2.440885846858634078, -15.68015151901639648 ) ) ;
#10790=CARTESIAN_POINT ( 'NONE',  ( 45.90332635223469993, -45.11618894461400231, -7.776724400097649870 ) ) ;
#10791=EDGE_CURVE ( 'NONE', #22762, #36880, #15408, .T. ) ;
#10793=CARTESIAN_POINT ( 'NONE',  ( 41.72084690663209727, -44.94167883794940366, -5.743073974472929777 ) ) ;
#10799=CARTESIAN_POINT ( 'NONE',  ( 53.99835063712060190, -51.20425914811980306, -75.55396929121511107 ) ) ;
#10800=CARTESIAN_POINT ( 'NONE',  ( -2.478971262080560400, 19.85746904953009917, -8.032436426861050194 ) ) ;
#10802=CARTESIAN_POINT ( 'NONE',  ( 49.60431418108288426, 21.56000271588285955, -52.10968937064622963 ) ) ;
#10804=CARTESIAN_POINT ( 'NONE',  ( 13.88455142272560039, 20.94377921756336036, -75.56421430877985301 ) ) ;
#10805=CARTESIAN_POINT ( 'NONE',  ( 47.60546839679840758, 23.29237299805700090, -54.74821169702579482 ) ) ;
#10807=CARTESIAN_POINT ( 'NONE',  ( 41.60145709364243061, -44.81526105809438576, -5.503720813836787684 ) ) ;
#10808=CARTESIAN_POINT ( 'NONE',  ( 84.02702888070515996, -44.63621333882932873, -47.45289756505584933 ) ) ;
#10809=CARTESIAN_POINT ( 'NONE',  ( 61.15817508718350126, 14.37771941245649998, -47.69147225523349931 ) ) ;
#10810=CARTESIAN_POINT ( 'NONE',  ( 12.02928806124960026, 34.13296712403600708, -17.22609667956750101 ) ) ;
#10812=CARTESIAN_POINT ( 'NONE',  ( 52.83531650484950148, 18.42562942600509857, -48.55819829956829636 ) ) ;
#10813=DIRECTION ( 'NONE',  ( -0.4640893551880601597, 0.8857883891771953788, 0.000000000000000000 ) ) ;
#10815=CARTESIAN_POINT ( 'NONE',  ( 56.29817967269709555, 14.91712830013440083, -26.17903964292329988 ) ) ;
#10816=CARTESIAN_POINT ( 'NONE',  ( 50.95940558857264335, 4.060833044306336070, -76.37898308257572921 ) ) ;
#10818=CARTESIAN_POINT ( 'NONE',  ( 12.13696592144739839, -65.16745155981689663, -16.64705455763589725 ) ) ;
#10821=CARTESIAN_POINT ( 'NONE',  ( 10.48644968250219911, 31.91257630746710561, -45.62816686667009947 ) ) ;
#10823=CARTESIAN_POINT ( 'NONE',  ( 12.56262532525460074, -39.78532101326960202, -74.14999999999999147 ) ) ;
#10824=CARTESIAN_POINT ( 'NONE',  ( 12.40077008615062404, 24.20909747964150682, -75.14569893024719249 ) ) ;
#10828=CARTESIAN_POINT ( 'NONE',  ( 76.49445432434755787, -3.248734881417176368, -13.20352109380791461 ) ) ;
#10830=CARTESIAN_POINT ( 'NONE',  ( 12.39116069916539864, -65.38104303664570693, -46.54587262935750402 ) ) ;
#10831=CARTESIAN_POINT ( 'NONE',  ( 56.92567216073919667, -45.20107943371309744, -25.36893163837739706 ) ) ;
#10834=CIRCLE ( 'NONE', #775, 1.999999999999998224 ) ;
#10840=PLANE ( 'NONE',  #50415 ) ;
#10841=CIRCLE ( 'NONE', #47642, 4.959400861452849085 ) ;
#10846=DIRECTION ( 'NONE',  ( -0.4439767838698117641, 0.8960382890170590642, 0.000000000000000000 ) ) ;
#10849=CARTESIAN_POINT ( 'NONE',  ( 62.49253998539199983, -29.48318676728260002, -16.12968574675709732 ) ) ;
#10851=CARTESIAN_POINT ( 'NONE',  ( 47.18783699164220025, -54.49278665692580148, -75.11697231728020085 ) ) ;
#10852=CARTESIAN_POINT ( 'NONE',  ( 49.41736058582200286, 13.88381311221330172, -8.069193831786499516 ) ) ;
#10853=B_SPLINE_CURVE_WITH_KNOTS ( 'NONE', 3,
 ( #8242, #12706, #6847, #14953, #2652, #22796, #35115, #11032, #38819, #23054, #27000, #22024, #18622, #34075, #19136, #14179, #10256, #2908, #18356, #26216, #18108, #38554 ),
 .UNSPECIFIED., .F., .F.,
 ( 4, 2, 2, 2, 2, 2, 2, 2, 2, 2, 4 ),
 ( 0.000000000000000000, 0.09821630342860182550, 0.2339808679556865390, 0.3375000544871513131, 0.4375000462626749687, 0.5000000411223781693, 0.6250000308417832384, 0.7117379798405728542, 0.7984759288393613597, 0.9372566472374248558, 1.000000000000000000 ),
 .UNSPECIFIED. ) ;
#10857=VERTEX_POINT ( 'NONE', #13807 ) ;
#10859=CARTESIAN_POINT ( 'NONE',  ( 4.773425314697229638, -58.71548316886770635, -13.16258282087829912 ) ) ;
#10860=CARTESIAN_POINT ( 'NONE',  ( 76.74972829916860917, 9.566990831016390473, -14.30201763231599976 ) ) ;
#10867=EDGE_CURVE ( 'NONE', #20094, #34780, #28471, .T. ) ;
#10868=VECTOR ( 'NONE', #9201, 1000.000000000000000 ) ;
#10869=CARTESIAN_POINT ( 'NONE',  ( 82.45925359270579236, -45.27638716885540049, -47.17632001488509985 ) ) ;
#10871=CARTESIAN_POINT ( 'NONE',  ( 41.26856152876109718, 13.06989385214870047, -4.473876091761409768 ) ) ;
#10873=CARTESIAN_POINT ( 'NONE',  ( 49.40539548389170221, -53.49785366682009879, -54.15746054660930042 ) ) ;
#10874=CARTESIAN_POINT ( 'NONE',  ( 70.83745409581581498, -49.21324915460289162, -70.54648330188271643 ) ) ;
#10875=EDGE_CURVE ( 'NONE', #12879, #6259, #24742, .T. ) ;
#10877=CARTESIAN_POINT ( 'NONE',  ( 76.38705314788980161, -43.26417677700779763, -13.94855457485863148 ) ) ;
#10878=CARTESIAN_POINT ( 'NONE',  ( 18.45990697330769947, -52.11465364279959545, -75.47164421335219231 ) ) ;
#10879=CARTESIAN_POINT ( 'NONE',  ( 60.34831028877889736, -45.11618894467940066, -11.22201639935360085 ) ) ;
#10880=EDGE_CURVE ( 'NONE', #16411, #29700, #17732, .T. ) ;
#10881=EDGE_LOOP ( 'NONE', ( #6182, #49377, #17694, #43633 ) ) ;
#10886=CARTESIAN_POINT ( 'NONE',  ( 16.13393739769620083, -15.61618894467929941, -11.54999999999999893 ) ) ;
#10890=CARTESIAN_POINT ( 'NONE',  ( 44.57967080629300227, -45.59411579619229826, -8.202780460755210612 ) ) ;
#10891=VERTEX_POINT ( 'NONE', #46566 ) ;
#10892=ORIENTED_EDGE ( 'NONE', *, *, #36955, .T. ) ;
#10893=ORIENTED_EDGE ( 'NONE', *, *, #42079, .F. ) ;
#10896=DIRECTION ( 'NONE',  ( 0.000000000000000000, 1.000000000000000000, 0.000000000000000000 ) ) ;
#10897=EDGE_LOOP ( 'NONE', ( #2128, #31425, #41254, #48885 ) ) ;
#10906=ORIENTED_EDGE ( 'NONE', *, *, #39474, .F. ) ;
#10907=DIRECTION ( 'NONE',  ( 0.000000000000000000, -1.000000000000000000, 0.000000000000000000 ) ) ;
#10908=CARTESIAN_POINT ( 'NONE',  ( 51.41094422139000386, -50.88107716530349478, -76.16757073797020894 ) ) ;
#10910=CARTESIAN_POINT ( 'NONE',  ( 60.86666111963769765, 14.22176795161809970, -47.11612196671629960 ) ) ;
#10913=CARTESIAN_POINT ( 'NONE',  ( 41.39168606550949647, -44.20447096405560217, -4.419064217266010175 ) ) ;
#10915=CARTESIAN_POINT ( 'NONE',  ( -2.895883735633389744, 17.91114786048130014, -5.678499123949679372 ) ) ;
#10917=DIRECTION ( 'NONE',  ( -1.224646799147358138E-16, 1.000000000000000000, 6.060292087350919618E-16 ) ) ;
#10918=CARTESIAN_POINT ( 'NONE',  ( 17.84258640648128136, -51.34461569807859860, -75.09855816271016238 ) ) ;
#10921=CARTESIAN_POINT ( 'NONE',  ( 43.81052300022479784, 14.82244714638200023, -8.159011786981970715 ) ) ;
#10924=CARTESIAN_POINT ( 'NONE',  ( 13.95190178771939848, 19.57559525226260178, -21.48693983945959829 ) ) ;
#10928=CARTESIAN_POINT ( 'NONE',  ( 48.07907502642350295, -54.29565632080440452, -54.84628907412789545 ) ) ;
#10930=ADVANCED_FACE ( 'NONE', ( #38425 ), #14318, .T. ) ;
#10931=CARTESIAN_POINT ( 'NONE',  ( -7.651755816028718904, -45.25221342046138773, -4.961742080343907624 ) ) ;
#10932=CARTESIAN_POINT ( 'NONE',  ( 47.71148510080310245, 23.26888792098559833, -55.04989704333419809 ) ) ;
#10934=ORIENTED_EDGE ( 'NONE', *, *, #41452, .T. ) ;
#10936=VERTEX_POINT ( 'NONE', #21390 ) ;
#10938=AXIS2_PLACEMENT_3D ( 'NONE', #35246, #22142, #38153 ) ;
#10940=CARTESIAN_POINT ( 'NONE',  ( 57.45452828658709876, -47.23787284142349563, -47.71980555553449932 ) ) ;
#10944=CIRCLE ( 'NONE', #51816, 38.61618927352878927 ) ;
#10945=CARTESIAN_POINT ( 'NONE',  ( 16.13393739769309931, -15.61618894467859953, -3.187564294432039702 ) ) ;
#10948=B_SPLINE_SURFACE_WITH_KNOTS ( 'NONE', 3, 3, ( 
 ( #14628, #5734, #41895, #10446, #2316, #37963, #26399, #30337, #5992, #49764, #30595, #14369 ),
 ( #17779, #34007, #2580, #46878, #34789, #18809, #46360, #38221, #13856, #10705, #21693, #37701 ),
 ( #42420, #21953, #2061, #50284, #29813, #42680, #34530, #50795, #46616, #46099, #38480, #26658 ),
 ( #6776, #9918, #18038, #6511, #30848, #10184, #22471, #18555, #26145, #25880, #1796, #14883 ),
 ( #10965, #22727, #50017, #42156, #38750, #14107, #30075, #26930, #33750, #45830, #22212, #6254 ),
 ( #50536, #18288, #2843, #34260, #7803, #11485, #39515, #23239, #22985, #27443, #32839, #48604 ) ),
 .UNSPECIFIED., .F., .F., .F.,
 ( 4, 1, 1, 4 ),
 ( 4, 2, 2, 2, 2, 4 ),
 ( -5.656587004999999529E-06, 0.3333333333333329818, 0.6666666666666670737, 1.000000000000000000 ),
 ( -8.926961658285021528, -8.407199725736200335, -7.356299760019170186, -5.674859814871930475, -2.984555902636349956, -0.2480234047818090093 ),
 .UNSPECIFIED. ) ;
#10950=FACE_OUTER_BOUND ( 'NONE', #31861, .T. ) ;
#10951=EDGE_LOOP ( 'NONE', ( #36004, #9394, #44241, #25462 ) ) ;
#10953=CARTESIAN_POINT ( 'NONE',  ( 12.00872700125690073, -64.88650295836660575, -16.20508613916799945 ) ) ;
#10956=CARTESIAN_POINT ( 'NONE',  ( 11.81871210215889967, -65.31307805416919621, -47.30065584137410184 ) ) ;
#10957=ORIENTED_EDGE ( 'NONE', *, *, #45969, .T. ) ;
#10961=CARTESIAN_POINT ( 'NONE',  ( 57.05132883896109774, 14.65902881311749972, -26.24859059622079727 ) ) ;
#10963=ADVANCED_FACE ( 'NONE', ( #17480 ), #22629, .T. ) ;
#10964=CARTESIAN_POINT ( 'NONE',  ( 65.38480309005331037, -0.6329806532248359874, -16.65168329525840107 ) ) ;
#10965=CARTESIAN_POINT ( 'NONE',  ( 56.91683350687570453, -50.66367375722730060, -53.20180161368870131 ) ) ;
#10966=EDGE_LOOP ( 'NONE', ( #29100, #35701, #21824, #29952 ) ) ;
#10968=CYLINDRICAL_SURFACE ( 'NONE', #30927, 1.999999999999996669 ) ;
#10970=CARTESIAN_POINT ( 'NONE',  ( 10.41791033310424375, -64.23844989214747159, -23.06400185344022802 ) ) ;
#10971=CARTESIAN_POINT ( 'NONE',  ( 49.60975479626670648, -45.11618894467940066, -10.01352555637939901 ) ) ;
#10973=CARTESIAN_POINT ( 'NONE',  ( 13.38498534606780055, -51.10135539216639700, -21.91519318942190253 ) ) ;
#10974=CARTESIAN_POINT ( 'NONE',  ( 55.30868802464280520, 19.38381105532069881, -76.41966175253659799 ) ) ;
#10976=CARTESIAN_POINT ( 'NONE',  ( 55.23395345995140104, 14.09343332238140079, -15.21757741273719944 ) ) ;
#10977=CARTESIAN_POINT ( 'NONE',  ( 60.76024220928780295, -45.50591669753300295, -47.06490144688479660 ) ) ;
#10978=AXIS2_PLACEMENT_3D ( 'NONE', #21735, #25664, #16791 ) ;
#10980=CARTESIAN_POINT ( 'NONE',  ( 56.83258908092710016, -50.30522036972260480, -52.72698303625519856 ) ) ;
#10985=VERTEX_POINT ( 'NONE', #6592 ) ;
#10986=CARTESIAN_POINT ( 'NONE',  ( 47.52155195348809968, 23.26505193837810026, -74.72489557265679139 ) ) ;
#10989=DIRECTION ( 'NONE',  ( -0.2260571801428161443, 1.249000902703300615E-16, 0.9741140340359945027 ) ) ;
#10991=CARTESIAN_POINT ( 'NONE',  ( 82.33636559101309160, 14.30306463946360118, -47.60086789927839845 ) ) ;
#10994=ADVANCED_FACE ( 'NONE', ( #51138 ), #9313, .T. ) ;
#10996=CARTESIAN_POINT ( 'NONE',  ( 49.57944902481020222, 22.47411269264829770, -55.02902090455440032 ) ) ;
#10998=CARTESIAN_POINT ( 'NONE',  ( 53.40905300656029908, -49.37518268217669970, -48.94487162954590076 ) ) ;
#10999=ORIENTED_EDGE ( 'NONE', *, *, #22869, .F. ) ;
#11002=CARTESIAN_POINT ( 'NONE',  ( 13.72890770306269914, 19.91029111355249626, -22.20512747466040082 ) ) ;
#11005=CARTESIAN_POINT ( 'NONE',  ( 52.73507126972099712, 18.49830744958629936, -48.76328856354190577 ) ) ;
#11006=CARTESIAN_POINT ( 'NONE',  ( 56.28192874346009233, -45.52819744086340137, -17.75909607022310155 ) ) ;
#11007=CARTESIAN_POINT ( 'NONE',  ( 16.36911989528830347, 19.86384299893705574, -15.67312363240488260 ) ) ;
#11012=CARTESIAN_POINT ( 'NONE',  ( 10.53031889316589975, 33.70290473908939788, -47.11352251503090116 ) ) ;
#11016=CARTESIAN_POINT ( 'NONE',  ( 52.62851868536466071, -49.80923738442962900, -48.67162951074862320 ) ) ;
#11020=CARTESIAN_POINT ( 'NONE',  ( 51.80256375288589510, -52.76240455486869507, -54.49703439224219892 ) ) ;
#11024=CARTESIAN_POINT ( 'NONE',  ( 10.14177886503980019, -63.22230780886520307, -45.99369029958189969 ) ) ;
#11025=CARTESIAN_POINT ( 'NONE',  ( 65.43393739769584272, 16.88381105531917825, -74.20000000000047180 ) ) ;
#11027=EDGE_CURVE ( 'NONE', #22139, #26146, #1433, .T. ) ;
#11029=CARTESIAN_POINT ( 'NONE',  ( 56.94659877973650453, 19.40673623115929658, -53.72521299826679808 ) ) ;
#11030=CARTESIAN_POINT ( 'NONE',  ( 54.17317666804649434, 19.38381105980860042, -77.01210127079860968 ) ) ;
#11032=CARTESIAN_POINT ( 'NONE',  ( 9.758904658578256175, -64.50914076886910209, -46.91371261186735353 ) ) ;
#11038=DIRECTION ( 'NONE',  ( 0.000000000000000000, -1.000000000000000000, 0.000000000000000000 ) ) ;
#11040=EDGE_LOOP ( 'NONE', ( #6129, #9651, #18527, #18102, #49119, #3863 ) ) ;
#11041=CARTESIAN_POINT ( 'NONE',  ( 53.35699421374690132, -49.92639189236809472, -74.14999999999999147 ) ) ;
#11043=VECTOR ( 'NONE', #45785, 1000.000000000000114 ) ;
#11044=CARTESIAN_POINT ( 'NONE',  ( 49.90995254736770192, 13.88381105525079917, -10.51652384872640056 ) ) ;
#11048=CARTESIAN_POINT ( 'NONE',  ( 46.03121886948380137, -45.11618894467940066, -7.582877905987319700 ) ) ;
#11049=CARTESIAN_POINT ( 'NONE',  ( 37.33393739769619657, -15.61618894467929941, -12.65000000000000036 ) ) ;
#11053=CARTESIAN_POINT ( 'NONE',  ( 12.11414304660310037, 33.92875631211279597, -16.63763903706830405 ) ) ;
#11056=CARTESIAN_POINT ( 'NONE',  ( 54.96130583373059864, -50.78188363031180330, -75.77346936485569984 ) ) ;
#11057=CARTESIAN_POINT ( 'NONE',  ( -5.707727980563209513, 16.52479455181530099, -7.103282072075530529 ) ) ;
#11061=DIRECTION ( 'NONE',  ( 1.000000000000000000, 0.000000000000000000, 0.000000000000000000 ) ) ;
#11062=EDGE_CURVE ( 'NONE', #26440, #3287, #21488, .T. ) ;
#11063=ORIENTED_EDGE ( 'NONE', *, *, #40499, .F. ) ;
#11064=CARTESIAN_POINT ( 'NONE',  ( 14.04522320185620821, 21.07288667591008391, -75.74021525116319253 ) ) ;
#11066=CARTESIAN_POINT ( 'NONE',  ( 47.58181567201759776, 23.31431080387180188, -54.81048423692320171 ) ) ;
#11067=CARTESIAN_POINT ( 'NONE',  ( 46.03121886948380137, -45.11618894467940066, -7.582877905987319700 ) ) ;
#11070=CARTESIAN_POINT ( 'NONE',  ( 11.41271396217749867, 33.75416681246609585, -16.69425700585249928 ) ) ;
#11072=CARTESIAN_POINT ( 'NONE',  ( 51.21769383437759871, 18.09844762758200076, -76.45366765079749882 ) ) ;
#11073=CARTESIAN_POINT ( 'NONE',  ( 52.83236039598959621, 18.42717821426129987, -48.53480049868939972 ) ) ;
#11075=CARTESIAN_POINT ( 'NONE',  ( 52.96846357502160174, -49.58824783477410136, -48.76456334744820253 ) ) ;
#11076=CARTESIAN_POINT ( 'NONE',  ( 56.24187033329050678, 15.29152766842380018, -26.31653598774670044 ) ) ;
#11077=CARTESIAN_POINT ( 'NONE',  ( 49.44978923146629768, 22.30861604384239882, -54.25462396068649440 ) ) ;
#11078=CARTESIAN_POINT ( 'NONE',  ( 64.31441352423868807, -32.07208572738768027, -17.57633156439366573 ) ) ;
#11079=DIRECTION ( 'NONE',  ( -0.5110015285683607855, -0.4887508954475661693, -0.7071067811865481278 ) ) ;
#11080=CARTESIAN_POINT ( 'NONE',  ( 62.70348755430340049, -30.98672360713329965, -16.57902117255940055 ) ) ;
#11082=CARTESIAN_POINT ( 'NONE',  ( 11.13393739769619906, 32.00438138744689809, -43.91353227418159832 ) ) ;
#11084=EDGE_CURVE ( 'NONE', #22139, #23745, #2922, .T. ) ;
#11085=CARTESIAN_POINT ( 'NONE',  ( 50.95939809116894992, -35.29322421015848477, -76.37898009206955408 ) ) ;
#11087=ORIENTED_EDGE ( 'NONE', *, *, #11824, .F. ) ;
#11088=ORIENTED_EDGE ( 'NONE', *, *, #51596, .F. ) ;
#11090=CARTESIAN_POINT ( 'NONE',  ( 49.99045098147789901, -1.393666479833739702, -15.95592623815259792 ) ) ;
#11091=ORIENTED_EDGE ( 'NONE', *, *, #1783, .F. ) ;
#11093=CARTESIAN_POINT ( 'NONE',  ( 57.46797901588330149, -45.11472323586909994, -25.39910589255679696 ) ) ;
#11098=ORIENTED_EDGE ( 'NONE', *, *, #40702, .T. ) ;
#11103=ORIENTED_EDGE ( 'NONE', *, *, #24509, .F. ) ;
#11108=CARTESIAN_POINT ( 'NONE',  ( 59.28138515986110235, -28.60838227528750011, -15.68089638718410050 ) ) ;
#11109=DIRECTION ( 'NONE',  ( 0.000000000000000000, -1.000000000000000000, 0.000000000000000000 ) ) ;
#11110=CARTESIAN_POINT ( 'NONE',  ( 47.16986572260749710, -54.60797753722280135, -74.94873378728740931 ) ) ;
#11112=ADVANCED_FACE ( 'NONE', ( #50364 ), #21327, .T. ) ;
#11114=CARTESIAN_POINT ( 'NONE',  ( 83.73985275199801492, -44.66878937119359705, -47.11072319708490141 ) ) ;
#11115=CARTESIAN_POINT ( 'NONE',  ( 16.65420337845429799, 19.88381105532299742, -20.15000000000000213 ) ) ;
#11117=ORIENTED_EDGE ( 'NONE', *, *, #4769, .T. ) ;
#11118=CARTESIAN_POINT ( 'NONE',  ( 55.25527325933540368, -47.47676794944560186, -26.53763385803990005 ) ) ;
#11119=CARTESIAN_POINT ( 'NONE',  ( 7.530214027689599909, -59.71025360061080534, -11.77218490757650038 ) ) ;
#11120=CARTESIAN_POINT ( 'NONE',  ( 76.38557192511220251, -34.90188143910140184, -13.09796983512340063 ) ) ;
#11121=CARTESIAN_POINT ( 'NONE',  ( 75.41849744931550958, 12.82902632849465974, -13.61737176862969534 ) ) ;
#11122=CARTESIAN_POINT ( 'NONE',  ( 75.46827467797460542, -43.69088997238642946, -13.44466669527831293 ) ) ;
#11126=CARTESIAN_POINT ( 'NONE',  ( 11.13393739769619906, -55.30245861064819479, -24.15000000000000213 ) ) ;
#11127=CARTESIAN_POINT ( 'NONE',  ( 82.61192755713619817, -45.25363691089199847, -47.15270809369890515 ) ) ;
#11128=CARTESIAN_POINT ( 'NONE',  ( 57.27556706372909900, -50.61618894467930119, -53.86432103813280037 ) ) ;
#11129=CARTESIAN_POINT ( 'NONE',  ( 41.89087154105590116, 12.34395647913080118, -3.657595757375029955 ) ) ;
#11130=EDGE_CURVE ( 'NONE', #34780, #29238, #50615, .T. ) ;
#11131=LINE ( 'NONE', #27098, #34252 ) ;
#11132=CARTESIAN_POINT ( 'NONE',  ( 71.76327752318150033, -45.11618894467940066, -14.40146755345420004 ) ) ;
#11135=CARTESIAN_POINT ( 'NONE',  ( 18.46964007651970263, -51.65733818267800359, -75.17186369576970151 ) ) ;
#11136=CARTESIAN_POINT ( 'NONE',  ( 60.85049484021050148, -43.74509675106619966, -9.364400423546438645 ) ) ;
#11139=ORIENTED_EDGE ( 'NONE', *, *, #22029, .T. ) ;
#11140=CARTESIAN_POINT ( 'NONE',  ( 8.799473741179280495, 31.95986279266500318, -46.67015979934819825 ) ) ;
#11145=CARTESIAN_POINT ( 'NONE',  ( 40.92026923330519850, -45.27152901351649916, -5.766248515459809987 ) ) ;
#11146=ORIENTED_EDGE ( 'NONE', *, *, #5904, .F. ) ;
#11147=CARTESIAN_POINT ( 'NONE',  ( 17.75132308693969918, 20.71403734715240219, -75.77237669558989808 ) ) ;
#11151=ORIENTED_EDGE ( 'NONE', *, *, #8533, .T. ) ;
#11152=EDGE_CURVE ( 'NONE', #14552, #30210, #35006, .T. ) ;
#11157=CARTESIAN_POINT ( 'NONE',  ( 69.63393739769620083, 11.88381105532070059, -71.50000000000000000 ) ) ;
#11162=ORIENTED_EDGE ( 'NONE', *, *, #26788, .T. ) ;
#11164=CIRCLE ( 'NONE', #47973, 3.500000000000003109 ) ;
#11165=CARTESIAN_POINT ( 'NONE',  ( 52.32303883665399979, -51.41740952823399624, -75.90202711987829787 ) ) ;
#11166=CARTESIAN_POINT ( 'NONE',  ( 60.31036077509780569, 14.53093637234490032, -47.43321563248520079 ) ) ;
#11167=ADVANCED_FACE ( 'NONE', ( #45198 ), #38570, .T. ) ;
#11168=EDGE_CURVE ( 'NONE', #9424, #26391, #16615, .T. ) ;
#11172=DIRECTION ( 'NONE',  ( -0.000000000000000000, 1.000000000000000000, 0.000000000000000000 ) ) ;
#11173=CARTESIAN_POINT ( 'NONE',  ( -11.32734370190460105, 10.64934056395049922, -6.430192534648650593 ) ) ;
#11177=ORIENTED_EDGE ( 'NONE', *, *, #19963, .F. ) ;
#11178=CARTESIAN_POINT ( 'NONE',  ( 58.91181031229810117, 15.24198406853699872, -47.44472854892460134 ) ) ;
#11180=CARTESIAN_POINT ( 'NONE',  ( 57.47665759692250020, 19.32680757954669915, -53.44461618367620304 ) ) ;
#11183=CARTESIAN_POINT ( 'NONE',  ( 13.96942586498170158, 19.12044695617580103, -20.94633231277839869 ) ) ;
#11188=CARTESIAN_POINT ( 'NONE',  ( 48.03353091937740516, -54.28691148336039873, -54.73610278459779721 ) ) ;
#11190=CARTESIAN_POINT ( 'NONE',  ( 56.37791565511199821, 19.35890332112400003, -52.96495788585040287 ) ) ;
#11191=LINE ( 'NONE', #35013, #10569 ) ;
#11193=VECTOR ( 'NONE', #38981, 1000.000000000000114 ) ;
#11196=ORIENTED_EDGE ( 'NONE', *, *, #20132, .F. ) ;
#11199=CARTESIAN_POINT ( 'NONE',  ( 49.02351734455767485, -53.72042385326151503, -54.35736896012733865 ) ) ;
#11200=CARTESIAN_POINT ( 'NONE',  ( 50.03007040746459921, 17.53271468411620049, -76.14999999999999147 ) ) ;
#11203=DIRECTION ( 'NONE',  ( 0.000000000000000000, 1.000000000000000000, 0.000000000000000000 ) ) ;
#11205=DIRECTION ( 'NONE',  ( -1.000000000000000000, 0.000000000000000000, 0.000000000000000000 ) ) ;
#11207=FACE_OUTER_BOUND ( 'NONE', #2568, .T. ) ;
#11209=VERTEX_POINT ( 'NONE', #21752 ) ;
#11213=CARTESIAN_POINT ( 'NONE',  ( 10.93697074075429931, -64.96690227797920159, -46.97388299885609797 ) ) ;
#11216=CARTESIAN_POINT ( 'NONE',  ( 12.16981617636240109, -50.04926268091029584, -21.14999999999999858 ) ) ;
#11217=CARTESIAN_POINT ( 'NONE',  ( 56.71680104101439923, 14.84105079357200019, -26.25052735258839931 ) ) ;
#11218=CARTESIAN_POINT ( 'NONE',  ( 56.30185301883670235, -50.62326390979490043, -52.97278795026579701 ) ) ;
#11221=CARTESIAN_POINT ( 'NONE',  ( 61.00510007021379977, -1.210019244661300064, -16.05925380967549998 ) ) ;
#11222=CARTESIAN_POINT ( 'NONE',  ( 51.70526341691190453, -49.35822289825209452, -76.83585704126669214 ) ) ;
#11225=DIRECTION ( 'NONE',  ( 0.000000000000000000, 0.000000000000000000, 1.000000000000000000 ) ) ;
#11231=CARTESIAN_POINT ( 'NONE',  ( 12.98723924364920101, -50.01451381740049840, -21.05373175809789998 ) ) ;
#11234=CARTESIAN_POINT ( 'NONE',  ( 56.21309269942560150, 13.89837739344449830, -15.33240308013389885 ) ) ;
#11235=CARTESIAN_POINT ( 'NONE',  ( 61.02222211035100230, -45.36865808718979309, -46.91825944054690467 ) ) ;
#11241=CARTESIAN_POINT ( 'NONE',  ( 13.39996378792660003, -51.78681560013630047, -74.34711752987760747 ) ) ;
#11244=CARTESIAN_POINT ( 'NONE',  ( 17.91444327278706439, 19.90989047429554404, -74.52173647802152345 ) ) ;
#11247=EDGE_CURVE ( 'NONE', #22605, #45901, #857, .T. ) ;
#11248=CARTESIAN_POINT ( 'NONE',  ( 82.54540508975100011, 13.91912072063600014, -46.85689288513360395 ) ) ;
#11250=CARTESIAN_POINT ( 'NONE',  ( 53.07820085554459411, 19.12200233530915483, -77.22362300132772361 ) ) ;
#11251=CARTESIAN_POINT ( 'NONE',  ( 11.67619456822290047, 33.65927054772580362, -23.88710972541020183 ) ) ;
#11252=EDGE_CURVE ( 'NONE', #13982, #48724, #45965, .T. ) ;
#11254=FACE_OUTER_BOUND ( 'NONE', #18616, .T. ) ;
#11256=CARTESIAN_POINT ( 'NONE',  ( 53.43952110370909736, -49.36024459135060027, -48.94167683225650478 ) ) ;
#11257=EDGE_LOOP ( 'NONE', ( #47712, #13506 ) ) ;
#11260=CARTESIAN_POINT ( 'NONE',  ( 13.87199023920160101, 19.96799697009089769, -22.54889071416870294 ) ) ;
#11261=CARTESIAN_POINT ( 'NONE',  ( 14.19855276898660001, 24.33696219936630101, -76.14999999999999147 ) ) ;
#11264=CARTESIAN_POINT ( 'NONE',  ( 52.89232545687240616, 18.42626852396410086, -48.97387498997640165 ) ) ;
#11265=CARTESIAN_POINT ( 'NONE',  ( 55.29971770016739896, -46.05203773004579659, -16.43383186550930120 ) ) ;
#11266=CARTESIAN_POINT ( 'NONE',  ( 53.46882080935260007, 17.64232885596709721, -26.54419876889340202 ) ) ;
#11268=VECTOR ( 'NONE', #50379, 1000.000000000000000 ) ;
#11271=CARTESIAN_POINT ( 'NONE',  ( 11.94527162332230041, -65.41218007247690025, -17.48520172073260071 ) ) ;
#11272=FACE_OUTER_BOUND ( 'NONE', #37201, .T. ) ;
#11274=DIRECTION ( 'NONE',  ( 1.000000000000000000, 0.000000000000000000, 0.000000000000000000 ) ) ;
#11275=CARTESIAN_POINT ( 'NONE',  ( 53.55176271296412693, -49.41894048401645989, -49.22385363220949017 ) ) ;
#11276=CARTESIAN_POINT ( 'NONE',  ( 11.51160566532390028, -51.12796951774690513, -23.15000000000000213 ) ) ;
#11277=CARTESIAN_POINT ( 'NONE',  ( 53.42313316096070253, -52.07210377827539816, -54.29429654136570349 ) ) ;
#11279=DIRECTION ( 'NONE',  ( -0.000000000000000000, -1.000000000000000000, -0.000000000000000000 ) ) ;
#11280=CARTESIAN_POINT ( 'NONE',  ( 10.49009406874180073, -63.23676620627490053, -45.62574497862269851 ) ) ;
#11281=CARTESIAN_POINT ( 'NONE',  ( 67.04038824939809160, 19.47158195952189885, -72.59354914830210248 ) ) ;
#11282=ORIENTED_EDGE ( 'NONE', *, *, #19161, .F. ) ;
#11283=CARTESIAN_POINT ( 'NONE',  ( 11.13393738245069642, -63.63465678867208197, -43.78329441304022396 ) ) ;
#11284=CARTESIAN_POINT ( 'NONE',  ( 57.07649178892390296, 19.21884141067920027, -53.03413607196730339 ) ) ;
#11290=CARTESIAN_POINT ( 'NONE',  ( 51.98443725223855694, 20.13520455629937445, -75.98853295767540317 ) ) ;
#11300=VERTEX_POINT ( 'NONE', #49024 ) ;
#11301=CYLINDRICAL_SURFACE ( 'NONE', #45963, 2.000000000000003997 ) ;
#11303=CARTESIAN_POINT ( 'NONE',  ( 48.23725916559990168, 13.88381105525269987, -9.350495514648539341 ) ) ;
#11304=CARTESIAN_POINT ( 'NONE',  ( 41.64265090550289727, -46.42699119286240261, -4.296538310234230273 ) ) ;
#11305=CARTESIAN_POINT ( 'NONE',  ( 46.47158024012890110, 21.92595096433829838, -76.13722091323529639 ) ) ;
#11306=VECTOR ( 'NONE', #27026, 1000.000000000000114 ) ;
#11309=CARTESIAN_POINT ( 'NONE',  ( 68.13393739769790614, -49.95860450174040324, -75.14853292321149070 ) ) ;
#11310=CARTESIAN_POINT ( 'NONE',  ( 12.16177399483199828, 33.87933705409069773, -16.53048058984360225 ) ) ;
#11313=CARTESIAN_POINT ( 'NONE',  ( 52.63509980015960110, -49.78733083141809601, -27.75246021167879817 ) ) ;
#11314=CARTESIAN_POINT ( 'NONE',  ( 54.52355283502430439, -50.61618499730730036, -76.78771584484479718 ) ) ;
#11315=CARTESIAN_POINT ( 'NONE',  ( -0.2630675345621850125, 21.64344005583900099, -7.960913005788690988 ) ) ;
#11318=ADVANCED_FACE ( 'NONE', ( #37469 ), #32593, .T. ) ;
#11323=CARTESIAN_POINT ( 'NONE',  ( 47.71564501992030216, 23.23377652775180024, -54.78142672066789487 ) ) ;
#11324=CARTESIAN_POINT ( 'NONE',  ( 57.58883330952520652, -45.77669918862839893, -26.30132602238209927 ) ) ;
#11326=CARTESIAN_POINT ( 'NONE',  ( 61.18397614727650335, 14.12635359917990030, -47.22202979286220170 ) ) ;
#11328=CARTESIAN_POINT ( 'NONE',  ( 51.57818300252989729, 18.30842999037989927, -76.64184120677319356 ) ) ;
#11329=CARTESIAN_POINT ( 'NONE',  ( 52.79916028495409819, 18.44511419399770347, -48.53935649295149801 ) ) ;
#11332=CARTESIAN_POINT ( 'NONE',  ( 52.81882390656510040, 18.43111101854420042, -28.02887802125319894 ) ) ;
#11333=CARTESIAN_POINT ( 'NONE',  ( 50.68559394812662333, 4.538207541409860823, -76.25990402181635375 ) ) ;
#11337=CARTESIAN_POINT ( 'NONE',  ( 58.93926773726619928, -28.47565881710299962, -15.64941876695289835 ) ) ;
#11339=FACE_OUTER_BOUND ( 'NONE', #946, .T. ) ;
#11341=DIRECTION ( 'NONE',  ( 0.000000000000000000, -1.000000000000000000, 0.000000000000000000 ) ) ;
#11344=ORIENTED_EDGE ( 'NONE', *, *, #30139, .T. ) ;
#11349=CARTESIAN_POINT ( 'NONE',  ( 56.67477918058570197, -45.29516814663779911, -25.36359513125130150 ) ) ;
#11354=CARTESIAN_POINT ( 'NONE',  ( 11.24122293634809999, 33.45921853044769989, -23.69861594586010156 ) ) ;
#11355=ORIENTED_EDGE ( 'NONE', *, *, #2480, .T. ) ;
#11356=CARTESIAN_POINT ( 'NONE',  ( 49.92842301056370502, -45.11618894467940066, -10.23644921156189902 ) ) ;
#11357=EDGE_CURVE ( 'NONE', #46486, #30000, #2341, .T. ) ;
#11358=CARTESIAN_POINT ( 'NONE',  ( 51.87294918393343579, 1.517735892164268963, -18.77191922990750328 ) ) ;
#11362=CARTESIAN_POINT ( 'NONE',  ( 65.38525663775149610, -30.59946264837140006, -16.65175604392959841 ) ) ;
#11364=EDGE_CURVE ( 'NONE', #46679, #9855, #10841, .T. ) ;
#11366=CARTESIAN_POINT ( 'NONE',  ( 47.20687114674009877, -54.68447329799499812, -74.72520730820738777 ) ) ;
#11369=CARTESIAN_POINT ( 'NONE',  ( 41.02379277421620429, 14.08177072860459944, -5.860738561689210258 ) ) ;
#11371=VECTOR ( 'NONE', #16987, 1000.000000000000000 ) ;
#11373=CARTESIAN_POINT ( 'NONE',  ( 83.58813978703560110, -44.72666681364290042, -46.95981403914270658 ) ) ;
#11375=CARTESIAN_POINT ( 'NONE',  ( 57.75721184438519629, 13.88381124262000021, -25.37415236305640320 ) ) ;
#11377=B_SPLINE_SURFACE_WITH_KNOTS ( 'NONE', 3, 3, ( 
 ( #10132, #17224, #26090, #33184, #42098, #5432, #49715, #30284, #9616, #13803, #21899, #25570, #45779, #6202, #37137, #10391 ),
 ( #22156, #37392, #41576, #38168, #13552, #1493, #14315, #5178, #45262, #21637, #33444, #2264, #37910, #29515, #5941, #5688 ),
 ( #37645, #1745, #17477, #1233, #17728, #46303, #18238, #49461, #49204, #29256, #34205, #45520, #50226, #17984, #21133, #13296 ),
 ( #14059, #9369, #41319, #9868, #33699, #29760, #25823, #41836, #21387, #25316, #30018, #2004, #33950, #49968, #46044, #39914 ),
 ( #20230, #4258, #31762, #23639, #51203, #48037, #6461, #22419, #15552, #47780, #7431, #39403, #35720, #15295, #28091, #40165 ),
 ( #51457, #8198, #19971, #19474, #19730, #12136, #11888, #44097, #84, #327, #16058, #43844, #24141, #38422, #15798, #32011 ),
 ( #36218, #2525, #16312, #19215, #32266, #51706, #27587, #43591, #48289, #7697, #23890, #11369, #35197, #27332, #12384, #3506 ),
 ( #42359, #31250, #47279, #39655, #43338, #35967, #23379, #35461, #31508, #4009, #47527, #11625, #3761, #27844, #7942, #4778 ),
 ( #17614, #5569, #41449, #17101, #8978, #36473, #33322, #44350, #8457, #840, #33053, #44607, #24665, #21008, #578, #13437 ) ),
 .UNSPECIFIED., .F., .F., .F.,
 ( 4, 1, 1, 1, 1, 1, 4 ),
 ( 4, 2, 2, 2, 2, 2, 2, 4 ),
 ( 0.000000000000000000, 0.1666666666666670182, 0.3333333333333329818, 0.5000000000000000000, 0.6666666666666670737, 0.8333333333333330373, 1.000018175590269953 ),
 ( -6.893240790936180140, -6.545934836083509900, -4.902226309511959812, -3.475139087181930098, -2.335777911127269846, -1.766097323099940164, -1.310352852678080104, -1.260096513052359812 ),
 .UNSPECIFIED. ) ;
#11379=CARTESIAN_POINT ( 'NONE',  ( 56.24801412391880007, -46.41377194224050129, -26.27554225235660468 ) ) ;
#11380=CARTESIAN_POINT ( 'NONE',  ( 5.823743871885240786, -59.81362112911330087, -13.76841564489329883 ) ) ;
#11381=CARTESIAN_POINT ( 'NONE',  ( 75.27120125568490039, -12.48297921181119996, -11.39499376737289893 ) ) ;
#11388=CARTESIAN_POINT ( 'NONE',  ( 57.26468601612680231, -50.61618894467930119, -53.86352240777100064 ) ) ;
#11389=CARTESIAN_POINT ( 'NONE',  ( 43.52841460851590227, 12.16320807519920066, -4.940445812209770082 ) ) ;
#11390=DIRECTION ( 'NONE',  ( 0.000000000000000000, 0.000000000000000000, 1.000000000000000000 ) ) ;
#11392=CARTESIAN_POINT ( 'NONE',  ( 56.57055814460980514, -47.72537394096760011, -48.17140897430749646 ) ) ;
#11395=CARTESIAN_POINT ( 'NONE',  ( 18.31744345942739827, -52.17403775882070249, -75.62474771911479365 ) ) ;
#11396=CARTESIAN_POINT ( 'NONE',  ( 50.32921795836180223, -43.79877554599289624, -6.640512624164829347 ) ) ;
#11401=CARTESIAN_POINT ( 'NONE',  ( 88.13393739769620083, 17.38381105532069881, -65.65000000000000568 ) ) ;
#11402=DIRECTION ( 'NONE',  ( 0.000000000000000000, -1.000000000000000000, 0.000000000000000000 ) ) ;
#11405=ADVANCED_FACE ( 'NONE', ( #8599 ), #2564, .T. ) ;
#11409=CARTESIAN_POINT ( 'NONE',  ( 18.05058737638259814, 20.91286242874560131, -75.79069550273320033 ) ) ;
#11413=CARTESIAN_POINT ( 'NONE',  ( 56.92059784994150107, -45.11618894467940066, -15.82169481042769732 ) ) ;
#11415=B_SPLINE_CURVE_WITH_KNOTS ( 'NONE', 3,
 ( #30842, #10698, #34255, #35038 ),
 .UNSPECIFIED., .F., .F.,
 ( 4, 4 ),
 ( 0.000000000000000000, 1.000000000000000000 ),
 .UNSPECIFIED. ) ;
#11417=ORIENTED_EDGE ( 'NONE', *, *, #15680, .F. ) ;
#11419=VERTEX_POINT ( 'NONE', #721 ) ;
#11420=DIRECTION ( 'NONE',  ( 0.2260571801428170324, 0.000000000000000000, -0.9741140340359940586 ) ) ;
#11425=CARTESIAN_POINT ( 'NONE',  ( 52.35627137497320405, -51.18167454132500183, -76.02218069147700419 ) ) ;
#11426=CARTESIAN_POINT ( 'NONE',  ( 60.64220689335409986, 14.52815193633730040, -47.73569869354479778 ) ) ;
#11428=EDGE_CURVE ( 'NONE', #12119, #28125, #5626, .T. ) ;
#11430=CARTESIAN_POINT ( 'NONE',  ( 15.36759654800740016, 19.45617199961630206, -15.64999998510980106 ) ) ;
#11432=CARTESIAN_POINT ( 'NONE',  ( -4.916317923618620078, 16.33985541905360250, -5.410848070223339690 ) ) ;
#11433=( BOUNDED_CURVE ( )  B_SPLINE_CURVE ( 3, ( #11566, #19668, #42765, #51139 ),
 .UNSPECIFIED., .F., .T. ) 
 B_SPLINE_CURVE_WITH_KNOTS ( ( 4, 4 ),
 ( 0.3709736340029385904, 0.5134355668666845673 ),
 .UNSPECIFIED. ) 
 CURVE ( )  GEOMETRIC_REPRESENTATION_ITEM ( )  RATIONAL_B_SPLINE_CURVE ( ( 1.000000000000000000, 0.9983094314627841692, 0.9983094314627841692, 1.000000000000000000 ) ) 
 REPRESENTATION_ITEM ( '' )  );
#11435=CIRCLE ( 'NONE', #32303, 1.999999999999999556 ) ;
#11441=CARTESIAN_POINT ( 'NONE',  ( 56.57438608668749680, -50.73277124350089906, -53.83822343189740423 ) ) ;
#11442=CARTESIAN_POINT ( 'NONE',  ( 57.37416030811479573, 19.38381105532069881, -53.87117748315449717 ) ) ;
#11444=ADVANCED_FACE ( 'NONE', ( #41854 ), #13428, .T. ) ;
#11446=DIRECTION ( 'NONE',  ( 0.000000000000000000, 0.9319748226751540798, -0.3625230060280524302 ) ) ;
#11447=CARTESIAN_POINT ( 'NONE',  ( 12.28937881627030038, 18.77527563989950110, -21.14656491300549845 ) ) ;
#11449=CARTESIAN_POINT ( 'NONE',  ( 48.88334854381270134, -54.00587892617620156, -55.28861537459440001 ) ) ;
#11450=CARTESIAN_POINT ( 'NONE',  ( -18.43768031504652072, -52.44180990538531262, -54.46295789858312730 ) ) ;
#11452=CARTESIAN_POINT ( 'NONE',  ( 53.29384558423090112, 19.31433099946569953, -48.47378032971769812 ) ) ;
#11453=CARTESIAN_POINT ( 'NONE',  ( 47.81228839791550200, 23.19211001100039837, -54.83188706475510088 ) ) ;
#11458=CARTESIAN_POINT ( 'NONE',  ( 18.30675733062039967, 21.00530369360563299, -75.65677362367951275 ) ) ;
#11459=CARTESIAN_POINT ( 'NONE',  ( 60.31614849589169580, -45.76049255903560464, -47.43342490989579829 ) ) ;
#11460=VECTOR ( 'NONE', #9690, 1000.000000000000000 ) ;
#11461=CARTESIAN_POINT ( 'NONE',  ( 56.23228709081130461, -47.87823924875339543, -47.98841366488070292 ) ) ;
#11463=CARTESIAN_POINT ( 'NONE',  ( 82.91592277202030914, 14.33044519534860051, -47.63723459745410338 ) ) ;
#11467=LINE ( 'NONE', #7784, #41198 ) ;
#11469=CARTESIAN_POINT ( 'NONE',  ( -1.120159439602289808, -49.66006368695019546, -9.067476037955330526 ) ) ;
#11471=VERTEX_POINT ( 'NONE', #38386 ) ;
#11474=CARTESIAN_POINT ( 'NONE',  ( 76.72600243236601614, -38.56416636073712567, -14.20129635329269213 ) ) ;
#11475=CARTESIAN_POINT ( 'NONE',  ( 11.13041996959340096, -64.93485056432389513, -46.76691452483890288 ) ) ;
#11477=VERTEX_POINT ( 'NONE', #42848 ) ;
#11479=DIRECTION ( 'NONE',  ( 0.000000000000000000, 0.000000000000000000, 1.000000000000000000 ) ) ;
#11482=CARTESIAN_POINT ( 'NONE',  ( 55.80143501159730590, 17.65504461344360010, -53.84278118897309895 ) ) ;
#11483=CARTESIAN_POINT ( 'NONE',  ( 59.21739082243699670, -2.567626630675630128, -15.67947117406909996 ) ) ;
#11484=CARTESIAN_POINT ( 'NONE',  ( 51.51548137828859808, -48.78072553410009249, -76.79511588528808375 ) ) ;
#11485=CARTESIAN_POINT ( 'NONE',  ( 58.12686860087589480, -49.47667484878260780, -51.90689371356720017 ) ) ;
#11490=DIRECTION ( 'NONE',  ( 1.000000000000000000, 0.000000000000000000, 0.000000000000000000 ) ) ;
#11494=CARTESIAN_POINT ( 'NONE',  ( 12.38542397377720050, -50.11868687779320197, -21.15108247198449831 ) ) ;
#11495=CARTESIAN_POINT ( 'NONE',  ( 54.23304704891260286, 19.38381105532069881, -76.90112508198619423 ) ) ;
#11497=CARTESIAN_POINT ( 'NONE',  ( 56.46652749404960048, 14.04259878450300114, -16.69312833544830355 ) ) ;
#11502=EDGE_LOOP ( 'NONE', ( #6470, #19318, #9077, #8512, #34326, #50762 ) ) ;
#11503=CARTESIAN_POINT ( 'NONE',  ( 47.46022130281730256, 23.07192592923020413, -75.17786410264480423 ) ) ;
#11505=CARTESIAN_POINT ( 'NONE',  ( 45.07858682377059978, -46.11248607424209922, -9.026855431852869316 ) ) ;
#11506=DIRECTION ( 'NONE',  ( 0.05023550054956202326, 0.000000000000000000, -0.9987374001630934250 ) ) ;
#11507=CARTESIAN_POINT ( 'NONE',  ( 46.03122142033570441, 13.88381105532070059, -7.582879021622040305 ) ) ;
#11508=CIRCLE ( 'NONE', #34938, 37.99999999999998579 ) ;
#11509=CARTESIAN_POINT ( 'NONE',  ( 10.66246720348149957, -64.86660773051299600, -18.01843150775420099 ) ) ;
#11510=CARTESIAN_POINT ( 'NONE',  ( 10.69832412674970001, 33.66039914567009816, -17.91220997198119846 ) ) ;
#11514=CARTESIAN_POINT ( 'NONE',  ( 14.56862749054800510, -51.74825541291210129, -75.61049359297885530 ) ) ;
#11515=CARTESIAN_POINT ( 'NONE',  ( 49.10486152449200148, 22.59225939694159990, -54.68079418519389634 ) ) ;
#11516=ORIENTED_EDGE ( 'NONE', *, *, #40800, .T. ) ;
#11517=CARTESIAN_POINT ( 'NONE',  ( 52.84810396677629996, -49.67168591043049730, -48.89993306498779901 ) ) ;
#11518=ORIENTED_EDGE ( 'NONE', *, *, #11709, .T. ) ;
#11521=CARTESIAN_POINT ( 'NONE',  ( 14.34417029580639991, 19.88381105532299742, -22.49240189291109715 ) ) ;
#11523=EDGE_CURVE ( 'NONE', #5858, #28005, #1562, .T. ) ;
#11525=FACE_OUTER_BOUND ( 'NONE', #28910, .T. ) ;
#11526=CARTESIAN_POINT ( 'NONE',  ( 54.76549198871529711, -46.18106625824350431, -15.95314268619899956 ) ) ;
#11533=CARTESIAN_POINT ( 'NONE',  ( 11.82896782150969983, -65.41720043581369737, -17.62577516534809874 ) ) ;
#11534=CARTESIAN_POINT ( 'NONE',  ( 12.24650116540029998, 34.20510744208910126, -47.55800081758569320 ) ) ;
#11537=CYLINDRICAL_SURFACE ( 'NONE', #24613, 6.049999999999999822 ) ;
#11538=CARTESIAN_POINT ( 'NONE',  ( 11.13393739769619906, 32.24968758154479787, -24.15000000000000213 ) ) ;
#11540=CARTESIAN_POINT ( 'NONE',  ( 47.40322300430479885, -54.65574458090379295, -74.14999999999999147 ) ) ;
#11541=CARTESIAN_POINT ( 'NONE',  ( 11.10541238240669948, -63.19988511540091025, -44.25031800029979934 ) ) ;
#11542=CARTESIAN_POINT ( 'NONE',  ( 65.43042069958039519, 17.98087126524892909, -71.50000000000090949 ) ) ;
#11543=VERTEX_POINT ( 'NONE', #30504 ) ;
#11545=CARTESIAN_POINT ( 'NONE',  ( 56.66762828431429710, 19.14715517649329968, -52.77094437924129977 ) ) ;
#11546=CARTESIAN_POINT ( 'NONE',  ( 52.26507113521689973, 18.55109022033200006, -77.19475929129460212 ) ) ;
#11547=EDGE_LOOP ( 'NONE', ( #3572, #41503, #30267, #41962 ) ) ;
#11550=CARTESIAN_POINT ( 'NONE',  ( 83.45566975099262663, -44.67438659557244307, -46.48562894644376797 ) ) ;
#11552=CARTESIAN_POINT ( 'NONE',  ( 58.92073396209919878, -3.116188944679349593, -18.64999999999999858 ) ) ;
#11555=CARTESIAN_POINT ( 'NONE',  ( 52.11631747943250303, -52.62875743058319955, -46.39999999999999858 ) ) ;
#11556=CARTESIAN_POINT ( 'NONE',  ( -1.266062602303798856, -15.61618894467929941, -10.44999999999999929 ) ) ;
#11557=CIRCLE ( 'NONE', #29115, 2.999999999999998668 ) ;
#11562=CARTESIAN_POINT ( 'NONE',  ( 52.88388587306730670, -49.67261804826029703, -49.00306437247580504 ) ) ;
#11565=CARTESIAN_POINT ( 'NONE',  ( 47.31505028482810360, 23.34690877818389865, -74.80618026387669772 ) ) ;
#11566=CARTESIAN_POINT ( 'NONE',  ( 61.62036109055981115, 14.01986140997038888, -47.09707863094710945 ) ) ;
#11567=DIRECTION ( 'NONE',  ( -1.000000000000000000, 0.000000000000000000, 0.000000000000000000 ) ) ;
#11568=CARTESIAN_POINT ( 'NONE',  ( 12.23389792222850048, 33.66370788264119795, -16.17187715585779983 ) ) ;
#11570=CARTESIAN_POINT ( 'NONE',  ( 52.57246135266289855, -49.85409740178759819, -27.98331546413460202 ) ) ;
#11571=CARTESIAN_POINT ( 'NONE',  ( 55.76783084160810233, -50.62194379187450011, -76.00493532411560693 ) ) ;
#11572=CARTESIAN_POINT ( 'NONE',  ( -10.38035879666180072, 11.60169614569439922, -5.947267209420609824 ) ) ;
#11573=DIRECTION ( 'NONE',  ( 0.6888026391158250661, 0.7071067811865571207, 0.1598465650148950534 ) ) ;
#11575=CARTESIAN_POINT ( 'NONE',  ( 61.19844447806200094, 14.05756157773689985, -46.92762932161960521 ) ) ;
#11577=CYLINDRICAL_SURFACE ( 'NONE', #39849, 5.000000000000000000 ) ;
#11579=CARTESIAN_POINT ( 'NONE',  ( 53.26900104180390372, -49.43078783544130062, -48.80948086996689739 ) ) ;
#11580=CARTESIAN_POINT ( 'NONE',  ( 47.63850175670210518, 23.27425725622169850, -54.75827116794159366 ) ) ;
#11582=CARTESIAN_POINT ( 'NONE',  ( 60.92349151070310143, -45.26865707020169793, -27.39016921351189993 ) ) ;
#11584=CARTESIAN_POINT ( 'NONE',  ( 60.86406060055869460, 14.33749672913939932, -47.52785898179379842 ) ) ;
#11586=CARTESIAN_POINT ( 'NONE',  ( 51.78078201309870110, 18.91896746419559960, -76.50453762827730486 ) ) ;
#11587=CARTESIAN_POINT ( 'NONE',  ( 52.78558019943060486, 18.45415968697669840, -48.61477091151370189 ) ) ;
#11589=CARTESIAN_POINT ( 'NONE',  ( 52.90855289046150034, -49.61963672099809486, -48.71990427169439641 ) ) ;
#11596=CARTESIAN_POINT ( 'NONE',  ( 58.94101292899819811, -28.10821987741100259, -15.65000625949619995 ) ) ;
#11598=DIRECTION ( 'NONE',  ( 0.000000000000000000, 0.000000000000000000, 1.000000000000000000 ) ) ;
#11600=CARTESIAN_POINT ( 'NONE',  ( 50.99271603304481459, -35.23405637081515351, -76.39685558562041479 ) ) ;
#11602=EDGE_LOOP ( 'NONE', ( #43036, #16626, #35761, #19005 ) ) ;
#11604=CARTESIAN_POINT ( 'NONE',  ( 40.92757333388379948, 13.18145061293710008, -3.805844904963549880 ) ) ;
#11606=ORIENTED_EDGE ( 'NONE', *, *, #26721, .F. ) ;
#11612=CARTESIAN_POINT ( 'NONE',  ( 10.87442115971020051, 33.42441897061950584, -23.33560984931230209 ) ) ;
#11613=EDGE_CURVE ( 'NONE', #24756, #36035, #6225, .T. ) ;
#11619=CARTESIAN_POINT ( 'NONE',  ( 60.85624101447609746, -29.02149448471999804, -15.89604434587320014 ) ) ;
#11620=CARTESIAN_POINT ( 'NONE',  ( 14.41157406479737801, 20.07361857726730037, -75.01676221295032576 ) ) ;
#11621=CARTESIAN_POINT ( 'NONE',  ( 47.21888195866840476, -54.18123867552319695, -75.46887108633241326 ) ) ;
#11623=DIRECTION ( 'NONE',  ( 0.000000000000000000, -0.7071067811865582309, 0.7071067811865366926 ) ) ;
#11624=AXIS2_PLACEMENT_3D ( 'NONE', #21066, #4314, #44413 ) ;
#11625=CARTESIAN_POINT ( 'NONE',  ( 40.95780214525460394, 14.16802372685690159, -5.890450655994820650 ) ) ;
#11627=LINE ( 'NONE', #11890, #4985 ) ;
#11628=CARTESIAN_POINT ( 'NONE',  ( 82.66152712818241355, -45.35408509398140353, -47.35223793503389800 ) ) ;
#11629=DIRECTION ( 'NONE',  ( 0.000000000000000000, 0.000000000000000000, -1.000000000000000000 ) ) ;
#11633=CARTESIAN_POINT ( 'NONE',  ( 16.19673815768810243, -51.06918470345650007, -20.37207796061799669 ) ) ;
#11634=CARTESIAN_POINT ( 'NONE',  ( 76.33997785262350533, -18.72318222815389888, -12.53642027154039873 ) ) ;
#11636=FACE_OUTER_BOUND ( 'NONE', #17368, .T. ) ;
#11638=CARTESIAN_POINT ( 'NONE',  ( -10.87046103729910129, -42.35940093361649161, -6.284374684026399649 ) ) ;
#11639=CARTESIAN_POINT ( 'NONE',  ( 71.71126032029680175, 15.88381105532069704, -46.37203261889099792 ) ) ;
#11642=CARTESIAN_POINT ( 'NONE',  ( 57.55751162061849868, -50.19856700622089818, -52.70112124861869773 ) ) ;
#11643=CARTESIAN_POINT ( 'NONE',  ( 41.70176497865799803, 13.04736526282390230, -4.832746521660269856 ) ) ;
#11649=CARTESIAN_POINT ( 'NONE',  ( 17.79719214914599945, -51.84692819978400280, -75.69083100613939052 ) ) ;
#11650=DIRECTION ( 'NONE',  ( 0.000000000000000000, 0.000000000000000000, -1.000000000000000000 ) ) ;
#11653=CARTESIAN_POINT ( 'NONE',  ( 53.40543070545079729, -53.45144757578069772, -56.07519854833829953 ) ) ;
#11655=CARTESIAN_POINT ( 'NONE',  ( 8.788582027835408539, 31.90262041517649649, -46.67125809046000029 ) ) ;
#11656=DIRECTION ( 'NONE',  ( 0.000000000000000000, 0.000000000000000000, 1.000000000000000000 ) ) ;
#11658=AXIS2_PLACEMENT_3D ( 'NONE', #20287, #8778, #40231 ) ;
#11664=CARTESIAN_POINT ( 'NONE',  ( 17.36506832604939987, 21.76199957607230218, -76.14999999999999147 ) ) ;
#11666=CONICAL_SURFACE ( 'NONE', #2452, 20.98392344168889778, 0.7480182347898678419 ) ;
#11668=CARTESIAN_POINT ( 'NONE',  ( 55.75441314946239402, -45.11618894467940066, -14.47055463458629987 ) ) ;
#11671=ORIENTED_EDGE ( 'NONE', *, *, #41690, .T. ) ;
#11675=EDGE_CURVE ( 'NONE', #20725, #10696, #41832, .T. ) ;
#11676=DIRECTION ( 'NONE',  ( 0.000000000000000000, 0.000000000000000000, 1.000000000000000000 ) ) ;
#11679=CARTESIAN_POINT ( 'NONE',  ( 53.68570370335149988, -51.14635124491550755, -75.73808979161600519 ) ) ;
#11680=CARTESIAN_POINT ( 'NONE',  ( 60.73825411176089517, 14.46861665316230017, -47.68938770369700109 ) ) ;
#11681=CARTESIAN_POINT ( 'NONE',  ( 15.21636614235080032, 19.37178131641699963, -15.64999999240779971 ) ) ;
#11683=CARTESIAN_POINT ( 'NONE',  ( -5.389730541883220205, 15.98232200020200189, -5.411213624794680044 ) ) ;
#11685=VECTOR ( 'NONE', #8380, 1000.000000000000000 ) ;
#11686=AXIS2_PLACEMENT_3D ( 'NONE', #51394, #19415, #3700 ) ;
#11688=CARTESIAN_POINT ( 'NONE',  ( 76.87859641664680055, 11.88381105532059934, -14.85884654260030047 ) ) ;
#11689=VECTOR ( 'NONE', #39230, 1000.000000000000000 ) ;
#11690=CIRCLE ( 'NONE', #45999, 1.999999999999996669 ) ;
#11694=CARTESIAN_POINT ( 'NONE',  ( 42.67728079040009703, 14.69073914472930120, -7.341720920331609612 ) ) ;
#11698=CARTESIAN_POINT ( 'NONE',  ( 13.79543417967160046, 19.20548902729790086, -21.08562091375049974 ) ) ;
#11699=DIRECTION ( 'NONE',  ( -0.4316160343590931259, -0.9020574254913764634, 0.000000000000000000 ) ) ;
#11701=CARTESIAN_POINT ( 'NONE',  ( 61.19897450384227966, 14.07984771058140616, -47.06085141197393540 ) ) ;
#11702=CARTESIAN_POINT ( 'NONE',  ( 48.76197234853290041, -53.91797685349600044, -54.58489184698370167 ) ) ;
#11706=CARTESIAN_POINT ( 'NONE',  ( 47.77433725855070179, 23.22049558335110220, -54.88289543892820177 ) ) ;
#11709=EDGE_CURVE ( 'NONE', #23561, #22246, #21720, .T. ) ;
#11711=EDGE_LOOP ( 'NONE', ( #42204, #3650, #33418, #49256, #34141, #35359 ) ) ;
#11713=CARTESIAN_POINT ( 'NONE',  ( 60.78914095713869159, -45.49441526409999881, -47.15145036089220554 ) ) ;
#11714=CARTESIAN_POINT ( 'NONE',  ( 60.08410996676487770, 14.17546795341159971, -26.92089435490699501 ) ) ;
#11715=CARTESIAN_POINT ( 'NONE',  ( 1.027904703268279984, -42.68661147989060112, -15.65000000000000036 ) ) ;
#11728=DIRECTION ( 'NONE',  ( 0.05355673487304403457, 0.9985648081870993620, 0.000000000000000000 ) ) ;
#11729=AXIS2_PLACEMENT_3D ( 'NONE', #135, #32580, #16900 ) ;
#11730=LINE ( 'NONE', #23743, #47830 ) ;
#11731=CARTESIAN_POINT ( 'NONE',  ( 12.43884059054600044, -65.45834671174260677, -47.53658363125300212 ) ) ;
#11732=AXIS2_PLACEMENT_3D ( 'NONE', #10567, #46740, #42540 ) ;
#11733=EDGE_CURVE ( 'NONE', #48724, #13982, #46872, .T. ) ;
#11737=CARTESIAN_POINT ( 'NONE',  ( 56.61928470354429521, -45.32411298099489727, -25.29356197036729981 ) ) ;
#11738=CARTESIAN_POINT ( 'NONE',  ( 56.44265207942110152, -50.69875850325810518, -53.28298857138560152 ) ) ;
#11740=CARTESIAN_POINT ( 'NONE',  ( 62.12101911243640018, -1.046128620244999974, -16.19753051798430121 ) ) ;
#11742=CARTESIAN_POINT ( 'NONE',  ( 51.81471763238939587, -49.53261600392220743, -76.85964251417181003 ) ) ;
#11745=VERTEX_POINT ( 'NONE', #20253 ) ;
#11751=CARTESIAN_POINT ( 'NONE',  ( 13.73527021832320116, -50.20735446946800096, -20.93080062246840001 ) ) ;
#11752=CARTESIAN_POINT ( 'NONE',  ( 56.11474826664630200, 19.38381105532069881, -75.99278311555809751 ) ) ;
#11754=CARTESIAN_POINT ( 'NONE',  ( 11.19961949155312908, -65.24734059375452944, -18.17421237899869979 ) ) ;
#11757=ADVANCED_FACE ( 'NONE', ( #39168 ), #8783, .T. ) ;
#11764=CARTESIAN_POINT ( 'NONE',  ( 11.42523121511829132, 34.02364939928509102, -47.34553053285857516 ) ) ;
#11765=CARTESIAN_POINT ( 'NONE',  ( 14.42528838908026323, -51.34461569805392145, -75.09855816266191653 ) ) ;
#11766=VECTOR ( 'NONE', #43471, 1000.000000000000114 ) ;
#11771=CARTESIAN_POINT ( 'NONE',  ( 10.98984918195399985, 33.92088487140379982, -18.13296861412510097 ) ) ;
#11772=LINE ( 'NONE', #27470, #11766 ) ;
#11775=CARTESIAN_POINT ( 'NONE',  ( 9.342084535698248260, -63.49213292503509365, -16.98578758134890165 ) ) ;
#11776=CARTESIAN_POINT ( 'NONE',  ( 49.22713800240349968, 22.39287771768360358, -54.29674177404830004 ) ) ;
#11778=CARTESIAN_POINT ( 'NONE',  ( 53.44638498043019581, -49.38818856033790183, -49.05897242516689971 ) ) ;
#11785=CARTESIAN_POINT ( 'NONE',  ( 52.63649320657160047, 18.56913157916169865, -48.66852570238020093 ) ) ;
#11786=EDGE_CURVE ( 'NONE', #25615, #51745, #36053, .T. ) ;
#11787=CARTESIAN_POINT ( 'NONE',  ( 55.99869819504039725, -45.41806919520020358, -16.36330855170579923 ) ) ;
#11789=ORIENTED_EDGE ( 'NONE', *, *, #12983, .F. ) ;
#11792=CARTESIAN_POINT ( 'NONE',  ( 11.10349387995800008, -65.15484720641850913, -17.61839559469159866 ) ) ;
#11793=CARTESIAN_POINT ( 'NONE',  ( 10.71073732096479958, 32.53643514237809597, -45.47433255531149854 ) ) ;
#11795=CARTESIAN_POINT ( 'NONE',  ( 52.76718212758399318, -50.10714647214729922, -49.94264780762849654 ) ) ;
#11796=CARTESIAN_POINT ( 'NONE',  ( 11.63041745226685286, -65.37747845517948520, -22.51826834756352014 ) ) ;
#11797=CARTESIAN_POINT ( 'NONE',  ( 40.36721523010999846, -44.88645108046029719, -4.296538310233220415 ) ) ;
#11800=CARTESIAN_POINT ( 'NONE',  ( 10.97887834524160056, -63.27147703799300160, -44.74240717694910074 ) ) ;
#11801=CARTESIAN_POINT ( 'NONE',  ( 68.13393739769810509, 19.38381105532030091, -71.50000000000198952 ) ) ;
#11803=CARTESIAN_POINT ( 'NONE',  ( 66.72561048563109409, -33.11618894467930829, -20.64999999980150136 ) ) ;
#11815=DIRECTION ( 'NONE',  ( -0.4640893551880615475, -0.8857883891771946017, 0.000000000000000000 ) ) ;
#11820=CARTESIAN_POINT ( 'NONE',  ( 52.97659487819839796, -49.63248385376320471, -49.06742264967090250 ) ) ;
#11824=EDGE_CURVE ( 'NONE', #23479, #16151, #18149, .T. ) ;
#11825=CARTESIAN_POINT ( 'NONE',  ( 47.28692500774510421, 23.29813155386499801, -74.94563673128509151 ) ) ;
#11827=EDGE_CURVE ( 'NONE', #21370, #13586, #51042, .T. ) ;
#11828=B_SPLINE_SURFACE_WITH_KNOTS ( 'NONE', 3, 3, ( 
 ( #19372, #51354, #3405, #22773, #35354, #35091, #15452, #47176, #46664, #6552, #11265, #31405, #47433, #11526, #34836, #22258 ),
 ( #23279, #30640, #2627, #27485, #38265, #46406, #38792, #50580, #46920, #10747, #2358, #22519, #26704, #23028, #42725, #2884 ),
 ( #18334, #6819, #34313, #27226, #50836, #50326, #30380, #10493, #14928, #14412, #26449, #42465, #38528, #18599, #15190, #3145 ),
 ( #30893, #11006, #26974, #42983, #7078, #51092, #39050, #31151, #43240, #39300, #3659, #19880, #40324, #32686, #20647, #4674 ),
 ( #24046, #20386, #31659, #35871, #4160, #36633, #16213, #11787, #31918, #735, #8357, #7845, #32170, #44512, #51864, #8616 ),
 ( #24564, #48186, #43744, #40578, #27746, #28515, #16732, #15964, #47939, #481, #12040, #48713, #16469, #12817, #48447, #19631 ),
 ( #27994, #43997, #23793, #8103, #40067, #43491, #20135, #24307, #39809, #23538, #3917, #12549, #36126, #12290, #7592, #39556 ),
 ( #231, #35621, #36374, #51609, #32424, #28251, #44249, #15703, #47683, #4419, #37424, #45813, #33220, #45551, #49238, #21422 ),
 ( #13332, #48980, #44773, #5976, #21932, #36906, #18018, #8878, #13085, #37681, #25602, #37944, #1006, #2038, #49999, #41351 ),
 ( #5715, #20909, #1780, #1524, #28772, #40838, #5212, #41609, #33984, #24830, #41873, #17510, #9402, #21671, #17006, #21165 ) ),
 .UNSPECIFIED., .F., .F., .F.,
 ( 4, 1, 1, 1, 1, 1, 1, 4 ),
 ( 4, 2, 2, 2, 2, 2, 2, 4 ),
 ( -1.163108567600000046E-05, 0.1428571428571430157, 0.2857142857142860315, 0.4285714285714289917, 0.5714285714285709528, 0.7142857142857139685, 0.8571428571428569843, 1.000000000000000000 ),
 ( -4.238739900490239521, -3.496950822258759750, -2.649205168377850139, -2.119364134702280023, -1.854443617864500071, -1.430570790924039937, -0.7523742678193099387, 1.163108567600000046E-05 ),
 .UNSPECIFIED. ) ;
#11829=DIRECTION ( 'NONE',  ( 1.000000000000000000, 0.000000000000000000, 0.000000000000000000 ) ) ;
#11830=CARTESIAN_POINT ( 'NONE',  ( 11.70888777237000156, 33.68434717559169655, -16.37375727425619942 ) ) ;
#11833=CARTESIAN_POINT ( 'NONE',  ( 54.37045953228780348, -50.66722079764569742, -76.42819221719689438 ) ) ;
#11834=CARTESIAN_POINT ( 'NONE',  ( -3.470041707072629933, 18.86435022852390020, -8.135964718609921320 ) ) ;
#11835=DIRECTION ( 'NONE',  ( 0.000000000000000000, 0.000000000000000000, -1.000000000000000000 ) ) ;
#11837=CARTESIAN_POINT ( 'NONE',  ( 61.30905961866820064, 13.99617788076260005, -46.74474789437339695 ) ) ;
#11839=FACE_OUTER_BOUND ( 'NONE', #36451, .T. ) ;
#11842=CARTESIAN_POINT ( 'NONE',  ( 53.42190059083360154, -49.35067947775139885, -48.77466594535759725 ) ) ;
#11843=CIRCLE ( 'NONE', #35247, 28.31678667024650409 ) ;
#11844=CARTESIAN_POINT ( 'NONE',  ( 61.28606390168010165, -45.23047506471469603, -28.05549306702249979 ) ) ;
#11846=CARTESIAN_POINT ( 'NONE',  ( 61.19909455212179950, 14.07977596102159978, -47.06069650264579707 ) ) ;
#11847=VECTOR ( 'NONE', #33305, 1000.000000000000000 ) ;
#11849=CARTESIAN_POINT ( 'NONE',  ( 52.22857431453229538, 18.58359186129870011, -77.10487740174788485 ) ) ;
#11850=CARTESIAN_POINT ( 'NONE',  ( 52.73517490894950299, 18.48512909520229996, -48.54844146395180360 ) ) ;
#11856=CARTESIAN_POINT ( 'NONE',  ( 47.51836951350739469, -54.59047688859140379, -54.92482226801399747 ) ) ;
#11858=FACE_OUTER_BOUND ( 'NONE', #32245, .T. ) ;
#11859=CARTESIAN_POINT ( 'NONE',  ( 61.24027180500640100, -30.79518016777799971, -16.42551006422069904 ) ) ;
#11861=CARTESIAN_POINT ( 'NONE',  ( 10.41791033310428816, 33.00607200278869868, -23.06400185344025644 ) ) ;
#11863=FACE_OUTER_BOUND ( 'NONE', #11257, .T. ) ;
#11871=CARTESIAN_POINT ( 'NONE',  ( 12.10067309664009905, -65.23675881185819492, -45.96376834473689854 ) ) ;
#11875=CARTESIAN_POINT ( 'NONE',  ( 10.97710700053788280, 33.58282929631926095, -23.21943985317197701 ) ) ;
#11879=DIRECTION ( 'NONE',  ( 0.000000000000000000, 0.000000000000000000, 1.000000000000000000 ) ) ;
#11881=CARTESIAN_POINT ( 'NONE',  ( 59.91100987953519308, -28.69340720916260068, -15.76101076566429882 ) ) ;
#11882=VECTOR ( 'NONE', #12725, 1000.000000000000114 ) ;
#11888=CARTESIAN_POINT ( 'NONE',  ( 42.89817685944129977, 14.29758682696679983, -7.114970889050010072 ) ) ;
#11890=CARTESIAN_POINT ( 'NONE',  ( 83.89200044194980421, 19.38381105532069881, -53.92796738110899923 ) ) ;
#11891=EDGE_CURVE ( 'NONE', #42867, #9498, #27577, .T. ) ;
#11892=CARTESIAN_POINT ( 'NONE',  ( 83.27189663703491362, -44.88035785588050430, -46.76788818508799750 ) ) ;
#11896=DIRECTION ( 'NONE',  ( 0.000000000000000000, 0.000000000000000000, 1.000000000000000000 ) ) ;
#11897=CARTESIAN_POINT ( 'NONE',  ( 16.08016673437809985, -51.03387969365790156, -20.14986617604289876 ) ) ;
#11898=CARTESIAN_POINT ( 'NONE',  ( 50.95029971905736943, -35.30930468315340676, -76.37425139971915655 ) ) ;
#11902=CARTESIAN_POINT ( 'NONE',  ( -6.924536278744959361, -46.06766666375389718, -5.623594431461650167 ) ) ;
#11904=DIRECTION ( 'NONE',  ( 0.000000000000000000, 0.000000000000000000, -1.000000000000000000 ) ) ;
#11906=CARTESIAN_POINT ( 'NONE',  ( 57.40560941794409899, -50.51630527438410212, -53.29417222457460213 ) ) ;
#11907=CARTESIAN_POINT ( 'NONE',  ( 43.05690220861699657, 12.44174133896570034, -4.900907769916179824 ) ) ;
#11909=LINE ( 'NONE', #19495, #19054 ) ;
#11910=CARTESIAN_POINT ( 'NONE',  ( 55.04426526048000312, -48.50067717176560222, -48.28429872967510050 ) ) ;
#11913=CARTESIAN_POINT ( 'NONE',  ( 17.52125950177649827, -52.24941868644869913, -75.96018872839380265 ) ) ;
#11921=CARTESIAN_POINT ( 'NONE',  ( 8.804713206766638933, 31.98843531701869836, -46.67024040703379484 ) ) ;
#11922=AXIS2_PLACEMENT_3D ( 'NONE', #39237, #3083, #31342 ) ;
#11927=CARTESIAN_POINT ( 'NONE',  ( 17.21347160910339724, 21.88381105532300097, -76.14999999999999147 ) ) ;
#11935=EDGE_LOOP ( 'NONE', ( #3051, #49191, #5949, #12552 ) ) ;
#11938=ORIENTED_EDGE ( 'NONE', *, *, #15841, .T. ) ;
#11940=CARTESIAN_POINT ( 'NONE',  ( 46.40057797168859821, -53.02061573618119894, -76.14999999999999147 ) ) ;
#11941=CARTESIAN_POINT ( 'NONE',  ( 61.18292228697600876, 14.26772679133280164, -47.53321244258839329 ) ) ;
#11945=CARTESIAN_POINT ( 'NONE',  ( -5.359418298255730129, 15.90354631731749890, -5.235650387110280413 ) ) ;
#11949=CARTESIAN_POINT ( 'NONE',  ( 57.34384300794079792, 14.38573366476320103, -26.19324057846490206 ) ) ;
#11951=ORIENTED_EDGE ( 'NONE', *, *, #8678, .T. ) ;
#11954=CARTESIAN_POINT ( 'NONE',  ( -0.8677628140554130010, -51.96998285431273246, -20.56421356237309794 ) ) ;
#11959=CARTESIAN_POINT ( 'NONE',  ( 12.44373459733649945, 18.75032477250240248, -21.13286269089030256 ) ) ;
#11960=CARTESIAN_POINT ( 'NONE',  ( 47.01289654797179907, 23.18946113012230015, -75.36289900858220392 ) ) ;
#11961=CARTESIAN_POINT ( 'NONE',  ( 48.65508916750899715, -53.94707814549249747, -54.55809205546240293 ) ) ;
#11964=CARTESIAN_POINT ( 'NONE',  ( 59.01105867686166562, -2.461703131905387920, -15.68225890942153988 ) ) ;
#11967=CARTESIAN_POINT ( 'NONE',  ( 47.66581657685510010, 23.29145150881430126, -55.09436269531529717 ) ) ;
#11973=CARTESIAN_POINT ( 'NONE',  ( 60.81220464489970823, -45.55367163794920060, -47.44138936351279767 ) ) ;
#11974=CARTESIAN_POINT ( 'NONE',  ( 49.40539548398250247, -53.49785366680099941, -54.15746054658189479 ) ) ;
#11980=EDGE_LOOP ( 'NONE', ( #26269, #34173, #29449, #6708 ) ) ;
#11986=AXIS2_PLACEMENT_3D ( 'NONE', #48830, #45670, #1643 ) ;
#11987=CARTESIAN_POINT ( 'NONE',  ( 76.40287782345053813, -19.96602362163603317, -12.80893705397542348 ) ) ;
#11988=ORIENTED_EDGE ( 'NONE', *, *, #16122, .T. ) ;
#11989=ORIENTED_EDGE ( 'NONE', *, *, #32012, .T. ) ;
#11990=DIRECTION ( 'NONE',  ( 1.000000000000000000, 0.000000000000000000, 0.000000000000000000 ) ) ;
#11994=CARTESIAN_POINT ( 'NONE',  ( 58.92068922470849657, -3.124196156303379990, -15.65000643880829934 ) ) ;
#11995=CARTESIAN_POINT ( 'NONE',  ( 51.57064462678510353, -49.04885115171509824, -76.80688256002839864 ) ) ;
#11997=DIRECTION ( 'NONE',  ( -0.7226652920947608250, -0.6911981449639416075, 0.000000000000000000 ) ) ;
#11998=FACE_OUTER_BOUND ( 'NONE', #29905, .T. ) ;
#12000=LINE ( 'NONE', #20098, #42055 ) ;
#12002=CARTESIAN_POINT ( 'NONE',  ( 13.29231789701340105, -50.60014296140869305, -21.35983077129230168 ) ) ;
#12003=VECTOR ( 'NONE', #49740, 1000.000000000000000 ) ;
#12004=EDGE_CURVE ( 'NONE', #48345, #14040, #35419, .T. ) ;
#12006=CARTESIAN_POINT ( 'NONE',  ( 70.83393739769717001, -48.11618894467422081, -70.54999999999975557 ) ) ;
#12007=CARTESIAN_POINT ( 'NONE',  ( 61.05532957801759864, -45.35430874236069343, -46.96571179725230394 ) ) ;
#12008=EDGE_CURVE ( 'NONE', #17711, #25812, #28419, .T. ) ;
#12010=CARTESIAN_POINT ( 'NONE',  ( 14.34417029198879945, -51.11618894467930119, -74.14999999999999147 ) ) ;
#12013=EDGE_CURVE ( 'NONE', #39953, #23932, #15307, .T. ) ;
#12014=ORIENTED_EDGE ( 'NONE', *, *, #36788, .F. ) ;
#12015=CARTESIAN_POINT ( 'NONE',  ( 14.34420760053260047, -51.11618258419110106, -74.34711752987750799 ) ) ;
#12016=CARTESIAN_POINT ( 'NONE',  ( 47.32074021863829927, -54.70663448010740382, -54.72782118794329875 ) ) ;
#12019=CARTESIAN_POINT ( 'NONE',  ( 61.28610861176739633, 13.99802266614350010, -46.37203261889099792 ) ) ;
#12023=CARTESIAN_POINT ( 'NONE',  ( 16.13393740247629893, -15.61618988478180015, -4.296538730098649950 ) ) ;
#12026=DIRECTION ( 'NONE',  ( 0.000000000000000000, 1.000000000000000000, 0.000000000000000000 ) ) ;
#12027=CARTESIAN_POINT ( 'NONE',  ( -3.547017152609819757, -48.75843093089891767, -5.665571190130843426 ) ) ;
#12029=EDGE_CURVE ( 'NONE', #38811, #5608, #29025, .T. ) ;
#12030=CARTESIAN_POINT ( 'NONE',  ( 13.10176660314549935, 34.29157359959339857, -47.73582792185820267 ) ) ;
#12032=CARTESIAN_POINT ( 'NONE',  ( 52.74572974338470033, -49.72478476443930617, -48.77972035026300546 ) ) ;
#12037=CARTESIAN_POINT ( 'NONE',  ( 83.13571748553259511, 13.71928646809350028, -46.75830440892689666 ) ) ;
#12039=CARTESIAN_POINT ( 'NONE',  ( 53.23851273770399928, 18.29663818490410421, -49.17579072038760302 ) ) ;
#12040=CARTESIAN_POINT ( 'NONE',  ( 55.98847043416329683, -45.29423959430500446, -15.93199093155540247 ) ) ;
#12041=CARTESIAN_POINT ( 'NONE',  ( 52.90929476643909624, 18.25992211886340044, -27.14407627714519933 ) ) ;
#12045=ORIENTED_EDGE ( 'NONE', *, *, #48917, .F. ) ;
#12046=CARTESIAN_POINT ( 'NONE',  ( 11.65058183552799953, -65.39170010508581754, -17.77752805455190099 ) ) ;
#12047=CARTESIAN_POINT ( 'NONE',  ( 9.869349621126580985, 32.08736743983219952, -46.22151743497509813 ) ) ;
#12050=CARTESIAN_POINT ( 'NONE',  ( 48.94887823264109272, -53.89549600984270228, -54.63676433852469927 ) ) ;
#12051=CARTESIAN_POINT ( 'NONE',  ( 11.08250670836754459, -64.97041830570583443, -23.10046800189048710 ) ) ;
#12052=CARTESIAN_POINT ( 'NONE',  ( 51.35161527711753848, 3.349069727626160287, -76.64881736422908887 ) ) ;
#12053=EDGE_CURVE ( 'NONE', #51185, #18289, #29096, .T. ) ;
#12055=CARTESIAN_POINT ( 'NONE',  ( 50.87748861976533021, -52.21589981770337374, -52.61226359342039416 ) ) ;
#12056=CARTESIAN_POINT ( 'NONE',  ( 68.13393739769620083, 19.38381105532069881, -65.65000000000000568 ) ) ;
#12057=AXIS2_PLACEMENT_3D ( 'NONE', #6114, #33615, #42014 ) ;
#12058=CARTESIAN_POINT ( 'NONE',  ( 68.13393739769814772, 19.38381105532029736, -71.50000000000200373 ) ) ;
#12059=ORIENTED_EDGE ( 'NONE', *, *, #4317, .F. ) ;
#12060=CARTESIAN_POINT ( 'NONE',  ( 11.67619942398489918, -64.89165360645620240, -45.08494251881790404 ) ) ;
#12061=CARTESIAN_POINT ( 'NONE',  ( 56.48517904086930486, 19.30797284152329851, -52.93690031776429805 ) ) ;
#12065=ORIENTED_EDGE ( 'NONE', *, *, #45992, .F. ) ;
#12071=CARTESIAN_POINT ( 'NONE',  ( 56.50083414075169941, 19.52878523282910450, -74.28948443064300022 ) ) ;
#12072=ORIENTED_EDGE ( 'NONE', *, *, #39212, .F. ) ;
#12077=ADVANCED_FACE ( 'NONE', ( #49038 ), #17556, .F. ) ;
#12079=CARTESIAN_POINT ( 'NONE',  ( 47.37011575340810055, 23.44240931280840101, -74.19735651161070678 ) ) ;
#12082=CARTESIAN_POINT ( 'NONE',  ( 11.98449920102340016, 33.55497157401369890, -16.08642242877740003 ) ) ;
#12084=CARTESIAN_POINT ( 'NONE',  ( 56.68744973047850522, -50.63300783658069548, -75.04390987627759557 ) ) ;
#12085=CARTESIAN_POINT ( 'NONE',  ( 57.34991680858041718, 19.38381105532069881, -53.92361874566621793 ) ) ;
#12088=CARTESIAN_POINT ( 'NONE',  ( 61.30667203655529818, 14.01553559058869780, -46.90228508237380112 ) ) ;
#12089=EDGE_CURVE ( 'NONE', #33592, #12246, #24209, .T. ) ;
#12092=CARTESIAN_POINT ( 'NONE',  ( 52.98014239974310158, -49.58212897128409935, -48.77045029443840463 ) ) ;
#12093=CARTESIAN_POINT ( 'NONE',  ( 61.19443126428920010, -45.21152309989860640, -27.59429383128480140 ) ) ;
#12095=CARTESIAN_POINT ( 'NONE',  ( 57.35253518667929740, 14.57826363733579988, -26.27218797145850004 ) ) ;
#12097=CARTESIAN_POINT ( 'NONE',  ( 51.21390329036389488, 18.63858452962650247, -76.33091581055249719 ) ) ;
#12098=CARTESIAN_POINT ( 'NONE',  ( 53.13943604555799993, 18.27600435916260224, -48.93645284067880397 ) ) ;
#12101=EDGE_LOOP ( 'NONE', ( #24128, #6702, #50192, #49381 ) ) ;
#12103=CARTESIAN_POINT ( 'NONE',  ( 47.70972474023349719, -54.46928834314500278, -54.77964464375110509 ) ) ;
#12106=CARTESIAN_POINT ( 'NONE',  ( 59.54770650857670233, -29.44221205149689879, -15.81971576896729736 ) ) ;
#12111=CARTESIAN_POINT ( 'NONE',  ( 51.35163416435118933, -34.58141209747533651, -76.64883399551484899 ) ) ;
#12114=EDGE_CURVE ( 'NONE', #33533, #15737, #38471, .T. ) ;
#12115=VERTEX_POINT ( 'NONE', #16529 ) ;
#12116=CIRCLE ( 'NONE', #22931, 15.56227766016840164 ) ;
#12118=CARTESIAN_POINT ( 'NONE',  ( 51.15515350355274649, 0.3890328154924098114, -17.08415396337089120 ) ) ;
#12119=VERTEX_POINT ( 'NONE', #8944 ) ;
#12125=DIRECTION ( 'NONE',  ( 0.000000000000000000, 1.000000000000000000, 0.000000000000000000 ) ) ;
#12129=CARTESIAN_POINT ( 'NONE',  ( 10.72320681404810117, 33.67578529855150293, -17.84617904793899967 ) ) ;
#12130=B_SPLINE_CURVE_WITH_KNOTS ( 'NONE', 3,
 ( #10804, #30438, #11064, #39357, #31201, #10286, #42778, #2681 ),
 .UNSPECIFIED., .F., .F.,
 ( 4, 2, 2, 4 ),
 ( 0.5000003605096956516, 0.6249999999981298293, 0.8249999999991262101, 1.000000000000000000 ),
 .UNSPECIFIED. ) ;
#12136=CARTESIAN_POINT ( 'NONE',  ( 43.28347309149560829, 14.32586227162870074, -7.371246978530599847 ) ) ;
#12137=ADVANCED_FACE ( 'NONE', ( #36185, #16277 ), #28833, .T. ) ;
#12138=CARTESIAN_POINT ( 'NONE',  ( 14.53578026856690109, 20.42331001517590394, -75.51792558472199346 ) ) ;
#12140=CARTESIAN_POINT ( 'NONE',  ( 82.57306898050271116, -45.18814731124680151, -46.98632580443239704 ) ) ;
#12143=ORIENTED_EDGE ( 'NONE', *, *, #5646, .F. ) ;
#12144=CARTESIAN_POINT ( 'NONE',  ( 52.84768130634319760, -49.63793414090860523, -27.92371165755740137 ) ) ;
#12146=CARTESIAN_POINT ( 'NONE',  ( 15.72190426419749976, -50.88626546307889953, -20.14992017774540045 ) ) ;
#12147=CARTESIAN_POINT ( 'NONE',  ( 50.87985442507742562, -35.43346530991949805, -76.33943627716247704 ) ) ;
#12153=CARTESIAN_POINT ( 'NONE',  ( 47.31649804177600060, 23.47503745077689885, -54.66794107860329177 ) ) ;
#12156=CARTESIAN_POINT ( 'NONE',  ( 13.79563961991219934, 19.20557301982950094, -21.08562558918019647 ) ) ;
#12157=CARTESIAN_POINT ( 'NONE',  ( 57.37198100508690857, -50.16664033240260068, -52.65631614168299990 ) ) ;
#12158=CARTESIAN_POINT ( 'NONE',  ( 42.29463403588689374, 12.88442639002479950, -4.936190358464100036 ) ) ;
#12160=DIRECTION ( 'NONE',  ( 0.000000000000000000, 0.000000000000000000, -1.000000000000000000 ) ) ;
#12161=CARTESIAN_POINT ( 'NONE',  ( 55.51244966342819964, -48.25538224542870580, -48.24951049977990181 ) ) ;
#12164=CARTESIAN_POINT ( 'NONE',  ( 17.49174741965450153, -52.84830569448709525, -76.12661215459480957 ) ) ;
#12166=CARTESIAN_POINT ( 'NONE',  ( 55.99539635179259989, -50.96576843986699856, -53.34422020842900025 ) ) ;
#12171=ORIENTED_EDGE ( 'NONE', *, *, #34954, .F. ) ;
#12172=CARTESIAN_POINT ( 'NONE',  ( 17.36026107283840147, 21.75858530671060009, -76.14999999999999147 ) ) ;
#12173=ADVANCED_FACE ( 'NONE', ( #8164 ), #4738, .T. ) ;
#12176=CARTESIAN_POINT ( 'NONE',  ( 61.62035637548115119, -45.25224449890009737, -47.09707516299204144 ) ) ;
#12178=EDGE_CURVE ( 'NONE', #19324, #11300, #40972, .T. ) ;
#12181=CIRCLE ( 'NONE', #47351, 2.000000000000000000 ) ;
#12182=CYLINDRICAL_SURFACE ( 'NONE', #22405, 0.9999999999999991118 ) ;
#12184=CARTESIAN_POINT ( 'NONE',  ( 11.47625293935331037, -64.64303150479236137, -23.97637485116214506 ) ) ;
#12187=ORIENTED_EDGE ( 'NONE', *, *, #22888, .F. ) ;
#12188=CARTESIAN_POINT ( 'NONE',  ( 60.83133136721959744, 14.23629320661039976, -47.01992809069390233 ) ) ;
#12189=FACE_OUTER_BOUND ( 'NONE', #42672, .T. ) ;
#12190=CARTESIAN_POINT ( 'NONE',  ( 61.05085642621550335, 14.40809333551259996, -47.70073481199239751 ) ) ;
#12193=CARTESIAN_POINT ( 'NONE',  ( 41.30229995814859478, -44.08664243540900429, -3.681965999269640299 ) ) ;
#12194=CARTESIAN_POINT ( 'NONE',  ( -8.896400163295020036, 12.99350780695079877, -5.517956762993129871 ) ) ;
#12196=CARTESIAN_POINT ( 'NONE',  ( 57.82760759097259751, 14.44856554515060054, -26.31132835932049829 ) ) ;
#12199=AXIS2_PLACEMENT_3D ( 'NONE', #7131, #19167, #35407 ) ;
#12200=CARTESIAN_POINT ( 'NONE',  ( 54.33950582513909922, 17.73388049035199998, -48.90971789431980454 ) ) ;
#12201=CARTESIAN_POINT ( 'NONE',  ( 41.98716862695110308, 14.55766279460999968, -6.812372419885229569 ) ) ;
#12209=CARTESIAN_POINT ( 'NONE',  ( 48.82583097700369734, -53.98510752664869727, -54.88051616806440336 ) ) ;
#12210=CARTESIAN_POINT ( 'NONE',  ( -10.87564126230760131, 11.12160698687080185, -6.291562883898949465 ) ) ;
#12213=CARTESIAN_POINT ( 'NONE',  ( 56.56302216566690078, 13.88381105532070059, -15.29297957052069989 ) ) ;
#12214=VERTEX_POINT ( 'NONE', #49807 ) ;
#12217=EDGE_LOOP ( 'NONE', ( #14045, #32614, #12989, #8548, #30235, #36994 ) ) ;
#12219=CARTESIAN_POINT ( 'NONE',  ( 61.04997942697300317, -45.41016238768720115, -47.26479615961620340 ) ) ;
#12227=CARTESIAN_POINT ( 'NONE',  ( 83.69028489729539899, -45.07031961188679503, -47.49660994411200221 ) ) ;
#12228=ORIENTED_EDGE ( 'NONE', *, *, #12029, .T. ) ;
#12229=EDGE_CURVE ( 'NONE', #21630, #38460, #14859, .T. ) ;
#12232=CARTESIAN_POINT ( 'NONE',  ( 53.05496371557740076, -49.60060548025979443, -49.11011777256759814 ) ) ;
#12233=CARTESIAN_POINT ( 'NONE',  ( 53.31390740451600152, -50.46142145313445582, -77.17777227673258267 ) ) ;
#12234=CARTESIAN_POINT ( 'NONE',  ( 76.39343546571723209, -13.87943195375858529, -12.76821643264017325 ) ) ;
#12235=CARTESIAN_POINT ( 'NONE',  ( 53.79565702846219466, -51.91342281481009735, -54.22862211494859963 ) ) ;
#12238=ORIENTED_EDGE ( 'NONE', *, *, #20022, .F. ) ;
#12239=CARTESIAN_POINT ( 'NONE',  ( 48.36908225894410407, 22.86152331119799896, -54.63163985339289752 ) ) ;
#12240=CARTESIAN_POINT ( 'NONE',  ( 57.02670666273519373, -45.17403284636800009, -25.30271567922349973 ) ) ;
#12241=CARTESIAN_POINT ( 'NONE',  ( 56.43116296087830364, -50.73498357634339584, -53.39631301164680366 ) ) ;
#12243=CARTESIAN_POINT ( 'NONE',  ( 65.07836497255370034, 0.9425083649366529093, -17.72664388599960006 ) ) ;
#12246=VERTEX_POINT ( 'NONE', #19305 ) ;
#12248=DIRECTION ( 'NONE',  ( 0.000000000000000000, 0.000000000000000000, 1.000000000000000000 ) ) ;
#12249=CARTESIAN_POINT ( 'NONE',  ( 52.63065799377530141, -50.23288335026530405, -76.99620445994730744 ) ) ;
#12254=ADVANCED_FACE ( 'NONE', ( #45612 ), #25959, .T. ) ;
#12256=CARTESIAN_POINT ( 'NONE',  ( 12.82092494627180201, -50.09900319257889834, -21.11499762262549851 ) ) ;
#12259=CARTESIAN_POINT ( 'NONE',  ( 68.13393739769745139, -49.21324915460503036, -70.54648330188275906 ) ) ;
#12260=CARTESIAN_POINT ( 'NONE',  ( 61.36964513858340098, -45.41361601159059092, -47.42035206001249747 ) ) ;
#12263=CARTESIAN_POINT ( 'NONE',  ( 8.784728771152170879, 23.70287936274029761, -46.67204636145419983 ) ) ;
#12265=CARTESIAN_POINT ( 'NONE',  ( 13.50743972583810049, -51.62277378238770353, -74.57010117179498820 ) ) ;
#12266=CARTESIAN_POINT ( 'NONE',  ( 47.31834723158630140, -54.70509784558640121, -54.64514906959579577 ) ) ;
#12267=DIRECTION ( 'NONE',  ( 0.000000000000000000, 0.000000000000000000, 1.000000000000000000 ) ) ;
#12269=CARTESIAN_POINT ( 'NONE',  ( 68.13393739769620083, 1.883811055320649963, -65.65000000000000568 ) ) ;
#12271=CIRCLE ( 'NONE', #19787, 4.000000000000050626 ) ;
#12274=CARTESIAN_POINT ( 'NONE',  ( 60.98011298598618168, 14.15834234790303370, -46.91885902330013636 ) ) ;
#12275=CARTESIAN_POINT ( 'NONE',  ( 13.61938558678000000, -51.42721352342299923, -23.15000000000000213 ) ) ;
#12277=DIRECTION ( 'NONE',  ( 0.000000000000000000, 0.000000000000000000, -1.000000000000000000 ) ) ;
#12278=CARTESIAN_POINT ( 'NONE',  ( 48.51124500827120301, 22.78135976125399864, -54.58137771766570268 ) ) ;
#12280=CARTESIAN_POINT ( 'NONE',  ( 52.71531615687540295, -49.74189531715239809, -48.72996495230640335 ) ) ;
#12284=FACE_OUTER_BOUND ( 'NONE', #1798, .T. ) ;
#12285=CARTESIAN_POINT ( 'NONE',  ( 41.03393739769614967, -15.61618894467929586, 4.449999999999957545 ) ) ;
#12286=CARTESIAN_POINT ( 'NONE',  ( 83.10006388208910266, 13.66738427442989767, -46.45756164887520612 ) ) ;
#12287=CARTESIAN_POINT ( 'NONE',  ( 55.70021556852680078, 15.31776400109049874, -26.09178003392089806 ) ) ;
#12289=CARTESIAN_POINT ( 'NONE',  ( 53.55182622754160349, 18.18654131614419711, -49.22385694762949981 ) ) ;
#12290=CARTESIAN_POINT ( 'NONE',  ( 55.53797971117669618, -45.20374984908950466, -15.09128669035350079 ) ) ;
#12291=CARTESIAN_POINT ( 'NONE',  ( 41.64265090550289727, 15.19461330350370076, -4.296538310234210734 ) ) ;
#12292=AXIS2_PLACEMENT_3D ( 'NONE', #30422, #46448, #38052 ) ;
#12293=ORIENTED_EDGE ( 'NONE', *, *, #10147, .T. ) ;
#12297=CARTESIAN_POINT ( 'NONE',  ( 11.51051965274460009, -65.34949819799740567, -17.72953754264250037 ) ) ;
#12298=CARTESIAN_POINT ( 'NONE',  ( 11.31462425921800019, 33.80730954441699510, -46.86167435056430719 ) ) ;
#12299=CARTESIAN_POINT ( 'NONE',  ( 18.35639339474798959, 19.96346599773298536, -15.69083011943929407 ) ) ;
#12300=CARTESIAN_POINT ( 'NONE',  ( 47.65699260619980038, -54.43196373011130618, -54.14466233815100082 ) ) ;
#12301=CARTESIAN_POINT ( 'NONE',  ( 8.786667189176620596, 31.89283771814190160, -46.67161560189330061 ) ) ;
#12302=LINE ( 'NONE', #48722, #23291 ) ;
#12303=VERTEX_POINT ( 'NONE', #26325 ) ;
#12304=DIRECTION ( 'NONE',  ( 0.000000000000000000, 0.000000000000000000, -1.000000000000000000 ) ) ;
#12305=CARTESIAN_POINT ( 'NONE',  ( 11.10533145046600012, -63.13707322673510447, -44.25027853318809434 ) ) ;
#12306=ADVANCED_BREP_SHAPE_REPRESENTATION ( '', ( #44299, #20940 ), #5952 ) ;
#12310=CARTESIAN_POINT ( 'NONE',  ( 50.98563555873659681, -50.83528032372250038, -76.14999999999999147 ) ) ;
#12314=DIRECTION ( 'NONE',  ( 0.6888026391158391659, 0.7071067811865435759, 0.1598465650148942763 ) ) ;
#12315=DIRECTION ( 'NONE',  ( 0.000000000000000000, 0.000000000000000000, -1.000000000000000000 ) ) ;
#12318=CARTESIAN_POINT ( 'NONE',  ( 55.20045915843670059, 19.79101985246630235, -75.15517561605419417 ) ) ;
#12320=ADVANCED_FACE ( 'NONE', ( #2238 ), #18214, .T. ) ;
#12324=DIRECTION ( 'NONE',  ( 0.000000000000000000, 0.000000000000000000, 1.000000000000000000 ) ) ;
#12325=CARTESIAN_POINT ( 'NONE',  ( 12.36961003038774365, 34.13847818779984777, -23.58850009407127502 ) ) ;
#12326=CARTESIAN_POINT ( 'NONE',  ( 47.29375078065829996, 23.46074027222400105, -74.50151902752439526 ) ) ;
#12328=CARTESIAN_POINT ( 'NONE',  ( 56.46551779669420057, -50.77616595281960343, -53.85225392423020452 ) ) ;
#12331=CARTESIAN_POINT ( 'NONE',  ( 56.95004443788039339, -50.62929017573570434, -74.61329603206479533 ) ) ;
#12332=DIRECTION ( 'NONE',  ( 0.000000000000000000, 1.000000000000000000, 0.000000000000000000 ) ) ;
#12335=CARTESIAN_POINT ( 'NONE',  ( 61.29873811675859940, 13.99300715493670033, -46.60505303728890425 ) ) ;
#12336=CARTESIAN_POINT ( 'NONE',  ( -32.24202920327260102, -25.12181407414389867, -55.86711240520629929 ) ) ;
#12339=CARTESIAN_POINT ( 'NONE',  ( 53.05172806475840019, -49.54462323568909454, -48.80720635931050566 ) ) ;
#12340=CARTESIAN_POINT ( 'NONE',  ( 61.48973982512229952, -45.14485638884580254, -27.91396448414770148 ) ) ;
#12342=CARTESIAN_POINT ( 'NONE',  ( 57.23047368777599786, 14.59927084644489881, -26.25848675732999737 ) ) ;
#12344=CARTESIAN_POINT ( 'NONE',  ( 50.88311850049529284, 17.84955123746129857, -76.31540042328140316 ) ) ;
#12345=CARTESIAN_POINT ( 'NONE',  ( 52.85389958694200629, 18.41787986729509896, -48.74486367440029966 ) ) ;
#12348=ORIENTED_EDGE ( 'NONE', *, *, #10133, .F. ) ;
#12351=CARTESIAN_POINT ( 'NONE',  ( 47.71647669724200114, -54.49282706777620433, -54.97429864921259934 ) ) ;
#12352=DIRECTION ( 'NONE',  ( 1.000000000000000000, 0.000000000000000000, 0.000000000000000000 ) ) ;
#12354=CARTESIAN_POINT ( 'NONE',  ( 58.65609766748040244, 17.55276584502570003, -51.15249613422370345 ) ) ;
#12363=ORIENTED_EDGE ( 'NONE', *, *, #34990, .F. ) ;
#12365=CIRCLE ( 'NONE', #17416, 1.416095994175718964 ) ;
#12366=CARTESIAN_POINT ( 'NONE',  ( 49.85987176298878865, -29.64260838442978141, -15.88869185456543143 ) ) ;
#12368=CARTESIAN_POINT ( 'NONE',  ( 11.23030410197340068, -64.15300103173049706, -44.07781775651169909 ) ) ;
#12369=CARTESIAN_POINT ( 'NONE',  ( 12.95205818299439926, -65.51487522592771029, -47.64438484965779708 ) ) ;
#12372=CARTESIAN_POINT ( 'NONE',  ( 16.65420337941489848, 17.88381105532299742, -20.15000000000000213 ) ) ;
#12375=CARTESIAN_POINT ( 'NONE',  ( 68.13393739769620083, 17.38381105532069881, -65.65000000000000568 ) ) ;
#12380=EDGE_CURVE ( 'NONE', #31547, #1664, #28463, .T. ) ;
#12381=ORIENTED_EDGE ( 'NONE', *, *, #19984, .T. ) ;
#12382=CARTESIAN_POINT ( 'NONE',  ( 11.24784815691280038, -64.69222497390319404, -23.70517260836590268 ) ) ;
#12384=CARTESIAN_POINT ( 'NONE',  ( 40.79813495724229711, 13.98026726342900083, -5.648533830653249765 ) ) ;
#12385=CARTESIAN_POINT ( 'NONE',  ( 14.76083081978829981, 21.63336578114690312, -76.12563501418100032 ) ) ;
#12387=CARTESIAN_POINT ( 'NONE',  ( 83.53665286397169609, -44.61316599402150018, -46.51476939800770083 ) ) ;
#12388=AXIS2_PLACEMENT_3D ( 'NONE', #2771, #31297, #31047 ) ;
#12390=EDGE_CURVE ( 'NONE', #35377, #10891, #1693, .T. ) ;
#12394=CARTESIAN_POINT ( 'NONE',  ( 52.83348354832899929, -49.61280751446100368, -27.68241839973370233 ) ) ;
#12395=CARTESIAN_POINT ( 'NONE',  ( 15.79694611016350336, -50.96353045011390037, -20.52360778208860026 ) ) ;
#12396=DIRECTION ( 'NONE',  ( 1.000000000000000000, 0.000000000000000000, 0.000000000000000000 ) ) ;
#12398=DIRECTION ( 'NONE',  ( -0.2389682100435167045, 0.9710273912658683448, 0.000000000000000000 ) ) ;
#12400=CARTESIAN_POINT ( 'NONE',  ( -7.446190786415279206, -45.59035109774320205, -5.628040487542099513 ) ) ;
#12401=CARTESIAN_POINT ( 'NONE',  ( 47.24267966324089230, 23.52891476845359975, -54.64850595551979495 ) ) ;
#12405=CARTESIAN_POINT ( 'NONE',  ( 41.18706483287339637, 13.38317691818800093, -5.042666801615239613 ) ) ;
#12409=B_SPLINE_CURVE_WITH_KNOTS ( 'NONE', 3,
 ( #17339, #13414, #16547, #41432, #48525, #44591, #20991, #8696, #24648 ),
 .UNSPECIFIED., .F., .F.,
 ( 4, 2, 1, 2, 4 ),
 ( 0.000000000000000000, 0.2496952128132839399, 0.3745428192199221629, 0.4369666224232462426, 0.4993904256265703223 ),
 .UNSPECIFIED. ) ;
#12410=CARTESIAN_POINT ( 'NONE',  ( 56.37863599685000082, -47.94388181700620066, -48.46423989679689726 ) ) ;
#12413=CARTESIAN_POINT ( 'NONE',  ( 17.29410413645300437, -52.94069807145589834, -76.14999999999999147 ) ) ;
#12416=CARTESIAN_POINT ( 'NONE',  ( 68.13393739769620083, -43.11618894467930119, -73.60861006572370968 ) ) ;
#12417=ORIENTED_EDGE ( 'NONE', *, *, #26721, .T. ) ;
#12418=DIRECTION ( 'NONE',  ( 0.000000000000000000, 0.000000000000000000, -1.000000000000000000 ) ) ;
#12419=CARTESIAN_POINT ( 'NONE',  ( 10.14396384489010039, 32.02340138881569231, -45.99320603557470122 ) ) ;
#12424=CARTESIAN_POINT ( 'NONE',  ( 17.74772103310080240, 20.37930389448669644, -75.46937177410659103 ) ) ;
#12425=EDGE_LOOP ( 'NONE', ( #27751, #35187, #25662, #15681 ) ) ;
#12428=DIRECTION ( 'NONE',  ( 0.000000000000000000, 0.000000000000000000, 1.000000000000000000 ) ) ;
#12429=DIRECTION ( 'NONE',  ( 0.5685928097855378338, 0.5944782866685498490, -0.5685928097855378338 ) ) ;
#12434=DIRECTION ( 'NONE',  ( 0.000000000000000000, 0.000000000000000000, 1.000000000000000000 ) ) ;
#12436=CARTESIAN_POINT ( 'NONE',  ( 48.91612303624370384, -46.17268314339860069, -11.68043221219750016 ) ) ;
#12438=CARTESIAN_POINT ( 'NONE',  ( 57.82770531258893243, -45.74095387556897663, -26.33626789187744421 ) ) ;
#12441=DIRECTION ( 'NONE',  ( 0.000000000000000000, 0.000000000000000000, 1.000000000000000000 ) ) ;
#12443=CARTESIAN_POINT ( 'NONE',  ( 60.81154475074989563, 14.44468362946420115, -47.68343931016890025 ) ) ;
#12444=CARTESIAN_POINT ( 'NONE',  ( 53.62232554824719699, 14.37784769650350114, -14.60904475022659987 ) ) ;
#12446=CARTESIAN_POINT ( 'NONE',  ( -10.45347530949710091, 11.54094627941979923, -5.983182295287229557 ) ) ;
#12448=CARTESIAN_POINT ( 'NONE',  ( 61.30976794464369561, 13.98564738790680018, -28.10341086548599776 ) ) ;
#12449=ADVANCED_FACE ( 'NONE', ( #46539, #10627 ), #35230, .T. ) ;
#12451=ORIENTED_EDGE ( 'NONE', *, *, #31387, .F. ) ;
#12452=CARTESIAN_POINT ( 'NONE',  ( 59.69762033831859327, 14.85484429090200109, -47.57821500189280073 ) ) ;
#12453=ADVANCED_FACE ( 'NONE', ( #44391 ), #3272, .F. ) ;
#12454=CARTESIAN_POINT ( 'NONE',  ( 40.93884659071979826, 14.21788489420559998, -5.915596512093559411 ) ) ;
#12455=CARTESIAN_POINT ( 'NONE',  ( 53.99624024582704607, -50.67301592132088217, -76.54980271157616301 ) ) ;
#12457=ADVANCED_FACE ( 'NONE', ( #8230 ), #3538, .T. ) ;
#12463=CARTESIAN_POINT ( 'NONE',  ( 46.91120985881580197, 22.91722024179730255, -75.65750144867429583 ) ) ;
#12464=CARTESIAN_POINT ( 'NONE',  ( 48.72281879484769718, -54.07425847834139887, -55.27155626217439988 ) ) ;
#12465=DIRECTION ( 'NONE',  ( 0.000000000000000000, 0.000000000000000000, -1.000000000000000000 ) ) ;
#12467=CARTESIAN_POINT ( 'NONE',  ( 66.72561048563109409, -33.11618894467930829, -20.64999999980150136 ) ) ;
#12469=VERTEX_POINT ( 'NONE', #39690 ) ;
#12473=CARTESIAN_POINT ( 'NONE',  ( 17.21347160910339724, 21.88381105532300097, -76.14999999999999147 ) ) ;
#12474=CARTESIAN_POINT ( 'NONE',  ( 60.66957880285420401, -45.55654657165910493, -47.20039331182919540 ) ) ;
#12476=CARTESIAN_POINT ( 'NONE',  ( 69.11290641955770297, -43.39767609583565644, -11.59169279273430497 ) ) ;
#12479=CARTESIAN_POINT ( 'NONE',  ( -31.86606260230380627, -15.61618894467930474, -74.14999999999999147 ) ) ;
#12483=CARTESIAN_POINT ( 'NONE',  ( 84.28893459517129827, -43.90990963716989626, -47.31525200062240089 ) ) ;
#12485=VERTEX_POINT ( 'NONE', #39177 ) ;
#12488=CARTESIAN_POINT ( 'NONE',  ( 52.97651386206310065, -49.63284518666780087, -49.06832845556920120 ) ) ;
#12489=CARTESIAN_POINT ( 'NONE',  ( 53.07820087960804756, -50.35438023692758236, -77.22362299732516533 ) ) ;
#12490=CARTESIAN_POINT ( 'NONE',  ( 76.39890160524630858, -19.26235143558729135, -12.79181377051713753 ) ) ;
#12491=CARTESIAN_POINT ( 'NONE',  ( 51.36789317581919789, -52.94755764699569767, -54.71052196913720422 ) ) ;
#12495=CARTESIAN_POINT ( 'NONE',  ( 47.84600491270340683, 23.14802384070760155, -54.72009433156399894 ) ) ;
#12496=CARTESIAN_POINT ( 'NONE',  ( 57.33512764681800178, -45.12355306711239677, -25.31953145138690431 ) ) ;
#12498=CARTESIAN_POINT ( 'NONE',  ( -10.36489612227181745, 11.27711771225501813, -2.281195398064152169 ) ) ;
#12501=CARTESIAN_POINT ( 'NONE',  ( 51.90728952832269982, -49.37557461706570194, -77.08409367958790881 ) ) ;
#12503=EDGE_LOOP ( 'NONE', ( #44327, #25075, #42512, #24649 ) ) ;
#12504=CARTESIAN_POINT ( 'NONE',  ( 12.36320305029179956, 33.31445045633500257, -15.76422791923680045 ) ) ;
#12505=CARTESIAN_POINT ( 'NONE',  ( 52.35198176182720431, -50.04795459678859970, -76.97988188672849219 ) ) ;
#12507=AXIS2_PLACEMENT_3D ( 'NONE', #6589, #34609, #34870 ) ;
#12508=DIRECTION ( 'NONE',  ( 0.000000000000000000, 1.000000000000000000, 0.000000000000000000 ) ) ;
#12514=CARTESIAN_POINT ( 'NONE',  ( 41.35617304474619971, -44.65133728268560276, -5.195209045859010111 ) ) ;
#12515=CARTESIAN_POINT ( 'NONE',  ( 18.34117720853386402, -51.20617678333719880, -15.69346472551720240 ) ) ;
#12516=CARTESIAN_POINT ( 'NONE',  ( 56.43809645418499343, 13.88381105532070059, -15.14067943257860094 ) ) ;
#12521=VERTEX_POINT ( 'NONE', #4044 ) ;
#12522=CARTESIAN_POINT ( 'NONE',  ( 14.09775367411850056, -52.29987767205390270, -75.77396328158880578 ) ) ;
#12524=CARTESIAN_POINT ( 'NONE',  ( 47.29427773876249574, -54.72467116367779738, -54.70583352925600451 ) ) ;
#12525=PLANE ( 'NONE',  #12388 ) ;
#12528=DIRECTION ( 'NONE',  ( 0.3569024281753349626, 0.000000000000000000, 0.9341416684649872515 ) ) ;
#12529=CARTESIAN_POINT ( 'NONE',  ( 60.95893300201414178, -45.44404501095668536, -47.26315862579021143 ) ) ;
#12530=CARTESIAN_POINT ( 'NONE',  ( 61.75019796695539753, 13.88381105532070059, -28.15000000000000213 ) ) ;
#12531=CARTESIAN_POINT ( 'NONE',  ( 11.41644049898670055, 34.12404561335850417, -18.17421237887380414 ) ) ;
#12532=DIRECTION ( 'NONE',  ( 0.6888026391158329487, -0.7071067811865494601, 0.1598465650148944150 ) ) ;
#12533=CARTESIAN_POINT ( 'NONE',  ( 12.54923790319493726, -50.40993839913490149, -21.20205464686137020 ) ) ;
#12536=CARTESIAN_POINT ( 'NONE',  ( 48.75009304688830269, 22.82040167798450270, -55.10293387284019673 ) ) ;
#12537=EDGE_LOOP ( 'NONE', ( #19038, #32818, #3844, #16139, #15072 ) ) ;
#12540=VECTOR ( 'NONE', #4094, 1000.000000000000000 ) ;
#12544=CARTESIAN_POINT ( 'NONE',  ( 83.88693549187640031, 13.20239946185910007, -47.02124945944449763 ) ) ;
#12545=CARTESIAN_POINT ( 'NONE',  ( 54.22684962163910427, 16.84931794028459962, -26.38907994676030100 ) ) ;
#12548=CARTESIAN_POINT ( 'NONE',  ( 53.16274087092459411, 18.32513333159890223, -49.15255084583340306 ) ) ;
#12549=CARTESIAN_POINT ( 'NONE',  ( 55.99720521707869381, -45.19575551719779583, -15.52253582168630075 ) ) ;
#12552=ORIENTED_EDGE ( 'NONE', *, *, #31291, .T. ) ;
#12556=CARTESIAN_POINT ( 'NONE',  ( 12.13696592144739839, -65.16745155981689663, -16.64705455763589725 ) ) ;
#12557=CARTESIAN_POINT ( 'NONE',  ( 10.54842637916130066, 33.25339676159590141, -46.47926574070720562 ) ) ;
#12558=CARTESIAN_POINT ( 'NONE',  ( 18.66493251958384647, 20.21052494929402243, -15.73461886919979413 ) ) ;
#12559=CARTESIAN_POINT ( 'NONE',  ( 52.06890086575109677, -50.39494763447100212, -49.13506827049639725 ) ) ;
#12561=CARTESIAN_POINT ( 'NONE',  ( 11.45862936884678973, -65.29787451153411837, -22.69679117090718279 ) ) ;
#12563=ORIENTED_EDGE ( 'NONE', *, *, #43362, .F. ) ;
#12564=CARTESIAN_POINT ( 'NONE',  ( 12.89984683830242673, 19.51084698340348922, -21.40242721859379671 ) ) ;
#12565=CARTESIAN_POINT ( 'NONE',  ( 11.13393739769619906, -63.52234721269329754, -43.76018303787720498 ) ) ;
#12568=CARTESIAN_POINT ( 'NONE',  ( 50.90853239270390418, -50.90159765347700471, -76.14999999999999147 ) ) ;
#12572=DIRECTION ( 'NONE',  ( 0.000000000000000000, -1.000000000000000000, 0.000000000000000000 ) ) ;
#12574=CARTESIAN_POINT ( 'NONE',  ( 52.63898214176290224, 22.88375766151639823, -56.80548791163010236 ) ) ;
#12577=CARTESIAN_POINT ( 'NONE',  ( 55.44685761138700286, 19.71482051860210305, -75.10951000879100548 ) ) ;
#12579=CARTESIAN_POINT ( 'NONE',  ( 46.66850325959620704, -53.37252818194050263, -76.07618347743780873 ) ) ;
#12580=VERTEX_POINT ( 'NONE', #614 ) ;
#12581=VECTOR ( 'NONE', #34145, 1000.000000000000000 ) ;
#12585=CIRCLE ( 'NONE', #15914, 21.19999999999999929 ) ;
#12587=CARTESIAN_POINT ( 'NONE',  ( 47.29840941369229768, 23.06589208105410194, -75.29255935572381020 ) ) ;
#12589=CARTESIAN_POINT ( 'NONE',  ( 67.35174094906719233, 16.63381105532069881, -50.14999999999999858 ) ) ;
#12590=CARTESIAN_POINT ( 'NONE',  ( 75.04939620295748171, -15.61618894467929941, -11.30491871076499955 ) ) ;
#12591=CARTESIAN_POINT ( 'NONE',  ( 41.43651938946120339, -44.81260903795949702, -5.462494701013549836 ) ) ;
#12594=DIRECTION ( 'NONE',  ( 1.000000000000000000, 0.000000000000000000, 0.000000000000000000 ) ) ;
#12598=CARTESIAN_POINT ( 'NONE',  ( 61.55001819026519883, 13.91412166380790083, -46.61080972681389767 ) ) ;
#12599=CARTESIAN_POINT ( 'NONE',  ( -29.85095995338080144, -36.05272250015970315, -56.22640780866669985 ) ) ;
#12602=CARTESIAN_POINT ( 'NONE',  ( 53.11114670112049652, -49.51349214730240078, -48.80212167156650338 ) ) ;
#12603=CARTESIAN_POINT ( 'NONE',  ( 60.21567619441049857, -45.11618902539440512, -26.18204139926109875 ) ) ;
#12604=DIRECTION ( 'NONE',  ( 0.000000000000000000, 0.000000000000000000, -1.000000000000000000 ) ) ;
#12605=CARTESIAN_POINT ( 'NONE',  ( 56.17536208834479794, 14.86527153403829971, -26.07752106846319862 ) ) ;
#12607=CARTESIAN_POINT ( 'NONE',  ( 50.31585484903259697, 17.65744928731360375, -76.16276048729488934 ) ) ;
#12608=CARTESIAN_POINT ( 'NONE',  ( 53.28345105766870660, 18.19680193626409803, -48.89794168120269546 ) ) ;
#12617=CARTESIAN_POINT ( 'NONE',  ( 47.53847576963629251, -54.58151887390520329, -54.98789247430620009 ) ) ;
#12618=CARTESIAN_POINT ( 'NONE',  ( -3.777837493383019662, 16.75613853327890013, -4.322105422597779523 ) ) ;
#12620=CARTESIAN_POINT ( 'NONE',  ( 41.50224533218039369, 12.67611161623769966, -3.489448898335199889 ) ) ;
#12621=CARTESIAN_POINT ( 'NONE',  ( 59.95492767597970385, 15.44492512077309954, -48.75686613284650406 ) ) ;
#12623=DIRECTION ( 'NONE',  ( 1.000000000000000000, 0.000000000000000000, 0.000000000000000000 ) ) ;
#12626=AXIS2_PLACEMENT_3D ( 'NONE', #26405, #35318, #11490 ) ;
#12630=ORIENTED_EDGE ( 'NONE', *, *, #29278, .F. ) ;
#12631=CARTESIAN_POINT ( 'NONE',  ( 57.03107157439150399, 18.99627872735710099, -52.68131390763750233 ) ) ;
#12633=ORIENTED_EDGE ( 'NONE', *, *, #38152, .F. ) ;
#12635=CARTESIAN_POINT ( 'NONE',  ( 12.58828357193830172, -65.45077103634190507, -46.93561978748050478 ) ) ;
#12637=CARTESIAN_POINT ( 'NONE',  ( 51.41094451178410196, 19.64869940956030092, -76.16757071412951063 ) ) ;
#12639=DIRECTION ( 'NONE',  ( 1.000000000000000000, 0.000000000000000000, 0.000000000000000000 ) ) ;
#12641=CARTESIAN_POINT ( 'NONE',  ( 61.06898323382710458, 14.42329441383000166, -47.72188698851990551 ) ) ;
#12646=CARTESIAN_POINT ( 'NONE',  ( 12.20062103054560154, -65.06698704065620120, -24.22096211478449845 ) ) ;
#12650=CARTESIAN_POINT ( 'NONE',  ( 14.72993406020890106, 21.17773733622360410, -76.03043890231919022 ) ) ;
#12652=EDGE_CURVE ( 'NONE', #42937, #35762, #29166, .T. ) ;
#12656=EDGE_CURVE ( 'NONE', #14552, #35613, #21509, .T. ) ;
#12658=CARTESIAN_POINT ( 'NONE',  ( 83.66217889154638954, -44.50588631589649680, -46.56966809452229938 ) ) ;
#12659=CARTESIAN_POINT ( 'NONE',  ( 52.13393739769620083, -15.61618894467929941, 8.349999999999999645 ) ) ;
#12662=ORIENTED_EDGE ( 'NONE', *, *, #9872, .T. ) ;
#12663=CARTESIAN_POINT ( 'NONE',  ( 55.73706246701259914, -46.50826300295120319, -26.08342414098009954 ) ) ;
#12664=CARTESIAN_POINT ( 'NONE',  ( 15.33884134719679970, -50.95795189269119874, -21.05298682722330028 ) ) ;
#12665=CARTESIAN_POINT ( 'NONE',  ( 75.67065349138719910, 10.96988367743719905, -13.30225599929439895 ) ) ;
#12668=CARTESIAN_POINT ( 'NONE',  ( 48.01233081821040116, 14.92652286517469840, -11.04035587481109992 ) ) ;
#12669=ORIENTED_EDGE ( 'NONE', *, *, #42970, .F. ) ;
#12670=CARTESIAN_POINT ( 'NONE',  ( -8.353750934443111120, -44.79785993618280315, -5.771191893815999840 ) ) ;
#12671=CARTESIAN_POINT ( 'NONE',  ( 47.37241341519619908, 23.44179538337159840, -54.81883836474389682 ) ) ;
#12674=CARTESIAN_POINT ( 'NONE',  ( 57.26283650403279779, -50.61205995118769607, -53.75815461969219911 ) ) ;
#12675=CARTESIAN_POINT ( 'NONE',  ( 11.65058176314570204, 34.15932221946850689, -17.77752836889980159 ) ) ;
#12679=CARTESIAN_POINT ( 'NONE',  ( 57.78559058653489444, -47.16042636242490005, -48.07973249810120109 ) ) ;
#12682=CARTESIAN_POINT ( 'NONE',  ( 56.35963046933279941, 19.47216735375640084, -53.17943760849389889 ) ) ;
#12686=VERTEX_POINT ( 'NONE', #36769 ) ;
#12687=CARTESIAN_POINT ( 'NONE',  ( 20.08792735693718257, 24.05142850327904114, -19.47857086969157336 ) ) ;
#12688=CARTESIAN_POINT ( 'NONE',  ( 9.276689947635228251, 31.90394069607099681, -46.53283565787430831 ) ) ;
#12692=CARTESIAN_POINT ( 'NONE',  ( 18.76339275528779993, 20.38750180725810068, -74.54610039094001195 ) ) ;
#12693=ORIENTED_EDGE ( 'NONE', *, *, #32094, .F. ) ;
#12694=VERTEX_POINT ( 'NONE', #25226 ) ;
#12696=CARTESIAN_POINT ( 'NONE',  ( 11.48931359425379917, -64.94058050441130092, -46.32476902050240142 ) ) ;
#12697=CARTESIAN_POINT ( 'NONE',  ( 13.19564766795559940, 10.36739510386719942, -74.14999999999999147 ) ) ;
#12700=CARTESIAN_POINT ( 'NONE',  ( 61.44121449269439950, 14.11490161821189915, -47.30183376429939557 ) ) ;
#12704=ORIENTED_EDGE ( 'NONE', *, *, #45777, .T. ) ;
#12705=AXIS2_PLACEMENT_3D ( 'NONE', #40790, #36861, #44467 ) ;
#12706=CARTESIAN_POINT ( 'NONE',  ( 8.835310940912428634, -63.39783216298952340, -46.67672963611274639 ) ) ;
#12711=VERTEX_POINT ( 'NONE', #41232 ) ;
#12712=ORIENTED_EDGE ( 'NONE', *, *, #2055, .T. ) ;
#12715=CARTESIAN_POINT ( 'NONE',  ( 66.37097619575690999, 13.88381105527300008, -12.87819276387750200 ) ) ;
#12716=CARTESIAN_POINT ( 'NONE',  ( 48.60513791338269840, 13.96979094684940037, -10.18381246284539898 ) ) ;
#12717=DIRECTION ( 'NONE',  ( 0.5685928097855371677, 0.5944782866685501821, -0.5685928097855381669 ) ) ;
#12718=CARTESIAN_POINT ( 'NONE',  ( -4.835991491254990393, 16.08822738447750211, -4.623964749956109621 ) ) ;
#12720=CARTESIAN_POINT ( 'NONE',  ( 61.22342406473160281, 14.00737724369909998, -27.78055241644990048 ) ) ;
#12723=ORIENTED_EDGE ( 'NONE', *, *, #32815, .T. ) ;
#12724=FACE_OUTER_BOUND ( 'NONE', #34192, .T. ) ;
#12725=DIRECTION ( 'NONE',  ( 0.6911981449639432729, -0.7226652920947591596, -1.665334536937735304E-16 ) ) ;
#12726=CARTESIAN_POINT ( 'NONE',  ( 11.43204200631220147, 33.34744811485270333, -44.55415195516030025 ) ) ;
#12731=CARTESIAN_POINT ( 'NONE',  ( 12.32752973435950139, 18.90079518381709889, -21.15176878868719967 ) ) ;
#12732=CARTESIAN_POINT ( 'NONE',  ( 46.91750385626450282, 22.97282184422540396, -75.61476978748720512 ) ) ;
#12733=CARTESIAN_POINT ( 'NONE',  ( 49.30791778510940304, -53.55500811875160139, -54.21103610182979793 ) ) ;
#12734=CARTESIAN_POINT ( 'NONE',  ( -6.464119761774720807, 15.22590418212459973, -5.599264135990670077 ) ) ;
#12736=CARTESIAN_POINT ( 'NONE',  ( 65.36111454919441144, -32.61132143204090283, -18.37584003036852565 ) ) ;
#12738=EDGE_CURVE ( 'NONE', #26641, #7703, #12585, .T. ) ;
#12739=VERTEX_POINT ( 'NONE', #4813 ) ;
#12744=CARTESIAN_POINT ( 'NONE',  ( 61.28745719582129681, -45.57643085924389936, -47.65111777937660520 ) ) ;
#12745=CARTESIAN_POINT ( 'NONE',  ( 55.91596999402320023, 14.67228162054319895, -25.32543311652580087 ) ) ;
#12746=CARTESIAN_POINT ( 'NONE',  ( 72.30699981945301147, -43.38479194641627856, -12.49561599343400076 ) ) ;
#12752=CARTESIAN_POINT ( 'NONE',  ( 83.74313374146190370, -44.96662509718390055, -47.44649717229009411 ) ) ;
#12755=ORIENTED_EDGE ( 'NONE', *, *, #24143, .T. ) ;
#12756=CARTESIAN_POINT ( 'NONE',  ( 61.68987997863069950, -45.11739586860179685, -46.50241001583690093 ) ) ;
#12757=CARTESIAN_POINT ( 'NONE',  ( 53.11711213144224075, -50.37382258259036405, -77.21690155561020674 ) ) ;
#12758=CARTESIAN_POINT ( 'NONE',  ( 76.45005458917839292, -6.303208319860135411, -13.01219602681204890 ) ) ;
#12759=CARTESIAN_POINT ( 'NONE',  ( 52.54597304093680776, -52.44574054386669815, -54.34384594454520112 ) ) ;
#12760=EDGE_LOOP ( 'NONE', ( #19770, #33450, #34068, #30674 ) ) ;
#12765=ADVANCED_FACE ( 'NONE', ( #25741 ), #9789, .F. ) ;
#12767=DIRECTION ( 'NONE',  ( -0.7226652920947586045, 0.6911981449639438280, 0.000000000000000000 ) ) ;
#12769=CARTESIAN_POINT ( 'NONE',  ( 52.25096642469739550, -49.77129145263110388, -77.19024991109920109 ) ) ;
#12774=CIRCLE ( 'NONE', #47084, 2.000000000000000000 ) ;
#12775=CARTESIAN_POINT ( 'NONE',  ( 52.87559987180819832, -50.28015522989610275, -77.15855498308799554 ) ) ;
#12777=CARTESIAN_POINT ( 'NONE',  ( 60.61199691158600444, 14.35120867319030147, -47.15909868881769995 ) ) ;
#12780=CARTESIAN_POINT ( 'NONE',  ( 54.26302937888129918, 19.38381105532069881, -76.97756791992739522 ) ) ;
#12781=CARTESIAN_POINT ( 'NONE',  ( 43.52841460840770083, -43.39558596462239848, -4.940445812193139830 ) ) ;
#12782=DIRECTION ( 'NONE',  ( 0.000000000000000000, 0.000000000000000000, -1.000000000000000000 ) ) ;
#12783=CARTESIAN_POINT ( 'NONE',  ( 61.28293951100584991, -45.60372950919332879, -47.68063998090632083 ) ) ;
#12784=CARTESIAN_POINT ( 'NONE',  ( 61.44929317945270242, -45.39846556447219683, -47.39907545912859632 ) ) ;
#12788=CARTESIAN_POINT ( 'NONE',  ( 65.13923175699828505, 0.9544840682940559651, -17.74408481280750038 ) ) ;
#12789=B_SPLINE_SURFACE_WITH_KNOTS ( 'NONE', 3, 3, ( 
 ( #26199, #50068, #37495, #13909, #22526, #29866 ),
 ( #50333, #49817, #14163, #26457, #42210, #34320 ),
 ( #45886, #42472, #22266, #2635, #1595, #46153 ),
 ( #9973, #1855, #17583, #49571, #34059, #6561 ),
 ( #38538, #13656, #42734, #25935, #14421, #50588 ),
 ( #41950, #30131, #33553, #10240, #30390, #18090 ),
 ( #41681, #29617, #14678, #22007, #30648, #37759 ),
 ( #18606, #45620, #26716, #46671, #34584, #2111 ),
 ( #10757, #6308, #17833, #9720, #25679, #5789 ),
 ( #38274, #21749, #33806, #2365, #18343, #46413 ) ),
 .UNSPECIFIED., .F., .F., .F.,
 ( 4, 2, 2, 2, 4 ),
 ( 4, 1, 1, 4 ),
 ( 1.507842000000000029E-11, 0.03085333683225299772, 0.08021867573973200105, 0.1592032179916990087, 0.2468266945524750233 ),
 ( 0.000000000000000000, 0.3333333333333329818, 0.6666666666666670737, 1.000000000000000000 ),
 .UNSPECIFIED. ) ;
#12792=CARTESIAN_POINT ( 'NONE',  ( 13.93677001678689997, -51.54257389745239948, -75.18091805976820297 ) ) ;
#12793=CARTESIAN_POINT ( 'NONE',  ( 47.29837881414660217, -54.72153260654879858, -54.69571569007759848 ) ) ;
#12796=CARTESIAN_POINT ( 'NONE',  ( 60.84935194822133298, -45.45999311571661394, -47.05836674529819419 ) ) ;
#12798=DIRECTION ( 'NONE',  ( 0.000000000000000000, 0.000000000000000000, -1.000000000000000000 ) ) ;
#12799=CARTESIAN_POINT ( 'NONE',  ( 47.72549663628029748, -54.49022007495739928, -54.99080477840750092 ) ) ;
#12800=B_SPLINE_CURVE_WITH_KNOTS ( 'NONE', 3,
 ( #24772, #4883, #41816, #49441, #26075, #5923, #17970, #21887, #1212, #37625 ),
 .UNSPECIFIED., .F., .F.,
 ( 4, 2, 2, 2, 4 ),
 ( 0.000000000000000000, 0.2500000000000000000, 0.5000000000000000000, 0.7500000000000000000, 1.000000000000000000 ),
 .UNSPECIFIED. ) ;
#12801=CARTESIAN_POINT ( 'NONE',  ( 47.41053031099697535, 23.00881197028234126, -75.29848679969852299 ) ) ;
#12802=CARTESIAN_POINT ( 'NONE',  ( -8.353750934443111120, -44.79785993618280315, -5.771191893815999840 ) ) ;
#12804=CARTESIAN_POINT ( 'NONE',  ( 48.89501045483829955, 22.56229972626200109, -54.41963477494619639 ) ) ;
#12810=CARTESIAN_POINT ( 'NONE',  ( 18.86789271228509790, -51.78678246903520233, -74.14999999999999147 ) ) ;
#12813=CARTESIAN_POINT ( 'NONE',  ( 83.93027249483741059, 13.00900601712620031, -46.75947739037570017 ) ) ;
#12814=CARTESIAN_POINT ( 'NONE',  ( 52.66238559674269482, 18.53796498309249685, -28.15003238672679942 ) ) ;
#12816=CARTESIAN_POINT ( 'NONE',  ( 12.16231664502931054, 33.44509448364060233, -15.91745067705889838 ) ) ;
#12817=CARTESIAN_POINT ( 'NONE',  ( 55.34563173526050406, -45.32107452727160535, -15.30572482678790003 ) ) ;
#12821=CARTESIAN_POINT ( 'NONE',  ( 11.74706319441139968, -64.93826315237700442, -16.38446683801559800 ) ) ;
#12822=CARTESIAN_POINT ( 'NONE',  ( 11.17936320866890121, 33.58498632846880128, -46.45233409225559740 ) ) ;
#12824=CARTESIAN_POINT ( 'NONE',  ( 52.81610072646800091, -49.60570963100419561, -48.45273747379939522 ) ) ;
#12828=CARTESIAN_POINT ( 'NONE',  ( 57.08024762781600003, 14.64810207517410134, -26.24981380567940192 ) ) ;
#12829=EDGE_CURVE ( 'NONE', #19377, #29939, #47154, .T. ) ;
#12831=CARTESIAN_POINT ( 'NONE',  ( 52.20232727811570328, 19.58445708673409769, -50.88848071883410284 ) ) ;
#12833=CARTESIAN_POINT ( 'NONE',  ( 50.35727174400659578, -49.18175002857950062, -76.16289466383710760 ) ) ;
#12837=CARTESIAN_POINT ( 'NONE',  ( 55.48119509741179911, -46.46935189257190757, -25.44855095864909700 ) ) ;
#12841=CARTESIAN_POINT ( 'NONE',  ( 54.67502978642529854, 16.95168370974520400, -47.75230923849440501 ) ) ;
#12843=CARTESIAN_POINT ( 'NONE',  ( 14.29753605308300024, -51.11618894450129602, -22.54695281101919946 ) ) ;
#12844=CARTESIAN_POINT ( 'NONE',  ( 56.50762836072709661, 19.50983102606420161, -74.45401218589749703 ) ) ;
#12845=CARTESIAN_POINT ( 'NONE',  ( 47.42184924485919595, -54.61356341195660491, -74.50157339271500234 ) ) ;
#12846=ORIENTED_EDGE ( 'NONE', *, *, #48977, .F. ) ;
#12851=CARTESIAN_POINT ( 'NONE',  ( 52.74518595131819865, -49.73996312209429504, -48.86818382069139943 ) ) ;
#12855=CARTESIAN_POINT ( 'NONE',  ( 47.06884450802159847, 22.81823520743029832, -75.65261601872900599 ) ) ;
#12861=CIRCLE ( 'NONE', #32917, 1.000000000000000888 ) ;
#12866=CARTESIAN_POINT ( 'NONE',  ( 61.05616912171839772, 14.11849417979069976, -46.88539273277700659 ) ) ;
#12867=CARTESIAN_POINT ( 'NONE',  ( -18.27909364759860011, -51.95925980240359365, -53.14840429075749739 ) ) ;
#12869=CARTESIAN_POINT ( 'NONE',  ( 52.72694793081979725, -49.72266251536069603, -48.50422612237640152 ) ) ;
#12870=CARTESIAN_POINT ( 'NONE',  ( 57.65728964160980041, -45.29188684180090263, -25.94504736113060162 ) ) ;
#12871=CARTESIAN_POINT ( 'NONE',  ( 47.64143405402000297, -54.53488714544439375, -55.14905519569939685 ) ) ;
#12872=CARTESIAN_POINT ( 'NONE',  ( 57.20820941486360312, 14.23063652483599917, -26.05769543974410141 ) ) ;
#12874=CARTESIAN_POINT ( 'NONE',  ( 51.47089496436409917, 18.97848234860349947, -76.34335219576519194 ) ) ;
#12875=CARTESIAN_POINT ( 'NONE',  ( 53.10972315773789632, 18.29799478634210175, -48.97251032828970096 ) ) ;
#12877=CARTESIAN_POINT ( 'NONE',  ( 41.36297991754139503, -44.03288059546800781, -3.553637027260359904 ) ) ;
#12878=CARTESIAN_POINT ( 'NONE',  ( 72.02934741333440627, -44.96049524349189852, -13.48211756204479883 ) ) ;
#12879=VERTEX_POINT ( 'NONE', #19063 ) ;
#12883=AXIS2_PLACEMENT_3D ( 'NONE', #35553, #43679, #27417 ) ;
#12885=CARTESIAN_POINT ( 'NONE',  ( 47.46911263023690708, -54.60293551959159686, -54.68220836887759617 ) ) ;
#12888=CARTESIAN_POINT ( 'NONE',  ( 59.79179082184240457, -29.88504740574800067, -15.96111194127940180 ) ) ;
#12897=CARTESIAN_POINT ( 'NONE',  ( 9.299128317299539148, -63.29430534918720497, -46.53057822423220102 ) ) ;
#12898=EDGE_CURVE ( 'NONE', #25812, #30115, #2124, .T. ) ;
#12901=CARTESIAN_POINT ( 'NONE',  ( 11.55362782463430094, -64.75226748267719756, -44.82234361046789672 ) ) ;
#12903=CARTESIAN_POINT ( 'NONE',  ( 56.46551567295650642, 19.54378694285259854, -74.14999999999999147 ) ) ;
#12904=CARTESIAN_POINT ( 'NONE',  ( 52.36416843628920503, 19.71812798544510059, -76.17671310447180133 ) ) ;
#12908=DIRECTION ( 'NONE',  ( 0.000000000000000000, 0.000000000000000000, 1.000000000000000000 ) ) ;
#12913=SHAPE_REPRESENTATION_RELATIONSHIP ( 'NONE' , 'NONE' ,  #4683, #12306 ) ;
#12915=CARTESIAN_POINT ( 'NONE',  ( 12.73541647155440160, -65.46958205238559003, -23.66121539185130018 ) ) ;
#12918=EDGE_CURVE ( 'NONE', #15737, #14356, #36807, .T. ) ;
#12922=CARTESIAN_POINT ( 'NONE',  ( 84.41931940662119871, -43.28155674284490573, -47.35294421590279512 ) ) ;
#12925=CARTESIAN_POINT ( 'NONE',  ( 52.87930525205649701, -49.56712260999589859, -27.60362057165029981 ) ) ;
#12926=CARTESIAN_POINT ( 'NONE',  ( 15.80909573684840019, -51.11619220056719826, -21.61146777487360282 ) ) ;
#12928=DIRECTION ( 'NONE',  ( 0.000000000000000000, 0.000000000000000000, 1.000000000000000000 ) ) ;
#12929=DIRECTION ( 'NONE',  ( 0.000000000000000000, 0.000000000000000000, 1.000000000000000000 ) ) ;
#12930=ORIENTED_EDGE ( 'NONE', *, *, #31503, .F. ) ;
#12931=CARTESIAN_POINT ( 'NONE',  ( -8.073667307587539810, -44.97251519369510220, -5.525879325573529677 ) ) ;
#12932=CARTESIAN_POINT ( 'NONE',  ( 47.45724465533079695, 23.37779319940769795, -54.67644539602360254 ) ) ;
#12936=CARTESIAN_POINT ( 'NONE',  ( 11.64437502030500049, 34.15964300405810405, -17.80448360229059901 ) ) ;
#12940=CARTESIAN_POINT ( 'NONE',  ( 57.19193614679419824, -47.47137610322729984, -48.20267525396420183 ) ) ;
#12944=CARTESIAN_POINT ( 'NONE',  ( 17.78432835213279972, -52.62916658892859800, -76.03098605356829864 ) ) ;
#12950=CARTESIAN_POINT ( 'NONE',  ( 10.13445450645900081, 31.88305279702909800, -45.99826666626069738 ) ) ;
#12952=VECTOR ( 'NONE', #41079, 1000.000000000000000 ) ;
#12953=CYLINDRICAL_SURFACE ( 'NONE', #23, 2.000000000000000444 ) ;
#12954=VERTEX_POINT ( 'NONE', #11216 ) ;
#12955=CARTESIAN_POINT ( 'NONE',  ( 18.20176657162249967, 20.17488022308399920, -75.08736963500949457 ) ) ;
#12956=ORIENTED_EDGE ( 'NONE', *, *, #34703, .T. ) ;
#12961=CARTESIAN_POINT ( 'NONE',  ( 13.00893739769619906, -65.51843714052719747, -47.75434321273180416 ) ) ;
#12965=CARTESIAN_POINT ( 'NONE',  ( 61.54660442415410415, 14.01734467809300000, -47.08946784971580257 ) ) ;
#12968=EDGE_LOOP ( 'NONE', ( #36527, #15597, #18724, #22904, #688 ) ) ;
#12972=CARTESIAN_POINT ( 'NONE',  ( 49.62157902422839584, -46.18329155571620248, -12.18456390873380002 ) ) ;
#12974=CARTESIAN_POINT ( 'NONE',  ( 9.125046732747128075, -54.99886678830583264, -46.59642014776720487 ) ) ;
#12977=EDGE_LOOP ( 'NONE', ( #35774, #9091, #18734, #50473, #50631 ) ) ;
#12979=CARTESIAN_POINT ( 'NONE',  ( 3.901957390959666760, -24.50324262128464170, -6.721843382729280059 ) ) ;
#12980=CARTESIAN_POINT ( 'NONE',  ( 75.48397637297750862, 12.14069267741320068, -13.40632821845509959 ) ) ;
#12981=CARTESIAN_POINT ( 'NONE',  ( 47.44609020368039864, 14.70937406344200049, -10.50457812665930035 ) ) ;
#12983=EDGE_CURVE ( 'NONE', #19647, #16412, #33385, .T. ) ;
#12984=FACE_OUTER_BOUND ( 'NONE', #38341, .T. ) ;
#12985=CARTESIAN_POINT ( 'NONE',  ( -3.223188684962630113, 17.15855307271669616, -4.799566724645049298 ) ) ;
#12986=CARTESIAN_POINT ( 'NONE',  ( 3.310925894260581703, -55.48813533678121246, -8.795375239069176843 ) ) ;
#12989=ORIENTED_EDGE ( 'NONE', *, *, #38834, .T. ) ;
#12990=CARTESIAN_POINT ( 'NONE',  ( 53.48663704682059716, 18.10898805450199944, -49.00013169075800334 ) ) ;
#12991=VECTOR ( 'NONE', #10668, 1000.000000000000227 ) ;
#12992=CARTESIAN_POINT ( 'NONE',  ( -8.936454256227198911, -44.38145435695279417, -6.564742439952559572 ) ) ;
#12993=CARTESIAN_POINT ( 'NONE',  ( 12.43322004349129983, 34.16501222894959966, -46.71928908691679538 ) ) ;
#12996=EDGE_CURVE ( 'NONE', #41755, #24512, #41009, .T. ) ;
#12998=CARTESIAN_POINT ( 'NONE',  ( 47.03254114365169869, 23.23399901970210379, -75.29848703692678669 ) ) ;
#12999=CARTESIAN_POINT ( 'NONE',  ( 49.58793114173199967, -53.63459837187430423, -54.62161527680289907 ) ) ;
#13008=CARTESIAN_POINT ( 'NONE',  ( 84.37071824919731000, -43.44691537143197024, -47.23470636383878229 ) ) ;
#13009=CARTESIAN_POINT ( 'NONE',  ( 60.98979597045209999, -45.65772911195310257, -47.70964152097329958 ) ) ;
#13011=CARTESIAN_POINT ( 'NONE',  ( 44.97169576857614715, -43.53794996313975219, -5.328605099819570867 ) ) ;
#13014=CARTESIAN_POINT ( 'NONE',  ( 50.97251369907100838, -50.96426704539258168, -76.14992187625421138 ) ) ;
#13017=CARTESIAN_POINT ( 'NONE',  ( 84.02703262422839714, -44.63621804162450246, -47.45290575524859378 ) ) ;
#13023=CARTESIAN_POINT ( 'NONE',  ( 61.57010480345100234, -45.13191874552030214, -46.48558154903869166 ) ) ;
#13024=CARTESIAN_POINT ( 'NONE',  ( 52.75990471363306256, -50.16877946593007209, -77.25922079919111241 ) ) ;
#13026=CARTESIAN_POINT ( 'NONE',  ( 76.40893147262282525, -10.52065843673467604, -12.83499039722492086 ) ) ;
#13028=EDGE_CURVE ( 'NONE', #42929, #28327, #38508, .T. ) ;
#13033=CARTESIAN_POINT ( 'NONE',  ( 56.83258906378680564, 19.07284248766010393, -52.72698304056530105 ) ) ;
#13039=ORIENTED_EDGE ( 'NONE', *, *, #31387, .T. ) ;
#13040=CARTESIAN_POINT ( 'NONE',  ( 8.784728771177240603, -63.11543068614769680, -46.67204636144870022 ) ) ;
#13041=CARTESIAN_POINT ( 'NONE',  ( 53.23471707971139466, -50.42895756372370641, -77.19501644749119862 ) ) ;
#13043=B_SPLINE_CURVE_WITH_KNOTS ( 'NONE', 3,
 ( #28723, #25814, #25560, #5680, #5931, #45511, #46030, #5420, #45768, #6193, #41566, #9358, #46293, #33432, #37632, #25305 ),
 .UNSPECIFIED., .F., .F.,
 ( 4, 2, 2, 2, 2, 2, 2, 4 ),
 ( 0.000000000000000000, 1.325233610615540014, 2.839786308461869968, 3.786381744615829881, 4.259679462692810503, 5.016955811615980032, 6.228597969893040265, 7.438175257738109281 ),
 .UNSPECIFIED. ) ;
#13047=DIRECTION ( 'NONE',  ( 0.000000000000000000, 0.000000000000000000, 1.000000000000000000 ) ) ;
#13049=CARTESIAN_POINT ( 'NONE',  ( 42.99451563336680238, -43.12780611646349627, -4.474847206139059175 ) ) ;
#13051=CARTESIAN_POINT ( 'NONE',  ( 68.13393739769847457, -50.70395984887981200, -74.34354914830335304 ) ) ;
#13052=CARTESIAN_POINT ( 'NONE',  ( 53.43679795862831128, 18.11049644000932446, -48.83615822496557257 ) ) ;
#13056=CARTESIAN_POINT ( 'NONE',  ( 65.33368228454421001, 0.7990771883881800930, -17.55777972051419766 ) ) ;
#13057=VERTEX_POINT ( 'NONE', #45247 ) ;
#13058=CIRCLE ( 'NONE', #16392, 1.500000000000001332 ) ;
#13059=CARTESIAN_POINT ( 'NONE',  ( 13.89821648398999798, -52.00201191962840142, -75.51495726157199329 ) ) ;
#13060=CARTESIAN_POINT ( 'NONE',  ( 47.28596910495269867, -54.73079917377950210, -54.72607146539549916 ) ) ;
#13066=CARTESIAN_POINT ( 'NONE',  ( 57.49550338311457409, 13.88380786636074404, -25.40179352645802169 ) ) ;
#13067=CARTESIAN_POINT ( 'NONE',  ( 47.73402016065340092, -54.47968219234450515, -54.93079182720929765 ) ) ;
#13068=ADVANCED_FACE ( 'NONE', ( #41052 ), #30216, .F. ) ;
#13069=CARTESIAN_POINT ( 'NONE',  ( 14.16379049197029971, 19.89932140060919963, -22.70798727815419937 ) ) ;
#13070=CARTESIAN_POINT ( 'NONE',  ( 13.58165717576775755, -51.39134915169243811, -22.62650423440272718 ) ) ;
#13073=CARTESIAN_POINT ( 'NONE',  ( 48.47402464779260356, 22.93984571062519962, -55.13672603318829601 ) ) ;
#13074=VERTEX_POINT ( 'NONE', #26539 ) ;
#13077=AXIS2_PLACEMENT_3D ( 'NONE', #47620, #35027, #46859 ) ;
#13079=CARTESIAN_POINT ( 'NONE',  ( 61.31807987960689843, -45.64188066342459393, -47.72348187499480332 ) ) ;
#13081=CARTESIAN_POINT ( 'NONE',  ( 83.71081252132779582, 13.23966547877859945, -46.63777445865510174 ) ) ;
#13082=CARTESIAN_POINT ( 'NONE',  ( 56.15977899178509603, 14.78509994814519857, -26.01523765823269940 ) ) ;
#13085=CARTESIAN_POINT ( 'NONE',  ( 56.79492093344569525, -45.11618894467940066, -15.79526079812830197 ) ) ;
#13086=CARTESIAN_POINT ( 'NONE',  ( 17.21347160910339724, 21.88381105532300097, -76.14999999999999147 ) ) ;
#13087=B_SPLINE_CURVE_WITH_KNOTS ( 'NONE', 3,
 ( #8381, #31684, #24072, #48735, #40092, #28797, #8636, #8128, #24331, #36655, #36397, #24588, #16493, #20161, #760, #48472 ),
 .UNSPECIFIED., .F., .F.,
 ( 4, 2, 2, 2, 2, 2, 2, 4 ),
 ( -1.480557251969420118, -1.467872963798670050, -1.112024972574749970, -0.8896199780598010864, -0.7784174808023259784, -0.6004934851903659387, -0.3158150922112299419, 0.000000000000000000 ),
 .UNSPECIFIED. ) ;
#13088=VECTOR ( 'NONE', #24096, 1000.000000000000000 ) ;
#13090=EDGE_LOOP ( 'NONE', ( #6032, #32709 ) ) ;
#13091=CARTESIAN_POINT ( 'NONE',  ( 12.07292176418390106, -65.23870394393370020, -16.81897063589060082 ) ) ;
#13092=CARTESIAN_POINT ( 'NONE',  ( 10.99330672749469962, 32.73200627569549681, -45.08259804521770064 ) ) ;
#13095=CARTESIAN_POINT ( 'NONE',  ( 49.41922605943800306, -52.95060041720219601, -52.58244047610669725 ) ) ;
#13098=ORIENTED_EDGE ( 'NONE', *, *, #17177, .F. ) ;
#13100=CARTESIAN_POINT ( 'NONE',  ( 65.03603135455020379, -32.24781572988710110, -17.83403478221860183 ) ) ;
#13101=LINE ( 'NONE', #1280, #44625 ) ;
#13104=CARTESIAN_POINT ( 'NONE',  ( 50.29495137051839748, -49.91812883465070172, -76.14999999999999147 ) ) ;
#13109=ORIENTED_EDGE ( 'NONE', *, *, #34427, .T. ) ;
#13115=CARTESIAN_POINT ( 'NONE',  ( 47.24300521349800164, -54.11747037892259726, -75.51940560377390455 ) ) ;
#13117=CARTESIAN_POINT ( 'NONE',  ( 56.08436785131110014, 14.47011228136549832, -17.93020320136680112 ) ) ;
#13118=CARTESIAN_POINT ( 'NONE',  ( 57.24718409717750234, -50.61618894895349996, -53.91456318682789828 ) ) ;
#13122=ORIENTED_EDGE ( 'NONE', *, *, #41817, .T. ) ;
#13123=CARTESIAN_POINT ( 'NONE',  ( 47.50285655629340198, 23.36688955440150295, -74.19742682671839873 ) ) ;
#13126=VECTOR ( 'NONE', #26835, 1000.000000000000000 ) ;
#13130=EDGE_CURVE ( 'NONE', #44442, #51033, #46076, .T. ) ;
#13134=CARTESIAN_POINT ( 'NONE',  ( -12.01951210174429896, -55.39328561125270056, -51.29522465964590339 ) ) ;
#13135=EDGE_CURVE ( 'NONE', #35688, #14446, #42553, .T. ) ;
#13137=CARTESIAN_POINT ( 'NONE',  ( 53.43246109065159999, -49.34667644580379431, -48.81566079192110408 ) ) ;
#13138=CARTESIAN_POINT ( 'NONE',  ( 61.66984040017980107, -45.11833727456389198, -28.15134406664559563 ) ) ;
#13139=CARTESIAN_POINT ( 'NONE',  ( 47.67211062985429493, -54.52182009381669303, -55.16489596303849652 ) ) ;
#13140=CARTESIAN_POINT ( 'NONE',  ( 13.58375825965479855, 19.57881046872019937, -21.57335430205159810 ) ) ;
#13141=CARTESIAN_POINT ( 'NONE',  ( 56.14448110115399970, 14.68078269655329926, -25.90882037036080021 ) ) ;
#13143=CARTESIAN_POINT ( 'NONE',  ( 51.40462280232849679, 19.31602561253640005, -76.23573550552218592 ) ) ;
#13144=CARTESIAN_POINT ( 'NONE',  ( 52.76130411716530233, 18.47365434860499889, -48.70176833931630256 ) ) ;
#13152=CARTESIAN_POINT ( 'NONE',  ( 47.46188864440789956, -54.61821625934059909, -54.80977015378280015 ) ) ;
#13156=CARTESIAN_POINT ( 'NONE',  ( 53.02240706027900075, 18.32760744209570092, -48.78672998508179859 ) ) ;
#13162=EDGE_CURVE ( 'NONE', #3494, #12469, #23990, .T. ) ;
#13165=ORIENTED_EDGE ( 'NONE', *, *, #15560, .F. ) ;
#13166=CARTESIAN_POINT ( 'NONE',  ( 8.956863767676178867, -63.15483629195879445, -46.63369080061400496 ) ) ;
#13167=CARTESIAN_POINT ( 'NONE',  ( -4.849986043992698725, -15.61618894467930119, 6.789625226207629538 ) ) ;
#13168=ORIENTED_EDGE ( 'NONE', *, *, #12229, .T. ) ;
#13171=CARTESIAN_POINT ( 'NONE',  ( 56.13223116304230587, 19.60886586524600261, -74.69896703041874275 ) ) ;
#13172=CARTESIAN_POINT ( 'NONE',  ( 52.30043100026959735, 19.46767200232369888, -76.35983844399039810 ) ) ;
#13175=CARTESIAN_POINT ( 'NONE',  ( 63.88393739769619373, 11.88381105532070059, -61.44999999999999574 ) ) ;
#13181=CARTESIAN_POINT ( 'NONE',  ( 53.65235395033388244, 20.09310193608997963, -75.57543365061850693 ) ) ;
#13182=ORIENTED_EDGE ( 'NONE', *, *, #27452, .T. ) ;
#13185=LINE ( 'NONE', #20745, #28741 ) ;
#13186=CARTESIAN_POINT ( 'NONE',  ( 14.77000656121960098, 21.15196775986840194, -76.02269426304029309 ) ) ;
#13187=CARTESIAN_POINT ( 'NONE',  ( 51.80594958079759493, 17.96077681129019865, -77.05312856993060677 ) ) ;
#13188=CARTESIAN_POINT ( 'NONE',  ( 84.12790934798559306, -43.97578464600089632, -46.91176635807759254 ) ) ;
#13191=CARTESIAN_POINT ( 'NONE',  ( 52.93948662983430609, -49.53590707237739821, -27.64880802112100255 ) ) ;
#13193=CARTESIAN_POINT ( 'NONE',  ( 16.33938386690050137, -51.09625719537829980, -20.40297663956910057 ) ) ;
#13197=ORIENTED_EDGE ( 'NONE', *, *, #46823, .F. ) ;
#13198=CARTESIAN_POINT ( 'NONE',  ( -4.005781160639729777, -47.98584768802999889, -5.016607454399269805 ) ) ;
#13199=CARTESIAN_POINT ( 'NONE',  ( 47.21267495741800246, 23.55157179986399996, -54.62953672193049925 ) ) ;
#13203=CARTESIAN_POINT ( 'NONE',  ( 11.88601302014030026, 34.20290939426369903, -17.88642737458170018 ) ) ;
#13205=CARTESIAN_POINT ( 'NONE',  ( 53.11114665040049942, 18.28111428451730092, -48.80212166739749335 ) ) ;
#13207=CARTESIAN_POINT ( 'NONE',  ( 60.26929283095270051, -45.78778679473020219, -47.49574889169500125 ) ) ;
#13209=CARTESIAN_POINT ( 'NONE',  ( 52.69990148663700325, 21.03144630651199876, -53.73602009713189886 ) ) ;
#13214=CARTESIAN_POINT ( 'NONE',  ( 8.962435484615378201, 31.95416093520460521, -46.63293154189879886 ) ) ;
#13215=CARTESIAN_POINT ( 'NONE',  ( 41.99202299628319679, 13.65299255882769991, -5.712667844576049703 ) ) ;
#13216=CARTESIAN_POINT ( 'NONE',  ( 67.93181682611671590, -30.30591887840110132, -17.84857444314360109 ) ) ;
#13218=EDGE_CURVE ( 'NONE', #37955, #42552, #35912, .T. ) ;
#13219=CARTESIAN_POINT ( 'NONE',  ( 18.30878848283549942, 19.99149262732870014, -74.56034069004439857 ) ) ;
#13222=DIRECTION ( 'NONE',  ( 0.000000000000000000, 0.000000000000000000, 1.000000000000000000 ) ) ;
#13225=CARTESIAN_POINT ( 'NONE',  ( 11.93682371713649992, -65.18248445933780033, -46.46134574452209876 ) ) ;
#13226=CARTESIAN_POINT ( 'NONE',  ( 57.44440056792399929, -45.44038579893220486, -26.07919784721820022 ) ) ;
#13228=CARTESIAN_POINT ( 'NONE',  ( 61.68987241420879997, 13.88502446954749914, -46.37201345370000638 ) ) ;
#13232=ORIENTED_EDGE ( 'NONE', *, *, #37514, .T. ) ;
#13233=CARTESIAN_POINT ( 'NONE',  ( 49.49077763376009642, -45.96749055206419854, -11.95218223477760056 ) ) ;
#13235=CARTESIAN_POINT ( 'NONE',  ( 16.13393739769620083, -15.61618894467929941, -7.349999999999999645 ) ) ;
#13238=CARTESIAN_POINT ( 'NONE',  ( 46.35275103504449845, -52.90993241930539881, -76.14999999999999147 ) ) ;
#13239=CARTESIAN_POINT ( 'NONE',  ( 60.65419404070010501, 14.53878550406569836, -47.75595165931559904 ) ) ;
#13240=STYLED_ITEM ( 'NONE', ( #462 ), #44299 ) ;
#13241=CARTESIAN_POINT ( 'NONE',  ( 51.83641662704179964, 14.98333576533859990, -13.79431318377310056 ) ) ;
#13244=CARTESIAN_POINT ( 'NONE',  ( -7.993718939281059477, 13.74763319926180039, -5.173449967684150330 ) ) ;
#13246=CARTESIAN_POINT ( 'NONE',  ( 59.69861616638479518, 13.89146436216049807, -26.11287264892089865 ) ) ;
#13248=EDGE_LOOP ( 'NONE', ( #24357, #3991, #12065, #8107, #41363, #5232 ) ) ;
#13249=CARTESIAN_POINT ( 'NONE',  ( 54.37486050126969417, 17.76197798406979800, -48.98148910212459839 ) ) ;
#13254=CARTESIAN_POINT ( 'NONE',  ( 82.45639937995038338, -45.09267748618990623, -46.38982090304390482 ) ) ;
#13256=CARTESIAN_POINT ( 'NONE',  ( 49.22434610110619246, -53.62684526786699735, -54.29818755095050165 ) ) ;
#13257=CARTESIAN_POINT ( 'NONE',  ( 51.35265160182996880, -31.92979185925464591, -17.41534043387646236 ) ) ;
#13259=CARTESIAN_POINT ( 'NONE',  ( 18.66237950319839811, -51.43164378700720363, -74.36773579015570590 ) ) ;
#13260=CARTESIAN_POINT ( 'NONE',  ( 55.89576372857870012, -50.73744799429999830, -52.91533302817010309 ) ) ;
#13261=VERTEX_POINT ( 'NONE', #28078 ) ;
#13265=CARTESIAN_POINT ( 'NONE',  ( 60.70915627887830368, -45.63243799255800326, -47.54512464986149922 ) ) ;
#13268=CARTESIAN_POINT ( 'NONE',  ( 13.04450223504579931, 18.79195994071550047, -21.04428001324339803 ) ) ;
#13271=CARTESIAN_POINT ( 'NONE',  ( 51.55044215929650164, -51.25128868776180013, -76.08578283986020097 ) ) ;
#13272=CYLINDRICAL_SURFACE ( 'NONE', #32782, 20.00000000000000355 ) ;
#13273=ORIENTED_EDGE ( 'NONE', *, *, #27106, .T. ) ;
#13276=EDGE_CURVE ( 'NONE', #43378, #27228, #10944, .T. ) ;
#13278=CARTESIAN_POINT ( 'NONE',  ( 61.68987299561999293, -45.11740230825230213, -46.37193444313120239 ) ) ;
#13280=( BOUNDED_CURVE ( )  B_SPLINE_CURVE ( 3, ( #6615, #42005, #6103, #14734 ),
 .UNSPECIFIED., .F., .T. ) 
 B_SPLINE_CURVE_WITH_KNOTS ( ( 4, 4 ),
 ( 0.5363495246926816007, 0.7853981633974366217 ),
 .UNSPECIFIED. ) 
 CURVE ( )  GEOMETRIC_REPRESENTATION_ITEM ( )  RATIONAL_B_SPLINE_CURVE ( ( 1.000000000000000000, 0.9948379068877994946, 0.9948379068877994946, 1.000000000000000000 ) ) 
 REPRESENTATION_ITEM ( '' )  );
#13284=CARTESIAN_POINT ( 'NONE',  ( 11.47911758231620993, 34.07625331222116927, -22.67538628410606805 ) ) ;
#13290=DIRECTION ( 'NONE',  ( 1.562192859871379910E-09, -1.089021445294679944E-09, 1.000000000000000000 ) ) ;
#13291=CARTESIAN_POINT ( 'NONE',  ( 52.90771576829140344, -50.68587721302630200, -76.48668075183719850 ) ) ;
#13293=CARTESIAN_POINT ( 'NONE',  ( 60.39237854593780241, 14.46627288824030089, -47.20777951346740053 ) ) ;
#13295=CARTESIAN_POINT ( 'NONE',  ( 57.24929578595760660, -52.61618894467940066, -74.14999999999999147 ) ) ;
#13296=CARTESIAN_POINT ( 'NONE',  ( 41.21726848154669653, 13.59251350426850102, -5.423354614126240314 ) ) ;
#13297=CARTESIAN_POINT ( 'NONE',  ( 42.05805429857900180, -44.46257822744319554, -5.167112339002620125 ) ) ;
#13298=CARTESIAN_POINT ( 'NONE',  ( 0.8851803632885527628, -42.94237738927703418, -20.85710678118654471 ) ) ;
#13300=AXIS2_PLACEMENT_3D ( 'NONE', #6139, #29701, #2456 ) ;
#13304=CARTESIAN_POINT ( 'NONE',  ( 66.36401773903131129, -0.6008215590598360301, -16.96146227724700495 ) ) ;
#13306=CARTESIAN_POINT ( 'NONE',  ( 14.00960937400600059, -52.10962414010410271, -75.64877291256318870 ) ) ;
#13308=CARTESIAN_POINT ( 'NONE',  ( 47.18324198357289845, -54.80726809202429450, -54.61058319554170026 ) ) ;
#13309=CARTESIAN_POINT ( 'NONE',  ( 8.839329447558961661, 32.18893842047796738, -46.67772192970179645 ) ) ;
#13312=CARTESIAN_POINT ( 'NONE',  ( 61.25373297964098640, -45.57865225153049948, -47.65126977280955600 ) ) ;
#13314=CARTESIAN_POINT ( 'NONE',  ( 55.91595717589669334, -45.90465048314089103, -17.93019253464870033 ) ) ;
#13315=EDGE_CURVE ( 'NONE', #50462, #26977, #6640, .T. ) ;
#13316=CARTESIAN_POINT ( 'NONE',  ( 10.78192289013670013, 33.70626262526499772, -17.70651626560779945 ) ) ;
#13317=DIRECTION ( 'NONE',  ( 0.000000000000000000, 0.000000000000000000, -1.000000000000000000 ) ) ;
#13318=DIRECTION ( 'NONE',  ( 0.000000000000000000, 1.000000000000000000, 0.000000000000000000 ) ) ;
#13320=CARTESIAN_POINT ( 'NONE',  ( 48.61563435628440288, 22.86626419475689787, -55.02610085215599867 ) ) ;
#13321=ORIENTED_EDGE ( 'NONE', *, *, #23278, .F. ) ;
#13324=CARTESIAN_POINT ( 'NONE',  ( 29.52882095054619782, 21.88381105532300097, -74.14999999999999147 ) ) ;
#13326=DIRECTION ( 'NONE',  ( -0.6643794812577346054, -0.7473954140103507005, 3.025357742103549206E-15 ) ) ;
#13328=CARTESIAN_POINT ( 'NONE',  ( 83.20652121431659509, 13.83669318944459903, -47.10047235024320145 ) ) ;
#13329=CARTESIAN_POINT ( 'NONE',  ( 52.66238325897660388, 18.53796739974139740, -28.07429613766819898 ) ) ;
#13332=CARTESIAN_POINT ( 'NONE',  ( 57.41961282341689810, -45.11618894467940066, -17.93020390954330168 ) ) ;
#13333=FACE_OUTER_BOUND ( 'NONE', #35645, .T. ) ;
#13334=EDGE_LOOP ( 'NONE', ( #1514, #12072, #6822, #6290 ) ) ;
#13335=EDGE_CURVE ( 'NONE', #34463, #48131, #2550, .T. ) ;
#13337=CARTESIAN_POINT ( 'NONE',  ( 11.78008937360669961, -65.13730895740229698, -16.70885295319099839 ) ) ;
#13338=CARTESIAN_POINT ( 'NONE',  ( 11.52264128144989996, 33.52070032263379318, -45.36557337499360187 ) ) ;
#13340=AXIS2_PLACEMENT_3D ( 'NONE', #27317, #7418, #24129 ) ;
#13341=CARTESIAN_POINT ( 'NONE',  ( 47.83911115347329712, -54.64680175183159605, -55.43863697538600377 ) ) ;
#13344=ORIENTED_EDGE ( 'NONE', *, *, #25757, .F. ) ;
#13349=FACE_OUTER_BOUND ( 'NONE', #8763, .T. ) ;
#13350=CARTESIAN_POINT ( 'NONE',  ( 1.027904703268279984, -42.68661147989060112, -20.15000000000000213 ) ) ;
#13351=ORIENTED_EDGE ( 'NONE', *, *, #48674, .F. ) ;
#13352=CYLINDRICAL_SURFACE ( 'NONE', #20750, 3.500000000000003109 ) ;
#13354=ORIENTED_EDGE ( 'NONE', *, *, #37747, .T. ) ;
#13356=CARTESIAN_POINT ( 'NONE',  ( 50.20834198929310332, -46.19201399287660337, -12.60657503851190064 ) ) ;
#13359=CARTESIAN_POINT ( 'NONE',  ( 13.77296168685579936, -51.29346510576050377, -23.09857317148069811 ) ) ;
#13360=CARTESIAN_POINT ( 'NONE',  ( 55.60062637994129631, 19.57032068857209950, -75.31308341371119752 ) ) ;
#13361=CARTESIAN_POINT ( 'NONE',  ( 46.35275103504449845, -52.90993241930539881, -76.14999999999999147 ) ) ;
#13362=VERTEX_POINT ( 'NONE', #40666 ) ;
#13363=CARTESIAN_POINT ( 'NONE',  ( 54.70309273011209683, 14.87826559838519991, -15.84802628241609845 ) ) ;
#13364=CARTESIAN_POINT ( 'NONE',  ( 57.19888501910689627, -50.26827476893720359, -52.76365438030089194 ) ) ;
#13368=CARTESIAN_POINT ( 'NONE',  ( 47.11288066194880031, 22.79292711817570094, -75.65359354181590845 ) ) ;
#13371=CARTESIAN_POINT ( 'NONE',  ( 60.79255070202935940, -45.73115554882355838, -47.75226182717861434 ) ) ;
#13374=CIRCLE ( 'NONE', #15045, 1.000000000000000888 ) ;
#13383=CARTESIAN_POINT ( 'NONE',  ( 61.11046412718479814, 14.09004753107949881, -46.82997413804069708 ) ) ;
#13385=CARTESIAN_POINT ( 'NONE',  ( -28.69324816627959862, -35.41536148188630051, -54.99967661823389875 ) ) ;
#13386=VERTEX_POINT ( 'NONE', #33042 ) ;
#13387=CARTESIAN_POINT ( 'NONE',  ( 53.00693771576430180, -49.57086939845230233, -48.85763912010190069 ) ) ;
#13388=CARTESIAN_POINT ( 'NONE',  ( 57.43557945885349625, -45.19660671630600035, -25.73777145330879890 ) ) ;
#13389=CARTESIAN_POINT ( 'NONE',  ( 47.82090655655320433, -54.45843870253389696, -55.22757576880370323 ) ) ;
#13390=CARTESIAN_POINT ( 'NONE',  ( 13.95210466151760187, 19.57561797166449935, -21.48689998016190117 ) ) ;
#13391=CARTESIAN_POINT ( 'NONE',  ( 57.51732571122479243, 13.88248103308219861, -25.33327368259680057 ) ) ;
#13393=CARTESIAN_POINT ( 'NONE',  ( 50.12047694090430383, 18.16987201063400192, -76.14999999999999147 ) ) ;
#13394=CARTESIAN_POINT ( 'NONE',  ( 53.30565515969109924, 18.20461000561270026, -49.00291067189689898 ) ) ;
#13397=CARTESIAN_POINT ( 'NONE',  ( 47.26412996261229438, 22.82317408360536604, -75.56727799573911852 ) ) ;
#13401=CARTESIAN_POINT ( 'NONE',  ( 47.42532149332459568, -54.64264661477289309, -54.89680082169689967 ) ) ;
#13404=CARTESIAN_POINT ( 'NONE',  ( 56.78254780598179963, 19.37920438373040355, -53.13068928018909531 ) ) ;
#13405=CARTESIAN_POINT ( 'NONE',  ( 52.83236039598949674, 18.42717821426129987, -48.53480049868920077 ) ) ;
#13411=EDGE_LOOP ( 'NONE', ( #20931, #46941, #39694, #32370 ) ) ;
#13412=CARTESIAN_POINT ( 'NONE',  ( 8.793990757808609615, -63.16307462209709911, -46.67050766270720175 ) ) ;
#13414=CARTESIAN_POINT ( 'NONE',  ( 15.75369840593345394, -50.90400523626287566, -15.65824089793746055 ) ) ;
#13415=VERTEX_POINT ( 'NONE', #1355 ) ;
#13416=CARTESIAN_POINT ( 'NONE',  ( 11.93218571260559990, -65.12547012744420272, -45.62050932637900047 ) ) ;
#13420=CARTESIAN_POINT ( 'NONE',  ( 51.18087450704700103, 19.51486598760920188, -76.16568686306109726 ) ) ;
#13423=DIRECTION ( 'NONE',  ( 0.000000000000000000, 0.000000000000000000, 1.000000000000000000 ) ) ;
#13428=B_SPLINE_SURFACE_WITH_KNOTS ( 'NONE', 3, 3, ( 
 ( #49730, #21656, #45018, #29778, #49481, #13067, #49221, #5702, #1509, #45797, #9885 ),
 ( #13569, #36616, #16711, #48698, #12799, #28756, #44755, #8861, #40821, #990, #16989 ),
 ( #32937, #21149, #1252, #25067, #17240, #41085, #33203, #29273, #21918, #26361, #46580 ),
 ( #42380, #10670, #5959, #42642, #38970, #26626, #22433, #6740, #15112, #42116, #14851 ),
 ( #26107, #38442, #22697, #38713, #2805, #18776, #51014, #3061, #33966, #10150, #18523 ),
 ( #30037, #34749, #30302, #50500, #34496, #37926, #38185, #31071, #50758, #11188, #22950 ),
 ( #42902, #2542, #30814, #46842, #6218, #14590, #22174, #10928, #26896, #2024, #6998 ),
 ( #19034, #35009, #47100, #27151, #2279, #18002, #18255, #34224, #49983, #14076, #46060 ),
 ( #50243, #14333, #40245, #19295, #47352, #3835, #23457, #15373, #47860, #15630, #35797 ),
 ( #43158, #39483, #39221, #7252, #3318, #24221, #23718, #43920, #20303, #3581, #20054 ),
 ( #28168, #51782, #19549, #35542, #39991, #39731, #32348, #48110, #19809, #44173, #51532 ),
 ( #405, #12464, #36294, #8271, #15885, #16391, #31328, #4338, #48365, #31838, #36045 ),
 ( #23967, #27918, #51275, #23201, #35278, #8014, #4081, #155, #31581, #11961, #16131 ),
 ( #11449, #7769, #32090, #27407, #47603, #12209, #43409, #7511, #11702, #27665, #43667 ),
 ( #659, #13515, #25531, #29471, #36822, #45474, #5386, #4859, #5131, #33402, #33135 ),
 ( #49419, #25272, #9325, #29210, #9575, #8540, #1186, #37349, #41533, #5650, #40497 ),
 ( #41276, #24747, #17690, #21597, #21088, #37596, #40757, #28432, #1707, #16646, #926 ),
 ( #17181, #33660, #32605, #49675, #44432, #25003, #21342, #48899, #1447, #13256, #36557 ),
 ( #24483, #45217, #17432, #4588, #16924, #49160, #9054, #20562, #48632, #44953, #12733 ),
 ( #20826, #28687, #44689, #8793, #32865, #12999, #28950, #37090, #41018, #50697, #10873 ) ),
 .UNSPECIFIED., .F., .F., .F.,
 ( 4, 2, 2, 2, 2, 2, 2, 2, 2, 4 ),
 ( 4, 1, 1, 1, 1, 1, 1, 1, 4 ),
 ( 0.000000000000000000, 0.05535613038339300129, 0.2869944836127450438, 0.5186328368420959345, 0.8630971313986249838, 1.150796175198169902, 1.294645697097940085, 1.524804932137569846, 1.893059708200979907, 2.301592350396330033 ),
 ( 0.000000000000000000, 0.1250000000000000000, 0.2500000000000000000, 0.3750000000000000000, 0.5000000000000000000, 0.6250000000000000000, 0.7500000000000000000, 0.8750000000000000000, 1.000000000000000000 ),
 .UNSPECIFIED. ) ;
#13430=ADVANCED_FACE ( 'NONE', ( #33312 ), #316, .T. ) ;
#13433=EDGE_CURVE ( 'NONE', #36317, #9892, #9230, .T. ) ;
#13435=DIRECTION ( 'NONE',  ( -0.2389682100435167045, 0.9710273912658683448, 0.000000000000000000 ) ) ;
#13437=CARTESIAN_POINT ( 'NONE',  ( 40.69061996557520189, 14.09050113835410123, -5.669818638807839761 ) ) ;
#13438=CARTESIAN_POINT ( 'NONE',  ( 14.48181959901199889, 20.27135023148479576, -75.33782839756391070 ) ) ;
#13444=ORIENTED_EDGE ( 'NONE', *, *, #22029, .F. ) ;
#13445=CARTESIAN_POINT ( 'NONE',  ( 52.82291935875819888, -49.60365082802910308, -27.55752660507549834 ) ) ;
#13446=CARTESIAN_POINT ( 'NONE',  ( 55.07813547831889878, -51.04730606513820135, -75.19531985927159212 ) ) ;
#13447=CARTESIAN_POINT ( 'NONE',  ( 6.305142788495140316, 28.78716984886350261, -12.89664123648359961 ) ) ;
#13448=CARTESIAN_POINT ( 'NONE',  ( 11.13393739769619906, 32.28996932333459569, -43.76018303787720498 ) ) ;
#13449=CARTESIAN_POINT ( 'NONE',  ( 50.71554959566909559, 14.96708580405049993, -12.97453803614309997 ) ) ;
#13450=ORIENTED_EDGE ( 'NONE', *, *, #49040, .F. ) ;
#13451=AXIS2_PLACEMENT_3D ( 'NONE', #19128, #39314, #19388 ) ;
#13452=CARTESIAN_POINT ( 'NONE',  ( -5.145198839953950554, -47.14946543292239767, -4.849579887423169033 ) ) ;
#13454=CARTESIAN_POINT ( 'NONE',  ( 47.42191991419499431, 23.41235274918789955, -54.90470402679689954 ) ) ;
#13459=CARTESIAN_POINT ( 'NONE',  ( 11.96242378326880029, 34.20360896090840441, -17.67418126880570028 ) ) ;
#13461=CARTESIAN_POINT ( 'NONE',  ( 53.06963667952170027, 18.30286252129070235, -48.79723990062230143 ) ) ;
#13463=CARTESIAN_POINT ( 'NONE',  ( 59.45724307632730188, -46.21313155759460045, -47.61455192236069678 ) ) ;
#13464=CARTESIAN_POINT ( 'NONE',  ( 53.82324154614039458, 17.55874562463440114, -27.07948292951889968 ) ) ;
#13465=CARTESIAN_POINT ( 'NONE',  ( 53.65245010158729855, 20.72074997219770154, -53.90489108192829804 ) ) ;
#13470=CARTESIAN_POINT ( 'NONE',  ( 9.746758075853771075, 32.08108121953329572, -46.29788637164419640 ) ) ;
#13471=CARTESIAN_POINT ( 'NONE',  ( 42.44160469162459748, 13.71702471974399984, -5.942261413879579734 ) ) ;
#13472=CARTESIAN_POINT ( 'NONE',  ( 67.08845630739949684, -31.07791224506899752, -17.50640734377579832 ) ) ;
#13473=CARTESIAN_POINT ( 'NONE',  ( 18.51915660836230160, 20.76921105827980085, -75.35480091913980516 ) ) ;
#13478=CARTESIAN_POINT ( 'NONE',  ( 12.01043929807459953, -65.26379547360380684, -46.82866647765490598 ) ) ;
#13479=CARTESIAN_POINT ( 'NONE',  ( 57.34482800150080095, -45.61704748136379806, -26.19284480059729958 ) ) ;
#13482=CARTESIAN_POINT ( 'NONE',  ( 61.67253348274019942, 13.94162801194639911, -46.85000153395669997 ) ) ;
#13485=CARTESIAN_POINT ( 'NONE',  ( 75.04878402891587541, -10.96810985108981207, -11.30472392811527271 ) ) ;
#13487=CARTESIAN_POINT ( 'NONE',  ( 53.99846808212529936, -46.02098823835780195, -15.26947028995409994 ) ) ;
#13491=ADVANCED_FACE ( 'NONE', ( #24912 ), #23361, .T. ) ;
#13494=CARTESIAN_POINT ( 'NONE',  ( 16.13393739769620083, -15.61618894467929941, -17.93019253464870033 ) ) ;
#13495=CARTESIAN_POINT ( 'NONE',  ( 46.45656088628239644, -53.12694234138209737, -76.13971323818920212 ) ) ;
#13496=AXIS2_PLACEMENT_3D ( 'NONE', #42087, #14305, #34194 ) ;
#13497=CARTESIAN_POINT ( 'NONE',  ( 60.40232013370989961, 14.60517343624429998, -47.72046811377730080 ) ) ;
#13498=AXIS2_PLACEMENT_3D ( 'NONE', #18293, #23243, #31365 ) ;
#13499=CARTESIAN_POINT ( 'NONE',  ( 45.07857608053570431, 14.88012197229889999, -9.026857927713109575 ) ) ;
#13501=DIRECTION ( 'NONE',  ( 0.3281607301299678814, 0.6263469766835031427, 0.7071067811865485719 ) ) ;
#13503=CARTESIAN_POINT ( 'NONE',  ( 60.40002696937390425, 13.91362826609339898, -26.58785703793860122 ) ) ;
#13505=ADVANCED_FACE ( 'NONE', ( #5555 ), #36995, .T. ) ;
#13506=ORIENTED_EDGE ( 'NONE', *, *, #9715, .F. ) ;
#13507=CARTESIAN_POINT ( 'NONE',  ( 53.57228486832382686, 18.19337119796120561, -49.24858181519383749 ) ) ;
#13508=CARTESIAN_POINT ( 'NONE',  ( -10.49744324907189963, -41.58055173219970158, -4.376973931108589788 ) ) ;
#13509=CARTESIAN_POINT ( 'NONE',  ( 15.21636614235080032, -50.60415920577569437, -15.64999998222989852 ) ) ;
#13510=EDGE_CURVE ( 'NONE', #24819, #31554, #10834, .T. ) ;
#13514=CARTESIAN_POINT ( 'NONE',  ( 47.51793462813986935, -54.37766851147189584, -75.00961803996818844 ) ) ;
#13515=CARTESIAN_POINT ( 'NONE',  ( 48.94958679002760249, -53.97766395890939606, -55.24468684015499775 ) ) ;
#13517=CARTESIAN_POINT ( 'NONE',  ( 76.82615602979319647, -43.14551972207646457, -14.66829194415775461 ) ) ;
#13518=DIRECTION ( 'NONE',  ( 0.000000000000000000, 0.000000000000000000, -1.000000000000000000 ) ) ;
#13520=AXIS2_PLACEMENT_3D ( 'NONE', #25850, #50512, #46592 ) ;
#13526=CARTESIAN_POINT ( 'NONE',  ( 60.98388430596229881, -45.56993733780140587, -47.58050232604119856 ) ) ;
#13528=CARTESIAN_POINT ( 'NONE',  ( 56.84932596551129791, 19.42421318737730118, -53.85230338955989993 ) ) ;
#13530=CARTESIAN_POINT ( 'NONE',  ( 18.86789271228450104, 20.55440457967890211, -74.14999999999999147 ) ) ;
#13533=CARTESIAN_POINT ( 'NONE',  ( 8.133937397696209715, -59.02534396924340143, -43.74348518090240390 ) ) ;
#13534=ORIENTED_EDGE ( 'NONE', *, *, #38152, .T. ) ;
#13536=ORIENTED_EDGE ( 'NONE', *, *, #13130, .T. ) ;
#13537=CARTESIAN_POINT ( 'NONE',  ( 61.44594299458270115, -45.22213083583160653, -46.96386565649149958 ) ) ;
#13538=DIRECTION ( 'NONE',  ( 1.000000000000000000, 0.000000000000000000, 0.000000000000000000 ) ) ;
#13539=CARTESIAN_POINT ( 'NONE',  ( 56.51581731585299906, -50.73333708345260362, -53.50072361911870189 ) ) ;
#13541=ORIENTED_EDGE ( 'NONE', *, *, #25820, .F. ) ;
#13542=ORIENTED_EDGE ( 'NONE', *, *, #2409, .F. ) ;
#13547=ORIENTED_EDGE ( 'NONE', *, *, #47447, .T. ) ;
#13548=CARTESIAN_POINT ( 'NONE',  ( 52.16338473820870547, -49.90420398983260242, -76.93802979155799449 ) ) ;
#13549=CARTESIAN_POINT ( 'NONE',  ( 60.63032377830810304, 14.34160671423079947, -47.11936141799559152 ) ) ;
#13552=CARTESIAN_POINT ( 'NONE',  ( 44.70619667840409761, 13.88245460051030022, -7.106835951036900134 ) ) ;
#13553=CARTESIAN_POINT ( 'NONE',  ( 42.28714451724680146, -44.27662781396410452, -5.063832641217489439 ) ) ;
#13554=CARTESIAN_POINT ( 'NONE',  ( 70.03247032090770574, -49.95860450173900347, -75.14853292321149070 ) ) ;
#13555=CARTESIAN_POINT ( 'NONE',  ( -10.87564126230760131, 11.12160698687080185, -6.291562883898949465 ) ) ;
#13560=CARTESIAN_POINT ( 'NONE',  ( 67.09948597405160342, 1.833213267668650115, -20.09058995088950184 ) ) ;
#13561=ORIENTED_EDGE ( 'NONE', *, *, #10700, .F. ) ;
#13562=CARTESIAN_POINT ( 'NONE',  ( 14.42532105552479926, -51.34461045803089974, -75.09854824053580558 ) ) ;
#13563=CARTESIAN_POINT ( 'NONE',  ( 47.21205592235610737, -54.78444012246939820, -54.63239976220819472 ) ) ;
#13568=LINE ( 'NONE', #29531, #5533 ) ;
#13569=CARTESIAN_POINT ( 'NONE',  ( 47.65668213871590098, -54.52839204276340013, -55.15716614278580465 ) ) ;
#13570=DIRECTION ( 'NONE',  ( 0.000000000000000000, 0.000000000000000000, -1.000000000000000000 ) ) ;
#13571=CARTESIAN_POINT ( 'NONE',  ( 56.47574016726019863, 19.53693441320439916, -53.73400676226840034 ) ) ;
#13572=CARTESIAN_POINT ( 'NONE',  ( 48.01070916242489517, 23.12336947638609885, -54.98721641925899206 ) ) ;
#13576=DIRECTION ( 'NONE',  ( -1.000000000000000000, 0.000000000000000000, 0.000000000000000000 ) ) ;
#13579=CARTESIAN_POINT ( 'NONE',  ( 84.24389573796460695, 12.93914432394539915, -47.41156961578170126 ) ) ;
#13580=CARTESIAN_POINT ( 'NONE',  ( 55.05148602120549839, 15.77693620304509992, -25.60753014925489879 ) ) ;
#13582=DIRECTION ( 'NONE',  ( 1.000000000000000000, 0.000000000000000000, 0.000000000000000000 ) ) ;
#13586=VERTEX_POINT ( 'NONE', #30664 ) ;
#13588=CARTESIAN_POINT ( 'NONE',  ( 11.99500145081920088, -65.25785463067840908, -16.88883237368289869 ) ) ;
#13589=CARTESIAN_POINT ( 'NONE',  ( 11.49485748460980084, 33.59317259934719146, -45.88007095197389873 ) ) ;
#13592=CARTESIAN_POINT ( 'NONE',  ( 12.39013027377469989, 34.14800971684240238, -46.54379730670240178 ) ) ;
#13593=CARTESIAN_POINT ( 'NONE',  ( 10.73552252728440060, -65.02568017880969364, -47.16673514230450337 ) ) ;
#13594=TOROIDAL_SURFACE ( 'NONE', #30290, 24.89999999999999858, 4.000000000000059508 ) ;
#13599=CARTESIAN_POINT ( 'NONE',  ( 52.96770052557779707, 18.26589706774769795, -48.58772269060800397 ) ) ;
#13600=CARTESIAN_POINT ( 'NONE',  ( 61.63186543861399969, -2.018559880675780072, -16.00684823669729795 ) ) ;
#13601=CARTESIAN_POINT ( 'NONE',  ( 51.24580075538570156, -49.39897230491230573, -76.45613186134289663 ) ) ;
#13602=EDGE_CURVE ( 'NONE', #14356, #15737, #26743, .T. ) ;
#13603=CARTESIAN_POINT ( 'NONE',  ( 35.69765375167399668, -15.61618894467929941, 6.850000000000000533 ) ) ;
#13606=DIRECTION ( 'NONE',  ( 0.000000000000000000, 0.000000000000000000, -1.000000000000000000 ) ) ;
#13607=CARTESIAN_POINT ( 'NONE',  ( 70.83745409581388230, 17.98087126524299606, -74.20351669811765305 ) ) ;
#13608=ORIENTED_EDGE ( 'NONE', *, *, #37719, .T. ) ;
#13611=EDGE_CURVE ( 'NONE', #4756, #44974, #30408, .T. ) ;
#13614=CARTESIAN_POINT ( 'NONE',  ( 56.79288268143969987, 19.43545220660120165, -74.14914690165589661 ) ) ;
#13615=CARTESIAN_POINT ( 'NONE',  ( 47.50498297817869542, -54.47480520914279367, -74.80901628187270092 ) ) ;
#13616=ORIENTED_EDGE ( 'NONE', *, *, #45449, .F. ) ;
#13617=CARTESIAN_POINT ( 'NONE',  ( 56.24180394757939894, 14.16774694249440003, -16.78461393623150144 ) ) ;
#13619=CARTESIAN_POINT ( 'NONE',  ( 57.13721805172019685, -50.61838845098209561, -53.74365126625890099 ) ) ;
#13623=ORIENTED_EDGE ( 'NONE', *, *, #38533, .F. ) ;
#13624=CARTESIAN_POINT ( 'NONE',  ( 47.19371938996339821, 22.91183880830930164, -75.51723258725729693 ) ) ;
#13625=CARTESIAN_POINT ( 'NONE',  ( 20.13393739083949896, -55.41568640430479320, -20.65000000000000213 ) ) ;
#13627=CARTESIAN_POINT ( 'NONE',  ( 75.25323313020308547, -34.43977339652462888, -12.29989660903943438 ) ) ;
#13636=CARTESIAN_POINT ( 'NONE',  ( 61.30391762588470073, 13.98869191317340110, -46.37202200358919413 ) ) ;
#13637=CARTESIAN_POINT ( 'NONE',  ( -18.27909364759700139, 20.72688191304690264, -53.14840429075709949 ) ) ;
#13639=CARTESIAN_POINT ( 'NONE',  ( 53.21742324705429894, -49.46290330832970028, -48.89816740597070321 ) ) ;
#13640=VERTEX_POINT ( 'NONE', #37778 ) ;
#13642=CARTESIAN_POINT ( 'NONE',  ( 58.74123455927210102, -45.12673593262880445, -25.78612740298530071 ) ) ;
#13643=CYLINDRICAL_SURFACE ( 'NONE', #10978, 1.999999999999970246 ) ;
#13644=CARTESIAN_POINT ( 'NONE',  ( 56.14548367315779842, 14.43159843830459899, -25.51430258618709956 ) ) ;
#13647=CARTESIAN_POINT ( 'NONE',  ( 52.87767298794570081, 18.41793525666839670, -48.88837531658360547 ) ) ;
#13648=CARTESIAN_POINT ( 'NONE',  ( 60.23130391296999875, -45.78304229081430066, -47.24246919202539630 ) ) ;
#13649=CARTESIAN_POINT ( 'NONE',  ( 73.82352657437539278, -44.30885758721080236, -13.22070786789489993 ) ) ;
#13650=VERTEX_POINT ( 'NONE', #1611 ) ;
#13653=CARTESIAN_POINT ( 'NONE',  ( 47.45628758025669924, -54.61120735724659880, -54.67911033738580073 ) ) ;
#13654=DIRECTION ( 'NONE',  ( 0.000000000000000000, 0.000000000000000000, -1.000000000000000000 ) ) ;
#13656=CARTESIAN_POINT ( 'NONE',  ( 11.74201408114130096, -65.42316349444709545, -18.09919823657899940 ) ) ;
#13663=CARTESIAN_POINT ( 'NONE',  ( 8.977345137891989069, -63.27590191225959870, -46.63353902393470207 ) ) ;
#13664=LINE ( 'NONE', #45629, #17673 ) ;
#13665=ORIENTED_EDGE ( 'NONE', *, *, #46377, .F. ) ;
#13670=CARTESIAN_POINT ( 'NONE',  ( 51.93758447892039953, 19.58744159688830067, -76.23465794037869614 ) ) ;
#13673=EDGE_CURVE ( 'NONE', #46679, #13415, #4149, .T. ) ;
#13675=DIRECTION ( 'NONE',  ( 1.000000000000000000, 0.000000000000000000, 0.000000000000000000 ) ) ;
#13678=EDGE_CURVE ( 'NONE', #12521, #38625, #27336, .T. ) ;
#13683=CARTESIAN_POINT ( 'NONE',  ( 56.82260617504960010, -46.00315474979750263, -26.24626356014529804 ) ) ;
#13685=CARTESIAN_POINT ( 'NONE',  ( 52.56949981068910205, -49.85724369911659437, -48.49331493222930334 ) ) ;
#13687=CARTESIAN_POINT ( 'NONE',  ( 14.13832751391059972, 19.89797661840560039, -74.34810712130391153 ) ) ;
#13688=ADVANCED_FACE ( 'NONE', ( #17852 ), #49835, .F. ) ;
#13689=CARTESIAN_POINT ( 'NONE',  ( 17.52127312675804305, -52.24942673177908148, -75.96019247807906538 ) ) ;
#13690=CARTESIAN_POINT ( 'NONE',  ( 45.65337825043140185, -45.22678660988140109, -8.155634320957650729 ) ) ;
#13694=CARTESIAN_POINT ( 'NONE',  ( 55.13720784205819569, -47.03157555599469930, -26.02069266286289917 ) ) ;
#13695=CARTESIAN_POINT ( 'NONE',  ( 15.46269294851370013, -51.02814174995680219, -21.20027565687029991 ) ) ;
#13696=CARTESIAN_POINT ( 'NONE',  ( 1.943467852530839979, 24.47558943821050192, -10.50290134495580041 ) ) ;
#13698=VECTOR ( 'NONE', #6492, 1000.000000000000114 ) ;
#13703=CARTESIAN_POINT ( 'NONE',  ( -8.354434865538138411, -44.72889599991650300, -5.578549619731169251 ) ) ;
#13705=VECTOR ( 'NONE', #10989, 999.9999999999998863 ) ;
#13706=CARTESIAN_POINT ( 'NONE',  ( 47.51579407122170551, 23.33782210192210016, -54.66949387222739887 ) ) ;
#13710=CARTESIAN_POINT ( 'NONE',  ( 61.08978246524510070, 14.10367963069579922, -46.92961180776249819 ) ) ;
#13711=CARTESIAN_POINT ( 'NONE',  ( 41.34908647067909726, 13.52015569396220052, -5.352709625395239534 ) ) ;
#13712=CARTESIAN_POINT ( 'NONE',  ( 51.90728853546290367, 18.14319514060320060, -77.08409337567729835 ) ) ;
#13713=CARTESIAN_POINT ( 'NONE',  ( 52.84731125486479897, 18.41934504040209930, -48.60966020774090168 ) ) ;
#13714=CARTESIAN_POINT ( 'NONE',  ( 68.13393739769620083, -43.11618894467930119, -73.25000000000000000 ) ) ;
#13715=B_SPLINE_CURVE_WITH_KNOTS ( 'NONE', 3,
 ( #44811, #521, #16507, #32457, #48484, #773, #8650, #24603, #4715, #16772, #8919, #24865, #37725, #30354, #5507, #5249, #45855, #46383, #17299, #6016, #34282, #2336, #14129, #13625 ),
 .UNSPECIFIED., .F., .F.,
 ( 4, 2, 1, 1, 2, 2, 1, 1, 2, 2, 1, 1, 2, 2, 4 ),
 ( 0.000000000000000000, 0.2499999999999947820, 0.3749999999999936162, 0.4374999999999935052, 0.4687499999999939493, 0.4999999999999943379, 0.5624999999999930056, 0.5937499999999930056, 0.6093749999999936717, 0.6249999999999942268, 0.6874999999999985567, 0.7187500000000000000, 0.7343750000000007772, 0.7500000000000015543, 1.000000000000000000 ),
 .UNSPECIFIED. ) ;
#13718=CARTESIAN_POINT ( 'NONE',  ( 54.86690915992559781, 20.20342982344670091, -53.70992542625590005 ) ) ;
#13720=PLANE ( 'NONE',  #50870 ) ;
#13723=CARTESIAN_POINT ( 'NONE',  ( 10.49050030533310007, 32.01494398242250128, -45.62565322571249737 ) ) ;
#13724=CARTESIAN_POINT ( 'NONE',  ( 41.40756759976829926, 13.53921337778190015, -5.393983492778530398 ) ) ;
#13727=ORIENTED_EDGE ( 'NONE', *, *, #25757, .T. ) ;
#13728=ORIENTED_EDGE ( 'NONE', *, *, #26820, .F. ) ;
#13729=VECTOR ( 'NONE', #51313, 1000.000000000000000 ) ;
#13732=CARTESIAN_POINT ( 'NONE',  ( 10.70946016660839994, -64.33455432219130898, -46.11556548067969885 ) ) ;
#13733=CARTESIAN_POINT ( 'NONE',  ( 56.80041699543109956, -45.59906731679899394, -26.04381423261900252 ) ) ;
#13740=EDGE_CURVE ( 'NONE', #30578, #42328, #1618, .T. ) ;
#13742=CARTESIAN_POINT ( 'NONE',  ( 55.10456398469269601, -45.21089673982120161, -14.92011640338920131 ) ) ;
#13744=CARTESIAN_POINT ( 'NONE',  ( 16.19673815769250069, 19.83680681410009683, -20.37207796061779774 ) ) ;
#13745=DIRECTION ( 'NONE',  ( -0.8090169943749474513, -0.5877852522924732481, 0.000000000000000000 ) ) ;
#13747=DIRECTION ( 'NONE',  ( 0.000000000000000000, 1.000000000000000000, 0.000000000000000000 ) ) ;
#13748=CARTESIAN_POINT ( 'NONE',  ( 46.85564613059059980, -54.06445821833459320, -75.74423906255060501 ) ) ;
#13749=CARTESIAN_POINT ( 'NONE',  ( 60.96148484106869603, 14.45202308121209889, -47.73691995860960446 ) ) ;
#13750=CARTESIAN_POINT ( 'NONE',  ( 55.00116481104370081, 13.88381105532070059, -13.90662477428320187 ) ) ;
#13751=DIRECTION ( 'NONE',  ( 1.000000000000000000, 0.000000000000000000, 0.000000000000000000 ) ) ;
#13752=CARTESIAN_POINT ( 'NONE',  ( 51.90125962217079802, 20.02812747325270237, -76.04050507973269646 ) ) ;
#13753=CARTESIAN_POINT ( 'NONE',  ( 61.58485588298179891, 13.89573119013970093, -28.02799758715149991 ) ) ;
#13756=CARTESIAN_POINT ( 'NONE',  ( 68.13393739769620083, -48.11618894467930119, -73.25000000000000000 ) ) ;
#13769=CARTESIAN_POINT ( 'NONE',  ( 17.98015038839400148, -51.14708712906670485, -74.55381114263370534 ) ) ;
#13778=CARTESIAN_POINT ( 'NONE',  ( 60.67537254770959976, -45.75026917865599785, -47.73567082154549723 ) ) ;
#13779=DIRECTION ( 'NONE',  ( 0.6888026391158372785, -0.7071067811865469066, 0.1598465650148877537 ) ) ;
#13784=DIRECTION ( 'NONE',  ( -1.000000000000000000, 4.735514272306495889E-33, 9.834501533011742432E-16 ) ) ;
#13785=VERTEX_POINT ( 'NONE', #35897 ) ;
#13787=ORIENTED_EDGE ( 'NONE', *, *, #8710, .F. ) ;
#13791=ORIENTED_EDGE ( 'NONE', *, *, #18376, .T. ) ;
#13792=EDGE_CURVE ( 'NONE', #32428, #10642, #15219, .T. ) ;
#13793=ORIENTED_EDGE ( 'NONE', *, *, #24609, .F. ) ;
#13794=FACE_OUTER_BOUND ( 'NONE', #36721, .T. ) ;
#13799=CARTESIAN_POINT ( 'NONE',  ( 52.15433690512320197, -49.89707748732470804, -76.93549829881520452 ) ) ;
#13800=CARTESIAN_POINT ( 'NONE',  ( 47.81335647231890107, -54.39749252969859583, -54.71582838609030119 ) ) ;
#13803=CARTESIAN_POINT ( 'NONE',  ( 41.99202299628319679, 13.65299255882769991, -5.712667844576049703 ) ) ;
#13805=CARTESIAN_POINT ( 'NONE',  ( 41.41708184556559758, -44.31838638563439758, -4.679819512558520245 ) ) ;
#13806=CARTESIAN_POINT ( 'NONE',  ( 68.13393739769840352, -50.61618894467879670, -73.25000000000220268 ) ) ;
#13807=CARTESIAN_POINT ( 'NONE',  ( 68.13393739769620083, 19.38381105532069881, -83.65000000000000568 ) ) ;
#13810=CARTESIAN_POINT ( 'NONE',  ( 65.88232188379309662, 0.1705518047408740023, -17.13915755217489689 ) ) ;
#13812=CARTESIAN_POINT ( 'NONE',  ( 14.91526764967280094, -52.98224883304730071, -76.14999999999999147 ) ) ;
#13813=CARTESIAN_POINT ( 'NONE',  ( 47.18324198357289845, -54.80726809202429450, -54.61058319554170026 ) ) ;
#13815=CARTESIAN_POINT ( 'NONE',  ( 11.61427276589894575, 33.59338474805557695, -44.95328842582802764 ) ) ;
#13816=LINE ( 'NONE', #2802, #12991 ) ;
#13818=CARTESIAN_POINT ( 'NONE',  ( 10.88578148295150072, 33.80155039833079655, -17.73314437547309907 ) ) ;
#13819=AXIS2_PLACEMENT_3D ( 'NONE', #35780, #39463, #7235 ) ;
#13821=EDGE_CURVE ( 'NONE', #3407, #13650, #11, .T. ) ;
#13822=CARTESIAN_POINT ( 'NONE',  ( 18.38906992954201058, -55.55385106823292318, -76.14999999999999147 ) ) ;
#13823=CARTESIAN_POINT ( 'NONE',  ( 48.26315220932669803, 23.03099554315049957, -55.14606850299719554 ) ) ;
#13825=AXIS2_PLACEMENT_3D ( 'NONE', #11556, #3173, #39842 ) ;
#13828=CARTESIAN_POINT ( 'NONE',  ( 55.91595717589669334, -45.90465048314089103, -17.93019253464870033 ) ) ;
#13830=LINE ( 'NONE', #21417, #12003 ) ;
#13831=CARTESIAN_POINT ( 'NONE',  ( 84.30744353797240365, 12.70315578777099930, -47.37637942009979497 ) ) ;
#13832=CARTESIAN_POINT ( 'NONE',  ( 55.89862311850580312, 14.72947118455319959, -25.58674067759540094 ) ) ;
#13834=CARTESIAN_POINT ( 'NONE',  ( 12.26282170032090590, 33.38295891277739713, -15.83707920940340053 ) ) ;
#13837=B_SPLINE_SURFACE_WITH_KNOTS ( 'NONE', 3, 3, ( 
 ( #24746, #28167, #27917, #48898, #40755, #36293, #4587, #40496, #41017, #4858, #1185, #12998, #11960, #32864, #404, #12732, #20560, #32089, #16390, #48109, #32346, #658, #8013, #28686, #9052, #20825 ),
 ( #48364, #36821, #925, #24220, #23966, #5130, #16923, #21087, #37089, #17180, #154, #39990, #4080, #20053, #36044, #16130, #12463, #44172, #8270, #40244, #20302, #4337, #28431, #8539, #24482, #39850 ),
 ( #23576, #8396, #31186, #27269, #40358, #3444, #32207, #40103, #43531, #47217, #4199, #7631, #20173, #15742, #16000, #15490, #43781, #36411, #36161, #31442, #47721, #8138, #11305, #7370, #19667, #3699 ),
 ( #39594, #7884, #39342, #269, #12326, #16251, #35661, #48228, #44036, #51648, #23830, #28286, #19916, #27523, #31695, #28032, #44286, #31954, #24345, #43280, #3956, #24083, #4455, #20423, #23316, #51393 ),
 ( #35908, #15234, #12079, #19414, #35395, #47471, #11565, #11825, #47976, #27, #27783, #4977, #772, #36943, #41136, #520, #37208, #33521, #21201, #1044, #1309, #9684, #36670, #9439, #20682, #16771 ),
 ( #32722, #8649, #45590, #20948, #25646, #48748, #5248, #5506, #32456, #5754, #21463, #24602, #37461, #49533, #1560, #8918, #12855, #41649, #21711, #40616, #17038, #45069, #28810, #4714, #16506, #32992 ),
 ( #28549, #44810, #13123, #24864, #40876, #17298, #49019, #9174, #29076, #48483, #25132, #12587, #44548, #33258, #13624, #49276, #13368, #29585, #29334, #45334, #25388, #17548, #41389, #50036, #30094, #34550 ),
 ( #42699, #14389, #22748, #14128, #37724, #10986, #9940, #10205, #1819, #6796, #14903, #46121, #26166, #30868, #17800, #49783, #26949, #25899, #2861, #10722, #42176, #33773, #26677, #6276, #38768, #38241 ),
 ( #18308, #42955, #50812, #2334, #38497, #34809, #22233, #46638, #18826, #21973, #41915, #26422, #34280, #30353, #6015, #46895, #7054, #13875, #50304, #29834, #14646, #46382, #10467, #45853, #42440, #6529 ),
 ( #22491, #37985, #2080, #2601, #50554, #30614, #18059, #34027, #18574, #15937, #11503, #31636, #15682, #16185, #19857, #28226, #40044, #23004, #8075, #27460, #23773, #47655, #7305, #43463, #23257, #7564 ) ),
 .UNSPECIFIED., .F., .F., .F.,
 ( 4, 1, 1, 1, 1, 1, 1, 4 ),
 ( 4, 2, 2, 2, 2, 2, 2, 2, 2, 2, 2, 2, 4 ),
 ( -8.374790374999999340E-06, 0.1428571428571430157, 0.2857142857142860315, 0.4285714285714289917, 0.5714285714285709528, 0.7142857142857139685, 0.8571428571428569843, 1.000000000000000000 ),
 ( -6.275064945719149634, -6.131805065669529320, -5.288548408819579549, -4.761512998288360166, -4.381730680025620828, -4.001948361762890372, -3.527220463934470196, -3.134672448649570065, -2.742124433364669933, -2.114047608908829812, -1.109124689779479978, -0.2434889638270290035, 0.005711673629634999964 ),
 .UNSPECIFIED. ) ;
#13840=AXIS2_PLACEMENT_3D ( 'NONE', #13756, #21853, #37860 ) ;
#13842=CARTESIAN_POINT ( 'NONE',  ( 12.20485434016359960, -64.96606476350561366, -16.27613458665190294 ) ) ;
#13843=CARTESIAN_POINT ( 'NONE',  ( 11.68619745379040076, 33.77259971275340433, -46.13864009073310513 ) ) ;
#13844=EDGE_CURVE ( 'NONE', #10985, #28850, #35800, .T. ) ;
#13851=CARTESIAN_POINT ( 'NONE',  ( 53.40279069281933033, 17.93096837380682729, -27.32834194345275591 ) ) ;
#13852=CARTESIAN_POINT ( 'NONE',  ( 53.08510103305950167, 18.23200443139790039, -48.78473343235920368 ) ) ;
#13855=CARTESIAN_POINT ( 'NONE',  ( 51.43588982009890742, -49.74596692343669702, -76.47300594495250436 ) ) ;
#13856=CARTESIAN_POINT ( 'NONE',  ( 59.02019150423489435, -47.64116135995680423, -49.73071094584800278 ) ) ;
#13859=CARTESIAN_POINT ( 'NONE',  ( 66.23540447448930024, 18.72622661238430553, -73.39853292320987066 ) ) ;
#13860=VERTEX_POINT ( 'NONE', #31427 ) ;
#13861=CARTESIAN_POINT ( 'NONE',  ( 12.73487495346794240, -55.47150669537813883, -75.56421462368682285 ) ) ;
#13862=DIRECTION ( 'NONE',  ( 0.000000000000000000, 0.000000000000000000, -1.000000000000000000 ) ) ;
#13867=CARTESIAN_POINT ( 'NONE',  ( 55.67187328886809894, 19.41528913861149874, -75.85395822069619953 ) ) ;
#13868=CARTESIAN_POINT ( 'NONE',  ( 47.56586919366919375, -54.47692839446759905, -74.72677413543641478 ) ) ;
#13869=VERTEX_POINT ( 'NONE', #27001 ) ;
#13870=CARTESIAN_POINT ( 'NONE',  ( 55.25371901226309745, 14.61435477241920111, -16.15016637665110011 ) ) ;
#13872=CARTESIAN_POINT ( 'NONE',  ( 56.89024916085300276, -50.49705092091460301, -53.06448611164700679 ) ) ;
#13873=CARTESIAN_POINT ( 'NONE',  ( 68.13393739769840352, -50.61618894467879670, -73.25000000000220268 ) ) ;
#13875=CARTESIAN_POINT ( 'NONE',  ( 47.10376384439059905, 22.64445950907689564, -75.76537844053849824 ) ) ;
#13877=CARTESIAN_POINT ( 'NONE',  ( 60.49059093688927646, -45.82073196953276550, -47.74858579941451353 ) ) ;
#13881=DIRECTION ( 'NONE',  ( -2.565320000000000120E-13, 1.000000000000000000, -8.628712999999999808E-13 ) ) ;
#13883=DIRECTION ( 'NONE',  ( -0.5685928097855452723, 0.5944782866685394129, 0.5685928097855412755 ) ) ;
#13885=ADVANCED_FACE ( 'NONE', ( #47456 ), #43513, .T. ) ;
#13886=CARTESIAN_POINT ( 'NONE',  ( 61.18510815024300342, 14.05093947119190112, -46.73529673433709775 ) ) ;
#13887=CARTESIAN_POINT ( 'NONE',  ( -0.4147641054028919916, 31.50987371720300700, -49.23002488738170257 ) ) ;
#13889=CARTESIAN_POINT ( 'NONE',  ( 53.21185470119179683, -49.46165491835810002, -48.84882516131230545 ) ) ;
#13894=CARTESIAN_POINT ( 'NONE',  ( 13.31268657292839919, 19.90328963381880101, -21.89251117597479990 ) ) ;
#13895=CARTESIAN_POINT ( 'NONE',  ( 57.66356598520189891, 13.88992849527940088, -25.34725557404829743 ) ) ;
#13898=CARTESIAN_POINT ( 'NONE',  ( 52.93745296751840357, 18.38235333221300039, -48.89566025814650629 ) ) ;
#13901=CARTESIAN_POINT ( 'NONE',  ( 52.56521993351449851, 18.62941884369810097, -28.15000000000000213 ) ) ;
#13906=CARTESIAN_POINT ( 'NONE',  ( 47.40907417377749766, -54.65069181535059784, -54.79938858936409929 ) ) ;
#13907=DIRECTION ( 'NONE',  ( 0.000000000000000000, 0.000000000000000000, 1.000000000000000000 ) ) ;
#13909=CARTESIAN_POINT ( 'NONE',  ( 10.97864148254310024, -65.14694562472800499, -18.17421237900940412 ) ) ;
#13910=DIRECTION ( 'NONE',  ( 0.000000000000000000, 0.000000000000000000, 1.000000000000000000 ) ) ;
#13911=CYLINDRICAL_SURFACE ( 'NONE', #31672, 2.999999999999942712 ) ;
#13913=EDGE_CURVE ( 'NONE', #14500, #45267, #7617, .T. ) ;
#13915=ORIENTED_EDGE ( 'NONE', *, *, #8913, .T. ) ;
#13918=CARTESIAN_POINT ( 'NONE',  ( 13.92806294471009920, -51.20625127023169654, -22.96889534167359770 ) ) ;
#13920=ORIENTED_EDGE ( 'NONE', *, *, #20225, .F. ) ;
#13922=PLANE ( 'NONE',  #40938 ) ;
#13923=DIRECTION ( 'NONE',  ( 0.8320502943378438321, 0.000000000000000000, -0.5547001962252288143 ) ) ;
#13925=CARTESIAN_POINT ( 'NONE',  ( 53.23404575114440718, 19.38950307978380039, -76.66833037291560515 ) ) ;
#13928=DIRECTION ( 'NONE',  ( 1.000000000000000000, 0.000000000000000000, 0.000000000000000000 ) ) ;
#13941=CARTESIAN_POINT ( 'NONE',  ( 13.95908631254890153, 19.99149262732870014, -74.56034069004439857 ) ) ;
#13943=CARTESIAN_POINT ( 'NONE',  ( 41.02378997853850251, -45.15608259841430083, -5.717059075756449893 ) ) ;
#13947=CARTESIAN_POINT ( 'NONE',  ( 53.68844523372570166, -48.62671425848849793, -26.42115278879650120 ) ) ;
#13948=CARTESIAN_POINT ( 'NONE',  ( 14.38278649113050101, -51.04890725439349808, -21.89951529875390079 ) ) ;
#13949=CARTESIAN_POINT ( 'NONE',  ( 7.712457590364880211, 30.55593849442650267, -15.52623999900530016 ) ) ;
#13951=ADVANCED_FACE ( 'NONE', ( #49258 ), #24330, .F. ) ;
#13952=CARTESIAN_POINT ( 'NONE',  ( 12.13393739769649926, 24.18330853958550364, -74.14999999999999147 ) ) ;
#13953=CARTESIAN_POINT ( 'NONE',  ( -3.429778956281600344, -15.61618894467929763, 6.850000000000000533 ) ) ;
#13956=CARTESIAN_POINT ( 'NONE',  ( -7.612837316484470485, -45.36256704244740234, -5.450487342267620328 ) ) ;
#13958=CARTESIAN_POINT ( 'NONE',  ( 47.39219260321910099, 23.42968706821420355, -54.83958130849970303 ) ) ;
#13960=CARTESIAN_POINT ( 'NONE',  ( 56.61928470354429521, -45.32411298099489727, -25.29356197036729981 ) ) ;
#13962=DIRECTION ( 'NONE',  ( 0.000000000000000000, 0.000000000000000000, 1.000000000000000000 ) ) ;
#13963=CARTESIAN_POINT ( 'NONE',  ( 11.55844479304150063, 33.94000257695360290, -16.94284747318280182 ) ) ;
#13967=DIRECTION ( 'NONE',  ( 0.000000000000000000, -1.000000000000000000, 0.000000000000000000 ) ) ;
#13970=CARTESIAN_POINT ( 'NONE',  ( 51.63654749813390055, 21.60074325994370170, -54.53423779907880231 ) ) ;
#13972=CARTESIAN_POINT ( 'NONE',  ( 8.133937397696209715, -63.11543068638779630, -43.74348518090240390 ) ) ;
#13973=ORIENTED_EDGE ( 'NONE', *, *, #31858, .F. ) ;
#13974=CARTESIAN_POINT ( 'NONE',  ( 19.97121697892356096, 23.71689785217428437, -18.51157020816790677 ) ) ;
#13975=CARTESIAN_POINT ( 'NONE',  ( 11.10541747795749856, 31.97147113388010098, -44.25032562221770149 ) ) ;
#13977=CIRCLE ( 'NONE', #40746, 2.000000000000000888 ) ;
#13978=CARTESIAN_POINT ( 'NONE',  ( 65.33367464557400695, -32.03144653440359946, -17.55776891374469884 ) ) ;
#13980=CARTESIAN_POINT ( 'NONE',  ( 18.32671892753329956, 19.96087044110830178, -74.35527526576579760 ) ) ;
#13982=VERTEX_POINT ( 'NONE', #17281 ) ;
#13987=CARTESIAN_POINT ( 'NONE',  ( 11.09709421595390033, -63.47517990175989411, -44.33319825685619975 ) ) ;
#13988=CARTESIAN_POINT ( 'NONE',  ( 56.33219501251220152, -46.17132564709319809, -26.19903194913430156 ) ) ;
#13989=CARTESIAN_POINT ( 'NONE',  ( 62.09157612670949788, -15.61618894467929941, -65.34607522167520699 ) ) ;
#13993=ORIENTED_EDGE ( 'NONE', *, *, #41328, .T. ) ;
#13994=CARTESIAN_POINT ( 'NONE',  ( 49.66558981609640000, -45.58299324948399800, -11.70455807815109850 ) ) ;
#13996=CARTESIAN_POINT ( 'NONE',  ( 16.06830620277569821, 19.82972613027099840, -20.66285861647660127 ) ) ;
#13997=DIRECTION ( 'NONE',  ( 0.000000000000000000, 0.000000000000000000, -1.000000000000000000 ) ) ;
#13999=CARTESIAN_POINT ( 'NONE',  ( 47.03253577542010078, -54.46635581206609800, -75.29851419728690587 ) ) ;
#14000=CARTESIAN_POINT ( 'NONE',  ( 41.36014877832850800, 13.74763066256429944, -5.614912196991499904 ) ) ;
#14001=EDGE_CURVE ( 'NONE', #32635, #31811, #25867, .T. ) ;
#14002=CARTESIAN_POINT ( 'NONE',  ( 54.00440282445959639, 13.97710996490090096, -14.09294272437499984 ) ) ;
#14005=CARTESIAN_POINT ( 'NONE',  ( 51.49462702931260338, 19.89667258983029896, -76.11693519487849358 ) ) ;
#14006=VECTOR ( 'NONE', #12332, 1000.000000000000000 ) ;
#14007=CARTESIAN_POINT ( 'NONE',  ( 61.42876130599449880, 13.93441044190779898, -28.04346750121399978 ) ) ;
#14010=CARTESIAN_POINT ( 'NONE',  ( 57.50723796702470025, -47.11618894467930119, -31.98003398042899903 ) ) ;
#14011=CARTESIAN_POINT ( 'NONE',  ( -11.09336481576520228, -42.12635149981709759, -6.270041010354289845 ) ) ;
#14014=EDGE_CURVE ( 'NONE', #39800, #43431, #9997, .T. ) ;
#14016=LINE ( 'NONE', #9323, #1689 ) ;
#14017=CARTESIAN_POINT ( 'NONE',  ( 41.13550739303550330, 13.07993219133260077, -4.257233324915049799 ) ) ;
#14020=CARTESIAN_POINT ( 'NONE',  ( 20.13393739768839552, 24.18330853958629945, -74.14999999999999147 ) ) ;
#14021=CARTESIAN_POINT ( 'NONE',  ( 16.13393739769620083, -15.61618894467929941, -12.65000000000000036 ) ) ;
#14022=DIRECTION ( 'NONE',  ( 0.3445670372598625963, -0.6174735272333260472, -0.7071067811865442421 ) ) ;
#14023=CARTESIAN_POINT ( 'NONE',  ( 18.82012537086889736, -51.74366499200339575, -74.55381114263370534 ) ) ;
#14029=ORIENTED_EDGE ( 'NONE', *, *, #38233, .T. ) ;
#14030=CARTESIAN_POINT ( 'NONE',  ( 10.28183423898790139, 33.24228732221659754, -17.86145330243139995 ) ) ;
#14032=CYLINDRICAL_SURFACE ( 'NONE', #35463, 1.999999999999999556 ) ;
#14037=CARTESIAN_POINT ( 'NONE',  ( 43.92196079148860122, -45.97878081364699909, -8.176196025614100193 ) ) ;
#14040=VERTEX_POINT ( 'NONE', #1031 ) ;
#14041=CARTESIAN_POINT ( 'NONE',  ( 61.27231440712809984, -45.23762772617749306, -46.51050628912130236 ) ) ;
#14043=CARTESIAN_POINT ( 'NONE',  ( 54.62261979470829942, -51.56116820793610600, -54.09401641884280565 ) ) ;
#14044=AXIS2_PLACEMENT_3D ( 'NONE', #40467, #1155, #12434 ) ;
#14045=ORIENTED_EDGE ( 'NONE', *, *, #4701, .F. ) ;
#14047=CARTESIAN_POINT ( 'NONE',  ( 56.46551611171859975, 19.54378718077660082, -53.85224439323700096 ) ) ;
#14050=CARTESIAN_POINT ( 'NONE',  ( 10.64863409883700029, -63.44323389162830296, -23.66469670114080159 ) ) ;
#14053=CARTESIAN_POINT ( 'NONE',  ( 53.39545525563219996, -50.89097375543660462, -76.18303027081991274 ) ) ;
#14054=CARTESIAN_POINT ( 'NONE',  ( 60.45267362128890198, 14.46205442568079924, -47.42411346985809928 ) ) ;
#14058=FACE_OUTER_BOUND ( 'NONE', #29949, .T. ) ;
#14059=CARTESIAN_POINT ( 'NONE',  ( 45.65337825293430285, 13.99440872041340000, -8.155634322266280378 ) ) ;
#14060=CARTESIAN_POINT ( 'NONE',  ( 41.02005783313650511, -44.34833457011540503, -4.033361466744690205 ) ) ;
#14061=EDGE_CURVE ( 'NONE', #13869, #49655, #254, .T. ) ;
#14063=CARTESIAN_POINT ( 'NONE',  ( -3.979110003385970540, 17.20385159207049952, -5.632303519440180040 ) ) ;
#14065=CARTESIAN_POINT ( 'NONE',  ( -19.86606260230379917, -15.61618894467929408, 6.349999999999999645 ) ) ;
#14067=ORIENTED_EDGE ( 'NONE', *, *, #1535, .F. ) ;
#14068=CARTESIAN_POINT ( 'NONE',  ( 15.05440318628160057, -53.11618894467930119, -76.14999999999999147 ) ) ;
#14069=CARTESIAN_POINT ( 'NONE',  ( 57.32295481445549967, 19.23251083971900144, -53.14992580837979119 ) ) ;
#14070=CARTESIAN_POINT ( 'NONE',  ( 10.13410506222094298, 33.50987130397768254, -47.01082059560806670 ) ) ;
#14072=CIRCLE ( 'NONE', #51749, 21.19999999999999929 ) ;
#14073=CARTESIAN_POINT ( 'NONE',  ( 47.07821196700830058, -54.56982298144170329, -75.12266286288350159 ) ) ;
#14074=ADVANCED_FACE ( 'NONE', ( #14110 ), #45410, .F. ) ;
#14076=CARTESIAN_POINT ( 'NONE',  ( 48.21690961261940345, -54.18825503271109767, -54.70306002727500072 ) ) ;
#14078=CARTESIAN_POINT ( 'NONE',  ( 56.35191062136929929, 19.31104562819170312, -52.86474270505669892 ) ) ;
#14079=CARTESIAN_POINT ( 'NONE',  ( 48.19376166029200448, 23.04067999044779924, -54.98857909375249875 ) ) ;
#14080=ORIENTED_EDGE ( 'NONE', *, *, #27106, .F. ) ;
#14082=ORIENTED_EDGE ( 'NONE', *, *, #14800, .F. ) ;
#14084=DIRECTION ( 'NONE',  ( -0.4640893551880615475, -0.8857883891771946017, 0.000000000000000000 ) ) ;
#14086=CARTESIAN_POINT ( 'NONE',  ( 84.08245047910018855, 13.26582018360060111, -47.41523600659849791 ) ) ;
#14087=CARTESIAN_POINT ( 'NONE',  ( 53.88904214046930008, 17.16505862634210189, -26.27980819959719838 ) ) ;
#14095=CARTESIAN_POINT ( 'NONE',  ( 12.30205595647329986, -64.73832649162540065, -15.96528926833489948 ) ) ;
#14097=CARTESIAN_POINT ( 'NONE',  ( -33.86606260230181675, -10.73525358442780941, -57.75434594776561426 ) ) ;
#14098=FACE_OUTER_BOUND ( 'NONE', #22166, .T. ) ;
#14100=ORIENTED_EDGE ( 'NONE', *, *, #828, .F. ) ;
#14102=DIRECTION ( 'NONE',  ( 0.000000000000000000, 0.000000000000000000, -1.000000000000000000 ) ) ;
#14103=CARTESIAN_POINT ( 'NONE',  ( 53.56302256516740101, -49.38660883080410713, -49.17075139047770449 ) ) ;
#14104=CARTESIAN_POINT ( 'NONE',  ( 52.05055437614630165, 19.18114209767879785, -49.15813440252989608 ) ) ;
#14105=CARTESIAN_POINT ( 'NONE',  ( 60.35865778877810328, -2.352205281898970490, -15.82496069747729983 ) ) ;
#14106=CARTESIAN_POINT ( 'NONE',  ( 50.57709999312749716, -48.61618543841219520, -76.21964823130220168 ) ) ;
#14107=CARTESIAN_POINT ( 'NONE',  ( 58.05620727321760199, -49.44730473131560444, -51.87485358542139835 ) ) ;
#14110=FACE_OUTER_BOUND ( 'NONE', #16952, .T. ) ;
#14113=VECTOR ( 'NONE', #17161, 1000.000000000000000 ) ;
#14118=CARTESIAN_POINT ( 'NONE',  ( 13.64640607913560011, -50.80567383909779977, -21.56020319207080149 ) ) ;
#14119=CARTESIAN_POINT ( 'NONE',  ( 53.99861951552289696, 19.51405001656310034, -76.30342085868839774 ) ) ;
#14120=CARTESIAN_POINT ( 'NONE',  ( 47.60133233420110344, -54.52312452709470136, -74.50414561666529778 ) ) ;
#14123=CARTESIAN_POINT ( 'NONE',  ( 55.69613912887059826, 14.53694977389559995, -16.67869178985480261 ) ) ;
#14124=CARTESIAN_POINT ( 'NONE',  ( 47.71697316577869685, 23.26510924299340033, -55.03111162414960233 ) ) ;
#14125=CARTESIAN_POINT ( 'NONE',  ( 57.32828653034319899, -50.41406207962300812, -53.00038473087199975 ) ) ;
#14128=CARTESIAN_POINT ( 'NONE',  ( 47.56773526946430763, 23.32812596456290066, -74.36162932837530093 ) ) ;
#14129=CARTESIAN_POINT ( 'NONE',  ( 20.13393738107516029, -55.41568638132210367, -20.08918511024506159 ) ) ;
#14130=CARTESIAN_POINT ( 'NONE',  ( 41.14609131925150365, -45.53782844434120136, -6.107216659010040516 ) ) ;
#14131=CARTESIAN_POINT ( 'NONE',  ( 12.79282753983206611, -65.49328885638416864, -23.41071104114353574 ) ) ;
#14135=EDGE_CURVE ( 'NONE', #20725, #20296, #29568, .T. ) ;
#14136=CARTESIAN_POINT ( 'NONE',  ( 82.55595867320781167, 14.40020173682131954, -47.71333528890980347 ) ) ;
#14142=CARTESIAN_POINT ( 'NONE',  ( -26.85818705357539926, 10.53358274763490066, -55.57881993978430302 ) ) ;
#14144=CARTESIAN_POINT ( 'NONE',  ( 53.29389463559500228, -49.43182142001269597, -48.95065373416729670 ) ) ;
#14147=CARTESIAN_POINT ( 'NONE',  ( 17.21347160910339724, 21.88381105532300097, -76.14999999999999147 ) ) ;
#14148=CARTESIAN_POINT ( 'NONE',  ( 53.67901547079682700, -51.32026565108220240, -75.56983433779308257 ) ) ;
#14149=CARTESIAN_POINT ( 'NONE',  ( 13.47926327417509995, 19.82353983917930051, -21.90689185999260147 ) ) ;
#14150=CARTESIAN_POINT ( 'NONE',  ( 57.62061476366090318, 13.90145536118990144, -25.55370966833229929 ) ) ;
#14153=CARTESIAN_POINT ( 'NONE',  ( 50.98562399990609606, 19.60288930407019947, -76.14999999999999147 ) ) ;
#14154=CARTESIAN_POINT ( 'NONE',  ( 53.50489543215090293, 18.19328726694199716, -49.20411598972469847 ) ) ;
#14156=DIRECTION ( 'NONE',  ( -1.000000000000000000, 0.000000000000000000, 0.000000000000000000 ) ) ;
#14160=CARTESIAN_POINT ( 'NONE',  ( 49.40539548398250247, -53.49785366680099941, -54.15746054658189479 ) ) ;
#14163=CARTESIAN_POINT ( 'NONE',  ( 11.41950678098469929, -65.35719241412380143, -18.15863199444450160 ) ) ;
#14170=ORIENTED_EDGE ( 'NONE', *, *, #20069, .F. ) ;
#14171=CARTESIAN_POINT ( 'NONE',  ( 10.49392349455719931, -63.33912771724479995, -45.62648268597099843 ) ) ;
#14173=VERTEX_POINT ( 'NONE', #15152 ) ;
#14175=CARTESIAN_POINT ( 'NONE',  ( 56.94152841858620206, 19.37848640203839778, -53.44912207968510387 ) ) ;
#14177=CARTESIAN_POINT ( 'NONE',  ( 52.10718133714609479, 18.87579468230029889, -76.73077508321010498 ) ) ;
#14179=CARTESIAN_POINT ( 'NONE',  ( 11.55867067850401853, -65.29213368257272521, -47.38009360245612811 ) ) ;
#14187=ORIENTED_EDGE ( 'NONE', *, *, #12656, .T. ) ;
#14190=CARTESIAN_POINT ( 'NONE',  ( 56.56121202467220144, -46.20600250404840637, -26.26606259789259923 ) ) ;
#14192=AXIS2_PLACEMENT_3D ( 'NONE', #4456, #20683, #24085 ) ;
#14193=AXIS2_PLACEMENT_3D ( 'NONE', #32746, #24886, #5531 ) ;
#14197=CARTESIAN_POINT ( 'NONE',  ( 13.94115586785109961, 19.96087044110830178, -74.35527526576591129 ) ) ;
#14200=CARTESIAN_POINT ( 'NONE',  ( 45.76559021992609644, -45.11804673858839720, -7.588959103897489733 ) ) ;
#14204=CARTESIAN_POINT ( 'NONE',  ( 54.80419448789260173, -47.33494133938750537, -25.92210209326049863 ) ) ;
#14205=CARTESIAN_POINT ( 'NONE',  ( 55.66118929916900271, -50.90930937580999682, -75.01110568612280360 ) ) ;
#14206=CARTESIAN_POINT ( 'NONE',  ( 3.156509474638800050, 24.30419543549970030, -8.938496486758239712 ) ) ;
#14213=CARTESIAN_POINT ( 'NONE',  ( 47.47773078780689815, 23.37030520192059768, -54.73382622973240075 ) ) ;
#14217=CARTESIAN_POINT ( 'NONE',  ( 11.78008937361119912, 33.90493106804039769, -16.70885295318199937 ) ) ;
#14221=CARTESIAN_POINT ( 'NONE',  ( 55.85157221570699448, 15.39592295138489852, -26.24938425740990056 ) ) ;
#14223=CARTESIAN_POINT ( 'NONE',  ( 53.46638755025719547, 20.54076140048909949, -53.27253650584940203 ) ) ;
#14226=CARTESIAN_POINT ( 'NONE',  ( 12.21895752911560074, -64.97095625756598736, -16.28177273609240316 ) ) ;
#14229=CARTESIAN_POINT ( 'NONE',  ( 11.10530294771320037, 31.88305279702909800, -44.25053028539870326 ) ) ;
#14232=AXIS2_PLACEMENT_3D ( 'NONE', #42597, #6955, #29989 ) ;
#14233=CARTESIAN_POINT ( 'NONE',  ( 66.32946235891380127, -32.37525661809159772, -18.17791974922089793 ) ) ;
#14237=CARTESIAN_POINT ( 'NONE',  ( 48.85702442728309336, 22.78471410673780184, -55.29194429107999298 ) ) ;
#14239=CARTESIAN_POINT ( 'NONE',  ( 49.84506783314736822, -1.611968319188557208, -15.88097192665358470 ) ) ;
#14240=VERTEX_POINT ( 'NONE', #3619 ) ;
#14241=CARTESIAN_POINT ( 'NONE',  ( 13.00893739769619906, -65.51843714052719747, -47.75434321273180416 ) ) ;
#14242=CARTESIAN_POINT ( 'NONE',  ( 56.09983961787049367, -45.96733836777529802, -25.91450243792759878 ) ) ;
#14248=ORIENTED_EDGE ( 'NONE', *, *, #32660, .T. ) ;
#14249=CARTESIAN_POINT ( 'NONE',  ( 45.07857577476659827, -46.11250025407090192, -9.026857998747990663 ) ) ;
#14251=CARTESIAN_POINT ( 'NONE',  ( 51.92091365860093788, 1.594025306073798331, -18.96882430330588321 ) ) ;
#14252=CARTESIAN_POINT ( 'NONE',  ( 16.60577464339750264, 19.88381273883279832, -20.14978695510530216 ) ) ;
#14257=DIRECTION ( 'NONE',  ( 0.000000000000000000, 0.000000000000000000, 1.000000000000000000 ) ) ;
#14258=CARTESIAN_POINT ( 'NONE',  ( 47.18324198357279897, -54.80726809202429450, -74.17417149933299925 ) ) ;
#14259=CARTESIAN_POINT ( 'NONE',  ( 64.44913706933721187, 13.88381324743080114, -12.01620149882199939 ) ) ;
#14260=ADVANCED_FACE ( 'NONE', ( #3361 ), #10968, .T. ) ;
#14261=DIRECTION ( 'NONE',  ( 0.9441882088883087887, -0.3294064756441308917, 0.000000000000000000 ) ) ;
#14262=VECTOR ( 'NONE', #18581, 1000.000000000000000 ) ;
#14263=CIRCLE ( 'NONE', #2553, 29.70020322226740106 ) ;
#14264=CARTESIAN_POINT ( 'NONE',  ( 51.76047950956219523, 20.08324044957950250, -76.04144537520539870 ) ) ;
#14265=CARTESIAN_POINT ( 'NONE',  ( 59.34853940138299322, 13.89250407454670011, -25.97953579402879853 ) ) ;
#14268=B_SPLINE_SURFACE_WITH_KNOTS ( 'NONE', 3, 3, ( 
 ( #50807, #10977, #31886, #31375, #51578, #43965 ),
 ( #27712, #15422, #47906, #7559, #11235, #43209 ),
 ( #27455, #4129, #3886, #43457, #12007, #27196 ),
 ( #8070, #20105, #14895, #26944, #23503, #39528 ),
 ( #43712, #42950, #7046, #22998, #39019, #39267 ),
 ( #3628, #35056, #3369, #51062, #35590, #15676 ),
 ( #31630, #31121, #7815, #23768, #39780, #47146 ),
 ( #7299, #23250, #19342, #20613, #36876, #20881 ),
 ( #974, #29260, #33188, #12260, #40295, #48682 ),
 ( #8323, #40804, #8589, #28743, #12784, #36095 ),
 ( #32138, #201, #48155, #17227, #16700, #16976 ) ),
 .UNSPECIFIED., .F., .F., .F.,
 ( 4, 1, 1, 1, 1, 1, 1, 1, 4 ),
 ( 4, 2, 4 ),
 ( 0.000000000000000000, 0.1250000000000000000, 0.2500000000000000000, 0.3750000000000000000, 0.5000000000000000000, 0.6250000000000000000, 0.7500000000000000000, 0.8750000000000000000, 1.000001225116700088 ),
 ( -0.8336663705528200019, -0.6216045683949800171, -0.5133023023850340483 ),
 .UNSPECIFIED. ) ;
#14271=CARTESIAN_POINT ( 'NONE',  ( -5.339937516195930378, -47.24367322247450574, -5.307116475879639417 ) ) ;
#14275=CARTESIAN_POINT ( 'NONE',  ( 61.21108842818934903, -45.54439463435623026, -47.60783370497615863 ) ) ;
#14276=DIRECTION ( 'NONE',  ( 1.000000000000000000, 0.000000000000000000, 0.000000000000000000 ) ) ;
#14278=CARTESIAN_POINT ( 'NONE',  ( 1.027904703268279984, -42.68661147989060112, -15.65000000000000036 ) ) ;
#14279=CARTESIAN_POINT ( 'NONE',  ( 41.67695037001420388, 12.61921981549519955, -4.028589964710610261 ) ) ;
#14280=CARTESIAN_POINT ( 'NONE',  ( 68.13393739769630031, 16.88381105532302939, -68.79999999999976978 ) ) ;
#14282=CARTESIAN_POINT ( 'NONE',  ( 56.46551611171859975, 19.54378718077660082, -53.85224439323700096 ) ) ;
#14283=CARTESIAN_POINT ( 'NONE',  ( 76.64341730006429998, -43.20802362345402514, -14.27775341716986368 ) ) ;
#14284=ORIENTED_EDGE ( 'NONE', *, *, #32329, .T. ) ;
#14287=ORIENTED_EDGE ( 'NONE', *, *, #13844, .F. ) ;
#14293=EDGE_CURVE ( 'NONE', #18008, #3359, #15753, .T. ) ;
#14295=CARTESIAN_POINT ( 'NONE',  ( 44.98351759279099582, -46.11098047250180088, -8.963088896874140232 ) ) ;
#14296=ORIENTED_EDGE ( 'NONE', *, *, #32922, .T. ) ;
#14297=VERTEX_POINT ( 'NONE', #14886 ) ;
#14299=CARTESIAN_POINT ( 'NONE',  ( 61.43669518452560396, -45.19312879481820033, -46.80308561288980229 ) ) ;
#14305=DIRECTION ( 'NONE',  ( -1.129617809262089999E-08, -1.032305616123179888E-08, 1.000000000000000000 ) ) ;
#14307=FACE_OUTER_BOUND ( 'NONE', #8694, .T. ) ;
#14310=CARTESIAN_POINT ( 'NONE',  ( 53.83039865239790345, -50.85522019609880573, -76.11625649690100204 ) ) ;
#14311=CARTESIAN_POINT ( 'NONE',  ( 60.73605156023749885, 14.28962119872829994, -47.17434044904690182 ) ) ;
#14314=DIRECTION ( 'NONE',  ( -0.2260571801428140071, 0.000000000000000000, 0.9741140340359949468 ) ) ;
#14315=CARTESIAN_POINT ( 'NONE',  ( 43.41584083283380124, 13.83172669772440067, -6.498305962786799839 ) ) ;
#14316=CARTESIAN_POINT ( 'NONE',  ( 42.00588769014139956, -43.70649907349879726, -4.238533582109900166 ) ) ;
#14317=LINE ( 'NONE', #26092, #28673 ) ;
#14318=CYLINDRICAL_SURFACE ( 'NONE', #41587, 2.000000000000006217 ) ;
#14323=CARTESIAN_POINT ( 'NONE',  ( 14.51946302495829855, -52.60116553372549930, -76.03823174343609992 ) ) ;
#14324=CARTESIAN_POINT ( 'NONE',  ( 47.20824439995679711, -54.78745981783090713, -54.64190477282399883 ) ) ;
#14325=ADVANCED_FACE ( 'NONE', ( #31364 ), #51566, .T. ) ;
#14327=CARTESIAN_POINT ( 'NONE',  ( 11.13393739769619906, 32.28996932333459569, -43.76018303787720498 ) ) ;
#14328=TOROIDAL_SURFACE ( 'NONE', #29398, 19.56371635397779940, 1.000000000000000000 ) ;
#14331=CARTESIAN_POINT ( 'NONE',  ( 47.06489453142850010, -54.53966941020699721, -75.17791912558919876 ) ) ;
#14333=CARTESIAN_POINT ( 'NONE',  ( 48.31166452737429751, -54.24939451924300471, -55.28583570618040710 ) ) ;
#14334=CARTESIAN_POINT ( 'NONE',  ( 61.75019796695539753, -46.11618894467930119, -28.15000000000000213 ) ) ;
#14335=LINE ( 'NONE', #30304, #4981 ) ;
#14337=CARTESIAN_POINT ( 'NONE',  ( 48.08520103749209795, 23.02686870344080106, -54.72849252353350380 ) ) ;
#14343=CARTESIAN_POINT ( 'NONE',  ( 74.17629866868290378, -33.11618894467940066, -65.34607522167520699 ) ) ;
#14344=CARTESIAN_POINT ( 'NONE',  ( 83.66059785054299880, 13.61222787120309974, -47.23564833931240514 ) ) ;
#14345=CARTESIAN_POINT ( 'NONE',  ( 52.69501071984650054, 18.49099401042879975, -27.56727973799209863 ) ) ;
#14346=EDGE_CURVE ( 'NONE', #51329, #39, #34287, .T. ) ;
#14348=CARTESIAN_POINT ( 'NONE',  ( -33.86606260230380627, -15.61618894467929941, -56.14999999999999858 ) ) ;
#14351=ORIENTED_EDGE ( 'NONE', *, *, #10520, .T. ) ;
#14356=VERTEX_POINT ( 'NONE', #4898 ) ;
#14357=ADVANCED_FACE ( 'NONE', ( #11998 ), #10079, .T. ) ;
#14358=CARTESIAN_POINT ( 'NONE',  ( 12.16231664501490073, -64.67747237300790175, -15.91745067707079819 ) ) ;
#14361=LINE ( 'NONE', #1533, #40080 ) ;
#14363=ORIENTED_EDGE ( 'NONE', *, *, #11357, .T. ) ;
#14365=CARTESIAN_POINT ( 'NONE',  ( 56.83355978135429609, 14.76424485735420156, -26.24603836142980029 ) ) ;
#14367=CARTESIAN_POINT ( 'NONE',  ( 59.28498198370309780, -3.120077556817410169, -15.67198597102109936 ) ) ;
#14368=CARTESIAN_POINT ( 'NONE',  ( 51.08268012532420244, -48.61618608430239874, -76.44192738162151102 ) ) ;
#14369=CARTESIAN_POINT ( 'NONE',  ( 60.62314435019690251, -45.49594437324660134, -47.31712978262719815 ) ) ;
#14370=EDGE_CURVE ( 'NONE', #30581, #26391, #21, .T. ) ;
#14371=ORIENTED_EDGE ( 'NONE', *, *, #28294, .T. ) ;
#14372=CARTESIAN_POINT ( 'NONE',  ( 52.57246135266279907, -49.85409740178759819, -27.98331546413460202 ) ) ;
#14374=CARTESIAN_POINT ( 'NONE',  ( 70.83393739769690001, 16.88381105531749782, -71.50000000000000000 ) ) ;
#14377=CARTESIAN_POINT ( 'NONE',  ( 53.28808755212359216, -45.11618894467940066, -12.64220374978839878 ) ) ;
#14380=CARTESIAN_POINT ( 'NONE',  ( 12.80406157968080016, -50.65217205733890182, -21.33287590401240053 ) ) ;
#14381=CARTESIAN_POINT ( 'NONE',  ( 56.68161733921530043, 19.46491649270590329, -74.14923232710660272 ) ) ;
#14382=CARTESIAN_POINT ( 'NONE',  ( 47.61773728487339952, -54.54450626489860099, -74.19830160072660874 ) ) ;
#14383=CARTESIAN_POINT ( 'NONE',  ( 57.12074889286160584, 13.88381105532070059, -16.42681869645199910 ) ) ;
#14384=CARTESIAN_POINT ( 'NONE',  ( 47.78812228777269411, 23.20823330413379892, -54.85175909439769981 ) ) ;
#14385=CARTESIAN_POINT ( 'NONE',  ( 56.72395159914599816, -50.68578410791079847, -53.71484871590959642 ) ) ;
#14389=CARTESIAN_POINT ( 'NONE',  ( 47.57154853779519499, 23.33333473833040017, -74.17376148238459166 ) ) ;
#14393=CARTESIAN_POINT ( 'NONE',  ( 48.42521416700790127, -56.37491125791819968, -64.38029159777090626 ) ) ;
#14394=DIRECTION ( 'NONE',  ( 0.6415444970810870728, -0.4854844151940968522, 0.5939070136550171908 ) ) ;
#14395=CARTESIAN_POINT ( 'NONE',  ( 82.34852001369439733, 14.40950277491920062, -47.72348187592570667 ) ) ;
#14397=DIRECTION ( 'NONE',  ( 0.000000000000000000, 1.000000000000000000, 0.000000000000000000 ) ) ;
#14400=CARTESIAN_POINT ( 'NONE',  ( -32.74859963536999885, -5.990261158790339380, -56.32353328738960130 ) ) ;
#14402=CARTESIAN_POINT ( 'NONE',  ( 52.85417444733669612, -49.65285076575479906, -48.78849744257649945 ) ) ;
#14404=VERTEX_POINT ( 'NONE', #44671 ) ;
#14407=CARTESIAN_POINT ( 'NONE',  ( 13.86461347845260050, 19.85757936412190006, -22.12913923296040153 ) ) ;
#14408=CARTESIAN_POINT ( 'NONE',  ( 56.44408186407410000, 14.18700613804810118, -25.29404973353000230 ) ) ;
#14411=CARTESIAN_POINT ( 'NONE',  ( 53.40032980815939823, 18.21520279426259847, -49.16199818797040422 ) ) ;
#14412=CARTESIAN_POINT ( 'NONE',  ( 55.49709987488149210, -45.80398698926880030, -16.40980232892859902 ) ) ;
#14415=ORIENTED_EDGE ( 'NONE', *, *, #27076, .F. ) ;
#14418=CARTESIAN_POINT ( 'NONE',  ( 11.78395113718259957, -65.42271807190199695, -17.88069380536639841 ) ) ;
#14419=CARTESIAN_POINT ( 'NONE',  ( 11.89098172404790077, 34.12547406030940778, -47.42262565194260304 ) ) ;
#14421=CARTESIAN_POINT ( 'NONE',  ( 10.77197593517290031, -64.97501271978380544, -18.02693217527109937 ) ) ;
#14422=CARTESIAN_POINT ( 'NONE',  ( 53.02879952360030558, -49.61047114518112267, -49.09530619433566301 ) ) ;
#14428=EDGE_LOOP ( 'NONE', ( #39074, #9508, #18747, #22921, #32571 ) ) ;
#14429=CARTESIAN_POINT ( 'NONE',  ( 10.76935505275949900, -63.13244369400850076, -45.20656299583839655 ) ) ;
#14431=ORIENTED_EDGE ( 'NONE', *, *, #29492, .T. ) ;
#14432=LINE ( 'NONE', #33816, #27530 ) ;
#14433=CARTESIAN_POINT ( 'NONE',  ( 57.16059586828990291, 19.35048569732870050, -53.44447636780819977 ) ) ;
#14434=CARTESIAN_POINT ( 'NONE',  ( 52.22858155672869884, 18.58352814647409801, -77.10495058268929824 ) ) ;
#14436=FACE_OUTER_BOUND ( 'NONE', #28824, .T. ) ;
#14446=VERTEX_POINT ( 'NONE', #640 ) ;
#14447=CARTESIAN_POINT ( 'NONE',  ( 57.31659485773750617, -45.81640764159139678, -26.26798733862809954 ) ) ;
#14451=CARTESIAN_POINT ( 'NONE',  ( 16.13393739769620083, -15.61618894467929941, -6.649999999999999467 ) ) ;
#14452=CARTESIAN_POINT ( 'NONE',  ( 14.02313605303129762, 20.10118929730710136, -74.92517623884199907 ) ) ;
#14455=CARTESIAN_POINT ( 'NONE',  ( 45.45696629059829519, -45.23491596358309863, -8.052740744783449145 ) ) ;
#14459=CARTESIAN_POINT ( 'NONE',  ( 53.02464382135099896, -49.36657896306630278, -27.03748697953070135 ) ) ;
#14460=CARTESIAN_POINT ( 'NONE',  ( 55.34407407925619538, -50.75763021394610064, -75.61144563105409588 ) ) ;
#14461=FACE_OUTER_BOUND ( 'NONE', #3907, .T. ) ;
#14463=CARTESIAN_POINT ( 'NONE',  ( 12.06284766121009966, -63.44323389162830296, -22.25048313876769868 ) ) ;
#14466=CARTESIAN_POINT ( 'NONE',  ( -6.547582927393579943, -46.10825334578329660, -4.746448008273789654 ) ) ;
#14467=CARTESIAN_POINT ( 'NONE',  ( 47.46890301732349826, 23.37795228188129926, -54.75658226910749704 ) ) ;
#14468=CARTESIAN_POINT ( 'NONE',  ( 61.13393739769620083, -15.61618894467929941, -84.38499399519520239 ) ) ;
#14469=CARTESIAN_POINT ( 'NONE',  ( 83.95017614158776098, -44.74867211454660776, -47.46180894508327697 ) ) ;
#14471=CARTESIAN_POINT ( 'NONE',  ( 11.57186432615969984, 33.71257428197279182, -16.50172565923969970 ) ) ;
#14472=CARTESIAN_POINT ( 'NONE',  ( 51.65858043804030331, 17.70229134975009799, -76.94737799408660806 ) ) ;
#14473=CARTESIAN_POINT ( 'NONE',  ( 52.97622283594260040, 18.35180465121920079, -48.78091467802120462 ) ) ;
#14475=DIRECTION ( 'NONE',  ( 0.000000000000000000, 1.000000000000000000, 0.000000000000000000 ) ) ;
#14476=CARTESIAN_POINT ( 'NONE',  ( 54.85732554741899492, 16.42837036004689821, -26.50322149960979701 ) ) ;
#14477=EDGE_CURVE ( 'NONE', #19842, #34653, #20748, .T. ) ;
#14478=CARTESIAN_POINT ( 'NONE',  ( 50.03007040746459921, 5.621799825072190337, -76.14999999999999147 ) ) ;
#14481=FACE_OUTER_BOUND ( 'NONE', #8702, .T. ) ;
#14484=CARTESIAN_POINT ( 'NONE',  ( 10.97897909118739967, 32.05266905124919674, -44.74264738324500001 ) ) ;
#14485=AXIS2_PLACEMENT_3D ( 'NONE', #29172, #45173, #9286 ) ;
#14487=DIRECTION ( 'NONE',  ( 0.6676418852213139576, 0.2329255526947012489, -0.7071067811865460184 ) ) ;
#14489=CARTESIAN_POINT ( 'NONE',  ( 18.32671526147660046, 19.96087670211870346, -74.14993703734479880 ) ) ;
#14493=CARTESIAN_POINT ( 'NONE',  ( 76.49475457737827355, -3.230541735902681122, -13.20481492880512242 ) ) ;
#14495=CARTESIAN_POINT ( 'NONE',  ( 11.56725258447900018, -64.80210873993979703, -45.44585228502439378 ) ) ;
#14496=CARTESIAN_POINT ( 'NONE',  ( 56.47614208328440100, -45.49446754575470209, -25.70510218961669935 ) ) ;
#14497=LINE ( 'NONE', #10318, #10222 ) ;
#14498=EDGE_CURVE ( 'NONE', #6837, #7993, #17598, .T. ) ;
#14499=CARTESIAN_POINT ( 'NONE',  ( 11.87263725465938258, 24.15631867182189652, -22.13626404611502707 ) ) ;
#14500=VERTEX_POINT ( 'NONE', #4839 ) ;
#14501=CARTESIAN_POINT ( 'NONE',  ( 71.71126032029680175, 15.88381105532069704, -46.37203261889099792 ) ) ;
#14503=CARTESIAN_POINT ( 'NONE',  ( 11.89322115925799928, 34.20364973214489623, -22.25048088549079850 ) ) ;
#14504=ORIENTED_EDGE ( 'NONE', *, *, #48086, .F. ) ;
#14505=ADVANCED_FACE ( 'NONE', ( #48875 ), #28149, .T. ) ;
#14506=CARTESIAN_POINT ( 'NONE',  ( 46.47787128639799903, -45.11618894461340545, -8.157179474024399468 ) ) ;
#14509=CARTESIAN_POINT ( 'NONE',  ( 14.13974949994110020, 19.81019562857040128, -21.96874462324929667 ) ) ;
#14514=CARTESIAN_POINT ( 'NONE',  ( 47.32873553055200233, -54.60302095746399687, -74.72285389774751252 ) ) ;
#14515=CARTESIAN_POINT ( 'NONE',  ( 49.34439353803710304, 13.88381105527630055, -8.366262819176959908 ) ) ;
#14519=CARTESIAN_POINT ( 'NONE',  ( 52.61549993852860041, 20.12575500109499771, -75.86880970507380084 ) ) ;
#14520=CARTESIAN_POINT ( 'NONE',  ( 11.88236613208781023, 34.20274921340377006, -17.91369326123606598 ) ) ;
#14522=VERTEX_POINT ( 'NONE', #12979 ) ;
#14524=CARTESIAN_POINT ( 'NONE',  ( 5.283814748811780149, -58.95969427206990332, -12.16686142996949904 ) ) ;
#14525=CARTESIAN_POINT ( 'NONE',  ( 76.59602575693580206, 4.418458492249149216, -13.63971784130609777 ) ) ;
#14527=CARTESIAN_POINT ( 'NONE',  ( 19.64923255343473585, -55.46140024220354547, -75.44170189639848445 ) ) ;
#14528=DIRECTION ( 'NONE',  ( 0.4640893551880597712, -0.8857883891771956009, 0.000000000000000000 ) ) ;
#14530=CARTESIAN_POINT ( 'NONE',  ( 57.36123081079020380, 18.90300135422739913, -52.61896059691729732 ) ) ;
#14531=DIRECTION ( 'NONE',  ( -0.7071067811865475727, 0.000000000000000000, -0.7071067811865475727 ) ) ;
#14532=CARTESIAN_POINT ( 'NONE',  ( 40.53658511620930227, 13.51357186806880151, -4.211756100499810529 ) ) ;
#14535=CARTESIAN_POINT ( 'NONE',  ( 68.13393739769790614, -49.95860450174040324, -75.14853292321149070 ) ) ;
#14536=AXIS2_PLACEMENT_3D ( 'NONE', #40710, #48841, #26262 ) ;
#14537=ADVANCED_FACE ( 'NONE', ( #12189 ), #5849, .T. ) ;
#14539=CARTESIAN_POINT ( 'NONE',  ( 17.89921485063580064, -51.35369855969700126, -75.11575902015950135 ) ) ;
#14540=CARTESIAN_POINT ( 'NONE',  ( 53.33161320831360541, -44.97067256191790108, -8.409648214525970999 ) ) ;
#14545=VERTEX_POINT ( 'NONE', #28667 ) ;
#14548=DIRECTION ( 'NONE',  ( -0.2260571801428130634, -5.828670879282072626E-15, 0.9741140340359951688 ) ) ;
#14549=CARTESIAN_POINT ( 'NONE',  ( 7.571123728786868234, -60.97650226374818772, -20.43741446242723114 ) ) ;
#14551=CARTESIAN_POINT ( 'NONE',  ( 10.80839229981719818, 21.91123435898759908, -23.15000000000000213 ) ) ;
#14552=VERTEX_POINT ( 'NONE', #23697 ) ;
#14557=CARTESIAN_POINT ( 'NONE',  ( 56.44264214053480089, -45.11618894467940066, -15.14376385419100046 ) ) ;
#14558=CARTESIAN_POINT ( 'NONE',  ( 61.49690240543349518, -45.15381908667030331, -46.58186461253090016 ) ) ;
#14560=ADVANCED_FACE ( 'NONE', ( #31819 ), #831, .T. ) ;
#14561=DIRECTION ( 'NONE',  ( 1.000000000000000000, 0.000000000000000000, 0.000000000000000000 ) ) ;
#14564=ORIENTED_EDGE ( 'NONE', *, *, #42900, .T. ) ;
#14568=EDGE_LOOP ( 'NONE', ( #27951, #15921, #51686, #25493 ) ) ;
#14570=CARTESIAN_POINT ( 'NONE',  ( 51.74354729887659943, -51.02687482177999811, -76.13548131957189469 ) ) ;
#14571=CARTESIAN_POINT ( 'NONE',  ( 60.47761782512560558, 14.47093190675899876, -47.49433626963359956 ) ) ;
#14572=DIRECTION ( 'NONE',  ( 1.000000000000000000, 0.000000000000000000, 0.000000000000000000 ) ) ;
#14574=CARTESIAN_POINT ( 'NONE',  ( 41.84726576968089518, -43.59559707646589999, -3.460729485120859650 ) ) ;
#14576=CARTESIAN_POINT ( 'NONE',  ( 55.94825483526997800, 14.62989463075238916, -25.32139416924175634 ) ) ;
#14582=CARTESIAN_POINT ( 'NONE',  ( 14.91264436884699940, -52.75136490455189886, -76.12493046668770091 ) ) ;
#14584=CARTESIAN_POINT ( 'NONE',  ( 57.42543158765980138, 19.07922509033599567, -52.86045852939989942 ) ) ;
#14587=CARTESIAN_POINT ( 'NONE',  ( 52.68908936341578908, -49.75029824513269716, -38.31189016485959797 ) ) ;
#14588=DIRECTION ( 'NONE',  ( 0.1686178020941689892, 0.6660492713794449182, -0.7265992051412129005 ) ) ;
#14590=CARTESIAN_POINT ( 'NONE',  ( 48.06703750773939987, -54.33034557285180455, -54.98976173603559658 ) ) ;
#14593=CARTESIAN_POINT ( 'NONE',  ( 56.52383276625670305, 19.52002294768380253, -53.80484218896539517 ) ) ;
#14594=CARTESIAN_POINT ( 'NONE',  ( 48.26548450438669846, 23.00817015210510164, -54.98365607671500044 ) ) ;
#14598=EDGE_CURVE ( 'NONE', #4677, #22335, #7297, .T. ) ;
#14599=EDGE_LOOP ( 'NONE', ( #33193, #37705, #32824, #27670 ) ) ;
#14602=DIRECTION ( 'NONE',  ( 0.000000000000000000, 0.000000000000000000, -1.000000000000000000 ) ) ;
#14603=CARTESIAN_POINT ( 'NONE',  ( 83.47359158205310337, 13.98615420182590086, -47.48415154309289932 ) ) ;
#14604=CARTESIAN_POINT ( 'NONE',  ( 16.13393739769620083, -15.61618894467929941, -7.101316701949489385 ) ) ;
#14606=CARTESIAN_POINT ( 'NONE',  ( 52.82975622904280755, 18.42854261028849905, -28.15000000000000213 ) ) ;
#14610=ORIENTED_EDGE ( 'NONE', *, *, #15848, .T. ) ;
#14614=CARTESIAN_POINT ( 'NONE',  ( 12.21104395315190061, -64.88750845341350271, -16.16308188032050097 ) ) ;
#14615=CARTESIAN_POINT ( 'NONE',  ( 7.768034174689500304, -60.63850792724319660, -20.78409677699329805 ) ) ;
#14617=CARTESIAN_POINT ( 'NONE',  ( 12.48503350875200013, -65.45837120426659794, -47.47731082152539983 ) ) ;
#14618=EDGE_CURVE ( 'NONE', #13860, #48001, #51830, .T. ) ;
#14621=CARTESIAN_POINT ( 'NONE',  ( 52.99344130519229878, 21.02275823560590240, -54.37359777462930310 ) ) ;
#14622=CARTESIAN_POINT ( 'NONE',  ( 56.55522360613520760, 14.97957722649010037, -26.26695323647559732 ) ) ;
#14623=CARTESIAN_POINT ( 'NONE',  ( 52.76699503163899152, 18.41354606731650279, -48.30730215388749826 ) ) ;
#14624=B_SPLINE_CURVE_WITH_KNOTS ( 'NONE', 3,
 ( #26832, #31262, #22374, #42578, #6416, #27347, #19229, #50439, #38380, #38907, #6673, #23144 ),
 .UNSPECIFIED., .F., .F.,
 ( 4, 2, 2, 2, 2, 4 ),
 ( 0.000000000000000000, 0.2528991456833806772, 0.3793487185250741800, 0.4425735049459256776, 0.4741858981563524256, 0.5057982913667791181 ),
 .UNSPECIFIED. ) ;
#14625=CARTESIAN_POINT ( 'NONE',  ( 75.13393739769618662, -33.11618894467940066, -84.38499399519520239 ) ) ;
#14627=CARTESIAN_POINT ( 'NONE',  ( 51.25913874074879573, -49.93899559840220093, -76.33308073030519836 ) ) ;
#14628=CARTESIAN_POINT ( 'NONE',  ( 56.39270163676989966, -50.52750478097990339, -52.86271286804240077 ) ) ;
#14632=ORIENTED_EDGE ( 'NONE', *, *, #36645, .F. ) ;
#14633=CARTESIAN_POINT ( 'NONE',  ( 52.82975622904280755, -49.66092049964720445, -28.15000000000000213 ) ) ;
#14636=CARTESIAN_POINT ( 'NONE',  ( 14.13996207071699907, -51.04257905764659853, -21.96868406873729995 ) ) ;
#14637=CARTESIAN_POINT ( 'NONE',  ( 47.30391968620949683, -54.13632037683530029, -75.47331621149609759 ) ) ;
#14638=CARTESIAN_POINT ( 'NONE',  ( 56.50061946469200080, 14.14892819972229887, -17.74286813043059752 ) ) ;
#14639=CARTESIAN_POINT ( 'NONE',  ( 10.49497832658790131, 32.13626875971579722, -45.62743361653370044 ) ) ;
#14640=( BOUNDED_CURVE ( )  B_SPLINE_CURVE ( 3, ( #8631, #24581, #36647, #752 ),
 .UNSPECIFIED., .F., .T. ) 
 B_SPLINE_CURVE_WITH_KNOTS ( ( 4, 4 ),
 ( 4.416522867113069850, 4.551367696244820849 ),
 .UNSPECIFIED. ) 
 CURVE ( )  GEOMETRIC_REPRESENTATION_ITEM ( )  RATIONAL_B_SPLINE_CURVE ( ( 1.000000000000000000, 0.9984853132547846233, 0.9984853132547846233, 1.000000000000000000 ) ) 
 REPRESENTATION_ITEM ( '' )  );
#14642=ADVANCED_FACE ( 'NONE', ( #3112 ), #43710, .T. ) ;
#14646=CARTESIAN_POINT ( 'NONE',  ( 46.80224289649839875, 22.25487713458520034, -76.02816653588809004 ) ) ;
#14649=CARTESIAN_POINT ( 'NONE',  ( 45.24652675828470194, -45.11233960980349877, -7.238436661000799965 ) ) ;
#14650=LINE ( 'NONE', #22238, #11460 ) ;
#14651=CARTESIAN_POINT ( 'NONE',  ( 46.35275103504449845, -52.90993241930539881, -76.14999999999999147 ) ) ;
#14653=CARTESIAN_POINT ( 'NONE',  ( 82.61194114885600470, 14.02128113440400092, -47.15273303709880537 ) ) ;
#14658=CARTESIAN_POINT ( 'NONE',  ( -29.90021944857959824, 4.910539643151190958, -56.90940863684170381 ) ) ;
#14660=EDGE_CURVE ( 'NONE', #11419, #17917, #50805, .T. ) ;
#14661=CARTESIAN_POINT ( 'NONE',  ( 52.87767300843589879, -49.65031313576589866, -48.88837533472770502 ) ) ;
#14665=CARTESIAN_POINT ( 'NONE',  ( 13.58976835783069959, 19.98880259310410068, -22.27010927015149733 ) ) ;
#14666=CARTESIAN_POINT ( 'NONE',  ( 51.84382200394469464, -49.26715888966499790, -77.06468274235049876 ) ) ;
#14669=CARTESIAN_POINT ( 'NONE',  ( 53.54325352770920432, 18.17990710143569899, -49.20622422613530489 ) ) ;
#14672=DIRECTION ( 'NONE',  ( 0.000000000000000000, 0.000000000000000000, -1.000000000000000000 ) ) ;
#14675=CARTESIAN_POINT ( 'NONE',  ( 60.34379259250669492, 14.63564649040839960, -47.72732609510669732 ) ) ;
#14676=CARTESIAN_POINT ( 'NONE',  ( 12.91799614346290070, 34.28036428892229992, -47.72740221857549869 ) ) ;
#14678=CARTESIAN_POINT ( 'NONE',  ( 11.46916641884869925, -65.36694628387890305, -17.97103954075589982 ) ) ;
#14685=ORIENTED_EDGE ( 'NONE', *, *, #16367, .F. ) ;
#14687=CARTESIAN_POINT ( 'NONE',  ( 10.14580672186800214, -63.28459696954880087, -45.99312667690720957 ) ) ;
#14690=DIRECTION ( 'NONE',  ( 0.000000000000000000, 0.000000000000000000, 1.000000000000000000 ) ) ;
#14691=CYLINDRICAL_SURFACE ( 'NONE', #42827, 1.999999999999999778 ) ;
#14692=CARTESIAN_POINT ( 'NONE',  ( 53.05142854777299988, 19.34251570886219795, -76.69950310396559701 ) ) ;
#14694=FACE_OUTER_BOUND ( 'NONE', #9155, .T. ) ;
#14697=DIRECTION ( 'NONE',  ( 0.000000000000000000, 0.000000000000000000, 1.000000000000000000 ) ) ;
#14698=B_SPLINE_SURFACE_WITH_KNOTS ( 'NONE', 3, 3, ( 
 ( #37250, #33303, #45628, #45894, #40917, #49317, #25687, #8960, #5797, #5025, #1083, #13412, #17082, #29114, #21758, #33813 ),
 ( #37769, #13663, #33033, #33562, #1862, #25942, #45113, #44856, #41960, #6056, #21503, #49057, #13166, #22014, #38025, #18100 ),
 ( #12897, #37503, #29374, #1347, #25428, #34066, #9220, #24903, #49579, #1603, #28853, #29626, #2119, #20990, #45375, #25173 ),
 ( #5289, #17338, #9481, #17590, #34591, #30399, #30138, #18870, #38808, #50076, #34852, #31165, #50852, #50597, #14945, #7346 ),
 ( #7095, #18350, #34327, #14687, #30908, #46939, #2902, #11024, #43258, #47193, #26206, #2373, #10766, #46421, #22273, #35108 ),
 ( #3419, #27240, #14171, #10509, #46161, #10248, #42217, #11280, #30655, #26993, #23294, #26466, #42999, #46680, #51107, #6840 ),
 ( #42480, #50343, #23047, #39068, #6572, #15211, #3159, #22789, #19129, #39315, #19389, #6317, #26725, #38284, #14429, #42742 ),
 ( #22534, #38546, #2645, #18613, #23555, #496, #8372, #11800, #3933, #43758, #40339, #4433, #44526, #48462, #43505, #24062 ),
 ( #40589, #35639, #31675, #28007, #32185, #16229, #4690, #23808, #7859, #19893, #48202, #16482, #11541, #35886, #12305, #31419 ),
 ( #27502, #39569, #2, #3676, #51623, #28264, #20401, #24320, #44266, #36143, #19645, #4173, #36388, #32437, #15717, #15468 ),
 ( #12565, #44015, #47698, #27763, #28527, #8629, #35371, #24578, #51368, #8116, #15979, #39826, #47953, #47446, #7607, #31933 ) ),
 .UNSPECIFIED., .F., .F., .F.,
 ( 4, 1, 1, 1, 1, 1, 1, 1, 4 ),
 ( 4, 2, 2, 2, 2, 2, 2, 4 ),
 ( 0.000000000000000000, 0.1250000000000000000, 0.2500000000000000000, 0.3750000000000000000, 0.5000000000000000000, 0.6250000000000000000, 0.7500000000000000000, 0.8750000000000000000, 1.000000000000000000 ),
 ( -0.4072589812491170247, -0.3359886595305220380, -0.2545368632807000209, -0.2036294906245599834, -0.1781758042964910194, -0.1374499061715789838, -0.07228846917172100650, -3.520742999999999947E-15 ),
 .UNSPECIFIED. ) ;
#14702=ORIENTED_EDGE ( 'NONE', *, *, #5966, .F. ) ;
#14704=FACE_OUTER_BOUND ( 'NONE', #3921, .T. ) ;
#14706=CARTESIAN_POINT ( 'NONE',  ( 52.56874714592159847, -49.85803425300269964, -48.49333755979899507 ) ) ;
#14711=DIRECTION ( 'NONE',  ( 0.000000000000000000, 0.000000000000000000, 1.000000000000000000 ) ) ;
#14712=DIRECTION ( 'NONE',  ( -0.5481517552764691992, -0.4595822764623992418, -0.6987945222659983635 ) ) ;
#14715=CARTESIAN_POINT ( 'NONE',  ( 43.71655669661049615, -45.13538107674550304, -6.831381356293830365 ) ) ;
#14720=CARTESIAN_POINT ( 'NONE',  ( 52.58045726207989645, -49.84558690476340104, -28.15000000000000213 ) ) ;
#14722=CARTESIAN_POINT ( 'NONE',  ( 56.40006832003150095, -50.78900847487010850, -74.42134219975289966 ) ) ;
#14723=CARTESIAN_POINT ( 'NONE',  ( -9.486391603338390155, 12.57410522446340018, -6.341346566467760404 ) ) ;
#14726=FACE_OUTER_BOUND ( 'NONE', #9939, .T. ) ;
#14728=CARTESIAN_POINT ( 'NONE',  ( -8.393077763122880341, -44.64307718677159187, -5.215838194937219896 ) ) ;
#14729=CARTESIAN_POINT ( 'NONE',  ( 47.78813954756139992, 23.17881026155490076, -54.71474246861410506 ) ) ;
#14730=CARTESIAN_POINT ( 'NONE',  ( 41.40756764072759921, -44.77159127043780273, -5.393983506378570603 ) ) ;
#14733=CARTESIAN_POINT ( 'NONE',  ( 12.10371154477419964, 33.94898634442529328, -16.68259577208300115 ) ) ;
#14734=CARTESIAN_POINT ( 'NONE',  ( 7.635415421591214447, 29.62789471496180482, -20.56421356237308729 ) ) ;
#14735=CARTESIAN_POINT ( 'NONE',  ( 53.06503245504000432, 18.30587288450670158, -48.83676475384709903 ) ) ;
#14738=CARTESIAN_POINT ( 'NONE',  ( 58.76944267056379800, -46.69458659170329895, -47.97775221472399920 ) ) ;
#14739=CARTESIAN_POINT ( 'NONE',  ( 53.09178932327359490, 18.18835396469560095, -27.54443142566670133 ) ) ;
#14743=CARTESIAN_POINT ( 'NONE',  ( 75.41048247916201319, -48.61618894467930119, -82.11365365517008286 ) ) ;
#14745=CARTESIAN_POINT ( 'NONE',  ( 10.77042980482839951, 31.95257362349920172, -45.20517183706909492 ) ) ;
#14746=CARTESIAN_POINT ( 'NONE',  ( 17.92370450342619748, 19.88381105532299742, -15.67980087199299888 ) ) ;
#14749=CARTESIAN_POINT ( 'NONE',  ( 17.92367119475710169, 19.88380572466640217, -74.33583724502659607 ) ) ;
#14750=ORIENTED_EDGE ( 'NONE', *, *, #3185, .T. ) ;
#14751=ORIENTED_EDGE ( 'NONE', *, *, #29964, .F. ) ;
#14753=CARTESIAN_POINT ( 'NONE',  ( 76.55943877964870126, 0.2330598837798364131, -13.48354878354143516 ) ) ;
#14755=CARTESIAN_POINT ( 'NONE',  ( 11.17710517087889954, -63.96272249765520712, -44.13856387930640324 ) ) ;
#14756=CARTESIAN_POINT ( 'NONE',  ( 56.99474382507709436, -45.26449535605289753, -25.71127314621080018 ) ) ;
#14757=B_SPLINE_CURVE_WITH_KNOTS ( 'NONE', 3,
 ( #28484, #32921, #32654, #25319, #41071, #44742, #21136, #48415, #16180, #9373 ),
 .UNSPECIFIED., .F., .F.,
 ( 4, 1, 1, 1, 1, 1, 1, 4 ),
 ( 0.000000000000000000, 0.1428596598124854400, 0.2857193196249708800, 0.4285789794374563200, 0.5714386392499406497, 0.7142982990624261452, 0.8571579588749115297, 1.000000000000000000 ),
 .UNSPECIFIED. ) ;
#14760=EDGE_LOOP ( 'NONE', ( #50611, #23484, #38874, #26071, #9729, #12014, #36376, #24453, #28209, #37954 ) ) ;
#14763=AXIS2_PLACEMENT_3D ( 'NONE', #30626, #50824, #10733 ) ;
#14764=CARTESIAN_POINT ( 'NONE',  ( 11.36992640080890027, 32.26814655965639389, -24.38598900311270157 ) ) ;
#14768=DIRECTION ( 'NONE',  ( -1.000000000000000000, 0.000000000000000000, 0.000000000000000000 ) ) ;
#14771=FACE_OUTER_BOUND ( 'NONE', #32564, .T. ) ;
#14773=CARTESIAN_POINT ( 'NONE',  ( 47.37032927764639822, -54.67515752274410090, -74.17395249489511855 ) ) ;
#14774=CARTESIAN_POINT ( 'NONE',  ( 52.15685074734039972, 13.73913658471580135, -8.117659720543509039 ) ) ;
#14776=AXIS2_PLACEMENT_3D ( 'NONE', #4855, #28429, #4586 ) ;
#14777=CARTESIAN_POINT ( 'NONE',  ( 49.81371308193354253, 22.09252804302983009, -54.04984813473200234 ) ) ;
#14778=CARTESIAN_POINT ( 'NONE',  ( 65.17764417800763965, -31.69782882504341259, -17.21758621636998754 ) ) ;
#14781=CARTESIAN_POINT ( 'NONE',  ( 53.68666193310649959, -48.91266994132399759, -27.15311340496670311 ) ) ;
#14782=CARTESIAN_POINT ( 'NONE',  ( -3.663975856005799780, -49.36779947823060155, -6.368283874185619808 ) ) ;
#14783=CARTESIAN_POINT ( 'NONE',  ( 75.49632929579119889, 4.576312485752930037, -12.47599735184120107 ) ) ;
#14784=CARTESIAN_POINT ( 'NONE',  ( 75.25100069975053430, 13.51599575700000422, -14.19917115362995830 ) ) ;
#14787=B_SPLINE_CURVE_WITH_KNOTS ( 'NONE', 3,
 ( #18773, #10146, #42640, #18253, #46578, #49981, #46317, #33714, #34745, #14073, #14331, #26624, #9883, #25839, #34221, #10409, #42377, #6474, #22948, #41851, #5956, #2022, #46058, #26105, #20051, #31835 ),
 .UNSPECIFIED., .F., .F.,
 ( 4, 2, 2, 2, 2, 2, 2, 2, 2, 2, 2, 2, 4 ),
 ( 0.000000000000000000, 0.02309096440924889374, 0.1572026337881723412, 0.2410224271499988302, 0.3014770649499997623, 0.3619317027499990846, 0.4374999999999998335, 0.5000000000000000000, 0.6250000000000004441, 0.7081425603971044369, 0.7912851207942084297, 0.8880021141917445737, 1.000000000000000000 ),
 .UNSPECIFIED. ) ;
#14789=VECTOR ( 'NONE', #34434, 1000.000000000000000 ) ;
#14790=CARTESIAN_POINT ( 'NONE',  ( 82.68209466367581228, -45.40217087331220114, -47.42729881771100509 ) ) ;
#14791=DIRECTION ( 'NONE',  ( 0.000000000000000000, 0.000000000000000000, 1.000000000000000000 ) ) ;
#14792=CARTESIAN_POINT ( 'NONE',  ( 41.59466759967410354, 12.80917673894839837, -4.344851877681960239 ) ) ;
#14793=CARTESIAN_POINT ( 'NONE',  ( 68.38971107296249841, -30.11618894467929763, -18.15384911730639672 ) ) ;
#14797=CARTESIAN_POINT ( 'NONE',  ( 68.13393739769649926, -48.11618894467630270, -70.54999999999999716 ) ) ;
#14798=FACE_OUTER_BOUND ( 'NONE', #1334, .T. ) ;
#14799=CARTESIAN_POINT ( 'NONE',  ( 18.20232122522270046, -51.72389970538209525, -75.45052476223459337 ) ) ;
#14800=EDGE_CURVE ( 'NONE', #23175, #25078, #8344, .T. ) ;
#14801=CARTESIAN_POINT ( 'NONE',  ( 53.51285457508119947, -44.36157961519030124, -7.701314136274850952 ) ) ;
#14806=CARTESIAN_POINT ( 'NONE',  ( -0.9227350764160839880, 21.52762428946969919, -9.384582815335910766 ) ) ;
#14811=CARTESIAN_POINT ( 'NONE',  ( 45.12942576520030258, -45.58081347128780436, -8.542108704436810029 ) ) ;
#14815=VECTOR ( 'NONE', #34545, 1000.000000000000000 ) ;
#14818=CARTESIAN_POINT ( 'NONE',  ( 57.05054250623780376, -45.11618894467940066, -16.05309365090189999 ) ) ;
#14819=CARTESIAN_POINT ( 'NONE',  ( 61.07761260003830017, -45.33963634432910084, -46.86460514787039955 ) ) ;
#14820=CARTESIAN_POINT ( 'NONE',  ( 82.64648846854103681, -45.32234436122444521, -47.29314152744393596 ) ) ;
#14821=CIRCLE ( 'NONE', #39919, 18.50000000000000000 ) ;
#14827=ORIENTED_EDGE ( 'NONE', *, *, #42970, .T. ) ;
#14829=CARTESIAN_POINT ( 'NONE',  ( 50.96210775137730309, -50.95759000963079899, -76.15000017728290516 ) ) ;
#14830=CARTESIAN_POINT ( 'NONE',  ( 60.28321421690059623, 14.52514086966039919, -47.30254520759619652 ) ) ;
#14831=TOROIDAL_SURFACE ( 'NONE', #35738, 39.99999927950579348, 2.000000001564220309 ) ;
#14833=EDGE_CURVE ( 'NONE', #3421, #34462, #16698, .T. ) ;
#14834=CARTESIAN_POINT ( 'NONE',  ( 43.12694253603230266, -42.75409364460660555, -4.223455518406679765 ) ) ;
#14836=CARTESIAN_POINT ( 'NONE',  ( -6.891925080208380017, 14.67362240842299848, -5.213017414248930059 ) ) ;
#14838=CARTESIAN_POINT ( 'NONE',  ( 41.23393739769609567, -15.61618894467929586, 8.450000000000018829 ) ) ;
#14841=VERTEX_POINT ( 'NONE', #48949 ) ;
#14842=CARTESIAN_POINT ( 'NONE',  ( 14.77612737573100077, -52.84830569448709525, -76.12661215459480957 ) ) ;
#14843=B_SPLINE_CURVE_WITH_KNOTS ( 'NONE', 3,
 ( #9055, #37875, #41019, #1187, #21343, #21089, #9576, #28952, #25004, #1967, #37091, #1708, #9833, #25786, #17944, #5387 ),
 .UNSPECIFIED., .F., .F.,
 ( 4, 2, 2, 2, 2, 2, 2, 4 ),
 ( 0.000000000000000000, 0.1839239004051475279, 0.3399707309250580844, 0.4375000000000012768, 0.5000000000000000000, 0.6249999999999998890, 0.8250000000000015099, 1.000000000000000000 ),
 .UNSPECIFIED. ) ;
#14844=CARTESIAN_POINT ( 'NONE',  ( 57.40343761314740334, 19.28400752131850027, -53.29433798474970274 ) ) ;
#14847=CARTESIAN_POINT ( 'NONE',  ( 15.91925957857180052, 19.75099634535679982, -20.31192411766160077 ) ) ;
#14850=CARTESIAN_POINT ( 'NONE',  ( 61.04001029137710077, 14.12696047140060074, -46.86320535112459851 ) ) ;
#14851=CARTESIAN_POINT ( 'NONE',  ( 47.88879426235710213, -54.35786135377490069, -54.72388424469730239 ) ) ;
#14853=CARTESIAN_POINT ( 'NONE',  ( 56.47485682376580485, 19.50905819124500340, -53.50470829161239550 ) ) ;
#14859=LINE ( 'NONE', #3074, #11689 ) ;
#14860=CARTESIAN_POINT ( 'NONE',  ( 48.79180034249638709, -53.85388452497296896, -54.46585069627487741 ) ) ;
#14861=CARTESIAN_POINT ( 'NONE',  ( 83.74313374146190370, 13.73424720782510100, -47.44649717229000174 ) ) ;
#14862=DIRECTION ( 'NONE',  ( 1.000000000000000000, 0.000000000000000000, 0.000000000000000000 ) ) ;
#14867=ORIENTED_EDGE ( 'NONE', *, *, #11168, .F. ) ;
#14869=ORIENTED_EDGE ( 'NONE', *, *, #24321, .F. ) ;
#14870=AXIS2_PLACEMENT_3D ( 'NONE', #18332, #2356, #34311 ) ;
#14871=ORIENTED_EDGE ( 'NONE', *, *, #8269, .F. ) ;
#14872=CARTESIAN_POINT ( 'NONE',  ( 12.36320305068320025, -64.54682834576858852, -15.76422791927960176 ) ) ;
#14874=CARTESIAN_POINT ( 'NONE',  ( 76.47997422168397463, -27.07588652318575129, -13.14112417631144325 ) ) ;
#14875=CARTESIAN_POINT ( 'NONE',  ( 12.80749145503170006, -65.50216741970210421, -47.64796710884480291 ) ) ;
#14878=CARTESIAN_POINT ( 'NONE',  ( 52.47879378027160158, 21.24197845805020179, -54.47385978244420102 ) ) ;
#14881=CARTESIAN_POINT ( 'NONE',  ( 65.12608554791199822, 0.7709852564592141189, -17.50910145119379990 ) ) ;
#14882=CARTESIAN_POINT ( 'NONE',  ( 51.50850403090069562, -48.69821067683690075, -76.79363216376179935 ) ) ;
#14883=CARTESIAN_POINT ( 'NONE',  ( 61.09079324505120212, -45.54437747975160278, -47.59851791355200135 ) ) ;
#14886=CARTESIAN_POINT ( 'NONE',  ( 40.76017233408010298, 14.12870932884110076, -5.740519046195230679 ) ) ;
#14889=CARTESIAN_POINT ( 'NONE',  ( 48.77938445319979621, -45.11618894467940066, -9.436603585651489823 ) ) ;
#14891=CARTESIAN_POINT ( 'NONE',  ( 13.71441810546650153, -51.14956980057220193, -22.21276096959649848 ) ) ;
#14894=CARTESIAN_POINT ( 'NONE',  ( 56.48007840179790406, 14.15040822888880001, -17.55434835152090045 ) ) ;
#14895=CARTESIAN_POINT ( 'NONE',  ( 60.94787312208169539, -45.42919348794200118, -47.18994051989060523 ) ) ;
#14896=EDGE_CURVE ( 'NONE', #39662, #33083, #39371, .T. ) ;
#14897=CARTESIAN_POINT ( 'NONE',  ( 56.84186849725410440, -50.37971971411840144, -52.83665658960050138 ) ) ;
#14903=CARTESIAN_POINT ( 'NONE',  ( 47.40092525023009529, 23.10040719678089971, -75.17431006860279297 ) ) ;
#14905=B_SPLINE_CURVE_WITH_KNOTS ( 'NONE', 3,
 ( #3330, #31594, #51287, #43169, #23730, #7523, #7780, #47614, #19044, #39494 ),
 .UNSPECIFIED., .F., .F.,
 ( 4, 2, 2, 2, 4 ),
 ( 0.000000000000000000, 0.1775000000085890928, 0.3375000000163220770, 0.4375000000211544116, 0.4459052190640770963 ),
 .UNSPECIFIED. ) ;
#14910=DIRECTION ( 'NONE',  ( 0.000000000000000000, 0.000000000000000000, -1.000000000000000000 ) ) ;
#14913=CARTESIAN_POINT ( 'NONE',  ( 52.47677922141266293, 18.72919119518283182, -77.24546349350585217 ) ) ;
#14918=CARTESIAN_POINT ( 'NONE',  ( 48.92624713453859897, 22.59774914665240075, -54.51889614858499300 ) ) ;
#14920=CARTESIAN_POINT ( 'NONE',  ( 53.20331604642460377, -49.48552951222239926, -48.99213278053210274 ) ) ;
#14921=EDGE_LOOP ( 'NONE', ( #18026, #22204, #20326, #22144 ) ) ;
#14924=CARTESIAN_POINT ( 'NONE',  ( 14.03113113476580232, 19.93369484523139690, -22.86118034424179868 ) ) ;
#14927=CARTESIAN_POINT ( 'NONE',  ( 52.90146998106999376, 18.41335516957889951, -48.94440823327429513 ) ) ;
#14928=CARTESIAN_POINT ( 'NONE',  ( 55.59350741772299642, -45.78716744078080580, -16.53259405490819844 ) ) ;
#14932=ORIENTED_EDGE ( 'NONE', *, *, #16789, .T. ) ;
#14934=CARTESIAN_POINT ( 'NONE',  ( 9.342451040078868729, 32.74871876812539995, -46.70581140351080052 ) ) ;
#14936=CARTESIAN_POINT ( 'NONE',  ( 53.59019059237800064, -49.40616797538680061, -49.22498841376049938 ) ) ;
#14937=CARTESIAN_POINT ( 'NONE',  ( 16.13393739769620083, -15.61618894467929941, -170.7999095292539948 ) ) ;
#14941=CARTESIAN_POINT ( 'NONE',  ( 51.82317580592130213, -52.75362460619970051, -54.60923380648279846 ) ) ;
#14942=ORIENTED_EDGE ( 'NONE', *, *, #49040, .T. ) ;
#14943=CARTESIAN_POINT ( 'NONE',  ( 61.50409964636570237, 14.14168666559669951, -47.35437808293550432 ) ) ;
#14945=CARTESIAN_POINT ( 'NONE',  ( 9.727947716817020307, -63.12714292155349938, -46.30183543362019805 ) ) ;
#14946=CARTESIAN_POINT ( 'NONE',  ( 12.13393739769649926, 24.18330853958550364, -23.15000000000000213 ) ) ;
#14947=ORIENTED_EDGE ( 'NONE', *, *, #21686, .F. ) ;
#14948=CARTESIAN_POINT ( 'NONE',  ( 66.85007717593936150, -33.11601710128963560, -20.46329705161230805 ) ) ;
#14949=CARTESIAN_POINT ( 'NONE',  ( 56.95883372640280129, 19.02269652816849899, -52.69722348556799574 ) ) ;
#14950=CARTESIAN_POINT ( 'NONE',  ( 53.18839696306619658, 19.26518443456370022, -76.93089028591350598 ) ) ;
#14953=CARTESIAN_POINT ( 'NONE',  ( 9.013808796976707782, -63.78940032850923103, -46.72196777939856105 ) ) ;
#14954=CARTESIAN_POINT ( 'NONE',  ( 53.09962126454065867, 20.18306339911599778, -75.69942531578703893 ) ) ;
#14960=VERTEX_POINT ( 'NONE', #8843 ) ;
#14962=DIRECTION ( 'NONE',  ( 0.000000000000000000, 0.000000000000000000, 1.000000000000000000 ) ) ;
#14964=CARTESIAN_POINT ( 'NONE',  ( 52.58955037394610343, -49.83869439510250032, -48.57080679444320026 ) ) ;
#14965=CARTESIAN_POINT ( 'NONE',  ( 52.74287992188719443, 13.88381105524769943, -12.54865867989730077 ) ) ;
#14967=EDGE_CURVE ( 'NONE', #51304, #10101, #21950, .T. ) ;
#14969=CARTESIAN_POINT ( 'NONE',  ( 16.13393739769609780, -15.61618894467929941, 8.449999999999999289 ) ) ;
#14970=FACE_OUTER_BOUND ( 'NONE', #19652, .T. ) ;
#14971=CARTESIAN_POINT ( 'NONE',  ( 11.79626796994640081, 33.68213603922090016, -16.32611600087430048 ) ) ;
#14972=CIRCLE ( 'NONE', #13300, 2.000000000000002220 ) ;
#14976=CARTESIAN_POINT ( 'NONE',  ( 54.19674966252080139, -50.83120162869429493, -76.02018738249189767 ) ) ;
#14977=CARTESIAN_POINT ( 'NONE',  ( -5.639092938195660487, 16.55660679010130210, -6.778460780884890902 ) ) ;
#14978=CARTESIAN_POINT ( 'NONE',  ( 75.13393739769618662, -15.61618894467929941, -84.38499399519520239 ) ) ;
#14980=DIRECTION ( 'NONE',  ( -0.7226652920947608250, -0.6911981449639416075, 0.000000000000000000 ) ) ;
#14981=DIRECTION ( 'NONE',  ( 1.224646799147353207E-16, 1.000000000000000000, -0.000000000000000000 ) ) ;
#14983=CARTESIAN_POINT ( 'NONE',  ( -8.399016668626551052, -44.63805185196870440, -5.182633193463829890 ) ) ;
#14984=CARTESIAN_POINT ( 'NONE',  ( 47.71230462437779352, 23.25609537601400234, -54.91947580701529574 ) ) ;
#14985=CARTESIAN_POINT ( 'NONE',  ( 45.92996289863866366, -45.11618893962639021, -7.538592778498961700 ) ) ;
#14987=CARTESIAN_POINT ( 'NONE',  ( 61.12445714337039959, 14.53949875652389956, -47.85281647892329460 ) ) ;
#14988=CARTESIAN_POINT ( 'NONE',  ( 11.27698456966049889, 33.93186547003269737, -17.25002982802569917 ) ) ;
#14989=CARTESIAN_POINT ( 'NONE',  ( 51.95458709081180615, 18.47553477844409997, -76.89034002170231474 ) ) ;
#14990=CARTESIAN_POINT ( 'NONE',  ( 52.81826460758630049, 18.43456339274279898, -48.49937508744089598 ) ) ;
#14993=CARTESIAN_POINT ( 'NONE',  ( 54.53382703113199881, 16.91529470431860105, -26.77221820697280208 ) ) ;
#14994=CARTESIAN_POINT ( 'NONE',  ( 50.50556472799611640, 4.843111011011147049, -76.20733270045852237 ) ) ;
#14996=CARTESIAN_POINT ( 'NONE',  ( 53.55182622754160349, 18.18654131614419711, -49.22385694762949981 ) ) ;
#14997=CARTESIAN_POINT ( 'NONE',  ( 62.15049734348340138, -31.05978833337919554, -16.60284431732980082 ) ) ;
#14999=CARTESIAN_POINT ( 'NONE',  ( 11.13393739769619906, 32.18560202157300409, -43.92096349992370108 ) ) ;
#15002=CARTESIAN_POINT ( 'NONE',  ( 50.96349269431694040, -35.28592947176570505, -76.38117427622687217 ) ) ;
#15004=ORIENTED_EDGE ( 'NONE', *, *, #9563, .F. ) ;
#15005=ADVANCED_FACE ( 'NONE', ( #3543 ), #1696, .T. ) ;
#15006=VERTEX_POINT ( 'NONE', #42018 ) ;
#15007=DIRECTION ( 'NONE',  ( -0.6320511108061763750, -0.7748042566436798007, -0.01377523921801214815 ) ) ;
#15008=CARTESIAN_POINT ( 'NONE',  ( 76.56354261845024212, 0.4299193838037037585, -13.50123283572469290 ) ) ;
#15010=CARTESIAN_POINT ( 'NONE',  ( 11.51479647464729972, -64.70247410274960487, -44.93983864453959853 ) ) ;
#15011=CARTESIAN_POINT ( 'NONE',  ( 57.41391223940169652, -45.19612066180349785, -25.73569688666339772 ) ) ;
#15012=DIRECTION ( 'NONE',  ( 0.000000000000000000, -1.000000000000000000, 0.000000000000000000 ) ) ;
#15017=ORIENTED_EDGE ( 'NONE', *, *, #1763, .T. ) ;
#15018=DIRECTION ( 'NONE',  ( 0.05355673475992404897, -0.9985648081931662867, 0.000000000000000000 ) ) ;
#15021=CARTESIAN_POINT ( 'NONE',  ( 11.96620750885719886, 34.18065854861499986, -22.91770525601710062 ) ) ;
#15024=CARTESIAN_POINT ( 'NONE',  ( 51.51227227048835999, 0.9479476914507564134, -17.73309803839580212 ) ) ;
#15028=CARTESIAN_POINT ( 'NONE',  ( 59.73136311602019788, -29.07177110127760145, -15.76233559764669856 ) ) ;
#15030=CARTESIAN_POINT ( 'NONE',  ( 46.41634634279859739, -53.01112433162619908, -76.14999999999999147 ) ) ;
#15031=CARTESIAN_POINT ( 'NONE',  ( 41.17242422168380500, 13.88381105527830073, -6.491247222890830670 ) ) ;
#15032=EDGE_CURVE ( 'NONE', #36840, #12954, #3382, .T. ) ;
#15033=CARTESIAN_POINT ( 'NONE',  ( 14.96048611060250089, 21.72103359751309881, -76.14999999999999147 ) ) ;
#15034=CARTESIAN_POINT ( 'NONE',  ( 61.68315737383129971, 13.88381108669560149, -27.59559020379299810 ) ) ;
#15036=ORIENTED_EDGE ( 'NONE', *, *, #12390, .T. ) ;
#15038=CARTESIAN_POINT ( 'NONE',  ( 0.9985768606438358841, -53.36496704980149985, -7.599376136359519585 ) ) ;
#15039=CARTESIAN_POINT ( 'NONE',  ( 76.34491340151899408, -12.50878940850270027, -12.55768725632909977 ) ) ;
#15040=CARTESIAN_POINT ( 'NONE',  ( 75.40247264985536901, 12.93137384474434803, -13.67377317579595264 ) ) ;
#15041=CARTESIAN_POINT ( 'NONE',  ( 61.06707969152498805, -45.46952364607431463, -47.42741923847710694 ) ) ;
#15045=AXIS2_PLACEMENT_3D ( 'NONE', #45878, #28635, #21997 ) ;
#15046=DIRECTION ( 'NONE',  ( 0.000000000000000000, -1.000000000000000000, 0.000000000000000000 ) ) ;
#15048=CARTESIAN_POINT ( 'NONE',  ( 82.75410128693920342, -45.59485774729899532, -47.67218414831240381 ) ) ;
#15049=CARTESIAN_POINT ( 'NONE',  ( 57.30875059015219364, -50.56238778299910308, -53.44855692689219495 ) ) ;
#15050=CARTESIAN_POINT ( 'NONE',  ( 42.13038056796350617, 12.10098310850369963, -3.383138905913079864 ) ) ;
#15051=DIRECTION ( 'NONE',  ( 0.000000000000000000, 0.000000000000000000, -1.000000000000000000 ) ) ;
#15053=CARTESIAN_POINT ( 'NONE',  ( 56.51601257069349771, -47.72958752039729546, -47.92267345016610136 ) ) ;
#15054=CARTESIAN_POINT ( 'NONE',  ( 56.52536539877749533, 19.51942783438209972, -53.84278118897309895 ) ) ;
#15057=CARTESIAN_POINT ( 'NONE',  ( 18.36965831139549721, -52.00201191962840142, -75.51495726157199329 ) ) ;
#15058=CARTESIAN_POINT ( 'NONE',  ( 53.02870100497279537, -51.95943102007580450, -53.35088539576909739 ) ) ;
#15061=VERTEX_POINT ( 'NONE', #10044 ) ;
#15067=CARTESIAN_POINT ( 'NONE',  ( 44.44811449676429760, -45.82485402717239964, -8.385894475659950942 ) ) ;
#15068=ORIENTED_EDGE ( 'NONE', *, *, #43795, .T. ) ;
#15069=CARTESIAN_POINT ( 'NONE',  ( 18.14078639169169804, 20.99064699730730155, -75.77237669558989808 ) ) ;
#15072=ORIENTED_EDGE ( 'NONE', *, *, #46395, .F. ) ;
#15076=EDGE_CURVE ( 'NONE', #19, #20901, #24446, .T. ) ;
#15077=CYLINDRICAL_SURFACE ( 'NONE', #34337, 20.79999999999999716 ) ;
#15081=PLANE ( 'NONE',  #150 ) ;
#15082=CARTESIAN_POINT ( 'NONE',  ( 17.92370450347650035, -51.11618894467930119, -15.67980085856620143 ) ) ;
#15085=ORIENTED_EDGE ( 'NONE', *, *, #19555, .F. ) ;
#15087=CARTESIAN_POINT ( 'NONE',  ( 51.26685530262009394, -51.02395401094319993, -76.14349094382490080 ) ) ;
#15088=AXIS2_PLACEMENT_3D ( 'NONE', #19448, #8175, #23105 ) ;
#15089=CARTESIAN_POINT ( 'NONE',  ( 60.34240538927109299, 14.50246306764029924, -47.36430858416980527 ) ) ;
#15094=CARTESIAN_POINT ( 'NONE',  ( 41.08683558286960391, -44.27600910371930354, -3.799114098081400215 ) ) ;
#15095=CARTESIAN_POINT ( 'NONE',  ( 65.46029542295769943, -1.463538230407920082, -16.55376543218019947 ) ) ;
#15096=CARTESIAN_POINT ( 'NONE',  ( -11.32734370190460105, 10.64934056395049922, -6.430192534648650593 ) ) ;
#15099=CARTESIAN_POINT ( 'NONE',  ( 16.13393739769620083, -15.61618894467929941, -17.89999999999999858 ) ) ;
#15103=CARTESIAN_POINT ( 'NONE',  ( 57.37957920624790376, 19.37952914044570107, -53.76443781220810791 ) ) ;
#15104=B_SPLINE_CURVE_WITH_KNOTS ( 'NONE', 3,
 ( #14469, #10808, #18143, #34108, #30441, #50635, #27035, #50119 ),
 .UNSPECIFIED., .F., .F.,
 ( 4, 2, 2, 4 ),
 ( 0.5000013127411032654, 0.6249999999792921201, 0.8249999999903363523, 1.000000000000000000 ),
 .UNSPECIFIED. ) ;
#15108=CARTESIAN_POINT ( 'NONE',  ( 15.67956920600530069, 19.63025757447420006, -20.20255632743559815 ) ) ;
#15110=CARTESIAN_POINT ( 'NONE',  ( 12.16981616251349863, 18.81688478108560147, -21.14999999999999858 ) ) ;
#15112=CARTESIAN_POINT ( 'NONE',  ( 47.87513792687950342, -54.38076868848589385, -54.78262502738859752 ) ) ;
#15113=DIRECTION ( 'NONE',  ( -0.7288689868556628149, -0.6846531968814575375, 0.000000000000000000 ) ) ;
#15114=CARTESIAN_POINT ( 'NONE',  ( 56.36079227718369822, 19.32759065149559774, -52.89779386132410366 ) ) ;
#15117=ORIENTED_EDGE ( 'NONE', *, *, #45984, .F. ) ;
#15120=ORIENTED_EDGE ( 'NONE', *, *, #30844, .F. ) ;
#15125=CARTESIAN_POINT ( 'NONE',  ( 14.34417029198879945, -51.11618894467930119, -74.14999999999999147 ) ) ;
#15126=CARTESIAN_POINT ( 'NONE',  ( 69.63393739769620083, -43.11618894467930119, -73.25000000000000000 ) ) ;
#15129=DIRECTION ( 'NONE',  ( -0.2169304578186569410, 0.000000000000000000, 0.9761870601839526262 ) ) ;
#15132=B_SPLINE_SURFACE_WITH_KNOTS ( 'NONE', 3, 3, ( 
 ( #35982, #24680, #20498, #28625, #51720, #24159, #11902, #36489, #16329, #39929, #12670, #24420, #36234, #44369, #32801, #4526 ),
 ( #16579, #48303, #40432, #40181, #23904, #32533, #4027, #12400, #40693, #23654, #43608, #4274, #44624, #594, #11638, #8730 ),
 ( #20761, #4793, #19743, #343, #43858, #16853, #7955, #19987, #48564, #16072, #100, #15813, #36748, #858, #27602, #7711 ),
 ( #39669, #20244, #8474, #3777, #35736, #24939, #37022, #5584, #13956, #12931, #13703, #28887, #21800, #44889, #49352, #33337 ),
 ( #1901, #8994, #13198, #40951, #49865, #41730, #21023, #5064, #9517, #29147, #45667, #2159, #29913, #48827, #21538, #17369 ),
 ( #45932, #1120, #37535, #13452, #37284, #25463, #18139, #45148, #17117, #17630, #33069, #49096, #29661, #6097, #33599, #29410 ),
 ( #22052, #9259, #5835, #25207, #41213, #45411, #41469, #10021, #5325, #21278, #1382, #1641, #49613, #9769, #25721, #25984 ),
 ( #41998, #37806, #38064, #17879, #33849, #14466, #30182, #34103, #46201, #15249, #14728, #34890, #2936, #39104, #6609, #47231 ),
 ( #51153, #22312, #30699, #34368, #7133, #38848, #10548, #35148, #46979, #6877, #14983, #3458, #27030, #19169, #3196, #18907 ) ),
 .UNSPECIFIED., .F., .F., .F.,
 ( 4, 1, 1, 1, 1, 1, 4 ),
 ( 4, 2, 2, 2, 2, 2, 2, 4 ),
 ( 0.000000000000000000, 0.1666666666666670182, 0.3333333333333329818, 0.5000000000000000000, 0.6666666666666670737, 0.8333333333333330373, 1.000000005975759887 ),
 ( -11.87104306964520006, -9.393165086804188491, -7.415090133440680020, -5.929772490031120391, -5.187113668326339244, -3.998859553598700156, -2.097652970034459941, 0.01149808360710800025 ),
 .UNSPECIFIED. ) ;
#15133=VERTEX_POINT ( 'NONE', #2957 ) ;
#15136=EDGE_LOOP ( 'NONE', ( #6393, #20490, #1534, #1838, #2845 ) ) ;
#15140=CARTESIAN_POINT ( 'NONE',  ( 11.91942152901519947, -65.30442633750028847, -47.17797789126349528 ) ) ;
#15143=CARTESIAN_POINT ( 'NONE',  ( 16.13393739769620083, -15.61618894467929941, 5.729250452415290518 ) ) ;
#15147=CARTESIAN_POINT ( 'NONE',  ( 62.35336129981750020, -0.9719900955148390587, -16.24009828415930201 ) ) ;
#15148=CARTESIAN_POINT ( 'NONE',  ( 51.68242196786739839, -49.02157941676630060, -76.95384497480380048 ) ) ;
#15152=CARTESIAN_POINT ( 'NONE',  ( 61.13393739769620083, 1.883811055320649963, -84.38499399519520239 ) ) ;
#15154=CARTESIAN_POINT ( 'NONE',  ( 57.08228080684060046, -47.57523781541689800, -48.30570546696120005 ) ) ;
#15156=CARTESIAN_POINT ( 'NONE',  ( 13.75402769379000034, -50.28666754275069906, -20.97890654100260122 ) ) ;
#15157=CARTESIAN_POINT ( 'NONE',  ( 55.44813972691670045, 19.38381105532069881, -76.34352098789580054 ) ) ;
#15158=EDGE_CURVE ( 'NONE', #10936, #30581, #24286, .T. ) ;
#15160=CARTESIAN_POINT ( 'NONE',  ( 56.55949779134230226, 13.95391148746589849, -16.30411193604290077 ) ) ;
#15162=B_SPLINE_CURVE_WITH_KNOTS ( 'NONE', 3,
 ( #10009, #2145, #50367, #41713, #13689, #42507, #17359, #21528, #49849, #5822 ),
 .UNSPECIFIED., .F., .F.,
 ( 4, 2, 2, 2, 4 ),
 ( 0.000000000000000000, 0.1774999999982775079, 0.3374999999967193687, 0.4374999999957477348, 0.4999999271596042849 ),
 .UNSPECIFIED. ) ;
#15164=AXIS2_PLACEMENT_3D ( 'NONE', #18484, #22401, #34459 ) ;
#15168=ORIENTED_EDGE ( 'NONE', *, *, #9913, .F. ) ;
#15169=CARTESIAN_POINT ( 'NONE',  ( 14.13832835820899980, -51.13035289118570148, -74.36013246831049628 ) ) ;
#15171=CARTESIAN_POINT ( 'NONE',  ( 44.98351815555930244, -46.11094773564500571, -8.963066483085869507 ) ) ;
#15172=CARTESIAN_POINT ( 'NONE',  ( 54.86079194568145567, -47.84550249862039095, -26.65937158387647798 ) ) ;
#15174=DIRECTION ( 'NONE',  ( 0.3294064756441309472, 0.9441882088883087887, -3.053113317719179500E-16 ) ) ;
#15175=CARTESIAN_POINT ( 'NONE',  ( 82.46546147468319532, 13.86078240809950124, -46.44239936464539653 ) ) ;
#15176=CARTESIAN_POINT ( 'NONE',  ( 10.61751707702059910, 33.59325229219749787, -22.25048313876769868 ) ) ;
#15177=CARTESIAN_POINT ( 'NONE',  ( 47.48065465286614284, 23.09789386337090633, -75.12259495334244264 ) ) ;
#15180=CARTESIAN_POINT ( 'NONE',  ( 49.54598800151349991, 22.37956328914630078, -54.50101998263440350 ) ) ;
#15181=ORIENTED_EDGE ( 'NONE', *, *, #13792, .T. ) ;
#15182=CARTESIAN_POINT ( 'NONE',  ( 52.67442042553170012, -49.76228255682879364, -48.55745968341410190 ) ) ;
#15183=ORIENTED_EDGE ( 'NONE', *, *, #28118, .T. ) ;
#15186=CARTESIAN_POINT ( 'NONE',  ( 13.51721710176069813, 20.04444091306159947, -22.28354745645999913 ) ) ;
#15189=CARTESIAN_POINT ( 'NONE',  ( 52.78885562451659297, 18.47641143109279938, -48.87892841330330640 ) ) ;
#15190=CARTESIAN_POINT ( 'NONE',  ( 54.72151381108420765, -45.94167981062680184, -15.73273755979830213 ) ) ;
#15191=LINE ( 'NONE', #31152, #40705 ) ;
#15193=ADVANCED_FACE ( 'NONE', ( #19951 ), #51684, .F. ) ;
#15195=ORIENTED_EDGE ( 'NONE', *, *, #42419, .F. ) ;
#15197=CARTESIAN_POINT ( 'NONE',  ( 11.93174564592020026, -65.43929186371940432, -17.93019396377230024 ) ) ;
#15198=CARTESIAN_POINT ( 'NONE',  ( 9.548543281838000496, 32.54799942213450237, -46.53732641210050502 ) ) ;
#15202=CARTESIAN_POINT ( 'NONE',  ( 53.51280994016380532, -49.43204902681937796, -49.22146059094290393 ) ) ;
#15203=EDGE_CURVE ( 'NONE', #17902, #7053, #5881, .T. ) ;
#15207=CARTESIAN_POINT ( 'NONE',  ( 53.06587257203489827, -52.00459370491639532, -53.44894298165189639 ) ) ;
#15208=EDGE_CURVE ( 'NONE', #7609, #39844, #38890, .T. ) ;
#15211=CARTESIAN_POINT ( 'NONE',  ( 10.77236125395059929, -63.28329410503849317, -45.20487655624160084 ) ) ;
#15212=CARTESIAN_POINT ( 'NONE',  ( 69.22748654599826068, 19.47158195952029303, -72.59354914830210248 ) ) ;
#15213=ORIENTED_EDGE ( 'NONE', *, *, #32495, .T. ) ;
#15215=DIRECTION ( 'NONE',  ( -0.2517544074889990768, 0.9677911542837447367, 0.000000000000000000 ) ) ;
#15219=LINE ( 'NONE', #23302, #40106 ) ;
#15220=CARTESIAN_POINT ( 'NONE',  ( 82.45630311851421368, 13.86034003618500066, -46.38988467804559690 ) ) ;
#15227=VERTEX_POINT ( 'NONE', #31480 ) ;
#15229=ORIENTED_EDGE ( 'NONE', *, *, #46274, .T. ) ;
#15230=CARTESIAN_POINT ( 'NONE',  ( 43.60412366894710345, -43.70472620657429985, -5.064848484333539957 ) ) ;
#15234=CARTESIAN_POINT ( 'NONE',  ( 47.37032930261479891, 23.44277967668870133, -74.17365615959539582 ) ) ;
#15235=CARTESIAN_POINT ( 'NONE',  ( 45.07858682377059978, -46.11248607424209922, -9.026855431852869316 ) ) ;
#15236=DIRECTION ( 'NONE',  ( -0.6377178376951687655, 0.7702700562045746713, -4.336808689942011820E-16 ) ) ;
#15239=CARTESIAN_POINT ( 'NONE',  ( 12.14266246862359999, 33.62769506002970132, -16.13799733647190138 ) ) ;
#15242=CARTESIAN_POINT ( 'NONE',  ( 52.61516928385270120, -49.80859478947380126, -27.82854103740449858 ) ) ;
#15243=CARTESIAN_POINT ( 'NONE',  ( 56.79288265842479433, -50.66783009735559773, -74.14912528235450395 ) ) ;
#15244=CARTESIAN_POINT ( 'NONE',  ( -4.702024263459519737, 16.16474464310789827, -5.099307284078279601 ) ) ;
#15247=CARTESIAN_POINT ( 'NONE',  ( 27.73905384484250192, -53.11618894467930119, -74.14999999999999147 ) ) ;
#15249=CARTESIAN_POINT ( 'NONE',  ( -8.110719422787710187, -44.87935480251360332, -5.130695632534920669 ) ) ;
#15250=CARTESIAN_POINT ( 'NONE',  ( 47.60001556901690378, 23.30894354097369714, -54.85861573280610060 ) ) ;
#15251=CARTESIAN_POINT ( 'NONE',  ( 57.34505690168419534, -45.81270932441739774, -26.27162216713519882 ) ) ;
#15252=DIRECTION ( 'NONE',  ( -0.9486832980505123247, 1.161801964362114161E-16, 0.3162277660168421045 ) ) ;
#15253=CARTESIAN_POINT ( 'NONE',  ( 61.12214340571450322, 14.22653868544119860, -47.44127583901740053 ) ) ;
#15255=CARTESIAN_POINT ( 'NONE',  ( 52.13018002042409904, 18.64453568514510096, -76.92945343287659909 ) ) ;
#15256=CARTESIAN_POINT ( 'NONE',  ( 52.81415214587489970, 18.43716763046850105, -48.60514635218409296 ) ) ;
#15258=CARTESIAN_POINT ( 'NONE',  ( 52.82975622904280755, -49.66092049964720445, -48.48626292588439668 ) ) ;
#15259=CARTESIAN_POINT ( 'NONE',  ( 54.94524618045259956, 16.46847369675259642, -26.58277649024360301 ) ) ;
#15260=CARTESIAN_POINT ( 'NONE',  ( 16.13393739769620083, -15.61618894467929941, 4.450000000000000178 ) ) ;
#15262=CARTESIAN_POINT ( 'NONE',  ( 8.815605938724019097, -63.28267558148569094, -46.67186391142220003 ) ) ;
#15263=CARTESIAN_POINT ( 'NONE',  ( 42.78018059643970616, 11.47668021806869909, -3.187564294433590462 ) ) ;
#15264=CARTESIAN_POINT ( 'NONE',  ( 64.56161859372949152, -31.20701609037800139, -16.82687391434760116 ) ) ;
#15267=CARTESIAN_POINT ( 'NONE',  ( 11.13393739769619906, 32.06972070065159386, -43.74696042565229703 ) ) ;
#15269=CARTESIAN_POINT ( 'NONE',  ( 51.40028038159698553, -34.49096119182996745, -76.69282701588583961 ) ) ;
#15271=CARTESIAN_POINT ( 'NONE',  ( 61.28610861176739633, -45.23040055550220018, -28.15000000000000213 ) ) ;
#15273=ORIENTED_EDGE ( 'NONE', *, *, #14135, .T. ) ;
#15274=CARTESIAN_POINT ( 'NONE',  ( 56.66762828431429710, 19.14715517649329968, -52.77094437924129977 ) ) ;
#15275=CARTESIAN_POINT ( 'NONE',  ( 49.88572956512600598, -29.68138763751254672, -15.90126589776440902 ) ) ;
#15277=CARTESIAN_POINT ( 'NONE',  ( 55.96457922517269878, -45.97039086805419572, -25.73835096114130039 ) ) ;
#15281=CIRCLE ( 'NONE', #16116, 20.00000000000001421 ) ;
#15282=CARTESIAN_POINT ( 'NONE',  ( 11.11663740960502977, 33.77554069907087353, -23.06313725433601647 ) ) ;
#15284=CARTESIAN_POINT ( 'NONE',  ( 11.00910675228320024, 32.24153982397250218, -24.02516935458699976 ) ) ;
#15285=ORIENTED_EDGE ( 'NONE', *, *, #46532, .F. ) ;
#15286=CARTESIAN_POINT ( 'NONE',  ( 55.00894648611440374, -45.11618894467940066, -13.91245063309409957 ) ) ;
#15287=CARTESIAN_POINT ( 'NONE',  ( 51.23914035111342713, 0.5199290082084727649, -17.21756640535365790 ) ) ;
#15288=CARTESIAN_POINT ( 'NONE',  ( 10.64977475916229999, 33.62388472332079914, -18.05902683574160150 ) ) ;
#15290=CARTESIAN_POINT ( 'NONE',  ( 59.85171547485399657, -28.82033292544180014, -15.75458271846640024 ) ) ;
#15292=CARTESIAN_POINT ( 'NONE',  ( 46.84316060478769828, -53.76087950960219786, -75.90467361879859709 ) ) ;
#15295=CARTESIAN_POINT ( 'NONE',  ( 41.01789762497119796, 13.77558802515430081, -5.564947099249000217 ) ) ;
#15296=DIRECTION ( 'NONE',  ( -0.4439767838697923907, -0.8960382890170686121, 0.000000000000000000 ) ) ;
#15297=CARTESIAN_POINT ( 'NONE',  ( 84.44784216359251161, -43.11618894467930119, -47.47585302082339354 ) ) ;
#15298=CARTESIAN_POINT ( 'NONE',  ( 11.49541412066449375, 34.11692877646753175, -17.78290583436891836 ) ) ;
#15302=CARTESIAN_POINT ( 'NONE',  ( 54.62083344167059806, -48.06803323320840349, -26.73900343537430047 ) ) ;
#15303=EDGE_CURVE ( 'NONE', #47835, #35625, #49463, .T. ) ;
#15304=CARTESIAN_POINT ( 'NONE',  ( 0.4116173174696240444, -53.57266544184560075, -8.235445646974270062 ) ) ;
#15305=CARTESIAN_POINT ( 'NONE',  ( 76.15791883449350053, -14.05836797832549934, -12.10556864792070009 ) ) ;
#15306=CARTESIAN_POINT ( 'NONE',  ( 75.39077318432113373, 12.99911917340609513, -13.71505546934280417 ) ) ;
#15307=B_SPLINE_CURVE_WITH_KNOTS ( 'NONE', 3,
 ( #51672, #3722, #3207, #34901, #19941, #31719, #47240, #15515, #31469, #48000, #47744, #50900, #35931, #46990, #11075, #7395, #7658, #11589, #43046, #23344, #7142, #27550, #19178, #43557, #35157, #23601, #39366, #27808, #15258, #19439 ),
 .UNSPECIFIED., .F., .F.,
 ( 4, 2, 2, 2, 2, 2, 2, 2, 2, 2, 2, 2, 2, 2, 4 ),
 ( 0.000000000000000000, 0.09071737296906999537, 0.2140426870042120011, 0.2911210082761760409, 0.3773790848024499711, 0.4312903826313709832, 0.4852016804602920508, 0.5283307187234289604, 0.5714597569865670357, 0.6404662182075859800, 0.6753556120789150352, 0.7102450059502449786, 0.7544326870336059976, 0.8251329767669829396, 0.8625807652627419664 ),
 .UNSPECIFIED. ) ;
#15308=CARTESIAN_POINT ( 'NONE',  ( 12.44378449474779913, -49.98269640123930202, -21.13285771871539964 ) ) ;
#15309=DIRECTION ( 'NONE',  ( 0.000000000000000000, 0.000000000000000000, -1.000000000000000000 ) ) ;
#15312=CARTESIAN_POINT ( 'NONE',  ( 82.36128958404080436, -45.10908765980170188, -46.45434936409679949 ) ) ;
#15313=CARTESIAN_POINT ( 'NONE',  ( 57.39005023914570103, -50.59266058909979336, -53.60531501353280248 ) ) ;
#15314=CARTESIAN_POINT ( 'NONE',  ( 43.27773194996530037, 11.67331461295569994, -4.515873930613719445 ) ) ;
#15317=CARTESIAN_POINT ( 'NONE',  ( 59.42623547831379938, -46.20484020020990101, -47.44643030202959721 ) ) ;
#15318=CARTESIAN_POINT ( 'NONE',  ( 70.83393739769719843, -48.11618894467220287, -73.25000000000000000 ) ) ;
#15320=CARTESIAN_POINT ( 'NONE',  ( 18.43159307031459804, -52.07648608105650112, -75.48775473117470369 ) ) ;
#15321=CARTESIAN_POINT ( 'NONE',  ( 51.07994173643560032, -52.78781467787970882, -53.74568964421160189 ) ) ;
#15322=EDGE_CURVE ( 'NONE', #26340, #4326, #32631, .T. ) ;
#15326=VERTEX_POINT ( 'NONE', #31417 ) ;
#15327=DIRECTION ( 'NONE',  ( -1.000000000000000000, 0.000000000000000000, 0.000000000000000000 ) ) ;
#15332=CARTESIAN_POINT ( 'NONE',  ( 43.08927530004059747, -45.90404663275549524, -7.588629812463259405 ) ) ;
#15333=ADVANCED_FACE ( 'NONE', ( #39066 ), #3158, .T. ) ;
#15334=VERTEX_POINT ( 'NONE', #11540 ) ;
#15335=CARTESIAN_POINT ( 'NONE',  ( 17.59779143982609639, 21.21781726285519909, -76.03742712147929694 ) ) ;
#15338=ORIENTED_EDGE ( 'NONE', *, *, #20418, .T. ) ;
#15341=CARTESIAN_POINT ( 'NONE',  ( 71.71126032029680175, -45.25223929932899125, -47.09707863094710945 ) ) ;
#15349=ORIENTED_EDGE ( 'NONE', *, *, #36092, .F. ) ;
#15352=CARTESIAN_POINT ( 'NONE',  ( 52.01748110390389712, -51.11128007685600494, -76.09025191383899767 ) ) ;
#15353=CARTESIAN_POINT ( 'NONE',  ( 60.32372535534909730, 14.61230269747050059, -47.67141866289379948 ) ) ;
#15356=CARTESIAN_POINT ( 'NONE',  ( -3.258131835852990044, 17.22944021436429907, -5.041088719362160298 ) ) ;
#15357=CARTESIAN_POINT ( 'NONE',  ( 47.03254412713606314, 23.23399685673784631, -75.29848680170620412 ) ) ;
#15358=CARTESIAN_POINT ( 'NONE',  ( 33.53393739769619231, -15.61618894538776559, -7.049999999999999822 ) ) ;
#15361=EDGE_LOOP ( 'NONE', ( #4430, #45696, #20795, #44347, #15004 ) ) ;
#15362=CARTESIAN_POINT ( 'NONE',  ( 57.26570439199549867, 16.10442508092609870, -47.75313496841199878 ) ) ;
#15364=AXIS2_PLACEMENT_3D ( 'NONE', #39552, #27989, #23789 ) ;
#15365=DIRECTION ( 'NONE',  ( 0.000000000000000000, 0.000000000000000000, 1.000000000000000000 ) ) ;
#15367=EDGE_CURVE ( 'NONE', #19986, #44502, #32964, .T. ) ;
#15369=CARTESIAN_POINT ( 'NONE',  ( 15.00539844365889941, 19.69078932486479871, -21.20430891277120011 ) ) ;
#15370=DIRECTION ( 'NONE',  ( 0.000000000000000000, -1.000000000000000000, 0.000000000000000000 ) ) ;
#15372=CARTESIAN_POINT ( 'NONE',  ( 61.50409964636570237, 14.14168666559669951, -47.35437808293550432 ) ) ;
#15373=CARTESIAN_POINT ( 'NONE',  ( 48.30764984760519809, -54.18332414096600047, -54.81566210031060393 ) ) ;
#15374=PLANE ( 'NONE',  #33955 ) ;
#15376=CARTESIAN_POINT ( 'NONE',  ( 47.82941845642289991, 23.15673897679920046, -54.71834399002119653 ) ) ;
#15380=VECTOR ( 'NONE', #27963, 1000.000000000000000 ) ;
#15382=CARTESIAN_POINT ( 'NONE',  ( 17.82929433848870104, 21.38896804161856124, -76.01806011806066010 ) ) ;
#15383=CARTESIAN_POINT ( 'NONE',  ( 60.37123110817940130, -45.73378107691389971, -47.43125510679269752 ) ) ;
#15384=CARTESIAN_POINT ( 'NONE',  ( 53.41693480158270546, -49.35328119387190071, -48.75416851881869462 ) ) ;
#15385=LINE ( 'NONE', #11715, #1835 ) ;
#15386=CARTESIAN_POINT ( 'NONE',  ( 83.34325726105171839, 14.07779472782969954, -47.50551966704799867 ) ) ;
#15387=PLANE ( 'NONE',  #27278 ) ;
#15389=CARTESIAN_POINT ( 'NONE',  ( 16.13393739769620083, -15.61618894467929941, 8.349999999999999645 ) ) ;
#15390=EDGE_CURVE ( 'NONE', #39228, #5583, #35162, .T. ) ;
#15392=DIRECTION ( 'NONE',  ( 0.2169304578186566079, 0.000000000000000000, -0.9761870601839527373 ) ) ;
#15396=CARTESIAN_POINT ( 'NONE',  ( 12.96406378517139935, 34.28324915654220462, -47.66759396690779482 ) ) ;
#15397=CARTESIAN_POINT ( 'NONE',  ( 10.41800581969009976, -64.65214231680860735, -46.79321165223139900 ) ) ;
#15398=ORIENTED_EDGE ( 'NONE', *, *, #8583, .F. ) ;
#15402=CARTESIAN_POINT ( 'NONE',  ( 56.45988984176000258, -50.72305344967870155, -53.39311493514949802 ) ) ;
#15404=B_SPLINE_CURVE_WITH_KNOTS ( 'NONE', 3,
 ( #38593, #50386, #22058, #22318, #46464, #42525, #10552, #30188 ),
 .UNSPECIFIED., .F., .F.,
 ( 4, 2, 2, 4 ),
 ( 0.000000000000000000, 0.3098045115950139317, 0.9301223358193300150, 1.000000000000000000 ),
 .UNSPECIFIED. ) ;
#15406=CARTESIAN_POINT ( 'NONE',  ( 65.32687762751260152, -0.2389500108568909931, -16.78952551121680159 ) ) ;
#15407=CARTESIAN_POINT ( 'NONE',  ( 51.67588111593500599, -48.61618684213020458, -77.01364305260700860 ) ) ;
#15408=B_SPLINE_CURVE_WITH_KNOTS ( 'NONE', 3,
 ( #4387, #20355, #48951, #13052, #36342 ),
 .UNSPECIFIED., .F., .F.,
 ( 4, 1, 4 ),
 ( 0.000000000000000000, 0.5000000000000000000, 1.000000000000000000 ),
 .UNSPECIFIED. ) ;
#15409=CARTESIAN_POINT ( 'NONE',  ( 14.07181180123552267, -52.32662977626135614, -75.76245441612901743 ) ) ;
#15410=( BOUNDED_CURVE ( )  B_SPLINE_CURVE ( 2, ( #21283, #37288, #865, #40187, #37027 ),
 .UNSPECIFIED., .F., .T. ) 
 B_SPLINE_CURVE_WITH_KNOTS ( ( 3, 2, 3 ),
 ( -0.003205554299145560102, 0.8238407534178779912, 1.650887061134900025 ),
 .UNSPECIFIED. ) 
 CURVE ( )  GEOMETRIC_REPRESENTATION_ITEM ( )  RATIONAL_B_SPLINE_CURVE ( ( 1.000000000000000000, 0.9157107718028779653, 1.000000000000000000, 0.9157107718028449916, 1.000000000000000000 ) ) 
 REPRESENTATION_ITEM ( '' )  );
#15411=ORIENTED_EDGE ( 'NONE', *, *, #1757, .T. ) ;
#15415=DIRECTION ( 'NONE',  ( 0.000000000000000000, -1.000000000000000000, 0.000000000000000000 ) ) ;
#15417=CARTESIAN_POINT ( 'NONE',  ( 12.27824370503449991, -50.15233315604800168, -21.14999999870460101 ) ) ;
#15418=CARTESIAN_POINT ( 'NONE',  ( 56.85087055762509323, 19.38381105532069881, -75.22080214333730908 ) ) ;
#15421=CARTESIAN_POINT ( 'NONE',  ( 56.50061855791859955, 14.14892826505740153, -17.93020493892149858 ) ) ;
#15422=CARTESIAN_POINT ( 'NONE',  ( 60.77439903042079550, -45.49849954229439675, -47.09774554394410018 ) ) ;
#15424=CARTESIAN_POINT ( 'NONE',  ( 56.62432785517169975, -50.71560893929619596, -53.83726655417689955 ) ) ;
#15429=CARTESIAN_POINT ( 'NONE',  ( 13.76101809997250136, -51.29511715723850074, -74.14992839339309683 ) ) ;
#15430=EDGE_CURVE ( 'NONE', #17080, #47621, #10751, .T. ) ;
#15433=CARTESIAN_POINT ( 'NONE',  ( 17.92370450339619836, 19.88381105532299742, -74.14999999999999147 ) ) ;
#15435=CARTESIAN_POINT ( 'NONE',  ( 47.20372080753160304, -53.97904105312669287, -75.66073271794819277 ) ) ;
#15436=CARTESIAN_POINT ( 'NONE',  ( 11.89433743672330124, 34.20374474164479750, -18.12680249707489821 ) ) ;
#15441=CARTESIAN_POINT ( 'NONE',  ( 5.758805994657699934, -59.74572380576150010, -13.93820318808900005 ) ) ;
#15442=CARTESIAN_POINT ( 'NONE',  ( 49.36944273108730386, 22.50304657733999747, -54.70700368065020314 ) ) ;
#15444=CARTESIAN_POINT ( 'NONE',  ( 52.78885568635549674, -49.70878928925869644, -48.87892847977669675 ) ) ;
#15445=ORIENTED_EDGE ( 'NONE', *, *, #27139, .T. ) ;
#15447=LINE ( 'NONE', #24824, #21840 ) ;
#15448=CARTESIAN_POINT ( 'NONE',  ( 11.90611060580384084, 34.20474548859955632, -18.00436963405675428 ) ) ;
#15452=CARTESIAN_POINT ( 'NONE',  ( 55.58072258071959482, -45.98463045567079632, -16.80393901860190198 ) ) ;
#15453=ADVANCED_FACE ( 'NONE', ( #20659 ), #55, .T. ) ;
#15454=CARTESIAN_POINT ( 'NONE',  ( 16.65420337844999921, -51.11618894467930119, -20.15000000000000213 ) ) ;
#15455=ORIENTED_EDGE ( 'NONE', *, *, #33862, .F. ) ;
#15458=EDGE_CURVE ( 'NONE', #17902, #19884, #5924, .T. ) ;
#15460=CARTESIAN_POINT ( 'NONE',  ( 11.74995130100939988, -65.25618184072669692, -17.00864122140729862 ) ) ;
#15461=CARTESIAN_POINT ( 'NONE',  ( 10.41478454943800003, 33.42186449018819872, -46.79156209876850170 ) ) ;
#15463=CARTESIAN_POINT ( 'NONE',  ( 50.10014236208279215, -52.83395586467779736, -53.32348334894899722 ) ) ;
#15464=DIRECTION ( 'NONE',  ( -0.4872913772396108012, -0.8732394366197184787, 0.000000000000000000 ) ) ;
#15465=DIRECTION ( 'NONE',  ( 0.3294064756441278941, 0.9441882088883097879, 0.000000000000000000 ) ) ;
#15466=ORIENTED_EDGE ( 'NONE', *, *, #7052, .F. ) ;
#15468=CARTESIAN_POINT ( 'NONE',  ( 11.13393739769619906, -63.11543068638779630, -43.91250110351749925 ) ) ;
#15469=CARTESIAN_POINT ( 'NONE',  ( 65.43042069958036677, 17.98087126525108914, -68.79648330188406646 ) ) ;
#15472=CARTESIAN_POINT ( 'NONE',  ( 56.72051766552240082, 19.45439143119729763, -53.84018978621849527 ) ) ;
#15473=CARTESIAN_POINT ( 'NONE',  ( 20.13393739768839552, 24.18330853958629945, -74.14999999999999147 ) ) ;
#15477=CARTESIAN_POINT ( 'NONE',  ( 14.72165982897219116, 20.94681317766939443, -75.92929758211541014 ) ) ;
#15478=CARTESIAN_POINT ( 'NONE',  ( 83.89200044194980421, 19.38381105532069881, -53.92796738110899923 ) ) ;
#15485=VERTEX_POINT ( 'NONE', #13100 ) ;
#15486=CARTESIAN_POINT ( 'NONE',  ( 43.75992007188810362, -43.62559376723620375, -5.076600545282080823 ) ) ;
#15488=CARTESIAN_POINT ( 'NONE',  ( 46.03121500769550067, 13.88381105532070059, -7.582874790343590021 ) ) ;
#15490=CARTESIAN_POINT ( 'NONE',  ( 46.96102914747190482, 22.94339939543869988, -75.61154402005681163 ) ) ;
#15491=EDGE_CURVE ( 'NONE', #121, #48001, #46966, .T. ) ;
#15492=AXIS2_PLACEMENT_3D ( 'NONE', #39728, #48108, #151 ) ;
#15495=CARTESIAN_POINT ( 'NONE',  ( 11.74347662707550022, 33.65273995683249808, -16.31133514116600125 ) ) ;
#15498=CARTESIAN_POINT ( 'NONE',  ( 53.25888871246099399, -49.10877824327850050, -26.73652702851729757 ) ) ;
#15499=CARTESIAN_POINT ( 'NONE',  ( 55.87190314012450187, -50.61618894623149600, -76.15909243498199999 ) ) ;
#15501=CARTESIAN_POINT ( 'NONE',  ( -0.7705598404263119816, 21.64162338028269872, -8.889730355579660070 ) ) ;
#15502=CARTESIAN_POINT ( 'NONE',  ( 10.90462376991689197, -55.27285976101147469, -44.90618179855681547 ) ) ;
#15504=FACE_OUTER_BOUND ( 'NONE', #28728, .T. ) ;
#15505=EDGE_LOOP ( 'NONE', ( #10635, #37882, #5376, #15903 ) ) ;
#15506=CARTESIAN_POINT ( 'NONE',  ( 52.81743982411089888, -49.66737340927319622, -48.47378032971909789 ) ) ;
#15507=CARTESIAN_POINT ( 'NONE',  ( 47.64197321496929760, 23.30135080481779752, -55.08764324752890218 ) ) ;
#15508=CARTESIAN_POINT ( 'NONE',  ( 58.56772413253199971, -45.48424304623870285, -26.36790636083469863 ) ) ;
#15510=CARTESIAN_POINT ( 'NONE',  ( 61.54546893286627096, -45.33071755016126758, -47.27434214225175424 ) ) ;
#15512=CARTESIAN_POINT ( 'NONE',  ( 51.94901983112990251, 18.29135666841079910, -77.02691475221409689 ) ) ;
#15513=CARTESIAN_POINT ( 'NONE',  ( 53.00383623833999991, 18.33733721602849798, -48.79311473309799396 ) ) ;
#15515=CARTESIAN_POINT ( 'NONE',  ( 53.13663702127480093, -49.50013705438340139, -48.80285956223989530 ) ) ;
#15516=CARTESIAN_POINT ( 'NONE',  ( 50.10204865863599366, 22.25438125613730023, -54.90071668138480732 ) ) ;
#15517=EDGE_CURVE ( 'NONE', #44163, #14960, #19892, .T. ) ;
#15519=CARTESIAN_POINT ( 'NONE',  ( 53.36049947297766494, -49.20080844630853534, -27.35403009910411498 ) ) ;
#15522=CARTESIAN_POINT ( 'NONE',  ( 64.49515523001039696, -31.53426064655560168, -17.03999220943040172 ) ) ;
#15524=CARTESIAN_POINT ( 'NONE',  ( 11.13393739769619906, 32.19619796063980033, -43.75331349279139914 ) ) ;
#15527=CARTESIAN_POINT ( 'NONE',  ( 61.28610861988966718, -45.23040055124666736, -28.05484073064822326 ) ) ;
#15531=CARTESIAN_POINT ( 'NONE',  ( 55.55365133010059964, -45.11618894467940066, -14.32025150907159983 ) ) ;
#15532=ORIENTED_EDGE ( 'NONE', *, *, #2345, .T. ) ;
#15533=CARTESIAN_POINT ( 'NONE',  ( 12.17133881455110078, -65.27733590913939565, -46.10644673425740336 ) ) ;
#15534=DIRECTION ( 'NONE',  ( 0.3294064756440925335, -0.9441882088883222224, -3.330669073875471100E-16 ) ) ;
#15535=PLANE ( 'NONE',  #51261 ) ;
#15536=DIRECTION ( 'NONE',  ( 0.000000000000000000, -1.000000000000000000, 0.000000000000000000 ) ) ;
#15540=CARTESIAN_POINT ( 'NONE',  ( 11.60842185034129947, 33.48988549690440664, -24.06199962910709900 ) ) ;
#15546=CARTESIAN_POINT ( 'NONE',  ( 64.11006012897030359, -29.74545742325380360, -16.36070032634080107 ) ) ;
#15548=CARTESIAN_POINT ( 'NONE',  ( 47.11430437939870330, -54.02739288645709337, -75.65564156953989539 ) ) ;
#15550=FACE_OUTER_BOUND ( 'NONE', #35122, .T. ) ;
#15552=CARTESIAN_POINT ( 'NONE',  ( 42.05083776483330382, 14.02818861621179991, -6.331737915367179781 ) ) ;
#15553=CIRCLE ( 'NONE', #33932, 49.07571608970680188 ) ;
#15555=CARTESIAN_POINT ( 'NONE',  ( 15.05440318628110141, 21.88381105532300097, -76.14999999999999147 ) ) ;
#15556=ADVANCED_FACE ( 'NONE', ( #29842 ), #51073, .F. ) ;
#15557=EDGE_CURVE ( 'NONE', #4775, #51752, #45862, .T. ) ;
#15558=CARTESIAN_POINT ( 'NONE',  ( 84.42287661217571326, -43.28755984482599928, -47.36827274406740429 ) ) ;
#15559=CARTESIAN_POINT ( 'NONE',  ( 16.13393739769620083, -15.61618894467929941, -19.14999999999999858 ) ) ;
#15560=EDGE_CURVE ( 'NONE', #33030, #1308, #10731, .T. ) ;
#15562=ORIENTED_EDGE ( 'NONE', *, *, #1431, .F. ) ;
#15563=FACE_OUTER_BOUND ( 'NONE', #30804, .T. ) ;
#15564=CARTESIAN_POINT ( 'NONE',  ( 14.18385191392540001, -50.83394888710610360, -21.44137102719459875 ) ) ;
#15565=CARTESIAN_POINT ( 'NONE',  ( 75.68173550483029999, -14.05264239439859963, -11.58966857824820096 ) ) ;
#15569=CARTESIAN_POINT ( 'NONE',  ( 47.18324198357279897, 23.57489020266570279, -54.61058319554400242 ) ) ;
#15571=CARTESIAN_POINT ( 'NONE',  ( 82.30072302861961475, -45.28580905185120287, -47.18357684934780139 ) ) ;
#15572=CARTESIAN_POINT ( 'NONE',  ( 57.36123080243149985, -50.13537922777889833, -52.61896049783310048 ) ) ;
#15573=CARTESIAN_POINT ( 'NONE',  ( 42.28714465471179551, 13.04424985412589955, -5.063832622360679991 ) ) ;
#15576=CARTESIAN_POINT ( 'NONE',  ( 53.41693480158270546, -49.35328119387190071, -48.75416851881880120 ) ) ;
#15578=CARTESIAN_POINT ( 'NONE',  ( 68.13393739769841773, -50.61618894467878960, -73.25000000000220268 ) ) ;
#15579=CARTESIAN_POINT ( 'NONE',  ( 67.33936456850589991, -1.038934691447770176, -17.45360882802740221 ) ) ;
#15580=CARTESIAN_POINT ( 'NONE',  ( 18.23140400112239945, -51.35642126253560491, -74.98719232986280758 ) ) ;
#15581=CARTESIAN_POINT ( 'NONE',  ( 41.56669578563739975, -43.85542471345180360, -4.650716833944319895 ) ) ;
#15582=EDGE_CURVE ( 'NONE', #27219, #29806, #11772, .T. ) ;
#15585=CARTESIAN_POINT ( 'NONE',  ( 49.39082779805520573, -53.49490451538980551, -54.14527087032600150 ) ) ;
#15587=DIRECTION ( 'NONE',  ( -1.224646799147353207E-16, 1.000000000000000000, 0.000000000000000000 ) ) ;
#15594=CARTESIAN_POINT ( 'NONE',  ( 18.22113377645400334, 20.91311638024189890, -75.69337827730609547 ) ) ;
#15596=VERTEX_POINT ( 'NONE', #51593 ) ;
#15597=ORIENTED_EDGE ( 'NONE', *, *, #34452, .F. ) ;
#15598=CARTESIAN_POINT ( 'NONE',  ( 56.75109370957449784, -45.11618894467940066, -15.55230934101460072 ) ) ;
#15600=CARTESIAN_POINT ( 'NONE',  ( 61.70952355081560370, 13.92643276180479894, -46.78415134525790364 ) ) ;
#15602=ORIENTED_EDGE ( 'NONE', *, *, #13673, .F. ) ;
#15606=CARTESIAN_POINT ( 'NONE',  ( 54.17308944977700236, 19.38381105532069881, -77.01198594365929750 ) ) ;
#15609=CARTESIAN_POINT ( 'NONE',  ( 52.31626067747389897, -50.93885350010000224, -76.18456440015900455 ) ) ;
#15610=CARTESIAN_POINT ( 'NONE',  ( 60.53374381014149463, 14.50344111463789787, -47.62958190853139939 ) ) ;
#15614=CARTESIAN_POINT ( 'NONE',  ( -4.949082834145499987, 16.40845028330949873, -5.527623173694479419 ) ) ;
#15617=DIRECTION ( 'NONE',  ( 1.000000000000000000, 0.000000000000000000, 0.000000000000000000 ) ) ;
#15622=DIRECTION ( 'NONE',  ( -1.000000000000000000, 0.000000000000000000, 0.000000000000000000 ) ) ;
#15623=DIRECTION ( 'NONE',  ( -0.8090169943749474513, -0.5877852522924732481, 0.000000000000000000 ) ) ;
#15628=CARTESIAN_POINT ( 'NONE',  ( 12.98727014170039951, 18.78214033880969680, -21.05372677356080047 ) ) ;
#15630=CARTESIAN_POINT ( 'NONE',  ( 48.29783768768939467, -54.14418088742089452, -54.68165175005749745 ) ) ;
#15631=DIRECTION ( 'NONE',  ( 0.000000000000000000, -1.000000000000000000, 0.000000000000000000 ) ) ;
#15633=CARTESIAN_POINT ( 'NONE',  ( 47.73411684492059948, 23.25915219497479924, -55.05916737018710450 ) ) ;
#15639=CARTESIAN_POINT ( 'NONE',  ( 60.67119852934060020, -45.61627437969990240, -47.47040929001600063 ) ) ;
#15640=CARTESIAN_POINT ( 'NONE',  ( 48.08635818190295197, -54.25091888102404880, -54.70531615945150605 ) ) ;
#15641=CARTESIAN_POINT ( 'NONE',  ( 51.67587649748470113, -33.96749857170579645, -77.01363636363508647 ) ) ;
#15642=CARTESIAN_POINT ( 'NONE',  ( 16.13393740133140142, -15.61618822260889949, -4.296537984153929735 ) ) ;
#15653=CARTESIAN_POINT ( 'NONE',  ( 12.78992083550290104, -65.50145383207738803, -47.67074661757159504 ) ) ;
#15655=ORIENTED_EDGE ( 'NONE', *, *, #41294, .F. ) ;
#15656=ADVANCED_FACE ( 'NONE', ( #23522 ), #23781, .F. ) ;
#15659=EDGE_CURVE ( 'NONE', #9581, #14446, #4227, .T. ) ;
#15660=CARTESIAN_POINT ( 'NONE',  ( 56.47388559847290423, -50.68647850825969670, -53.28105505440640144 ) ) ;
#15662=CARTESIAN_POINT ( 'NONE',  ( 62.85974396480249737, -0.1941458833951940077, -16.61913982835589820 ) ) ;
#15663=CARTESIAN_POINT ( 'NONE',  ( 51.86329228654000190, -49.90667831135039734, -76.68384409933040047 ) ) ;
#15665=CARTESIAN_POINT ( 'NONE',  ( 13.92283413501615641, -52.20691909688449783, -75.61049359302393214 ) ) ;
#15668=CARTESIAN_POINT ( 'NONE',  ( 75.47966807050509885, 12.14072485751589880, -13.40512917118210012 ) ) ;
#15671=AXIS2_PLACEMENT_3D ( 'NONE', #15559, #11629, #27590 ) ;
#15672=CARTESIAN_POINT ( 'NONE',  ( 13.31385794004649981, -50.34529401456639874, -21.15365131572360013 ) ) ;
#15673=CARTESIAN_POINT ( 'NONE',  ( 54.92799477121080542, 19.38381105532069881, -76.61226657363050663 ) ) ;
#15675=CARTESIAN_POINT ( 'NONE',  ( 61.28085240419530066, -45.60177449860450594, -47.67834116410560341 ) ) ;
#15676=CARTESIAN_POINT ( 'NONE',  ( 61.25735456197249817, -45.31055611515090220, -47.12428047004050313 ) ) ;
#15680=EDGE_CURVE ( 'NONE', #34403, #31549, #20823, .T. ) ;
#15681=ORIENTED_EDGE ( 'NONE', *, *, #40504, .T. ) ;
#15682=CARTESIAN_POINT ( 'NONE',  ( 47.38034241041940220, 22.97049268725260163, -75.36289877400470516 ) ) ;
#15684=CARTESIAN_POINT ( 'NONE',  ( 43.05757823653970462, -45.97758008170070099, -7.621845463222870265 ) ) ;
#15688=CARTESIAN_POINT ( 'NONE',  ( 16.13393739769620083, -15.61618894467939889, -15.76422791930239953 ) ) ;
#15689=CARTESIAN_POINT ( 'NONE',  ( 11.75081654934500008, 34.19154675346119632, -18.04875625362609881 ) ) ;
#15690=DIRECTION ( 'NONE',  ( 0.000000000000000000, -1.000000000000000000, 0.000000000000000000 ) ) ;
#15693=CARTESIAN_POINT ( 'NONE',  ( 49.13365608953889563, 22.61156095028849933, -54.78978433424439487 ) ) ;
#15695=CARTESIAN_POINT ( 'NONE',  ( 52.91120713071100568, -49.63374342014000007, -48.91474119692630040 ) ) ;
#15700=CARTESIAN_POINT ( 'NONE',  ( 84.12560615065849845, 12.73461698676060116, -46.88422054015599372 ) ) ;
#15702=CARTESIAN_POINT ( 'NONE',  ( 52.84698447334999827, 18.45389268692349916, -48.96050381634810122 ) ) ;
#15703=CARTESIAN_POINT ( 'NONE',  ( 56.67833308803319881, -45.12936355862790094, -15.96402177979890169 ) ) ;
#15704=CARTESIAN_POINT ( 'NONE',  ( 55.05148602120549839, 15.77693620304509992, -25.60753014925489879 ) ) ;
#15708=CARTESIAN_POINT ( 'NONE',  ( 11.24176308004020086, -65.23165686211650893, -17.63707663737670117 ) ) ;
#15709=CARTESIAN_POINT ( 'NONE',  ( 10.74482708285359855, 32.66128207971850372, -45.52152800640289598 ) ) ;
#15712=CARTESIAN_POINT ( 'NONE',  ( 50.81914176117260240, -52.16949926219270139, -52.52140270191939919 ) ) ;
#15713=CARTESIAN_POINT ( 'NONE',  ( 8.808908491334550561, 32.01182072428549930, -46.67060441505820023 ) ) ;
#15717=CARTESIAN_POINT ( 'NONE',  ( 11.13393739769619906, -63.13870896646790953, -43.91241718390689641 ) ) ;
#15722=CARTESIAN_POINT ( 'NONE',  ( 56.84186848070030607, 19.14734183112060251, -52.83665659353640365 ) ) ;
#15725=ORIENTED_EDGE ( 'NONE', *, *, #29492, .F. ) ;
#15727=CARTESIAN_POINT ( 'NONE',  ( 53.62552786343490396, 20.09834016026489678, -75.58099297212140755 ) ) ;
#15728=CARTESIAN_POINT ( 'NONE',  ( 82.78853260230212641, -45.02051515586381925, -46.36933949548377853 ) ) ;
#15730=CARTESIAN_POINT ( 'NONE',  ( 50.95939078474921047, 17.38381105532069881, -76.37902184192927280 ) ) ;
#15733=CARTESIAN_POINT ( 'NONE',  ( 65.03603135424580728, -1.463538230407920082, -19.52361391316370032 ) ) ;
#15736=ORIENTED_EDGE ( 'NONE', *, *, #43362, .T. ) ;
#15737=VERTEX_POINT ( 'NONE', #21859 ) ;
#15741=EDGE_CURVE ( 'NONE', #51345, #25615, #14016, .T. ) ;
#15742=CARTESIAN_POINT ( 'NONE',  ( 47.02179957962620449, 23.06926496360710033, -75.47109446400469324 ) ) ;
#15746=CARTESIAN_POINT ( 'NONE',  ( 11.79921494304880092, 33.80856205050040586, -16.52202905012969936 ) ) ;
#15749=CARTESIAN_POINT ( 'NONE',  ( 57.01957019932739712, -50.62831541463020102, -74.14894682937750758 ) ) ;
#15750=CARTESIAN_POINT ( 'NONE',  ( -11.22445290707359966, 10.55079285699060243, -5.475728648851799996 ) ) ;
#15753=B_SPLINE_CURVE_WITH_KNOTS ( 'NONE', 3,
 ( #26661, #39258, #39772, #38753, #43703, #15668 ),
 .UNSPECIFIED., .F., .F.,
 ( 4, 2, 4 ),
 ( 0.000000000000000000, 0.5000000000000000000, 1.000000000000000000 ),
 .UNSPECIFIED. ) ;
#15754=CARTESIAN_POINT ( 'NONE',  ( 61.30530709542880174, 13.98952859230019996, -46.58604879334039595 ) ) ;
#15755=CARTESIAN_POINT ( 'NONE',  ( 57.50723796702470025, -45.11618894467940066, -17.93019253464870033 ) ) ;
#15756=ORIENTED_EDGE ( 'NONE', *, *, #44254, .F. ) ;
#15757=CARTESIAN_POINT ( 'NONE',  ( 53.41693480158970431, -49.35328119386819878, -48.75416851881659852 ) ) ;
#15759=CARTESIAN_POINT ( 'NONE',  ( 59.02328509747849949, -45.43582055027459887, -26.47283546404650068 ) ) ;
#15761=CARTESIAN_POINT ( 'NONE',  ( 56.50431216083380548, 15.03356263069209930, -26.27578698830990334 ) ) ;
#15763=CARTESIAN_POINT ( 'NONE',  ( 51.30775034956080560, 17.47491416869410230, -76.60305689054860068 ) ) ;
#15764=CARTESIAN_POINT ( 'NONE',  ( 52.93241475290810172, 18.38021004741200315, -48.85493842486449978 ) ) ;
#15769=CARTESIAN_POINT ( 'NONE',  ( 47.63442634882579796, -54.53229989956079748, -54.97162067429140109 ) ) ;
#15772=CARTESIAN_POINT ( 'NONE',  ( 61.55531029558209610, -30.52545227551890150, -16.28638563878910261 ) ) ;
#15774=CARTESIAN_POINT ( 'NONE',  ( 11.13393739769619906, 31.93056987172010608, -43.74365520157400056 ) ) ;
#15776=CARTESIAN_POINT ( 'NONE',  ( 51.02532063986365074, -35.17600456832372657, -76.41498861430551415 ) ) ;
#15783=EDGE_LOOP ( 'NONE', ( #31228, #45303, #15195, #21476, #22292, #27479, #13109, #33815, #48449, #51799, #47167, #21055, #22609 ) ) ;
#15793=CARTESIAN_POINT ( 'NONE',  ( 59.32366520224450568, -28.27453674296199537, -15.67709929047940065 ) ) ;
#15794=DIRECTION ( 'NONE',  ( -0.2260571801428161165, 0.000000000000000000, 0.9741140340359943917 ) ) ;
#15798=CARTESIAN_POINT ( 'NONE',  ( 40.90034125862820247, 13.87198803079870046, -5.606156744188270480 ) ) ;
#15799=AXIS2_PLACEMENT_3D ( 'NONE', #11276, #15465, #3930 ) ;
#15801=CARTESIAN_POINT ( 'NONE',  ( 14.90761372254600126, 21.75858530671060009, -76.14999999999999147 ) ) ;
#15803=CARTESIAN_POINT ( 'NONE',  ( 83.13571748553259511, -44.95166435745220213, -46.75830440892689666 ) ) ;
#15806=EDGE_LOOP ( 'NONE', ( #8227, #17628, #13542, #27157 ) ) ;
#15808=CARTESIAN_POINT ( 'NONE',  ( 13.96942586497290151, -50.35282484553089688, -20.94633231277909857 ) ) ;
#15811=CARTESIAN_POINT ( 'NONE',  ( 56.46551567295650642, -50.77616483221130750, -74.14999999999999147 ) ) ;
#15812=ORIENTED_EDGE ( 'NONE', *, *, #7504, .F. ) ;
#15813=CARTESIAN_POINT ( 'NONE',  ( -9.070458372979668837, -44.11014026221840112, -5.806348201939020015 ) ) ;
#15817=CARTESIAN_POINT ( 'NONE',  ( 13.68960069945450009, 19.17906422713569725, -21.10128301701960041 ) ) ;
#15818=CARTESIAN_POINT ( 'NONE',  ( 57.55751162050889747, -50.61165563123979894, -53.76309025934260433 ) ) ;
#15819=CARTESIAN_POINT ( 'NONE',  ( 42.34652499213279953, 12.85456310532500090, -4.929786138809819640 ) ) ;
#15822=CARTESIAN_POINT ( 'NONE',  ( 54.26618122617689721, -48.93283047810160014, -48.76497828246320410 ) ) ;
#15823=CARTESIAN_POINT ( 'NONE',  ( 68.13393739769840352, -50.61618894467879670, -73.25000000000220268 ) ) ;
#15829=CARTESIAN_POINT ( 'NONE',  ( 59.57331641441849968, -46.90860258996760024, -48.88667301442139745 ) ) ;
#15838=ORIENTED_EDGE ( 'NONE', *, *, #23203, .F. ) ;
#15839=CARTESIAN_POINT ( 'NONE',  ( 17.21347160910339724, 21.88381105532300097, -76.14999999999999147 ) ) ;
#15841=EDGE_CURVE ( 'NONE', #33091, #1308, #22613, .T. ) ;
#15843=ORIENTED_EDGE ( 'NONE', *, *, #2776, .T. ) ;
#15844=CARTESIAN_POINT ( 'NONE',  ( 56.86403571658450318, -45.97907451721239624, -26.24559329655039974 ) ) ;
#15846=ADVANCED_FACE ( 'NONE', ( #1184 ), #44774, .T. ) ;
#15848=EDGE_CURVE ( 'NONE', #15326, #45555, #31844, .T. ) ;
#15849=VERTEX_POINT ( 'NONE', #38382 ) ;
#15850=EDGE_CURVE ( 'NONE', #32096, #38625, #31000, .T. ) ;
#15852=EDGE_LOOP ( 'NONE', ( #13450, #47881, #23755, #31661 ) ) ;
#15853=CARTESIAN_POINT ( 'NONE',  ( 11.67620015026735203, -64.89165383396532150, -23.88711004025349283 ) ) ;
#15856=ORIENTED_EDGE ( 'NONE', *, *, #50060, .F. ) ;
#15858=B_SPLINE_CURVE_WITH_KNOTS ( 'NONE', 3,
 ( #49639, #26011, #25746, #17395, #5092, #14237, #29685, #29940, #30207, #37048, #45955, #42021, #46224, #10312, #17141, #21046, #33092, #1145, #49124, #41495 ),
 .UNSPECIFIED., .F., .F.,
 ( 4, 2, 2, 2, 2, 2, 2, 2, 2, 4 ),
 ( -3.516439999999999908E-13, 0.4027787201731649613, 0.8630972575143259773, 1.150796343352550100, 1.294645886271670099, 1.524805154942250107, 1.789982511918259966, 2.002124397499069897, 2.214266283079879827, 2.301592686705460356 ),
 .UNSPECIFIED. ) ;
#15860=DIRECTION ( 'NONE',  ( -0.4316160343590924597, 0.9020574254913767964, 0.000000000000000000 ) ) ;
#15861=CARTESIAN_POINT ( 'NONE',  ( 60.58628810321520319, 14.54561104465429899, -47.73487494779390516 ) ) ;
#15862=DIRECTION ( 'NONE',  ( 1.000000000000000000, 0.000000000000000000, 0.000000000000000000 ) ) ;
#15864=CARTESIAN_POINT ( 'NONE',  ( 11.13393739769619906, 31.88305279702909800, -43.74348518090240390 ) ) ;
#15865=CARTESIAN_POINT ( 'NONE',  ( -8.878336496226518548, 13.03716217029489854, -5.682102490148450258 ) ) ;
#15868=VECTOR ( 'NONE', #33774, 1000.000000000000000 ) ;
#15869=CARTESIAN_POINT ( 'NONE',  ( 47.06490849475201088, 23.30732314589785048, -75.17786410262570485 ) ) ;
#15870=CARTESIAN_POINT ( 'NONE',  ( 59.43897480784050202, 14.27109403266730148, -26.69952124243079794 ) ) ;
#15871=AXIS2_PLACEMENT_3D ( 'NONE', #44312, #20705, #36696 ) ;
#15872=AXIS2_PLACEMENT_3D ( 'NONE', #9778, #1908, #49872 ) ;
#15874=ORIENTED_EDGE ( 'NONE', *, *, #51064, .T. ) ;
#15875=CARTESIAN_POINT ( 'NONE',  ( 56.62432785517989942, -50.71560893929350300, -53.83726655417689955 ) ) ;
#15878=CARTESIAN_POINT ( 'NONE',  ( 13.00893739769619906, 34.28605925116850273, -47.75434321273180416 ) ) ;
#15882=EDGE_CURVE ( 'NONE', #31947, #8290, #31967, .T. ) ;
#15884=CARTESIAN_POINT ( 'NONE',  ( 61.48313171494003626, 14.13204535159540853, -47.33723770254623275 ) ) ;
#15885=CARTESIAN_POINT ( 'NONE',  ( 48.69693219778879723, -54.06267158604929790, -55.01166712023250227 ) ) ;
#15886=CARTESIAN_POINT ( 'NONE',  ( 51.88783817057427683, -32.77378372426147735, -18.83067710447933507 ) ) ;
#15894=CARTESIAN_POINT ( 'NONE',  ( 60.76922410162809740, -45.54289718728929870, -47.36000494951569806 ) ) ;
#15895=CARTESIAN_POINT ( 'NONE',  ( 49.30791778510987911, -53.55500811875207745, -54.21103610183089927 ) ) ;
#15903=ORIENTED_EDGE ( 'NONE', *, *, #14833, .T. ) ;
#15904=ORIENTED_EDGE ( 'NONE', *, *, #5742, .T. ) ;
#15905=DIRECTION ( 'NONE',  ( -0.2260571801428161443, -2.775557561562891351E-17, 0.9741140340359945027 ) ) ;
#15907=CARTESIAN_POINT ( 'NONE',  ( 53.51410843436200082, -49.43305938620899553, -49.22423862607029577 ) ) ;
#15908=CARTESIAN_POINT ( 'NONE',  ( 56.01715054582741260, 14.67189247168751720, -25.73175519691123014 ) ) ;
#15911=CARTESIAN_POINT ( 'NONE',  ( 76.39217513833645512, -17.42905162351204851, -12.76281908793090203 ) ) ;
#15914=AXIS2_PLACEMENT_3D ( 'NONE', #28643, #44644, #40716 ) ;
#15915=EDGE_CURVE ( 'NONE', #26391, #3281, #6612, .T. ) ;
#15917=CARTESIAN_POINT ( 'NONE',  ( 57.13225691960569463, -45.15146943985669736, -25.30757468707000157 ) ) ;
#15919=CARTESIAN_POINT ( 'NONE',  ( 60.87922264735060196, -0.7885390955128780410, -16.21936628598430019 ) ) ;
#15920=CARTESIAN_POINT ( 'NONE',  ( 52.11524330449060471, -49.86368024659240206, -76.92610723711719345 ) ) ;
#15921=ORIENTED_EDGE ( 'NONE', *, *, #17285, .F. ) ;
#15923=CARTESIAN_POINT ( 'NONE',  ( 52.93656365064889968, -50.31421972478020166, -77.15175517354180101 ) ) ;
#15925=DIRECTION ( 'NONE',  ( -1.000000000000000000, 0.000000000000000000, 0.000000000000000000 ) ) ;
#15930=CARTESIAN_POINT ( 'NONE',  ( 66.13393739769620083, -15.61618894467929941, -16.65000000000000213 ) ) ;
#15931=CARTESIAN_POINT ( 'NONE',  ( 56.56302216566690078, 13.88381105532070059, -15.29297957052069989 ) ) ;
#15932=LINE ( 'NONE', #35841, #9808 ) ;
#15937=CARTESIAN_POINT ( 'NONE',  ( 47.48065468354979402, 23.09789384912840049, -75.12259495528830655 ) ) ;
#15938=CARTESIAN_POINT ( 'NONE',  ( 47.21829295900949575, -54.77949880278709571, -54.61684610847309784 ) ) ;
#15941=CARTESIAN_POINT ( 'NONE',  ( 11.75935880766958519, -64.97634148314350000, -23.85050166126463012 ) ) ;
#15943=DIRECTION ( 'NONE',  ( 0.000000000000000000, 0.000000000000000000, 1.000000000000000000 ) ) ;
#15944=AXIS2_PLACEMENT_3D ( 'NONE', #17308, #37221, #25398 ) ;
#15945=EDGE_CURVE ( 'NONE', #35705, #33975, #34372, .T. ) ;
#15948=DIRECTION ( 'NONE',  ( -1.000000000000000000, -1.016537000000000039E-13, -1.878770999999999851E-12 ) ) ;
#15954=CARTESIAN_POINT ( 'NONE',  ( 49.40264607704519761, 22.51715297631980306, -54.82400704780420142 ) ) ;
#15956=CARTESIAN_POINT ( 'NONE',  ( 53.21057599194470100, -49.49334818133160496, -49.03900858120630346 ) ) ;
#15957=B_SPLINE_CURVE_WITH_KNOTS ( 'NONE', 3,
 ( #22800, #31429, #38822, #43267, #46692, #18880 ),
 .UNSPECIFIED., .F., .F.,
 ( 4, 1, 1, 4 ),
 ( 0.000000000000000000, 0.3333333333333329263, 0.6666666666666669627, 1.000000000000000000 ),
 .UNSPECIFIED. ) ;
#15961=CARTESIAN_POINT ( 'NONE',  ( 84.24534987432259925, 12.60397863988419864, -47.12743895163409746 ) ) ;
#15963=DIRECTION ( 'NONE',  ( 1.000000000000000000, 0.000000000000000000, 0.000000000000000000 ) ) ;
#15964=CARTESIAN_POINT ( 'NONE',  ( 56.21279806897850762, -45.28513128442910585, -16.23752131442829949 ) ) ;
#15965=CARTESIAN_POINT ( 'NONE',  ( 53.18037562183940281, 17.96329376868539995, -26.81634874583109962 ) ) ;
#15969=CARTESIAN_POINT ( 'NONE',  ( 11.41186172778549945, -65.13766231309419652, -17.00495023108739900 ) ) ;
#15970=CARTESIAN_POINT ( 'NONE',  ( 12.92260290766840036, 34.28065277568710201, -47.72142139346610179 ) ) ;
#15973=CARTESIAN_POINT ( 'NONE',  ( 52.27072484100800409, -50.81380991892629595, -50.92202115719549482 ) ) ;
#15974=CARTESIAN_POINT ( 'NONE',  ( 8.807322927776979782, 32.00291607516390258, -46.67042760097810117 ) ) ;
#15975=LINE ( 'NONE', #11538, #51048 ) ;
#15977=EDGE_CURVE ( 'NONE', #7222, #17870, #15104, .T. ) ;
#15978=DIRECTION ( 'NONE',  ( -0.6911981449639432729, -0.7226652920947591596, 0.000000000000000000 ) ) ;
#15979=CARTESIAN_POINT ( 'NONE',  ( 11.13393739769619906, -63.26646877388989054, -43.74576002344679893 ) ) ;
#15980=CARTESIAN_POINT ( 'NONE',  ( 68.13393739769810509, 19.38381105532030091, -71.50000000000198952 ) ) ;
#15982=CARTESIAN_POINT ( 'NONE',  ( 68.03757080751434216, -32.00242907265933923, -18.68196741761224189 ) ) ;
#15983=CARTESIAN_POINT ( 'NONE',  ( 56.87160281683760132, 19.05665430235150026, -52.71743055004790790 ) ) ;
#15984=CARTESIAN_POINT ( 'NONE',  ( 11.72616103466483573, 24.14067372595003036, -21.92230300879598559 ) ) ;
#15987=DIRECTION ( 'NONE',  ( 0.000000000000000000, 0.000000000000000000, -1.000000000000000000 ) ) ;
#15988=CARTESIAN_POINT ( 'NONE',  ( 52.71259303052651290, 20.20049112655129875, -75.79898569453698087 ) ) ;
#15991=CARTESIAN_POINT ( 'NONE',  ( 7.635415421591210894, -60.86027260432054931, -20.56421356237310150 ) ) ;
#15994=CARTESIAN_POINT ( 'NONE',  ( 16.13393739769620083, -15.61618894467929941, -76.14999999999999147 ) ) ;
#16000=CARTESIAN_POINT ( 'NONE',  ( 47.00221134363980013, 23.02870449882369641, -75.51940564623940588 ) ) ;
#16001=CARTESIAN_POINT ( 'NONE',  ( 11.13393739769619906, 24.07008072128950005, -43.74348518090240390 ) ) ;
#16006=CARTESIAN_POINT ( 'NONE',  ( 55.56331440656450127, -50.69060432040659947, -75.70197983327919644 ) ) ;
#16007=CARTESIAN_POINT ( 'NONE',  ( 88.13393739769620083, -33.11618894467940066, -65.65000000000000568 ) ) ;
#16008=CARTESIAN_POINT ( 'NONE',  ( 47.38073022375075283, 23.41843073406132802, -54.64585026063956974 ) ) ;
#16010=CARTESIAN_POINT ( 'NONE',  ( 61.19897335096789703, 14.07984942462570110, -47.06088098606709735 ) ) ;
#16013=ORIENTED_EDGE ( 'NONE', *, *, #31597, .F. ) ;
#16015=CARTESIAN_POINT ( 'NONE',  ( 52.88731329286200378, -49.63076474127340276, -48.71031102133859747 ) ) ;
#16017=CARTESIAN_POINT ( 'NONE',  ( 57.87157263515249639, -45.40826915251930274, -26.12905093743479767 ) ) ;
#16019=CARTESIAN_POINT ( 'NONE',  ( 61.25735466683790520, 14.07817815260590066, -47.12428023552489975 ) ) ;
#16022=CARTESIAN_POINT ( 'NONE',  ( 51.85163418285049630, 18.34999185856599979, -76.86771305873580218 ) ) ;
#16023=CARTESIAN_POINT ( 'NONE',  ( 53.40908402083690731, 18.14278958704170108, -48.94486837258570233 ) ) ;
#16028=CARTESIAN_POINT ( 'NONE',  ( 47.61882127642510198, -54.54439795203430208, -55.10468976659860374 ) ) ;
#16029=CARTESIAN_POINT ( 'NONE',  ( -10.45347530935170077, 11.54094627956400032, -5.983182295913979765 ) ) ;
#16030=DIRECTION ( 'NONE',  ( -0.5109955813515499878, -0.8595833385072046973, 0.000000000000000000 ) ) ;
#16031=CARTESIAN_POINT ( 'NONE',  ( 59.67048302056260667, -29.19628695015689956, -15.77538394522889931 ) ) ;
#16033=CARTESIAN_POINT ( 'NONE',  ( 11.13393739769619906, 31.88305279702909800, -43.74348518090240390 ) ) ;
#16035=CARTESIAN_POINT ( 'NONE',  ( 51.45476229416896530, -34.38915632507681863, -76.74519247898817298 ) ) ;
#16045=VERTEX_POINT ( 'NONE', #32224 ) ;
#16046=CARTESIAN_POINT ( 'NONE',  ( 10.75772284190022710, 33.13535827837971937, -23.47630699481211636 ) ) ;
#16048=CARTESIAN_POINT ( 'NONE',  ( 60.91971420063490683, 14.46337360283989959, -47.74179738751160329 ) ) ;
#16051=CARTESIAN_POINT ( 'NONE',  ( 10.78192289013670013, 33.70626262526499772, -17.70651626560779945 ) ) ;
#16052=CARTESIAN_POINT ( 'NONE',  ( 62.34145908511610656, -30.26177483428519821, -16.23785720254290155 ) ) ;
#16057=CIRCLE ( 'NONE', #31069, 25.00000000000000355 ) ;
#16058=CARTESIAN_POINT ( 'NONE',  ( 41.36999407038749865, 14.03644748879320048, -6.004979454220869428 ) ) ;
#16060=CARTESIAN_POINT ( 'NONE',  ( 84.27240597999899308, -43.88482305096810165, -47.25334685439979410 ) ) ;
#16063=ORIENTED_EDGE ( 'NONE', *, *, #23278, .T. ) ;
#16064=CARTESIAN_POINT ( 'NONE',  ( 53.25910687114200215, -49.18441974074990242, -27.17009175550089850 ) ) ;
#16066=CARTESIAN_POINT ( 'NONE',  ( 14.30723785210539845, -50.71453875907170072, -21.19168582719299820 ) ) ;
#16070=CARTESIAN_POINT ( 'NONE',  ( 72.38393739883420608, 11.88381105532070059, -61.44999999999999574 ) ) ;
#16072=CARTESIAN_POINT ( 'NONE',  ( -8.073139882959649682, -45.00859888370850115, -5.631272549003790040 ) ) ;
#16076=CARTESIAN_POINT ( 'NONE',  ( 57.49861655706580166, -50.10448309126950051, -52.59177543263909627 ) ) ;
#16077=CARTESIAN_POINT ( 'NONE',  ( 42.86117915671640333, 12.27262101796790006, -4.698036889951329620 ) ) ;
#16080=CARTESIAN_POINT ( 'NONE',  ( 58.27624582431690214, -46.80735200045160127, -47.55852830428500511 ) ) ;
#16086=DIRECTION ( 'NONE',  ( -0.000000000000000000, 1.000000000000000000, 0.000000000000000000 ) ) ;
#16089=CARTESIAN_POINT ( 'NONE',  ( 45.07858682377059978, 14.88010818488339915, -9.026855431852879974 ) ) ;
#16090=DIRECTION ( 'NONE',  ( 0.000000000000000000, -1.000000000000000000, 0.000000000000000000 ) ) ;
#16092=EDGE_LOOP ( 'NONE', ( #45068, #28836 ) ) ;
#16094=CARTESIAN_POINT ( 'NONE',  ( 17.92031055095850078, 21.20322725566390076, -75.94942944171690158 ) ) ;
#16096=ADVANCED_FACE ( 'NONE', ( #23847 ), #48247, .T. ) ;
#16097=ORIENTED_EDGE ( 'NONE', *, *, #41777, .T. ) ;
#16100=CARTESIAN_POINT ( 'NONE',  ( 61.69769988959340168, 13.93882227395219964, -46.83837617009780274 ) ) ;
#16102=B_SPLINE_SURFACE_WITH_KNOTS ( 'NONE', 1, 3, ( 
 ( #15585, #8226, #7726, #39687, #16342, #35752, #39945, #31539 ),
 ( #47558, #11653, #51734, #12166, #20260, #32298, #15829, #47812 ) ),
 .UNSPECIFIED., .F., .F., .F.,
 ( 2, 2 ),
 ( 4, 2, 2, 4 ),
 ( 0.1261347826432950014, 0.9339437630689100267 ),
 ( 3.992643801987300289, 8.116559215544439709, 13.46070403139630045, 18.66056373795289858 ),
 .UNSPECIFIED. ) ;
#16103=CARTESIAN_POINT ( 'NONE',  ( 12.02928788648473635, 34.13296709268954743, -17.22609660999479431 ) ) ;
#16104=ORIENTED_EDGE ( 'NONE', *, *, #518, .T. ) ;
#16106=DIRECTION ( 'NONE',  ( -0.8732394366197182567, 0.4872913772396111343, 0.000000000000000000 ) ) ;
#16107=VERTEX_POINT ( 'NONE', #44052 ) ;
#16109=DIRECTION ( 'NONE',  ( 0.000000000000000000, 1.000000000000000000, 0.000000000000000000 ) ) ;
#16110=DIRECTION ( 'NONE',  ( 0.000000000000000000, 1.784214116308896997E-11, 1.000000000000000000 ) ) ;
#16111=CARTESIAN_POINT ( 'NONE',  ( 61.12170114217160233, 14.23482143552810086, -47.45407097581740175 ) ) ;
#16113=CARTESIAN_POINT ( 'NONE',  ( 41.83063930241080186, -43.61086970063350066, -3.362295850879169823 ) ) ;
#16114=CARTESIAN_POINT ( 'NONE',  ( -2.656266623734050203, 17.48898290397159982, -4.829465371942860408 ) ) ;
#16116=AXIS2_PLACEMENT_3D ( 'NONE', #12375, #12125, #23881 ) ;
#16117=CARTESIAN_POINT ( 'NONE',  ( 47.07822794249411658, 23.33748126006274859, -75.12259495526954822 ) ) ;
#16118=CARTESIAN_POINT ( 'NONE',  ( 55.22144174253947568, 14.83847152459031449, -16.34786475617187307 ) ) ;
#16121=CARTESIAN_POINT ( 'NONE',  ( 57.40277299468780114, 16.17492991088059995, -48.23107244050790143 ) ) ;
#16122=EDGE_CURVE ( 'NONE', #7703, #39662, #16523, .T. ) ;
#16123=CARTESIAN_POINT ( 'NONE',  ( 41.06759784644540190, 14.27213265972969936, -6.034531555287039772 ) ) ;
#16124=CARTESIAN_POINT ( 'NONE',  ( 12.15072521531869931, 34.03384901777550198, -46.19630097385869760 ) ) ;
#16129=CARTESIAN_POINT ( 'NONE',  ( 13.23399064597960084, 18.92162210823540036, -21.05825742057550087 ) ) ;
#16130=CARTESIAN_POINT ( 'NONE',  ( 46.93194736084949881, 22.96293243065590062, -75.61358166513510071 ) ) ;
#16131=CARTESIAN_POINT ( 'NONE',  ( 48.64767879017799856, -53.93625458155220542, -54.52761353198660288 ) ) ;
#16132=CARTESIAN_POINT ( 'NONE',  ( -3.979110003385970540, 17.20385159207049952, -5.632303519440180040 ) ) ;
#16133=VECTOR ( 'NONE', #36703, 1000.000000000000114 ) ;
#16135=DIRECTION ( 'NONE',  ( 0.000000000000000000, 1.000000000000000000, 0.000000000000000000 ) ) ;
#16136=ORIENTED_EDGE ( 'NONE', *, *, #230, .T. ) ;
#16138=CARTESIAN_POINT ( 'NONE',  ( 15.67962062493140074, -50.86266781791879765, -20.15000000000000213 ) ) ;
#16139=ORIENTED_EDGE ( 'NONE', *, *, #25881, .F. ) ;
#16140=CARTESIAN_POINT ( 'NONE',  ( 57.24929578595760660, 21.38381105532069881, -63.99406948319570887 ) ) ;
#16141=CARTESIAN_POINT ( 'NONE',  ( 60.63571203433270540, -45.60655262937140719, -47.39339951304060605 ) ) ;
#16143=LINE ( 'NONE', #43680, #41147 ) ;
#16150=CARTESIAN_POINT ( 'NONE',  ( 83.34325726105160470, -45.31017261718839251, -47.50551966704799867 ) ) ;
#16151=VERTEX_POINT ( 'NONE', #41151 ) ;
#16152=VERTEX_POINT ( 'NONE', #45353 ) ;
#16153=ADVANCED_FACE ( 'NONE', ( #37227 ), #13643, .F. ) ;
#16154=ORIENTED_EDGE ( 'NONE', *, *, #33573, .T. ) ;
#16156=CARTESIAN_POINT ( 'NONE',  ( 53.99784841347855036, -50.61618894465041052, -77.02981973011630146 ) ) ;
#16158=CARTESIAN_POINT ( 'NONE',  ( 76.39889860447665626, -19.26176533219966203, -12.79180084499177816 ) ) ;
#16159=CARTESIAN_POINT ( 'NONE',  ( 53.21144349652569616, -51.94262854214029801, -53.42264529815139440 ) ) ;
#16160=CIRCLE ( 'NONE', #23655, 2.000000000000001776 ) ;
#16161=ORIENTED_EDGE ( 'NONE', *, *, #20255, .F. ) ;
#16165=FACE_OUTER_BOUND ( 'NONE', #50342, .T. ) ;
#16167=CARTESIAN_POINT ( 'NONE',  ( 62.09645049968020203, 0.05786461624523400044, -16.78440013667709962 ) ) ;
#16170=CARTESIAN_POINT ( 'NONE',  ( 62.88393739769619373, 4.883811055320659733, -84.94863984844531046 ) ) ;
#16171=CARTESIAN_POINT ( 'NONE',  ( 53.45777095194249995, -50.57384060062700115, -76.87859158467649934 ) ) ;
#16173=CARTESIAN_POINT ( 'NONE',  ( 57.55751162087899786, 17.38381105532069881, -53.92796738110899923 ) ) ;
#16175=CARTESIAN_POINT ( 'NONE',  ( 13.51862060011250044, -50.60094953679219998, -21.33274412383610041 ) ) ;
#16178=CARTESIAN_POINT ( 'NONE',  ( 18.49554612515125740, -51.29571572326634765, -15.70772097152689106 ) ) ;
#16179=CARTESIAN_POINT ( 'NONE',  ( 68.13393739769790614, -49.95860450174040324, -75.14853292321149070 ) ) ;
#16180=CARTESIAN_POINT ( 'NONE',  ( 68.38970075077773458, -0.8918033001876759513, -18.15384973117020451 ) ) ;
#16185=CARTESIAN_POINT ( 'NONE',  ( 47.32111516514320471, 22.89537558975190024, -75.47461153638720077 ) ) ;
#16188=CARTESIAN_POINT ( 'NONE',  ( 47.36150376523510630, -54.68114167742809428, -54.82442221309270280 ) ) ;
#16191=DIRECTION ( 'NONE',  ( 0.000000000000000000, -1.000000000000000000, 0.000000000000000000 ) ) ;
#16198=CARTESIAN_POINT ( 'NONE',  ( 10.61751707708940096, 33.59325229226949716, -18.17421237877550411 ) ) ;
#16201=CARTESIAN_POINT ( 'NONE',  ( 14.92239344893164699, -52.74445246665722919, -76.12392058102736314 ) ) ;
#16202=CARTESIAN_POINT ( 'NONE',  ( 48.56556163587730168, 22.87165378742070132, -54.94029309988020060 ) ) ;
#16204=CARTESIAN_POINT ( 'NONE',  ( 52.70624018093069907, -49.74719148043480033, -48.71312393436970467 ) ) ;
#16207=CARTESIAN_POINT ( 'NONE',  ( 49.40552051342540096, 22.26542118999089936, -54.15739458345379376 ) ) ;
#16209=CARTESIAN_POINT ( 'NONE',  ( 83.48374992014450413, 13.50741312754700019, -46.79909128427029685 ) ) ;
#16210=CARTESIAN_POINT ( 'NONE',  ( 55.17839213106780250, 15.74952588299860246, -26.00983945363739736 ) ) ;
#16212=CARTESIAN_POINT ( 'NONE',  ( 53.12218290940240450, 18.34074958227849805, -49.13784296393349393 ) ) ;
#16213=CARTESIAN_POINT ( 'NONE',  ( 56.10980393773469643, -45.40982727206459657, -16.53355515139729803 ) ) ;
#16214=CARTESIAN_POINT ( 'NONE',  ( 55.91596999402320023, 14.67228162054319895, -25.32543311652580087 ) ) ;
#16221=CARTESIAN_POINT ( 'NONE',  ( 12.02928808077719935, -65.36534498448229158, -17.22609656285550273 ) ) ;
#16222=CARTESIAN_POINT ( 'NONE',  ( 11.52812372297789878, 33.73647174606139743, -46.36286941860509359 ) ) ;
#16224=CARTESIAN_POINT ( 'NONE',  ( 47.88526556163500913, -54.30197853586789591, -54.48901645874850175 ) ) ;
#16225=DIRECTION ( 'NONE',  ( 1.000000000000000000, 0.000000000000000000, 0.000000000000000000 ) ) ;
#16227=ORIENTED_EDGE ( 'NONE', *, *, #12178, .T. ) ;
#16229=CARTESIAN_POINT ( 'NONE',  ( 11.10557205223450161, -63.32885013192529300, -44.25322260217060233 ) ) ;
#16230=CARTESIAN_POINT ( 'NONE',  ( 13.72056387933040433, 20.81200738410580442, -75.33783710294623859 ) ) ;
#16233=CARTESIAN_POINT ( 'NONE',  ( 50.17499495802539400, -49.21634929470250341, -76.14999999999999147 ) ) ;
#16238=CARTESIAN_POINT ( 'NONE',  ( 53.29384558423090112, -50.54670888882439783, -38.31189016485959797 ) ) ;
#16241=EDGE_CURVE ( 'NONE', #25078, #7053, #27525, .T. ) ;
#16243=CARTESIAN_POINT ( 'NONE',  ( 11.34407006786130623, -55.32883834980184190, -21.54741951671798716 ) ) ;
#16248=CARTESIAN_POINT ( 'NONE',  ( 72.13393739769620083, -1.116188944679340045, -20.65000000000000213 ) ) ;
#16250=VECTOR ( 'NONE', #41444, 1000.000000000000000 ) ;
#16251=CARTESIAN_POINT ( 'NONE',  ( 47.26713003401719959, 23.41039128977789829, -74.72332766641309831 ) ) ;
#16256=CARTESIAN_POINT ( 'NONE',  ( 12.26707159645439837, 33.49137753132240647, -15.95265749176260073 ) ) ;
#16261=CARTESIAN_POINT ( 'NONE',  ( 11.89321892218980103, -65.43602743108449715, -22.25048313876769868 ) ) ;
#16264=CARTESIAN_POINT ( 'NONE',  ( 61.51108477065319846, 13.91219452496449982, -46.37201720214299883 ) ) ;
#16266=FACE_OUTER_BOUND ( 'NONE', #4687, .T. ) ;
#16268=CARTESIAN_POINT ( 'NONE',  ( 53.00700885799259510, -49.56805288106040308, -48.78176285252619948 ) ) ;
#16269=CARTESIAN_POINT ( 'NONE',  ( 59.96235233370940421, -45.26212046306700643, -26.64974492922270244 ) ) ;
#16271=CARTESIAN_POINT ( 'NONE',  ( 13.86909323948760075, 19.40590670161929765, -21.27400668797769612 ) ) ;
#16272=CARTESIAN_POINT ( 'NONE',  ( 57.12645307100470404, 14.55895300901689993, -26.23065065375599758 ) ) ;
#16274=CARTESIAN_POINT ( 'NONE',  ( 51.15791182533700265, 19.03874145082539826, -76.23077825227480275 ) ) ;
#16275=CARTESIAN_POINT ( 'NONE',  ( 52.80366186835330211, 18.44443676282890010, -48.66065998140030047 ) ) ;
#16277=FACE_OUTER_BOUND ( 'NONE', #16092, .T. ) ;
#16280=CARTESIAN_POINT ( 'NONE',  ( 47.53109895159769849, -54.58212600392469938, -54.89453521545159731 ) ) ;
#16283=CARTESIAN_POINT ( 'NONE',  ( 56.39270695421159729, 19.29512507422779777, -52.86271299482670116 ) ) ;
#16290=ORIENTED_EDGE ( 'NONE', *, *, #7509, .T. ) ;
#16297=ORIENTED_EDGE ( 'NONE', *, *, #43095, .F. ) ;
#16298=DIRECTION ( 'NONE',  ( 0.9313175168445364527, 0.3616257875448561365, 0.04329517988286096797 ) ) ;
#16305=AXIS2_PLACEMENT_3D ( 'NONE', #14463, #46457, #14980 ) ;
#16307=B_SPLINE_CURVE_WITH_KNOTS ( 'NONE', 3,
 ( #29731, #48642, #41027, #936, #36566, #41543 ),
 .UNSPECIFIED., .F., .F.,
 ( 4, 1, 1, 4 ),
 ( 0.000000000000000000, 0.3333333332445770347, 0.6666666664890291694, 1.000000000000000000 ),
 .UNSPECIFIED. ) ;
#16309=ORIENTED_EDGE ( 'NONE', *, *, #37930, .F. ) ;
#16310=CARTESIAN_POINT ( 'NONE',  ( 10.65234009212060151, -63.87410165361089298, -23.62431477846339689 ) ) ;
#16312=CARTESIAN_POINT ( 'NONE',  ( 44.99439540629440160, 14.59120791265710082, -8.742832391549649529 ) ) ;
#16313=CARTESIAN_POINT ( 'NONE',  ( 14.15413451811019918, 20.61624280354940097, -75.59143512441710300 ) ) ;
#16316=CARTESIAN_POINT ( 'NONE',  ( 82.88019469981989573, -45.12199509848900192, -46.94529082815019194 ) ) ;
#16321=CARTESIAN_POINT ( 'NONE',  ( 53.24319873876810050, -49.24894743539400110, -27.32017878002559996 ) ) ;
#16323=CARTESIAN_POINT ( 'NONE',  ( 15.10819245919740084, -50.76188580677340667, -20.77789291004060246 ) ) ;
#16324=CARTESIAN_POINT ( 'NONE',  ( 50.30446722783852920, -36.40950912720241917, -76.16831878770071285 ) ) ;
#16327=CARTESIAN_POINT ( 'NONE',  ( 12.28937802692940018, -50.00765210412139794, -21.14656546108620105 ) ) ;
#16329=CARTESIAN_POINT ( 'NONE',  ( -7.625187662226220020, -45.45404276017920608, -5.684751090845729493 ) ) ;
#16330=CARTESIAN_POINT ( 'NONE',  ( 47.43160242963380568, 23.39460843266559920, -54.67048143933339333 ) ) ;
#16333=CARTESIAN_POINT ( 'NONE',  ( 12.82931922587579976, 19.41533729766869953, -21.34049584734400185 ) ) ;
#16335=CARTESIAN_POINT ( 'NONE',  ( 41.75077269581309736, 13.19527022550269990, -5.046632968629480409 ) ) ;
#16336=DIRECTION ( 'NONE',  ( 1.000000000000000000, 0.000000000000000000, 0.000000000000000000 ) ) ;
#16337=CARTESIAN_POINT ( 'NONE',  ( 60.31639983755060541, -45.83544975381190056, -47.65366050515999774 ) ) ;
#16338=CARTESIAN_POINT ( 'NONE',  ( 68.13393739769841773, -50.61618894467878960, -73.25000000000220268 ) ) ;
#16340=CARTESIAN_POINT ( 'NONE',  ( 17.21347160910390173, -53.11618894467930119, -76.14999999999999147 ) ) ;
#16342=CARTESIAN_POINT ( 'NONE',  ( 53.39190020003140091, -49.64277996747850352, -49.50885269097420149 ) ) ;
#16343=EDGE_LOOP ( 'NONE', ( #12171, #26111, #7114, #15838 ) ) ;
#16345=CARTESIAN_POINT ( 'NONE',  ( 10.14520404402119880, 32.04273756952679975, -45.99312054747319678 ) ) ;
#16349=CARTESIAN_POINT ( 'NONE',  ( 18.11674004330059873, 20.32108400380180058, -75.32473453343510528 ) ) ;
#16353=FACE_OUTER_BOUND ( 'NONE', #2320, .T. ) ;
#16354=CYLINDRICAL_SURFACE ( 'NONE', #32779, 2.000000000000000000 ) ;
#16356=CARTESIAN_POINT ( 'NONE',  ( 61.75019923867180438, 13.88381043675840054, -46.43277563447490053 ) ) ;
#16359=CARTESIAN_POINT ( 'NONE',  ( 75.29334099864146879, 5.095336761201883391, -12.50187872901068964 ) ) ;
#16363=CARTESIAN_POINT ( 'NONE',  ( 50.20833736503800537, -46.19202927519189927, -12.60658152119249920 ) ) ;
#16366=DIRECTION ( 'NONE',  ( -1.822422554782380175E-11, -1.784227544494129940E-11, -1.000000000000000000 ) ) ;
#16367=EDGE_CURVE ( 'NONE', #9892, #12485, #3457, .T. ) ;
#16368=ORIENTED_EDGE ( 'NONE', *, *, #19142, .F. ) ;
#16370=CARTESIAN_POINT ( 'NONE',  ( -8.766062602303898998, -15.61618894467929941, 8.450000000000024158 ) ) ;
#16372=CARTESIAN_POINT ( 'NONE',  ( 60.81833024471840332, 14.35563499692709932, -47.52759458687679484 ) ) ;
#16373=CARTESIAN_POINT ( 'NONE',  ( 51.26921915167240229, 14.36187956967640034, -12.86592481132139909 ) ) ;
#16374=DIRECTION ( 'NONE',  ( -1.000000000000000000, -1.004313591354993529E-15, 0.000000000000000000 ) ) ;
#16375=CARTESIAN_POINT ( 'NONE',  ( -6.133771980677649616, 15.17810994771089916, -4.670463077492210680 ) ) ;
#16377=CARTESIAN_POINT ( 'NONE',  ( 55.91595717589669334, 14.67227259378219983, -17.93019253464870033 ) ) ;
#16379=EDGE_CURVE ( 'NONE', #30000, #45437, #19999, .T. ) ;
#16380=ORIENTED_EDGE ( 'NONE', *, *, #2724, .F. ) ;
#16381=CARTESIAN_POINT ( 'NONE',  ( 52.56521993351449851, -49.86179673305689874, -28.15000000000000213 ) ) ;
#16383=CARTESIAN_POINT ( 'NONE',  ( 12.25380415244200094, 34.08744772712660165, -46.27199321433290180 ) ) ;
#16388=CARTESIAN_POINT ( 'NONE',  ( 10.87995450790350205, -64.97548900853969656, -17.51161086048150040 ) ) ;
#16389=CARTESIAN_POINT ( 'NONE',  ( 12.27824370503539875, 18.91995526668989669, -21.14999999870460101 ) ) ;
#16390=CARTESIAN_POINT ( 'NONE',  ( 46.80616873440099823, 22.71927177964060007, -75.82639822421660369 ) ) ;
#16391=CARTESIAN_POINT ( 'NONE',  ( 48.68378925563050075, -54.05006251182930299, -54.91526356565999833 ) ) ;
#16392=AXIS2_PLACEMENT_3D ( 'NONE', #47039, #35478, #26564 ) ;
#16393=LINE ( 'NONE', #40758, #17269 ) ;
#16394=DIRECTION ( 'NONE',  ( -1.000000000000000000, 4.735514272306495889E-33, 9.834501533011742432E-16 ) ) ;
#16402=CARTESIAN_POINT ( 'NONE',  ( 60.69273398595009894, -45.54451186045000100, -47.19142213667469576 ) ) ;
#16404=CARTESIAN_POINT ( 'NONE',  ( 12.86222958136720074, 18.76465491334460012, -21.07385132223840074 ) ) ;
#16406=DIRECTION ( 'NONE',  ( 0.000000000000000000, -1.000000000000000000, 0.000000000000000000 ) ) ;
#16410=CARTESIAN_POINT ( 'NONE',  ( 83.01976156432699838, -45.38357736965039635, -47.45812318453789658 ) ) ;
#16411=VERTEX_POINT ( 'NONE', #43483 ) ;
#16412=VERTEX_POINT ( 'NONE', #16207 ) ;
#16413=ORIENTED_EDGE ( 'NONE', *, *, #39575, .F. ) ;
#16414=CARTESIAN_POINT ( 'NONE',  ( 61.51109188950590578, -45.14456777294489598, -46.47690995681890058 ) ) ;
#16415=CARTESIAN_POINT ( 'NONE',  ( 52.58812961169699918, -49.84012128000139796, -48.57103837950110403 ) ) ;
#16416=CARTESIAN_POINT ( 'NONE',  ( 12.08165151496428713, -55.41053553174391055, -22.62766840197337714 ) ) ;
#16417=CARTESIAN_POINT ( 'NONE',  ( 76.44536772384181234, -6.686551103978267463, -12.99199962697529998 ) ) ;
#16421=ORIENTED_EDGE ( 'NONE', *, *, #45568, .T. ) ;
#16425=CARTESIAN_POINT ( 'NONE',  ( 56.27102574643829769, -50.57722701405970156, -52.87266565438959987 ) ) ;
#16429=CARTESIAN_POINT ( 'NONE',  ( 61.28398356449380202, -45.60471458446119897, -47.68178229846480320 ) ) ;
#16430=ORIENTED_EDGE ( 'NONE', *, *, #2281, .T. ) ;
#16432=CARTESIAN_POINT ( 'NONE',  ( 52.23775024128120492, -49.82363818699889890, -77.10775516233969995 ) ) ;
#16433=CARTESIAN_POINT ( 'NONE',  ( 60.23889825737600745, 14.54821815915974703, -47.30579064662337885 ) ) ;
#16435=CIRCLE ( 'NONE', #24790, 40.00000000000000711 ) ;
#16439=CARTESIAN_POINT ( 'NONE',  ( 41.23309865046339695, -44.72123908719060381, -5.265645747893140438 ) ) ;
#16440=CARTESIAN_POINT ( 'NONE',  ( 15.67962062493140074, -50.86266781791879765, -20.15000000000000213 ) ) ;
#16444=CARTESIAN_POINT ( 'NONE',  ( 18.38332337263111427, -52.17615710686938968, -75.56421430878999956 ) ) ;
#16446=CARTESIAN_POINT ( 'NONE',  ( 14.43104019203130051, -52.03647206054819918, -75.81086730487160708 ) ) ;
#16447=CARTESIAN_POINT ( 'NONE',  ( 47.23375364729769643, -54.76822368793749973, -54.67325007366670064 ) ) ;
#16451=CARTESIAN_POINT ( 'NONE',  ( 84.22672017751912676, 12.55805222647083497, -46.99906225624759770 ) ) ;
#16454=CARTESIAN_POINT ( 'NONE',  ( 55.48509142758890533, -46.00752295928280233, -16.66509390011597702 ) ) ;
#16455=CARTESIAN_POINT ( 'NONE',  ( 61.31807988003849630, -45.64188066314479642, -47.72348187468949732 ) ) ;
#16458=CARTESIAN_POINT ( 'NONE',  ( 48.68901951993020560, 22.76098662308300291, -54.71436045317769725 ) ) ;
#16459=ORIENTED_EDGE ( 'NONE', *, *, #513, .F. ) ;
#16460=CARTESIAN_POINT ( 'NONE',  ( 52.63212581583610472, -49.79676770012090259, -48.50959626792249679 ) ) ;
#16465=CARTESIAN_POINT ( 'NONE',  ( 84.38939444912799104, 12.25052432195479923, -47.32729711157580255 ) ) ;
#16466=CARTESIAN_POINT ( 'NONE',  ( 55.77169211825290063, 15.03234804280600123, -25.85730881726700048 ) ) ;
#16468=CARTESIAN_POINT ( 'NONE',  ( 52.57890692814670075, 18.61498511809359968, -48.49302657703999841 ) ) ;
#16469=CARTESIAN_POINT ( 'NONE',  ( 55.65085491148499841, -45.30818602241870252, -15.56796338809930091 ) ) ;
#16472=B_SPLINE_CURVE_WITH_KNOTS ( 'NONE', 3,
 ( #27209, #43221, #23779, #35603, #27975, #11509, #27467, #31642, #3641, #3899 ),
 .UNSPECIFIED., .F., .F.,
 ( 4, 2, 2, 2, 4 ),
 ( 0.000000000000000000, 0.3550177484190761845, 0.6750337469940175250, 0.8750437461033545583, 1.000000000000000000 ),
 .UNSPECIFIED. ) ;
#16474=CARTESIAN_POINT ( 'NONE',  ( 11.84416398830530071, -65.08858756582790761, -16.58498012168669788 ) ) ;
#16475=CARTESIAN_POINT ( 'NONE',  ( 12.85003218997280072, 34.27383497643789667, -47.67045162685929682 ) ) ;
#16476=CARTESIAN_POINT ( 'NONE',  ( 18.86789271246039945, 20.55440458018300021, -15.81497037201279987 ) ) ;
#16478=CARTESIAN_POINT ( 'NONE',  ( 10.97349868895814318, -64.80942964233447867, -23.22353997969214845 ) ) ;
#16480=ORIENTED_EDGE ( 'NONE', *, *, #50363, .T. ) ;
#16482=CARTESIAN_POINT ( 'NONE',  ( 11.10543711150969948, -63.21940129908220030, -44.25051057170020385 ) ) ;
#16491=ADVANCED_FACE ( 'NONE', ( #12284 ), #35866, .F. ) ;
#16492=DIRECTION ( 'NONE',  ( -0.6047562208151069374, 0.7964106436917012255, 0.000000000000000000 ) ) ;
#16493=CARTESIAN_POINT ( 'NONE',  ( 56.66762828736870006, -50.37953306433199430, -52.77094437832339935 ) ) ;
#16494=CARTESIAN_POINT ( 'NONE',  ( 56.42249077807360180, 19.27081265489739792, -52.83600065022080372 ) ) ;
#16497=CARTESIAN_POINT ( 'NONE',  ( 11.53605495837543948, -55.35105376503654639, -21.73576846289474318 ) ) ;
#16498=CARTESIAN_POINT ( 'NONE',  ( 54.35193248541229849, 19.95680887633289657, -75.41416007314899161 ) ) ;
#16499=CARTESIAN_POINT ( 'NONE',  ( 46.68683961171959851, -53.36165723267750138, -76.07661161287319374 ) ) ;
#16502=CARTESIAN_POINT ( 'NONE',  ( 52.67142628424050343, -49.78173758010149896, -48.75814597207470058 ) ) ;
#16504=LINE ( 'NONE', #16248, #9673 ) ;
#16506=CARTESIAN_POINT ( 'NONE',  ( 46.37528053896889446, 21.71340314309550124, -76.14999999999999147 ) ) ;
#16507=CARTESIAN_POINT ( 'NONE',  ( 19.21160129066574740, -52.77196524774721809, -16.16879274230204899 ) ) ;
#16508=EDGE_CURVE ( 'NONE', #19900, #1406, #36368, .T. ) ;
#16509=CARTESIAN_POINT ( 'NONE',  ( 58.91181031229810117, 15.24198406853699872, -47.44472854892460134 ) ) ;
#16516=CARTESIAN_POINT ( 'NONE',  ( 61.50836220838129975, 13.91397026120830027, -46.46408765477929848 ) ) ;
#16518=CARTESIAN_POINT ( 'NONE',  ( -17.94291051752670185, -51.49525275629270027, -52.69725456403789821 ) ) ;
#16519=EDGE_LOOP ( 'NONE', ( #37767, #46603, #18942, #9594 ) ) ;
#16520=CARTESIAN_POINT ( 'NONE',  ( 53.13663702127480093, -49.50013705438340139, -48.80285956223989530 ) ) ;
#16522=CARTESIAN_POINT ( 'NONE',  ( 57.98146860794130220, -45.12919884128839954, -25.62231485056000224 ) ) ;
#16523=LINE ( 'NONE', #28305, #45273 ) ;
#16524=CARTESIAN_POINT ( 'NONE',  ( 57.38644999245990164, 14.57387751478819915, -26.27655890715150022 ) ) ;
#16526=CARTESIAN_POINT ( 'NONE',  ( 51.38510966839819361, 18.87816813940790439, -76.33916217765379031 ) ) ;
#16527=CARTESIAN_POINT ( 'NONE',  ( 52.88917638043529479, 18.40237379729330058, -48.82176621297229246 ) ) ;
#16529=CARTESIAN_POINT ( 'NONE',  ( 46.35275103504439898, 21.67755452994670406, -76.14999999999999147 ) ) ;
#16530=CARTESIAN_POINT ( 'NONE',  ( 64.44836340493399973, -45.11618894467940066, -12.01833907808290114 ) ) ;
#16533=CARTESIAN_POINT ( 'NONE',  ( 47.58415360336899624, -54.56008480908929670, -55.08758729138420307 ) ) ;
#16534=CARTESIAN_POINT ( 'NONE',  ( -6.140345868814909736, 15.17335822560399983, -4.613862305479059955 ) ) ;
#16535=CARTESIAN_POINT ( 'NONE',  ( 40.64814283787880100, 13.41987867678509971, -4.018323132419280519 ) ) ;
#16536=CARTESIAN_POINT ( 'NONE',  ( 57.35949929755079779, 19.07198536079580364, -52.80982651506389658 ) ) ;
#16538=CARTESIAN_POINT ( 'NONE',  ( 16.65420337844999921, -51.11618894467930119, -20.15000000000000213 ) ) ;
#16540=AXIS2_PLACEMENT_3D ( 'NONE', #48425, #12267, #20364 ) ;
#16545=CARTESIAN_POINT ( 'NONE',  ( 14.12233147434080038, -51.14020415405890674, -22.75736350782009865 ) ) ;
#16546=AXIS2_PLACEMENT_3D ( 'NONE', #17647, #44640, #48843 ) ;
#16547=CARTESIAN_POINT ( 'NONE',  ( 15.83040942711627963, -50.94062305526537671, -15.66031378978091304 ) ) ;
#16550=CARTESIAN_POINT ( 'NONE',  ( 57.39214507209349847, -45.11761009216159835, -25.32322608115779872 ) ) ;
#16555=CARTESIAN_POINT ( 'NONE',  ( 61.25346184070040323, 14.37618061013010085, -47.68486562037010401 ) ) ;
#16556=EDGE_CURVE ( 'NONE', #10857, #49956, #2634, .T. ) ;
#16565=CARTESIAN_POINT ( 'NONE',  ( 14.12425648473279871, 20.57417486552859742, -75.54540032568620234 ) ) ;
#16568=CARTESIAN_POINT ( 'NONE',  ( 82.65203287802668797, -45.07757861141610078, -46.57208626984790101 ) ) ;
#16571=ORIENTED_EDGE ( 'NONE', *, *, #14833, .F. ) ;
#16572=CARTESIAN_POINT ( 'NONE',  ( 52.81005256294240269, -49.67124369057780342, -28.15000000000000213 ) ) ;
#16573=CARTESIAN_POINT ( 'NONE',  ( 15.70006563680280109, -50.87966732221310195, -20.26432904851890271 ) ) ;
#16577=CARTESIAN_POINT ( 'NONE',  ( 49.42599753308910238, 14.94798595550149933, -12.04388482386629988 ) ) ;
#16579=CARTESIAN_POINT ( 'NONE',  ( -2.895883733608759947, -49.14352575125250411, -5.678499124190959257 ) ) ;
#16580=CARTESIAN_POINT ( 'NONE',  ( 47.38766415547200239, 23.43125296332900120, -54.78230785539219738 ) ) ;
#16581=EDGE_CURVE ( 'NONE', #5608, #9812, #41949, .T. ) ;
#16584=CARTESIAN_POINT ( 'NONE',  ( 54.68494843651092197, 16.77593801893483416, -26.71884417013828994 ) ) ;
#16585=CARTESIAN_POINT ( 'NONE',  ( 11.10349381579360006, 33.92246930422219720, -17.61839574234429762 ) ) ;
#16586=DIRECTION ( 'NONE',  ( 7.800826455589531184E-12, 7.212287414728286387E-06, 0.9999999999739914713 ) ) ;
#16588=FACE_OUTER_BOUND ( 'NONE', #26825, .T. ) ;
#16589=CARTESIAN_POINT ( 'NONE',  ( 55.65042755000810359, -48.32738405545750027, -48.64421902443349666 ) ) ;
#16591=EDGE_CURVE ( 'NONE', #260, #39471, #23642, .T. ) ;
#16593=CARTESIAN_POINT ( 'NONE',  ( 17.21347160910390173, -53.11618894467930119, -76.14999999999999147 ) ) ;
#16594=EDGE_CURVE ( 'NONE', #10696, #45486, #15447, .T. ) ;
#16596=CARTESIAN_POINT ( 'NONE',  ( 51.75217146148440150, 13.88381105532070059, -11.53056162591239975 ) ) ;
#16598=CARTESIAN_POINT ( 'NONE',  ( 20.13393739496619972, 24.18330852864180258, -20.65000000000000213 ) ) ;
#16599=CARTESIAN_POINT ( 'NONE',  ( 10.13628986064439985, 31.90905804943249535, -45.99669294954719589 ) ) ;
#16603=CARTESIAN_POINT ( 'NONE',  ( 18.84633586404639871, 20.57176844745119837, -74.52171359303420672 ) ) ;
#16606=EDGE_LOOP ( 'NONE', ( #15017, #31077, #10400, #32051 ) ) ;
#16607=CARTESIAN_POINT ( 'NONE',  ( 10.02596761237749945, -63.80904651843830067, -46.25874165023890328 ) ) ;
#16610=EDGE_CURVE ( 'NONE', #16107, #44442, #40048, .T. ) ;
#16611=CARTESIAN_POINT ( 'NONE',  ( 61.62707301771609991, 13.89267493316299884, -46.47916889091800385 ) ) ;
#16613=TOROIDAL_SURFACE ( 'NONE', #31671, 3.000000013056939974, 2.000000000021340263 ) ;
#16615=CIRCLE ( 'NONE', #20822, 20.79999999999999716 ) ;
#16616=CIRCLE ( 'NONE', #15799, 1.999999999999998224 ) ;
#16618=CARTESIAN_POINT ( 'NONE',  ( 12.63673173825685936, -65.49512871884734011, -22.96425544219204440 ) ) ;
#16619=ORIENTED_EDGE ( 'NONE', *, *, #13162, .F. ) ;
#16620=CARTESIAN_POINT ( 'NONE',  ( 11.20408340530847902, -64.05422569580414915, -24.10527562562518611 ) ) ;
#16622=AXIS2_PLACEMENT_3D ( 'NONE', #46209, #29668, #6106 ) ;
#16625=( BOUNDED_CURVE ( )  B_SPLINE_CURVE ( 3, ( #5714, #25088, #17005, #40837 ),
 .UNSPECIFIED., .F., .T. ) 
 B_SPLINE_CURVE_WITH_KNOTS ( ( 4, 4 ),
 ( 6.078858056860969583, 6.232210822545849460 ),
 .UNSPECIFIED. ) 
 CURVE ( )  GEOMETRIC_REPRESENTATION_ITEM ( )  RATIONAL_B_SPLINE_CURVE ( ( 1.000000000000000000, 0.9980412040773770643, 0.9980412040773770643, 1.000000000000000000 ) ) 
 REPRESENTATION_ITEM ( '' )  );
#16626=ORIENTED_EDGE ( 'NONE', *, *, #8119, .T. ) ;
#16627=CARTESIAN_POINT ( 'NONE',  ( 11.49541412067671509, -65.34930666582664571, -17.78290583432579908 ) ) ;
#16628=CARTESIAN_POINT ( 'NONE',  ( 71.09324853129349719, 12.47263593864819953, -12.19466500508340090 ) ) ;
#16630=CARTESIAN_POINT ( 'NONE',  ( 12.06284766121009966, 32.21085600226960111, -22.25048313876769868 ) ) ;
#16631=CARTESIAN_POINT ( 'NONE',  ( -6.441449436784619564, 14.95323763042179976, -4.672284524380850179 ) ) ;
#16633=CARTESIAN_POINT ( 'NONE',  ( 61.35834738731979598, 13.96262971120960117, -28.10103293363079757 ) ) ;
#16638=CARTESIAN_POINT ( 'NONE',  ( 12.18715281654259996, 34.05328359747860389, -46.13824078873810208 ) ) ;
#16641=AXIS2_PLACEMENT_3D ( 'NONE', #16630, #12717, #33118 ) ;
#16643=CARTESIAN_POINT ( 'NONE',  ( 12.75999515594850031, 18.86331954735589989, -21.12209177392130144 ) ) ;
#16644=AXIS2_PLACEMENT_3D ( 'NONE', #18286, #17527, #29563 ) ;
#16646=CARTESIAN_POINT ( 'NONE',  ( 49.03570248356319894, -53.73371453229830763, -54.39120251675719686 ) ) ;
#16647=CARTESIAN_POINT ( 'NONE',  ( -3.454818612163319536, 17.59177618004110144, -5.676727923997320069 ) ) ;
#16648=EDGE_CURVE ( 'NONE', #39953, #19884, #48806, .T. ) ;
#16649=VECTOR ( 'NONE', #39365, 1000.000000000000114 ) ;
#16651=CARTESIAN_POINT ( 'NONE',  ( 65.04848046133125195, -32.26190002985004668, -17.85478322451875854 ) ) ;
#16659=CARTESIAN_POINT ( 'NONE',  ( 60.37202493514429591, -45.79855239338960615, -47.62297778162039918 ) ) ;
#16660=CARTESIAN_POINT ( 'NONE',  ( 57.12444641458250061, 19.38683328974900277, -53.89324253167760048 ) ) ;
#16661=CARTESIAN_POINT ( 'NONE',  ( 61.75019796695539753, 13.88381105532070059, -46.37203261889099792 ) ) ;
#16666=ORIENTED_EDGE ( 'NONE', *, *, #35768, .F. ) ;
#16667=CARTESIAN_POINT ( 'NONE',  ( 83.63395638909621255, -44.98627285813419974, -47.37153147893519645 ) ) ;
#16670=EDGE_LOOP ( 'NONE', ( #4611, #20470, #3161, #35255, #36533, #45255, #41296, #33649, #24240 ) ) ;
#16673=CARTESIAN_POINT ( 'NONE',  ( 76.44639894005106839, -6.601916875635619242, -12.99644329064062909 ) ) ;
#16674=CARTESIAN_POINT ( 'NONE',  ( 51.34626689658080068, -52.95676961735540544, -54.59842079273609272 ) ) ;
#16675=AXIS2_PLACEMENT_3D ( 'NONE', #8907, #28280, #44029 ) ;
#16680=CARTESIAN_POINT ( 'NONE',  ( 16.15069456443690044, 19.81939336389048734, -20.15000000000000213 ) ) ;
#16682=CARTESIAN_POINT ( 'NONE',  ( 8.808591387964359143, -63.24239172143919774, -46.67055361988870033 ) ) ;
#16686=AXIS2_PLACEMENT_3D ( 'NONE', #28795, #36653, #16754 ) ;
#16687=ORIENTED_EDGE ( 'NONE', *, *, #36092, .T. ) ;
#16689=CARTESIAN_POINT ( 'NONE',  ( 53.07595679201899941, -50.38449176261200080, -77.13124877896089515 ) ) ;
#16691=CARTESIAN_POINT ( 'NONE',  ( 60.83884119656880074, 14.23235859654429980, -47.05422022228049883 ) ) ;
#16692=AXIS2_PLACEMENT_3D ( 'NONE', #37234, #48773, #17319 ) ;
#16693=AXIS2_PLACEMENT_3D ( 'NONE', #23537, #47432, #27745 ) ;
#16695=DIRECTION ( 'NONE',  ( -0.3918900565005491998, 0.9200120562340454722, 0.000000000000000000 ) ) ;
#16696=B_SPLINE_CURVE_WITH_KNOTS ( 'NONE', 3,
 ( #32939, #29023, #16991, #468, #41087, #12802, #31905, #8863, #8339, #28758, #40823, #47925, #4924, #28501, #12027, #48432 ),
 .UNSPECIFIED., .F., .F.,
 ( 4, 2, 2, 2, 2, 2, 2, 4 ),
 ( 0.000000000000000000, 0.1775020625791663698, 0.3375039218054580181, 0.4375050838218894067, 0.5000058100821596074, 0.6250072626026996758, 0.7914782147670768042, 1.000000000000000000 ),
 .UNSPECIFIED. ) ;
#16697=CARTESIAN_POINT ( 'NONE',  ( 43.67695093021549724, -43.30705450646729560, -4.963296560282329573 ) ) ;
#16698=LINE ( 'NONE', #16440, #35125 ) ;
#16699=CARTESIAN_POINT ( 'NONE',  ( 57.20485010882750743, 13.88381105532070059, -16.39258517501439982 ) ) ;
#16700=CARTESIAN_POINT ( 'NONE',  ( 61.47037426737699661, -45.40940486849099500, -47.41703440505000344 ) ) ;
#16703=ORIENTED_EDGE ( 'NONE', *, *, #32788, .F. ) ;
#16704=CARTESIAN_POINT ( 'NONE',  ( 14.57025157893530043, -52.06302405750739837, -75.84958893011570069 ) ) ;
#16705=CARTESIAN_POINT ( 'NONE',  ( 47.33575985341339987, -54.69488657390869690, -54.69046143333279986 ) ) ;
#16708=CARTESIAN_POINT ( 'NONE',  ( 60.86909712740357747, -45.45332394799820719, -47.09890482454854066 ) ) ;
#16710=FACE_OUTER_BOUND ( 'NONE', #14428, .T. ) ;
#16711=CARTESIAN_POINT ( 'NONE',  ( 47.68046934622199728, -54.51757764637919479, -55.10164272630390059 ) ) ;
#16713=CARTESIAN_POINT ( 'NONE',  ( 12.89984684562703343, -50.74322487993451603, -21.40242722397054109 ) ) ;
#16717=CARTESIAN_POINT ( 'NONE',  ( 48.39474571203390241, 22.93079767860760043, -54.88276765605429830 ) ) ;
#16719=ORIENTED_EDGE ( 'NONE', *, *, #8461, .F. ) ;
#16727=CARTESIAN_POINT ( 'NONE',  ( 82.62217614637150120, 13.83472246775060022, -46.37143498965760102 ) ) ;
#16728=CARTESIAN_POINT ( 'NONE',  ( 53.41792665956379693, 17.70733950191389994, -26.73822481760680247 ) ) ;
#16732=CARTESIAN_POINT ( 'NONE',  ( 56.32875602673239968, -45.28046490780249655, -16.42171413587569972 ) ) ;
#16735=ORIENTED_EDGE ( 'NONE', *, *, #45449, .T. ) ;
#16738=CARTESIAN_POINT ( 'NONE',  ( 12.04145588157719970, -65.07204108492659600, -16.48289738546709771 ) ) ;
#16739=CARTESIAN_POINT ( 'NONE',  ( 10.92611299134039982, 33.35840257386460195, -46.27040258753400082 ) ) ;
#16741=CARTESIAN_POINT ( 'NONE',  ( 52.70905074378630673, -49.70817001306580352, -48.28317273910510465 ) ) ;
#16747=CARTESIAN_POINT ( 'NONE',  ( 49.20928845107640370, 22.41119391493339918, -54.30076444815649950 ) ) ;
#16748=EDGE_CURVE ( 'NONE', #4775, #13785, #36924, .T. ) ;
#16750=CARTESIAN_POINT ( 'NONE',  ( 50.85761971603020015, -50.68614562676760471, -76.14999999999999147 ) ) ;
#16754=DIRECTION ( 'NONE',  ( 0.4145156864928219997, 0.9100421669633689259, 0.000000000000000000 ) ) ;
#16759=CARTESIAN_POINT ( 'NONE',  ( 13.79441456740149974, -51.27878729324490337, -22.92979596798970121 ) ) ;
#16760=CARTESIAN_POINT ( 'NONE',  ( 53.62535340796430461, 20.09876804296569830, -75.58067205068070393 ) ) ;
#16761=CARTESIAN_POINT ( 'NONE',  ( 47.48804938961460209, -54.57746163137669981, -74.50208837960660446 ) ) ;
#16766=AXIS2_PLACEMENT_3D ( 'NONE', #10823, #6896, #14487 ) ;
#16767=CARTESIAN_POINT ( 'NONE',  ( 52.70648214874140081, -49.76125733399389617, -48.81430935866210064 ) ) ;
#16771=CARTESIAN_POINT ( 'NONE',  ( 46.35275103504439898, 21.67755452994670406, -76.14999999999999147 ) ) ;
#16772=CARTESIAN_POINT ( 'NONE',  ( 19.80201486048481030, -54.46428635315598399, -17.67512396564999833 ) ) ;
#16773=B_SPLINE_CURVE_WITH_KNOTS ( 'NONE', 3,
 ( #47811, #51733, #42130, #7459, #6230, #43873, #38196, #50256, #47310, #35494 ),
 .UNSPECIFIED., .F., .F.,
 ( 4, 2, 2, 2, 4 ),
 ( 0.000000000000000000, 0.2009658351805388987, 0.5348857748336580675, 0.9393348933166768555, 1.000000000000000000 ),
 .UNSPECIFIED. ) ;
#16777=CARTESIAN_POINT ( 'NONE',  ( 12.29622276841139872, 33.50355195994969648, -15.96315064374149983 ) ) ;
#16778=PLANE ( 'NONE',  #19696 ) ;
#16780=DIRECTION ( 'NONE',  ( -1.822422554782380175E-11, -1.784227544494129940E-11, -1.000000000000000000 ) ) ;
#16782=ADVANCED_FACE ( 'NONE', ( #49993 ), #14328, .T. ) ;
#16784=CARTESIAN_POINT ( 'NONE',  ( 61.33122422115619798, 14.00089233987130122, -46.85723822856199661 ) ) ;
#16785=CARTESIAN_POINT ( 'NONE',  ( -33.14787555410379838, -25.36774897639840276, -57.37579723497079698 ) ) ;
#16786=EDGE_CURVE ( 'NONE', #38464, #51752, #34411, .T. ) ;
#16788=CARTESIAN_POINT ( 'NONE',  ( 52.83465167515200278, -49.65874968186350458, -48.65907986970169929 ) ) ;
#16789=EDGE_CURVE ( 'NONE', #51255, #24834, #44989, .T. ) ;
#16790=CARTESIAN_POINT ( 'NONE',  ( 18.65687415773260582, -13.78316809304479662, -28.02168704970069868 ) ) ;
#16791=DIRECTION ( 'NONE',  ( 0.4646601886423053496, 0.000000000000000000, 0.8854890790353641128 ) ) ;
#16792=CARTESIAN_POINT ( 'NONE',  ( 56.29024440006210739, 14.53176988408540105, -25.89618347059580117 ) ) ;
#16794=ADVANCED_FACE ( 'NONE', ( #46071 ), #43638, .T. ) ;
#16795=CARTESIAN_POINT ( 'NONE',  ( 50.35727174223609381, 17.94937212879660038, -76.16289466383139484 ) ) ;
#16796=CARTESIAN_POINT ( 'NONE',  ( 52.87179753541859384, 18.40851527081879979, -48.76566975022370087 ) ) ;
#16798=DIRECTION ( 'NONE',  ( 1.000000000000000000, 0.000000000000000000, 0.000000000000000000 ) ) ;
#16799=CARTESIAN_POINT ( 'NONE',  ( 64.36428085589631110, -45.11618894467940066, -12.32250341870529908 ) ) ;
#16800=ORIENTED_EDGE ( 'NONE', *, *, #40826, .T. ) ;
#16804=CARTESIAN_POINT ( 'NONE',  ( 47.65145214304179433, -54.48884158768570529, -54.70160429609599362 ) ) ;
#16806=CARTESIAN_POINT ( 'NONE',  ( 13.39998208310050032, -51.78678246903520233, -23.15000000000000213 ) ) ;
#16807=CARTESIAN_POINT ( 'NONE',  ( 60.41042365232780043, 14.86001756475369895, -48.11601410346130336 ) ) ;
#16812=AXIS2_PLACEMENT_3D ( 'NONE', #7602, #31413, #11274 ) ;
#16815=ORIENTED_EDGE ( 'NONE', *, *, #13433, .T. ) ;
#16819=ORIENTED_EDGE ( 'NONE', *, *, #12652, .F. ) ;
#16820=EDGE_CURVE ( 'NONE', #39844, #11209, #18264, .T. ) ;
#16824=CARTESIAN_POINT ( 'NONE',  ( 52.21153807214869857, 19.18935477659329791, -76.55085343138060239 ) ) ;
#16832=CARTESIAN_POINT ( 'NONE',  ( 13.04106483549849926, -65.52043803436799863, -23.35241516560489927 ) ) ;
#16836=CARTESIAN_POINT ( 'NONE',  ( 14.51655170844479947, 20.71403734715240219, -75.77237669558989808 ) ) ;
#16837=CARTESIAN_POINT ( 'NONE',  ( 51.84382198560120258, 18.03478096587799939, -77.06468273675109515 ) ) ;
#16838=AXIS2_PLACEMENT_3D ( 'NONE', #46334, #2555, #10420 ) ;
#16840=CARTESIAN_POINT ( 'NONE',  ( 84.12560615065839897, -43.96699487611929413, -46.88422054015599372 ) ) ;
#16845=CARTESIAN_POINT ( 'NONE',  ( 53.08857600003049981, -49.42354551114720351, -27.55244750385169894 ) ) ;
#16846=CARTESIAN_POINT ( 'NONE',  ( 16.36412298843900004, -51.09682246409949613, -20.14982337726360129 ) ) ;
#16848=CARTESIAN_POINT ( 'NONE',  ( 54.51878663346509057, 12.23944275751169286, -7.640492836310381009 ) ) ;
#16853=CARTESIAN_POINT ( 'NONE',  ( -6.547816903263669275, -46.29994198797230354, -5.461245372614969895 ) ) ;
#16854=EDGE_CURVE ( 'NONE', #12115, #8205, #36096, .T. ) ;
#16855=CARTESIAN_POINT ( 'NONE',  ( 47.46651691217249436, 23.36841135167989947, -54.65114297014489608 ) ) ;
#16858=CARTESIAN_POINT ( 'NONE',  ( 41.93138973097610034, 13.29046345406609930, -5.197897844688459834 ) ) ;
#16860=FACE_OUTER_BOUND ( 'NONE', #51094, .T. ) ;
#16861=CARTESIAN_POINT ( 'NONE',  ( 83.95017614158776098, -44.74867211454660776, -47.46180894508327697 ) ) ;
#16863=CARTESIAN_POINT ( 'NONE',  ( 58.32272783024919960, -46.80742713280790213, -47.80927467149849974 ) ) ;
#16864=B_SPLINE_CURVE_WITH_KNOTS ( 'NONE', 3,
 ( #7526, #32106, #19568, #4605 ),
 .UNSPECIFIED., .F., .F.,
 ( 4, 4 ),
 ( 0.6437608425907387355, 1.000000000000000000 ),
 .UNSPECIFIED. ) ;
#16867=CARTESIAN_POINT ( 'NONE',  ( 17.52098156358690062, -52.86909850055779714, -76.12391999848780699 ) ) ;
#16869=CARTESIAN_POINT ( 'NONE',  ( 55.55365133010059964, 13.88381105532070059, -14.32025150907159983 ) ) ;
#16872=CARTESIAN_POINT ( 'NONE',  ( 9.292254072159270351, 32.01117642126040153, -46.52992118075790273 ) ) ;
#16873=CARTESIAN_POINT ( 'NONE',  ( 46.03122142033570441, 13.88381105532070059, -7.582879021622040305 ) ) ;
#16875=CARTESIAN_POINT ( 'NONE',  ( 66.71082852131469565, -30.88066898215729950, -17.22174391961319984 ) ) ;
#16876=ORIENTED_EDGE ( 'NONE', *, *, #5742, .F. ) ;
#16877=B_SPLINE_CURVE_WITH_KNOTS ( 'NONE', 3,
 ( #6849, #42753, #26476, #18879, #15477, #51122, #23056, #46431 ),
 .UNSPECIFIED., .F., .F.,
 ( 4, 2, 2, 4 ),
 ( 0.000000000000000000, 0.1749999999997750855, 0.3749999999995158317, 0.4999999271553960956 ),
 .UNSPECIFIED. ) ;
#16878=CARTESIAN_POINT ( 'NONE',  ( 18.06569355283950173, 20.03470611338460472, -74.90176971618339508 ) ) ;
#16879=VERTEX_POINT ( 'NONE', #6487 ) ;
#16880=ORIENTED_EDGE ( 'NONE', *, *, #22908, .F. ) ;
#16882=ADVANCED_FACE ( 'NONE', ( #38451 ), #38631, .T. ) ;
#16883=CARTESIAN_POINT ( 'NONE',  ( 12.21006104367689993, -65.32600393230370628, -46.80110686342489856 ) ) ;
#16886=CIRCLE ( 'NONE', #46185, 14.50000000000000178 ) ;
#16887=CARTESIAN_POINT ( 'NONE',  ( 61.68987301043100047, 13.88502391956650150, -46.42924174078329713 ) ) ;
#16888=ORIENTED_EDGE ( 'NONE', *, *, #5430, .T. ) ;
#16889=AXIS2_PLACEMENT_3D ( 'NONE', #30787, #7226, #23176 ) ;
#16892=CARTESIAN_POINT ( 'NONE',  ( 11.89321892218980103, -65.43602743108449715, -22.25048313876769868 ) ) ;
#16893=ORIENTED_EDGE ( 'NONE', *, *, #1875, .F. ) ;
#16894=CARTESIAN_POINT ( 'NONE',  ( 47.27830075994679504, -46.14751112267819622, -10.52819442205299971 ) ) ;
#16896=CARTESIAN_POINT ( 'NONE',  ( 15.21636614235080032, -50.60415920577569437, -15.65000000000000036 ) ) ;
#16899=DIRECTION ( 'NONE',  ( 0.000000000000000000, 0.000000000000000000, 1.000000000000000000 ) ) ;
#16900=DIRECTION ( 'NONE',  ( 0.000000000000000000, -8.635067969306036542E-13, -1.000000000000000000 ) ) ;
#16901=CARTESIAN_POINT ( 'NONE',  ( 61.25419824969329596, 14.37591664557439941, -47.68510568119449999 ) ) ;
#16902=EDGE_CURVE ( 'NONE', #4255, #46423, #34505, .T. ) ;
#16904=CARTESIAN_POINT ( 'NONE',  ( 51.64028867487969876, 13.97398019946970038, -12.35102539111250053 ) ) ;
#16906=CARTESIAN_POINT ( 'NONE',  ( -8.011283399686980999, 13.73034950201170012, -5.061381373397489725 ) ) ;
#16908=CARTESIAN_POINT ( 'NONE',  ( 60.17742417565860080, 14.13461826297539936, -26.93847057974990022 ) ) ;
#16913=CARTESIAN_POINT ( 'NONE',  ( 12.62473742531370036, 34.22812217844730043, -47.06777474994189703 ) ) ;
#16919=AXIS2_PLACEMENT_3D ( 'NONE', #29489, #2244, #25546 ) ;
#16923=CARTESIAN_POINT ( 'NONE',  ( 47.15609049642320372, 23.45578653585020135, -74.81054835449099016 ) ) ;
#16924=CARTESIAN_POINT ( 'NONE',  ( 49.51373360999449602, -53.70010315684200464, -54.78591011099970132 ) ) ;
#16928=CARTESIAN_POINT ( 'NONE',  ( 57.14903038794989953, 13.88381105532070059, -16.26185532857629923 ) ) ;
#16934=CARTESIAN_POINT ( 'NONE',  ( 61.16964974363630603, -45.44848929056309572, -47.43903885526919595 ) ) ;
#16936=CARTESIAN_POINT ( 'NONE',  ( 46.02646716740153465, -43.52997999968917497, -5.570501089956091612 ) ) ;
#16940=CARTESIAN_POINT ( 'NONE',  ( 68.13393739769620083, -15.61618894467929941, -65.65000000000000568 ) ) ;
#16942=CARTESIAN_POINT ( 'NONE',  ( 84.24389573796460695, -44.17152221330420048, -47.41156961578170126 ) ) ;
#16947=CARTESIAN_POINT ( 'NONE',  ( 53.36551680243020002, -49.48411605007570557, -49.20677719568929831 ) ) ;
#16949=CARTESIAN_POINT ( 'NONE',  ( 76.45881442385368132, -5.621145002420384174, -13.04994345818161072 ) ) ;
#16952=EDGE_LOOP ( 'NONE', ( #5695, #14504, #16687 ) ) ;
#16953=EDGE_LOOP ( 'NONE', ( #34446, #31332, #24775, #46572, #24654, #20010 ) ) ;
#16957=CARTESIAN_POINT ( 'NONE',  ( 13.73527022026340028, -50.20735447812900532, -20.93080062776369843 ) ) ;
#16962=ORIENTED_EDGE ( 'NONE', *, *, #15203, .F. ) ;
#16964=VECTOR ( 'NONE', #41901, 1000.000000000000114 ) ;
#16965=CARTESIAN_POINT ( 'NONE',  ( 52.47683827954009672, -49.96152992937280857, -77.24560335664398281 ) ) ;
#16967=DIRECTION ( 'NONE',  ( -0.9441882088883221114, -0.3294064756440929775, 0.000000000000000000 ) ) ;
#16968=EDGE_CURVE ( 'NONE', #19040, #3407, #32986, .T. ) ;
#16972=CARTESIAN_POINT ( 'NONE',  ( 41.90536115952740204, -44.14555587430140093, -4.781910971784859576 ) ) ;
#16973=DIRECTION ( 'NONE',  ( 0.000000000000000000, 0.000000000000000000, 1.000000000000000000 ) ) ;
#16974=EDGE_CURVE ( 'NONE', #41755, #34714, #15385, .T. ) ;
#16976=CARTESIAN_POINT ( 'NONE',  ( 61.50420641992440096, -45.37395360146110335, -47.35413577371650007 ) ) ;
#16978=CARTESIAN_POINT ( 'NONE',  ( -11.00461184790393432, 20.00401265374111759, -51.06967761013340379 ) ) ;
#16979=CARTESIAN_POINT ( 'NONE',  ( 66.62369684436269779, 1.869841767515120212, -20.10141910231079976 ) ) ;
#16980=EDGE_LOOP ( 'NONE', ( #22630, #24097 ) ) ;
#16981=CARTESIAN_POINT ( 'NONE',  ( 13.60694591982639956, -51.71967070379349707, -74.96248001587449039 ) ) ;
#16982=CARTESIAN_POINT ( 'NONE',  ( 47.32222669057270537, -54.70165496723960530, -54.63504270530570039 ) ) ;
#16987=DIRECTION ( 'NONE',  ( 0.000000000000000000, 0.000000000000000000, -1.000000000000000000 ) ) ;
#16989=CARTESIAN_POINT ( 'NONE',  ( 47.82353814990229779, -54.39218320395399786, -54.71742302521079893 ) ) ;
#16990=CARTESIAN_POINT ( 'NONE',  ( 14.03113113058140016, 19.93369484661189617, -22.86118033164979835 ) ) ;
#16991=CARTESIAN_POINT ( 'NONE',  ( -10.40242566545200020, -42.83441872489630242, -6.165522616775290565 ) ) ;
#16992=CARTESIAN_POINT ( 'NONE',  ( 56.32099966199259455, 19.34387771064809769, -52.90109585754750299 ) ) ;
#16993=CARTESIAN_POINT ( 'NONE',  ( 48.44635283126329739, 22.88212911225959800, -54.78388658047989423 ) ) ;
#16994=ORIENTED_EDGE ( 'NONE', *, *, #36590, .F. ) ;
#16997=CIRCLE ( 'NONE', #14485, 2.000000000000000000 ) ;
#17002=CARTESIAN_POINT ( 'NONE',  ( 83.24078296369471275, 13.59326884860229967, -46.48094294254000403 ) ) ;
#17003=CARTESIAN_POINT ( 'NONE',  ( 53.57711009519410084, 17.56838801165940112, -26.77252265506880136 ) ) ;
#17005=CARTESIAN_POINT ( 'NONE',  ( 82.55417034916339958, -45.62620260807315020, -47.70637854188411353 ) ) ;
#17006=CARTESIAN_POINT ( 'NONE',  ( 55.75440718692259878, -45.11618894467940066, -14.47054954719470032 ) ) ;
#17010=CARTESIAN_POINT ( 'NONE',  ( 11.90346178786399811, -64.96824711458259571, -16.35924802167970427 ) ) ;
#17011=CARTESIAN_POINT ( 'NONE',  ( 12.20877050462410018, 34.09266550635960158, -46.79949035583759809 ) ) ;
#17012=CARTESIAN_POINT ( 'NONE',  ( 61.05618096262753625, -45.35086615659341902, -46.88538666599615112 ) ) ;
#17013=CARTESIAN_POINT ( 'NONE',  ( 52.17625961327589579, -50.29609475764150517, -49.30498256536409940 ) ) ;
#17015=EDGE_LOOP ( 'NONE', ( #28776, #20581, #3436, #40595 ) ) ;
#17016=CARTESIAN_POINT ( 'NONE',  ( 11.13393739769619906, 24.07008072128950005, -43.74348518090240390 ) ) ;
#17020=CARTESIAN_POINT ( 'NONE',  ( 50.03007040746729928, -48.61618473956929876, -76.14999999999999147 ) ) ;
#17027=LINE ( 'NONE', #20933, #16964 ) ;
#17029=EDGE_CURVE ( 'NONE', #13057, #46423, #16143, .T. ) ;
#17030=CARTESIAN_POINT ( 'NONE',  ( 13.61605695543079975, -51.38252537174340517, -22.70458615691660142 ) ) ;
#17031=FACE_OUTER_BOUND ( 'NONE', #39206, .T. ) ;
#17032=CARTESIAN_POINT ( 'NONE',  ( 47.39374880179290273, -54.43861217925859819, -75.00425604315580586 ) ) ;
#17034=CARTESIAN_POINT ( 'NONE',  ( 55.91593944087500034, 14.67229672235290039, -17.77972553223289864 ) ) ;
#17035=CARTESIAN_POINT ( 'NONE',  ( 57.03355805182570037, -50.46038680774910290, -53.04057969670439832 ) ) ;
#17038=CARTESIAN_POINT ( 'NONE',  ( 46.73880816492100365, 22.29221772442059901, -76.02645024177060407 ) ) ;
#17040=DIRECTION ( 'NONE',  ( -1.000000000000000000, 2.473715676742926917E-14, 0.000000000000000000 ) ) ;
#17041=CARTESIAN_POINT ( 'NONE',  ( 12.36320305067610015, 33.31445045643330616, -15.76422791930239953 ) ) ;
#17042=CARTESIAN_POINT ( 'NONE',  ( 12.13393739769630031, -55.41568642894329599, -76.14999999999999147 ) ) ;
#17043=EDGE_CURVE ( 'NONE', #32099, #31690, #38666, .T. ) ;
#17049=EDGE_CURVE ( 'NONE', #17080, #13415, #7264, .T. ) ;
#17051=CARTESIAN_POINT ( 'NONE',  ( -0.3561701380305670184, -63.29997699608469475, -50.35138997524259707 ) ) ;
#17053=CARTESIAN_POINT ( 'NONE',  ( 52.74229065118059623, -49.71327796806070154, -48.57746011431329691 ) ) ;
#17055=CARTESIAN_POINT ( 'NONE',  ( 49.72648160330889766, -53.64673639094029767, -55.11972614036120177 ) ) ;
#17056=CARTESIAN_POINT ( 'NONE',  ( 13.29207020058240118, 19.63039169006109930, -21.61097671908079931 ) ) ;
#17057=CARTESIAN_POINT ( 'NONE',  ( 57.41578767303399644, 14.06885415636270054, -25.91887996722570264 ) ) ;
#17059=CARTESIAN_POINT ( 'NONE',  ( 50.92008762292839918, 19.20681001037759827, -76.16477590611239634 ) ) ;
#17060=CARTESIAN_POINT ( 'NONE',  ( 53.50263409105239987, 18.15269513763240283, -49.11500990822519697 ) ) ;
#17062=CARTESIAN_POINT ( 'NONE',  ( 40.36721523010999846, -44.88645108046029719, -4.296538310233220415 ) ) ;
#17063=CARTESIAN_POINT ( 'NONE',  ( 46.81019908227018789, 22.25026678916544753, -76.02856692465805111 ) ) ;
#17069=CARTESIAN_POINT ( 'NONE',  ( 47.48443198299139567, -54.60544348543930226, -54.82495138136360424 ) ) ;
#17073=CARTESIAN_POINT ( 'NONE',  ( 57.31413766567600021, 18.54505573934330087, -52.15320908590850024 ) ) ;
#17074=CARTESIAN_POINT ( 'NONE',  ( 52.98014233026830055, 18.34975111832529748, -48.77045026161920305 ) ) ;
#17075=PLANE ( 'NONE',  #35134 ) ;
#17078=DIRECTION ( 'NONE',  ( -1.000000000000000000, 0.000000000000000000, 0.000000000000000000 ) ) ;
#17080=VERTEX_POINT ( 'NONE', #23471 ) ;
#17081=ORIENTED_EDGE ( 'NONE', *, *, #4200, .T. ) ;
#17082=CARTESIAN_POINT ( 'NONE',  ( 8.792282373222519709, -63.15413706425750462, -46.67070408018280148 ) ) ;
#17086=DIRECTION ( 'NONE',  ( 0.5547001962252313678, 0.000000000000000000, 0.8320502943378423888 ) ) ;
#17088=CARTESIAN_POINT ( 'NONE',  ( 52.30891881186520465, 19.23820029767140127, -76.54990093770538806 ) ) ;
#17094=VECTOR ( 'NONE', #20927, 1000.000000000000000 ) ;
#17095=EDGE_CURVE ( 'NONE', #566, #9786, #14905, .T. ) ;
#17096=CARTESIAN_POINT ( 'NONE',  ( 53.70553476669380188, 20.08271752784780162, -75.56421356237311215 ) ) ;
#17099=CARTESIAN_POINT ( 'NONE',  ( 11.69299373377159945, -65.25245614431548802, -23.21666815710909759 ) ) ;
#17101=CARTESIAN_POINT ( 'NONE',  ( 44.34217248106909892, 14.86060539202009956, -8.529414471301580036 ) ) ;
#17102=CONICAL_SURFACE ( 'NONE', #9577, 1.715179901029911802, 0.08257045569470247703 ) ;
#17103=CARTESIAN_POINT ( 'NONE',  ( 14.14316338426450059, 20.82672717200830093, -75.71427953954510315 ) ) ;
#17105=CARTESIAN_POINT ( 'NONE',  ( 51.90728449415519918, 18.14319716981249897, -77.08408619744250245 ) ) ;
#17106=CARTESIAN_POINT ( 'NONE',  ( 83.93027249483731111, -44.24138390648490571, -46.75947739037560069 ) ) ;
#17109=CARTESIAN_POINT ( 'NONE',  ( 53.65698216514989838, -48.90957431119100107, -27.12425740866480339 ) ) ;
#17110=CARTESIAN_POINT ( 'NONE',  ( 16.35031946893619903, -51.11201358154099950, -20.80740584792820158 ) ) ;
#17115=CARTESIAN_POINT ( 'NONE',  ( 68.13393739769620083, -49.36618894467930829, -76.75000000000000000 ) ) ;
#17117=CARTESIAN_POINT ( 'NONE',  ( -7.621746992312569802, -45.29489141125190343, -5.208053594245360074 ) ) ;
#17118=CARTESIAN_POINT ( 'NONE',  ( 47.23856716980339598, 23.53214383509299878, -54.65873215110720196 ) ) ;
#17121=CARTESIAN_POINT ( 'NONE',  ( 11.09248976068989911, 33.92026768257339597, -17.64371789481230124 ) ) ;
#17125=CARTESIAN_POINT ( 'NONE',  ( 57.08353988017420022, -47.57643501793450014, -48.30860928975249635 ) ) ;
#17126=CARTESIAN_POINT ( 'NONE',  ( 10.72855169901638561, 33.70933666265226236, -18.17421237785139709 ) ) ;
#17128=CARTESIAN_POINT ( 'NONE',  ( 54.44122174944140369, 20.40605896927280227, -54.00583347857779870 ) ) ;
#17133=CARTESIAN_POINT ( 'NONE',  ( 8.978915886419921222, 32.05342364452790349, -46.63388789120410394 ) ) ;
#17135=VECTOR ( 'NONE', #11506, 1000.000000000000000 ) ;
#17136=CARTESIAN_POINT ( 'NONE',  ( 67.87921200600509053, -30.71850411471519848, -17.86500106063319748 ) ) ;
#17138=CARTESIAN_POINT ( 'NONE',  ( 17.98151656396600018, 19.91124285304369934, -74.53071772762450564 ) ) ;
#17139=ORIENTED_EDGE ( 'NONE', *, *, #16610, .F. ) ;
#17140=VERTEX_POINT ( 'NONE', #15641 ) ;
#17141=CARTESIAN_POINT ( 'NONE',  ( 47.96474501199910634, 23.16479111562100002, -55.26734477448599847 ) ) ;
#17143=EDGE_LOOP ( 'NONE', ( #23369, #11355, #713, #37528 ) ) ;
#17144=CARTESIAN_POINT ( 'NONE',  ( 10.36556321007419967, -63.68101588646130296, -45.87904799880939777 ) ) ;
#17145=CARTESIAN_POINT ( 'NONE',  ( 56.71466712695590218, -45.83984592708740280, -26.16804175456279680 ) ) ;
#17147=CARTESIAN_POINT ( 'NONE',  ( 61.62976647988480039, 13.89047783355900023, -46.42559179425300186 ) ) ;
#17149=VERTEX_POINT ( 'NONE', #8029 ) ;
#17152=VERTEX_POINT ( 'NONE', #19822 ) ;
#17153=CARTESIAN_POINT ( 'NONE',  ( 49.68658769026319533, -45.96991040253789862, -12.09272027885839940 ) ) ;
#17156=DIRECTION ( 'NONE',  ( 6.940534999999999567E-13, 2.999089000000000026E-13, 1.000000000000000000 ) ) ;
#17160=EDGE_CURVE ( 'NONE', #37505, #19930, #35020, .T. ) ;
#17161=DIRECTION ( 'NONE',  ( 0.000000000000000000, 1.000000000000000000, 0.000000000000000000 ) ) ;
#17162=CARTESIAN_POINT ( 'NONE',  ( 47.20319696544930110, -54.79145866998830172, -74.14999999999999147 ) ) ;
#17163=CARTESIAN_POINT ( 'NONE',  ( 70.65074043265579462, 13.88381329038599965, -13.75217218087989934 ) ) ;
#17164=EDGE_CURVE ( 'NONE', #22272, #10985, #34283, .T. ) ;
#17165=CARTESIAN_POINT ( 'NONE',  ( 53.92601192165510327, 15.01257601730690006, -15.35060719856840095 ) ) ;
#17169=CARTESIAN_POINT ( 'NONE',  ( 58.59489568202110377, 14.12396963892440027, -26.25482318927760161 ) ) ;
#17171=B_SPLINE_SURFACE_WITH_KNOTS ( 'NONE', 3, 3, ( 
 ( #44108, #7949, #8207, #32528, #7705, #32276, #43602, #23648, #39924, #40173 ),
 ( #12146, #4268, #16573, #20492, #51465, #27595, #35975, #51714, #15808, #94 ),
 ( #28100, #28358, #44362, #20238, #36228, #16323, #36483, #3514, #48047, #48298 ),
 ( #8467, #35473, #39664, #12395, #47791, #40426, #19981, #16066, #48556, #32022 ),
 ( #11897, #27852, #39414, #24414, #43853, #12664, #28617, #44618, #15564, #23388 ),
 ( #31518, #47536, #11633, #49090, #41462, #13695, #41722, #45660, #5317, #1377 ),
 ( #16846, #1895, #13193, #17872, #24934, #49347, #29655, #40687, #13948, #9763 ),
 ( #25714, #5829, #21792, #17110, #5057, #33843, #29907, #48818, #25202, #37015 ),
 ( #37800, #25457, #29405, #45405, #49859, #12926, #17364, #8724, #24674, #4787 ),
 ( #20755, #1114, #36742, #32795, #29142, #28882, #21273, #5578, #849, #33331 ) ),
 .UNSPECIFIED., .F., .F., .F.,
 ( 4, 1, 1, 1, 1, 1, 1, 4 ),
 ( 4, 2, 2, 2, 4 ),
 ( -7.647483565995659741E-05, 0.1428571428571430157, 0.2857142857142860315, 0.4285714285714289917, 0.5714285714285709528, 0.7142857142857139685, 0.8571428571428569843, 1.000068219203670061 ),
 ( -7.344577000600000058E-05, 0.1578379958887999868, 0.4200977637876570081, 0.7377509475170059838, 0.8959923838504209037 ),
 .UNSPECIFIED. ) ;
#17172=VERTEX_POINT ( 'NONE', #13528 ) ;
#17173=CARTESIAN_POINT ( 'NONE',  ( 60.26929283095309842, 14.55540890537130139, -47.49574889169500125 ) ) ;
#17174=CARTESIAN_POINT ( 'NONE',  ( -11.32756405082269957, -41.88149022528619980, -6.268906610209949548 ) ) ;
#17175=CARTESIAN_POINT ( 'NONE',  ( 15.36759650335590166, -50.68854986405820284, -15.64999996598500154 ) ) ;
#17177=EDGE_CURVE ( 'NONE', #30462, #48001, #17417, .T. ) ;
#17178=DIRECTION ( 'NONE',  ( 0.000000000000000000, 0.000000000000000000, -1.000000000000000000 ) ) ;
#17180=CARTESIAN_POINT ( 'NONE',  ( 47.09613377138079926, 23.32416568916539745, -75.12131136925759733 ) ) ;
#17181=CARTESIAN_POINT ( 'NONE',  ( 49.48213591681090406, -53.75081833664800257, -55.18208724449640101 ) ) ;
#17182=CARTESIAN_POINT ( 'NONE',  ( 51.18395887421012702, -31.66627047883219248, -17.12905876552815698 ) ) ;
#17183=CARTESIAN_POINT ( 'NONE',  ( 76.76118738540560571, -43.17102546891605641, -14.50675714471237931 ) ) ;
#17190=CARTESIAN_POINT ( 'NONE',  ( 60.76390515915409907, -45.61011419412700008, -47.53678005598290213 ) ) ;
#17191=CARTESIAN_POINT ( 'NONE',  ( 56.84932596551129791, 19.42421318737730118, -53.85230338955989993 ) ) ;
#17192=CARTESIAN_POINT ( 'NONE',  ( 60.86353915101335588, -43.43619376203384519, -9.316164839326646074 ) ) ;
#17198=VERTEX_POINT ( 'NONE', #45490 ) ;
#17199=VECTOR ( 'NONE', #49713, 1000.000000000000000 ) ;
#17200=ORIENTED_EDGE ( 'NONE', *, *, #17729, .T. ) ;
#17202=ORIENTED_EDGE ( 'NONE', *, *, #22352, .F. ) ;
#17203=CARTESIAN_POINT ( 'NONE',  ( 61.65765287950929974, -45.18895564470849990, -46.92879811375530608 ) ) ;
#17205=CARTESIAN_POINT ( 'NONE',  ( 54.49456226560189975, -51.49951853336879992, -53.42564530602280115 ) ) ;
#17210=CARTESIAN_POINT ( 'NONE',  ( 56.52536539877740296, 19.51942783438209972, -53.84278118897309895 ) ) ;
#17212=CARTESIAN_POINT ( 'NONE',  ( 16.13393739769620083, -15.61618894467929941, -17.89999999999999858 ) ) ;
#17213=CARTESIAN_POINT ( 'NONE',  ( 8.812257860101720297, -63.26324333009419831, -46.67111697731629505 ) ) ;
#17216=CARTESIAN_POINT ( 'NONE',  ( 57.36123081458359962, -50.13537923174280309, -52.61896056486340001 ) ) ;
#17217=CARTESIAN_POINT ( 'NONE',  ( 52.96724630752039786, -50.54849023173969869, -76.71296415157679860 ) ) ;
#17224=CARTESIAN_POINT ( 'NONE',  ( 45.93003902655789972, 13.88381108677270070, -7.538626085152499989 ) ) ;
#17225=CARTESIAN_POINT ( 'NONE',  ( 41.49029323204549513, -44.57544611689359471, -5.136314801332729552 ) ) ;
#17227=CARTESIAN_POINT ( 'NONE',  ( 61.43330014371199610, -45.44825325816589867, -47.47801797575630189 ) ) ;
#17231=CARTESIAN_POINT ( 'NONE',  ( 66.86288126489500883, 1.795758268595449847, -19.74634579401690360 ) ) ;
#17232=VERTEX_POINT ( 'NONE', #4350 ) ;
#17233=CARTESIAN_POINT ( 'NONE',  ( 14.51934924390189963, -51.60940715663139855, -75.47164421335219231 ) ) ;
#17234=CARTESIAN_POINT ( 'NONE',  ( 57.33058001265040104, 19.23207308441419983, -53.14947967088009761 ) ) ;
#17236=CARTESIAN_POINT ( 'NONE',  ( 83.92831069525388443, 12.99935915314664037, -46.72265495489138942 ) ) ;
#17239=CARTESIAN_POINT ( 'NONE',  ( 55.45161425650417186, -46.01554884395809353, -16.61969664790585810 ) ) ;
#17240=CARTESIAN_POINT ( 'NONE',  ( 47.73911847905110051, -54.48427846072730318, -54.99607381330790901 ) ) ;
#17242=CARTESIAN_POINT ( 'NONE',  ( 14.54299284624212341, -46.73222572554120546, -21.73578643762710527 ) ) ;
#17243=CARTESIAN_POINT ( 'NONE',  ( 56.33032549915870391, 19.43049768199900029, -53.07630012612180082 ) ) ;
#17244=CARTESIAN_POINT ( 'NONE',  ( 48.71617454467180153, 22.66482838071829775, -54.49917290083569554 ) ) ;
#17245=ORIENTED_EDGE ( 'NONE', *, *, #31202, .F. ) ;
#17248=CIRCLE ( 'NONE', #46560, 1.999999999984542365 ) ;
#17250=DIRECTION ( 'NONE',  ( 0.000000000000000000, 0.000000000000000000, 1.000000000000000000 ) ) ;
#17252=CARTESIAN_POINT ( 'NONE',  ( 82.86439673227779679, 14.20358350717769902, -47.48719404937710209 ) ) ;
#17253=CARTESIAN_POINT ( 'NONE',  ( 52.98397839259559561, 18.23000655168990036, -27.44922917074499935 ) ) ;
#17254=EDGE_CURVE ( 'NONE', #30077, #24770, #37464, .T. ) ;
#17258=CARTESIAN_POINT ( 'NONE',  ( 57.34776334542480214, -45.81180625069929846, -26.27178910182970029 ) ) ;
#17260=EDGE_CURVE ( 'NONE', #9581, #22075, #4228, .T. ) ;
#17264=CARTESIAN_POINT ( 'NONE',  ( 11.63839622732749923, -64.98507644367438729, -16.51998659930730184 ) ) ;
#17265=CARTESIAN_POINT ( 'NONE',  ( 12.14904065733069949, 34.04125641336589325, -46.43067368610769563 ) ) ;
#17268=DIRECTION ( 'NONE',  ( 0.000000000000000000, 0.000000000000000000, -1.000000000000000000 ) ) ;
#17269=VECTOR ( 'NONE', #28169, 1000.000000000000000 ) ;
#17275=DIRECTION ( 'NONE',  ( 0.000000000000000000, 1.000000000000000000, 0.000000000000000000 ) ) ;
#17277=CARTESIAN_POINT ( 'NONE',  ( 50.12047694534370379, -49.40224992130570314, -76.14999999999999147 ) ) ;
#17278=LINE ( 'NONE', #5485, #17905 ) ;
#17281=CARTESIAN_POINT ( 'NONE',  ( 68.13393739769649926, -48.11618894468163887, -75.95000000000023022 ) ) ;
#17283=CARTESIAN_POINT ( 'NONE',  ( 56.46551647426587550, -50.77616449088402817, -74.41179840258179468 ) ) ;
#17284=CARTESIAN_POINT ( 'NONE',  ( 68.13393739769620083, 17.38381105532069881, -65.65000000000000568 ) ) ;
#17285=EDGE_CURVE ( 'NONE', #28130, #21618, #8536, .T. ) ;
#17287=CARTESIAN_POINT ( 'NONE',  ( 14.03111719544759950, -51.16607778725470013, -22.86119529785250037 ) ) ;
#17289=CARTESIAN_POINT ( 'NONE',  ( 47.49946256140629686, -54.59426934545189880, -74.36173831268348522 ) ) ;
#17291=CARTESIAN_POINT ( 'NONE',  ( 56.10793225295759612, 14.17759732785500049, -16.53469904412530056 ) ) ;
#17292=CARTESIAN_POINT ( 'NONE',  ( 56.96373072582949959, -50.33643366695780230, -52.80952917442810701 ) ) ;
#17293=AXIS2_PLACEMENT_3D ( 'NONE', #32026, #8472, #7444 ) ;
#17298=CARTESIAN_POINT ( 'NONE',  ( 47.45608139774180501, 23.29801033333230009, -74.72332766641309831 ) ) ;
#17299=CARTESIAN_POINT ( 'NONE',  ( 20.02454065068388189, -55.10211906991936104, -18.88252341927455902 ) ) ;
#17300=CARTESIAN_POINT ( 'NONE',  ( 75.12017559335848205, -26.67552810556109932, -11.65274274207780714 ) ) ;
#17301=CARTESIAN_POINT ( 'NONE',  ( 12.36320305067610015, 33.31445045643330616, -15.76422791930239953 ) ) ;
#17305=CARTESIAN_POINT ( 'NONE',  ( 11.89321892218980103, -65.43602743108449715, -22.25048313876769868 ) ) ;
#17308=CARTESIAN_POINT ( 'NONE',  ( 21.78494278233659998, -33.82423023735729828, -74.14999999999999147 ) ) ;
#17309=CARTESIAN_POINT ( 'NONE',  ( -0.1608700869902630060, -61.64316105046779626, -48.65898601561310244 ) ) ;
#17310=VERTEX_POINT ( 'NONE', #1719 ) ;
#17311=CARTESIAN_POINT ( 'NONE',  ( 53.04797527815239988, -49.54715477933019940, -48.83268162150049818 ) ) ;
#17312=CARTESIAN_POINT ( 'NONE',  ( 60.14908144350449959, -45.12251587736449210, -26.30467219823789904 ) ) ;
#17314=CARTESIAN_POINT ( 'NONE',  ( 56.79136515448639955, 14.01381614805959863, -25.29529548441849940 ) ) ;
#17316=CARTESIAN_POINT ( 'NONE',  ( 51.12155852695169500, 18.48105606206009810, -76.32652952292480109 ) ) ;
#17317=CARTESIAN_POINT ( 'NONE',  ( 53.11153472725679592, 18.30627989090099916, -49.01452488218580328 ) ) ;
#17319=DIRECTION ( 'NONE',  ( 0.000000000000000000, 0.000000000000000000, 1.000000000000000000 ) ) ;
#17322=VECTOR ( 'NONE', #2391, 1000.000000000000000 ) ;
#17323=VERTEX_POINT ( 'NONE', #51168 ) ;
#17327=CARTESIAN_POINT ( 'NONE',  ( 47.40072637641420528, -54.65652856110890667, -54.81947631438220014 ) ) ;
#17331=LINE ( 'NONE', #33294, #10403 ) ;
#17337=ORIENTED_EDGE ( 'NONE', *, *, #40177, .T. ) ;
#17338=CARTESIAN_POINT ( 'NONE',  ( 9.745678311054680520, -63.30192500947659795, -46.29763742019599704 ) ) ;
#17339=CARTESIAN_POINT ( 'NONE',  ( 15.67962062535580081, -50.86266781815560023, -15.65622421709140077 ) ) ;
#17341=CARTESIAN_POINT ( 'NONE',  ( 11.13393739477719890, -63.63465712356870796, -43.78329177822379847 ) ) ;
#17343=FACE_OUTER_BOUND ( 'NONE', #45377, .T. ) ;
#17344=CARTESIAN_POINT ( 'NONE',  ( 52.19402247633719583, 19.67376017629629814, -76.20338399122979922 ) ) ;
#17346=LINE ( 'NONE', #33313, #51076 ) ;
#17347=CIRCLE ( 'NONE', #44116, 18.00000000000000355 ) ;
#17353=ADVANCED_FACE ( 'NONE', ( #37886 ), #5888, .T. ) ;
#17355=CARTESIAN_POINT ( 'NONE',  ( 57.17168871552530618, -45.85041182722559228, -26.25507473453999907 ) ) ;
#17358=CARTESIAN_POINT ( 'NONE',  ( 13.48116298479809849, 20.36471648394369893, -74.34810712130391153 ) ) ;
#17359=CARTESIAN_POINT ( 'NONE',  ( 17.63529210099531142, -51.92835184178156993, -75.76245441612823583 ) ) ;
#17363=CARTESIAN_POINT ( 'NONE',  ( 53.11249465950879767, -49.29926820387549924, -27.16890043460400150 ) ) ;
#17364=CARTESIAN_POINT ( 'NONE',  ( 15.45006552727480020, -51.11619292586900087, -21.87030236029440289 ) ) ;
#17365=CARTESIAN_POINT ( 'NONE',  ( 12.63912502739619903, 33.58996157896420698, -16.00788927292039787 ) ) ;
#17366=LINE ( 'NONE', #13952, #4553 ) ;
#17368=EDGE_LOOP ( 'NONE', ( #15120, #31677, #31347, #9480 ) ) ;
#17369=CARTESIAN_POINT ( 'NONE',  ( -11.32734370190460105, -41.88171845330919751, -6.430192534648670133 ) ) ;
#17370=CARTESIAN_POINT ( 'NONE',  ( 47.21062522706190379, 23.55319570774130256, -54.63464825132839309 ) ) ;
#17371=CIRCLE ( 'NONE', #5675, 0.9999999999999991118 ) ;
#17372=CARTESIAN_POINT ( 'NONE',  ( 56.50535457420483709, -50.75957590060649238, -53.84464170001397321 ) ) ;
#17374=CARTESIAN_POINT ( 'NONE',  ( 56.02488392748924895, 15.50430221806558606, -26.35754376592503689 ) ) ;
#17375=CARTESIAN_POINT ( 'NONE',  ( 11.63826667102929946, 34.15960232121609863, -17.83149736357780313 ) ) ;
#17376=DIRECTION ( 'NONE',  ( 0.000000000000000000, 0.000000000000000000, -1.000000000000000000 ) ) ;
#17378=FACE_OUTER_BOUND ( 'NONE', #27313, .T. ) ;
#17379=CARTESIAN_POINT ( 'NONE',  ( 57.73173547914959158, -47.11702968912669576, -47.92373006181999529 ) ) ;
#17380=CARTESIAN_POINT ( 'NONE',  ( 53.40280527584940273, 17.93096761773750103, -27.32835562702450005 ) ) ;
#17382=CIRCLE ( 'NONE', #3174, 4.960803362786369242 ) ;
#17383=CARTESIAN_POINT ( 'NONE',  ( 55.90187133018510224, 19.50246215684880013, -52.91463811559199826 ) ) ;
#17385=CARTESIAN_POINT ( 'NONE',  ( 55.00116069800729690, 13.88381105532070059, -13.90662172087169957 ) ) ;
#17386=ORIENTED_EDGE ( 'NONE', *, *, #9913, .T. ) ;
#17387=CARTESIAN_POINT ( 'NONE',  ( 18.86789271246039945, 20.55440458018300021, -15.81497037201279987 ) ) ;
#17388=CARTESIAN_POINT ( 'NONE',  ( 9.745662885843259460, 32.06938234726919745, -46.29763386374680323 ) ) ;
#17391=CARTESIAN_POINT ( 'NONE',  ( 67.25969285220541849, -30.55435842736649832, -17.44085799406789761 ) ) ;
#17392=CARTESIAN_POINT ( 'NONE',  ( 18.03195613579949708, 20.10714342530040000, -75.06145659859170394 ) ) ;
#17394=ORIENTED_EDGE ( 'NONE', *, *, #33300, .T. ) ;
#17395=CARTESIAN_POINT ( 'NONE',  ( 49.22498099147640005, 22.62797864033339934, -55.23666898610209586 ) ) ;
#17397=CARTESIAN_POINT ( 'NONE',  ( 9.877817271165479696, -63.39606316702139566, -46.22144567296060558 ) ) ;
#17398=CARTESIAN_POINT ( 'NONE',  ( 57.43249943431290205, -45.60969068493010070, -26.20294208203680242 ) ) ;
#17401=CARTESIAN_POINT ( 'NONE',  ( 61.73009041877960357, 13.88381044681140075, -46.43160995025269244 ) ) ;
#17403=VERTEX_POINT ( 'NONE', #42109 ) ;
#17404=CARTESIAN_POINT ( 'NONE',  ( 75.24562878474803540, 2.899702436808165640, -12.26857522025693825 ) ) ;
#17406=CARTESIAN_POINT ( 'NONE',  ( 53.14291664956020611, -45.11618894460600160, -12.84078445876880004 ) ) ;
#17412=CARTESIAN_POINT ( 'NONE',  ( 47.18055146300900304, -54.80119377569329941, -74.36335264244719667 ) ) ;
#17413=CARTESIAN_POINT ( 'NONE',  ( 60.83513156569119928, 14.48683582043410034, -47.74920551991019835 ) ) ;
#17414=CARTESIAN_POINT ( 'NONE',  ( 47.61773923874600456, 14.33581883698849957, -10.25420216154219943 ) ) ;
#17415=ADVANCED_FACE ( 'NONE', ( #5951 ), #25517, .T. ) ;
#17416=AXIS2_PLACEMENT_3D ( 'NONE', #601, #44631, #16586 ) ;
#17417=B_SPLINE_CURVE_WITH_KNOTS ( 'NONE', 3,
 ( #20318, #8808, #1458, #36307, #28966, #13268, #17448, #25285, #16404, #40513, #1200, #672, #49431, #40770, #4871, #29485 ),
 .UNSPECIFIED., .F., .F.,
 ( 4, 2, 2, 2, 2, 2, 2, 4 ),
 ( -1.909583999999999989E-14, 0.4484665168913320454, 0.8527180250750849844, 1.105375217689929856, 1.263285963074209928, 1.579107453842770070, 2.084421839072459814, 2.526571926148439839 ),
 .UNSPECIFIED. ) ;
#17420=DIRECTION ( 'NONE',  ( -0.9899494936611664686, 0.000000000000000000, 0.1414213562373098920 ) ) ;
#17421=CARTESIAN_POINT ( 'NONE',  ( 10.62796209095821354, 24.00384274327042888, -21.20043923476212910 ) ) ;
#17422=CARTESIAN_POINT ( 'NONE',  ( 59.23839464417140022, 13.99532105124600001, -26.26701623619180026 ) ) ;
#17425=CARTESIAN_POINT ( 'NONE',  ( 53.58118161341838004, 18.18361553717124579, -49.23682030730962822 ) ) ;
#17426=CARTESIAN_POINT ( 'NONE',  ( -10.62062192548610007, -41.45185578373610014, -4.375821978402089307 ) ) ;
#17428=B_SPLINE_CURVE_WITH_KNOTS ( 'NONE', 3,
 ( #15262, #23347, #7146, #6890, #23605, #31218, #39116, #3210, #6622, #26517, #46993 ),
 .UNSPECIFIED., .F., .F.,
 ( 4, 1, 1, 1, 1, 1, 1, 1, 4 ),
 ( 0.000000000000000000, 0.1250000000000000000, 0.2500000000000000000, 0.3750000000000000000, 0.5000000000000000000, 0.6250000000000000000, 0.7500000000000000000, 0.8750000000000000000, 1.000000000000000000 ),
 .UNSPECIFIED. ) ;
#17431=CARTESIAN_POINT ( 'NONE',  ( 47.38033551211754713, -54.20286183681685088, -75.36291177508510941 ) ) ;
#17432=CARTESIAN_POINT ( 'NONE',  ( 49.57777172146020206, -53.70720745051439593, -55.02952289821030263 ) ) ;
#17433=CARTESIAN_POINT ( 'NONE',  ( 51.20713017066216821, -31.70237965034690575, -17.16575294922130368 ) ) ;
#17436=CARTESIAN_POINT ( 'NONE',  ( 18.78670792145450008, -51.59710020169690381, -74.14993170018701107 ) ) ;
#17437=CARTESIAN_POINT ( 'NONE',  ( 57.50723796702470025, 13.88381105532070059, -17.67940111168049810 ) ) ;
#17438=ORIENTED_EDGE ( 'NONE', *, *, #27626, .T. ) ;
#17439=ADVANCED_FACE ( 'NONE', ( #3308 ), #45348, .T. ) ;
#17441=EDGE_CURVE ( 'NONE', #44194, #14297, #46862, .T. ) ;
#17445=CARTESIAN_POINT ( 'NONE',  ( 60.90359205743109783, -45.68240515407420332, -47.72054110957569861 ) ) ;
#17448=CARTESIAN_POINT ( 'NONE',  ( 12.98727014690059889, 18.78214035054229925, -21.05372677721659969 ) ) ;
#17455=ORIENTED_EDGE ( 'NONE', *, *, #16786, .T. ) ;
#17456=ORIENTED_EDGE ( 'NONE', *, *, #27469, .F. ) ;
#17458=CARTESIAN_POINT ( 'NONE',  ( 61.55597312494089834, -45.14216928434709786, -46.59921423066880664 ) ) ;
#17459=CARTESIAN_POINT ( 'NONE',  ( -11.32734372065470119, 10.64934054434680100, -6.430561461456250072 ) ) ;
#17461=ORIENTED_EDGE ( 'NONE', *, *, #23203, .T. ) ;
#17468=EDGE_CURVE ( 'NONE', #42744, #22490, #48103, .T. ) ;
#17472=CARTESIAN_POINT ( 'NONE',  ( 52.64727089593759501, -50.60815907346550091, -76.52291747471450378 ) ) ;
#17477=CARTESIAN_POINT ( 'NONE',  ( 45.63996532923849969, 13.90945843731140030, -7.778295627879400875 ) ) ;
#17478=CARTESIAN_POINT ( 'NONE',  ( 42.35079386031210191, -44.32234244509449894, -5.113119501825009294 ) ) ;
#17479=CARTESIAN_POINT ( 'NONE',  ( 70.03247032090770574, -49.95860450174168221, -71.35146707679193412 ) ) ;
#17480=FACE_OUTER_BOUND ( 'NONE', #4046, .T. ) ;
#17484=CARTESIAN_POINT ( 'NONE',  ( 68.13393739769620083, 11.88381105532070059, -65.65000000000000568 ) ) ;
#17485=CARTESIAN_POINT ( 'NONE',  ( 67.45418716456319430, 1.609579353070809793, -19.55846898103779807 ) ) ;
#17486=ORIENTED_EDGE ( 'NONE', *, *, #38437, .F. ) ;
#17487=CARTESIAN_POINT ( 'NONE',  ( 13.73894405924890094, -52.05919180694159820, -75.36996982820370761 ) ) ;
#17488=CARTESIAN_POINT ( 'NONE',  ( 57.33945456437729860, 19.08983581863999746, -52.87108254538590302 ) ) ;
#17493=CARTESIAN_POINT ( 'NONE',  ( 11.11361097580029877, 33.96900867391000389, -17.79075125673440283 ) ) ;
#17494=CARTESIAN_POINT ( 'NONE',  ( 14.34417029198830029, 19.88381105532299742, -22.49240188329279988 ) ) ;
#17496=CARTESIAN_POINT ( 'NONE',  ( 56.46328101745149297, 19.53148718691070229, -53.62057548195900125 ) ) ;
#17498=CARTESIAN_POINT ( 'NONE',  ( 48.25395546892340093, 22.92590509088350004, -54.66662523256869832 ) ) ;
#17505=CARTESIAN_POINT ( 'NONE',  ( 83.38337402972518930, 13.83610802003009965, -47.24826086172119233 ) ) ;
#17506=CARTESIAN_POINT ( 'NONE',  ( 54.85035616863589780, 16.02459751768919816, -25.69268928997570001 ) ) ;
#17508=CARTESIAN_POINT ( 'NONE',  ( 16.13393739769620083, -15.61618894467929941, -11.65000000000000036 ) ) ;
#17510=CARTESIAN_POINT ( 'NONE',  ( 56.44264214053460904, -45.11618894467940066, -15.14376385419089921 ) ) ;
#17514=CARTESIAN_POINT ( 'NONE',  ( 11.54952630610340059, -65.01896633571658413, -16.63601099843520004 ) ) ;
#17515=CARTESIAN_POINT ( 'NONE',  ( 12.95024349288270038, 34.28238369627520399, -47.68553644283399962 ) ) ;
#17518=CARTESIAN_POINT ( 'NONE',  ( 11.72329413022310085, 33.70814486805359422, -45.18478288877800253 ) ) ;
#17519=CARTESIAN_POINT ( 'NONE',  ( 47.64143405400680109, 23.30250925609140111, -74.14999999999999147 ) ) ;
#17520=VECTOR ( 'NONE', #27010, 1000.000000000000000 ) ;
#17524=CARTESIAN_POINT ( 'NONE',  ( 53.82322419959533732, 17.55874272043913109, -27.07946608715714731 ) ) ;
#17526=CARTESIAN_POINT ( 'NONE',  ( 52.81501434156309926, 18.37449448283769726, -48.45418012326710056 ) ) ;
#17527=DIRECTION ( 'NONE',  ( 0.000000000000000000, 0.000000000000000000, 1.000000000000000000 ) ) ;
#17528=ADVANCED_FACE ( 'NONE', ( #654 ), #48683, .F. ) ;
#17529=CARTESIAN_POINT ( 'NONE',  ( 50.83757486290169680, -48.61618577117480555, -76.31330845207050118 ) ) ;
#17534=ORIENTED_EDGE ( 'NONE', *, *, #39575, .T. ) ;
#17536=DIRECTION ( 'NONE',  ( 0.000000000000000000, 0.000000000000000000, 1.000000000000000000 ) ) ;
#17538=CARTESIAN_POINT ( 'NONE',  ( 13.79106882486509988, -51.24459767255270037, -22.61434474859899879 ) ) ;
#17539=CARTESIAN_POINT ( 'NONE',  ( 57.13424245449340333, 19.38601785914529785, -74.14888481814519139 ) ) ;
#17540=CARTESIAN_POINT ( 'NONE',  ( 47.18871270837350806, -53.98686607640210156, -75.65958371907380808 ) ) ;
#17541=ORIENTED_EDGE ( 'NONE', *, *, #49196, .F. ) ;
#17542=CARTESIAN_POINT ( 'NONE',  ( 54.77399211316150485, 14.69977379240920001, -15.76359807579460082 ) ) ;
#17543=CARTESIAN_POINT ( 'NONE',  ( 56.91872543020900110, -50.64361015893680218, -53.86107397471379699 ) ) ;
#17548=CARTESIAN_POINT ( 'NONE',  ( 46.58993879724850018, 22.02491853214390005, -76.11254988220410667 ) ) ;
#17551=CARTESIAN_POINT ( 'NONE',  ( 40.84819990301859605, -45.40787957530859842, -5.828857708371039337 ) ) ;
#17553=CARTESIAN_POINT ( 'NONE',  ( 44.76356921293569968, -45.10235736362039916, -7.023953210218369492 ) ) ;
#17554=LINE ( 'NONE', #41919, #36538 ) ;
#17556=TOROIDAL_SURFACE ( 'NONE', #31748, 15.56227766038949945, 0.9999999999568489617 ) ;
#17558=CARTESIAN_POINT ( 'NONE',  ( 82.35525732794108933, 13.87593127045350094, -46.40107902847420007 ) ) ;
#17563=CARTESIAN_POINT ( 'NONE',  ( 61.03999680408450246, 14.12696753779889924, -46.86320879711829690 ) ) ;
#17564=CARTESIAN_POINT ( 'NONE',  ( -31.60239111126589862, -24.98565332602689892, -55.64697389277930029 ) ) ;
#17567=CARTESIAN_POINT ( 'NONE',  ( 53.10865797006830036, -49.51857916385080216, -48.88762732764140395 ) ) ;
#17569=CARTESIAN_POINT ( 'NONE',  ( 61.26000939124259759, -45.11942681417600198, -27.10278859166270138 ) ) ;
#17570=CARTESIAN_POINT ( 'NONE',  ( 56.53714865535440737, 14.14923065729820095, -25.50329352154150087 ) ) ;
#17573=CARTESIAN_POINT ( 'NONE',  ( 53.21885458705129679, 18.27078423299469989, -49.08533969520789952 ) ) ;
#17575=CARTESIAN_POINT ( 'NONE',  ( 60.64847374440059724, -45.56447532782619447, -47.14388410539569918 ) ) ;
#17576=CARTESIAN_POINT ( 'NONE',  ( 71.76678105856730383, -45.11618894467940066, -14.40246108749630061 ) ) ;
#17577=ORIENTED_EDGE ( 'NONE', *, *, #14618, .T. ) ;
#17580=CARTESIAN_POINT ( 'NONE',  ( 47.46120807750819637, -54.60632935821639933, -54.66578937757580547 ) ) ;
#17583=CARTESIAN_POINT ( 'NONE',  ( 11.43201365335179887, -65.36003045264970979, -18.10223070864369888 ) ) ;
#17584=CARTESIAN_POINT ( 'NONE',  ( 53.06963667952179975, 18.30286252129070235, -48.79723990062230143 ) ) ;
#17590=CARTESIAN_POINT ( 'NONE',  ( 9.742198651190470571, -63.26564277683720405, -46.29734320245890444 ) ) ;
#17592=VERTEX_POINT ( 'NONE', #49154 ) ;
#17594=LINE ( 'NONE', #33038, #41121 ) ;
#17597=CARTESIAN_POINT ( 'NONE',  ( 53.75480394283020047, 19.75577102335120117, -75.91868723632779847 ) ) ;
#17598=CIRCLE ( 'NONE', #11729, 2.700000000000230216 ) ;
#17601=CIRCLE ( 'NONE', #36804, 2.000000000000001776 ) ;
#17604=AXIS2_PLACEMENT_3D ( 'NONE', #37826, #50134, #34123 ) ;
#17606=B_SPLINE_SURFACE_WITH_KNOTS ( 'NONE', 3, 3, ( 
 ( #7270, #3337, #19316, #35296, #1206, #28450, #13017, #44452, #24239, #44972, #12227, #8559, #4876, #32109, #20844, #28190 ),
 ( #24501, #8291, #36313, #24766, #16942, #947, #36841, #44709, #40266, #12752, #32886, #48921, #16150, #48128, #40519, #28708 ),
 ( #423, #678, #4356, #28973, #9074, #25022, #48386, #41036, #5153, #32367, #16667, #21107, #48653, #16410, #173, #37109 ),
 ( #44193, #20325, #4608, #12483, #20582, #36575, #32625, #8815, #40776, #23134, #88, #23643, #31511, #47530, #4263, #11628 ),
 ( #15297, #27082, #31253, #16060, #43341, #35724, #8201, #333, #11114, #31764, #19217, #23893, #24147, #35970, #35465, #27846 ),
 ( #28095, #32017, #43597, #39659, #47283, #3245, #40168, #51459, #20233, #11373, #51708, #48041, #43086, #16316, #36221, #12140 ),
 ( #27589, #44101, #3509, #7435, #47028, #7178, #35202, #7699, #23383, #39148, #51205, #11892, #15803, #47783, #27337, #39406 ),
 ( #19476, #15558, #3763, #19733, #43848, #7944, #39918, #4013, #19975, #40682, #33325, #45138, #21529, #48292, #16568, #41203 ),
 ( #32522, #37011, #28877, #843, #13188, #17106, #40421, #4781, #48551, #44879, #5053, #44356, #8719, #29138, #37526, #9505 ),
 ( #21012, #12922, #4514, #40942, #16840, #20749, #8984, #1629, #12658, #12387, #1109, #28612, #20487, #32271, #49343, #33058 ) ),
 .UNSPECIFIED., .F., .F., .F.,
 ( 4, 1, 1, 1, 1, 1, 1, 4 ),
 ( 4, 2, 2, 2, 2, 2, 2, 4 ),
 ( -1.166380231000000015E-05, 0.1428571428571430157, 0.2857142857142860315, 0.4285714285714289917, 0.5714285714285709528, 0.7142857142857139685, 0.8571428571428569843, 1.000014690989259991 ),
 ( -1.570796326794899889, -1.322743703599180032, -1.039254991375500037, -0.8620745462357000122, -0.7734843236657999999, -0.6317399675539610016, -0.4049489977750179714, -0.1533416749778369892 ),
 .UNSPECIFIED. ) ;
#17610=ORIENTED_EDGE ( 'NONE', *, *, #13218, .F. ) ;
#17613=CARTESIAN_POINT ( 'NONE',  ( 52.67198760255850232, -49.78119412946660560, -48.75777783608979377 ) ) ;
#17614=CARTESIAN_POINT ( 'NONE',  ( 45.07859124227709202, 14.88014128531450098, -9.026881354359289844 ) ) ;
#17616=CARTESIAN_POINT ( 'NONE',  ( 13.71097881326609880, 20.32289363718010122, -74.92517623884199907 ) ) ;
#17617=ADVANCED_FACE ( 'NONE', ( #45726 ), #28865, .T. ) ;
#17619=CARTESIAN_POINT ( 'NONE',  ( 45.06694394734220310, -45.15390109120389894, -7.502817270234459990 ) ) ;
#17623=CARTESIAN_POINT ( 'NONE',  ( 52.66238559624279958, -49.77034287296790183, -28.07828440529620195 ) ) ;
#17624=CARTESIAN_POINT ( 'NONE',  ( 55.63096065035139759, -50.93928849674639991, -74.97610068968259611 ) ) ;
#17625=CARTESIAN_POINT ( 'NONE',  ( 12.47113786592370133, 33.67127610693530215, -16.09695680451569899 ) ) ;
#17627=CARTESIAN_POINT ( 'NONE',  ( 54.47259832750690123, 15.01994964729280113, -15.76422791930239953 ) ) ;
#17628=ORIENTED_EDGE ( 'NONE', *, *, #10700, .T. ) ;
#17630=CARTESIAN_POINT ( 'NONE',  ( -8.086920474589250674, -44.91374637176360096, -5.311490494450340272 ) ) ;
#17632=CARTESIAN_POINT ( 'NONE',  ( 47.46673305269209919, 23.38706694144839915, -54.94265356273070466 ) ) ;
#17633=CARTESIAN_POINT ( 'NONE',  ( 55.92677794998609642, -45.89053595373002992, -25.32409385810630909 ) ) ;
#17635=CARTESIAN_POINT ( 'NONE',  ( 60.77432506344459284, 14.26616040630690030, -47.09778254978269274 ) ) ;
#17636=AXIS2_PLACEMENT_3D ( 'NONE', #28731, #3620, #7807 ) ;
#17637=CARTESIAN_POINT ( 'NONE',  ( 10.87995435926830012, 33.74311107132329823, -17.51161114007549813 ) ) ;
#17638=CARTESIAN_POINT ( 'NONE',  ( 51.80595387025849874, 17.96077523470199822, -77.05313553437329688 ) ) ;
#17640=ADVANCED_FACE ( 'NONE', ( #3772 ), #17171, .T. ) ;
#17641=CARTESIAN_POINT ( 'NONE',  ( 47.18324198357279897, -54.80726809202429450, -54.61059023085309860 ) ) ;
#17642=CARTESIAN_POINT ( 'NONE',  ( 53.29384558423090112, -50.54670888882439783, -28.15000000000000213 ) ) ;
#17643=CARTESIAN_POINT ( 'NONE',  ( 54.10076142776490116, 17.30991513604229937, -26.94462959976219807 ) ) ;
#17644=CARTESIAN_POINT ( 'NONE',  ( 54.32603732818120079, 20.33894821613250059, -53.45081835463139441 ) ) ;
#17646=CARTESIAN_POINT ( 'NONE',  ( 12.02928808077719935, -65.36534498448229158, -17.22609656285550273 ) ) ;
#17647=CARTESIAN_POINT ( 'NONE',  ( 32.61507622778040627, -15.61618894467929941, -7.049999999999999822 ) ) ;
#17650=CARTESIAN_POINT ( 'NONE',  ( 10.97872622502669948, 32.01874292912219744, -44.74211950928979320 ) ) ;
#17652=CARTESIAN_POINT ( 'NONE',  ( 66.66072342652930161, -29.91655757336389954, -17.00118403369340214 ) ) ;
#17654=ORIENTED_EDGE ( 'NONE', *, *, #19775, .T. ) ;
#17655=ORIENTED_EDGE ( 'NONE', *, *, #18506, .T. ) ;
#17658=CARTESIAN_POINT ( 'NONE',  ( 9.869349599861529043, -63.31974513753180389, -46.22151743515530598 ) ) ;
#17659=CARTESIAN_POINT ( 'NONE',  ( 56.83034892914880487, -45.92143544903500185, -26.22419937669090118 ) ) ;
#17661=CARTESIAN_POINT ( 'NONE',  ( 61.59490267384730089, 13.91893133687459994, -46.70618209336589643 ) ) ;
#17662=LINE ( 'NONE', #31938, #38501 ) ;
#17665=ORIENTED_EDGE ( 'NONE', *, *, #32972, .T. ) ;
#17666=CARTESIAN_POINT ( 'NONE',  ( 45.87783615456250175, -45.55524548511859706, -9.057579235710109700 ) ) ;
#17668=CARTESIAN_POINT ( 'NONE',  ( -14.37046249213279658, -15.61618894467929941, 7.349999999999999645 ) ) ;
#17669=ORIENTED_EDGE ( 'NONE', *, *, #12229, .F. ) ;
#17671=CARTESIAN_POINT ( 'NONE',  ( 47.00221226121089302, -54.26108178918599378, -75.51940560377390455 ) ) ;
#17673=VECTOR ( 'NONE', #2903, 1000.000000000000000 ) ;
#17674=CARTESIAN_POINT ( 'NONE',  ( 54.85251692984100202, 13.88381105524550030, -14.10626792861419965 ) ) ;
#17677=FACE_OUTER_BOUND ( 'NONE', #19578, .T. ) ;
#17678=CARTESIAN_POINT ( 'NONE',  ( 61.42166429544719364, 13.88661517629680020, -27.30521883883519862 ) ) ;
#17681=LINE ( 'NONE', #33650, #2923 ) ;
#17682=CARTESIAN_POINT ( 'NONE',  ( -9.296035807754268632, -42.83485695790410119, -4.399682342286669545 ) ) ;
#17683=CARTESIAN_POINT ( 'NONE',  ( 76.56552468136949585, -40.98740743049830115, -13.88134112481359850 ) ) ;
#17686=DIRECTION ( 'NONE',  ( 0.3294064756440934771, -0.9441882088883220003, -3.885780586188049864E-16 ) ) ;
#17689=ADVANCED_FACE ( 'NONE', ( #33063 ), #33045, .T. ) ;
#17690=CARTESIAN_POINT ( 'NONE',  ( 49.22821711787649690, -53.85658415721609771, -55.11852911525630105 ) ) ;
#17693=CARTESIAN_POINT ( 'NONE',  ( 54.77086636619779370, -51.21734551792319223, -53.06498560372889983 ) ) ;
#17694=ORIENTED_EDGE ( 'NONE', *, *, #23122, .F. ) ;
#17701=CARTESIAN_POINT ( 'NONE',  ( 60.41344223070770170, -45.75562068724720177, -47.56364136414550359 ) ) ;
#17706=CARTESIAN_POINT ( 'NONE',  ( 53.35835984455025027, -51.38288689484378580, -75.63635970964975286 ) ) ;
#17707=FACE_OUTER_BOUND ( 'NONE', #23553, .T. ) ;
#17709=ORIENTED_EDGE ( 'NONE', *, *, #50000, .T. ) ;
#17711=VERTEX_POINT ( 'NONE', #20687 ) ;
#17712=B_SPLINE_CURVE_WITH_KNOTS ( 'NONE', 3,
 ( #50186, #41793, #2225, #17431, #18202, #33401, #49417, #13514, #45473, #46526, #31018, #39424, #31530, #35484, #10615, #39676 ),
 .UNSPECIFIED., .F., .F.,
 ( 4, 2, 2, 2, 2, 2, 2, 4 ),
 ( 0.000000000000000000, 0.1213476983427276695, 0.2731151459108055457, 0.3945291039652654153, 0.5159430620197285045, 0.6842823862752845931, 0.9536253050841766443, 1.000000000000000000 ),
 .UNSPECIFIED. ) ;
#17714=FACE_OUTER_BOUND ( 'NONE', #10966, .T. ) ;
#17715=CARTESIAN_POINT ( 'NONE',  ( 56.04685572940000782, -50.83791839738839968, -53.21420621680360341 ) ) ;
#17719=DIRECTION ( 'NONE',  ( -1.000000000000000000, 0.000000000000000000, 0.000000000000000000 ) ) ;
#17723=CARTESIAN_POINT ( 'NONE',  ( 53.60866176960309559, -50.88321737380339727, -76.14577100024149559 ) ) ;
#17725=CARTESIAN_POINT ( 'NONE',  ( 7.433595052712614226, -61.36773602579286546, -19.83583517853760370 ) ) ;
#17728=CARTESIAN_POINT ( 'NONE',  ( 44.59168717410679506, 13.92269748457639977, -7.270472794180020237 ) ) ;
#17729=EDGE_CURVE ( 'NONE', #19952, #25535, #8037, .T. ) ;
#17730=CARTESIAN_POINT ( 'NONE',  ( 42.93197233849409855, -42.55807683903029925, -3.307825584507050110 ) ) ;
#17731=CARTESIAN_POINT ( 'NONE',  ( 68.13393739769841773, -50.61618894467878960, -73.25000000000220268 ) ) ;
#17732=LINE ( 'NONE', #38172, #39096 ) ;
#17734=AXIS2_PLACEMENT_3D ( 'NONE', #14551, #5403, #45494 ) ;
#17737=CARTESIAN_POINT ( 'NONE',  ( 67.26280899804329749, 1.086883144305099913, -18.54866898292119970 ) ) ;
#17738=VERTEX_POINT ( 'NONE', #17305 ) ;
#17739=CARTESIAN_POINT ( 'NONE',  ( 14.67572115279929967, -52.29221104373330320, -75.97756937697440094 ) ) ;
#17740=CARTESIAN_POINT ( 'NONE',  ( 57.31065200125909342, 19.28726522077679917, -53.29731268387590148 ) ) ;
#17741=DIRECTION ( 'NONE',  ( 0.1686178020941689615, 0.6660492713794448072, -0.7265992051412127894 ) ) ;
#17742=CARTESIAN_POINT ( 'NONE',  ( 11.14789759607523401, 32.56083963050009089, -43.84340685703310214 ) ) ;
#17746=CARTESIAN_POINT ( 'NONE',  ( 11.92216765568830006, 34.20610614520490600, -17.95790456664920143 ) ) ;
#17750=CARTESIAN_POINT ( 'NONE',  ( 48.26498440238650289, 23.02110959576539884, -55.06465735757110025 ) ) ;
#17755=CARTESIAN_POINT ( 'NONE',  ( 53.43679795856343873, -49.34287432940195828, -48.83615822498648384 ) ) ;
#17756=CARTESIAN_POINT ( 'NONE',  ( 57.12444643032910108, -50.61921117833989570, -53.89324253442650559 ) ) ;
#17757=CARTESIAN_POINT ( 'NONE',  ( 82.88019469981981047, 13.88961720913030007, -46.94529082815019194 ) ) ;
#17758=CARTESIAN_POINT ( 'NONE',  ( 55.91595998539320078, 14.67226890368210057, -25.32542959099430036 ) ) ;
#17764=ORIENTED_EDGE ( 'NONE', *, *, #46084, .T. ) ;
#17765=ORIENTED_EDGE ( 'NONE', *, *, #15322, .T. ) ;
#17766=CARTESIAN_POINT ( 'NONE',  ( 12.28455908802260055, -64.73110178338430387, -15.95890976726639998 ) ) ;
#17767=CARTESIAN_POINT ( 'NONE',  ( 12.07551473733020053, 33.99943997505149440, -46.31242131770569870 ) ) ;
#17769=CIRCLE ( 'NONE', #45393, 20.00000000000000355 ) ;
#17775=CARTESIAN_POINT ( 'NONE',  ( 53.20716069589280295, 18.10213603062282317, -27.47938434864637713 ) ) ;
#17776=CARTESIAN_POINT ( 'NONE',  ( 53.40992735058819818, 18.17061601739440135, -49.09007107978719375 ) ) ;
#17777=CARTESIAN_POINT ( 'NONE',  ( 63.04562385509341027, -1.096656852449789943, -16.27512118587200263 ) ) ;
#17778=CARTESIAN_POINT ( 'NONE',  ( 51.15792108380730241, -50.27113159165210732, -76.23077843503030238 ) ) ;
#17779=CARTESIAN_POINT ( 'NONE',  ( 56.45552426919280009, -50.53433981852420231, -52.91205187155370027 ) ) ;
#17781=CARTESIAN_POINT ( 'NONE',  ( 52.59996064233959601, -49.82480704385319825, -27.82108120899960113 ) ) ;
#17782=CARTESIAN_POINT ( 'NONE',  ( 68.13393739769810509, 19.38381105532030091, -71.50000000000198952 ) ) ;
#17787=CARTESIAN_POINT ( 'NONE',  ( 13.97463716696829827, -51.18681913482190282, -22.92153293571290007 ) ) ;
#17788=CARTESIAN_POINT ( 'NONE',  ( 54.52045198098380752, 19.43253422766209937, -76.37641636170799586 ) ) ;
#17789=EDGE_CURVE ( 'NONE', #18259, #31649, #16886, .T. ) ;
#17790=CARTESIAN_POINT ( 'NONE',  ( 46.96102864795940235, -53.69224363991650506, -75.90771320283761270 ) ) ;
#17792=CARTESIAN_POINT ( 'NONE',  ( 55.74284278219830213, 14.65117925743319915, -16.98778742111269935 ) ) ;
#17793=CARTESIAN_POINT ( 'NONE',  ( 11.13393739769619906, 32.28996932333459569, -43.76018303787720498 ) ) ;
#17795=CARTESIAN_POINT ( 'NONE',  ( 56.92789890539140174, -50.64206873198590131, -53.72375501711709944 ) ) ;
#17800=CARTESIAN_POINT ( 'NONE',  ( 47.24300521349680082, 22.88509248956220077, -75.51940560377610723 ) ) ;
#17802=CARTESIAN_POINT ( 'NONE',  ( 75.39234309038256754, -40.43989336811801394, -12.98456726386316085 ) ) ;
#17805=VECTOR ( 'NONE', #9372, 1000.000000000000000 ) ;
#17808=CARTESIAN_POINT ( 'NONE',  ( 10.61751707702059910, -64.82563018155620682, -22.25048313876769868 ) ) ;
#17813=CARTESIAN_POINT ( 'NONE',  ( -33.86618693412709291, -10.74011431604400002, -57.52971779843680622 ) ) ;
#17814=ORIENTED_EDGE ( 'NONE', *, *, #49298, .F. ) ;
#17815=CARTESIAN_POINT ( 'NONE',  ( 52.91916941891219750, -49.61445646718999569, -48.76921093002629704 ) ) ;
#17818=CARTESIAN_POINT ( 'NONE',  ( 48.88334854381260186, -54.00587892617620156, -55.28861537459440001 ) ) ;
#17819=CARTESIAN_POINT ( 'NONE',  ( 56.80572106195580773, 14.09462252995199982, -25.70585579729069892 ) ) ;
#17822=CARTESIAN_POINT ( 'NONE',  ( 52.99414826126849931, 18.35427201954029641, -48.92816828239389082 ) ) ;
#17830=CARTESIAN_POINT ( 'NONE',  ( 47.49470543983129289, -54.59752074366780050, -54.79943125224989586 ) ) ;
#17833=CARTESIAN_POINT ( 'NONE',  ( 11.51841290285589992, -65.37424786629888729, -17.84188021312800387 ) ) ;
#17837=EDGE_CURVE ( 'NONE', #45267, #17917, #17769, .T. ) ;
#17841=CARTESIAN_POINT ( 'NONE',  ( 13.61938558678000000, -51.42721352342299923, -23.15000000000000213 ) ) ;
#17842=FACE_OUTER_BOUND ( 'NONE', #24238, .T. ) ;
#17845=CARTESIAN_POINT ( 'NONE',  ( 13.39998208310050032, -51.78678246903520233, -74.14999999999999147 ) ) ;
#17847=CARTESIAN_POINT ( 'NONE',  ( 53.50362149015870017, 19.53775296350150370, -76.38491669520200844 ) ) ;
#17848=AXIS2_PLACEMENT_3D ( 'NONE', #33339, #33852, #49354 ) ;
#17849=B_SPLINE_CURVE_WITH_KNOTS ( 'NONE', 3,
 ( #402, #37345, #21084, #9050, #24999, #29468, #8538, #28945, #9322, #1444, #33398, #41273, #8791, #45471, #20557, #16388, #24744, #9572 ),
 .UNSPECIFIED., .F., .F.,
 ( 4, 2, 2, 2, 2, 2, 2, 2, 4 ),
 ( 0.000000000000000000, 0.1774999104124761473, 0.3374998296575247303, 0.4374997791856805596, 0.4999997476407779806, 0.6249996845509727672, 0.7565685563123135671, 0.9670787511304582695, 1.000000000000000000 ),
 .UNSPECIFIED. ) ;
#17852=FACE_OUTER_BOUND ( 'NONE', #23415, .T. ) ;
#17860=DIRECTION ( 'NONE',  ( 0.000000000000000000, 0.000000000000000000, 1.000000000000000000 ) ) ;
#17865=CARTESIAN_POINT ( 'NONE',  ( 14.30359793617770059, 20.25300558755819935, -75.29799846200430125 ) ) ;
#17867=CARTESIAN_POINT ( 'NONE',  ( 41.10495109285060522, -44.90785437222480425, -5.488531188786208936 ) ) ;
#17870=VERTEX_POINT ( 'NONE', #25394 ) ;
#17871=CARTESIAN_POINT ( 'NONE',  ( 55.49059146526019504, -46.45735698793969704, -25.52441156651820009 ) ) ;
#17872=CARTESIAN_POINT ( 'NONE',  ( 16.20840964857250199, -51.09324699765929978, -20.73468313311619937 ) ) ;
#17873=CARTESIAN_POINT ( 'NONE',  ( 8.283081141223801680, 30.83908974943280157, -14.51842061854859978 ) ) ;
#17875=DIRECTION ( 'NONE',  ( 1.000000000000000000, 0.000000000000000000, 0.000000000000000000 ) ) ;
#17876=DIRECTION ( 'NONE',  ( 0.000000000000000000, -1.000000000000000000, 0.000000000000000000 ) ) ;
#17879=CARTESIAN_POINT ( 'NONE',  ( -5.153449232133100466, -47.10011955755160784, -4.520249556061699536 ) ) ;
#17881=CARTESIAN_POINT ( 'NONE',  ( 47.45072472674559805, 23.39242017868889789, -54.80215748663960085 ) ) ;
#17882=CARTESIAN_POINT ( 'NONE',  ( 56.60951721479818843, -45.32895253404118563, -25.29352247433434187 ) ) ;
#17884=CARTESIAN_POINT ( 'NONE',  ( 61.10824109186599884, 14.10765967360200079, -47.03638507362239807 ) ) ;
#17885=CARTESIAN_POINT ( 'NONE',  ( 11.54952630610960007, 33.78658844635589276, -16.63601099842679787 ) ) ;
#17887=DIRECTION ( 'NONE',  ( 0.6888026391158399431, 0.7071067811865427988, 0.1598465650148944706 ) ) ;
#17888=CARTESIAN_POINT ( 'NONE',  ( 19.49111017241425969, 24.24266684409263917, -75.60405384317246558 ) ) ;
#17890=DIRECTION ( 'NONE',  ( 1.000000000000000000, 0.000000000000000000, 0.000000000000000000 ) ) ;
#17891=CARTESIAN_POINT ( 'NONE',  ( 55.93394966927949952, 19.54994930437460354, -53.01357101662289750 ) ) ;
#17893=CARTESIAN_POINT ( 'NONE',  ( 68.13393739769620083, 16.88381105532069881, -71.50000000000000000 ) ) ;
#17894=VERTEX_POINT ( 'NONE', #5514 ) ;
#17895=CARTESIAN_POINT ( 'NONE',  ( 19.86997031299514660, 23.42669132854136294, -17.96412134175789532 ) ) ;
#17896=CARTESIAN_POINT ( 'NONE',  ( 11.10557753124879987, 32.10104306594170254, -44.25340448499940749 ) ) ;
#17899=CARTESIAN_POINT ( 'NONE',  ( 66.62368884664920188, -33.10221915192529707, -20.10140631842839909 ) ) ;
#17900=ORIENTED_EDGE ( 'NONE', *, *, #30938, .F. ) ;
#17901=CARTESIAN_POINT ( 'NONE',  ( 18.66237388380359974, 20.19927249694829996, -74.14993703734479880 ) ) ;
#17902=VERTEX_POINT ( 'NONE', #14160 ) ;
#17903=EDGE_CURVE ( 'NONE', #36035, #22762, #41825, .T. ) ;
#17904=EDGE_LOOP ( 'NONE', ( #12348, #17386, #6687, #23428, #42611 ) ) ;
#17905=VECTOR ( 'NONE', #21182, 1000.000000000000000 ) ;
#17907=DIRECTION ( 'NONE',  ( -1.000000000000000000, 0.000000000000000000, 0.000000000000000000 ) ) ;
#17908=CARTESIAN_POINT ( 'NONE',  ( 76.48977085477018534, -3.534982534879841598, -13.18333932634366334 ) ) ;
#17909=EDGE_LOOP ( 'NONE', ( #46553, #34859, #37899, #46168 ) ) ;
#17910=CARTESIAN_POINT ( 'NONE',  ( 10.93149295491969930, -63.50462161081620138, -44.89510998098330674 ) ) ;
#17911=CARTESIAN_POINT ( 'NONE',  ( 57.30237695512850138, -45.45193249669419799, -26.06568594713050047 ) ) ;
#17913=EDGE_CURVE ( 'NONE', #23932, #39634, #5219, .T. ) ;
#17915=ORIENTED_EDGE ( 'NONE', *, *, #19676, .T. ) ;
#17917=VERTEX_POINT ( 'NONE', #30898 ) ;
#17918=CARTESIAN_POINT ( 'NONE',  ( 55.40394017515929903, -45.11618894460369944, -14.52023579739710080 ) ) ;
#17920=CARTESIAN_POINT ( 'NONE',  ( 15.93086454162719789, 19.78639745450599818, -20.59235730855439783 ) ) ;
#17924=CARTESIAN_POINT ( 'NONE',  ( 46.86866897037879909, -54.05579343596940589, -75.74320899229410031 ) ) ;
#17925=CARTESIAN_POINT ( 'NONE',  ( 44.89546122686059704, 13.88381105527729886, -7.313136318628219890 ) ) ;
#17926=ADVANCED_FACE ( 'NONE', ( #51098 ), #2362, .F. ) ;
#17927=CARTESIAN_POINT ( 'NONE',  ( 50.08385623720359803, -49.23364898979970405, -76.14999999999999147 ) ) ;
#17928=DIRECTION ( 'NONE',  ( -1.000000000000000000, 0.000000000000000000, 0.000000000000000000 ) ) ;
#17929=CARTESIAN_POINT ( 'NONE',  ( 51.81953054287640015, 20.00644079818270171, -76.05779033163869940 ) ) ;
#17930=CARTESIAN_POINT ( 'NONE',  ( 61.44557787504049884, 13.91402711005510007, -27.69105617369679706 ) ) ;
#17936=CARTESIAN_POINT ( 'NONE',  ( 76.60139863843768637, -42.13230907256439650, -14.03747475277350176 ) ) ;
#17938=CARTESIAN_POINT ( 'NONE',  ( 7.635415421591214447, 29.62789471496180482, -20.56421356237308729 ) ) ;
#17940=CARTESIAN_POINT ( 'NONE',  ( 12.49509346338439997, 19.12609117445460072, -21.18371118359339889 ) ) ;
#17941=CIRCLE ( 'NONE', #47267, 20.00000000000000355 ) ;
#17944=CARTESIAN_POINT ( 'NONE',  ( 43.75992007188810362, -43.62559376723620375, -5.076600545282080823 ) ) ;
#17945=CIRCLE ( 'NONE', #47271, 22.00000000000000000 ) ;
#17946=CARTESIAN_POINT ( 'NONE',  ( 76.51215728517360048, -43.23923739644211395, -14.09245988324813581 ) ) ;
#17947=CARTESIAN_POINT ( 'NONE',  ( 18.12954643717650072, -51.13035289118570148, -74.36013246830410139 ) ) ;
#17948=DIRECTION ( 'NONE',  ( 0.3805321250008311118, 0.000000000000000000, -0.9247677015566405645 ) ) ;
#17954=CARTESIAN_POINT ( 'NONE',  ( 10.64863409883700029, -63.44323389162830296, -23.66469670114080159 ) ) ;
#17961=CARTESIAN_POINT ( 'NONE',  ( 45.11068418564629923, -46.01207058399690197, -8.978235659328069218 ) ) ;
#17962=VERTEX_POINT ( 'NONE', #18087 ) ;
#17968=ADVANCED_FACE ( 'NONE', ( #46149 ), #5469, .T. ) ;
#17969=CARTESIAN_POINT ( 'NONE',  ( 52.90377914247349622, -49.66458043520950127, -49.02092677081500227 ) ) ;
#17970=CARTESIAN_POINT ( 'NONE',  ( 61.14661496961065978, 14.27331964475400561, -47.53223270648921073 ) ) ;
#17971=CARTESIAN_POINT ( 'NONE',  ( 56.14494575505310081, -50.91271539411779656, -53.77253383582240076 ) ) ;
#17973=ORIENTED_EDGE ( 'NONE', *, *, #36378, .F. ) ;
#17975=VECTOR ( 'NONE', #22676, 1000.000000000000000 ) ;
#17977=ORIENTED_EDGE ( 'NONE', *, *, #42079, .T. ) ;
#17979=CARTESIAN_POINT ( 'NONE',  ( 53.33359569267409483, -50.64165965796969715, -76.65020871703400474 ) ) ;
#17980=CARTESIAN_POINT ( 'NONE',  ( 60.67112978390429845, 14.38394182225979989, -47.47021178863389679 ) ) ;
#17984=CARTESIAN_POINT ( 'NONE',  ( 41.24055256048669804, 13.59911224018700082, -5.438976187443009813 ) ) ;
#17986=ADVANCED_FACE ( 'NONE', ( #46347 ), #51551, .T. ) ;
#17987=CARTESIAN_POINT ( 'NONE',  ( 41.00922517319189353, -44.50642897861339975, -4.614727984880420131 ) ) ;
#17989=CARTESIAN_POINT ( 'NONE',  ( -6.464119761774720807, 15.22590418212459973, -5.599264135990670077 ) ) ;
#17991=DIRECTION ( 'NONE',  ( 1.224646799147353207E-16, 1.000000000000000000, -0.000000000000000000 ) ) ;
#17994=CARTESIAN_POINT ( 'NONE',  ( 15.05440318628160057, -53.11618894467930119, -76.14999999999999147 ) ) ;
#17995=B_SPLINE_CURVE_WITH_KNOTS ( 'NONE', 3,
 ( #43066, #28013, #39832, #38620, #50413, #19898, #40088, #42288 ),
 .UNSPECIFIED., .F., .F.,
 ( 4, 2, 2, 4 ),
 ( 0.4999999271596955452, 0.6249999999960698105, 0.8117231960751974951, 1.000000000000000000 ),
 .UNSPECIFIED. ) ;
#17997=CARTESIAN_POINT ( 'NONE',  ( 48.82567944589380460, -3.116188925162400203, -15.64999999106299988 ) ) ;
#17999=( BOUNDED_CURVE ( )  B_SPLINE_CURVE ( 3, ( #28868, #13181, #21255, #9238 ),
 .UNSPECIFIED., .F., .T. ) 
 B_SPLINE_CURVE_WITH_KNOTS ( ( 4, 4 ),
 ( 5.485850788481889673, 5.497787143782139729 ),
 .UNSPECIFIED. ) 
 CURVE ( )  GEOMETRIC_REPRESENTATION_ITEM ( )  RATIONAL_B_SPLINE_CURVE ( ( 1.000000000000000000, 0.9999881269870877221, 0.9999881269870877221, 1.000000000000000000 ) ) 
 REPRESENTATION_ITEM ( '' )  );
#18002=CARTESIAN_POINT ( 'NONE',  ( 48.22056116383330249, -54.26093726109029802, -54.98805926112070352 ) ) ;
#18004=LINE ( 'NONE', #29779, #21393 ) ;
#18005=CARTESIAN_POINT ( 'NONE',  ( 56.42319918597290496, 19.43625241695789896, -53.17468697167449676 ) ) ;
#18006=CARTESIAN_POINT ( 'NONE',  ( 41.93138972908788276, 13.29046345300131016, -5.197897843198316714 ) ) ;
#18007=CARTESIAN_POINT ( 'NONE',  ( 48.37923893010100329, 22.88832752567240192, -54.71411453344789777 ) ) ;
#18008=VERTEX_POINT ( 'NONE', #39755 ) ;
#18012=DIRECTION ( 'NONE',  ( 0.4042525045258790750, 0.000000000000000000, -0.9146474252872273114 ) ) ;
#18014=CARTESIAN_POINT ( 'NONE',  ( 84.41203222934960593, 12.28655387197119886, -47.41895602134439969 ) ) ;
#18015=DIRECTION ( 'NONE',  ( 0.000000000000000000, 1.000000000000000000, 0.000000000000000000 ) ) ;
#18018=CARTESIAN_POINT ( 'NONE',  ( 56.96825255358579909, -45.11618894467940066, -16.09511754741749812 ) ) ;
#18020=B_SPLINE_SURFACE_WITH_KNOTS ( 'NONE', 3, 3, ( 
 ( #35737, #2998, #31779, #18968, #39161, #39670, #19231, #34949, #23396, #39419, #50949, #15569, #3778 ),
 ( #35214, #31013, #31263, #51721, #47797, #40952, #13199, #24160, #17370, #40434, #24940, #25208, #37024 ),
 ( #28888, #1122, #29148, #33070, #44626, #40694, #12401, #36749, #17118, #28107, #1383, #49097, #20245 ),
 ( #24681, #48054, #28365, #44115, #12153, #8215, #45149, #28626, #48829, #41214, #44371, #5066, #48567 ),
 ( #4794, #8475, #4527, #44890, #8731, #37285, #9261, #20762, #5328, #24421, #40183, #21279, #36237 ),
 ( #4275, #344, #16330, #20499, #36490, #32283, #48304, #595, #16580, #32534, #12671, #21024, #860 ),
 ( #16855, #32802, #12932, #8995, #34105, #33600, #10022, #2682, #6355, #49614, #13958, #26250, #49353 ),
 ( #37807, #21802, #5836, #1902, #14213, #14467, #9519, #17881, #46202, #29411, #10287, #25465, #21539 ),
 ( #37536, #13706, #30184, #42256, #33850, #22573, #29914, #1642, #2160, #22313, #38321, #29662, #13454 ),
 ( #2410, #49866, #41999, #25986, #26505, #18391, #38590, #50383, #33338, #34370, #45933, #50117, #6098 ),
 ( #22054, #45669, #38065, #18140, #45413, #30439, #46461, #10549, #42521, #6610, #41470, #17632, #5585 ),
 ( #9770, #25722, #41731, #10805, #7649, #11066, #23593, #31461, #39358, #46981, #35149, #51155, #39610 ),
 ( #3714, #47485, #18654, #11580, #27032, #27287, #15250, #22828, #43038, #38849, #7134, #31203, #34628 ),
 ( #43548, #43295, #23086, #11323, #19686, #2937, #35410, #18908, #34891, #39105, #7386, #23335, #47232 ),
 ( #50633, #14729, #42781, #50891, #3460, #30949, #14984, #19430, #3197, #51412, #15507, #30700, #19170 ),
 ( #46721, #27542, #26765, #6878, #14384, #42694, #9933, #42434, #14124, #50548, #22227, #25895, #6008 ) ),
 .UNSPECIFIED., .F., .F., .F.,
 ( 4, 2, 2, 2, 2, 2, 2, 4 ),
 ( 4, 1, 1, 1, 1, 1, 1, 1, 1, 1, 4 ),
 ( -1.194374153756279977, -0.9853586768489350778, -0.7464838460976789269, -0.5971870768781439853, -0.5225386922683770141, -0.4031012768927489942, -0.2120014122917439903, 0.04002625521051070279 ),
 ( -0.04002625527861099902, 0.1000000000000000056, 0.2000000000000000111, 0.2999999999999999889, 0.4000000000000000222, 0.5000000000000000000, 0.5999999999999999778, 0.6999999999999999556, 0.8000000000000000444, 0.9000000000000000222, 1.000000000000000000 ),
 .UNSPECIFIED. ) ;
#18021=VERTEX_POINT ( 'NONE', #36070 ) ;
#18023=AXIS2_PLACEMENT_3D ( 'NONE', #14838, #10917, #7240 ) ;
#18026=ORIENTED_EDGE ( 'NONE', *, *, #19055, .F. ) ;
#18027=CARTESIAN_POINT ( 'NONE',  ( 12.04070883442799911, -64.81472977847060690, -16.10368401052740239 ) ) ;
#18028=CARTESIAN_POINT ( 'NONE',  ( 55.55365133010059964, 13.88381105532070059, -14.32025150907159983 ) ) ;
#18030=CARTESIAN_POINT ( 'NONE',  ( 50.96419009180484494, 4.052314248501449612, -76.38154650529611445 ) ) ;
#18031=ORIENTED_EDGE ( 'NONE', *, *, #45315, .T. ) ;
#18035=CARTESIAN_POINT ( 'NONE',  ( 49.60427607923370630, 21.56003884501200218, -52.10971779361800316 ) ) ;
#18036=CARTESIAN_POINT ( 'NONE',  ( 65.43644619362240178, -1.044793625667630010, -16.56989681762950184 ) ) ;
#18037=CARTESIAN_POINT ( 'NONE',  ( 51.06184044748430040, -49.59582491932100368, -76.32371533191239621 ) ) ;
#18038=CARTESIAN_POINT ( 'NONE',  ( 56.96982729888789976, -50.41531670947319554, -52.91641933479590421 ) ) ;
#18039=ORIENTED_EDGE ( 'NONE', *, *, #15945, .F. ) ;
#18041=CARTESIAN_POINT ( 'NONE',  ( 68.13393739769819035, 19.47158195952109594, -72.59354914830207406 ) ) ;
#18043=CARTESIAN_POINT ( 'NONE',  ( 12.13393739769598234, -55.41568642894408470, -74.40623532128907414 ) ) ;
#18044=CARTESIAN_POINT ( 'NONE',  ( 49.62158364714009195, -46.18327638186429596, -12.18455737752769963 ) ) ;
#18046=B_SPLINE_CURVE_WITH_KNOTS ( 'NONE', 3,
 ( #37602, #13260, #1710, #17693, #33663, #8422, #20448, #38663, #15058, #26842, #10621, #31536, #15321, #19242, #35224, #47307 ),
 .UNSPECIFIED., .F., .F.,
 ( 4, 2, 2, 2, 2, 2, 2, 4 ),
 ( 4.583155019233440007E-09, 1.209577291029928503, 2.421219448687449205, 3.178495797223401365, 3.651793515058360473, 4.598388950728297786, 6.112941647800201217, 7.438175257738109281 ),
 .UNSPECIFIED. ) ;
#18049=CARTESIAN_POINT ( 'NONE',  ( 14.04136291104570056, -51.13553769603730359, -22.40089439151919848 ) ) ;
#18050=CARTESIAN_POINT ( 'NONE',  ( 53.75469708788489953, 19.75578442515150002, -75.91870210712610856 ) ) ;
#18052=CARTESIAN_POINT ( 'NONE',  ( 47.00901173922259346, -53.75426067600269420, -75.86421395400510903 ) ) ;
#18054=CARTESIAN_POINT ( 'NONE',  ( 56.18893761250490115, 14.30662584625740053, -17.25705736110630184 ) ) ;
#18056=CARTESIAN_POINT ( 'NONE',  ( 57.07649182089729578, -50.45121929360420410, -53.03413606727519891 ) ) ;
#18059=CARTESIAN_POINT ( 'NONE',  ( 47.57073486567139753, 23.21246683545610168, -74.81156575899859718 ) ) ;
#18060=CARTESIAN_POINT ( 'NONE',  ( 69.63393739769620083, -43.11618894467930119, -73.25000000000000000 ) ) ;
#18065=AXIS2_PLACEMENT_3D ( 'NONE', #6607, #45930, #22569 ) ;
#18067=LINE ( 'NONE', #34035, #19083 ) ;
#18069=CARTESIAN_POINT ( 'NONE',  ( 61.28610426219869112, 13.99802494501810024, -46.37202244447839661 ) ) ;
#18070=CARTESIAN_POINT ( 'NONE',  ( 6.188526101449100203, 32.65406634132989439, -47.34841622259180127 ) ) ;
#18072=CARTESIAN_POINT ( 'NONE',  ( 52.76130783809809799, -49.70603018815580043, -48.70177521040290003 ) ) ;
#18073=EDGE_LOOP ( 'NONE', ( #16063, #22747, #122, #32063, #27886 ) ) ;
#18077=CARTESIAN_POINT ( 'NONE',  ( 55.82532434612180339, 14.80164250910239865, -25.33867224380599836 ) ) ;
#18080=CARTESIAN_POINT ( 'NONE',  ( 52.89023671311360175, 18.40607031815540040, -48.86102654974850168 ) ) ;
#18082=CARTESIAN_POINT ( 'NONE',  ( 16.17111167639663094, 19.82470455841618318, -15.66946045147826005 ) ) ;
#18083=EDGE_LOOP ( 'NONE', ( #23281, #18031, #12363, #26963 ) ) ;
#18086=EDGE_CURVE ( 'NONE', #9786, #35377, #43180, .T. ) ;
#18087=CARTESIAN_POINT ( 'NONE',  ( -14.37046249213279658, -15.61618894467929941, 8.349999999999999645 ) ) ;
#18090=CARTESIAN_POINT ( 'NONE',  ( 10.69832412670059973, -64.89277703499729455, -17.91220997211459931 ) ) ;
#18095=DIRECTION ( 'NONE',  ( 0.4646601886423053496, 0.000000000000000000, 0.8854890790353641128 ) ) ;
#18099=ORIENTED_EDGE ( 'NONE', *, *, #24991, .F. ) ;
#18100=CARTESIAN_POINT ( 'NONE',  ( 8.949719927774109962, -63.11543068638779630, -46.63538165998269847 ) ) ;
#18102=ORIENTED_EDGE ( 'NONE', *, *, #80, .F. ) ;
#18104=CARTESIAN_POINT ( 'NONE',  ( 57.02861369184739715, 19.39567887796529888, -53.87746547175619583 ) ) ;
#18106=CARTESIAN_POINT ( 'NONE',  ( 54.08403600539600831, 19.39417787207790056, -76.77913599485849261 ) ) ;
#18108=CARTESIAN_POINT ( 'NONE',  ( 12.89074585065517731, -65.51103569875144217, -47.72398483027909322 ) ) ;
#18110=CARTESIAN_POINT ( 'NONE',  ( 44.34239523011500239, 12.74369304937430059, -3.187564294433600232 ) ) ;
#18114=VECTOR ( 'NONE', #35355, 1000.000000000000000 ) ;
#18118=ORIENTED_EDGE ( 'NONE', *, *, #17441, .F. ) ;
#18119=CARTESIAN_POINT ( 'NONE',  ( 18.38332385620206111, 20.94377882893676102, -75.56421372420827254 ) ) ;
#18123=CIRCLE ( 'NONE', #35713, 2.000000000000001332 ) ;
#18124=CARTESIAN_POINT ( 'NONE',  ( 13.60550091158079944, 20.19927249694839944, -74.14993703734479880 ) ) ;
#18125=DIRECTION ( 'NONE',  ( 0.000000000000000000, 0.000000000000000000, 1.000000000000000000 ) ) ;
#18126=CARTESIAN_POINT ( 'NONE',  ( 42.47711269216279817, -45.17107499119040170, -6.396649047033399427 ) ) ;
#18130=ORIENTED_EDGE ( 'NONE', *, *, #28482, .T. ) ;
#18131=CARTESIAN_POINT ( 'NONE',  ( 55.52353368598859618, -46.44448769124329601, -25.67613055164300206 ) ) ;
#18133=CARTESIAN_POINT ( 'NONE',  ( 55.27852839649509065, -50.91660802450510204, -75.28002343649311001 ) ) ;
#18134=CARTESIAN_POINT ( 'NONE',  ( 10.54211419205399913, 33.45297732329429863, -17.34131202171619890 ) ) ;
#18136=CARTESIAN_POINT ( 'NONE',  ( 47.47677450096290386, -54.59520210331019285, -54.66133488802340423 ) ) ;
#18139=CARTESIAN_POINT ( 'NONE',  ( -6.896489314860550834, -45.87074079319390307, -5.066771418161060581 ) ) ;
#18140=CARTESIAN_POINT ( 'NONE',  ( 47.55224309786800063, 23.32284541588479954, -54.73177068379369814 ) ) ;
#18143=CARTESIAN_POINT ( 'NONE',  ( 84.09627344016217876, -44.51518917121880037, -47.44643142112443712 ) ) ;
#18144=CARTESIAN_POINT ( 'NONE',  ( 33.83393739769579867, -15.61618894467939711, -10.44999999999995310 ) ) ;
#18145=CARTESIAN_POINT ( 'NONE',  ( 11.73811129726390057, 33.93366749707369934, -16.79398347924830048 ) ) ;
#18147=CARTESIAN_POINT ( 'NONE',  ( 68.13393739769819035, 19.47158195952289717, -70.40645085170193340 ) ) ;
#18149=LINE ( 'NONE', #30194, #777 ) ;
#18150=CARTESIAN_POINT ( 'NONE',  ( 56.49023934083049880, 15.04448206350489947, -26.27690413241280254 ) ) ;
#18151=CARTESIAN_POINT ( 'NONE',  ( 54.72925936106919664, 20.06372169638630254, -53.17373675974890546 ) ) ;
#18153=CARTESIAN_POINT ( 'NONE',  ( 53.59007319875249920, 18.17385789302069554, -49.22505640236219904 ) ) ;
#18154=FACE_BOUND ( 'NONE', #4785, .T. ) ;
#18156=CARTESIAN_POINT ( 'NONE',  ( 10.48948069982380105, 31.98855470695709968, -45.62594161163059425 ) ) ;
#18159=CARTESIAN_POINT ( 'NONE',  ( 65.03565853454030332, -32.24739025123630398, -17.83341341673349945 ) ) ;
#18164=LINE ( 'NONE', #41753, #35391 ) ;
#18165=CARTESIAN_POINT ( 'NONE',  ( 76.55049685366816448, -0.2018179213733399535, -13.44501669363641660 ) ) ;
#18167=CARTESIAN_POINT ( 'NONE',  ( 11.35394641258329962, -64.66333705649719832, -45.68067175734550744 ) ) ;
#18168=CARTESIAN_POINT ( 'NONE',  ( 57.50591362654369476, -45.29938006876010093, -25.92779769412700119 ) ) ;
#18175=CARTESIAN_POINT ( 'NONE',  ( 50.22560452902379780, -45.20442735010659874, -11.33119790093519974 ) ) ;
#18178=CARTESIAN_POINT ( 'NONE',  ( 15.24233146012789852, 19.83809465259359683, -21.55962016778659773 ) ) ;
#18179=DIRECTION ( 'NONE',  ( 0.000000000000000000, 0.000000000000000000, 1.000000000000000000 ) ) ;
#18182=CARTESIAN_POINT ( 'NONE',  ( 47.18305862770080239, -54.80685414274160649, -74.19838441418400521 ) ) ;
#18183=CARTESIAN_POINT ( 'NONE',  ( 57.81379994192599270, 13.88381319346640019, -10.22123296806000070 ) ) ;
#18184=CARTESIAN_POINT ( 'NONE',  ( 53.38983091223769151, 13.88381105532070059, -12.71718895194310051 ) ) ;
#18186=CARTESIAN_POINT ( 'NONE',  ( 51.03828701151719827, 19.65712598545220047, -76.15016576382599567 ) ) ;
#18188=CARTESIAN_POINT ( 'NONE',  ( 57.97678121319430034, 13.89683454802320028, -25.62129778225950005 ) ) ;
#18192=CYLINDRICAL_SURFACE ( 'NONE', #18838, 1.999999999999999112 ) ;
#18194=CARTESIAN_POINT ( 'NONE',  ( 9.342107117190629140, -63.49215653426838912, -16.98584847438329959 ) ) ;
#18197=EDGE_CURVE ( 'NONE', #4375, #4255, #39503, .T. ) ;
#18198=CARTESIAN_POINT ( 'NONE',  ( 19.54510609474682070, -55.47047341688053024, -75.55236793428606745 ) ) ;
#18201=CARTESIAN_POINT ( 'NONE',  ( 42.42181532145059464, 11.95990745222249885, -3.882827786777780066 ) ) ;
#18202=CARTESIAN_POINT ( 'NONE',  ( 47.41051750051865099, -54.24117355796746409, -75.29851419690288594 ) ) ;
#18205=CARTESIAN_POINT ( 'NONE',  ( 75.88268604566961528, -43.33643966824376292, -13.56553953253932221 ) ) ;
#18206=CARTESIAN_POINT ( 'NONE',  ( 18.66092887556369817, -51.71967070378909881, -74.96248001586319276 ) ) ;
#18214=CYLINDRICAL_SURFACE ( 'NONE', #10001, 21.19999999999999929 ) ;
#18219=FACE_OUTER_BOUND ( 'NONE', #38991, .T. ) ;
#18228=ORIENTED_EDGE ( 'NONE', *, *, #48977, .T. ) ;
#18234=CARTESIAN_POINT ( 'NONE',  ( 53.05142860133209837, -50.57489361360730129, -76.69950309512469744 ) ) ;
#18235=CARTESIAN_POINT ( 'NONE',  ( 60.77470318442130548, 14.33787658508280138, -47.45003995119949991 ) ) ;
#18238=CARTESIAN_POINT ( 'NONE',  ( 43.31519929709109817, 13.88514758459549903, -6.625476116054790587 ) ) ;
#18239=CARTESIAN_POINT ( 'NONE',  ( 41.78486010873790235, -43.67282288760589637, -3.688051967278440202 ) ) ;
#18240=DIRECTION ( 'NONE',  ( -0.8732394366197182567, 0.4872913772396111343, 0.000000000000000000 ) ) ;
#18246=CARTESIAN_POINT ( 'NONE',  ( 14.94451915430260058, -52.96147345225150360, -76.14999999999999147 ) ) ;
#18248=CARTESIAN_POINT ( 'NONE',  ( 57.25902743554100027, 19.38381105532069881, -53.91576847614940249 ) ) ;
#18252=AXIS2_PLACEMENT_3D ( 'NONE', #19334, #11225, #11997 ) ;
#18253=CARTESIAN_POINT ( 'NONE',  ( 47.18055146300900304, -54.80119377569329941, -74.36335264244719667 ) ) ;
#18255=CARTESIAN_POINT ( 'NONE',  ( 48.22131873952969983, -54.24500364010060594, -54.90936548946649509 ) ) ;
#18256=DIRECTION ( 'NONE',  ( 0.000000000000000000, 0.000000000000000000, 1.000000000000000000 ) ) ;
#18257=CARTESIAN_POINT ( 'NONE',  ( 56.50529364678479993, 19.52722159213979936, -53.84464738411570295 ) ) ;
#18258=CARTESIAN_POINT ( 'NONE',  ( 48.06666922905080241, 23.09813023377000007, -54.98957115198240331 ) ) ;
#18259=VERTEX_POINT ( 'NONE', #20848 ) ;
#18264=LINE ( 'NONE', #6229, #27713 ) ;
#18266=CARTESIAN_POINT ( 'NONE',  ( 83.98295738300248559, 13.34738318005249980, -47.35112499062080360 ) ) ;
#18267=CARTESIAN_POINT ( 'NONE',  ( 52.67986940689019804, 18.50721041040169723, -27.55370633776830047 ) ) ;
#18269=FACE_OUTER_BOUND ( 'NONE', #16519, .T. ) ;
#18272=ADVANCED_FACE ( 'NONE', ( #25026 ), #37683, .T. ) ;
#18273=ORIENTED_EDGE ( 'NONE', *, *, #13913, .F. ) ;
#18274=CARTESIAN_POINT ( 'NONE',  ( 11.51160566532330165, 19.89559162839070083, -21.14999999999999858 ) ) ;
#18277=CARTESIAN_POINT ( 'NONE',  ( 12.36320305068320025, -64.54682834576858852, -15.76422791927960176 ) ) ;
#18281=EDGE_LOOP ( 'NONE', ( #30294, #41182, #41123, #31908 ) ) ;
#18284=CARTESIAN_POINT ( 'NONE',  ( 56.63366319918780079, 14.90690265212999854, -26.25716060252799622 ) ) ;
#18285=CARTESIAN_POINT ( 'NONE',  ( 52.70796924836110264, 18.47694211103949513, -48.28462455411140297 ) ) ;
#18286=CARTESIAN_POINT ( 'NONE',  ( 16.13393739769620083, -15.61618894467929941, -5.093415854460129566 ) ) ;
#18287=CARTESIAN_POINT ( 'NONE',  ( 51.58109477403640852, -50.32311754940320014, -76.34882668000840056 ) ) ;
#18288=CARTESIAN_POINT ( 'NONE',  ( 57.07871704937310398, -50.59515825109639309, -53.12705742518219409 ) ) ;
#18289=VERTEX_POINT ( 'NONE', #34977 ) ;
#18291=CARTESIAN_POINT ( 'NONE',  ( 67.04038824939814845, 19.47158195952278703, -71.50000000000200373 ) ) ;
#18293=CARTESIAN_POINT ( 'NONE',  ( 16.13393739769620083, -15.61618894467929941, -6.649999999999999467 ) ) ;
#18298=CARTESIAN_POINT ( 'NONE',  ( 13.86858776757270029, -50.80169362180370030, -21.50776138482320121 ) ) ;
#18299=CARTESIAN_POINT ( 'NONE',  ( 56.55362051290479997, 19.42426019843370355, -75.00522130597019554 ) ) ;
#18300=CARTESIAN_POINT ( 'NONE',  ( 47.44035392459380063, -54.31358006272590444, -75.17661032366730467 ) ) ;
#18301=CARTESIAN_POINT ( 'NONE',  ( 56.79703944736839816, 13.88381105532070059, -15.79381048012069932 ) ) ;
#18304=CARTESIAN_POINT ( 'NONE',  ( 56.39270784037409356, -50.52750194525590643, -52.86271187285759510 ) ) ;
#18308=CARTESIAN_POINT ( 'NONE',  ( 47.61801185651960111, 23.31248621914309993, -74.14999581977218668 ) ) ;
#18311=CARTESIAN_POINT ( 'NONE',  ( 60.41799884498815487, -45.84359652593187917, -47.74079192425801921 ) ) ;
#18312=CARTESIAN_POINT ( 'NONE',  ( 12.16144474485684768, -65.27546953796887408, -23.67678868528984282 ) ) ;
#18313=FACE_OUTER_BOUND ( 'NONE', #16343, .T. ) ;
#18315=CARTESIAN_POINT ( 'NONE',  ( 82.13853704237929776, 14.37236558661899899, -47.68296857959820301 ) ) ;
#18320=CARTESIAN_POINT ( 'NONE',  ( -32.51565489538130294, -10.90840876578639929, -55.84912116621229927 ) ) ;
#18322=CARTESIAN_POINT ( 'NONE',  ( 53.30562535473109875, -49.43700197435749999, -49.00290876415049723 ) ) ;
#18324=CIRCLE ( 'NONE', #25870, 2.000000000005381029 ) ;
#18325=CARTESIAN_POINT ( 'NONE',  ( 13.61938558678000000, -51.42721352342299923, -23.15000000000000213 ) ) ;
#18327=CARTESIAN_POINT ( 'NONE',  ( 14.26125502349160001, 19.88540718429639753, -22.45522374605300087 ) ) ;
#18328=CARTESIAN_POINT ( 'NONE',  ( 55.88236915028019780, 14.71303907941189948, -25.32898514049750105 ) ) ;
#18332=CARTESIAN_POINT ( 'NONE',  ( 53.29384558423090112, 19.31433099946569953, -38.31189016485890875 ) ) ;
#18333=CARTESIAN_POINT ( 'NONE',  ( 52.68730263070079900, 18.52618134853540255, -48.67466845563539835 ) ) ;
#18334=CARTESIAN_POINT ( 'NONE',  ( 56.08437014463689962, -45.70248814750440403, -17.93020000568909822 ) ) ;
#18336=DIRECTION ( 'NONE',  ( -0.4640893551880601597, 0.8857883891771953788, 0.000000000000000000 ) ) ;
#18339=ADVANCED_FACE ( 'NONE', ( #373 ), #16354, .T. ) ;
#18341=CARTESIAN_POINT ( 'NONE',  ( 11.42523121492209803, 34.02364939933359977, -47.34553053307450199 ) ) ;
#18343=CARTESIAN_POINT ( 'NONE',  ( 10.95445192191350081, -65.05736586563961055, -17.59525104008959673 ) ) ;
#18344=CARTESIAN_POINT ( 'NONE',  ( 68.13393739769620083, -5.291188944679320549, -65.65000000000000568 ) ) ;
#18350=CARTESIAN_POINT ( 'NONE',  ( 10.14834886040009998, -63.32547621192500031, -45.99365407406120454 ) ) ;
#18353=CARTESIAN_POINT ( 'NONE',  ( 56.99190255423440021, 19.40009799747580033, -53.87165542209760360 ) ) ;
#18354=CARTESIAN_POINT ( 'NONE',  ( 52.94902642261280334, 19.16795121501379739, -76.96923112046120252 ) ) ;
#18356=CARTESIAN_POINT ( 'NONE',  ( 12.39246200372603646, -65.46010474685600400, -47.59569286707705515 ) ) ;
#18361=CARTESIAN_POINT ( 'NONE',  ( 61.28398356453099893, 14.37233669519349988, -47.68178229854910199 ) ) ;
#18363=VERTEX_POINT ( 'NONE', #25750 ) ;
#18364=VECTOR ( 'NONE', #46786, 1000.000000000000000 ) ;
#18366=CARTESIAN_POINT ( 'NONE',  ( 56.77874227380610250, -46.03157376887470065, -26.24782688674920195 ) ) ;
#18368=CIRCLE ( 'NONE', #42669, 2.000990444728826478 ) ;
#18369=AXIS2_PLACEMENT_3D ( 'NONE', #47804, #31787, #51728 ) ;
#18371=AXIS2_PLACEMENT_3D ( 'NONE', #39555, #51608, #15963 ) ;
#18372=DIRECTION ( 'NONE',  ( -0.7288689868556628149, -0.6846531968814575375, 0.000000000000000000 ) ) ;
#18373=ADVANCED_FACE ( 'NONE', ( #22083 ), #6639, .T. ) ;
#18374=AXIS2_PLACEMENT_3D ( 'NONE', #22391, #50707, #50456 ) ;
#18375=CARTESIAN_POINT ( 'NONE',  ( 13.67086563049960013, 20.77210737664869811, -75.25165125838280744 ) ) ;
#18376=EDGE_CURVE ( 'NONE', #5505, #6515, #14497, .T. ) ;
#18379=CARTESIAN_POINT ( 'NONE',  ( 41.48255094495939233, -45.14737637117200109, -5.927812803735399427 ) ) ;
#18382=ORIENTED_EDGE ( 'NONE', *, *, #680, .T. ) ;
#18383=CARTESIAN_POINT ( 'NONE',  ( 53.30594783414570514, -49.06367964803780524, -26.83653110996110414 ) ) ;
#18384=CARTESIAN_POINT ( 'NONE',  ( 55.72320022523830119, -50.85322541441449573, -75.08289664133350527 ) ) ;
#18385=CARTESIAN_POINT ( 'NONE',  ( 8.676985760002459358, 30.83576240877370012, -14.06454189394279908 ) ) ;
#18391=CARTESIAN_POINT ( 'NONE',  ( 47.51200636829759816, 23.35279827620210114, -54.77739120475299472 ) ) ;
#18392=EDGE_CURVE ( 'NONE', #42976, #5735, #31140, .T. ) ;
#18394=CARTESIAN_POINT ( 'NONE',  ( 16.65420337943509566, -51.11618894467930119, -15.67544740040250062 ) ) ;
#18396=CARTESIAN_POINT ( 'NONE',  ( 12.07292176418630092, 34.00632605457140301, -16.81897063588079888 ) ) ;
#18398=CARTESIAN_POINT ( 'NONE',  ( 53.01430328511310108, 18.33235873846370012, -48.82220831118790016 ) ) ;
#18399=CARTESIAN_POINT ( 'NONE',  ( 19.31281851427826979, 24.25684300136392579, -75.75074683321228974 ) ) ;
#18400=CARTESIAN_POINT ( 'NONE',  ( 57.45269164222676750, -50.61618894467929408, -53.92796674551637182 ) ) ;
#18401=CARTESIAN_POINT ( 'NONE',  ( 55.20995175243899666, 16.06746250602089887, -26.39668292074910028 ) ) ;
#18403=CARTESIAN_POINT ( 'NONE',  ( 50.54226496161154358, 4.781393461198343076, -76.21662484925313663 ) ) ;
#18408=CARTESIAN_POINT ( 'NONE',  ( 52.82359344163219816, 18.46824642947949968, -48.95125676800460468 ) ) ;
#18409=CARTESIAN_POINT ( 'NONE',  ( 20.00021293481310991, 23.80000987844158900, -18.69523849944957661 ) ) ;
#18410=CARTESIAN_POINT ( 'NONE',  ( 10.49122530401870002, 32.03394370215789877, -45.62557954680809758 ) ) ;
#18414=CARTESIAN_POINT ( 'NONE',  ( 67.26279129939560164, -32.31925440466879706, -18.54865058075920103 ) ) ;
#18417=EDGE_LOOP ( 'NONE', ( #49287, #38883, #3931, #38213 ) ) ;
#18418=CARTESIAN_POINT ( 'NONE',  ( 56.83258906378680564, 19.07284248766010393, -52.72698304056530105 ) ) ;
#18419=CARTESIAN_POINT ( 'NONE',  ( 76.49775090137842426, -3.049984699541625321, -13.21772653487406579 ) ) ;
#18421=CARTESIAN_POINT ( 'NONE',  ( 12.71291116475580019, -65.48164264958541025, -47.17968986901090034 ) ) ;
#18422=CARTESIAN_POINT ( 'NONE',  ( 56.05387567297529472, -45.72969253901850095, -25.37923299446759984 ) ) ;
#18424=CARTESIAN_POINT ( 'NONE',  ( 51.67587649748470113, -33.96749857170579645, -77.01363636363508647 ) ) ;
#18425=CARTESIAN_POINT ( 'NONE',  ( 11.53606103740170674, 24.11867657901759188, -21.73577486392030167 ) ) ;
#18433=CARTESIAN_POINT ( 'NONE',  ( 14.61081989482540067, 19.82232334755109804, -21.82083395457759778 ) ) ;
#18437=CARTESIAN_POINT ( 'NONE',  ( 46.40846215724359780, -53.01587003390369546, -76.14999999999999147 ) ) ;
#18438=CARTESIAN_POINT ( 'NONE',  ( 61.43493858089180293, 13.88381322377179927, -11.19371918816710121 ) ) ;
#18441=AXIS2_PLACEMENT_3D ( 'NONE', #17668, #37847, #33109 ) ;
#18442=EDGE_CURVE ( 'NONE', #19573, #30462, #8576, .T. ) ;
#18446=CARTESIAN_POINT ( 'NONE',  ( 53.12919740953070402, 20.11397505193579960, -75.74183034380359913 ) ) ;
#18447=DIRECTION ( 'NONE',  ( -0.1999849291396485207, 0.9797989733190221040, 0.000000000000000000 ) ) ;
#18449=CLOSED_SHELL ( 'NONE', ( #2229, #23551, #27947, #21730, #39611, #9917, #21564, #644, #1892, #27720, #14260, #19685, #14325, #37490, #32690, #44127, #4039, #21202, #31840, #23500, #12765, #5427, #34104, #9817, #30005, #20974, #49485, #29214, #48574, #49005, #26809, #39241, #4491, #51217, #13068, #3371, #31741, #2415, #20693, #30739, #13491, #9430, #22880, #5625, #35527, #45973, #28799, #25397, #16491, #47177, #36480, #7823, #46358, #35193, #44883, #13505, #15656, #33753, #41161, #39680, #44135, #4016, #25209, #51825, #41000, #29516, #5040, #43671, #48339, #46520, #11167, #558, #42587, #43534, #22741, #37429, #19156, #50780, #6797, #47341, #12320, #41204, #21914, #44060, #4363, #49338, #12077, #29427, #17528, #2948, #8265, #15556, #9366, #2784, #22282, #6165, #2760, #3826, #51796, #22111, #44718, #30230, #16782, #3560, #14537, #51475, #50101, #49360, #5228, #3702, #25998, #44715, #33231, #33526, #27142, #39095, #16882, #44358, #1108, #7312, #38643, #38094, #35662, #10963, #17617, #43845, #6281, #39596, #18495, #16096, #48738, #11757, #3481, #12254, #19402, #37911, #35502, #37616, #41706, #42580, #15453, #18774, #20313, #14074, #17968, #38206, #7383, #26524, #10071, #1348, #17439, #9822, #13951, #3321, #38809, #30166, #11405, #14505, #1471, #18834, #17353, #49070, #11444, #12457, #28428, #6014, #46328, #10994, #24279, #28029, #33055, #48500, #5000, #37791, #18339, #22091, #36109, #47282, #46950, #26230, #45399, #25780, #32134, #17640, #27660, #9466, #23218, #2437, #10172, #4111, #24870, #36316, #41929, #34805, #10704, #25431, #18272, #19498, #9751, #47823, #27378, #26114, #47338, #22039, #46631, #37518, #19146, #26488, #42295, #49478, #32262, #42349, #28409, #36856, #23504, #13688, #30803, #10523, #28082, #22502, #12137, #21074, #49935, #26827, #30950, #35893, #25185, #51456, #23685, #44549, #37321, #48565, #41920, #23868, #21936, #7634, #28021, #44470, #31073, #38872, #21960, #23208, #33452, #37050, #31750, #9478, #50231, #7440, #18928, #44353, #11112, #1243, #15193, #1306, #26366, #17689, #49659, #29134, #47285, #3454, #19328, #12449, #32246, #13885, #44660, #15846, #37873, #28498, #40985, #23342, #10422, #4307, #11318, #47587, #2222, #25764, #12453, #39512, #17415, #9167, #14560, #14357, #20986, #9240, #47324, #7121, #46508, #50931, #16153, #17926, #10210, #28008, #37607, #33648, #25459, #19750, #15005, #13430, #1010, #25761, #51190, #28675, #7568, #45838, #32993, #6731, #48547, #27839, #14642, #25636, #4852, #10930, #16794, #24548, #29619, #46468, #50498, #42506, #41626, #36014, #1414, #43780, #5382, #8519, #33272, #19090, #27270, #32182, #34490, #36649, #25362, #25367, #47090, #48615, #24052, #50344, #33506, #29773, #27662, #12173, #3244, #27629, #22537, #9981, #4054, #40939, #25863, #18373, #8336, #40551, #28046, #17986, #19691, #15333, #808, #39737, #26082, #22042, #50191 ) ) ;
#18452=B_SPLINE_SURFACE_WITH_KNOTS ( 'NONE', 3, 3, ( 
 ( #27586, #43590, #24860, #7695, #23132, #4972, #20941, #3760, #19727, #35719, #30998, #47025, #47779, #34019, #17034, #38235 ),
 ( #41383, #13363, #22226, #49268, #49012, #37714, #5749, #32985, #1812, #50029, #17792, #1554, #33765, #26158, #1301, #25894 ),
 ( #37202, #17542, #49777, #13870, #21705, #29826, #10199, #14123, #45064, #21195, #29578, #29323, #41132, #2075, #45328, #13117 ),
 ( #29068, #9433, #9166, #25122, #5243, #30088, #49526, #45845, #46113, #25382, #9932, #33513, #18054, #25637, #5500, #21456 ),
 ( #41907, #6007, #37455, #42168, #21966, #41640, #37976, #6267, #17291, #33252, #13617, #45584, #9678, #14894, #14638, #15421 ),
 ( #46890, #10976, #42433, #19341, #27195, #30608, #22742, #10715, #7298, #23249, #11497, #31374, #10460, #42949, #22485, #7558 ),
 ( #50547, #26943, #51061, #35055, #23502, #42693, #26671, #38760, #15160, #35325, #30348, #2855, #31120, #50295, #47145, #46372 ),
 ( #18819, #6523, #18567, #11234, #39266, #43208, #3368, #3113, #38491, #22997, #51324, #47401, #7045, #46629, #6788, #2593 ),
 ( #39018, #34802, #27454, #43456, #19080, #2327, #18301, #34273, #26414, #50806, #14383, #34544, #30861, #51831, #707, #24274 ),
 ( #32137, #27711, #4638, #12516, #15931, #8069, #47905, #44478, #8588, #48681, #16699, #47649, #28219, #7814, #44741, #39779 ) ),
 .UNSPECIFIED., .F., .F., .F.,
 ( 4, 1, 1, 1, 1, 1, 1, 4 ),
 ( 4, 2, 2, 2, 2, 2, 2, 4 ),
 ( -1.660620507699999833E-05, 0.1428571428571430157, 0.2857142857142860315, 0.4285714285714289917, 0.5714285714285709528, 0.7142857142857139685, 0.8571428571428569843, 1.000000000000000000 ),
 ( -4.238744881723909508, -3.233993249338640297, -2.649205172199279978, -2.119364137759419897, -1.854443620539500071, -1.430570792987609918, -0.7523742689045949117, 1.660620507699999833E-05 ),
 .UNSPECIFIED. ) ;
#18453=VERTEX_POINT ( 'NONE', #2708 ) ;
#18454=CARTESIAN_POINT ( 'NONE',  ( 50.87608087775580401, 20.94596473442846474, -52.56694610553643798 ) ) ;
#18455=CARTESIAN_POINT ( 'NONE',  ( -3.169058842316599733, -49.13863347070289933, -5.723027784144280261 ) ) ;
#18456=CARTESIAN_POINT ( 'NONE',  ( 76.42237218134170007, -8.479666956846260817, -12.89291724745850054 ) ) ;
#18458=CARTESIAN_POINT ( 'NONE',  ( 61.28085240419530066, -45.60177449860450594, -47.67834116410560341 ) ) ;
#18460=CYLINDRICAL_SURFACE ( 'NONE', #28144, 1.999999999999997113 ) ;
#18462=CARTESIAN_POINT ( 'NONE',  ( 42.10819013808320221, 12.38958205234360044, -4.221348723159180416 ) ) ;
#18463=CARTESIAN_POINT ( 'NONE',  ( 83.89200044194980421, -48.61618894467930119, -53.92796738110899923 ) ) ;
#18464=CARTESIAN_POINT ( 'NONE',  ( 20.08284749614042752, 24.18831317000414316, -74.66536237503798645 ) ) ;
#18465=CARTESIAN_POINT ( 'NONE',  ( 56.48535462447713229, 19.53533792649655609, -53.84780261153423453 ) ) ;
#18466=CARTESIAN_POINT ( 'NONE',  ( 76.09582226312808473, -43.31040105692301267, -13.69678534746457998 ) ) ;
#18467=CARTESIAN_POINT ( 'NONE',  ( 18.17711126944659839, -51.44957460136649274, -75.17186369576970151 ) ) ;
#18468=DIRECTION ( 'NONE',  ( 0.3294064756440933661, -0.9441882088883217783, -3.885780586188048878E-16 ) ) ;
#18482=ORIENTED_EDGE ( 'NONE', *, *, #49978, .F. ) ;
#18484=CARTESIAN_POINT ( 'NONE',  ( -8.719958794165998839, 10.48190171173589924, -1.467676683391609949 ) ) ;
#18485=CARTESIAN_POINT ( 'NONE',  ( 61.37851597766940159, -45.20507541364400339, -46.76684488029780340 ) ) ;
#18488=CARTESIAN_POINT ( 'NONE',  ( 82.61176104757076644, -45.25366171719064567, -47.15273383853318734 ) ) ;
#18495=ADVANCED_FACE ( 'NONE', ( #31488, #27060 ), #15535, .T. ) ;
#18497=ORIENTED_EDGE ( 'NONE', *, *, #19210, .T. ) ;
#18499=CARTESIAN_POINT ( 'NONE',  ( 53.12920058238260168, -51.34635257275360232, -75.74182960172289825 ) ) ;
#18500=CARTESIAN_POINT ( 'NONE',  ( 60.35981425105420328, 14.50694145909750077, -47.43164998684069644 ) ) ;
#18503=CARTESIAN_POINT ( 'NONE',  ( 41.26856075654099953, -44.30227235397150309, -4.473876447391639921 ) ) ;
#18504=CARTESIAN_POINT ( 'NONE',  ( 72.38393739883420608, 11.88381105532070059, -61.34712802272770915 ) ) ;
#18505=CARTESIAN_POINT ( 'NONE',  ( 53.35699421374690132, 18.69401400300939642, -74.14999999999999147 ) ) ;
#18506=EDGE_CURVE ( 'NONE', #1848, #41267, #39133, .T. ) ;
#18513=CARTESIAN_POINT ( 'NONE',  ( 15.05440318628160057, -53.11618894467930119, -76.14999999999999147 ) ) ;
#18514=CARTESIAN_POINT ( 'NONE',  ( 43.44336167987420083, 14.78804531073750006, -7.898836396374890434 ) ) ;
#18517=CARTESIAN_POINT ( 'NONE',  ( 11.25398292730271699, 32.98847748115480982, -44.13762314148468846 ) ) ;
#18519=AXIS2_PLACEMENT_3D ( 'NONE', #42485, #2905, #3163 ) ;
#18523=CARTESIAN_POINT ( 'NONE',  ( 47.93639096317230042, -54.33238953985980402, -54.72300757058719967 ) ) ;
#18525=CARTESIAN_POINT ( 'NONE',  ( 56.51188083447149779, 19.51190917532160185, -53.61551639950400272 ) ) ;
#18526=CARTESIAN_POINT ( 'NONE',  ( 47.87127561442579804, 23.20009848796649976, -55.10367382876560072 ) ) ;
#18527=ORIENTED_EDGE ( 'NONE', *, *, #40911, .F. ) ;
#18531=CARTESIAN_POINT ( 'NONE',  ( 82.68191173840780550, 14.16984533597115892, -47.42735572498546048 ) ) ;
#18532=CARTESIAN_POINT ( 'NONE',  ( 56.17779366879769753, -45.64891426883350078, -28.15000000000000213 ) ) ;
#18534=CARTESIAN_POINT ( 'NONE',  ( 46.63833728752520358, -15.61618894467929586, 8.349999999999999645 ) ) ;
#18541=CARTESIAN_POINT ( 'NONE',  ( 12.13449217321720042, -64.93994367287498903, -16.24910028839300224 ) ) ;
#18542=CARTESIAN_POINT ( 'NONE',  ( 55.40394000045360201, 13.88381105524500114, -14.52023566624100148 ) ) ;
#18543=CARTESIAN_POINT ( 'NONE',  ( 11.96163130524179863, 33.91328095712900392, -45.68067242534929306 ) ) ;
#18544=CARTESIAN_POINT ( 'NONE',  ( 9.596651609803041438, -63.85482046095769704, -46.54795879700470351 ) ) ;
#18549=CARTESIAN_POINT ( 'NONE',  ( 56.65715976508769813, 14.88738284562609948, -26.25499670583540279 ) ) ;
#18550=EDGE_CURVE ( 'NONE', #35503, #1409, #44210, .T. ) ;
#18551=CARTESIAN_POINT ( 'NONE',  ( 53.24163931742309330, 18.19088059586060169, -48.94155518170179420 ) ) ;
#18552=CARTESIAN_POINT ( 'NONE',  ( 59.45957930948410564, -2.821832259794109898, -15.69652041387840313 ) ) ;
#18553=CARTESIAN_POINT ( 'NONE',  ( 50.76151237207749745, -49.57686851637080139, -76.22310723638240404 ) ) ;
#18555=CARTESIAN_POINT ( 'NONE',  ( 58.94369020000790726, -48.22803363231889762, -50.52845975241639565 ) ) ;
#18558=CARTESIAN_POINT ( 'NONE',  ( 68.13393739769810509, 19.38381105532030091, -71.50000000000198952 ) ) ;
#18559=ORIENTED_EDGE ( 'NONE', *, *, #8212, .F. ) ;
#18560=DIRECTION ( 'NONE',  ( 0.000000000000000000, 1.000000000000000000, 0.000000000000000000 ) ) ;
#18562=CIRCLE ( 'NONE', #44487, 1.999999999999999556 ) ;
#18564=CARTESIAN_POINT ( 'NONE',  ( 13.72445191873659986, -50.97659916996759932, -21.83805850002029914 ) ) ;
#18565=CARTESIAN_POINT ( 'NONE',  ( 55.08889524890580702, 19.54142126883120056, -75.71946145358849378 ) ) ;
#18566=CARTESIAN_POINT ( 'NONE',  ( 47.45530976305949622, -54.40699705883139359, -75.00633330157590706 ) ) ;
#18567=CARTESIAN_POINT ( 'NONE',  ( 55.86383447201379937, 13.89944776690939854, -14.96898266773339969 ) ) ;
#18574=CARTESIAN_POINT ( 'NONE',  ( 47.51796367685790301, 23.14532755365199890, -75.00952367221340467 ) ) ;
#18576=CARTESIAN_POINT ( 'NONE',  ( 42.48913188665730445, -45.89176091220130616, -7.200515191634200285 ) ) ;
#18580=CARTESIAN_POINT ( 'NONE',  ( 82.31238640809949914, 14.12525339545430114, -47.32928036526049453 ) ) ;
#18581=DIRECTION ( 'NONE',  ( 0.000000000000000000, 0.000000000000000000, 1.000000000000000000 ) ) ;
#18585=CARTESIAN_POINT ( 'NONE',  ( -12.40573950840240158, 24.76782207504269806, -51.46982831076010001 ) ) ;
#18586=ORIENTED_EDGE ( 'NONE', *, *, #47979, .T. ) ;
#18588=CARTESIAN_POINT ( 'NONE',  ( 52.79729141543799642, -49.69127189832200031, -48.80671576205540418 ) ) ;
#18590=EDGE_LOOP ( 'NONE', ( #33903, #37064, #2551, #47360 ) ) ;
#18594=CARTESIAN_POINT ( 'NONE',  ( 13.81672828808540032, 19.99687498807509911, -22.59435085047379843 ) ) ;
#18598=CARTESIAN_POINT ( 'NONE',  ( 52.61723362075139931, 18.57919235090369980, -48.56631533107179877 ) ) ;
#18599=CARTESIAN_POINT ( 'NONE',  ( 54.87171479455280121, -45.91467920100570410, -15.83443052021550201 ) ) ;
#18600=DIRECTION ( 'NONE',  ( 0.6676418852214537347, -0.2329255526947816568, 0.7071067811863875896 ) ) ;
#18603=CARTESIAN_POINT ( 'NONE',  ( 10.85466582836159866, -64.96696992582000973, -17.55961494274349732 ) ) ;
#18604=CARTESIAN_POINT ( 'NONE',  ( 12.82693890801849967, 34.27287537764330239, -47.70039286047789773 ) ) ;
#18606=CARTESIAN_POINT ( 'NONE',  ( 11.91450189635219914, -65.43783483100590104, -17.98631677234039827 ) ) ;
#18607=CARTESIAN_POINT ( 'NONE',  ( 53.41947877929934663, -49.46401953720203437, -49.21225703112888539 ) ) ;
#18610=ORIENTED_EDGE ( 'NONE', *, *, #40800, .F. ) ;
#18612=VERTEX_POINT ( 'NONE', #24652 ) ;
#18613=CARTESIAN_POINT ( 'NONE',  ( 10.97954134168909945, -63.36237133050840242, -44.74488567032319963 ) ) ;
#18616=EDGE_LOOP ( 'NONE', ( #11177, #24419, #44668, #28710, #11989, #1271, #44719, #28105, #13039, #6763, #4312, #29373, #23362, #44178 ) ) ;
#18618=CARTESIAN_POINT ( 'NONE',  ( 56.94040701897879586, 19.11191676585499977, -52.81451654899269954 ) ) ;
#18619=CARTESIAN_POINT ( 'NONE',  ( 52.47790439711100419, 19.10383386520929605, -76.75890347663309399 ) ) ;
#18620=( BOUNDED_CURVE ( )  B_SPLINE_CURVE ( 3, ( #34694, #3002, #18973, #14793 ),
 .UNSPECIFIED., .F., .T. ) 
 B_SPLINE_CURVE_WITH_KNOTS ( ( 4, 4 ),
 ( 4.114144097965610314, 4.712388980384689674 ),
 .UNSPECIFIED. ) 
 CURVE ( )  GEOMETRIC_REPRESENTATION_ITEM ( )  RATIONAL_B_SPLINE_CURVE ( ( 1.000000000000000000, 0.9703969717270918283, 0.9703969717270918283, 1.000000000000000000 ) ) 
 REPRESENTATION_ITEM ( '' )  );
#18622=CARTESIAN_POINT ( 'NONE',  ( 10.73552253366480791, -65.02568017672894030, -47.16673513639202042 ) ) ;
#18623=CARTESIAN_POINT ( 'NONE',  ( 73.38393739769610136, 11.88381105532070059, -84.94863984844540994 ) ) ;
#18630=EDGE_LOOP ( 'NONE', ( #24264, #48523, #37771, #8866 ) ) ;
#18634=CARTESIAN_POINT ( 'NONE',  ( 53.55180673896649779, -49.41892566828619948, -49.22385633645210135 ) ) ;
#18639=CARTESIAN_POINT ( 'NONE',  ( 45.31002868286061869, -45.55093754943392526, -8.676028226913116370 ) ) ;
#18641=CARTESIAN_POINT ( 'NONE',  ( 45.73972096110129826, -45.13933825624529561, -7.826076092515011240 ) ) ;
#18645=CARTESIAN_POINT ( 'NONE',  ( 53.67452698258109933, -48.64253627208800168, -26.37822025900080192 ) ) ;
#18646=CIRCLE ( 'NONE', #34541, 1.000000000000000444 ) ;
#18647=CARTESIAN_POINT ( 'NONE',  ( 54.67791766314789470, -50.80000226043880218, -75.87478752159950091 ) ) ;
#18648=CARTESIAN_POINT ( 'NONE',  ( -2.620161787266110043, 18.79900506017029826, -6.313712515450228935 ) ) ;
#18652=ORIENTED_EDGE ( 'NONE', *, *, #2724, .T. ) ;
#18653=FACE_OUTER_BOUND ( 'NONE', #46656, .T. ) ;
#18654=CARTESIAN_POINT ( 'NONE',  ( 47.65224270186909905, 23.25978157783099931, -54.72055524659549519 ) ) ;
#18655=CARTESIAN_POINT ( 'NONE',  ( 42.44161405036800261, -44.94940367324450392, -5.942266020708489194 ) ) ;
#18656=CARTESIAN_POINT ( 'NONE',  ( 16.29798161965023340, -51.09008541970372619, -15.67302014731996884 ) ) ;
#18657=CARTESIAN_POINT ( 'NONE',  ( 12.13393739769600010, -55.41568642894409180, -74.14999999999999147 ) ) ;
#18658=CARTESIAN_POINT ( 'NONE',  ( 11.98493272671680110, 33.91167211021750205, -16.63579482024520217 ) ) ;
#18660=CARTESIAN_POINT ( 'NONE',  ( 52.92965938904679746, 18.37620054566669836, -48.75165688956650456 ) ) ;
#18662=CARTESIAN_POINT ( 'NONE',  ( 59.53646453344369860, -46.29317990693370177, -47.84962771692820382 ) ) ;
#18663=CARTESIAN_POINT ( 'NONE',  ( 53.47775468590610615, 17.84057308464530323, -27.23453477576759951 ) ) ;
#18664=CARTESIAN_POINT ( 'NONE',  ( 50.50438588722870747, 22.08300093761100058, -54.79905802874080223 ) ) ;
#18666=CARTESIAN_POINT ( 'NONE',  ( 52.93759153535863504, -49.56812172796623628, -27.78191009280273249 ) ) ;
#18667=CARTESIAN_POINT ( 'NONE',  ( 12.33251669429900055, -64.64566256145140244, -15.86092359077770020 ) ) ;
#18670=CARTESIAN_POINT ( 'NONE',  ( 11.10533104901869983, 31.90439051286449867, -44.25028207899379851 ) ) ;
#18674=CARTESIAN_POINT ( 'NONE',  ( 12.61864224197218753, 24.22902235285175365, -75.44170189642458979 ) ) ;
#18679=CARTESIAN_POINT ( 'NONE',  ( 49.44253838235640330, -2.211264110977851249, -15.73253926033974004 ) ) ;
#18681=CARTESIAN_POINT ( 'NONE',  ( 11.61883035538269837, -64.83086464985760244, -45.15685323010969654 ) ) ;
#18682=CARTESIAN_POINT ( 'NONE',  ( 57.58585165456680244, -45.11742656075429636, -25.40978046210479846 ) ) ;
#18688=CARTESIAN_POINT ( 'NONE',  ( 11.68627894964089897, 34.01944678469089922, -23.21012450963720042 ) ) ;
#18694=DIRECTION ( 'NONE',  ( 1.000000000000000000, 0.000000000000000000, 0.000000000000000000 ) ) ;
#18696=CARTESIAN_POINT ( 'NONE',  ( 14.53575789044414179, 20.42331746235014123, -75.51793353177379231 ) ) ;
#18697=CARTESIAN_POINT ( 'NONE',  ( 47.29369706019910780, -54.69301655985149324, -74.50208837960660446 ) ) ;
#18698=CARTESIAN_POINT ( 'NONE',  ( 56.12350828326769658, 13.88381105527479953, -10.09721077832690028 ) ) ;
#18701=CIRCLE ( 'NONE', #37116, 20.00000000000001421 ) ;
#18703=CARTESIAN_POINT ( 'NONE',  ( 52.03944399862420056, 20.14552308598300101, -75.97489327918991364 ) ) ;
#18704=CARTESIAN_POINT ( 'NONE',  ( 65.44700836391344012, -29.90809997924516495, -16.55186812364802051 ) ) ;
#18706=EDGE_LOOP ( 'NONE', ( #40085, #4273, #48137, #50985 ) ) ;
#18707=CARTESIAN_POINT ( 'NONE',  ( 55.20622393724549681, -47.44937218557269887, -26.50255988908530114 ) ) ;
#18708=CARTESIAN_POINT ( 'NONE',  ( -0.1141852257953769878, -53.55957259884640109, -9.165264109987230512 ) ) ;
#18709=CARTESIAN_POINT ( 'NONE',  ( 75.09787083995549040, -5.899466855358239670, -11.55750054373280022 ) ) ;
#18711=CARTESIAN_POINT ( 'NONE',  ( 75.23800589958599971, 13.54856819491975628, -14.24441830867649550 ) ) ;
#18712=CARTESIAN_POINT ( 'NONE',  ( 61.12479307673544326, -45.49567662917237243, -47.50325115173827584 ) ) ;
#18713=PLANE ( 'NONE',  #8015 ) ;
#18714=CARTESIAN_POINT ( 'NONE',  ( 82.13853704237929776, -45.64188066427789892, -47.72348187592570667 ) ) ;
#18715=CARTESIAN_POINT ( 'NONE',  ( 20.13393739768959634, -55.41568642894479524, -74.14999999999999147 ) ) ;
#18716=CARTESIAN_POINT ( 'NONE',  ( 41.80294713309100274, 12.64028208340220161, -4.284453812058900191 ) ) ;
#18717=CARTESIAN_POINT ( 'NONE',  ( 61.50409964634459925, -45.37406455498979341, -47.35437808299670337 ) ) ;
#18721=CARTESIAN_POINT ( 'NONE',  ( 76.42619217002265941, -43.25680179181886587, -13.99059237503525921 ) ) ;
#18722=CARTESIAN_POINT ( 'NONE',  ( 18.19607795909060144, -52.32664520840270228, -75.76244777734170555 ) ) ;
#18723=CARTESIAN_POINT ( 'NONE',  ( 50.34331689155069967, -43.49784654392259853, -6.583704156889679915 ) ) ;
#18724=ORIENTED_EDGE ( 'NONE', *, *, #11827, .F. ) ;
#18729=CARTESIAN_POINT ( 'NONE',  ( 61.25261794522180026, -45.60868630189549577, -47.68548325530770882 ) ) ;
#18733=CARTESIAN_POINT ( 'NONE',  ( 40.95781332748470049, -45.40040647908620741, -5.890461096499439719 ) ) ;
#18734=ORIENTED_EDGE ( 'NONE', *, *, #30208, .T. ) ;
#18735=ORIENTED_EDGE ( 'NONE', *, *, #28969, .T. ) ;
#18736=EDGE_CURVE ( 'NONE', #21139, #32383, #35344, .T. ) ;
#18738=CYLINDRICAL_SURFACE ( 'NONE', #15164, 2.000000000000000000 ) ;
#18739=CARTESIAN_POINT ( 'NONE',  ( 61.27165170594810206, -45.24929849883929478, -46.82601857492619501 ) ) ;
#18743=VECTOR ( 'NONE', #7826, 1000.000000000000000 ) ;
#18747=ORIENTED_EDGE ( 'NONE', *, *, #46923, .T. ) ;
#18749=CARTESIAN_POINT ( 'NONE',  ( 57.24929578595761370, 19.38381105532069881, -75.24227954309296251 ) ) ;
#18752=CARTESIAN_POINT ( 'NONE',  ( 51.08534762786979400, -51.03566300605200468, -76.14824064460249531 ) ) ;
#18753=CARTESIAN_POINT ( 'NONE',  ( 60.57311214287879864, 14.37431803774079953, -47.23458252443460026 ) ) ;
#18757=CARTESIAN_POINT ( 'NONE',  ( 43.01559835719150016, -42.64215176563499909, -3.897419375871189917 ) ) ;
#18759=CARTESIAN_POINT ( 'NONE',  ( -7.075746994739700035, 14.57312359469660201, -5.375837286899690426 ) ) ;
#18763=CARTESIAN_POINT ( 'NONE',  ( 27.73905384484250192, -51.70197538230620182, -75.56421356237308373 ) ) ;
#18767=CARTESIAN_POINT ( 'NONE',  ( 14.46581869571789980, -52.64324949044350177, -76.02664804518839503 ) ) ;
#18768=AXIS2_PLACEMENT_3D ( 'NONE', #25779, #34946, #10607 ) ;
#18769=CARTESIAN_POINT ( 'NONE',  ( 57.43834588691519372, 18.88596480251339926, -52.60518497626989642 ) ) ;
#18772=CARTESIAN_POINT ( 'NONE',  ( 15.03857555098429977, 19.44687904844289861, -20.69450120486289890 ) ) ;
#18773=CARTESIAN_POINT ( 'NONE',  ( 47.18324198357289845, -54.80726809202429450, -74.14999999999999147 ) ) ;
#18774=ADVANCED_FACE ( 'NONE', ( #17343 ), #25178, .T. ) ;
#18776=CARTESIAN_POINT ( 'NONE',  ( 47.88635031718219892, -54.41166180851149647, -54.97299310976289632 ) ) ;
#18778=CARTESIAN_POINT ( 'NONE',  ( 56.44265055894529581, 19.46638121170060387, -53.28298866551109114 ) ) ;
#18780=CARTESIAN_POINT ( 'NONE',  ( 47.89164947663859806, 23.14006492512999813, -54.78346000236360425 ) ) ;
#18784=CARTESIAN_POINT ( 'NONE',  ( 60.82468473753360172, -45.47215345142849685, -47.02385344690110713 ) ) ;
#18785=CARTESIAN_POINT ( 'NONE',  ( 82.71778650988362358, 14.26036297868509806, -47.55446714344091674 ) ) ;
#18788=DIRECTION ( 'NONE',  ( 0.000000000000000000, 0.000000000000000000, 1.000000000000000000 ) ) ;
#18791=FACE_OUTER_BOUND ( 'NONE', #41507, .T. ) ;
#18792=VERTEX_POINT ( 'NONE', #10253 ) ;
#18793=DIRECTION ( 'NONE',  ( 1.000000000000000000, 0.000000000000000000, 0.000000000000000000 ) ) ;
#18795=ORIENTED_EDGE ( 'NONE', *, *, #36418, .F. ) ;
#18796=CARTESIAN_POINT ( 'NONE',  ( 12.21465728043759924, -64.70109133449230399, -15.93455456223260036 ) ) ;
#18799=CARTESIAN_POINT ( 'NONE',  ( 9.874256513748090214, -64.47111594000269008, -46.84384315240179575 ) ) ;
#18800=VERTEX_POINT ( 'NONE', #5295 ) ;
#18803=CARTESIAN_POINT ( 'NONE',  ( 50.52790554252050015, 22.07298246124559782, -54.91101322106069915 ) ) ;
#18804=CARTESIAN_POINT ( 'NONE',  ( 56.75395847353610179, 14.81488913387570072, -26.24860350449169744 ) ) ;
#18807=CARTESIAN_POINT ( 'NONE',  ( 62.79356416660980500, 0.07457836432415800021, -16.79771323086600177 ) ) ;
#18808=CARTESIAN_POINT ( 'NONE',  ( 52.11373191115499992, -49.71238562294659857, -77.07264795032170923 ) ) ;
#18809=CARTESIAN_POINT ( 'NONE',  ( 57.57137425765949956, -49.32502029382759900, -51.58238510503450414 ) ) ;
#18814=DIRECTION ( 'NONE',  ( 0.000000000000000000, 0.000000000000000000, 1.000000000000000000 ) ) ;
#18815=CARTESIAN_POINT ( 'NONE',  ( 60.34379258661509482, -45.86802437805019395, -47.72732609191810127 ) ) ;
#18817=CARTESIAN_POINT ( 'NONE',  ( 13.41567315973499852, -51.08505356990979607, -21.91538238065540156 ) ) ;
#18819=CARTESIAN_POINT ( 'NONE',  ( 55.36114547021439591, 13.90104188525289963, -14.57735786978359904 ) ) ;
#18824=ORIENTED_EDGE ( 'NONE', *, *, #34767, .T. ) ;
#18825=CIRCLE ( 'NONE', #25512, 1.999999999999999556 ) ;
#18826=CARTESIAN_POINT ( 'NONE',  ( 47.49699394960070009, 23.15488270540389948, -75.00831418912220272 ) ) ;
#18832=CARTESIAN_POINT ( 'NONE',  ( 52.13393739769620083, -15.61618894467929941, 6.349999999999999645 ) ) ;
#18833=CARTESIAN_POINT ( 'NONE',  ( 82.13853704237929776, 14.40950277491920062, -47.72348187592570667 ) ) ;
#18834=ADVANCED_FACE ( 'NONE', ( #16165 ), #33481, .T. ) ;
#18838=AXIS2_PLACEMENT_3D ( 'NONE', #14010, #26039, #10342 ) ;
#18841=CARTESIAN_POINT ( 'NONE',  ( -33.86618693412709291, -20.49226357331469828, -57.52971779843680622 ) ) ;
#18844=CARTESIAN_POINT ( 'NONE',  ( 52.68891395819000678, -49.75006725190949197, -48.47378032971909789 ) ) ;
#18845=ORIENTED_EDGE ( 'NONE', *, *, #23318, .T. ) ;
#18848=CARTESIAN_POINT ( 'NONE',  ( 14.07775902432950055, 19.81371361753149785, -22.00375624323179835 ) ) ;
#18849=CARTESIAN_POINT ( 'NONE',  ( 13.09383361200632123, 24.26765008030419679, -75.86242720135740569 ) ) ;
#18851=CARTESIAN_POINT ( 'NONE',  ( 53.12059652019419786, 18.33618219888390044, -49.12440246944070310 ) ) ;
#18857=CARTESIAN_POINT ( 'NONE',  ( 11.22168587317889887, -65.22927114923599845, -17.68872783567509899 ) ) ;
#18858=CARTESIAN_POINT ( 'NONE',  ( 9.071903935231079075, 32.31445225605110494, -46.64254262187220235 ) ) ;
#18861=CARTESIAN_POINT ( 'NONE',  ( 52.84346301666477785, -49.69122173838943013, -48.96941052353703583 ) ) ;
#18863=AXIS2_PLACEMENT_3D ( 'NONE', #14978, #30944, #39099 ) ;
#18864=CARTESIAN_POINT ( 'NONE',  ( 50.12109376404330163, -53.47864665676989659, -55.01406006385839476 ) ) ;
#18866=EDGE_CURVE ( 'NONE', #14297, #5682, #46259, .T. ) ;
#18870=CARTESIAN_POINT ( 'NONE',  ( 9.736686533375289443, -63.21034557680579979, -46.29811293505660075 ) ) ;
#18874=CARTESIAN_POINT ( 'NONE',  ( 57.18371624250119822, 19.38400875315999983, -53.90359198974339705 ) ) ;
#18875=CARTESIAN_POINT ( 'NONE',  ( 52.93656362771660184, 19.08184182246549909, -77.15175517737969813 ) ) ;
#18877=CYLINDRICAL_SURFACE ( 'NONE', #4841, 2.000000000000003553 ) ;
#18878=CARTESIAN_POINT ( 'NONE',  ( 7.517033938252880354, 30.35161808146150264, -19.14999999999999858 ) ) ;
#18879=CARTESIAN_POINT ( 'NONE',  ( 14.79003424252982057, 21.13935400224803018, -76.01806011803036256 ) ) ;
#18880=CARTESIAN_POINT ( 'NONE',  ( 57.36123081458359962, -50.13537923174280309, -52.61896056486340001 ) ) ;
#18881=B_SPLINE_SURFACE_WITH_KNOTS ( 'NONE', 3, 3, ( 
 ( #38964, #43661, #3831, #46838, #27149, #19028, #31578, #27403, #15108, #47348 ),
 ( #43404, #11183, #7248, #22947, #18772, #43154, #39727, #35538, #35003, #34744 ),
 ( #11698, #31068, #27661, #7505, #38710, #50753, #6993, #39477, #2801, #23196 ),
 ( #51271, #39213, #23452, #3577, #19291, #42898, #23714, #14847, #30810, #3057 ),
 ( #10924, #26889, #35272, #15369, #31323, #1940, #17920, #26808, #30479, #38888 ),
 ( #33636, #42297, #2202, #22094, #46240, #2976, #13996, #13744, #2453, #49653 ),
 ( #14509, #42820, #18433, #18178, #34407, #6916, #33891, #42561, #49902, #29955 ),
 ( #10590, #45971, #38105, #29697, #5871, #10328, #42036, #37845, #26289, #10064 ),
 ( #38628, #26024, #34144, #34668, #6137, #50156, #22867, #45709, #21838, #14252 ),
 ( #50672, #50421, #30221, #46499, #6397, #26545, #22356, #38359, #6652, #9810 ) ),
 .UNSPECIFIED., .F., .F., .F.,
 ( 4, 1, 1, 1, 1, 1, 1, 4 ),
 ( 4, 2, 2, 2, 4 ),
 ( -7.647483580428189077E-05, 0.1428571428571430157, 0.2857142857142860315, 0.4285714285714289917, 0.5714285714285709528, 0.7142857142857139685, 0.8571428571428569843, 1.000068219203180009 ),
 ( -0.8959923838512789951, -0.7377509475120830329, -0.4200977637871100012, -0.1578379958887219936, 7.344577026599998924E-05 ),
 .UNSPECIFIED. ) ;
#18891=VECTOR ( 'NONE', #16135, 1000.000000000000000 ) ;
#18892=CARTESIAN_POINT ( 'NONE',  ( 59.13393739769620083, -15.61618894467929941, -15.65000000000000036 ) ) ;
#18893=CARTESIAN_POINT ( 'NONE',  ( 69.63393739769620083, 6.883811055320649963, -71.50000000000000000 ) ) ;
#18894=FACE_OUTER_BOUND ( 'NONE', #28624, .T. ) ;
#18895=CARTESIAN_POINT ( 'NONE',  ( 11.88460916116889976, 33.59273172673110963, -16.16716782997540136 ) ) ;
#18897=CARTESIAN_POINT ( 'NONE',  ( 53.55220836886790181, -48.78100643530040514, -26.47327747818699706 ) ) ;
#18900=CARTESIAN_POINT ( 'NONE',  ( 55.36944056199379816, -50.82556113491280314, -75.41474324147199582 ) ) ;
#18901=CARTESIAN_POINT ( 'NONE',  ( -6.745630838839370647, 14.94319942760500020, -5.463640701264131039 ) ) ;
#18903=CARTESIAN_POINT ( 'NONE',  ( 47.25382592556910311, -54.75228172359690149, -54.62311712267080566 ) ) ;
#18904=FACE_OUTER_BOUND ( 'NONE', #9677, .T. ) ;
#18905=EDGE_CURVE ( 'NONE', #2493, #37502, #46502, .T. ) ;
#18907=CARTESIAN_POINT ( 'NONE',  ( -11.32734370190460105, -41.88171845330919751, -6.430192534648670133 ) ) ;
#18908=CARTESIAN_POINT ( 'NONE',  ( 47.65564868057830239, 23.28640233928300063, -54.93645362307179880 ) ) ;
#18910=CARTESIAN_POINT ( 'NONE',  ( 16.46706851333994592, -51.11618894468167440, -15.67516967139586548 ) ) ;
#18911=CARTESIAN_POINT ( 'NONE',  ( 13.51940423530409952, 19.36859641292999967, -21.33263318241190021 ) ) ;
#18912=CARTESIAN_POINT ( 'NONE',  ( 60.99063469145590233, 14.41619031400530027, -47.70729047236519449 ) ) ;
#18913=CARTESIAN_POINT ( 'NONE',  ( 11.22384627824540004, 33.78040140241470368, -16.94931753701080268 ) ) ;
#18914=CARTESIAN_POINT ( 'NONE',  ( 51.86328208370509429, 18.67428979098259845, -76.68384257635129586 ) ) ;
#18915=CARTESIAN_POINT ( 'NONE',  ( 52.79481764036179925, 18.44745459499829821, -48.50058864900179856 ) ) ;
#18917=DIRECTION ( 'NONE',  ( -0.9151634328774630456, 0.3898247278254499681, -0.1025308377989340020 ) ) ;
#18918=CARTESIAN_POINT ( 'NONE',  ( 53.04703063237690230, 18.20237249300480187, -27.50709361416090104 ) ) ;
#18921=CARTESIAN_POINT ( 'NONE',  ( 52.66149042093859123, 18.55528232251300125, -48.73886901161859697 ) ) ;
#18924=CARTESIAN_POINT ( 'NONE',  ( 11.13393739769619906, 32.11747391597780421, -43.91739627612010111 ) ) ;
#18927=CARTESIAN_POINT ( 'NONE',  ( 65.95897347940848476, -32.09849744266369953, -17.73193878851440175 ) ) ;
#18928=ADVANCED_FACE ( 'NONE', ( #25036 ), #48665, .F. ) ;
#18929=AXIS2_PLACEMENT_3D ( 'NONE', #30894, #26705, #2105 ) ;
#18931=ORIENTED_EDGE ( 'NONE', *, *, #35386, .T. ) ;
#18933=CARTESIAN_POINT ( 'NONE',  ( 42.93197233849409855, 11.32569894967160096, -3.187564294433600232 ) ) ;
#18935=CARTESIAN_POINT ( 'NONE',  ( 51.06529787577495227, 0.2493625510273632662, -16.95223896232651484 ) ) ;
#18936=ORIENTED_EDGE ( 'NONE', *, *, #21437, .F. ) ;
#18937=CARTESIAN_POINT ( 'NONE',  ( 11.42316304585989961, -64.61387295428639277, -45.17482744339589829 ) ) ;
#18938=CARTESIAN_POINT ( 'NONE',  ( 56.13881711988070577, -45.75862301436319513, -25.71798066937759941 ) ) ;
#18942=ORIENTED_EDGE ( 'NONE', *, *, #6699, .T. ) ;
#18943=CARTESIAN_POINT ( 'NONE',  ( 11.69795627133467697, 34.16744399712961666, -22.44873498087175179 ) ) ;
#18945=CIRCLE ( 'NONE', #26486, 19.56371635397779940 ) ;
#18946=CARTESIAN_POINT ( 'NONE',  ( 11.82668577431979884, 33.14159547282380203, -24.59829236961180143 ) ) ;
#18949=VECTOR ( 'NONE', #43294, 1000.000000000000000 ) ;
#18951=DIRECTION ( 'NONE',  ( -1.000000000000000000, 0.000000000000000000, 0.000000000000000000 ) ) ;
#18953=CARTESIAN_POINT ( 'NONE',  ( 61.47160170490100484, -29.95828558899940219, -16.07879158819200072 ) ) ;
#18955=CARTESIAN_POINT ( 'NONE',  ( 47.24443041864720527, -54.45681227993460283, -75.11586948118589646 ) ) ;
#18956=CARTESIAN_POINT ( 'NONE',  ( 43.44710262568360548, 12.61051141539170040, -5.048133889203059610 ) ) ;
#18957=PLANE ( 'NONE',  #30930 ) ;
#18959=DIRECTION ( 'NONE',  ( 0.000000000000000000, 0.000000000000000000, 1.000000000000000000 ) ) ;
#18963=CARTESIAN_POINT ( 'NONE',  ( 4.835529188070480267, -58.78041738421249818, -12.99353756526149972 ) ) ;
#18964=CARTESIAN_POINT ( 'NONE',  ( 75.04668702423900584, -18.75119728547959852, -11.30405884009489981 ) ) ;
#18965=CARTESIAN_POINT ( 'NONE',  ( 75.41376673900958849, 12.86054230907423879, -13.63390496164747567 ) ) ;
#18966=CARTESIAN_POINT ( 'NONE',  ( 19.53780474230963193, -55.47109714356856358, -75.55954122747178303 ) ) ;
#18967=CARTESIAN_POINT ( 'NONE',  ( 14.84957949698884683, -16.54932958072287263, -11.23251175440650051 ) ) ;
#18968=CARTESIAN_POINT ( 'NONE',  ( 47.18324198357279897, 23.57489020266570279, -54.61058319554400242 ) ) ;
#18969=CARTESIAN_POINT ( 'NONE',  ( 82.34851808037059584, -45.64188066427789892, -47.72348187592570667 ) ) ;
#18970=CARTESIAN_POINT ( 'NONE',  ( 12.94455701826820082, 19.08483511945829747, -21.18967814235449865 ) ) ;
#18971=CARTESIAN_POINT ( 'NONE',  ( 57.48892408827569511, -50.38497325094370183, -52.98966502147489877 ) ) ;
#18972=CARTESIAN_POINT ( 'NONE',  ( 41.57697698334229841, 12.60893760990930090, -3.558127426236100010 ) ) ;
#18973=CARTESIAN_POINT ( 'NONE',  ( 67.78236843376265597, -30.11618894467929763, -17.74895402404430911 ) ) ;
#18976=CIRCLE ( 'NONE', #12292, 17.39999999999999503 ) ;
#18980=CARTESIAN_POINT ( 'NONE',  ( 17.92442291492480066, -51.57142019855179882, -75.41551559479479749 ) ) ;
#18981=CARTESIAN_POINT ( 'NONE',  ( 42.99567057238449763, -45.11618894467940066, -6.881716687611570293 ) ) ;
#18984=ORIENTED_EDGE ( 'NONE', *, *, #30459, .F. ) ;
#18990=CARTESIAN_POINT ( 'NONE',  ( 42.22416898896209858, -45.44812850840609997, -6.646931848296280698 ) ) ;
#18991=ORIENTED_EDGE ( 'NONE', *, *, #7236, .T. ) ;
#18992=CARTESIAN_POINT ( 'NONE',  ( 17.30738868478190184, 21.72103359751309881, -76.14999999999999147 ) ) ;
#18997=ORIENTED_EDGE ( 'NONE', *, *, #26844, .F. ) ;
#18998=CARTESIAN_POINT ( 'NONE',  ( 8.815605938724019097, -63.28267558148569094, -46.67186391142220003 ) ) ;
#19002=CIRCLE ( 'NONE', #25683, 2.000000000000001776 ) ;
#19005=ORIENTED_EDGE ( 'NONE', *, *, #5966, .T. ) ;
#19007=B_SPLINE_CURVE_WITH_KNOTS ( 'NONE', 3,
 ( #21018, #4522, #28359, #44363, #37017, #8726 ),
 .UNSPECIFIED., .F., .F.,
 ( 4, 1, 1, 4 ),
 ( 0.000000000000000000, 0.3333333333333329263, 0.6666666666666669627, 1.000000000000000000 ),
 .UNSPECIFIED. ) ;
#19011=CARTESIAN_POINT ( 'NONE',  ( 51.61430885013370329, -51.17530555596519548, -76.09751502629850961 ) ) ;
#19012=CARTESIAN_POINT ( 'NONE',  ( 60.53709663307620303, 14.40413707899699958, -47.33107028358159596 ) ) ;
#19015=LINE ( 'NONE', #7753, #46827 ) ;
#19016=CARTESIAN_POINT ( 'NONE',  ( 65.05986622648850926, 0.9377769643968115743, -17.72011801484886107 ) ) ;
#19017=CARTESIAN_POINT ( 'NONE',  ( -3.812186623206120117, 16.87714592095479915, -5.022395698517160056 ) ) ;
#19019=CYLINDRICAL_SURFACE ( 'NONE', #2990, 31.00000000000000000 ) ;
#19022=FACE_OUTER_BOUND ( 'NONE', #4313, .T. ) ;
#19024=CARTESIAN_POINT ( 'NONE',  ( 57.39562476827909876, 19.32839297046770000, -53.44831944760920095 ) ) ;
#19028=CARTESIAN_POINT ( 'NONE',  ( 15.41374403315509944, 19.54065027890899842, -20.47798662115040003 ) ) ;
#19034=CARTESIAN_POINT ( 'NONE',  ( 48.20452265730919805, -54.29503287064169825, -55.30665343754630214 ) ) ;
#19036=CARTESIAN_POINT ( 'NONE',  ( 56.40078553072510203, 19.31196876521530115, -52.89577359589869587 ) ) ;
#19037=CARTESIAN_POINT ( 'NONE',  ( 12.14367607025980789, 22.37708546437701429, -21.73578643762689211 ) ) ;
#19038=ORIENTED_EDGE ( 'NONE', *, *, #22802, .F. ) ;
#19040=VERTEX_POINT ( 'NONE', #43354 ) ;
#19043=CARTESIAN_POINT ( 'NONE',  ( 47.93639096317219384, -54.33238953986003139, -54.72300757058784626 ) ) ;
#19044=CARTESIAN_POINT ( 'NONE',  ( 83.62685937867283315, 13.30364075603329255, -46.55427984015698684 ) ) ;
#19046=CARTESIAN_POINT ( 'NONE',  ( 82.75388200178990417, 14.36257604166400093, -47.67228907607350408 ) ) ;
#19051=ORIENTED_EDGE ( 'NONE', *, *, #19285, .F. ) ;
#19053=ORIENTED_EDGE ( 'NONE', *, *, #4549, .T. ) ;
#19054=VECTOR ( 'NONE', #12160, 1000.000000000000000 ) ;
#19055=EDGE_CURVE ( 'NONE', #22521, #11543, #39932, .T. ) ;
#19060=CARTESIAN_POINT ( 'NONE',  ( 12.26489985407230066, -65.41013428201999602, -47.36052460643420403 ) ) ;
#19061=ORIENTED_EDGE ( 'NONE', *, *, #10372, .F. ) ;
#19063=CARTESIAN_POINT ( 'NONE',  ( 65.03603135454920903, 1.015437840524759938, -17.83403478221330118 ) ) ;
#19064=CARTESIAN_POINT ( 'NONE',  ( 56.61099403853209822, 14.92704628377260079, -26.25969108334859925 ) ) ;
#19067=CARTESIAN_POINT ( 'NONE',  ( 59.58714391122960308, -1.728360499025269892, -15.83152262783869801 ) ) ;
#19068=CARTESIAN_POINT ( 'NONE',  ( 51.43375901386550453, -49.25898423961760386, -76.62099598227180763 ) ) ;
#19069=DIRECTION ( 'NONE',  ( 0.000000000000000000, 0.000000000000000000, 1.000000000000000000 ) ) ;
#19071=ORIENTED_EDGE ( 'NONE', *, *, #48674, .T. ) ;
#19074=CARTESIAN_POINT ( 'NONE',  ( 68.13393739769620083, 1.883811055320649963, -65.65000000000000568 ) ) ;
#19078=CARTESIAN_POINT ( 'NONE',  ( 13.21399250059920050, -50.88310479779730144, -21.61005667689260079 ) ) ;
#19080=CARTESIAN_POINT ( 'NONE',  ( 56.48652151861699622, 13.88381105532070059, -15.35311052695679912 ) ) ;
#19083=VECTOR ( 'NONE', #30108, 999.9999999999998863 ) ;
#19086=ORIENTED_EDGE ( 'NONE', *, *, #2134, .F. ) ;
#19087=CARTESIAN_POINT ( 'NONE',  ( 13.60549529218709885, -51.43164378700710415, -74.36773579016251290 ) ) ;
#19089=DIRECTION ( 'NONE',  ( -6.940534999999999567E-13, 3.000959000000000097E-13, -1.000000000000000000 ) ) ;
#19090=ADVANCED_FACE ( 'NONE', ( #36492 ), #36238, .T. ) ;
#19091=CARTESIAN_POINT ( 'NONE',  ( 54.63655381128389621, -48.05296878824569973, -26.73577887340519865 ) ) ;
#19094=CARTESIAN_POINT ( 'NONE',  ( 8.784728771152170879, 23.70287936274029761, -46.67204636145419983 ) ) ;
#19096=CARTESIAN_POINT ( 'NONE',  ( 82.25807928850851169, 13.89010898168029939, -46.55740818416200000 ) ) ;
#19098=CARTESIAN_POINT ( 'NONE',  ( 47.57073483231042133, 23.21246685024514633, -74.81156575745629311 ) ) ;
#19101=CARTESIAN_POINT ( 'NONE',  ( 49.66352655669150096, 22.42445118933569859, -54.86856413023149770 ) ) ;
#19103=CARTESIAN_POINT ( 'NONE',  ( 52.73806811560410068, -49.71908181329310139, -48.65317700872209628 ) ) ;
#19105=ORIENTED_EDGE ( 'NONE', *, *, #3724, .T. ) ;
#19108=CARTESIAN_POINT ( 'NONE',  ( 13.79101907244350045, 20.01225008817899820, -22.61438297437780065 ) ) ;
#19109=CARTESIAN_POINT ( 'NONE',  ( 52.08784026747549945, -49.61362475023040020, -77.13961137824819048 ) ) ;
#19111=CARTESIAN_POINT ( 'NONE',  ( 52.85422457117920203, 18.44426668863140151, -48.94261452190229988 ) ) ;
#19117=ORIENTED_EDGE ( 'NONE', *, *, #6498, .T. ) ;
#19118=CARTESIAN_POINT ( 'NONE',  ( 55.16626882053050451, 17.34692063200439804, -48.76159087390789892 ) ) ;
#19119=CARTESIAN_POINT ( 'NONE',  ( 10.79909669237359893, 33.81695037855629948, -47.18321592309199985 ) ) ;
#19122=CARTESIAN_POINT ( 'NONE',  ( 53.36461353568414268, -49.48324289032532164, -49.20419813977648005 ) ) ;
#19125=CARTESIAN_POINT ( 'NONE',  ( 52.59140206479120394, -52.14549427466430842, -53.43195377655929690 ) ) ;
#19128=CARTESIAN_POINT ( 'NONE',  ( 63.88393739769619373, -15.61618894467929941, -61.44999999999999574 ) ) ;
#19129=CARTESIAN_POINT ( 'NONE',  ( 10.77166557288789939, -63.24731521998059947, -45.20467220225359739 ) ) ;
#19130=CARTESIAN_POINT ( 'NONE',  ( 68.13393739769706769, 17.98087126524489321, -74.20351669811762463 ) ) ;
#19133=CARTESIAN_POINT ( 'NONE',  ( 57.22241557355649633, 19.34714437185240143, -53.44445692377340151 ) ) ;
#19134=CARTESIAN_POINT ( 'NONE',  ( 52.63065796082889847, 19.00050544084379922, -76.99620446115829964 ) ) ;
#19136=CARTESIAN_POINT ( 'NONE',  ( 11.24959019013326689, -65.20486053845806396, -47.30001787599645979 ) ) ;
#19137=DIRECTION ( 'NONE',  ( 0.000000000000000000, -0.7371541402007413257, 0.6757246285173463818 ) ) ;
#19138=DIRECTION ( 'NONE',  ( 0.1686178020941689892, 0.6660492713794449182, -0.7265992051412129005 ) ) ;
#19142=EDGE_CURVE ( 'NONE', #23772, #17403, #28714, .T. ) ;
#19146=ADVANCED_FACE ( 'NONE', ( #32803 ), #1903, .F. ) ;
#19148=FACE_OUTER_BOUND ( 'NONE', #23624, .T. ) ;
#19151=CARTESIAN_POINT ( 'NONE',  ( 50.89984241516300045, 13.88381105524969961, -11.21907654918599917 ) ) ;
#19156=ADVANCED_FACE ( 'NONE', ( #45150 ), #33721, .T. ) ;
#19157=CARTESIAN_POINT ( 'NONE',  ( 12.00872700126539883, 33.65412506900099743, -16.20508613915610141 ) ) ;
#19160=CIRCLE ( 'NONE', #34213, 2.000000000000002220 ) ;
#19161=EDGE_CURVE ( 'NONE', #19396, #1406, #3566, .T. ) ;
#19163=CARTESIAN_POINT ( 'NONE',  ( 56.29089617305770332, -50.69853828341889113, -75.05641376200790660 ) ) ;
#19164=CARTESIAN_POINT ( 'NONE',  ( -5.266416193449879657, 16.47668896006809902, -5.857206300276859956 ) ) ;
#19165=FACE_OUTER_BOUND ( 'NONE', #48715, .T. ) ;
#19167=DIRECTION ( 'NONE',  ( 0.000000000000000000, 0.000000000000000000, 1.000000000000000000 ) ) ;
#19169=CARTESIAN_POINT ( 'NONE',  ( -10.44076365005610008, -42.78597905884220154, -5.977015742479820481 ) ) ;
#19170=CARTESIAN_POINT ( 'NONE',  ( 47.62315909503939793, 23.31001273183260025, -55.12979940376899890 ) ) ;
#19171=FACE_OUTER_BOUND ( 'NONE', #22807, .T. ) ;
#19175=CARTESIAN_POINT ( 'NONE',  ( 51.91394611766279610, 18.24433502379679695, -77.01723340761438408 ) ) ;
#19176=CARTESIAN_POINT ( 'NONE',  ( 52.84630368501289865, 18.42025081107430040, -48.68178166803490114 ) ) ;
#19177=CARTESIAN_POINT ( 'NONE',  ( 61.13393739769620083, -33.11618894467940066, -84.38499399519520239 ) ) ;
#19178=CARTESIAN_POINT ( 'NONE',  ( 52.85589391196879916, -49.64722623523429945, -48.63421165633150167 ) ) ;
#19179=CARTESIAN_POINT ( 'NONE',  ( 53.73157595231050720, 17.54735927887150027, -26.98518945364950383 ) ) ;
#19180=CARTESIAN_POINT ( 'NONE',  ( 49.70112820465420356, 22.42515808270010069, -55.00786376658820132 ) ) ;
#19183=CARTESIAN_POINT ( 'NONE',  ( 62.59312592420069876, -31.41572991903020196, -16.88303165987050036 ) ) ;
#19185=CARTESIAN_POINT ( 'NONE',  ( 11.13393739769619906, 31.97814667466609961, -43.91303247421570433 ) ) ;
#19187=CARTESIAN_POINT ( 'NONE',  ( 59.49262858449159808, 19.24776070067098743, -53.20292136905285929 ) ) ;
#19188=CARTESIAN_POINT ( 'NONE',  ( 16.13393739769620083, -15.61618894467929941, -7.049999999999999822 ) ) ;
#19194=CARTESIAN_POINT ( 'NONE',  ( 55.92590552531359549, -45.91410834023890430, -25.53549666432709842 ) ) ;
#19206=B_SPLINE_CURVE_WITH_KNOTS ( 'NONE', 3,
 ( #43472, #39542, #23523, #38512 ),
 .UNSPECIFIED., .F., .F.,
 ( 4, 4 ),
 ( 0.8075652778063105997, 1.000000000000000000 ),
 .UNSPECIFIED. ) ;
#19208=CIRCLE ( 'NONE', #40159, 36.00000000000000000 ) ;
#19209=CYLINDRICAL_SURFACE ( 'NONE', #4617, 1.999999999999997113 ) ;
#19210=EDGE_CURVE ( 'NONE', #39784, #26977, #49850, .T. ) ;
#19211=CARTESIAN_POINT ( 'NONE',  ( 61.11794773234890243, -29.17036088169449926, -15.93336420193230296 ) ) ;
#19213=CARTESIAN_POINT ( 'NONE',  ( 47.13611152337789889, -54.39493520228780454, -75.29258675765889564 ) ) ;
#19215=CARTESIAN_POINT ( 'NONE',  ( 44.44825913150810237, 14.59247941183189923, -8.385990530560489375 ) ) ;
#19216=FACE_OUTER_BOUND ( 'NONE', #35641, .T. ) ;
#19217=CARTESIAN_POINT ( 'NONE',  ( 83.54413676250719334, -44.84521321811879346, -47.09683803678880309 ) ) ;
#19218=CARTESIAN_POINT ( 'NONE',  ( 11.78395124410701733, 34.19034018309990586, -17.88069317967955740 ) ) ;
#19221=ORIENTED_EDGE ( 'NONE', *, *, #31100, .F. ) ;
#19222=CARTESIAN_POINT ( 'NONE',  ( 53.40733904913949459, -49.15934302735570327, -27.32642110322520423 ) ) ;
#19223=CARTESIAN_POINT ( 'NONE',  ( -0.2286426098680529873, -53.48569616968499929, -9.495855095443920035 ) ) ;
#19224=CARTESIAN_POINT ( 'NONE',  ( 76.27673450680259748, -29.93995206988050128, -12.62359417470960032 ) ) ;
#19225=CYLINDRICAL_SURFACE ( 'NONE', #1188, 1.999999999999997113 ) ;
#19228=AXIS2_PLACEMENT_3D ( 'NONE', #35777, #32072, #28931 ) ;
#19229=CARTESIAN_POINT ( 'NONE',  ( 12.90754703535734826, -55.48555899889392862, -75.71503644607005867 ) ) ;
#19231=CARTESIAN_POINT ( 'NONE',  ( 47.18324198357279897, 23.57489020266570279, -54.61058319554400242 ) ) ;
#19234=CARTESIAN_POINT ( 'NONE',  ( 57.28635611951199991, -50.59344279636220421, -53.60270239407589798 ) ) ;
#19235=CARTESIAN_POINT ( 'NONE',  ( 41.57451193271510448, 12.62954792915630087, -3.761783078136979874 ) ) ;
#19238=CARTESIAN_POINT ( 'NONE',  ( 57.09844697708260242, -47.42443381619079901, -47.88085270719169273 ) ) ;
#19239=FACE_OUTER_BOUND ( 'NONE', #42289, .T. ) ;
#19240=CARTESIAN_POINT ( 'NONE',  ( 68.16820805406568695, -1.116429576517300015, -18.00618044202539991 ) ) ;
#19241=CARTESIAN_POINT ( 'NONE',  ( 18.43783208065170243, -51.93606027628250388, -75.41551559479479749 ) ) ;
#19242=CARTESIAN_POINT ( 'NONE',  ( 50.21208614976480078, -53.15602288804570463, -53.95043619330500206 ) ) ;
#19247=CARTESIAN_POINT ( 'NONE',  ( 8.786667189176620596, 31.89283771814190160, -46.67161560189330061 ) ) ;
#19252=CARTESIAN_POINT ( 'NONE',  ( 44.99427537170129199, -45.82358684235350665, -8.742754287369370658 ) ) ;
#19254=CARTESIAN_POINT ( 'NONE',  ( 17.48782757528399756, 21.61970083732919790, -76.12726769927830617 ) ) ;
#19255=ORIENTED_EDGE ( 'NONE', *, *, #16581, .F. ) ;
#19259=DIRECTION ( 'NONE',  ( 0.000000000000000000, 0.000000000000000000, 1.000000000000000000 ) ) ;
#19262=ORIENTED_EDGE ( 'NONE', *, *, #34201, .T. ) ;
#19263=DIRECTION ( 'NONE',  ( 1.000000000000000000, 0.000000000000000000, 0.000000000000000000 ) ) ;
#19264=EDGE_CURVE ( 'NONE', #30581, #10936, #27045, .T. ) ;
#19267=AXIS2_PLACEMENT_3D ( 'NONE', #37062, #1160, #13745 ) ;
#19269=ORIENTED_EDGE ( 'NONE', *, *, #35181, .T. ) ;
#19271=CARTESIAN_POINT ( 'NONE',  ( 51.90125965379149875, -51.26050537052380207, -76.04050507290840244 ) ) ;
#19273=CARTESIAN_POINT ( 'NONE',  ( 60.91201348210339717, 14.41240981587099945, -47.67204987013359840 ) ) ;
#19274=AXIS2_PLACEMENT_3D ( 'NONE', #47314, #27875, #47561 ) ;
#19275=AXIS2_PLACEMENT_3D ( 'NONE', #18110, #37259, #49326 ) ;
#19276=B_SPLINE_CURVE_WITH_KNOTS ( 'NONE', 3,
 ( #3677, #4175, #47699, #20151, #1282, #28528, #16230, #41367, #40340, #40590 ),
 .UNSPECIFIED., .F., .F.,
 ( 4, 2, 2, 2, 4 ),
 ( 0.000000000000000000, 0.1774999999994806010, 0.3374999999985014987, 0.4374999999978896326, 0.5000003605096956516 ),
 .UNSPECIFIED. ) ;
#19280=CARTESIAN_POINT ( 'NONE',  ( -6.118916323140140001, 15.26694961539969952, -5.118327416809539621 ) ) ;
#19282=CARTESIAN_POINT ( 'NONE',  ( 47.13701521578290965, 23.47046883074774470, -74.81156575898371841 ) ) ;
#19285=EDGE_CURVE ( 'NONE', #45555, #1409, #9488, .T. ) ;
#19287=DIRECTION ( 'NONE',  ( 0.8535492322677342703, -0.3460892072839221734, 0.3894559907059431669 ) ) ;
#19291=CARTESIAN_POINT ( 'NONE',  ( 15.22027405775829934, 19.63653300932890033, -20.91173439138579937 ) ) ;
#19294=CARTESIAN_POINT ( 'NONE',  ( 61.25723466965784780, 14.07825688653815632, -47.12444968528875222 ) ) ;
#19295=CARTESIAN_POINT ( 'NONE',  ( 48.31521067748249720, -54.24088337835979701, -55.14618947275539540 ) ) ;
#19298=CARTESIAN_POINT ( 'NONE',  ( 7.853097003783780394, -60.52042854835909935, -20.86915960608759946 ) ) ;
#19300=VECTOR ( 'NONE', #3200, 1000.000000000000000 ) ;
#19304=VECTOR ( 'NONE', #19259, 1000.000000000000000 ) ;
#19305=CARTESIAN_POINT ( 'NONE',  ( 10.10517893431049963, -55.15925497894330931, -21.14999999999999858 ) ) ;
#19306=CARTESIAN_POINT ( 'NONE',  ( 61.28610861176739633, 13.99802266614350010, -28.15000000000000213 ) ) ;
#19308=CARTESIAN_POINT ( 'NONE',  ( 61.75019796695546148, 13.88381105532070059, -26.84765975578291020 ) ) ;
#19313=CARTESIAN_POINT ( 'NONE',  ( 56.62432785584509531, 19.48323104975959907, -53.83726655423080132 ) ) ;
#19314=B_SPLINE_SURFACE_WITH_KNOTS ( 'NONE', 3, 3, ( 
 ( #508, #44803, #32982, #9162, #41128, #32199, #12318, #4705, #1298, #16498, #20673, #28802, #32449, #16760 ),
 ( #24077, #12071, #28025, #5240, #36403, #12577, #40097, #28542, #44540, #4189, #20167, #48219, #8641, #24592 ),
 ( #4969, #40605, #12844, #36661, #20936, #32714, #48740, #36936, #1037, #33762, #38489, #2325, #41637, #45325 ),
 ( #14381, #5745, #50293, #10196, #2590, #13360, #33509, #6264, #49265, #49522, #2072, #45840, #29574, #18050 ),
 ( #13614, #1551, #9929, #45580, #21453, #34270, #9675, #18565, #26410, #29318, #25633, #9429, #25379, #41380 ),
 ( #29823, #50026, #34016, #18299, #21702, #10457, #22224, #30346, #37452, #25891, #37710, #38232, #14119, #1809 ),
 ( #26155, #21963, #30085, #46369, #42431, #5497, #13867, #46110, #42165, #41904, #17788, #6520, #22482, #6004 ),
 ( #17539, #49773, #37972, #35587, #27451, #3882, #31627, #43454, #43708, #47646, #42689, #23247, #34800, #39777 ),
 ( #46887, #51322, #31371, #15418, #34542, #3111, #51574, #15157, #10974, #15673, #6786, #31118, #11495, #46626 ),
 ( #26941, #7043, #7556, #39525, #19596, #11752, #27709, #7812, #50545, #23763, #40034, #40545, #12780, #28737 ) ),
 .UNSPECIFIED., .F., .F., .F.,
 ( 4, 1, 1, 1, 1, 1, 1, 4 ),
 ( 4, 2, 2, 2, 2, 2, 4 ),
 ( -0.0003127823370728670155, 0.1428571428571430157, 0.2857142857142860315, 0.4285714285714289917, 0.5714285714285709528, 0.7142857142857139685, 0.8571428571428569843, 1.000000000000000000 ),
 ( -0.0003008787986270000095, 0.2008536346930439864, 0.4304006457708079991, 0.5738675276944109616, 0.6456009686562129701, 0.7603744741950950736, 0.7973406569620060669 ),
 .UNSPECIFIED. ) ;
#19316=CARTESIAN_POINT ( 'NONE',  ( 84.42051485081360340, -43.53095137563540362, -47.44928677006510043 ) ) ;
#19318=ORIENTED_EDGE ( 'NONE', *, *, #36916, .F. ) ;
#19321=CARTESIAN_POINT ( 'NONE',  ( 76.47354785737799432, -26.64541773940327118, -13.11343201606089259 ) ) ;
#19322=CARTESIAN_POINT ( 'NONE',  ( 9.788883518080631063, -64.09936060989920747, -46.59784358706489371 ) ) ;
#19324=VERTEX_POINT ( 'NONE', #20763 ) ;
#19326=CARTESIAN_POINT ( 'NONE',  ( 56.90065466210369749, -45.21025265706699514, -25.29837482150149697 ) ) ;
#19327=CARTESIAN_POINT ( 'NONE',  ( 56.40159924779830192, -50.63276481660309969, -53.06856169275020818 ) ) ;
#19328=ADVANCED_FACE ( 'NONE', ( #36751 ), #1123, .T. ) ;
#19330=CARTESIAN_POINT ( 'NONE',  ( 59.16206914407690221, -2.876195328580839927, -15.65935069007090163 ) ) ;
#19331=CARTESIAN_POINT ( 'NONE',  ( 51.37477222274990396, -49.09661486018149645, -76.61256277772369572 ) ) ;
#19334=CARTESIAN_POINT ( 'NONE',  ( 12.06284766121009966, -63.44323389162830296, -22.25048313876769868 ) ) ;
#19337=CARTESIAN_POINT ( 'NONE',  ( 56.65979965533069418, -47.79656003688090493, -48.39907199131990012 ) ) ;
#19339=CARTESIAN_POINT ( 'NONE',  ( 12.16981616251259801, -50.04926267044390187, -21.14999999999999858 ) ) ;
#19341=CARTESIAN_POINT ( 'NONE',  ( 55.78258317375759390, 14.07033184101250178, -15.69927152601569631 ) ) ;
#19342=CARTESIAN_POINT ( 'NONE',  ( 61.18526399883489830, -45.48745254298339802, -47.51713262586719821 ) ) ;
#19343=CARTESIAN_POINT ( 'NONE',  ( 56.85837508264230422, -50.62728578079150310, -53.45324575303870063 ) ) ;
#19349=CARTESIAN_POINT ( 'NONE',  ( 13.44774942451820010, -51.74366499200459657, -74.55381114264599773 ) ) ;
#19352=CARTESIAN_POINT ( 'NONE',  ( 42.03135417276770625, -45.79966294656320258, -6.846959983868809552 ) ) ;
#19354=CARTESIAN_POINT ( 'NONE',  ( 72.74715221972319057, 13.88381105532070059, -14.68167674020449986 ) ) ;
#19356=CARTESIAN_POINT ( 'NONE',  ( 82.50626185013108227, 14.19657067018509977, -47.45622494215220399 ) ) ;
#19360=CARTESIAN_POINT ( 'NONE',  ( 14.66318557257089950, -52.01452886429046885, -75.82251645564090836 ) ) ;
#19364=CARTESIAN_POINT ( 'NONE',  ( 52.91963055335400412, -49.63709126784409875, -48.95754079928280333 ) ) ;
#19368=CARTESIAN_POINT ( 'NONE',  ( 13.93400774615080095, 19.94011110403380371, -22.49576377567830221 ) ) ;
#19369=CARTESIAN_POINT ( 'NONE',  ( 16.13393739769620083, -15.61618894467929941, -6.649999999999999467 ) ) ;
#19371=CARTESIAN_POINT ( 'NONE',  ( 52.97667581671070280, 18.39974466412820320, -49.06651679849090186 ) ) ;
#19372=CARTESIAN_POINT ( 'NONE',  ( 55.91594421088640132, -45.90466751205540419, -17.93019951326149908 ) ) ;
#19373=DIRECTION ( 'NONE',  ( 0.000000000000000000, -1.000000000000000000, 0.000000000000000000 ) ) ;
#19374=ORIENTED_EDGE ( 'NONE', *, *, #29278, .T. ) ;
#19377=VERTEX_POINT ( 'NONE', #38066 ) ;
#19378=CARTESIAN_POINT ( 'NONE',  ( 11.91784411962730061, -65.43085189686328818, -17.65793976188430037 ) ) ;
#19379=CARTESIAN_POINT ( 'NONE',  ( 13.00893739769619906, 34.28605925116850273, -47.75434321273180416 ) ) ;
#19383=FACE_OUTER_BOUND ( 'NONE', #51548, .T. ) ;
#19388=DIRECTION ( 'NONE',  ( 0.000000000000000000, -1.000000000000000000, 0.000000000000000000 ) ) ;
#19389=CARTESIAN_POINT ( 'NONE',  ( 10.77117107879669966, -63.22212903752630098, -45.20474350506940198 ) ) ;
#19391=CARTESIAN_POINT ( 'NONE',  ( 68.13393739769814772, 19.38381105532029736, -71.50000000000200373 ) ) ;
#19393=CARTESIAN_POINT ( 'NONE',  ( 48.42521416700790127, 25.14253336855949783, -74.14999999999999147 ) ) ;
#19396=VERTEX_POINT ( 'NONE', #13960 ) ;
#19397=EDGE_CURVE ( 'NONE', #40665, #40081, #46754, .T. ) ;
#19399=CARTESIAN_POINT ( 'NONE',  ( 53.35835817625017796, 20.15050933124701160, -75.63636005538151608 ) ) ;
#19400=CARTESIAN_POINT ( 'NONE',  ( 83.63329919740728258, -44.53040215208500996, -46.55718455497714103 ) ) ;
#19401=DIRECTION ( 'NONE',  ( 0.000000000000000000, -1.000000000000000000, 0.000000000000000000 ) ) ;
#19402=ADVANCED_FACE ( 'NONE', ( #19171 ), #10550, .T. ) ;
#19404=CARTESIAN_POINT ( 'NONE',  ( 52.77888429003910176, -49.71941859661360041, -48.89378112591379733 ) ) ;
#19407=ORIENTED_EDGE ( 'NONE', *, *, #3623, .T. ) ;
#19412=CARTESIAN_POINT ( 'NONE',  ( 50.12047694534380327, -49.40224992130579551, -76.14999999999999147 ) ) ;
#19414=CARTESIAN_POINT ( 'NONE',  ( 47.36716192977550577, 23.43728642252559879, -74.36069403054010252 ) ) ;
#19415=DIRECTION ( 'NONE',  ( 6.008901426488883237E-29, 1.000000000000000000, -1.065814103640210074E-14 ) ) ;
#19420=CARTESIAN_POINT ( 'NONE',  ( 12.13696592145019792, 33.93507367045299361, -16.64705455762469910 ) ) ;
#19422=CARTESIAN_POINT ( 'NONE',  ( 52.56521993351449851, -49.86179673305689874, -28.06704019101890069 ) ) ;
#19423=CARTESIAN_POINT ( 'NONE',  ( 54.95770575214509535, -50.62412422504770149, -76.43951288111850317 ) ) ;
#19424=CARTESIAN_POINT ( 'NONE',  ( -9.182228926101151600, 12.40783594017670133, -5.100143237003939234 ) ) ;
#19429=CARTESIAN_POINT ( 'NONE',  ( 53.11047205726560350, -49.51384561212010027, -48.81638560371479940 ) ) ;
#19430=CARTESIAN_POINT ( 'NONE',  ( 47.69543556716480026, 23.26888818243800117, -54.96140342535039736 ) ) ;
#19432=CARTESIAN_POINT ( 'NONE',  ( 61.28592748474870433, -45.23049522091189800, -28.15095074383799911 ) ) ;
#19433=CARTESIAN_POINT ( 'NONE',  ( 68.88393739769620083, -38.11618894467930119, -73.25000000000000000 ) ) ;
#19434=CARTESIAN_POINT ( 'NONE',  ( 61.52542916938325135, -45.35171639540813970, -47.31474053514811828 ) ) ;
#19436=CARTESIAN_POINT ( 'NONE',  ( 51.43375900340840445, 18.02660632394349705, -76.62099598077431040 ) ) ;
#19437=CARTESIAN_POINT ( 'NONE',  ( 53.06801998396470310, 18.30370955338970163, -48.81041485190910123 ) ) ;
#19439=CARTESIAN_POINT ( 'NONE',  ( 52.82975622904280755, -49.66092049964720445, -48.47378032971909789 ) ) ;
#19444=CARTESIAN_POINT ( 'NONE',  ( 63.70037062081990342, -31.89081416583059436, -17.35709357403409925 ) ) ;
#19446=CARTESIAN_POINT ( 'NONE',  ( 11.13393739769619906, 32.27621211514449584, -43.92731420739779225 ) ) ;
#19448=CARTESIAN_POINT ( 'NONE',  ( 16.13393752749879795, -15.61618872006030045, -20.64999988453819668 ) ) ;
#19452=CYLINDRICAL_SURFACE ( 'NONE', #7006, 3.000000000000000000 ) ;
#19454=ORIENTED_EDGE ( 'NONE', *, *, #15882, .F. ) ;
#19455=CARTESIAN_POINT ( 'NONE',  ( 56.34641762111630214, -45.71298718759459945, -25.89277606233699913 ) ) ;
#19457=EDGE_CURVE ( 'NONE', #3287, #25228, #51333, .T. ) ;
#19458=ORIENTED_EDGE ( 'NONE', *, *, #8212, .T. ) ;
#19461=FACE_OUTER_BOUND ( 'NONE', #45063, .T. ) ;
#19463=ORIENTED_EDGE ( 'NONE', *, *, #23237, .F. ) ;
#19469=CARTESIAN_POINT ( 'NONE',  ( 61.73979651615039899, -29.77994616252469839, -16.06604299805859881 ) ) ;
#19471=CARTESIAN_POINT ( 'NONE',  ( 46.84762105052649872, -53.84887631677259634, -75.86145147363799879 ) ) ;
#19474=CARTESIAN_POINT ( 'NONE',  ( 44.57981642832929481, 14.36173779840500053, -8.202871819132159459 ) ) ;
#19476=CARTESIAN_POINT ( 'NONE',  ( 84.44784216359251161, -43.11618894467930119, -47.47585302082339354 ) ) ;
#19480=CARTESIAN_POINT ( 'NONE',  ( 55.48396116477669437, -47.17766655192640002, -26.43082136174480112 ) ) ;
#19481=CARTESIAN_POINT ( 'NONE',  ( 10.61757787825930066, -64.82569375050010763, -18.17423461342389857 ) ) ;
#19482=CARTESIAN_POINT ( 'NONE',  ( 75.06396332937768534, -21.88785010825060340, -11.38986195257589884 ) ) ;
#19483=CARTESIAN_POINT ( 'NONE',  ( 75.41871150549854974, 12.82758396796481470, -13.61662653247154431 ) ) ;
#19488=DIRECTION ( 'NONE',  ( 0.000000000000000000, 0.000000000000000000, -1.000000000000000000 ) ) ;
#19492=CARTESIAN_POINT ( 'NONE',  ( 57.27138006146679317, -50.61618894467930119, -53.91678089496280535 ) ) ;
#19493=CARTESIAN_POINT ( 'NONE',  ( 41.15934842087519741, 13.27345145488459899, -4.800414586038529663 ) ) ;
#19495=CARTESIAN_POINT ( 'NONE',  ( 20.13393739768839552, 24.18330853958629945, -20.65000000000000213 ) ) ;
#19496=DIRECTION ( 'NONE',  ( 0.4872913772396113563, 0.8732394366197181457, 0.000000000000000000 ) ) ;
#19497=CARTESIAN_POINT ( 'NONE',  ( 65.43042069957887463, -49.21324915460321137, -75.95351669811965678 ) ) ;
#19498=ADVANCED_FACE ( 'NONE', ( #3969 ), #29712, .T. ) ;
#19500=CARTESIAN_POINT ( 'NONE',  ( 18.01765265267910010, -51.72416169445279621, -75.53980707817230211 ) ) ;
#19501=CARTESIAN_POINT ( 'NONE',  ( 49.87147262927059899, -45.11618894467940066, -8.489676102032369442 ) ) ;
#19502=EDGE_CURVE ( 'NONE', #34738, #19, #24621, .T. ) ;
#19513=CARTESIAN_POINT ( 'NONE',  ( 17.45899407771650047, 21.59920855125570327, -76.12873484255680978 ) ) ;
#19514=EDGE_LOOP ( 'NONE', ( #41932, #39240, #43954, #48743, #41631, #50269, #16994, #2245 ) ) ;
#19517=CARTESIAN_POINT ( 'NONE',  ( 56.66909264166819327, -45.11618894467940066, -15.43624580850259953 ) ) ;
#19519=DIRECTION ( 'NONE',  ( 1.000000000000000000, 0.000000000000000000, 0.000000000000000000 ) ) ;
#19521=EDGE_CURVE ( 'NONE', #5028, #17403, #21215, .T. ) ;
#19524=CARTESIAN_POINT ( 'NONE',  ( 82.34864690492790373, 14.40950277491920772, -47.72348187592567115 ) ) ;
#19527=VECTOR ( 'NONE', #33924, 1000.000000000000000 ) ;
#19531=CARTESIAN_POINT ( 'NONE',  ( 52.03944403422909915, -51.37790098174010467, -75.97489327030881157 ) ) ;
#19532=CARTESIAN_POINT ( 'NONE',  ( 60.40062465321539520, 14.52871210431360005, -47.56306476889139390 ) ) ;
#19535=CARTESIAN_POINT ( 'NONE',  ( -6.423395424222389849, 15.09401038596259959, -5.304779371069330729 ) ) ;
#19540=CARTESIAN_POINT ( 'NONE',  ( 56.53717807884549984, 16.48612042830059821, -47.91220710008310135 ) ) ;
#19542=CARTESIAN_POINT ( 'NONE',  ( 44.00679900668159661, 14.83686777303820037, -8.295979038165928188 ) ) ;
#19545=FACE_OUTER_BOUND ( 'NONE', #43748, .T. ) ;
#19549=CARTESIAN_POINT ( 'NONE',  ( 48.58883753202030675, -54.12974218542010618, -55.21967372154079357 ) ) ;
#19554=CARTESIAN_POINT ( 'NONE',  ( 47.87778036368489865, 23.16084776458309946, -54.84373880101900056 ) ) ;
#19555=EDGE_CURVE ( 'NONE', #29700, #4830, #41059, .T. ) ;
#19559=CARTESIAN_POINT ( 'NONE',  ( 7.517033938252880354, 30.35161808146150264, -19.14999999999999858 ) ) ;
#19563=CARTESIAN_POINT ( 'NONE',  ( 60.64942649656659768, -45.57996615352359981, -47.30139731918439594 ) ) ;
#19564=CARTESIAN_POINT ( 'NONE',  ( 60.23130391296999875, -45.78304229081430066, -47.24246919202539630 ) ) ;
#19566=CARTESIAN_POINT ( 'NONE',  ( 83.87142430054399256, 13.62662911754079964, -47.47134017317799959 ) ) ;
#19567=DIRECTION ( 'NONE',  ( 0.000000000000000000, 0.000000000000000000, -1.000000000000000000 ) ) ;
#19568=CARTESIAN_POINT ( 'NONE',  ( 58.16408830537058350, 14.45890994950174147, -26.37137507050323038 ) ) ;
#19569=CARTESIAN_POINT ( 'NONE',  ( 56.82514454922279867, 19.42926546485919914, -53.84957932253210089 ) ) ;
#19572=ORIENTED_EDGE ( 'NONE', *, *, #4669, .F. ) ;
#19573=VERTEX_POINT ( 'NONE', #22510 ) ;
#19576=CARTESIAN_POINT ( 'NONE',  ( 76.42344249101890341, -22.54073511903138183, -12.89752473310971403 ) ) ;
#19577=CARTESIAN_POINT ( 'NONE',  ( 12.89366548528570000, -65.51121853336410084, -47.72019435537529830 ) ) ;
#19578=EDGE_LOOP ( 'NONE', ( #25297, #45843, #8118, #7760 ) ) ;
#19580=EDGE_CURVE ( 'NONE', #2407, #43345, #2878, .T. ) ;
#19582=CARTESIAN_POINT ( 'NONE',  ( 56.33033006273769416, -50.66288601196639974, -53.07632196026260374 ) ) ;
#19583=AXIS2_PLACEMENT_3D ( 'NONE', #36650, #9154, #29309 ) ;
#19586=CARTESIAN_POINT ( 'NONE',  ( 61.33519241402679967, -0.8007228105548149788, -16.23036785962110073 ) ) ;
#19587=CARTESIAN_POINT ( 'NONE',  ( 51.78350021394049918, -49.14267277433249603, -77.04630018407770820 ) ) ;
#19589=VERTEX_POINT ( 'NONE', #18325 ) ;
#19595=CARTESIAN_POINT ( 'NONE',  ( 12.53567562190739970, -49.97757163118789947, -21.12174283171160027 ) ) ;
#19596=CARTESIAN_POINT ( 'NONE',  ( 56.64426558924419908, 19.38381105532069881, -75.54079041445969267 ) ) ;
#19597=AXIS2_PLACEMENT_3D ( 'NONE', #45145, #25460, #17875 ) ;
#19601=AXIS2_PLACEMENT_3D ( 'NONE', #4146, #12277, #29277 ) ;
#19604=DIRECTION ( 'NONE',  ( -1.000000000000000000, 0.000000000000000000, 0.000000000000000000 ) ) ;
#19606=CARTESIAN_POINT ( 'NONE',  ( 13.94115515399420069, -51.19324711185789312, -74.36773579016251290 ) ) ;
#19608=CARTESIAN_POINT ( 'NONE',  ( 42.16682223010890596, -45.82892464120780573, -6.952852404606489678 ) ) ;
#19612=CARTESIAN_POINT ( 'NONE',  ( 11.89339496836129939, 34.20366452798109691, -18.15362147985830177 ) ) ;
#19615=CARTESIAN_POINT ( 'NONE',  ( 52.38380668138933771, 18.65349054039470644, -77.22917124323686267 ) ) ;
#19620=CARTESIAN_POINT ( 'NONE',  ( 49.42204313923240022, 22.28165337735409679, -54.19389682688740351 ) ) ;
#19622=CARTESIAN_POINT ( 'NONE',  ( 53.31858331305709697, -49.44472013427339618, -49.05455764246600125 ) ) ;
#19625=DIRECTION ( 'NONE',  ( 0.000000000000000000, 0.000000000000000000, -1.000000000000000000 ) ) ;
#19627=CARTESIAN_POINT ( 'NONE',  ( 51.78349586844800001, -49.14267421975780081, -77.04629326711500426 ) ) ;
#19629=CIRCLE ( 'NONE', #48942, 2.999999999999997780 ) ;
#19630=CARTESIAN_POINT ( 'NONE',  ( 53.41952757764659765, 18.23162460577420063, -49.21226385651820578 ) ) ;
#19631=CARTESIAN_POINT ( 'NONE',  ( 54.99585155449699414, -45.33621571906800085, -15.06529551545699874 ) ) ;
#19633=ORIENTED_EDGE ( 'NONE', *, *, #8583, .T. ) ;
#19637=CARTESIAN_POINT ( 'NONE',  ( 11.93810467663310071, -65.43945453151620484, -17.87564855520800222 ) ) ;
#19638=CARTESIAN_POINT ( 'NONE',  ( 10.38317543238860097, 32.50360296011269412, -45.89016348143990598 ) ) ;
#19640=CARTESIAN_POINT ( 'NONE',  ( 48.42505861925889832, -54.27772236143609774, -55.06615293675599787 ) ) ;
#19641=CARTESIAN_POINT ( 'NONE',  ( 11.61157517248314441, -65.37040442588083522, -22.53770969513777800 ) ) ;
#19643=VERTEX_POINT ( 'NONE', #45027 ) ;
#19645=CARTESIAN_POINT ( 'NONE',  ( 11.13393739769619906, -63.26135015252509675, -43.91418615158710281 ) ) ;
#19647=VERTEX_POINT ( 'NONE', #24822 ) ;
#19650=CARTESIAN_POINT ( 'NONE',  ( 56.87927060707500004, 19.41808733271159682, -53.72034555577639736 ) ) ;
#19652=EDGE_LOOP ( 'NONE', ( #11098, #8036, #14871, #43507 ) ) ;
#19654=DIRECTION ( 'NONE',  ( 0.000000000000000000, 0.000000000000000000, 1.000000000000000000 ) ) ;
#19665=DIRECTION ( 'NONE',  ( 0.5685928097855377228, -0.5944782866685527356, -0.5685928097855347252 ) ) ;
#19667=CARTESIAN_POINT ( 'NONE',  ( 46.37109089150850139, 21.71592500402280024, -76.14999999999999147 ) ) ;
#19668=CARTESIAN_POINT ( 'NONE',  ( 61.58747524351382197, 14.05432104330237308, -47.18566752083825833 ) ) ;
#19669=CARTESIAN_POINT ( 'NONE',  ( 68.13393739769649926, -48.11618894468163887, -75.95000000000023022 ) ) ;
#19670=CARTESIAN_POINT ( 'NONE',  ( 12.12214211478229942, 33.82440024855289806, -16.43788246314790058 ) ) ;
#19672=CARTESIAN_POINT ( 'NONE',  ( 53.87584899166630237, -48.41195041224410289, -26.23515327084989934 ) ) ;
#19673=CARTESIAN_POINT ( 'NONE',  ( 55.96492549803009808, -50.64339188080709420, -75.67011080619238328 ) ) ;
#19674=CARTESIAN_POINT ( 'NONE',  ( -11.30855951853859942, 10.63123909960889968, -5.947173849478319951 ) ) ;
#19676=EDGE_CURVE ( 'NONE', #45486, #20296, #3604, .T. ) ;
#19678=CARTESIAN_POINT ( 'NONE',  ( 61.19582091169579741, 14.04751127219729945, -46.80238762625980087 ) ) ;
#19680=CYLINDRICAL_SURFACE ( 'NONE', #43187, 1.999999999999997780 ) ;
#19684=CARTESIAN_POINT ( 'NONE',  ( 52.90228699065409756, -49.62291960146570347, -48.72753553419400419 ) ) ;
#19685=ADVANCED_FACE ( 'NONE', ( #5205 ), #4930, .T. ) ;
#19686=CARTESIAN_POINT ( 'NONE',  ( 47.70131400676309852, 23.24817081282549935, -54.82001053506050425 ) ) ;
#19687=CARTESIAN_POINT ( 'NONE',  ( 57.59318069304929821, -45.71254049200430103, -26.27850964665099909 ) ) ;
#19689=CARTESIAN_POINT ( 'NONE',  ( 61.43319361452919480, 14.21598701041570045, -47.47819310727240349 ) ) ;
#19691=ADVANCED_FACE ( 'NONE', ( #40831, #41094 ), #25344, .T. ) ;
#19692=CARTESIAN_POINT ( 'NONE',  ( 51.97623849038839694, 18.77915525888139925, -76.70088623176620501 ) ) ;
#19693=CARTESIAN_POINT ( 'NONE',  ( 52.91697747311700084, 18.38500394665459936, -48.80601309169850310 ) ) ;
#19696=AXIS2_PLACEMENT_3D ( 'NONE', #17042, #44815, #28814 ) ;
#19697=VERTEX_POINT ( 'NONE', #28764 ) ;
#19699=CARTESIAN_POINT ( 'NONE',  ( 47.64889676501250193, -54.52888567683150001, -55.03601200310530572 ) ) ;
#19702=CARTESIAN_POINT ( 'NONE',  ( 61.34707231617679923, -30.42972915830750225, -16.23350102184249621 ) ) ;
#19707=CARTESIAN_POINT ( 'NONE',  ( 51.49832567296675734, -34.30705569774075059, -76.79133718297113376 ) ) ;
#19712=CARTESIAN_POINT ( 'NONE',  ( 49.97510569688304116, -29.81569084455778906, -15.94715247223231458 ) ) ;
#19720=CARTESIAN_POINT ( 'NONE',  ( 12.91816786240429948, 34.28039554897920027, -23.43576497212680110 ) ) ;
#19724=CARTESIAN_POINT ( 'NONE',  ( 64.62455173613830084, -30.85405543856260024, -16.65869106914230358 ) ) ;
#19727=CARTESIAN_POINT ( 'NONE',  ( 55.57908331551900005, 14.75265853258540183, -16.80478259867470214 ) ) ;
#19730=CARTESIAN_POINT ( 'NONE',  ( 44.12345869187539904, 14.36007666331510002, -7.915795181119260171 ) ) ;
#19732=CARTESIAN_POINT ( 'NONE',  ( 14.98451991090269964, 21.70396400196510100, -76.14999999999999147 ) ) ;
#19733=CARTESIAN_POINT ( 'NONE',  ( 84.23484834998549786, -43.81302277605040274, -47.06355581890329631 ) ) ;
#19736=VERTEX_POINT ( 'NONE', #21415 ) ;
#19738=CARTESIAN_POINT ( 'NONE',  ( 11.30323766776139927, -63.48480417437669843, -14.81980353719009891 ) ) ;
#19739=CARTESIAN_POINT ( 'NONE',  ( 50.69188217665702467, -35.76023418930356002, -76.26103740547989673 ) ) ;
#19740=CARTESIAN_POINT ( 'NONE',  ( 61.73642047736571925, -45.13062725877497172, -46.64902933540918184 ) ) ;
#19741=CARTESIAN_POINT ( 'NONE',  ( 13.61751436261749859, -50.16766668102790305, -20.94898426700639860 ) ) ;
#19743=CARTESIAN_POINT ( 'NONE',  ( -4.095824978346090717, -48.17436604277430234, -5.432754358006550710 ) ) ;
#19748=CARTESIAN_POINT ( 'NONE',  ( 57.55751162060460047, -50.29421797927160043, -52.83558909277360272 ) ) ;
#19749=CARTESIAN_POINT ( 'NONE',  ( 43.13712996753829998, 11.78398668836219976, -4.491635650878129660 ) ) ;
#19750=ADVANCED_FACE ( 'NONE', ( #40570 ), #49230, .T. ) ;
#19752=CARTESIAN_POINT ( 'NONE',  ( 74.93037156228848517, -45.11618894467250129, -15.31097063366330069 ) ) ;
#19753=CARTESIAN_POINT ( 'NONE',  ( 59.83314911148339377, -45.99164674684980270, -47.38390679353289414 ) ) ;
#19757=CARTESIAN_POINT ( 'NONE',  ( 17.21347160910390173, -53.11618894467930119, -76.14999999999999147 ) ) ;
#19761=PLANE ( 'NONE',  #33304 ) ;
#19762=VERTEX_POINT ( 'NONE', #29285 ) ;
#19763=CARTESIAN_POINT ( 'NONE',  ( 45.90333292994009184, 13.88381105525539994, -7.776728755756193046 ) ) ;
#19768=EDGE_CURVE ( 'NONE', #44451, #25228, #1517, .T. ) ;
#19770=ORIENTED_EDGE ( 'NONE', *, *, #30369, .F. ) ;
#19771=CARTESIAN_POINT ( 'NONE',  ( 17.27854763127069759, 21.70054973260339892, -76.14999999999999147 ) ) ;
#19775=EDGE_CURVE ( 'NONE', #41037, #5215, #4825, .T. ) ;
#19779=ORIENTED_EDGE ( 'NONE', *, *, #39396, .T. ) ;
#19780=DIRECTION ( 'NONE',  ( 0.000000000000000000, 0.000000000000000000, 1.000000000000000000 ) ) ;
#19784=CARTESIAN_POINT ( 'NONE',  ( 68.13393739769620083, 18.13381105532069881, -67.99999999999998579 ) ) ;
#19786=CARTESIAN_POINT ( 'NONE',  ( 61.34213663493859769, 14.32983721081379969, -47.63657398781069929 ) ) ;
#19787=AXIS2_PLACEMENT_3D ( 'NONE', #23518, #30873, #38774 ) ;
#19792=CARTESIAN_POINT ( 'NONE',  ( 42.78018059632909598, -42.70905810753730236, -3.187564294433590462 ) ) ;
#19793=CARTESIAN_POINT ( 'NONE',  ( -8.872901943480378861, 13.06271670022229969, -5.763478819725060376 ) ) ;
#19798=ORIENTED_EDGE ( 'NONE', *, *, #51230, .T. ) ;
#19799=CIRCLE ( 'NONE', #49930, 36.00000000000000000 ) ;
#19800=CARTESIAN_POINT ( 'NONE',  ( 41.04960996913820281, 14.26468518160199928, -6.018009378594939562 ) ) ;
#19801=CARTESIAN_POINT ( 'NONE',  ( 12.91917450912220033, 34.27891870250100226, -47.58062843003349940 ) ) ;
#19809=CARTESIAN_POINT ( 'NONE',  ( 48.52733106884640080, -54.04267712022559778, -54.66955039445610254 ) ) ;
#19810=CARTESIAN_POINT ( 'NONE',  ( 51.94631124322077653, -32.86688835305900369, -19.08860917923622935 ) ) ;
#19817=ORIENTED_EDGE ( 'NONE', *, *, #46241, .F. ) ;
#19819=CARTESIAN_POINT ( 'NONE',  ( 60.55103620144870291, -45.67013093256520051, -47.48780874919079764 ) ) ;
#19822=CARTESIAN_POINT ( 'NONE',  ( -4.162817235437208829, -15.61618894467929763, 7.530187386896120216 ) ) ;
#19825=CARTESIAN_POINT ( 'NONE',  ( 61.28610861176739633, 13.99802266614350010, -46.37203261889099792 ) ) ;
#19829=ORIENTED_EDGE ( 'NONE', *, *, #29048, .T. ) ;
#19836=CARTESIAN_POINT ( 'NONE',  ( 56.85665997422760398, -45.22495964200660268, -25.29717091828119990 ) ) ;
#19837=CARTESIAN_POINT ( 'NONE',  ( 56.47574211739829764, -50.76931576605299767, -53.73401891104529682 ) ) ;
#19838=CARTESIAN_POINT ( 'NONE',  ( 47.40322300430479885, 23.42336669154508755, -74.14999999999999147 ) ) ;
#19839=CARTESIAN_POINT ( 'NONE',  ( 59.27809708943870248, -2.630911221516660348, -15.68030308388919991 ) ) ;
#19840=CARTESIAN_POINT ( 'NONE',  ( 51.55656801642479792, -49.50504146151539686, -76.63870299401109776 ) ) ;
#19842=VERTEX_POINT ( 'NONE', #33725 ) ;
#19845=CARTESIAN_POINT ( 'NONE',  ( 68.13393739769620083, -48.11618894467930119, -73.25000000000000000 ) ) ;
#19851=CARTESIAN_POINT ( 'NONE',  ( 11.12718406851114317, -65.21267171038789456, -18.17421237898564357 ) ) ;
#19852=CARTESIAN_POINT ( 'NONE',  ( 29.34926776287277761, -6.014689412737906693, 5.856814007409659517 ) ) ;
#19856=ORIENTED_EDGE ( 'NONE', *, *, #31369, .T. ) ;
#19857=CARTESIAN_POINT ( 'NONE',  ( 47.29285256804710258, 22.85955254686820126, -75.52284329973508648 ) ) ;
#19858=CARTESIAN_POINT ( 'NONE',  ( 47.40880866017789685, -54.64074575612490037, -54.64987641489110359 ) ) ;
#19859=CARTESIAN_POINT ( 'NONE',  ( 11.28331493930094354, 33.98248205778411801, -47.30875510483342339 ) ) ;
#19860=CARTESIAN_POINT ( 'NONE',  ( 56.31076453717512464, -46.45614141085656001, -26.30375982980395477 ) ) ;
#19862=CIRCLE ( 'NONE', #3988, 15.11955878774480233 ) ;
#19865=CARTESIAN_POINT ( 'NONE',  ( 10.75976506916620146, 33.73421398272039795, -18.06526995537059932 ) ) ;
#19867=SPHERICAL_SURFACE ( 'NONE', #50786, 2.000000000000000000 ) ;
#19868=CARTESIAN_POINT ( 'NONE',  ( 11.13393739269939964, 32.53943438258615828, -24.14230604835864114 ) ) ;
#19870=CARTESIAN_POINT ( 'NONE',  ( 49.39892223771079927, 22.40179904714300108, -54.43183785437209821 ) ) ;
#19871=ORIENTED_EDGE ( 'NONE', *, *, #36167, .F. ) ;
#19872=CARTESIAN_POINT ( 'NONE',  ( 52.91162675532969928, -49.64972226872590255, -48.98817416027189608 ) ) ;
#19873=ORIENTED_EDGE ( 'NONE', *, *, #50879, .F. ) ;
#19876=DIRECTION ( 'NONE',  ( -1.000000000000000000, 5.464378949326942347E-15, 0.000000000000000000 ) ) ;
#19877=CARTESIAN_POINT ( 'NONE',  ( 83.25003658253979211, 13.60998241570020184, -46.59700837026780107 ) ) ;
#19879=CARTESIAN_POINT ( 'NONE',  ( 52.77888422556929982, 18.48704073958080230, -48.89378105638989780 ) ) ;
#19880=CARTESIAN_POINT ( 'NONE',  ( 55.41258925948719849, -45.63128349684820506, -16.01983445647000082 ) ) ;
#19881=CARTESIAN_POINT ( 'NONE',  ( 53.87546017034450330, 17.18069085124139761, -26.23270880884989964 ) ) ;
#19884=VERTEX_POINT ( 'NONE', #38194 ) ;
#19885=CARTESIAN_POINT ( 'NONE',  ( 11.31612280585429886, -65.07844770564609860, -16.97569922736749959 ) ) ;
#19886=CARTESIAN_POINT ( 'NONE',  ( 10.66704074922019885, 32.15531322180049756, -45.39606957910810081 ) ) ;
#19889=CARTESIAN_POINT ( 'NONE',  ( 11.68864222515470708, -65.39868967919012732, -22.45823848831452096 ) ) ;
#19892=LINE ( 'NONE', #28526, #30147 ) ;
#19893=CARTESIAN_POINT ( 'NONE',  ( 11.10549195505100073, -63.26330928660971153, -44.25128882018109522 ) ) ;
#19894=CARTESIAN_POINT ( 'NONE',  ( 65.43393739769578588, 16.88381105532129922, -71.50000000000000000 ) ) ;
#19898=CARTESIAN_POINT ( 'NONE',  ( 13.42427360708462913, -51.80630186999076869, -74.54430098197724419 ) ) ;
#19900=VERTEX_POINT ( 'NONE', #13828 ) ;
#19904=TOROIDAL_SURFACE ( 'NONE', #26595, 17.69999999999999929, 3.799999999999830180 ) ;
#19910=CARTESIAN_POINT ( 'NONE',  ( 57.36123081079020380, 18.90300135422739913, -52.61896059691729732 ) ) ;
#19912=ORIENTED_EDGE ( 'NONE', *, *, #680, .F. ) ;
#19915=CARTESIAN_POINT ( 'NONE',  ( -21.86606260230379917, -15.61618894467929408, -19.14999999999999858 ) ) ;
#19916=CARTESIAN_POINT ( 'NONE',  ( 47.11383090458340206, 23.12040445463469851, -75.35698732394219235 ) ) ;
#19919=CARTESIAN_POINT ( 'NONE',  ( 54.20961013379049831, 17.70559848872130360, -48.50941760523620161 ) ) ;
#19920=CARTESIAN_POINT ( 'NONE',  ( 12.21895752911930089, 33.73857836819860267, -16.28177273607870035 ) ) ;
#19923=CARTESIAN_POINT ( 'NONE',  ( 55.83720749917949888, -50.61618650412209774, -76.10769951055490878 ) ) ;
#19924=CARTESIAN_POINT ( 'NONE',  ( 57.55751162087899786, 19.38381105532069881, -53.92796738110899923 ) ) ;
#19928=CARTESIAN_POINT ( 'NONE',  ( 61.55709258699470610, 13.90898581735810069, -46.56616023981329988 ) ) ;
#19929=CARTESIAN_POINT ( 'NONE',  ( 67.20199456633832824, -1.235504130748810159, -17.36203811242808470 ) ) ;
#19930=VERTEX_POINT ( 'NONE', #30569 ) ;
#19931=CARTESIAN_POINT ( 'NONE',  ( 52.79307622657449883, -49.68079306134869455, -48.47378032971909789 ) ) ;
#19933=CARTESIAN_POINT ( 'NONE',  ( 60.90224615744529757, -45.28718561006350285, -27.40856525842869829 ) ) ;
#19935=CARTESIAN_POINT ( 'NONE',  ( 13.77456432040950141, 19.39060544165389999, -21.29084665975700119 ) ) ;
#19936=CARTESIAN_POINT ( 'NONE',  ( 60.75158961744540420, 14.30615305676900029, -47.32592388962400776 ) ) ;
#19938=CARTESIAN_POINT ( 'NONE',  ( 51.73941885623040093, 18.18506110802390197, -76.84325746863240170 ) ) ;
#19939=CARTESIAN_POINT ( 'NONE',  ( 52.80965344031350384, 18.44124166929070086, -48.67334067697609612 ) ) ;
#19940=LINE ( 'NONE', #23343, #16649 ) ;
#19941=CARTESIAN_POINT ( 'NONE',  ( 53.26660255314480708, -49.43204447085090436, -48.79175800379049832 ) ) ;
#19944=CARTESIAN_POINT ( 'NONE',  ( 47.53978851393139848, -54.55594495545970091, -54.68076641372660163 ) ) ;
#19946=CARTESIAN_POINT ( 'NONE',  ( 54.63655771189059607, 16.82059223505549994, -26.73578643762699869 ) ) ;
#19947=CARTESIAN_POINT ( 'NONE',  ( 61.42640818143939896, -30.97378847031719928, -16.54492983442209919 ) ) ;
#19949=CARTESIAN_POINT ( 'NONE',  ( 11.13393739769619906, 32.25300621514130484, -43.92547639555999694 ) ) ;
#19951=FACE_OUTER_BOUND ( 'NONE', #37460, .T. ) ;
#19952=VERTEX_POINT ( 'NONE', #26372 ) ;
#19955=CARTESIAN_POINT ( 'NONE',  ( 49.86419038289391636, -29.64908286110574309, -15.89077235228104534 ) ) ;
#19959=ORIENTED_EDGE ( 'NONE', *, *, #41104, .T. ) ;
#19962=CARTESIAN_POINT ( 'NONE',  ( 60.65419404070010501, 14.53878550406569836, -47.75595165931559904 ) ) ;
#19963=EDGE_CURVE ( 'NONE', #29321, #4867, #45805, .T. ) ;
#19967=CARTESIAN_POINT ( 'NONE',  ( 64.02385614546949455, -30.35404338245150058, -16.43221122146919910 ) ) ;
#19968=CARTESIAN_POINT ( 'NONE',  ( 12.45110396332199976, -65.31062155621590648, -23.95537965760280130 ) ) ;
#19971=CARTESIAN_POINT ( 'NONE',  ( 45.12954658315720025, 14.34843193608710088, -8.542182965482949086 ) ) ;
#19973=DIRECTION ( 'NONE',  ( -0.05023550054956103100, 0.000000000000000000, 0.9987374001630935361 ) ) ;
#19975=CARTESIAN_POINT ( 'NONE',  ( 83.67009235204480433, -44.53553140227840146, -46.70940576878270178 ) ) ;
#19976=EDGE_CURVE ( 'NONE', #566, #24834, #47349, .T. ) ;
#19980=CARTESIAN_POINT ( 'NONE',  ( 56.12605853786319443, -46.33585505558260564, -26.20103473702469898 ) ) ;
#19981=CARTESIAN_POINT ( 'NONE',  ( 14.89545651468249865, -50.81498301574369947, -21.03875510983650088 ) ) ;
#19983=CARTESIAN_POINT ( 'NONE',  ( 75.45574671126698263, 12.51734667287785996, -13.48816435240556011 ) ) ;
#19984=EDGE_CURVE ( 'NONE', #17403, #40337, #7825, .T. ) ;
#19985=CARTESIAN_POINT ( 'NONE',  ( 12.22498025668750010, -50.02555234895769587, -21.14999999999999858 ) ) ;
#19986=VERTEX_POINT ( 'NONE', #36059 ) ;
#19987=CARTESIAN_POINT ( 'NONE',  ( -7.439310335423879650, -45.55625616355589358, -5.547491402514559411 ) ) ;
#19991=CARTESIAN_POINT ( 'NONE',  ( 57.49763721924109916, -50.14068302088079321, -52.63210796847160822 ) ) ;
#19992=CARTESIAN_POINT ( 'NONE',  ( 42.69362902231169699, 12.38631381078020155, -4.694965688683719662 ) ) ;
#19995=CARTESIAN_POINT ( 'NONE',  ( 60.23130391296999875, -45.78304229081430066, -47.24246919202539630 ) ) ;
#19997=CARTESIAN_POINT ( 'NONE',  ( 68.39017795531430011, -0.8919439843293410775, -18.15414638955719795 ) ) ;
#19998=CARTESIAN_POINT ( 'NONE',  ( 17.74841177042720020, -52.60116553372549930, -76.03823174343609992 ) ) ;
#19999=B_SPLINE_CURVE_WITH_KNOTS ( 'NONE', 3,
 ( #50054, #14148, #30117, #46136 ),
 .UNSPECIFIED., .F., .F.,
 ( 4, 4 ),
 ( 0.9850318682126864012, 1.000000000000000000 ),
 .UNSPECIFIED. ) ;
#20003=FACE_OUTER_BOUND ( 'NONE', #21176, .T. ) ;
#20005=FACE_OUTER_BOUND ( 'NONE', #37338, .T. ) ;
#20010=ORIENTED_EDGE ( 'NONE', *, *, #26707, .T. ) ;
#20011=CARTESIAN_POINT ( 'NONE',  ( 17.21347160910339724, 21.88381105532300097, -76.14999999999999147 ) ) ;
#20020=VERTEX_POINT ( 'NONE', #7779 ) ;
#20022=EDGE_CURVE ( 'NONE', #17902, #23175, #5428, .T. ) ;
#20023=LINE ( 'NONE', #16896, #8425 ) ;
#20024=EDGE_LOOP ( 'NONE', ( #24297, #33736, #46436, #6812 ) ) ;
#20026=EDGE_CURVE ( 'NONE', #25535, #39953, #26006, .T. ) ;
#20028=CARTESIAN_POINT ( 'NONE',  ( 11.93174526809839975, -65.43929183185349530, -17.93019253464870033 ) ) ;
#20029=CARTESIAN_POINT ( 'NONE',  ( 60.32681533046309852, 14.53973477817790005, -47.49738862531440731 ) ) ;
#20033=CARTESIAN_POINT ( 'NONE',  ( -6.916656312004059615, 14.59513431219300017, -4.826769747919490428 ) ) ;
#20037=CARTESIAN_POINT ( 'NONE',  ( 46.89723159848931999, 22.92670389814115239, -75.65864031440739268 ) ) ;
#20038=EDGE_CURVE ( 'NONE', #26643, #13074, #26651, .T. ) ;
#20039=CARTESIAN_POINT ( 'NONE',  ( 55.38286017496716340, 14.79966023998268732, -16.52948577675217834 ) ) ;
#20042=ORIENTED_EDGE ( 'NONE', *, *, #22675, .T. ) ;
#20044=CARTESIAN_POINT ( 'NONE',  ( 42.30369714865540232, 14.62323136802010026, -7.058027111948209864 ) ) ;
#20045=AXIS2_PLACEMENT_3D ( 'NONE', #43370, #15327, #35229 ) ;
#20046=CARTESIAN_POINT ( 'NONE',  ( 11.13393739769499824, 32.42518242049779786, -43.78800780971030093 ) ) ;
#20051=CARTESIAN_POINT ( 'NONE',  ( 46.40057797168859821, -53.02061573618119894, -76.14999999999999147 ) ) ;
#20052=CARTESIAN_POINT ( 'NONE',  ( 13.50362949724940087, 18.90074600912790004, -20.96762847177769729 ) ) ;
#20053=CARTESIAN_POINT ( 'NONE',  ( 46.99011478535390296, 23.09104886575959981, -75.47331634174820181 ) ) ;
#20054=CARTESIAN_POINT ( 'NONE',  ( 48.44331161791639317, -54.05217057865549890, -54.60670978497749672 ) ) ;
#20055=CARTESIAN_POINT ( 'NONE',  ( 51.86283645288276034, -32.73404737421963517, -18.73275447517399073 ) ) ;
#20057=CARTESIAN_POINT ( 'NONE',  ( 12.73487912048826232, 24.23912916116268690, -75.56421958049274679 ) ) ;
#20058=CARTESIAN_POINT ( 'NONE',  ( 55.55365133010059964, 13.88381105532070059, -14.32025150907159983 ) ) ;
#20059=EDGE_LOOP ( 'NONE', ( #39134, #18559, #27487, #9352, #37248, #37127 ) ) ;
#20061=DIRECTION ( 'NONE',  ( 0.000000000000000000, -0.8263253571357117577, 0.5631930434180969502 ) ) ;
#20062=ORIENTED_EDGE ( 'NONE', *, *, #50756, .T. ) ;
#20064=CARTESIAN_POINT ( 'NONE',  ( 60.83106467324910227, -45.48877508199960573, -47.24035188271849250 ) ) ;
#20066=CARTESIAN_POINT ( 'NONE',  ( 7.517033938252880354, 30.35161808146150264, -19.14999999999999858 ) ) ;
#20069=EDGE_CURVE ( 'NONE', #35735, #15737, #3847, .T. ) ;
#20071=CARTESIAN_POINT ( 'NONE',  ( 12.13393739769600010, -55.41568642894409180, -23.15000000000000213 ) ) ;
#20072=ORIENTED_EDGE ( 'NONE', *, *, #41821, .T. ) ;
#20075=CIRCLE ( 'NONE', #38499, 2.000000000000000888 ) ;
#20076=ORIENTED_EDGE ( 'NONE', *, *, #25037, .F. ) ;
#20077=CARTESIAN_POINT ( 'NONE',  ( 84.19224659786166853, 13.29802461769379818, -48.96577344625911365 ) ) ;
#20081=CARTESIAN_POINT ( 'NONE',  ( 76.39919602841192159, -19.31896256756559893, -12.79308182705372054 ) ) ;
#20082=CARTESIAN_POINT ( 'NONE',  ( 51.58417065388699996, -52.63486567717929177, -53.74111633605280502 ) ) ;
#20084=ORIENTED_EDGE ( 'NONE', *, *, #25037, .T. ) ;
#20087=CARTESIAN_POINT ( 'NONE',  ( 49.21269661613270330, 22.37820248916990096, -54.26152208607290106 ) ) ;
#20089=CARTESIAN_POINT ( 'NONE',  ( 56.49779928568679566, -50.76024185320960669, -53.73084170065449428 ) ) ;
#20090=CARTESIAN_POINT ( 'NONE',  ( 8.786694880862668811, -63.12535539208791135, -46.67160944818530766 ) ) ;
#20091=CARTESIAN_POINT ( 'NONE',  ( 61.20693769746879553, -0.3648949609556400575, -16.46666462177489976 ) ) ;
#20092=CARTESIAN_POINT ( 'NONE',  ( 52.23706849658200468, -49.75889047595390480, -77.18592309284780129 ) ) ;
#20094=VERTEX_POINT ( 'NONE', #12745 ) ;
#20096=CARTESIAN_POINT ( 'NONE',  ( 52.94902644660979973, -50.40032911565540275, -76.96923111675658902 ) ) ;
#20098=CARTESIAN_POINT ( 'NONE',  ( 83.30738730474247689, -42.20963518668898473, -44.69194689374966600 ) ) ;
#20101=CARTESIAN_POINT ( 'NONE',  ( 12.76348253639140040, -50.31877257918069546, -21.19734575724999814 ) ) ;
#20102=CARTESIAN_POINT ( 'NONE',  ( 18.14749711188961001, -51.13605320025961731, -15.68318871053545749 ) ) ;
#20103=AXIS2_PLACEMENT_3D ( 'NONE', #50034, #22231, #29584 ) ;
#20104=CARTESIAN_POINT ( 'NONE',  ( 68.13393739769745139, -49.21324915460503036, -70.54648330188275906 ) ) ;
#20105=CARTESIAN_POINT ( 'NONE',  ( 60.85479269726300089, -45.48099585699259961, -47.26080742266869805 ) ) ;
#20109=ORIENTED_EDGE ( 'NONE', *, *, #8706, .F. ) ;
#20110=CARTESIAN_POINT ( 'NONE',  ( 13.94115953405779962, -51.19325459173029458, -74.14992922886710858 ) ) ;
#20111=CARTESIAN_POINT ( 'NONE',  ( 47.24145533690699494, -54.76228788933499203, -54.65423412537209913 ) ) ;
#20114=AXIS2_PLACEMENT_3D ( 'NONE', #28947, #7316, #43728 ) ;
#20115=CARTESIAN_POINT ( 'NONE',  ( 60.87740474328280982, -45.45106909386917948, -47.11566480119547862 ) ) ;
#20116=AXIS2_PLACEMENT_3D ( 'NONE', #29499, #10896, #50469 ) ;
#20123=CARTESIAN_POINT ( 'NONE',  ( 48.59172395386560339, 22.89772199268099939, -55.28129228068259948 ) ) ;
#20125=CARTESIAN_POINT ( 'NONE',  ( 52.62897960803029918, -49.80262906116220023, -48.60272236542579805 ) ) ;
#20126=ORIENTED_EDGE ( 'NONE', *, *, #46823, .T. ) ;
#20130=CARTESIAN_POINT ( 'NONE',  ( 83.53868183867639630, 13.38921618474499908, -46.56548196350910018 ) ) ;
#20131=CARTESIAN_POINT ( 'NONE',  ( 53.13430510201229851, 18.01985497199409991, -27.00377261849559929 ) ) ;
#20132=EDGE_CURVE ( 'NONE', #44083, #9344, #18701, .T. ) ;
#20134=CARTESIAN_POINT ( 'NONE',  ( 52.90670253716960048, 18.42639719312259672, -49.00842835936489905 ) ) ;
#20135=CARTESIAN_POINT ( 'NONE',  ( 56.56153180275769898, -45.18625296881599951, -16.30282656199999991 ) ) ;
#20142=CARTESIAN_POINT ( 'NONE',  ( 10.97564840259020080, -65.00352292546099875, -17.33480504156820245 ) ) ;
#20143=CARTESIAN_POINT ( 'NONE',  ( 11.37064335167489837, 33.60134013189160385, -46.20549124663499896 ) ) ;
#20145=CARTESIAN_POINT ( 'NONE',  ( 47.54352022508510345, -54.65002938982319591, -55.12334797975140077 ) ) ;
#20146=CARTESIAN_POINT ( 'NONE',  ( 11.52000135041339846, -65.33009319714545882, -22.63267478229686347 ) ) ;
#20147=CARTESIAN_POINT ( 'NONE',  ( 51.40027097486221663, 3.258603514984763638, -76.69281807238613169 ) ) ;
#20149=CARTESIAN_POINT ( 'NONE',  ( 49.40539548398250247, -53.49785366680099941, -54.15746054658189479 ) ) ;
#20150=DIRECTION ( 'NONE',  ( 0.3805321250008311118, 0.000000000000000000, -0.9247677015566405645 ) ) ;
#20151=CARTESIAN_POINT ( 'NONE',  ( 13.50201805292255308, 20.63639536108878048, -74.86151687916519393 ) ) ;
#20152=ORIENTED_EDGE ( 'NONE', *, *, #44610, .T. ) ;
#20161=CARTESIAN_POINT ( 'NONE',  ( 56.53399784783299964, -50.44739419118339896, -52.81205167950179913 ) ) ;
#20162=CARTESIAN_POINT ( 'NONE',  ( 56.91947791887660202, 18.74135835950649920, -52.25429733693979983 ) ) ;
#20163=AXIS2_PLACEMENT_3D ( 'NONE', #36930, #39837, #35898 ) ;
#20167=CARTESIAN_POINT ( 'NONE',  ( 54.14015757560070341, 19.94662053546359815, -75.52143025980080893 ) ) ;
#20169=ORIENTED_EDGE ( 'NONE', *, *, #16594, .T. ) ;
#20173=CARTESIAN_POINT ( 'NONE',  ( 47.06284717455670119, 23.15423693570959784, -75.35927708791611224 ) ) ;
#20176=CARTESIAN_POINT ( 'NONE',  ( 12.28895731154029924, 33.39433106751570079, -15.84602084848570058 ) ) ;
#20178=CARTESIAN_POINT ( 'NONE',  ( 55.31604533750469699, -50.61618591559609825, -76.42157388303350274 ) ) ;
#20180=CARTESIAN_POINT ( 'NONE',  ( 46.03121886948380137, -45.11618894467940066, -7.582877905987319700 ) ) ;
#20182=CARTESIAN_POINT ( 'NONE',  ( 61.35412202998309539, 13.97118731544910020, -46.63190125567759736 ) ) ;
#20186=CARTESIAN_POINT ( 'NONE',  ( 52.82122079009729276, -49.66539245525740398, -48.53632958723370194 ) ) ;
#20188=CARTESIAN_POINT ( 'NONE',  ( 61.51097123149799728, -45.14411397284619909, -28.15118130352110271 ) ) ;
#20190=CARTESIAN_POINT ( 'NONE',  ( 56.61906357297189629, 14.83060900076899991, -26.23212203939170095 ) ) ;
#20192=CARTESIAN_POINT ( 'NONE',  ( 50.17499495619189531, 17.98397139427959956, -76.14999999999999147 ) ) ;
#20193=CARTESIAN_POINT ( 'NONE',  ( 52.80835558948090380, 18.44458679360339559, -48.72774772676130084 ) ) ;
#20196=B_SPLINE_CURVE_WITH_KNOTS ( 'NONE', 3,
 ( #41120, #32706, #12837, #28794, #1288, #44795, #8899, #29311, #40856, #45316, #25372, #5487, #21445, #37444, #33501, #29567, #41897, #42158, #22215, #22730, #17781, #14372, #38482, #6257 ),
 .UNSPECIFIED., .F., .F.,
 ( 4, 2, 2, 2, 2, 2, 2, 2, 2, 2, 2, 4 ),
 ( 0.000000000000000000, 1.104949632659680159, 2.367749212842169992, 3.156998950456220143, 3.551623819263250326, 4.183023609354489913, 4.647713308159810097, 5.112403006965129393, 5.464321026995399677, 5.816239047025679731, 6.065118473969059565, 6.313997900912440286 ),
 .UNSPECIFIED. ) ;
#20197=EDGE_CURVE ( 'NONE', #17323, #17172, #45434, .T. ) ;
#20201=CARTESIAN_POINT ( 'NONE',  ( 47.52872824421969966, -54.58671296295030118, -55.01004339176270008 ) ) ;
#20203=DIRECTION ( 'NONE',  ( 0.000000000000000000, 0.000000000000000000, -1.000000000000000000 ) ) ;
#20204=CARTESIAN_POINT ( 'NONE',  ( 60.55719807483880146, -30.01614910288270011, -16.03343430148349924 ) ) ;
#20208=CARTESIAN_POINT ( 'NONE',  ( 82.75389963950340189, -45.59493862562520405, -47.67227237921369465 ) ) ;
#20210=ORIENTED_EDGE ( 'NONE', *, *, #8316, .T. ) ;
#20211=EDGE_LOOP ( 'NONE', ( #5138, #38719, #20675, #22051, #16136, #18984 ) ) ;
#20212=CARTESIAN_POINT ( 'NONE',  ( 56.93466172174790074, 19.03186587073140146, -52.70269903729370498 ) ) ;
#20213=CARTESIAN_POINT ( 'NONE',  ( 50.49064792301818727, -30.59810442101372274, -16.30494328501868395 ) ) ;
#20214=ORIENTED_EDGE ( 'NONE', *, *, #874, .T. ) ;
#20215=DIRECTION ( 'NONE',  ( 1.000000000000000000, 0.000000000000000000, 0.000000000000000000 ) ) ;
#20216=CARTESIAN_POINT ( 'NONE',  ( 53.70553476669380188, 20.08271752784780162, -75.56421356237311215 ) ) ;
#20217=ORIENTED_EDGE ( 'NONE', *, *, #9245, .T. ) ;
#20225=EDGE_CURVE ( 'NONE', #21835, #9203, #9066, .T. ) ;
#20228=CARTESIAN_POINT ( 'NONE',  ( 11.47481840896679905, -64.34949529473630037, -24.24805382140619869 ) ) ;
#20230=CARTESIAN_POINT ( 'NONE',  ( 45.47878560944119641, 14.14190573372439808, -8.420277138987120935 ) ) ;
#20231=CARTESIAN_POINT ( 'NONE',  ( 14.72167300019409986, 20.94680560585010198, -75.92929371827810314 ) ) ;
#20232=CARTESIAN_POINT ( 'NONE',  ( 51.67587649748560352, 17.45826286971839991, -77.01363636363639387 ) ) ;
#20233=CARTESIAN_POINT ( 'NONE',  ( 83.70962855682149950, -44.61778334324309725, -46.98048264170719790 ) ) ;
#20236=ORIENTED_EDGE ( 'NONE', *, *, #31503, .T. ) ;
#20237=CARTESIAN_POINT ( 'NONE',  ( 56.36055522987030031, -46.08204502026070770, -26.17081810832250000 ) ) ;
#20238=CARTESIAN_POINT ( 'NONE',  ( 15.66736729373610260, -50.89670101629940291, -20.45701610577929941 ) ) ;
#20243=VERTEX_POINT ( 'NONE', #25015 ) ;
#20244=CARTESIAN_POINT ( 'NONE',  ( -3.404429431994520083, -48.49755752188070090, -5.261476749836609734 ) ) ;
#20245=CARTESIAN_POINT ( 'NONE',  ( 47.23233947733660187, 23.53691302697210119, -54.67407144479440007 ) ) ;
#20249=CARTESIAN_POINT ( 'NONE',  ( 43.37850551145179878, 12.25211561368529978, -4.923475879823000056 ) ) ;
#20250=CARTESIAN_POINT ( 'NONE',  ( 16.13393739769620083, -15.61618894467929941, -7.049999999999999822 ) ) ;
#20253=CARTESIAN_POINT ( 'NONE',  ( 7.635415421591214447, 29.62789471496180482, -20.56421356237308729 ) ) ;
#20255=EDGE_CURVE ( 'NONE', #30697, #36299, #21196, .T. ) ;
#20257=CARTESIAN_POINT ( 'NONE',  ( 17.35523042653849757, -52.75136490455189886, -76.12493046668770091 ) ) ;
#20258=AXIS2_PLACEMENT_3D ( 'NONE', #51297, #32113, #3088 ) ;
#20260=CARTESIAN_POINT ( 'NONE',  ( 56.94972635783080506, -49.95903273471010664, -52.23813480702960277 ) ) ;
#20266=CARTESIAN_POINT ( 'NONE',  ( 18.26047510295519771, 20.40964180427139851, -75.33373089150879309 ) ) ;
#20270=CARTESIAN_POINT ( 'NONE',  ( 57.41357375845870337, -45.73808401094120057, -26.25850225888439837 ) ) ;
#20277=CARTESIAN_POINT ( 'NONE',  ( 53.93371030420179579, -46.24505842335499750, -15.35643322793939980 ) ) ;
#20279=FACE_OUTER_BOUND ( 'NONE', #6275, .T. ) ;
#20285=CARTESIAN_POINT ( 'NONE',  ( 60.61871271361510338, 14.50847209906229907, -47.69407632338739944 ) ) ;
#20286=CARTESIAN_POINT ( 'NONE',  ( 49.42599303854620274, 14.94800067427769896, -12.04389119005679909 ) ) ;
#20287=CARTESIAN_POINT ( 'NONE',  ( 16.65420337941059969, -49.11618894467930829, -20.15000000000000213 ) ) ;
#20289=CARTESIAN_POINT ( 'NONE',  ( -6.905391680084830064, 14.60833507279039978, -4.924128923718519957 ) ) ;
#20291=B_SPLINE_CURVE_WITH_KNOTS ( 'NONE', 3,
 ( #45320, #9426, #2068, #25376, #37969, #49262, #41377, #36931, #18044, #13356, #49519, #8903, #24853, #1034, #40861, #32979 ),
 .UNSPECIFIED., .F., .F.,
 ( 4, 2, 2, 2, 2, 2, 2, 4 ),
 ( 0.000000000000000000, 2.070511893743609999, 3.936888812047710573, 5.103374385987770268, 5.832427869700300249, 7.290534837125381529, 9.623505985005499141, 11.66485573940060050 ),
 .UNSPECIFIED. ) ;
#20294=FACE_OUTER_BOUND ( 'NONE', #49229, .T. ) ;
#20296=VERTEX_POINT ( 'NONE', #41545 ) ;
#20297=CARTESIAN_POINT ( 'NONE',  ( 55.07039890521039638, 17.27901299975469840, -48.53535122690350079 ) ) ;
#20299=CARTESIAN_POINT ( 'NONE',  ( 11.33958473649649967, 33.18416475853179293, -44.55219422208060109 ) ) ;
#20302=CARTESIAN_POINT ( 'NONE',  ( 46.65228552882730639, 22.34474942460779801, -76.02816657613060158 ) ) ;
#20303=CARTESIAN_POINT ( 'NONE',  ( 48.45666297591670002, -54.07999444344789453, -54.69197698175730693 ) ) ;
#20304=CARTESIAN_POINT ( 'NONE',  ( -9.414006712227710238, 12.57454005906549988, -5.942694572982400558 ) ) ;
#20313=ADVANCED_FACE ( 'NONE', ( #49685 ), #14032, .T. ) ;
#20316=CARTESIAN_POINT ( 'NONE',  ( 60.42880969657360168, -45.68174640767169592, -47.27616847270299871 ) ) ;
#20317=CARTESIAN_POINT ( 'NONE',  ( 12.13393739769600010, -55.41568642894409180, -23.15000000000000213 ) ) ;
#20318=CARTESIAN_POINT ( 'NONE',  ( 13.73527022026379996, 18.97497658877130178, -20.93080062776429884 ) ) ;
#20322=CARTESIAN_POINT ( 'NONE',  ( 16.13393739769620083, -15.61618894467929941, -7.349999999999999645 ) ) ;
#20325=CARTESIAN_POINT ( 'NONE',  ( 84.43710458089100257, -43.31157081238789885, -47.42958317885469910 ) ) ;
#20326=ORIENTED_EDGE ( 'NONE', *, *, #36551, .T. ) ;
#20327=EDGE_LOOP ( 'NONE', ( #41403, #172, #28087, #6544 ) ) ;
#20330=CARTESIAN_POINT ( 'NONE',  ( 53.59153692561029914, -49.40734274622519706, -49.22791863455219641 ) ) ;
#20331=CARTESIAN_POINT ( 'NONE',  ( 56.24502371864222283, 14.78143158593881878, -26.06737860630848402 ) ) ;
#20332=CARTESIAN_POINT ( 'NONE',  ( 76.40835530721405178, -10.60522176584313314, -12.83250761640861626 ) ) ;
#20333=CARTESIAN_POINT ( 'NONE',  ( 53.26253095931190273, -52.14051419252140107, -54.20764878218570004 ) ) ;
#20335=EDGE_LOOP ( 'NONE', ( #15756, #35285 ) ) ;
#20340=DIRECTION ( 'NONE',  ( 0.5685928097855377228, 0.5944782866685497380, -0.5685928097855377228 ) ) ;
#20345=CARTESIAN_POINT ( 'NONE',  ( 57.55751162049570269, -50.09049722528730086, -52.57651812429949700 ) ) ;
#20346=CARTESIAN_POINT ( 'NONE',  ( 53.79479401630810287, -50.60286759701570247, -76.98386069065520587 ) ) ;
#20348=DIRECTION ( 'NONE',  ( -0.1686178020941689615, 0.6660492713794448072, 0.7265992051412127894 ) ) ;
#20350=CARTESIAN_POINT ( 'NONE',  ( 13.52884004244890015, -50.22107084656090592, -21.01312649677589661 ) ) ;
#20352=DIRECTION ( 'NONE',  ( 0.9200120562340469155, 0.3918900565005459247, 8.326672684688669123E-17 ) ) ;
#20353=DIRECTION ( 'NONE',  ( 0.4778512656426511240, -0.8513147483649062819, 0.2166134048024561665 ) ) ;
#20354=CARTESIAN_POINT ( 'NONE',  ( -19.86606260230379917, -15.61618894467929408, 8.349999999999999645 ) ) ;
#20355=CARTESIAN_POINT ( 'NONE',  ( 53.55347996450810655, 18.14618377272432426, -49.15350056088379205 ) ) ;
#20357=EDGE_CURVE ( 'NONE', #17962, #7646, #43005, .T. ) ;
#20361=CARTESIAN_POINT ( 'NONE',  ( 14.59877825211439983, -51.94403353591209793, -75.77396328158880578 ) ) ;
#20363=CARTESIAN_POINT ( 'NONE',  ( 47.37100612791930132, -54.67334532463610230, -54.74722572687750244 ) ) ;
#20364=DIRECTION ( 'NONE',  ( 1.000000000000000000, 0.000000000000000000, 0.000000000000000000 ) ) ;
#20366=CARTESIAN_POINT ( 'NONE',  ( 84.12560686116410125, 12.73461969822788653, -46.88422903745967574 ) ) ;
#20367=AXIS2_PLACEMENT_3D ( 'NONE', #36452, #44328, #27823 ) ;
#20368=CARTESIAN_POINT ( 'NONE',  ( 60.94144441405484258, -45.44327996998872266, -47.23355084903774070 ) ) ;
#20369=CARTESIAN_POINT ( 'NONE',  ( 55.91595771132564607, -45.90465035585578590, -17.78184172665631380 ) ) ;
#20370=CARTESIAN_POINT ( 'NONE',  ( 11.73545769478199929, 34.19022130663289971, -18.15007894723629889 ) ) ;
#20371=LINE ( 'NONE', #16455, #31448 ) ;
#20374=CARTESIAN_POINT ( 'NONE',  ( 48.43561012759799667, 22.85868164950310089, -54.69790868973249331 ) ) ;
#20375=EDGE_LOOP ( 'NONE', ( #36779, #33848, #47064, #10097, #35014 ) ) ;
#20376=CARTESIAN_POINT ( 'NONE',  ( 52.76221414360290396, -49.72258092212369718, -48.84748662852409495 ) ) ;
#20378=DIRECTION ( 'NONE',  ( 0.000000000000000000, 0.000000000000000000, 1.000000000000000000 ) ) ;
#20380=CARTESIAN_POINT ( 'NONE',  ( 14.25134538048030031, 19.88704348275010148, -22.60288544069040029 ) ) ;
#20381=CARTESIAN_POINT ( 'NONE',  ( 84.14547009360870788, 12.78988100953520046, -47.04794573760770504 ) ) ;
#20382=CARTESIAN_POINT ( 'NONE',  ( 52.61201418189830292, 18.58180670245910093, -28.15003492000239760 ) ) ;
#20384=CARTESIAN_POINT ( 'NONE',  ( 53.59007319642049794, 18.17385789206429791, -49.22505640095170065 ) ) ;
#20386=CARTESIAN_POINT ( 'NONE',  ( 56.50061918389100413, -45.38130610931129638, -17.74550412614280148 ) ) ;
#20392=ORIENTED_EDGE ( 'NONE', *, *, #16748, .T. ) ;
#20393=CARTESIAN_POINT ( 'NONE',  ( 11.31751865133579926, -65.23669584953859157, -17.44711623494750086 ) ) ;
#20394=CARTESIAN_POINT ( 'NONE',  ( 11.56529054650530064, 33.93083920818509824, -46.99198115399620690 ) ) ;
#20395=CARTESIAN_POINT ( 'NONE',  ( 68.13393739769620083, -50.61618894467930119, -76.75000000000000000 ) ) ;
#20396=CARTESIAN_POINT ( 'NONE',  ( 51.40213405747029896, -51.07147713869009920, -49.97437711432529994 ) ) ;
#20397=CARTESIAN_POINT ( 'NONE',  ( 10.96685795547830011, -64.79867901642927563, -23.23109294039089789 ) ) ;
#20401=CARTESIAN_POINT ( 'NONE',  ( 11.13393739769619906, -63.32855195616750166, -43.91646290072930015 ) ) ;
#20402=DIRECTION ( 'NONE',  ( 0.000000000000000000, -0.9319748226751467524, 0.3625230060280709155 ) ) ;
#20404=CARTESIAN_POINT ( 'NONE',  ( 50.52803994521560327, -50.37895321258069714, -76.14999999999999147 ) ) ;
#20415=CARTESIAN_POINT ( 'NONE',  ( 46.48805971088770406, -53.10800393395699359, -76.13964794981698958 ) ) ;
#20416=ORIENTED_EDGE ( 'NONE', *, *, #42112, .T. ) ;
#20418=EDGE_CURVE ( 'NONE', #23799, #18800, #7004, .T. ) ;
#20419=FACE_OUTER_BOUND ( 'NONE', #7981, .T. ) ;
#20423=CARTESIAN_POINT ( 'NONE',  ( 46.39225494580800557, 21.75266102372379962, -76.14870948285189911 ) ) ;
#20425=EDGE_CURVE ( 'NONE', #12119, #33592, #21875, .T. ) ;
#20428=DIRECTION ( 'NONE',  ( -1.224646799147353207E-16, 1.000000000000000000, 0.000000000000000000 ) ) ;
#20431=CARTESIAN_POINT ( 'NONE',  ( 56.79938825701810146, -50.61924877113020216, -75.12131854917910800 ) ) ;
#20432=CARTESIAN_POINT ( 'NONE',  ( 57.24929578234380045, 19.38381105828390361, -53.91492796160409284 ) ) ;
#20434=AXIS2_PLACEMENT_3D ( 'NONE', #591, #8727, #7952 ) ;
#20436=CARTESIAN_POINT ( 'NONE',  ( 61.45699444135679812, 13.94749824582279984, -46.72613800703339848 ) ) ;
#20437=CARTESIAN_POINT ( 'NONE',  ( 12.82281323259240047, -64.96593576180920593, -46.32794539105049836 ) ) ;
#20439=CARTESIAN_POINT ( 'NONE',  ( 53.18486246474859769, -49.47487039336269987, -48.80133351323340207 ) ) ;
#20440=CARTESIAN_POINT ( 'NONE',  ( 60.44012286426450942, -45.18239918516130160, -26.74847066535680185 ) ) ;
#20442=CARTESIAN_POINT ( 'NONE',  ( 56.88244700999120340, 14.33082729724810100, -26.04504088914069726 ) ) ;
#20444=CARTESIAN_POINT ( 'NONE',  ( 50.40317162242880045, 18.69648349058939729, -76.14999999999999147 ) ) ;
#20445=CARTESIAN_POINT ( 'NONE',  ( 53.29392286865769535, 18.19942959119120118, -48.95065426190299718 ) ) ;
#20448=CARTESIAN_POINT ( 'NONE',  ( 53.55397377960559879, -51.73583884506710717, -53.25782589811129242 ) ) ;
#20449=ORIENTED_EDGE ( 'NONE', *, *, #2098, .F. ) ;
#20450=FACE_OUTER_BOUND ( 'NONE', #11602, .T. ) ;
#20451=CARTESIAN_POINT ( 'NONE',  ( 47.76739131609710398, -54.44992707061860671, -54.84422872089319156 ) ) ;
#20452=CARTESIAN_POINT ( 'NONE',  ( -8.924323233577288406, 12.96044049090009942, -5.352796889411019166 ) ) ;
#20453=FACE_OUTER_BOUND ( 'NONE', #21109, .T. ) ;
#20454=CARTESIAN_POINT ( 'NONE',  ( 61.33485920126659607, 14.38743525284970026, -47.69940821548620136 ) ) ;
#20456=CARTESIAN_POINT ( 'NONE',  ( 18.38332337263111427, -52.17615710686938968, -75.56421430878999956 ) ) ;
#20461=ORIENTED_EDGE ( 'NONE', *, *, #28733, .T. ) ;
#20463=CARTESIAN_POINT ( 'NONE',  ( 14.25092084710789919, -51.11945063272739276, -22.60339915794170196 ) ) ;
#20468=FACE_OUTER_BOUND ( 'NONE', #43229, .T. ) ;
#20470=ORIENTED_EDGE ( 'NONE', *, *, #3756, .T. ) ;
#20471=CARTESIAN_POINT ( 'NONE',  ( 61.28610861176739633, 13.99802266614350010, -46.37203261889099792 ) ) ;
#20473=CARTESIAN_POINT ( 'NONE',  ( 61.13405154998650204, 14.40638383414069956, -47.71032547765840093 ) ) ;
#20478=ORIENTED_EDGE ( 'NONE', *, *, #3507, .F. ) ;
#20479=CARTESIAN_POINT ( 'NONE',  ( 11.07146966777600028, -64.97230528211619571, -23.11170492349029715 ) ) ;
#20484=CARTESIAN_POINT ( 'NONE',  ( 14.47481033283960095, 20.39333564065439930, -75.48537863783369062 ) ) ;
#20485=EDGE_CURVE ( 'NONE', #37502, #3421, #32853, .T. ) ;
#20487=CARTESIAN_POINT ( 'NONE',  ( 83.09574564639500238, -44.89486624088750233, -46.39644155595880193 ) ) ;
#20490=ORIENTED_EDGE ( 'NONE', *, *, #39326, .T. ) ;
#20491=CARTESIAN_POINT ( 'NONE',  ( 53.14742929986179831, -49.37086717498490174, -27.49438065588160285 ) ) ;
#20492=CARTESIAN_POINT ( 'NONE',  ( 15.58442563903250111, -50.84470211311809607, -20.41433498000790081 ) ) ;
#20498=CARTESIAN_POINT ( 'NONE',  ( -4.162343151726740409, -48.30019726062069907, -5.617366207439410175 ) ) ;
#20499=CARTESIAN_POINT ( 'NONE',  ( 47.42380321553230260, 23.40185720734870145, -54.69111192316769632 ) ) ;
#20502=CARTESIAN_POINT ( 'NONE',  ( 55.35733030022484513, 16.14712512605141725, -26.51179285998376756 ) ) ;
#20503=FACE_OUTER_BOUND ( 'NONE', #10581, .T. ) ;
#20508=CARTESIAN_POINT ( 'NONE',  ( 55.20295770280799275, -48.56198109356999737, -48.76073667618629770 ) ) ;
#20511=CARTESIAN_POINT ( 'NONE',  ( 17.36235827195499937, -52.98917440366089693, -76.14999999999999147 ) ) ;
#20515=ORIENTED_EDGE ( 'NONE', *, *, #27902, .F. ) ;
#20517=CARTESIAN_POINT ( 'NONE',  ( 10.48523087532110054, 31.88305279702909800, -45.62962604688630108 ) ) ;
#20519=CARTESIAN_POINT ( 'NONE',  ( 68.23802800759220588, -31.42890113106329508, -18.38247165234229996 ) ) ;
#20521=CARTESIAN_POINT ( 'NONE',  ( 18.45619610651039721, 20.68589454807339933, -75.38352342698830455 ) ) ;
#20525=CARTESIAN_POINT ( 'NONE',  ( 11.65161691330369997, -64.97831056663849836, -46.09346701959520232 ) ) ;
#20526=DIRECTION ( 'NONE',  ( 0.000000000000000000, -1.000000000000000000, 0.000000000000000000 ) ) ;
#20528=CARTESIAN_POINT ( 'NONE',  ( 56.83411512905762919, -46.90160822220050818, -26.73578643762690277 ) ) ;
#20530=ORIENTED_EDGE ( 'NONE', *, *, #13335, .F. ) ;
#20531=CARTESIAN_POINT ( 'NONE',  ( 75.25317828858366909, 3.262240055439041608, -12.30554431910427304 ) ) ;
#20534=VERTEX_POINT ( 'NONE', #24095 ) ;
#20537=CARTESIAN_POINT ( 'NONE',  ( 59.48252993831315649, -45.49665726213240902, -26.72040254028946649 ) ) ;
#20542=CARTESIAN_POINT ( 'NONE',  ( 73.01379001973170091, 13.72769019945460123, -13.76114987980459858 ) ) ;
#20543=CARTESIAN_POINT ( 'NONE',  ( 47.96938416189519216, 13.96888898634079901, -9.741253716576860455 ) ) ;
#20545=DIRECTION ( 'NONE',  ( 0.000000000000000000, 0.000000000000000000, 1.000000000000000000 ) ) ;
#20546=CARTESIAN_POINT ( 'NONE',  ( -8.918955708164858720, 12.96516353870340055, -5.380344673046240977 ) ) ;
#20547=CARTESIAN_POINT ( 'NONE',  ( 1.127242003616780508, -53.29999274968538714, -7.495163844720678092 ) ) ;
#20549=CARTESIAN_POINT ( 'NONE',  ( 61.05354884778520130, 14.03248421730429918, -27.55223363601019670 ) ) ;
#20551=ORIENTED_EDGE ( 'NONE', *, *, #7682, .T. ) ;
#20552=CARTESIAN_POINT ( 'NONE',  ( 60.24058964203619837, 14.54579934782940143, -47.32689780713820227 ) ) ;
#20553=CARTESIAN_POINT ( 'NONE',  ( 43.05762310336380239, 14.74520815673739982, -7.621878241775270624 ) ) ;
#20554=LINE ( 'NONE', #36550, #47143 ) ;
#20557=CARTESIAN_POINT ( 'NONE',  ( 10.97564840259020080, -65.00352292546099875, -17.33480504156820245 ) ) ;
#20559=CARTESIAN_POINT ( 'NONE',  ( 12.82083315176570082, 18.86661839715909750, -21.11500886439040059 ) ) ;
#20560=CARTESIAN_POINT ( 'NONE',  ( 46.89722913963129969, 22.92670556637019885, -75.65864051473879215 ) ) ;
#20562=CARTESIAN_POINT ( 'NONE',  ( 49.39745668169630477, -53.63492652054119958, -54.43253521562210295 ) ) ;
#20563=CIRCLE ( 'NONE', #31452, 2.999999999999997780 ) ;
#20564=CYLINDRICAL_SURFACE ( 'NONE', #3018, 20.79999999999999716 ) ;
#20566=FACE_OUTER_BOUND ( 'NONE', #30839, .T. ) ;
#20568=CARTESIAN_POINT ( 'NONE',  ( 56.07568765954189871, 13.88381105532070059, -14.74720511883509921 ) ) ;
#20569=EDGE_LOOP ( 'NONE', ( #20723, #28972, #14751, #30319, #22341 ) ) ;
#20573=DIRECTION ( 'NONE',  ( -1.000000000000000000, 0.000000000000000000, 0.000000000000000000 ) ) ;
#20574=CARTESIAN_POINT ( 'NONE',  ( 60.54364033361749620, -45.62202010502980443, -47.24421774848470079 ) ) ;
#20576=CARTESIAN_POINT ( 'NONE',  ( 50.34328701401641126, -43.49848369320205421, -6.583824542005403124 ) ) ;
#20579=DIRECTION ( 'NONE',  ( -2.565320000000000120E-13, -1.000000000000000000, 8.628712999999999808E-13 ) ) ;
#20580=DIRECTION ( 'NONE',  ( -0.05023550054956202326, 0.000000000000000000, 0.9987374001630934250 ) ) ;
#20581=ORIENTED_EDGE ( 'NONE', *, *, #24481, .T. ) ;
#20582=CARTESIAN_POINT ( 'NONE',  ( 84.20053740572899414, -44.11518990482350233, -47.28523898137510173 ) ) ;
#20585=CARTESIAN_POINT ( 'NONE',  ( 61.67800232651970305, -45.19184251940130537, -46.93943497666659681 ) ) ;
#20586=CARTESIAN_POINT ( 'NONE',  ( 53.12243681351169755, -49.57385822095360339, -49.13999347672969975 ) ) ;
#20587=CARTESIAN_POINT ( 'NONE',  ( 17.52154708603973887, -14.60803149382545563, -170.7999095292539948 ) ) ;
#20588=CARTESIAN_POINT ( 'NONE',  ( 76.44636341052239459, -6.604837239822047401, -12.99629018861355156 ) ) ;
#20589=CARTESIAN_POINT ( 'NONE',  ( 53.13499564549729826, -52.07858566517519705, -53.65455749828319654 ) ) ;
#20591=ORIENTED_EDGE ( 'NONE', *, *, #40865, .F. ) ;
#20592=ORIENTED_EDGE ( 'NONE', *, *, #50840, .F. ) ;
#20594=CIRCLE ( 'NONE', #49916, 1.999999999999999334 ) ;
#20596=CARTESIAN_POINT ( 'NONE',  ( 13.88443978363049069, -50.25762978063119846, -20.90776614285152846 ) ) ;
#20598=FACE_OUTER_BOUND ( 'NONE', #24399, .T. ) ;
#20599=CARTESIAN_POINT ( 'NONE',  ( 51.99248274614070198, -49.49756876763530045, -77.11023451094040126 ) ) ;
#20601=CARTESIAN_POINT ( 'NONE',  ( 52.98832978415040174, -50.41796700477780746, -76.96373676954098642 ) ) ;
#20603=DIRECTION ( 'NONE',  ( 0.000000000000000000, 0.000000000000000000, -1.000000000000000000 ) ) ;
#20604=VECTOR ( 'NONE', #24943, 999.9999999999998863 ) ;
#20608=DIRECTION ( 'NONE',  ( 0.000000000000000000, -0.9319748226751467524, 0.3625230060280709155 ) ) ;
#20610=CARTESIAN_POINT ( 'NONE',  ( 42.60880853662280288, -43.93543342225530068, -4.906336349381930084 ) ) ;
#20613=CARTESIAN_POINT ( 'NONE',  ( 61.30653360879629332, -45.38759780313989722, -47.35768905649830174 ) ) ;
#20614=EDGE_CURVE ( 'NONE', #19589, #20020, #39657, .T. ) ;
#20619=ORIENTED_EDGE ( 'NONE', *, *, #41923, .F. ) ;
#20620=CARTESIAN_POINT ( 'NONE',  ( 14.07179683629490086, -52.32664520840259570, -75.76244777734170555 ) ) ;
#20621=CARTESIAN_POINT ( 'NONE',  ( 47.28175591391539712, -54.73378013403499409, -54.73619099792320242 ) ) ;
#20622=CARTESIAN_POINT ( 'NONE',  ( 13.00893739761190027, 34.28605925116320208, -47.75434321210310173 ) ) ;
#20624=CARTESIAN_POINT ( 'NONE',  ( 61.02432256287157486, -45.45604146479874430, -47.36561844619770767 ) ) ;
#20625=CIRCLE ( 'NONE', #1384, 20.00000000000000355 ) ;
#20628=B_SPLINE_CURVE_WITH_KNOTS ( 'NONE', 3,
 ( #10728, #19354, #31130, #51074, #23261, #31900, #7059, #42705, #31385, #51336, #26681, #47413, #43725, #11507 ),
 .UNSPECIFIED., .F., .F.,
 ( 4, 2, 2, 2, 2, 2, 4 ),
 ( 11.92140392297045892, 18.73771508492814419, 24.98362011319689202, 28.10657262733126416, 33.10329664994625887, 41.09805508613030867, 41.83711151413364604 ),
 .UNSPECIFIED. ) ;
#20629=CARTESIAN_POINT ( 'NONE',  ( 11.91450189635799894, 34.20545694164769657, -17.98631677231880133 ) ) ;
#20630=FACE_OUTER_BOUND ( 'NONE', #46408, .T. ) ;
#20632=CARTESIAN_POINT ( 'NONE',  ( 56.46551649800760231, 19.54378829069240098, -53.85224769578630344 ) ) ;
#20633=CARTESIAN_POINT ( 'NONE',  ( 42.80890084343171509, 12.86785355401084807, -5.063862465213780695 ) ) ;
#20635=CARTESIAN_POINT ( 'NONE',  ( 48.59288953467110161, 22.89722549970059617, -55.31247818475549849 ) ) ;
#20636=EDGE_LOOP ( 'NONE', ( #28262, #4878 ) ) ;
#20642=CYLINDRICAL_SURFACE ( 'NONE', #15364, 5.000000000000000000 ) ;
#20643=CARTESIAN_POINT ( 'NONE',  ( 83.66401895982369297, 13.28260268565369984, -46.61643406624119734 ) ) ;
#20644=CARTESIAN_POINT ( 'NONE',  ( 56.02287817249710145, 14.72004393977189984, -25.81294518235560176 ) ) ;
#20647=CARTESIAN_POINT ( 'NONE',  ( 54.85121201869780094, -45.70040766398989973, -15.57405995174110025 ) ) ;
#20652=CARTESIAN_POINT ( 'NONE',  ( 11.82286116600939962, -65.20082272508568622, -16.82382485989019827 ) ) ;
#20653=CARTESIAN_POINT ( 'NONE',  ( 10.97424772006000104, 33.59586616593779951, -46.68812779134029967 ) ) ;
#20655=CARTESIAN_POINT ( 'NONE',  ( 48.31794077192549963, -54.26005012469399702, -54.97046006864109557 ) ) ;
#20659=FACE_OUTER_BOUND ( 'NONE', #25025, .T. ) ;
#20661=FACE_OUTER_BOUND ( 'NONE', #6483, .T. ) ;
#20663=CARTESIAN_POINT ( 'NONE',  ( 50.45186351439279804, -50.03424225457590069, -76.14999999999999147 ) ) ;
#20668=ORIENTED_EDGE ( 'NONE', *, *, #48877, .F. ) ;
#20670=CARTESIAN_POINT ( 'NONE',  ( 15.67962062493570130, 19.63028992856250099, -15.65622423491010196 ) ) ;
#20673=CARTESIAN_POINT ( 'NONE',  ( 54.11848747779500002, 20.00241981255700097, -75.47262416762160342 ) ) ;
#20674=CARTESIAN_POINT ( 'NONE',  ( 47.30205888664269764, -54.42250278362140392, -75.11586948118589646 ) ) ;
#20675=ORIENTED_EDGE ( 'NONE', *, *, #11084, .F. ) ;
#20677=EDGE_CURVE ( 'NONE', #9983, #43315, #41332, .T. ) ;
#20680=CARTESIAN_POINT ( 'NONE',  ( 12.32811467040465203, 34.12052296847067367, -23.60606026631527143 ) ) ;
#20682=CARTESIAN_POINT ( 'NONE',  ( 46.37388399891210611, 21.71424375792910055, -76.14999999999999147 ) ) ;
#20683=DIRECTION ( 'NONE',  ( 0.000000000000000000, 0.000000000000000000, 1.000000000000000000 ) ) ;
#20687=CARTESIAN_POINT ( 'NONE',  ( 56.27102044028909944, 19.34483705538490028, -52.87264067008490542 ) ) ;
#20688=CARTESIAN_POINT ( 'NONE',  ( 16.13393739707289853, -15.61618894541809865, -10.45000000021869901 ) ) ;
#20691=CARTESIAN_POINT ( 'NONE',  ( 61.57009831922090370, 13.89954555936719949, -46.42185750248089704 ) ) ;
#20693=ADVANCED_FACE ( 'NONE', ( #43984 ), #8090, .F. ) ;
#20694=CARTESIAN_POINT ( 'NONE',  ( 12.93945173865840204, -65.41176199011280801, -46.97472070025159496 ) ) ;
#20696=CARTESIAN_POINT ( 'NONE',  ( 52.85389961514279378, -49.65025774184390173, -48.74486371238739935 ) ) ;
#20697=CARTESIAN_POINT ( 'NONE',  ( 61.58984863193099812, -45.12803552000509910, -28.15126211424280100 ) ) ;
#20699=CARTESIAN_POINT ( 'NONE',  ( 13.17518462309900151, 19.66209683819560183, -21.60491894709759819 ) ) ;
#20700=CARTESIAN_POINT ( 'NONE',  ( 56.69484138974510046, 14.42054476167730215, -26.04356117224130074 ) ) ;
#20702=CARTESIAN_POINT ( 'NONE',  ( 50.98146089766679978, 18.17698877489110032, -76.31995468916950642 ) ) ;
#20703=CARTESIAN_POINT ( 'NONE',  ( 53.42160460796090149, 18.12642228866929983, -48.88221542113920037 ) ) ;
#20705=DIRECTION ( 'NONE',  ( -0.2260571801428161165, 1.249000902703300368E-16, 0.9741140340359943917 ) ) ;
#20706=CARTESIAN_POINT ( 'NONE',  ( 68.57574012094990223, -45.11618894467940066, -13.49754435276109987 ) ) ;
#20707=ORIENTED_EDGE ( 'NONE', *, *, #28926, .F. ) ;
#20711=CARTESIAN_POINT ( 'NONE',  ( 47.61217947097659930, -54.50984741584490223, -54.68372563208449577 ) ) ;
#20714=CARTESIAN_POINT ( 'NONE',  ( 41.72053738002289691, 12.47914145849190071, -3.400228433360679592 ) ) ;
#20715=CARTESIAN_POINT ( 'NONE',  ( 59.80688163256760248, 15.43365568175059899, -48.65827547727460001 ) ) ;
#20723=ORIENTED_EDGE ( 'NONE', *, *, #9104, .T. ) ;
#20725=VERTEX_POINT ( 'NONE', #25072 ) ;
#20727=AXIS2_PLACEMENT_3D ( 'NONE', #32038, #35991, #47549 ) ;
#20730=DIRECTION ( 'NONE',  ( 2.375726999999999900E-16, -1.726067000000000108E-16, 1.000000000000000000 ) ) ;
#20731=CARTESIAN_POINT ( 'NONE',  ( 56.50435945712200692, -45.38311456362110619, -25.29338994482560210 ) ) ;
#20733=CARTESIAN_POINT ( 'NONE',  ( 52.47362269241929766, 19.31045068696670342, -76.54035590729588989 ) ) ;
#20735=CARTESIAN_POINT ( 'NONE',  ( 61.04001029137710077, 14.12696047140060074, -46.86320535112459851 ) ) ;
#20741=EDGE_CURVE ( 'NONE', #15227, #14552, #50412, .T. ) ;
#20745=CARTESIAN_POINT ( 'NONE',  ( 75.13393739769618662, -33.11618894467940066, -84.38499399519520239 ) ) ;
#20747=CARTESIAN_POINT ( 'NONE',  ( 14.27929716716409914, 21.26099547410829871, -75.92929371827810314 ) ) ;
#20748=B_SPLINE_CURVE_WITH_KNOTS ( 'NONE', 3,
 ( #3816, #40739, #4315, #24464, #905, #4062, #16627, #8249, #24725, #32326, #20028 ),
 .UNSPECIFIED., .F., .F.,
 ( 4, 1, 1, 1, 1, 1, 1, 1, 4 ),
 ( 0.000000000000000000, 0.1249999449042852873, 0.2499998898085705745, 0.3749998347128558618, 0.4999997796171411490, 0.6249997245214263808, 0.7499996694257117236, 0.8749996143299969553, 1.000000000000000000 ),
 .UNSPECIFIED. ) ;
#20749=CARTESIAN_POINT ( 'NONE',  ( 83.92831008986510710, -44.23173406571270050, -46.72264359244280740 ) ) ;
#20750=AXIS2_PLACEMENT_3D ( 'NONE', #29058, #48732, #9666 ) ;
#20751=CARTESIAN_POINT ( 'NONE',  ( 11.22168610240190212, 33.99689329125807546, -17.68872724081435521 ) ) ;
#20754=CARTESIAN_POINT ( 'NONE',  ( 53.10146316558890334, -49.38330102694990131, -27.45415746263869750 ) ) ;
#20755=CARTESIAN_POINT ( 'NONE',  ( 16.65427257814090112, -51.11618894347309805, -20.14977964541890287 ) ) ;
#20756=CARTESIAN_POINT ( 'NONE',  ( 76.88109033428489170, 11.93863756556099887, -14.86960256363260058 ) ) ;
#20757=CARTESIAN_POINT ( 'NONE',  ( 43.91474985151640453, 12.31375205243809923, -5.093415854581109237 ) ) ;
#20760=EDGE_LOOP ( 'NONE', ( #50403, #17665, #13608, #48554 ) ) ;
#20761=CARTESIAN_POINT ( 'NONE',  ( -2.836119463527300155, -49.03823118242020485, -5.545754996175841001 ) ) ;
#20762=CARTESIAN_POINT ( 'NONE',  ( 47.33824183327239865, 23.46194572669929812, -54.72426965761560069 ) ) ;
#20763=CARTESIAN_POINT ( 'NONE',  ( 85.17508943611194638, -49.58715777506750300, -52.74015335379896641 ) ) ;
#20766=CARTESIAN_POINT ( 'NONE',  ( 11.19833776072039910, 33.93568566053470192, -17.40716472516109903 ) ) ;
#20770=CARTESIAN_POINT ( 'NONE',  ( 57.59063731204929582, -47.30990445082789364, -48.19963584321670425 ) ) ;
#20773=CARTESIAN_POINT ( 'NONE',  ( 17.51123789366869943, -52.86216653946310373, -76.12493046668770091 ) ) ;
#20775=DIRECTION ( 'NONE',  ( 1.898780000000000034E-11, 1.593211000000000006E-12, -1.000000000000000000 ) ) ;
#20776=ORIENTED_EDGE ( 'NONE', *, *, #7596, .T. ) ;
#20778=CARTESIAN_POINT ( 'NONE',  ( 9.742404792955269954, 32.03540899651829932, -46.29735760005750222 ) ) ;
#20781=CARTESIAN_POINT ( 'NONE',  ( 67.52396372158538895, -31.85234974313089751, -18.22675602796779870 ) ) ;
#20783=CARTESIAN_POINT ( 'NONE',  ( 18.11571509568589988, 19.92749982851029955, -74.54610039094001195 ) ) ;
#20786=ORIENTED_EDGE ( 'NONE', *, *, #16367, .T. ) ;
#20787=ORIENTED_EDGE ( 'NONE', *, *, #40761, .F. ) ;
#20788=CARTESIAN_POINT ( 'NONE',  ( 13.00893739769619906, -65.51843714052719747, -47.75434321273180416 ) ) ;
#20792=CARTESIAN_POINT ( 'NONE',  ( 61.65531616106190427, 13.91691178440649779, -46.72879703837820387 ) ) ;
#20795=ORIENTED_EDGE ( 'NONE', *, *, #47528, .F. ) ;
#20796=VECTOR ( 'NONE', #1077, 1000.000000000000000 ) ;
#20800=CARTESIAN_POINT ( 'NONE',  ( 52.10267380125439729, 1.883811055320649963, -20.65000000000000213 ) ) ;
#20802=ORIENTED_EDGE ( 'NONE', *, *, #14800, .T. ) ;
#20805=CARTESIAN_POINT ( 'NONE',  ( 65.03603135424580728, -1.463538230407920082, -19.52361391316370032 ) ) ;
#20807=CARTESIAN_POINT ( 'NONE',  ( 71.02745183554199571, 13.08237462510360061, -12.42623600195140021 ) ) ;
#20809=CARTESIAN_POINT ( 'NONE',  ( 54.53726782211339952, 14.79465002154760001, -15.67786077975019943 ) ) ;
#20810=DIRECTION ( 'NONE',  ( 0.3415390592402317571, -0.6017342458922744219, -0.7219882051209377538 ) ) ;
#20811=CARTESIAN_POINT ( 'NONE',  ( -3.777837492685370169, 16.75613853373169704, -4.322105417705759400 ) ) ;
#20812=CARTESIAN_POINT ( 'NONE',  ( 10.10517893431099878, 23.92687708958460036, -21.14999999999999858 ) ) ;
#20813=CARTESIAN_POINT ( 'NONE',  ( 57.33445156889590066, 14.51539213118700111, -26.24906306687159940 ) ) ;
#20818=CARTESIAN_POINT ( 'NONE',  ( 12.64313521576329968, 34.23242425603879724, -47.04313497434819880 ) ) ;
#20822=AXIS2_PLACEMENT_3D ( 'NONE', #45460, #26232, #42238 ) ;
#20823=LINE ( 'NONE', #15176, #46900 ) ;
#20825=CARTESIAN_POINT ( 'NONE',  ( 46.35275103504439898, 21.67755452994670406, -76.14999999999999147 ) ) ;
#20826=CARTESIAN_POINT ( 'NONE',  ( 49.72648160330909661, -53.64673639094029767, -55.11972614036100282 ) ) ;
#20827=DIRECTION ( 'NONE',  ( 0.000000000000000000, 0.000000000000000000, 1.000000000000000000 ) ) ;
#20828=CARTESIAN_POINT ( 'NONE',  ( 76.72248428439638701, -43.18406392197798027, -14.42532300465747319 ) ) ;
#20836=CARTESIAN_POINT ( 'NONE',  ( 60.32372535534879887, -45.84468058682939784, -47.67141866289389895 ) ) ;
#20838=CARTESIAN_POINT ( 'NONE',  ( 63.88483510052807191, -43.42126949022875948, -10.13989943727382581 ) ) ;
#20842=DIRECTION ( 'NONE',  ( 0.000000000000000000, 0.000000000000000000, 1.000000000000000000 ) ) ;
#20844=CARTESIAN_POINT ( 'NONE',  ( 82.91592277202040862, -45.56282308470729703, -47.63723459745410338 ) ) ;
#20847=ORIENTED_EDGE ( 'NONE', *, *, #51596, .T. ) ;
#20848=CARTESIAN_POINT ( 'NONE',  ( 1.633937397696199056, -15.61618894467930119, -6.928362978644219794 ) ) ;
#20849=CARTESIAN_POINT ( 'NONE',  ( 56.11803403278968005, 14.71426362913575403, -25.91247644177123988 ) ) ;
#20850=CARTESIAN_POINT ( 'NONE',  ( 76.46866432614550035, -4.873297363397687931, -13.09238815314908244 ) ) ;
#20852=CARTESIAN_POINT ( 'NONE',  ( 55.71337517921909210, -51.07520708147169586, -53.59468954495790172 ) ) ;
#20858=DIRECTION ( 'NONE',  ( 0.000000000000000000, 0.000000000000000000, -1.000000000000000000 ) ) ;
#20859=CARTESIAN_POINT ( 'NONE',  ( 8.796734227443069543, -63.17759121671350186, -46.67028841929619887 ) ) ;
#20860=DIRECTION ( 'NONE',  ( 0.000000000000000000, 0.000000000000000000, -1.000000000000000000 ) ) ;
#20862=AXIS2_PLACEMENT_3D ( 'NONE', #37876, #46269, #14022 ) ;
#20865=CARTESIAN_POINT ( 'NONE',  ( 11.18388210880936562, 32.13318903344607236, -14.72248478078991951 ) ) ;
#20866=CARTESIAN_POINT ( 'NONE',  ( 53.99792507037630429, -50.61618862432099775, -77.02993420784260081 ) ) ;
#20868=CIRCLE ( 'NONE', #46037, 1.999999999999995115 ) ;
#20869=CARTESIAN_POINT ( 'NONE',  ( 83.49396093869917479, -45.25227168876257622, -47.52772051731956537 ) ) ;
#20871=CIRCLE ( 'NONE', #27578, 2.000000000000001776 ) ;
#20873=EDGE_CURVE ( 'NONE', #12469, #5062, #48906, .T. ) ;
#20874=CARTESIAN_POINT ( 'NONE',  ( 68.13393739769620083, -49.36618894467930829, -73.25000000000000000 ) ) ;
#20878=CARTESIAN_POINT ( 'NONE',  ( 43.05690220640799737, -43.67411922962340043, -4.900907769805740166 ) ) ;
#20880=CARTESIAN_POINT ( 'NONE',  ( 67.04038824939736685, -50.70395984888217811, -72.15645085170115181 ) ) ;
#20881=CARTESIAN_POINT ( 'NONE',  ( 61.37892430293329937, -45.32812869357670849, -47.24517423587799669 ) ) ;
#20884=CARTESIAN_POINT ( 'NONE',  ( 66.71085391307920531, -0.3516942507182569955, -17.22176303687090027 ) ) ;
#20886=CARTESIAN_POINT ( 'NONE',  ( 14.14442474872529942, -52.06054985064280061, -75.71157996061791096 ) ) ;
#20887=CARTESIAN_POINT ( 'NONE',  ( 47.35501076093819961, -54.67813530284840340, -54.64069690081250030 ) ) ;
#20890=CARTESIAN_POINT ( 'NONE',  ( 61.04944787454328292, -45.46340257749388769, -47.40250302194245791 ) ) ;
#20892=CARTESIAN_POINT ( 'NONE',  ( 57.43837919783884161, 13.96417635576200134, -25.73816349075863741 ) ) ;
#20893=CARTESIAN_POINT ( 'NONE',  ( 11.17220089305429909, 33.98357240679010260, -17.67193522364469871 ) ) ;
#20897=CARTESIAN_POINT ( 'NONE',  ( 48.40744063480869386, 22.97621965999740112, -55.31593188200960043 ) ) ;
#20898=VERTEX_POINT ( 'NONE', #44693 ) ;
#20901=VERTEX_POINT ( 'NONE', #20057 ) ;
#20902=CARTESIAN_POINT ( 'NONE',  ( 18.86789271228535725, -51.78678246903497495, -74.34716300800680244 ) ) ;
#20905=CARTESIAN_POINT ( 'NONE',  ( 82.45627759125980560, 13.86034323648230071, -46.38986626917139233 ) ) ;
#20906=CARTESIAN_POINT ( 'NONE',  ( 53.92218800908630527, 17.13899829394239660, -26.37400648228619815 ) ) ;
#20909=CARTESIAN_POINT ( 'NONE',  ( 57.50723869802200028, -45.11618894467940066, -17.68294118799479975 ) ) ;
#20910=B_SPLINE_SURFACE_WITH_KNOTS ( 'NONE', 3, 3, ( 
 ( #50202, #14295, #10369, #30520, #5667, #46544, #21613, #37618, #41809, #10631, #21361, #49690, #29739, #45754, #9847, #25803 ),
 ( #17961, #5916, #37890, #33930, #14037, #15332, #35234, #42603, #30776, #22656, #6698, #18733, #51241, #34971, #27115, #31285 ),
 ( #23164, #3020, #19252, #15067, #26853, #42864, #46800, #39181, #47060, #6958, #38677, #3278, #11145, #7210, #2762, #34712 ),
 ( #31035, #50713, #14811, #10890, #43119, #22910, #38927, #18990, #50970, #25709, #2667, #10534, #13943, #6086, #45918, #42509 ),
 ( #46709, #50619, #45654, #26236, #5823, #42767, #37794, #33838, #30170, #34354, #18379, #6866, #25971, #10010, #38053, #50369 ),
 ( #13690, #2146, #14455, #33586, #30423, #29649, #41714, #18126, #21786, #1889, #46449, #6595, #26492, #22559, #38307, #17867 ),
 ( #38575, #18641, #49851, #17619, #34616, #14715, #46187, #29901, #41983, #30686, #10793, #37525, #26753, #1628, #49603, #34090 ),
 ( #50102, #9756, #14200, #10273, #6341, #42243, #22301, #2394, #43283, #43784, #31446, #36415, #12591, #8652, #48232, #30101 ),
 ( #22495, #38505, #2605, #14649, #17553, #41654, #22608, #30988, #35186, #43326, #27065, #26804, #27576, #51189, #7166, #23120 ) ),
 .UNSPECIFIED., .F., .F., .F.,
 ( 4, 1, 1, 1, 1, 1, 4 ),
 ( 4, 2, 2, 2, 2, 2, 2, 4 ),
 ( -1.817263145799999900E-05, 0.1666666666666670182, 0.3333333333333329818, 0.5000000000000000000, 0.6666666666666670737, 0.8333333333333330373, 1.000000000000000000 ),
 ( -1.817262822599999744E-05, 0.3475067738041929810, 1.991082141981049825, 3.418070884026870093, 4.557427845368080099, 5.127106326038690653, 5.582849110575169860, 5.633122992941930640 ),
 .UNSPECIFIED. ) ;
#20913=EDGE_CURVE ( 'NONE', #260, #15485, #46708, .T. ) ;
#20914=AXIS2_PLACEMENT_3D ( 'NONE', #42407, #17268, #46350 ) ;
#20916=CARTESIAN_POINT ( 'NONE',  ( 11.70612132433960006, -65.02222053889551034, -16.54010580623710069 ) ) ;
#20917=CARTESIAN_POINT ( 'NONE',  ( 11.26776687660830056, 33.31889147624380598, -45.55476822783580104 ) ) ;
#20919=CARTESIAN_POINT ( 'NONE',  ( 48.63054825335189690, -53.86377910125730040, -54.34287102679169834 ) ) ;
#20921=ORIENTED_EDGE ( 'NONE', *, *, #34201, .F. ) ;
#20924=CARTESIAN_POINT ( 'NONE',  ( 52.86588932659250162, 18.89687367272220087, -50.05840281104079992 ) ) ;
#20926=CARTESIAN_POINT ( 'NONE',  ( 50.50110134946189788, -49.67252027771040446, -76.16336504862310619 ) ) ;
#20927=DIRECTION ( 'NONE',  ( -2.306135999999999414E-12, 2.429896999999999860E-12, -1.000000000000000000 ) ) ;
#20928=ORIENTED_EDGE ( 'NONE', *, *, #6582, .F. ) ;
#20931=ORIENTED_EDGE ( 'NONE', *, *, #15557, .F. ) ;
#20932=PLANE ( 'NONE',  #20163 ) ;
#20933=CARTESIAN_POINT ( 'NONE',  ( 56.83411512905762919, 15.66923033284180633, -26.73578643762690277 ) ) ;
#20935=CARTESIAN_POINT ( 'NONE',  ( 13.59495223564569955, -51.40398734714930384, -22.70120839867610130 ) ) ;
#20936=CARTESIAN_POINT ( 'NONE',  ( 56.00368918932939266, 19.58097593056960051, -74.93707363489029660 ) ) ;
#20938=CARTESIAN_POINT ( 'NONE',  ( 46.81730464115280199, -53.59092212908089436, -75.98233228156729524 ) ) ;
#20939=ORIENTED_EDGE ( 'NONE', *, *, #21719, .F. ) ;
#20940=AXIS2_PLACEMENT_3D ( 'NONE', #26546, #22357, #18694 ) ;
#20941=CARTESIAN_POINT ( 'NONE',  ( 55.45319518098449407, 14.78280949324359916, -16.61882359200989967 ) ) ;
#20943=CARTESIAN_POINT ( 'NONE',  ( 57.03340749225579742, -50.31390957266170005, -52.79504027221379658 ) ) ;
#20944=CARTESIAN_POINT ( 'NONE',  ( 52.58883999282150512, -49.83940783755189585, -48.57092258697220188 ) ) ;
#20948=CARTESIAN_POINT ( 'NONE',  ( 47.43262305882279861, 23.39837035974399981, -74.36069403054010252 ) ) ;
#20949=PLANE ( 'NONE',  #38469 ) ;
#20950=DIRECTION ( 'NONE',  ( 0.000000000000000000, 0.000000000000000000, 1.000000000000000000 ) ) ;
#20951=CARTESIAN_POINT ( 'NONE',  ( 12.27153357072740114, 33.38674963102350546, -15.84005975576420155 ) ) ;
#20957=CARTESIAN_POINT ( 'NONE',  ( 61.25188761286670314, 14.01595200629009952, -46.56130740076640251 ) ) ;
#20958=CARTESIAN_POINT ( 'NONE',  ( -29.55684472351650172, -35.86170217675510230, -55.62305524083090091 ) ) ;
#20960=CARTESIAN_POINT ( 'NONE',  ( 53.31239004767299861, -49.40924252131510030, -48.83993499871439781 ) ) ;
#20961=CARTESIAN_POINT ( 'NONE',  ( 60.19345682049280555, -45.11617047991499874, -26.22295725826409907 ) ) ;
#20962=CARTESIAN_POINT ( 'NONE',  ( 48.02939153114380133, -54.36963205275330324, -55.28067537372130147 ) ) ;
#20963=CARTESIAN_POINT ( 'NONE',  ( 56.76514959097689683, 14.22673106357260053, -25.88737783761489908 ) ) ;
#20965=CARTESIAN_POINT ( 'NONE',  ( 50.50110133130939971, 18.44014233979840256, -76.16336504856330691 ) ) ;
#20966=CARTESIAN_POINT ( 'NONE',  ( 52.68891395819000678, 18.51768936255079723, -48.47378032971769812 ) ) ;
#20968=CARTESIAN_POINT ( 'NONE',  ( 41.27829218924360077, -44.10783499397969365, -3.596739496640999789 ) ) ;
#20969=CARTESIAN_POINT ( 'NONE',  ( 64.61644452598639532, -44.96401322665339961, -11.41031418918720064 ) ) ;
#20970=EDGE_LOOP ( 'NONE', ( #14564, #51756, #29122, #50714 ) ) ;
#20974=ADVANCED_FACE ( 'NONE', ( #40760 ), #48636, .F. ) ;
#20976=CARTESIAN_POINT ( 'NONE',  ( 47.42307040393540518, -54.63294004021819461, -54.67104605768700054 ) ) ;
#20985=CARTESIAN_POINT ( 'NONE',  ( 16.13393739769620083, -15.61618894467929941, 7.944363289481099599 ) ) ;
#20986=ADVANCED_FACE ( 'NONE', ( #20566 ), #30155, .T. ) ;
#20989=ORIENTED_EDGE ( 'NONE', *, *, #8706, .T. ) ;
#20990=CARTESIAN_POINT ( 'NONE',  ( 9.276735402967759114, -63.13661701015139727, -46.53281877167430025 ) ) ;
#20991=CARTESIAN_POINT ( 'NONE',  ( 16.10973090867273783, -51.04076668988478360, -15.66788158150958132 ) ) ;
#20992=EDGE_LOOP ( 'NONE', ( #51486, #19798, #4880, #45112 ) ) ;
#20996=CARTESIAN_POINT ( 'NONE',  ( 53.99629484646779787, 19.44063541514490012, -76.54982658315300625 ) ) ;
#20998=DIRECTION ( 'NONE',  ( 1.000000000000000000, 0.000000000000000000, 0.000000000000000000 ) ) ;
#21003=CARTESIAN_POINT ( 'NONE',  ( 16.15069521921704165, -51.05177107958204630, -15.66900421577824254 ) ) ;
#21006=CARTESIAN_POINT ( 'NONE',  ( 11.37791593499470011, -63.64622813626678521, -24.39397853729850141 ) ) ;
#21008=CARTESIAN_POINT ( 'NONE',  ( 40.71242742815670113, 14.10279950470690125, -5.692218735367429616 ) ) ;
#21009=CARTESIAN_POINT ( 'NONE',  ( 14.21728741900179926, 20.91286242874570078, -75.79069550273320033 ) ) ;
#21012=CARTESIAN_POINT ( 'NONE',  ( 84.44784216359251161, -43.11618894467930119, -47.47585302082339354 ) ) ;
#21016=CARTESIAN_POINT ( 'NONE',  ( 55.11178888707910062, -47.40156703920949610, -26.42191461600259572 ) ) ;
#21017=CARTESIAN_POINT ( 'NONE',  ( 53.80404574041880039, -51.29624668929719888, -75.54363968662481454 ) ) ;
#21018=CARTESIAN_POINT ( 'NONE',  ( 57.36123081079020380, 18.90300135422739913, -52.61896059691729732 ) ) ;
#21019=B_SPLINE_CURVE_WITH_KNOTS ( 'NONE', 3,
 ( #3616, #8768, #36530, #3358, #898, #635, #15409, #31361, #15665, #31617 ),
 .UNSPECIFIED., .F., .F.,
 ( 4, 2, 2, 2, 4 ),
 ( 0.000000000000000000, 0.1774999999982362353, 0.3374999999966465936, 0.4374999999956565855, 0.4999999271596955452 ),
 .UNSPECIFIED. ) ;
#21021=CARTESIAN_POINT ( 'NONE',  ( 45.63704616078170062, 14.88914480619270186, -9.401569148867338299 ) ) ;
#21023=CARTESIAN_POINT ( 'NONE',  ( -6.893020797678770073, -45.90759191447720156, -5.210453294515490441 ) ) ;
#21024=CARTESIAN_POINT ( 'NONE',  ( 47.36721828898109976, 23.44513434380789718, -54.83101768469499859 ) ) ;
#21027=LINE ( 'NONE', #45152, #20604 ) ;
#21028=CARTESIAN_POINT ( 'NONE',  ( 11.37397754636229941, 34.06366721452670276, -17.68262826289139866 ) ) ;
#21029=DIRECTION ( 'NONE',  ( 0.000000000000000000, 0.000000000000000000, 1.000000000000000000 ) ) ;
#21032=CARTESIAN_POINT ( 'NONE',  ( 56.37993369902870455, -47.94505858661049302, -48.46713487898719563 ) ) ;
#21034=CARTESIAN_POINT ( 'NONE',  ( 54.90250570405320474, 20.20956959306230161, -53.93623998597109903 ) ) ;
#21038=CARTESIAN_POINT ( 'NONE',  ( 8.968618095842160187, 31.99037451711150126, -46.63269056292379844 ) ) ;
#21042=ORIENTED_EDGE ( 'NONE', *, *, #6555, .T. ) ;
#21043=CARTESIAN_POINT ( 'NONE',  ( 18.71089559737819741, 20.68059730019909992, -75.01675372117850316 ) ) ;
#21044=ORIENTED_EDGE ( 'NONE', *, *, #27200, .T. ) ;
#21045=ORIENTED_EDGE ( 'NONE', *, *, #2409, .T. ) ;
#21046=CARTESIAN_POINT ( 'NONE',  ( 47.83780165944450147, 23.21886414354259998, -55.23279884646720461 ) ) ;
#21048=CARTESIAN_POINT ( 'NONE',  ( 10.78709078437059965, -64.43314706647589674, -46.17090595131550401 ) ) ;
#21049=CARTESIAN_POINT ( 'NONE',  ( 56.76506913988440317, -45.81015338506770718, -26.16735717962830066 ) ) ;
#21051=AXIS2_PLACEMENT_3D ( 'NONE', #21100, #29992, #22394 ) ;
#21053=CARTESIAN_POINT ( 'NONE',  ( 61.63685072850250179, 13.93395889737410087, -46.81169383245449467 ) ) ;
#21055=ORIENTED_EDGE ( 'NONE', *, *, #47308, .F. ) ;
#21056=CIRCLE ( 'NONE', #1800, 3.000000000000000000 ) ;
#21057=CARTESIAN_POINT ( 'NONE',  ( 16.13393739769620083, -15.61618894467929941, -21.14999999999999858 ) ) ;
#21059=CARTESIAN_POINT ( 'NONE',  ( 12.24533239789906780, 33.66790093028144071, -16.17634612495991320 ) ) ;
#21061=CARTESIAN_POINT ( 'NONE',  ( 11.53023960985226282, -64.72036740955095979, -23.95196799016841993 ) ) ;
#21063=CARTESIAN_POINT ( 'NONE',  ( 59.52869410915831594, -45.48984219772450643, -26.73579121603098585 ) ) ;
#21064=ORIENTED_EDGE ( 'NONE', *, *, #28393, .F. ) ;
#21065=ORIENTED_EDGE ( 'NONE', *, *, #31917, .F. ) ;
#21066=CARTESIAN_POINT ( 'NONE',  ( 8.133937397696209715, -59.02534396924340143, -43.74348518090240390 ) ) ;
#21067=CARTESIAN_POINT ( 'NONE',  ( 46.65865115320059431, -53.59114685036150405, -76.01705645362520158 ) ) ;
#21068=CARTESIAN_POINT ( 'NONE',  ( 73.21814398186710093, 13.07780085657029900, -13.04737355632260076 ) ) ;
#21069=CARTESIAN_POINT ( 'NONE',  ( 49.49099539719589558, 14.73512810581040000, -11.95182011558090096 ) ) ;
#21071=CARTESIAN_POINT ( 'NONE',  ( -3.774505099339080072, 16.75816115460079914, -4.401388191994590748 ) ) ;
#21073=CARTESIAN_POINT ( 'NONE',  ( 61.30969410147389453, 13.98565706813869980, -28.15107826849129680 ) ) ;
#21074=ADVANCED_FACE ( 'NONE', ( #32296 ), #50265, .T. ) ;
#21077=CARTESIAN_POINT ( 'NONE',  ( 58.46570011688019264, 15.47571369907180028, -47.60876906798830532 ) ) ;
#21079=CARTESIAN_POINT ( 'NONE',  ( -8.385535285650650650, -44.09170945325140423, -4.751637014762500222 ) ) ;
#21084=CARTESIAN_POINT ( 'NONE',  ( 12.16231664501490073, -64.67747237300790175, -15.91745067707079819 ) ) ;
#21085=CARTESIAN_POINT ( 'NONE',  ( 11.27206271277036009, 34.04961529007477594, -18.17421237816838087 ) ) ;
#21086=CARTESIAN_POINT ( 'NONE',  ( 12.94867006626759931, 18.87859900410219893, -21.09868194578459821 ) ) ;
#21087=CARTESIAN_POINT ( 'NONE',  ( 47.13218220315749818, 23.40331810880470087, -74.95061771218550462 ) ) ;
#21088=CARTESIAN_POINT ( 'NONE',  ( 49.18118975347450572, -53.84795997730500261, -54.89353827381820139 ) ) ;
#21089=CARTESIAN_POINT ( 'NONE',  ( 42.26864886252769793, -44.36179212852169940, -5.126484877156399556 ) ) ;
#21090=CARTESIAN_POINT ( 'NONE',  ( 76.70062604860851252, -43.19086386613712136, -14.38326864798454530 ) ) ;
#21093=ORIENTED_EDGE ( 'NONE', *, *, #43477, .F. ) ;
#21097=CARTESIAN_POINT ( 'NONE',  ( 84.12560686111216057, -43.96699758738883190, -46.88422903683994036 ) ) ;
#21098=CARTESIAN_POINT ( 'NONE',  ( 60.74931022661039748, -45.65492624904909746, -47.61700330749530252 ) ) ;
#21099=DIRECTION ( 'NONE',  ( 0.3805321250008310008, 0.000000000000000000, -0.9247677015566404535 ) ) ;
#21100=CARTESIAN_POINT ( 'NONE',  ( 16.13393739769620083, -15.61618894467929941, -14.65000000000000036 ) ) ;
#21103=FACE_OUTER_BOUND ( 'NONE', #6770, .T. ) ;
#21105=EDGE_CURVE ( 'NONE', #11543, #33996, #10395, .T. ) ;
#21107=CARTESIAN_POINT ( 'NONE',  ( 83.43488124258610128, -45.15430218069970181, -47.39353206303620425 ) ) ;
#21109=EDGE_LOOP ( 'NONE', ( #6497, #12755, #2901, #2044 ) ) ;
#21113=CARTESIAN_POINT ( 'NONE',  ( 52.57212603780299531, -49.85477880025769792, -48.51322654165320358 ) ) ;
#21115=CARTESIAN_POINT ( 'NONE',  ( 56.46551567295650642, 19.54378694285259854, -74.14999999999999147 ) ) ;
#21118=CARTESIAN_POINT ( 'NONE',  ( 11.58469291347408969, 34.12844306514984538, -22.56541115952017051 ) ) ;
#21119=ORIENTED_EDGE ( 'NONE', *, *, #18376, .F. ) ;
#21121=CARTESIAN_POINT ( 'NONE',  ( 56.89013219823429779, 19.38816751928939652, -53.45144266626400054 ) ) ;
#21122=DIRECTION ( 'NONE',  ( -0.5685928097855439400, -0.5944782866685399680, 0.5685928097855418306 ) ) ;
#21126=CARTESIAN_POINT ( 'NONE',  ( -64.19449136036995185, 21.25811091637316252, -62.88965083512582055 ) ) ;
#21127=AXIS2_PLACEMENT_3D ( 'NONE', #8971, #12908, #40409 ) ;
#21128=CARTESIAN_POINT ( 'NONE',  ( 52.75996719278299452, -50.16875253228529630, -77.25935876431830707 ) ) ;
#21130=CARTESIAN_POINT ( 'NONE',  ( 60.43524540865149675, 14.44381373781700084, -47.22144309172190191 ) ) ;
#21133=CARTESIAN_POINT ( 'NONE',  ( 41.22888721229060138, 13.59583590325410007, -5.431170674539309573 ) ) ;
#21134=CARTESIAN_POINT ( 'NONE',  ( 41.47267154800490374, -44.68978306873219708, -5.287754256597220426 ) ) ;
#21136=CARTESIAN_POINT ( 'NONE',  ( 68.23750919724679420, 0.1964239558528288465, -18.38207371053462325 ) ) ;
#21138=CARTESIAN_POINT ( 'NONE',  ( 66.13282613077339533, -0.2025808033276020048, -17.01779698185609746 ) ) ;
#21139=VERTEX_POINT ( 'NONE', #2692 ) ;
#21140=CARTESIAN_POINT ( 'NONE',  ( 13.83628172507089893, -52.07648608105650112, -75.48775473117470369 ) ) ;
#21142=CARTESIAN_POINT ( 'NONE',  ( 47.20893740402939898, -54.78691078231059919, -54.64017658907569341 ) ) ;
#21149=CARTESIAN_POINT ( 'NONE',  ( 47.67992640529440251, -54.51849087148959683, -55.14611402303650323 ) ) ;
#21152=CARTESIAN_POINT ( 'NONE',  ( 48.72320918298880343, 22.79968469717220358, -54.90669916513539306 ) ) ;
#21153=ORIENTED_EDGE ( 'NONE', *, *, #40865, .T. ) ;
#21158=DIRECTION ( 'NONE',  ( 0.000000000000000000, -1.000000000000000000, 0.000000000000000000 ) ) ;
#21159=CARTESIAN_POINT ( 'NONE',  ( 72.13393739769618662, -31.87354825726865570, -20.65000000000000213 ) ) ;
#21161=CARTESIAN_POINT ( 'NONE',  ( 83.25229294592290330, 13.91601796603040064, -47.26064541804080221 ) ) ;
#21162=CARTESIAN_POINT ( 'NONE',  ( 54.56756649838740714, 16.38481432401099980, -26.02999983734660105 ) ) ;
#21165=CARTESIAN_POINT ( 'NONE',  ( 55.55364201925849699, -45.11618894467940066, -14.32024453839470013 ) ) ;
#21166=EDGE_CURVE ( 'NONE', #33533, #22647, #6255, .T. ) ;
#21170=ORIENTED_EDGE ( 'NONE', *, *, #3507, .T. ) ;
#21171=CARTESIAN_POINT ( 'NONE',  ( 11.49145838456619906, -65.03764954149001198, -16.71591419049050131 ) ) ;
#21172=CARTESIAN_POINT ( 'NONE',  ( 11.70363152391320050, 33.71475452077960000, -45.68937680901829879 ) ) ;
#21173=CARTESIAN_POINT ( 'NONE',  ( 18.60924722850695545, 20.15530953838155170, -15.72404377366573947 ) ) ;
#21174=DIRECTION ( 'NONE',  ( 0.000000000000000000, 0.000000000000000000, -1.000000000000000000 ) ) ;
#21176=EDGE_LOOP ( 'NONE', ( #41282, #44720, #21333, #652 ) ) ;
#21178=CIRCLE ( 'NONE', #22819, 14.50000000000000178 ) ;
#21179=CARTESIAN_POINT ( 'NONE',  ( 30.63393739769620083, -15.61618894467929941, -7.349999999999999645 ) ) ;
#21181=CARTESIAN_POINT ( 'NONE',  ( 50.08385623720359803, -49.23364898979970405, -76.14999999999999147 ) ) ;
#21182=DIRECTION ( 'NONE',  ( 1.397030999999999991E-10, 0.000000000000000000, -1.000000000000000000 ) ) ;
#21191=CARTESIAN_POINT ( 'NONE',  ( -8.966062602303800588, -15.61618894467929763, 4.450000000000000178 ) ) ;
#21193=CARTESIAN_POINT ( 'NONE',  ( 47.34724033287390199, -54.49456303200130236, -74.94574354657768822 ) ) ;
#21194=ORIENTED_EDGE ( 'NONE', *, *, #11152, .F. ) ;
#21195=CARTESIAN_POINT ( 'NONE',  ( 55.80628784892600436, 14.51787704501589893, -16.86082891554699970 ) ) ;
#21196=CIRCLE ( 'NONE', #37978, 50.00000000000000000 ) ;
#21197=CARTESIAN_POINT ( 'NONE',  ( 57.24929579703059801, -50.61618895653209904, -53.91492794795339449 ) ) ;
#21201=CARTESIAN_POINT ( 'NONE',  ( 46.91399176935180293, 22.65135599081870055, -75.82172624862269572 ) ) ;
#21202=ADVANCED_FACE ( 'NONE', ( #20450 ), #23857, .T. ) ;
#21204=CARTESIAN_POINT ( 'NONE',  ( 75.18413422297084026, -30.89995173026953523, -11.96273407203979211 ) ) ;
#21205=CARTESIAN_POINT ( 'NONE',  ( 12.36320305067610015, 33.31445045643330616, -15.76422791930239953 ) ) ;
#21207=CIRCLE ( 'NONE', #25365, 1.999999999999999112 ) ;
#21212=CARTESIAN_POINT ( 'NONE',  ( -25.78889119571919863, -40.94810731387600100, -54.35424806255070251 ) ) ;
#21214=CARTESIAN_POINT ( 'NONE',  ( 52.80965640710000031, -49.67361798074160362, -48.67334656000949877 ) ) ;
#21215=LINE ( 'NONE', #16790, #27856 ) ;
#21217=CARTESIAN_POINT ( 'NONE',  ( 13.40139815547580149, 19.60627775220709879, -21.60243834236359817 ) ) ;
#21218=CARTESIAN_POINT ( 'NONE',  ( 57.41989411400300014, 14.57099383176320018, -26.28150916840570162 ) ) ;
#21219=CARTESIAN_POINT ( 'NONE',  ( 50.46752463075389983, 18.34784747648950187, -76.16325466870340222 ) ) ;
#21220=CARTESIAN_POINT ( 'NONE',  ( 52.78692660382639446, 18.45971159535350026, -48.74514607373690467 ) ) ;
#21223=CARTESIAN_POINT ( 'NONE',  ( 63.80692360858208900, -44.33172560060000222, -10.42320585664760024 ) ) ;
#21229=CARTESIAN_POINT ( 'NONE',  ( 47.51461438356749767, -54.58063482146310008, -54.74847341959169711 ) ) ;
#21232=CARTESIAN_POINT ( 'NONE',  ( 60.88462772975219650, 14.97986367131530017, -48.34569376290319553 ) ) ;
#21240=CARTESIAN_POINT ( 'NONE',  ( 13.89744741070980005, -51.22086835671689897, -22.99801678904039903 ) ) ;
#21243=ORIENTED_EDGE ( 'NONE', *, *, #41104, .F. ) ;
#21247=CARTESIAN_POINT ( 'NONE',  ( 52.52866728376119454, 19.54011015037300325, -76.33211554319051118 ) ) ;
#21248=ORIENTED_EDGE ( 'NONE', *, *, #25179, .F. ) ;
#21253=CIRCLE ( 'NONE', #19583, 31.00000000000000000 ) ;
#21254=LINE ( 'NONE', #24918, #51434 ) ;
#21255=CARTESIAN_POINT ( 'NONE',  ( 53.67902323473164472, 20.08789433012093539, -75.56984044762756980 ) ) ;
#21258=CARTESIAN_POINT ( 'NONE',  ( 56.99379930123120630, -45.91441121812820114, -26.24653336503459755 ) ) ;
#21262=AXIS2_PLACEMENT_3D ( 'NONE', #37532, #25204, #5320 ) ;
#21263=CARTESIAN_POINT ( 'NONE',  ( 14.04520966608050081, 21.07290090200200083, -75.74020909530109691 ) ) ;
#21272=CARTESIAN_POINT ( 'NONE',  ( 54.39377529478350226, -47.82348005630770160, -26.11201681070369673 ) ) ;
#21273=CARTESIAN_POINT ( 'NONE',  ( 15.49194271725979988, -51.11618894182689843, -21.93290768620759934 ) ) ;
#21274=DIRECTION ( 'NONE',  ( 0.6888026391158329487, -0.7071067811865494601, 0.1598465650148944150 ) ) ;
#21276=DIRECTION ( 'NONE',  ( 0.000000000000000000, 1.000000000000000000, 0.000000000000000000 ) ) ;
#21277=VERTEX_POINT ( 'NONE', #24109 ) ;
#21278=CARTESIAN_POINT ( 'NONE',  ( -8.099603983670419893, -44.89123915805890164, -5.203145410111580382 ) ) ;
#21279=CARTESIAN_POINT ( 'NONE',  ( 47.31777781540550620, 23.47673220148309881, -54.77383212233990406 ) ) ;
#21283=CARTESIAN_POINT ( 'NONE',  ( 68.13393739769630031, -48.11618894467697061, -70.54999999999976978 ) ) ;
#21284=CARTESIAN_POINT ( 'NONE',  ( 11.01107119607550011, 33.80107206112160156, -17.34607913294370007 ) ) ;
#21285=DIRECTION ( 'NONE',  ( 1.000000000000000000, 0.000000000000000000, 0.000000000000000000 ) ) ;
#21288=CARTESIAN_POINT ( 'NONE',  ( 53.55347996444280056, -49.37856166211740572, -49.15350056090500885 ) ) ;
#21291=CARTESIAN_POINT ( 'NONE',  ( 52.25110910887259763, 21.11888751745159709, -53.60439093749319994 ) ) ;
#21294=CARTESIAN_POINT ( 'NONE',  ( 11.89321892211240161, 34.20364954171930094, -18.17421237891140251 ) ) ;
#21296=CARTESIAN_POINT ( 'NONE',  ( 20.04366315139102284, 23.92455260968660369, -19.04010690988194909 ) ) ;
#21297=CARTESIAN_POINT ( 'NONE',  ( 8.967661537042060260, 31.98469721247670350, -46.63268446062889439 ) ) ;
#21299=CARTESIAN_POINT ( 'NONE',  ( 68.39016270601220526, -30.11595112179599809, -18.15415021036589849 ) ) ;
#21301=CARTESIAN_POINT ( 'NONE',  ( 18.22835651418590430, 20.70615929725470039, -75.58342519351550948 ) ) ;
#21302=B_SPLINE_CURVE_WITH_KNOTS ( 'NONE', 3,
 ( #25190, #29391, #14190, #41447, #33831, #6333, #38301, #42235, #9746, #2389, #22034, #18366, #34085, #13683, #45394, #50092, #34348, #21258, #1881, #10265, #29642, #37267, #50359, #17355, #21779, #1619, #25966, #25703, #26225, #14447, #9499 ),
 .UNSPECIFIED., .F., .F.,
 ( 4, 3, 3, 3, 3, 3, 3, 3, 3, 3, 4 ),
 ( -0.9179866166508640068, -0.9044986999917590254, -0.7348924114151850207, -0.6321994764267000466, -0.6191523904019210489, -0.4753206641776559493, -0.3314757346574650487, -0.2163403421623650846, -0.1749400520680369775, -0.1011994735390420175, 1.210143096841420629E-14 ),
 .UNSPECIFIED. ) ;
#21303=ORIENTED_EDGE ( 'NONE', *, *, #26051, .T. ) ;
#21304=ORIENTED_EDGE ( 'NONE', *, *, #21623, .F. ) ;
#21307=ORIENTED_EDGE ( 'NONE', *, *, #12380, .F. ) ;
#21308=CARTESIAN_POINT ( 'NONE',  ( 12.53104704357910038, -65.45992346937650552, -47.41792381619649888 ) ) ;
#21309=CARTESIAN_POINT ( 'NONE',  ( 56.20148638111029982, -46.06399181071520132, -26.07311021849060140 ) ) ;
#21312=CARTESIAN_POINT ( 'NONE',  ( 61.50946113848699781, 13.98876303943020005, -46.98789045329460379 ) ) ;
#21318=CARTESIAN_POINT ( 'NONE',  ( 54.86028353996010054, -45.11618894460420393, -14.11209852549220045 ) ) ;
#21319=CARTESIAN_POINT ( 'NONE',  ( 13.13393739769619906, 32.28996932333459569, -46.39999999999999858 ) ) ;
#21322=CARTESIAN_POINT ( 'NONE',  ( 46.65068702493330477, -53.59610475534989860, -76.01748491306379663 ) ) ;
#21323=CARTESIAN_POINT ( 'NONE',  ( 61.06898323382710458, 14.42329441383000166, -47.72188698851990551 ) ) ;
#21324=CARTESIAN_POINT ( 'NONE',  ( 53.37797796334299250, 15.00503494411220018, -14.93909541112770079 ) ) ;
#21327=PLANE ( 'NONE',  #28346 ) ;
#21329=CARTESIAN_POINT ( 'NONE',  ( 61.19331679372790234, 13.94935370702680011, -27.45781938327959537 ) ) ;
#21332=B_SPLINE_SURFACE_WITH_KNOTS ( 'NONE', 3, 3, ( 
 ( #32733, #45081, #49028, #20437, #20694, #28561, #8931 ),
 ( #24356, #40627, #9191, #1573, #41402, #25399, #1056 ),
 ( #36424, #17309, #28298, #44302, #36683, #17051, #8410 ),
 ( #13134, #44562, #24617, #4996, #532, #49286, #9450 ),
 ( #41145, #40370, #16518, #12867, #32466, #4728, #25142 ),
 ( #37222, #21212, #29084, #48496, #5260, #1319, #33271 ),
 ( #4467, #13385, #29344, #20958, #12599, #786, #5520 ),
 ( #17564, #45346, #12336, #36954, #48763, #16785, #24876 ),
 ( #28823, #44824, #37475, #40886, #33532, #18841, #50568 ),
 ( #34039, #18320, #6809, #33785, #6541, #17813, #49796 ),
 ( #50315, #34302, #38254, #14400, #42714, #46653, #25659 ),
 ( #29597, #2874, #22761, #2616, #29846, #50048, #14658 ),
 ( #45867, #38782, #49547, #37736, #14142, #25915, #9698 ),
 ( #30368, #46393, #10482, #13637, #1833, #6289, #9951 ),
 ( #30112, #45601, #18585, #41928, #41662, #21729, #30628 ),
 ( #10736, #26437, #5765, #13887, #6026, #22504, #21987 ),
 ( #2347, #46131, #18070, #42453, #38515, #37997, #2094 ),
 ( #10219, #22245, #26179, #42190, #34564, #26691, #12030 ) ),
 .UNSPECIFIED., .F., .F., .F.,
 ( 4, 2, 2, 2, 2, 2, 2, 2, 4 ),
 ( 4, 1, 1, 1, 4 ),
 ( -1.510109315586890100, -1.104486737752440106, -0.6746458442922780296, -0.2928561180551860210, 0.000000000000000000, 0.2928561180551860210, 0.6746458442922800280, 1.104486737752599979, 1.510109315586930068 ),
 ( -0.002513234661244860123, 0.2500000000000000000, 0.5000000000000000000, 0.7500000000000000000, 1.000404478440260148 ),
 .UNSPECIFIED. ) ;
#21333=ORIENTED_EDGE ( 'NONE', *, *, #21623, .T. ) ;
#21334=CARTESIAN_POINT ( 'NONE',  ( 56.55198054733560298, 16.47836500032180140, -47.99512079638530082 ) ) ;
#21335=CIRCLE ( 'NONE', #31392, 2.000000000000001776 ) ;
#21337=CARTESIAN_POINT ( 'NONE',  ( 76.10455262750920724, -42.22089123566479429, -13.51974447861309869 ) ) ;
#21340=CARTESIAN_POINT ( 'NONE',  ( 82.13853704237929776, -45.11618894467940066, -46.42699167578030028 ) ) ;
#21342=CARTESIAN_POINT ( 'NONE',  ( 49.33069834983029978, -53.71595991359180289, -54.59303725311939814 ) ) ;
#21343=CARTESIAN_POINT ( 'NONE',  ( 42.05805429857900180, -44.46257822744319554, -5.167112339002620125 ) ) ;
#21345=CARTESIAN_POINT ( 'NONE',  ( 18.39482185675899828, -51.45286096149530408, -74.99552951437290460 ) ) ;
#21346=CARTESIAN_POINT ( 'NONE',  ( 68.13393739769620083, 19.38381105532069881, -65.65000000000000568 ) ) ;
#21352=ORIENTED_EDGE ( 'NONE', *, *, #27475, .T. ) ;
#21353=CARTESIAN_POINT ( 'NONE',  ( 16.13393739769620083, -15.61618894467929941, -3.187564294433600232 ) ) ;
#21354=CARTESIAN_POINT ( 'NONE',  ( 60.67234038688799558, -45.64753983419380035, -47.54984858108749535 ) ) ;
#21356=CARTESIAN_POINT ( 'NONE',  ( 50.12047694090430383, 18.16987201063400192, -76.14999999999999147 ) ) ;
#21358=DIRECTION ( 'NONE',  ( 0.000000000000000000, 0.000000000000000000, 1.000000000000000000 ) ) ;
#21361=CARTESIAN_POINT ( 'NONE',  ( 41.16399130181100219, -45.54541204712649716, -6.123782152551889624 ) ) ;
#21366=CARTESIAN_POINT ( 'NONE',  ( 61.67596629463390201, -45.13022690132009984, -46.63288306418059648 ) ) ;
#21367=CARTESIAN_POINT ( 'NONE',  ( 52.82265541972740408, -49.70184132309329783, -48.95329528328969815 ) ) ;
#21368=DIRECTION ( 'NONE',  ( -0.6047562208151086027, -0.7964106436916998932, 0.000000000000000000 ) ) ;
#21369=CARTESIAN_POINT ( 'NONE',  ( 54.57122049157750610, -51.56176576482789642, -53.75487193063269586 ) ) ;
#21370=VERTEX_POINT ( 'NONE', #48512 ) ;
#21374=VECTOR ( 'NONE', #38956, 1000.000000000000114 ) ;
#21378=CARTESIAN_POINT ( 'NONE',  ( 68.13393739769620083, 18.13381105532069881, -71.50000000000000000 ) ) ;
#21379=ORIENTED_EDGE ( 'NONE', *, *, #1995, .T. ) ;
#21381=CARTESIAN_POINT ( 'NONE',  ( 52.38320847335089780, -50.28303243813110157, -76.75839862240199807 ) ) ;
#21383=FACE_OUTER_BOUND ( 'NONE', #37096, .T. ) ;
#21387=CARTESIAN_POINT ( 'NONE',  ( 42.17658700080410483, 13.90468392624960003, -6.213782667886099453 ) ) ;
#21388=CARTESIAN_POINT ( 'NONE',  ( 42.50318722107469682, -43.99659477718180511, -4.913421252495600022 ) ) ;
#21390=CARTESIAN_POINT ( 'NONE',  ( -1.266062602303798856, -15.61618894538776736, -7.049999999999999822 ) ) ;
#21393=VECTOR ( 'NONE', #13570, 1000.000000000000000 ) ;
#21395=CARTESIAN_POINT ( 'NONE',  ( 66.35712187483230196, -0.6058384114035900714, -16.95628796889650047 ) ) ;
#21399=CARTESIAN_POINT ( 'NONE',  ( 14.58589179554379989, -51.79680004542600358, -75.65449215554859563 ) ) ;
#21400=CARTESIAN_POINT ( 'NONE',  ( 57.37350358383859827, 18.90030437368070082, -52.61683795673179986 ) ) ;
#21405=CARTESIAN_POINT ( 'NONE',  ( 55.76693333300482891, -45.94012783645938924, -17.15566813129047219 ) ) ;
#21406=CARTESIAN_POINT ( 'NONE',  ( 10.91841378338849999, 33.81381314252419656, -17.66395372719320278 ) ) ;
#21407=CARTESIAN_POINT ( 'NONE',  ( 13.61938558678000000, 20.19483563406610216, -23.15000000000000213 ) ) ;
#21409=CARTESIAN_POINT ( 'NONE',  ( 18.06932202639930196, -55.56934008872529773, -76.14999999999999147 ) ) ;
#21410=CARTESIAN_POINT ( 'NONE',  ( 48.07874646582410350, 23.06343134960649977, -54.84615067176530090 ) ) ;
#21415=CARTESIAN_POINT ( 'NONE',  ( 72.38393739883420608, 4.883811055320659733, -61.44999999999999574 ) ) ;
#21417=CARTESIAN_POINT ( 'NONE',  ( 78.22251691734010137, -33.11618894467940066, -20.65000000000000213 ) ) ;
#21418=CARTESIAN_POINT ( 'NONE',  ( 83.62075525755088279, 13.54933044287569999, -47.10035895585609467 ) ) ;
#21419=CARTESIAN_POINT ( 'NONE',  ( 53.87546017034450330, 17.18069085124139761, -26.23270880884989964 ) ) ;
#21422=CARTESIAN_POINT ( 'NONE',  ( 55.36114930388180255, -45.13341976228700503, -14.57736059671599804 ) ) ;
#21423=LINE ( 'NONE', #13086, #8001 ) ;
#21424=CIRCLE ( 'NONE', #8916, 14.50000000000000178 ) ;
#21427=CARTESIAN_POINT ( 'NONE',  ( 11.70888777236110023, -64.91672506495389428, -16.37375727426629979 ) ) ;
#21428=CARTESIAN_POINT ( 'NONE',  ( 10.96434002348909864, 32.60498813690350062, -45.01351260974220025 ) ) ;
#21432=AXIS2_PLACEMENT_3D ( 'NONE', #41855, #37661, #49984 ) ;
#21437=EDGE_CURVE ( 'NONE', #23493, #28405, #1837, .T. ) ;
#21440=CARTESIAN_POINT ( 'NONE',  ( 59.32371920583819502, -2.960042943344160182, -15.67710711396670042 ) ) ;
#21441=CARTESIAN_POINT ( 'NONE',  ( 51.21769384557849492, -49.33082554619760174, -76.45366765177809043 ) ) ;
#21442=EDGE_CURVE ( 'NONE', #31681, #1406, #42330, .T. ) ;
#21445=CARTESIAN_POINT ( 'NONE',  ( 53.25888871246090162, -49.10877824327840102, -26.73652702851729757 ) ) ;
#21446=CARTESIAN_POINT ( 'NONE',  ( 68.13393739769810509, 19.38381105532030091, -71.50000000000198952 ) ) ;
#21451=CARTESIAN_POINT ( 'NONE',  ( 13.61938558664210142, -51.42721352535720314, -23.00040036072969940 ) ) ;
#21452=AXIS2_PLACEMENT_3D ( 'NONE', #36819, #17178, #44950 ) ;
#21453=CARTESIAN_POINT ( 'NONE',  ( 56.20907041320840136, 19.47117149094080091, -75.13105742454641245 ) ) ;
#21454=CARTESIAN_POINT ( 'NONE',  ( 46.93943911961020632, -53.70440791814009884, -75.90649761523269490 ) ) ;
#21455=EDGE_LOOP ( 'NONE', ( #38411, #3935, #48100, #3338 ) ) ;
#21456=CARTESIAN_POINT ( 'NONE',  ( 56.28192814615630368, 14.29581962067599932, -17.93020402604240005 ) ) ;
#21457=CARTESIAN_POINT ( 'NONE',  ( 57.02861371931150103, -50.62805676436050106, -53.87746547617770432 ) ) ;
#21460=CARTESIAN_POINT ( 'NONE',  ( 61.28085239525059791, 14.36939662108470017, -47.67834120296360112 ) ) ;
#21462=ORIENTED_EDGE ( 'NONE', *, *, #18086, .F. ) ;
#21463=CARTESIAN_POINT ( 'NONE',  ( 47.28501908003789822, 23.16294876505000033, -75.17093853428211503 ) ) ;
#21471=DIRECTION ( 'NONE',  ( 1.000000000000000000, 0.000000000000000000, 0.000000000000000000 ) ) ;
#21473=CARTESIAN_POINT ( 'NONE',  ( 61.30125735803210318, 13.99008570081610081, -46.43541770244350175 ) ) ;
#21475=DIRECTION ( 'NONE',  ( 0.7800418122827239564, 0.000000000000000000, -0.6257273935913973961 ) ) ;
#21476=ORIENTED_EDGE ( 'NONE', *, *, #15076, .F. ) ;
#21477=CARTESIAN_POINT ( 'NONE',  ( 53.27424401219509775, -49.42912581425869689, -48.84492659952799443 ) ) ;
#21478=ORIENTED_EDGE ( 'NONE', *, *, #28410, .T. ) ;
#21479=CARTESIAN_POINT ( 'NONE',  ( 60.08384063771620021, -45.15096763946600333, -26.42493554971499847 ) ) ;
#21481=CARTESIAN_POINT ( 'NONE',  ( 13.34067846651199929, 19.89164641777950138, -21.90730044338819837 ) ) ;
#21484=CARTESIAN_POINT ( 'NONE',  ( 50.08385623533860098, 18.00127108905680018, -76.14999999999999147 ) ) ;
#21485=CARTESIAN_POINT ( 'NONE',  ( 53.48012894133849926, 18.14102095893770183, -49.05829627934659243 ) ) ;
#21487=CARTESIAN_POINT ( 'NONE',  ( 75.02961066429510595, -45.11618894467940066, -15.00607640852310176 ) ) ;
#21488=CIRCLE ( 'NONE', #46625, 17.70000000000000284 ) ;
#21492=CARTESIAN_POINT ( 'NONE',  ( 47.51346078803879891, -54.57248623694759715, -54.67578198258269850 ) ) ;
#21495=CARTESIAN_POINT ( 'NONE',  ( 11.19961949155312553, 34.01496270439587732, -18.17421237848505911 ) ) ;
#21499=DIRECTION ( 'NONE',  ( -1.000000000000000000, 0.000000000000000000, 0.000000000000000000 ) ) ;
#21503=CARTESIAN_POINT ( 'NONE',  ( 8.961073636172280032, -63.17872192377240026, -46.63307763104060655 ) ) ;
#21509=B_SPLINE_CURVE_WITH_KNOTS ( 'NONE', 3,
 ( #13724, #28906, #8492, #24698, #13215, #13471, #40453, #24439, #29426, #48588, #45433, #5602, #25485, #16873 ),
 .UNSPECIFIED., .F., .F.,
 ( 4, 2, 2, 2, 2, 2, 4 ),
 ( 0.000000000000000000, 0.07234295340347396408, 0.1754160052195452568, 0.3815621088516880088, 0.6397668613124120052, 0.9371651888848793188, 1.000000000000000000 ),
 .UNSPECIFIED. ) ;
#21511=CARTESIAN_POINT ( 'NONE',  ( 52.95141701711300186, 19.80221096257439939, -76.06582151403830494 ) ) ;
#21519=CARTESIAN_POINT ( 'NONE',  ( 16.13393739769620083, -15.61618894467929941, -6.649999999999999467 ) ) ;
#21521=ORIENTED_EDGE ( 'NONE', *, *, #51754, .F. ) ;
#21522=CARTESIAN_POINT ( 'NONE',  ( 18.45800985347563739, 20.88376505810182238, -75.46937998430171035 ) ) ;
#21527=CARTESIAN_POINT ( 'NONE',  ( 14.27557590264609999, 19.88380863237500051, -74.14994161014911356 ) ) ;
#21528=CARTESIAN_POINT ( 'NONE',  ( 17.68200514164429293, -51.79680896053663020, -75.65449996341281746 ) ) ;
#21529=CARTESIAN_POINT ( 'NONE',  ( 83.11128256222379207, -44.91457445506669899, -46.57919617705099569 ) ) ;
#21531=ORIENTED_EDGE ( 'NONE', *, *, #8220, .F. ) ;
#21532=CARTESIAN_POINT ( 'NONE',  ( 53.96734575795409938, -48.30637184247790117, -26.23153061636689998 ) ) ;
#21533=CARTESIAN_POINT ( 'NONE',  ( 53.62362271036269590, -51.33149816580809954, -75.58100470206619548 ) ) ;
#21534=CARTESIAN_POINT ( 'NONE',  ( 10.20255366368179928, 33.09845870078689956, -17.03222616606660011 ) ) ;
#21538=CARTESIAN_POINT ( 'NONE',  ( -10.88064226659390066, -42.34875619867930396, -6.242712440991480705 ) ) ;
#21539=CARTESIAN_POINT ( 'NONE',  ( 47.41229157644860237, 23.41797196667260295, -54.89345655439770155 ) ) ;
#21543=LINE ( 'NONE', #18657, #5603 ) ;
#21544=CARTESIAN_POINT ( 'NONE',  ( 42.26864913267620238, 13.12941410943280118, -5.126484833154619558 ) ) ;
#21546=CARTESIAN_POINT ( 'NONE',  ( 52.90855285609560354, 18.38725884964460278, -48.71990423803699599 ) ) ;
#21548=CARTESIAN_POINT ( 'NONE',  ( 59.53589770979640150, -46.29254236635570408, -47.84815983218079793 ) ) ;
#21551=CARTESIAN_POINT ( 'NONE',  ( 53.57016373187970260, 20.66090427507980110, -53.57659063368220131 ) ) ;
#21553=CARTESIAN_POINT ( 'NONE',  ( 11.96242383438930013, -65.43598681641390158, -17.67418089159339800 ) ) ;
#21554=CARTESIAN_POINT ( 'NONE',  ( 50.04794199403829680, 13.88381105532070059, -10.32001505436120148 ) ) ;
#21556=CARTESIAN_POINT ( 'NONE',  ( 19.90664092702385801, 23.53180147038325742, -18.14526676646603320 ) ) ;
#21557=CARTESIAN_POINT ( 'NONE',  ( 10.14348297095079943, 32.01596363797860079, -45.99327272258569366 ) ) ;
#21559=CARTESIAN_POINT ( 'NONE',  ( 66.36400972822720234, -30.63155050328590079, -16.96145626638979920 ) ) ;
#21562=ORIENTED_EDGE ( 'NONE', *, *, #2011, .F. ) ;
#21564=ADVANCED_FACE ( 'NONE', ( #18791 ), #8537, .T. ) ;
#21565=ORIENTED_EDGE ( 'NONE', *, *, #50756, .F. ) ;
#21566=CARTESIAN_POINT ( 'NONE',  ( 12.57686355069400008, -65.46300284260451008, -47.35844541283869802 ) ) ;
#21567=CARTESIAN_POINT ( 'NONE',  ( 56.46641740571360657, -46.20943712337750497, -26.25094501701900285 ) ) ;
#21568=DIRECTION ( 'NONE',  ( 0.9987374001630935361, 0.000000000000000000, -0.05023550054956103100 ) ) ;
#21569=CARTESIAN_POINT ( 'NONE',  ( 61.67741675730779605, 13.93672178322469968, -46.82959687277750049 ) ) ;
#21571=ORIENTED_EDGE ( 'NONE', *, *, #12004, .F. ) ;
#21573=B_SPLINE_SURFACE_WITH_KNOTS ( 'NONE', 3, 3, ( 
 ( #32438, #4954, #37186, #29306, #45308, #8630, #36646, #751 ),
 ( #9417, #16747, #48727, #12831, #20924, #34527, #38477, #50014 ),
 ( #21690, #9661, #46613, #5988, #10701, #17776, #42152, #6508 ),
 ( #6773, #26655, #2577, #37960, #30071, #18551, #9914, #49761 ),
 ( #49508, #50533, #34003, #2312, #30592, #13852, #30334, #2057 ),
 ( #10181, #29810, #45827, #6251, #33746, #10443, #13599, #46096 ),
 ( #25877, #1539, #42676, #25620, #41891, #17526, #22467, #22724 ),
 ( #21948, #33495, #29562, #45567, #41623, #5730, #14623, #26396 ),
 ( #37696, #42416, #18035, #1793, #14104, #18285, #26141, #22208 ) ),
 .UNSPECIFIED., .F., .F., .F.,
 ( 4, 1, 1, 1, 1, 1, 4 ),
 ( 4, 2, 2, 4 ),
 ( 0.000000000000000000, 0.1666666666666670182, 0.3333333333333329818, 0.5000000000000000000, 0.6666666666666670737, 0.8333333333333330373, 1.000009836239660110 ),
 ( -17.15520582519389947, -10.97516758816430027, -7.142721168756169803, -6.988377030140479285 ),
 .UNSPECIFIED. ) ;
#21575=CARTESIAN_POINT ( 'NONE',  ( 49.19893965675269953, -45.20300092367129707, -10.60212966286649916 ) ) ;
#21576=CARTESIAN_POINT ( 'NONE',  ( 16.13393739769620083, -15.61618894467929941, -15.65000000000000036 ) ) ;
#21579=CARTESIAN_POINT ( 'NONE',  ( 47.13216420861670031, -54.63565002646070212, -74.95072482230889932 ) ) ;
#21580=FACE_OUTER_BOUND ( 'NONE', #51252, .T. ) ;
#21581=CARTESIAN_POINT ( 'NONE',  ( 45.90332653426600018, 13.88381105525539994, -7.776724520636079774 ) ) ;
#21583=CARTESIAN_POINT ( 'NONE',  ( -9.882013117715120032, -40.49932216338130075, -21.14999999999999858 ) ) ;
#21585=CARTESIAN_POINT ( 'NONE',  ( 61.51097107413969667, 13.91173608902099978, -28.15130629814199992 ) ) ;
#21589=CARTESIAN_POINT ( 'NONE',  ( -9.818857736406330972, -43.25243607249999656, -5.498528025088970317 ) ) ;
#21590=CARTESIAN_POINT ( 'NONE',  ( 16.13393739769620083, -15.61618894467929941, 4.450000000000000178 ) ) ;
#21595=CARTESIAN_POINT ( 'NONE',  ( 13.75402769379030055, 19.05428965339309855, -20.97890654100300267 ) ) ;
#21597=CARTESIAN_POINT ( 'NONE',  ( 49.20592918829389362, -53.85531719945320361, -55.00566101661709695 ) ) ;
#21600=CARTESIAN_POINT ( 'NONE',  ( 18.50686185362269853, -51.29510989453680736, -74.37030622952239867 ) ) ;
#21605=ORIENTED_EDGE ( 'NONE', *, *, #41504, .T. ) ;
#21607=CARTESIAN_POINT ( 'NONE',  ( 60.95561879329019916, -45.63102361682189922, -47.66564892484940685 ) ) ;
#21612=CARTESIAN_POINT ( 'NONE',  ( 53.29384558423090112, -50.54670888882439783, -38.31189016485959797 ) ) ;
#21613=CARTESIAN_POINT ( 'NONE',  ( 42.67454888401100277, -45.92793478434160193, -7.343008119757059582 ) ) ;
#21617=EDGE_CURVE ( 'NONE', #17172, #50841, #29130, .T. ) ;
#21618=VERTEX_POINT ( 'NONE', #7268 ) ;
#21619=CARTESIAN_POINT ( 'NONE',  ( 61.22099285190670059, -45.29906686168950358, -47.03247545010540165 ) ) ;
#21620=CARTESIAN_POINT ( 'NONE',  ( 52.88322703206500108, -49.67375961844999921, -49.00539243417760105 ) ) ;
#21622=CARTESIAN_POINT ( 'NONE',  ( 56.36239273759079538, -50.53819555927099572, -52.86232647623099723 ) ) ;
#21623=EDGE_CURVE ( 'NONE', #46423, #47971, #37840, .T. ) ;
#21624=ORIENTED_EDGE ( 'NONE', *, *, #35597, .T. ) ;
#21626=ORIENTED_EDGE ( 'NONE', *, *, #2098, .T. ) ;
#21627=CARTESIAN_POINT ( 'NONE',  ( 56.27102381480889903, -50.57721995146319927, -52.87265154067429762 ) ) ;
#21629=DIRECTION ( 'NONE',  ( 0.000000000000000000, 1.000000000000000000, 0.000000000000000000 ) ) ;
#21630=VERTEX_POINT ( 'NONE', #3335 ) ;
#21632=CARTESIAN_POINT ( 'NONE',  ( 52.00136175985360154, -50.03231718876410383, -76.70561731964021135 ) ) ;
#21637=CARTESIAN_POINT ( 'NONE',  ( 41.94961043596779149, 13.67826027404730027, -5.752299076171500047 ) ) ;
#21639=CARTESIAN_POINT ( 'NONE',  ( 41.87524915382199708, -44.35687246895969338, -5.012953300357450459 ) ) ;
#21640=CARTESIAN_POINT ( 'NONE',  ( 68.13393739769847457, -50.70395984888145335, -72.15645085170113759 ) ) ;
#21641=CARTESIAN_POINT ( 'NONE',  ( -10.41557261171689852, 11.58869671994870032, -6.169019698314530231 ) ) ;
#21642=CIRCLE ( 'NONE', #9955, 1.000000000000000888 ) ;
#21646=VECTOR ( 'NONE', #6503, 1000.000000000000114 ) ;
#21647=CARTESIAN_POINT ( 'NONE',  ( 66.72606221067250942, 1.883603582144870003, -20.65075287695389861 ) ) ;
#21648=EDGE_LOOP ( 'NONE', ( #1682, #11417, #32111, #3682, #42332 ) ) ;
#21649=CARTESIAN_POINT ( 'NONE',  ( 14.16789401284239958, -52.35976395901120384, -75.83262351151699932 ) ) ;
#21650=CARTESIAN_POINT ( 'NONE',  ( 57.27629353325620087, 19.36113991157819925, -53.60235154930700219 ) ) ;
#21653=( BOUNDED_CURVE ( )  B_SPLINE_CURVE ( 3, ( #49457, #5938, #17725, #700 ),
 .UNSPECIFIED., .F., .T. ) 
 B_SPLINE_CURVE_WITH_KNOTS ( ( 4, 4 ),
 ( 4.712388980384691450, 5.229612381435808643 ),
 .UNSPECIFIED. ) 
 CURVE ( )  GEOMETRIC_REPRESENTATION_ITEM ( )  RATIONAL_B_SPLINE_CURVE ( ( 1.000000000000000000, 0.9778306343446301341, 0.9778306343446301341, 1.000000000000000000 ) ) 
 REPRESENTATION_ITEM ( '' )  );
#21656=CARTESIAN_POINT ( 'NONE',  ( 47.64964229006469765, -54.53139074986410151, -55.13082436213850457 ) ) ;
#21659=CARTESIAN_POINT ( 'NONE',  ( 48.02726464836110409, 23.08853929931079918, -54.84894742480889818 ) ) ;
#21665=CARTESIAN_POINT ( 'NONE',  ( 58.88698566692261238, -48.67252618344199533, -51.02964062410481461 ) ) ;
#21666=CARTESIAN_POINT ( 'NONE',  ( 74.17629866868290378, 1.883811055320649963, -65.34607522167520699 ) ) ;
#21667=CARTESIAN_POINT ( 'NONE',  ( 84.02215818083939780, 13.18587566258590016, -47.25304732090640414 ) ) ;
#21668=CARTESIAN_POINT ( 'NONE',  ( 53.73390105979990494, 17.34280763946619786, -26.38585243011049997 ) ) ;
#21670=CARTESIAN_POINT ( 'NONE',  ( 10.85466640524320070, 33.73459223951330443, -17.55961383757199812 ) ) ;
#21671=CARTESIAN_POINT ( 'NONE',  ( 55.94725819174559689, -45.11618894467940066, -14.63509477631759914 ) ) ;
#21676=CARTESIAN_POINT ( 'NONE',  ( 11.98493272671300147, -65.14404999958080111, -16.63579482025560097 ) ) ;
#21677=CARTESIAN_POINT ( 'NONE',  ( 11.83192124503869991, 33.83054603674280969, -45.91061019192989789 ) ) ;
#21678=CARTESIAN_POINT ( 'NONE',  ( 12.06284766121009966, -63.44323389162830296, -22.25048313876769868 ) ) ;
#21681=CARTESIAN_POINT ( 'NONE',  ( 13.00893739761190027, 34.28605925116320208, -47.75434321210310173 ) ) ;
#21686=EDGE_CURVE ( 'NONE', #23531, #30985, #45396, .T. ) ;
#21688=CARTESIAN_POINT ( 'NONE',  ( 52.82975622904280755, 18.42854261028849905, -28.15000000000000213 ) ) ;
#21689=AXIS2_PLACEMENT_3D ( 'NONE', #16140, #32100, #36304 ) ;
#21690=CARTESIAN_POINT ( 'NONE',  ( 47.83902694909610176, 23.41449876227819971, -55.43872205723609881 ) ) ;
#21691=CARTESIAN_POINT ( 'NONE',  ( 61.12640465316060556, -1.652607533939269846, -15.96805516186100249 ) ) ;
#21692=CARTESIAN_POINT ( 'NONE',  ( 50.65222755239680197, -50.00564526808049948, -76.16386725643910438 ) ) ;
#21693=CARTESIAN_POINT ( 'NONE',  ( 60.29219879490389644, -46.03903543506309859, -47.96865620826579857 ) ) ;
#21696=CARTESIAN_POINT ( 'NONE',  ( 70.03247032090600044, 18.72622661238320063, -71.50000000000139266 ) ) ;
#21697=ORIENTED_EDGE ( 'NONE', *, *, #42017, .T. ) ;
#21701=CARTESIAN_POINT ( 'NONE',  ( 14.01766645441900039, -51.16976191506400085, -22.72052346470150397 ) ) ;
#21702=CARTESIAN_POINT ( 'NONE',  ( 56.31570272895609719, 19.43228892330789748, -75.23156124386549948 ) ) ;
#21703=CARTESIAN_POINT ( 'NONE',  ( 47.54867620891420188, -54.45453621600920258, -74.81076251056920512 ) ) ;
#21704=ORIENTED_EDGE ( 'NONE', *, *, #32926, .T. ) ;
#21705=CARTESIAN_POINT ( 'NONE',  ( 55.35087876542500140, 14.59724106507499997, -16.24598606757869845 ) ) ;
#21707=CARTESIAN_POINT ( 'NONE',  ( 57.18371625252699175, -50.61638664230610374, -53.90359199148200275 ) ) ;
#21708=CARTESIAN_POINT ( 'NONE',  ( 52.77321279212640093, -49.72572936949169531, -48.90236189552150137 ) ) ;
#21711=CARTESIAN_POINT ( 'NONE',  ( 46.95048156581290044, 22.62954421289450124, -75.82172624862269572 ) ) ;
#21714=CARTESIAN_POINT ( 'NONE',  ( 61.09252571675981613, -45.64957244923583346, -47.71760867771691750 ) ) ;
#21716=AXIS2_PLACEMENT_3D ( 'NONE', #40478, #4569, #15860 ) ;
#21719=EDGE_CURVE ( 'NONE', #14040, #17592, #11467, .T. ) ;
#21720=CIRCLE ( 'NONE', #41790, 0.9999999999999991118 ) ;
#21728=CARTESIAN_POINT ( 'NONE',  ( 61.25107916413389830, 14.01637543934619856, -46.61539294923009891 ) ) ;
#21729=CARTESIAN_POINT ( 'NONE',  ( -12.78066350546449925, 25.79908749870000051, -53.01233286176530157 ) ) ;
#21730=ADVANCED_FACE ( 'NONE', ( #944 ), #13272, .T. ) ;
#21731=EDGE_LOOP ( 'NONE', ( #12930, #48854, #50171, #2116 ) ) ;
#21732=CARTESIAN_POINT ( 'NONE',  ( 53.04305187236489871, -49.55227711057870010, -48.87083722906180583 ) ) ;
#21733=EDGE_LOOP ( 'NONE', ( #41093, #28191, #12712, #15085 ) ) ;
#21735=CARTESIAN_POINT ( 'NONE',  ( 50.03007040746459921, -32.48240620400619605, -78.14999999999999147 ) ) ;
#21736=CARTESIAN_POINT ( 'NONE',  ( 57.50545812844309523, 13.88245804299080000, -25.40235374574200122 ) ) ;
#21739=CARTESIAN_POINT ( 'NONE',  ( 52.71233980931599916, 18.50598591079160116, -48.66394846760560000 ) ) ;
#21742=CARTESIAN_POINT ( 'NONE',  ( 16.19514082297589042, 19.83054448556217153, -15.66998203262581413 ) ) ;
#21746=CARTESIAN_POINT ( 'NONE',  ( 47.49893771375030127, -54.58694222780890470, -54.71508793643310042 ) ) ;
#21749=CARTESIAN_POINT ( 'NONE',  ( 11.80006687032470047, -65.42818578075079472, -17.88619248980069898 ) ) ;
#21752=CARTESIAN_POINT ( 'NONE',  ( 61.28610861176739633, -45.23040055550220018, -46.37203261889099792 ) ) ;
#21758=CARTESIAN_POINT ( 'NONE',  ( 8.786694880862668811, -63.12535539208791135, -46.67160944818530766 ) ) ;
#21759=DIRECTION ( 'NONE',  ( 0.000000000000000000, 0.000000000000000000, 1.000000000000000000 ) ) ;
#21761=CARTESIAN_POINT ( 'NONE',  ( 66.72561048563099462, 1.883811055320649963, -20.64999999980150136 ) ) ;
#21764=CARTESIAN_POINT ( 'NONE',  ( 51.62681371164700295, 19.13241760220180154, -76.35210453837470368 ) ) ;
#21765=AXIS2_PLACEMENT_3D ( 'NONE', #29937, #34647, #5605 ) ;
#21767=DIRECTION ( 'NONE',  ( -0.04251717301921600217, 0.000000000000000000, 0.9990957361526742186 ) ) ;
#21768=AXIS2_PLACEMENT_3D ( 'NONE', #21612, #33674, #2243 ) ;
#21772=AXIS2_PLACEMENT_3D ( 'NONE', #47204, #19138, #50862 ) ;
#21773=B_SPLINE_SURFACE_WITH_KNOTS ( 'NONE', 3, 3, ( 
 ( #8429, #15263, #31219, #4747, #40649, #48515, #20714, #24636, #12620, #28580, #549, #8684, #44580, #16535, #32487, #6679 ),
 ( #31017, #29977, #22639, #6942, #15050, #3001, #10088, #18972, #26047, #34952, #26569, #34435, #50445, #7193, #14532, #30760 ),
 ( #46000, #34166, #50952, #46265, #38657, #11129, #47042, #42058, #19235, #42322, #26836, #27097, #38911, #38384, #46782, #43101 ),
 ( #23148, #46525, #42583, #18201, #6159, #39165, #2479, #3258, #14279, #2745, #49927, #22117, #14017, #38127, #2224, #30244 ),
 ( #50185, #6421, #10351, #26310, #22379, #18462, #30502, #10614, #18716, #34693, #14792, #50695, #10871, #42845, #22894, #43863 ),
 ( #15314, #19749, #24425, #40189, #27608, #31266, #7450, #349, #43613, #36241, #48058, #40439, #51220, #19493, #44120, #35217 ),
 ( #39935, #31784, #3781, #16077, #19992, #43357, #7716, #51474, #47801, #7961, #47299, #11643, #32035, #4531, #12405, #48310 ),
 ( #4279, #11389, #20249, #11907, #35742, #51725, #44377, #15819, #12158, #3523, #27351, #35483, #16335, #31529, #23910, #28369 ),
 ( #23401, #39423, #23661, #28113, #8479, #24165, #39675, #8219, #32288, #15573, #47547, #27863, #4032, #35989, #105, #13711 ),
 ( #29665, #36754, #9266, #25469, #600, #25727, #45673, #41474, #866, #5072, #21544, #28892, #16858, #9776, #41735, #8735 ) ),
 .UNSPECIFIED., .F., .F., .F.,
 ( 4, 1, 1, 1, 1, 1, 1, 4 ),
 ( 4, 2, 2, 2, 2, 2, 2, 4 ),
 ( 0.000000000000000000, 0.1428571428571430157, 0.2857142857142860315, 0.4285714285714289917, 0.5714285714285709528, 0.7142857142857139685, 0.8571428571428569843, 1.000000000000000000 ),
 ( -5.401102999999999791E-13, 0.6760851027942610392, 1.448753791702609872, 1.931671722270319913, 2.173130687554179818, 2.549919136921820151, 3.152780655910059959, 3.863343444541179839 ),
 .UNSPECIFIED. ) ;
#21776=DIRECTION ( 'NONE',  ( 0.000000000000000000, 0.000000000000000000, -1.000000000000000000 ) ) ;
#21779=CARTESIAN_POINT ( 'NONE',  ( 57.18457261690709714, -45.84679711968900051, -26.25601685834770294 ) ) ;
#21781=CARTESIAN_POINT ( 'NONE',  ( 52.70698372528340059, -49.76075902929100181, -48.81385732385550114 ) ) ;
#21783=CARTESIAN_POINT ( 'NONE',  ( 14.28635823141850203, 19.91124285304359987, -74.53071772762450564 ) ) ;
#21786=CARTESIAN_POINT ( 'NONE',  ( 42.17659605538639056, -45.13706293947769410, -6.213788242717720678 ) ) ;
#21787=DIRECTION ( 'NONE',  ( 1.000000000000000000, 0.000000000000000000, 0.000000000000000000 ) ) ;
#21789=ORIENTED_EDGE ( 'NONE', *, *, #49162, .T. ) ;
#21790=CARTESIAN_POINT ( 'NONE',  ( 53.13843262439830539, -49.24770168678169568, -27.00111715391960132 ) ) ;
#21792=CARTESIAN_POINT ( 'NONE',  ( 16.48362619534269768, -51.11256221897610175, -20.43421124880940098 ) ) ;
#21793=CARTESIAN_POINT ( 'NONE',  ( 11.78901682358320002, 33.45032075383200265, -15.99444886826960044 ) ) ;
#21796=CARTESIAN_POINT ( 'NONE',  ( 51.96927444999568735, 19.26340285573088806, -49.26020569436006014 ) ) ;
#21797=EDGE_CURVE ( 'NONE', #9344, #1848, #48651, .T. ) ;
#21799=EDGE_LOOP ( 'NONE', ( #34713, #9483, #9015, #5242, #32636 ) ) ;
#21800=CARTESIAN_POINT ( 'NONE',  ( -9.512669577913570151, -43.68334388704730031, -5.840848558116729983 ) ) ;
#21801=VECTOR ( 'NONE', #50592, 1000.000000000000000 ) ;
#21802=CARTESIAN_POINT ( 'NONE',  ( 47.50259510985190303, 23.34628208298549978, -54.66723688595389774 ) ) ;
#21804=CARTESIAN_POINT ( 'NONE',  ( 60.70258575398039369, 14.30887124488140039, -47.21990423911680068 ) ) ;
#21806=CARTESIAN_POINT ( 'NONE',  ( 12.05299951489699950, 34.04022587130140209, -16.91217736884900091 ) ) ;
#21807=CARTESIAN_POINT ( 'NONE',  ( 11.13393739768609869, -63.11566452787130288, -48.70428853817739423 ) ) ;
#21810=CARTESIAN_POINT ( 'NONE',  ( 57.81731062816049871, -47.19213156486770089, -48.15547591032719765 ) ) ;
#21811=CARTESIAN_POINT ( 'NONE',  ( 11.12718406860063958, 33.98029382107211660, -18.17421237808490631 ) ) ;
#21812=CARTESIAN_POINT ( 'NONE',  ( 52.84479356091129887, 20.96976391392999872, -53.70842335541510693 ) ) ;
#21814=DIRECTION ( 'NONE',  ( 0.000000000000000000, 1.000000000000000000, 0.000000000000000000 ) ) ;
#21817=CARTESIAN_POINT ( 'NONE',  ( 11.10549763774450049, 32.03550487100480382, -44.25138291837249227 ) ) ;
#21819=CARTESIAN_POINT ( 'NONE',  ( 65.14565750857379101, -32.19410384129359670, -17.75424278862539751 ) ) ;
#21823=VERTEX_POINT ( 'NONE', #36064 ) ;
#21824=ORIENTED_EDGE ( 'NONE', *, *, #21686, .T. ) ;
#21825=CARTESIAN_POINT ( 'NONE',  ( 52.82975622904280755, -49.66092049964720445, -28.15000000000000213 ) ) ;
#21827=CARTESIAN_POINT ( 'NONE',  ( 76.44385176486125033, -6.812219962908470983, -12.98546713699449384 ) ) ;
#21828=ORIENTED_EDGE ( 'NONE', *, *, #31597, .T. ) ;
#21829=CARTESIAN_POINT ( 'NONE',  ( 56.35466018300130031, -46.14412721853660315, -26.19499711794230024 ) ) ;
#21830=CARTESIAN_POINT ( 'NONE',  ( 14.34417029198830029, 17.88381105532299742, -22.49240188329279988 ) ) ;
#21833=ORIENTED_EDGE ( 'NONE', *, *, #20677, .T. ) ;
#21835=VERTEX_POINT ( 'NONE', #20071 ) ;
#21836=CARTESIAN_POINT ( 'NONE',  ( 45.31002603524360239, -45.55094031840040003, -8.676032240096109405 ) ) ;
#21838=CARTESIAN_POINT ( 'NONE',  ( 16.60579442219519919, 19.88381273878740174, -20.30246704093620025 ) ) ;
#21839=CARTESIAN_POINT ( 'NONE',  ( 85.84022851002180232, -48.61618894467930119, -53.47585302082339354 ) ) ;
#21840=VECTOR ( 'NONE', #25596, 1000.000000000000000 ) ;
#21841=ORIENTED_EDGE ( 'NONE', *, *, #38165, .T. ) ;
#21843=CARTESIAN_POINT ( 'NONE',  ( 46.94043888554279675, -54.13312419596409342, -75.65761316843601492 ) ) ;
#21845=CARTESIAN_POINT ( 'NONE',  ( 58.23988399474049515, 12.21801982902359995, -8.616684570808338606 ) ) ;
#21847=CARTESIAN_POINT ( 'NONE',  ( 50.29495137051839748, -49.91812883465070172, -76.14999999999999147 ) ) ;
#21848=CARTESIAN_POINT ( 'NONE',  ( 52.73680207265829978, 20.85125113597840141, -53.40499982253649591 ) ) ;
#21849=CARTESIAN_POINT ( 'NONE',  ( 52.71259303052620027, 20.20049112655190271, -75.79898569453669666 ) ) ;
#21850=CARTESIAN_POINT ( 'NONE',  ( 60.33389456548449914, 13.95383495194499979, -26.69150274143580148 ) ) ;
#21853=DIRECTION ( 'NONE',  ( 0.000000000000000000, 1.000000000000000000, 0.000000000000000000 ) ) ;
#21855=CARTESIAN_POINT ( 'NONE',  ( -11.21045583712350080, -42.00392984997720447, -6.268887757048219989 ) ) ;
#21859=CARTESIAN_POINT ( 'NONE',  ( 38.10178428107396797, -15.61618894467929941, 5.729250452415290518 ) ) ;
#21860=CARTESIAN_POINT ( 'NONE',  ( 12.53340213339009956, 19.11463212377349663, -21.18850784640499896 ) ) ;
#21864=CARTESIAN_POINT ( 'NONE',  ( 59.13340102237120277, -28.11618894467929763, -15.65754737356207116 ) ) ;
#21865=CARTESIAN_POINT ( 'NONE',  ( 75.73925199613023551, -43.35112943081499282, -13.49699557879452172 ) ) ;
#21866=B_SPLINE_CURVE_WITH_KNOTS ( 'NONE', 3,
 ( #24806, #5192, #1248, #49216, #17236, #20366, #16451, #40817, #5446, #4918 ),
 .UNSPECIFIED., .F., .F.,
 ( 4, 2, 2, 2, 4 ),
 ( 0.4459052190640770963, 0.5000000000194557703, 0.6250000000145918833, 0.8250000000068096195, 1.000000000000000000 ),
 .UNSPECIFIED. ) ;
#21867=CARTESIAN_POINT ( 'NONE',  ( 57.50723796702470025, 13.88381105532070059, -17.93019253464870033 ) ) ;
#21871=EDGE_LOOP ( 'NONE', ( #40013, #21153, #28804, #17977 ) ) ;
#21874=CARTESIAN_POINT ( 'NONE',  ( 61.07186058100219839, -45.48678447307229789, -47.46853448916699847 ) ) ;
#21875=LINE ( 'NONE', #46279, #19527 ) ;
#21879=AXIS2_PLACEMENT_3D ( 'NONE', #36328, #48400, #12767 ) ;
#21881=DIRECTION ( 'NONE',  ( 0.000000000000000000, 1.000000000000000000, 0.000000000000000000 ) ) ;
#21882=EDGE_LOOP ( 'NONE', ( #38159, #29625 ) ) ;
#21883=ORIENTED_EDGE ( 'NONE', *, *, #32834, .F. ) ;
#21884=EDGE_CURVE ( 'NONE', #30791, #22140, #36839, .T. ) ;
#21885=ORIENTED_EDGE ( 'NONE', *, *, #43594, .T. ) ;
#21886=CARTESIAN_POINT ( 'NONE',  ( 61.32609621975529990, -45.21089685825819515, -46.52851239421509888 ) ) ;
#21887=CARTESIAN_POINT ( 'NONE',  ( 61.23063308864373511, 14.32779774614108703, -47.62819202780649164 ) ) ;
#21894=CARTESIAN_POINT ( 'NONE',  ( 1.027904703268269992, 11.45423359053189927, -15.65000000000000036 ) ) ;
#21895=CARTESIAN_POINT ( 'NONE',  ( 53.91131433518199856, -50.74962858781439934, -76.32773059544709326 ) ) ;
#21896=CARTESIAN_POINT ( 'NONE',  ( 60.91431180673369994, 14.19281742933669932, -47.01365133320219769 ) ) ;
#21899=CARTESIAN_POINT ( 'NONE',  ( 41.84489819291530210, 13.62916984612999904, -5.635697468575719959 ) ) ;
#21900=CARTESIAN_POINT ( 'NONE',  ( 41.67343713632900659, -43.97793718056139767, -4.319880517921928842 ) ) ;
#21902=DIRECTION ( 'NONE',  ( 1.000000000000000000, 0.000000000000000000, 0.000000000000000000 ) ) ;
#21906=CARTESIAN_POINT ( 'NONE',  ( 68.11939347576729631, -0.4694106769779339827, -18.02961996124970057 ) ) ;
#21907=ORIENTED_EDGE ( 'NONE', *, *, #48025, .T. ) ;
#21908=CARTESIAN_POINT ( 'NONE',  ( 14.74433690757950011, -52.44145270522060542, -76.03823174343609992 ) ) ;
#21910=CARTESIAN_POINT ( 'NONE',  ( 57.26283653205659618, 19.37968206195550280, -53.75815473100109898 ) ) ;
#21914=ADVANCED_FACE ( 'NONE', ( #26330 ), #13594, .F. ) ;
#21918=CARTESIAN_POINT ( 'NONE',  ( 47.81682817682920472, -54.40980482828490494, -54.77348380241939907 ) ) ;
#21920=CARTESIAN_POINT ( 'NONE',  ( -6.924872749483005130, -45.82389030669077812, -4.775471302137791696 ) ) ;
#21921=CARTESIAN_POINT ( 'NONE',  ( 48.25899205962569738, 22.95127335475299901, -54.74446225849390402 ) ) ;
#21928=CARTESIAN_POINT ( 'NONE',  ( 84.28893459517129827, 12.67753174781119974, -47.31525200062240089 ) ) ;
#21931=PLANE ( 'NONE',  #10447 ) ;
#21932=CARTESIAN_POINT ( 'NONE',  ( 57.21870030722980260, -45.11618894467940066, -16.66793634595250140 ) ) ;
#21933=CARTESIAN_POINT ( 'NONE',  ( 55.91595722987329964, -45.90465052577939531, -25.32543029193989881 ) ) ;
#21934=CARTESIAN_POINT ( 'NONE',  ( 52.10267382257649871, -33.11618894464340457, -77.60820171200670359 ) ) ;
#21935=EDGE_LOOP ( 'NONE', ( #11516, #48271, #2763, #4679, #2097 ) ) ;
#21936=ADVANCED_FACE ( 'NONE', ( #9592 ), #30263, .F. ) ;
#21937=ORIENTED_EDGE ( 'NONE', *, *, #33117, .F. ) ;
#21938=CARTESIAN_POINT ( 'NONE',  ( 12.23212070001810048, -64.70875017051861278, -15.94047990890019939 ) ) ;
#21941=CARTESIAN_POINT ( 'NONE',  ( 51.05234094794748501, 3.895276377383162014, -76.43087611100055767 ) ) ;
#21942=AXIS2_PLACEMENT_3D ( 'NONE', #1548, #17536, #49004 ) ;
#21946=B_SPLINE_CURVE_WITH_KNOTS ( 'NONE', 3,
 ( #34418, #14777, #1687, #9816, #10335, #25771, #41778, #5879, #21848, #50428, #45980, #37854, #1949, #30486, #46509, #42568 ),
 .UNSPECIFIED., .F., .F.,
 ( 4, 2, 2, 2, 2, 2, 2, 4 ),
 ( 0.1347299975730832100, 1.477915555902800104, 2.688805424479379980, 3.445611592339730134, 3.918615447252459916, 4.864623157077900828, 6.378235492798619788, 7.568061678603579701 ),
 .UNSPECIFIED. ) ;
#21948=CARTESIAN_POINT ( 'NONE',  ( 47.21678712416260026, 23.54835302331790103, -54.66856283150690388 ) ) ;
#21949=CARTESIAN_POINT ( 'NONE',  ( 62.27287536084629949, -1.795422579115219852, -16.09831546515840017 ) ) ;
#21950=B_SPLINE_CURVE_WITH_KNOTS ( 'NONE', 3,
 ( #4904, #24532, #20102, #706, #12515, #28481, #36093, #4637, #199, #16178, #32136, #48153, #40548 ),
 .UNSPECIFIED., .F., .F.,
 ( 4, 2, 2, 1, 2, 2, 4 ),
 ( 0.000000000000000000, 0.2500000000000104916, 0.3750000000000195399, 0.4375000000000275890, 0.4687500000000315858, 0.5000000000000356382, 1.000000000000000000 ),
 .UNSPECIFIED. ) ;
#21951=CARTESIAN_POINT ( 'NONE',  ( 51.79789283343050244, -50.16750000966669631, -76.50613280422149387 ) ) ;
#21953=CARTESIAN_POINT ( 'NONE',  ( 56.67707220608559737, -50.45813178979619806, -52.89887292284029741 ) ) ;
#21954=ORIENTED_EDGE ( 'NONE', *, *, #24917, .T. ) ;
#21956=CARTESIAN_POINT ( 'NONE',  ( 68.13393739769810509, 19.38381105532030091, -71.50000000000198952 ) ) ;
#21960=ADVANCED_FACE ( 'NONE', ( #17707 ), #33675, .F. ) ;
#21962=CARTESIAN_POINT ( 'NONE',  ( 13.40141241860720100, -50.83865301178659735, -21.60243653193219870 ) ) ;
#21963=CARTESIAN_POINT ( 'NONE',  ( 57.01977359311290172, 19.39593467336339927, -74.37787343998699896 ) ) ;
#21964=CARTESIAN_POINT ( 'NONE',  ( 47.64115383555780170, -54.53453007470059788, -74.19838441418400521 ) ) ;
#21965=ORIENTED_EDGE ( 'NONE', *, *, #20022, .T. ) ;
#21966=CARTESIAN_POINT ( 'NONE',  ( 55.69313694499650325, 14.20859937458799926, -15.97679700106960077 ) ) ;
#21967=CARTESIAN_POINT ( 'NONE',  ( 11.10574934303680017, 32.24869790884810072, -44.26157399421149563 ) ) ;
#21969=FACE_OUTER_BOUND ( 'NONE', #48606, .T. ) ;
#21973=CARTESIAN_POINT ( 'NONE',  ( 47.46041225084670145, 23.10728982931480147, -75.12131124014999273 ) ) ;
#21975=CARTESIAN_POINT ( 'NONE',  ( 75.27017760932777435, -35.23061375743377965, -12.38324198906882145 ) ) ;
#21976=CARTESIAN_POINT ( 'NONE',  ( 12.94686910253266809, -65.51455027584026425, -23.34704060099317502 ) ) ;
#21978=DIRECTION ( 'NONE',  ( 0.9200120562340469155, 0.3918900565005459247, 8.326672684688669123E-17 ) ) ;
#21979=CARTESIAN_POINT ( 'NONE',  ( 68.13393739769620083, -48.61618894467930119, -65.65000000000000568 ) ) ;
#21980=EDGE_CURVE ( 'NONE', #45554, #25535, #26715, .T. ) ;
#21983=CARTESIAN_POINT ( 'NONE',  ( 45.07858682377059978, 14.88010818488339915, -9.026855431852879974 ) ) ;
#21985=CARTESIAN_POINT ( 'NONE',  ( 61.21318727958689720, 14.03622819520689902, -46.64662901492760483 ) ) ;
#21987=CARTESIAN_POINT ( 'NONE',  ( -0.3068767133109390199, 32.08499073367880783, -50.59628790670770115 ) ) ;
#21989=CARTESIAN_POINT ( 'NONE',  ( 53.03884173268740199, -49.55871672378989956, -48.90887834982989801 ) ) ;
#21992=CARTESIAN_POINT ( 'NONE',  ( 83.89200044194980421, 17.38381105532069881, -53.92796738110899923 ) ) ;
#21993=CARTESIAN_POINT ( 'NONE',  ( 56.25705355070190450, 14.33441359163029993, -25.50876077399200170 ) ) ;
#21996=CARTESIAN_POINT ( 'NONE',  ( 52.69140883990100122, 18.51580850568210224, -48.48983502735960371 ) ) ;
#21997=DIRECTION ( 'NONE',  ( -1.000000000000000000, 0.000000000000000000, 0.000000000000000000 ) ) ;
#21999=DIRECTION ( 'NONE',  ( 0.3569024281753415129, 0.000000000000000000, 0.9341416684649846980 ) ) ;
#22001=ORIENTED_EDGE ( 'NONE', *, *, #5990, .T. ) ;
#22004=CARTESIAN_POINT ( 'NONE',  ( 56.68070624494579590, 16.55316904772309883, -48.38861384420910383 ) ) ;
#22005=FACE_BOUND ( 'NONE', #21882, .T. ) ;
#22007=CARTESIAN_POINT ( 'NONE',  ( 11.06596496313670031, -65.18630305408680670, -17.90443099707960073 ) ) ;
#22008=CARTESIAN_POINT ( 'NONE',  ( 52.89416328055860106, 18.39479795143689955, -48.70339646180270421 ) ) ;
#22014=CARTESIAN_POINT ( 'NONE',  ( 8.953416032341278807, -63.13563415162649761, -46.63440066212280044 ) ) ;
#22015=CARTESIAN_POINT ( 'NONE',  ( 52.11631747943250303, 21.39637954122449770, -46.39999999999999858 ) ) ;
#22018=CARTESIAN_POINT ( 'NONE',  ( 57.20288281111999851, 18.94155152855249824, -52.64687565416169690 ) ) ;
#22020=CARTESIAN_POINT ( 'NONE',  ( 53.57534982089429576, 19.31353316830639955, -77.11818283286250164 ) ) ;
#22022=VERTEX_POINT ( 'NONE', #38145 ) ;
#22024=CARTESIAN_POINT ( 'NONE',  ( 10.52748815138901328, -64.93771388208423900, -47.11278009429390323 ) ) ;
#22029=EDGE_CURVE ( 'NONE', #36517, #42919, #39519, .T. ) ;
#22030=DIRECTION ( 'NONE',  ( 0.000000000000000000, 0.000000000000000000, -1.000000000000000000 ) ) ;
#22034=CARTESIAN_POINT ( 'NONE',  ( 56.77510575719860242, -46.03395327836230422, -26.24796325860310020 ) ) ;
#22037=CARTESIAN_POINT ( 'NONE',  ( 13.85739208368369901, 20.19843276291189937, -74.93307507168100301 ) ) ;
#22039=ADVANCED_FACE ( 'NONE', ( #18219 ), #20910, .T. ) ;
#22042=ADVANCED_FACE ( 'NONE', ( #19461 ), #10840, .F. ) ;
#22043=VERTEX_POINT ( 'NONE', #34662 ) ;
#22044=CARTESIAN_POINT ( 'NONE',  ( 53.45178337541119618, -48.93644626688359978, -26.86578694399930001 ) ) ;
#22045=CARTESIAN_POINT ( 'NONE',  ( 54.04287499173630493, -51.09449692274579746, -75.65863628419570830 ) ) ;
#22046=CARTESIAN_POINT ( 'NONE',  ( 12.12058638835210012, 33.31847000525309710, -15.78474273040839826 ) ) ;
#22049=CARTESIAN_POINT ( 'NONE',  ( 13.19564766795559940, 10.36739510386719942, -74.14999999999999147 ) ) ;
#22051=ORIENTED_EDGE ( 'NONE', *, *, #6269, .F. ) ;
#22052=CARTESIAN_POINT ( 'NONE',  ( -2.629620173063649702, -48.67441424446350595, -4.565428259182719550 ) ) ;
#22054=CARTESIAN_POINT ( 'NONE',  ( 47.57599655811520023, 23.29777716724849768, -54.66624935529340235 ) ) ;
#22057=CARTESIAN_POINT ( 'NONE',  ( 13.13594234983320064, 19.37673283217589670, -21.36925545734460030 ) ) ;
#22058=CARTESIAN_POINT ( 'NONE',  ( 56.79283174838518278, 14.01333454635517484, -25.29533692629807362 ) ) ;
#22059=CARTESIAN_POINT ( 'NONE',  ( 11.94685995288999969, 34.08567592416299874, -17.08231285071160244 ) ) ;
#22060=CARTESIAN_POINT ( 'NONE',  ( 52.26505149639940129, 18.55116626494530152, -77.19463936772390866 ) ) ;
#22063=CARTESIAN_POINT ( 'NONE',  ( 53.59226879027059454, -49.40789622861730379, -49.22934975137650326 ) ) ;
#22064=CARTESIAN_POINT ( 'NONE',  ( 54.49383788419760322, 16.89893908078170170, -26.73738845760439986 ) ) ;
#22065=CARTESIAN_POINT ( 'NONE',  ( 55.56556980353779807, 19.70710272740160107, -53.05958889729620154 ) ) ;
#22066=APPLICATION_CONTEXT ( 'automotive_design' ) ;
#22068=CYLINDRICAL_SURFACE ( 'NONE', #42859, 2.000000000000000888 ) ;
#22070=CARTESIAN_POINT ( 'NONE',  ( 19.44385660017238138, 22.20530810434653546, -16.61545052194239247 ) ) ;
#22071=CARTESIAN_POINT ( 'NONE',  ( 10.97782414026809938, 31.90204039037219985, -44.74265096482220372 ) ) ;
#22072=CARTESIAN_POINT ( 'NONE',  ( 17.07108633743450099, 19.88381105532299742, -15.67606611410359996 ) ) ;
#22073=CARTESIAN_POINT ( 'NONE',  ( 65.61835811606158586, -31.74415475557530186, -17.32553893461689754 ) ) ;
#22074=CARTESIAN_POINT ( 'NONE',  ( 17.99230109774930142, 19.88380302201240113, -74.34036667011370980 ) ) ;
#22075=VERTEX_POINT ( 'NONE', #23628 ) ;
#22076=EDGE_LOOP ( 'NONE', ( #49227, #40312, #43017, #6504, #16290 ) ) ;
#22079=CARTESIAN_POINT ( 'NONE',  ( 50.98083915167267577, 0.1184463107911828128, -16.83642266816315214 ) ) ;
#22081=CARTESIAN_POINT ( 'NONE',  ( 11.12442287039499966, -63.87901563523511328, -44.48448433309780370 ) ) ;
#22082=CARTESIAN_POINT ( 'NONE',  ( 57.53167045908470101, -45.29965578464429399, -25.93059424638790134 ) ) ;
#22083=FACE_OUTER_BOUND ( 'NONE', #38352, .T. ) ;
#22089=ORIENTED_EDGE ( 'NONE', *, *, #12053, .F. ) ;
#22090=CARTESIAN_POINT ( 'NONE',  ( 48.02062614174979416, -45.57114167671549865, -10.53674581177119940 ) ) ;
#22091=ADVANCED_FACE ( 'NONE', ( #47517 ), #38560, .T. ) ;
#22093=CIRCLE ( 'NONE', #16305, 1.999999999999997113 ) ;
#22094=CARTESIAN_POINT ( 'NONE',  ( 15.12151582312089992, 19.77629001565449940, -21.37863257646460013 ) ) ;
#22095=LINE ( 'NONE', #21839, #5921 ) ;
#22099=CARTESIAN_POINT ( 'NONE',  ( 47.07821196700830058, -54.56982298144170329, -75.12266286288350159 ) ) ;
#22100=CARTESIAN_POINT ( 'NONE',  ( 61.79285179583219900, 13.10481322255020054, -9.877340765310581361 ) ) ;
#22101=CARTESIAN_POINT ( 'NONE',  ( 50.67690155642070238, -50.61106055578139973, -76.14999999999999147 ) ) ;
#22103=CARTESIAN_POINT ( 'NONE',  ( 51.04849474376590024, 19.66358989377309996, -76.15025768601358891 ) ) ;
#22104=CARTESIAN_POINT ( 'NONE',  ( 59.29192855637670334, 13.93150092321869948, -26.12720780484039906 ) ) ;
#22107=EDGE_LOOP ( 'NONE', ( #383, #10893, #30821, #26731, #30309, #24443, #29713, #43273, #35505, #10773, #28649, #25291, #6966, #395, #2246, #2899 ) ) ;
#22109=CIRCLE ( 'NONE', #43904, 30.50439988982899564 ) ;
#22110=CARTESIAN_POINT ( 'NONE',  ( -11.07245470237450036, -42.11047228534719977, -5.947362040326959587 ) ) ;
#22111=ADVANCED_FACE ( 'NONE', ( #31747 ), #4410, .T. ) ;
#22113=CARTESIAN_POINT ( 'NONE',  ( 17.07108737582920455, -51.11618894467930119, -15.67606610107699971 ) ) ;
#22117=CARTESIAN_POINT ( 'NONE',  ( 41.26036483009979605, 12.97521128452129879, -4.192607600171130322 ) ) ;
#22119=CARTESIAN_POINT ( 'NONE',  ( 19.93042471013020034, 24.20303158999493576, -75.02879301527407563 ) ) ;
#22121=AXIS2_PLACEMENT_3D ( 'NONE', #44164, #29199, #8527 ) ;
#22123=CARTESIAN_POINT ( 'NONE',  ( 18.72308090817790216, -51.82694627962250422, -74.93568190818520236 ) ) ;
#22131=CARTESIAN_POINT ( 'NONE',  ( 60.79255070202940203, -45.73115554882360101, -47.75226182717869960 ) ) ;
#22136=CARTESIAN_POINT ( 'NONE',  ( 75.13393739769618662, 1.883811055320649963, -84.38499399519520239 ) ) ;
#22137=CARTESIAN_POINT ( 'NONE',  ( 60.83133137330749918, -45.46867109277970087, -47.01992810568810199 ) ) ;
#22139=VERTEX_POINT ( 'NONE', #27833 ) ;
#22140=VERTEX_POINT ( 'NONE', #4768 ) ;
#22142=DIRECTION ( 'NONE',  ( 0.000000000000000000, 0.000000000000000000, 1.000000000000000000 ) ) ;
#22143=ORIENTED_EDGE ( 'NONE', *, *, #9571, .F. ) ;
#22144=ORIENTED_EDGE ( 'NONE', *, *, #5872, .T. ) ;
#22147=EDGE_CURVE ( 'NONE', #24962, #36035, #39084, .T. ) ;
#22152=CARTESIAN_POINT ( 'NONE',  ( 53.80071036277350061, -50.68582778161849234, -76.57022530412510264 ) ) ;
#22153=CARTESIAN_POINT ( 'NONE',  ( 60.59756557471860106, 14.41685909332530002, -47.48166371871570846 ) ) ;
#22156=CARTESIAN_POINT ( 'NONE',  ( 45.96729298300089539, 13.88381088409749964, -7.679810999631830448 ) ) ;
#22157=AXIS2_PLACEMENT_3D ( 'NONE', #30556, #14588, #33964 ) ;
#22158=CARTESIAN_POINT ( 'NONE',  ( 41.13550660981270113, -44.31231073639379758, -4.257233742966690215 ) ) ;
#22159=CARTESIAN_POINT ( 'NONE',  ( 14.34417029198879945, -51.11618894467930119, -76.14999999999999147 ) ) ;
#22160=CARTESIAN_POINT ( 'NONE',  ( -10.87689599130639984, 11.12029513569609840, -6.286428452389710486 ) ) ;
#22165=EDGE_CURVE ( 'NONE', #49956, #29481, #15281, .T. ) ;
#22166=EDGE_LOOP ( 'NONE', ( #42813, #20152, #42893, #2567 ) ) ;
#22170=CARTESIAN_POINT ( 'NONE',  ( 61.28085240419530066, -45.60177449860450594, -47.67834116410560341 ) ) ;
#22174=CARTESIAN_POINT ( 'NONE',  ( 48.07362292129520398, -54.31422102361820237, -54.91777794127389711 ) ) ;
#22177=CARTESIAN_POINT ( 'NONE',  ( -9.120882960378676074, -44.01580188157885232, -5.427931971034974268 ) ) ;
#22179=CARTESIAN_POINT ( 'NONE',  ( 48.17397874823690529, 23.07566552192859888, -55.30238548989590441 ) ) ;
#22180=ORIENTED_EDGE ( 'NONE', *, *, #11062, .T. ) ;
#22185=CARTESIAN_POINT ( 'NONE',  ( 83.87141997196457055, 13.62662327952309127, -47.47133103277113264 ) ) ;
#22187=CARTESIAN_POINT ( 'NONE',  ( 84.39650841167410533, 12.26252976892699920, -47.35795223498069362 ) ) ;
#22188=CARTESIAN_POINT ( 'NONE',  ( 52.63503755353740132, 18.55503091818710004, -27.72364810048630090 ) ) ;
#22190=FACE_OUTER_BOUND ( 'NONE', #12977, .T. ) ;
#22193=B_SPLINE_SURFACE_WITH_KNOTS ( 'NONE', 3, 3, ( 
 ( #36103, #3634, #39786, #20110, #15429, #31895, #47911, #39272, #27203 ),
 ( #12015, #206, #15169, #19606, #27968, #19087, #43972, #31126, #11241 ),
 ( #43214, #3377, #24021, #35596, #48163, #43720, #12265, #19349, #7820 ),
 ( #44227, #3120, #35064, #9381, #1245, #48690, #16981, #981, #1502 ),
 ( #13562, #25324, #8328, #45268, #12792, #9110, #32928, #44490, #28748 ),
 ( #44747, #48956, #24281, #45007, #41327, #29011, #8853, #25059, #17487 ),
 ( #17233, #28489, #8593, #24802, #41076, #5189, #13059, #21140, #33451 ),
 ( #36348, #33194, #40814, #37147, #49213, #49471, #13306, #29525, #5442 ),
 ( #21399, #4913, #29266, #37400, #24537, #20886, #40555, #36881, #40301 ),
 ( #4392, #20361, #460, #16446, #32400, #48422, #4645, #12522, #20620 ),
 ( #36608, #714, #16704, #32659, #30295, #38706, #42633, #21649, #49724 ),
 ( #50746, #50492, #17739, #30548, #6730, #46573, #2013, #41847, #2794 ),
 ( #33708, #10140, #21908, #5696, #26618, #10401, #14323, #46312, #18767 ),
 ( #2272, #14582, #22686, #34739, #34487, #49975, #14842, #45788, #25581 ),
 ( #45529, #9624, #41586, #10661, #18246, #37654, #13812, #1753, #29770 ),
 ( #9878, #25834, #5950, #18513, #37919, #17994, #33960, #14068, #30030 ) ),
 .UNSPECIFIED., .F., .F., .F.,
 ( 4, 2, 2, 2, 2, 2, 2, 4 ),
 ( 4, 1, 1, 1, 1, 1, 4 ),
 ( -3.203522274500000355E-05, 0.2957445120220140167, 0.5890486225480849880, 0.7853981633974459475, 0.8835729338221269824, 1.040652566501619969, 1.291979978788799999, 1.570796326794889897 ),
 ( -3.203522271700000133E-05, 0.1666666666666670182, 0.3333333333333329818, 0.5000000000000000000, 0.6666666666666670737, 0.8333333333333330373, 1.000032035222700122 ),
 .UNSPECIFIED. ) ;
#22199=CARTESIAN_POINT ( 'NONE',  ( 12.10858429747099940, -64.84551244548728732, -16.12611387919940142 ) ) ;
#22201=CARTESIAN_POINT ( 'NONE',  ( -33.86606260230286125, -15.61618894467806484, -57.75434458024869855 ) ) ;
#22202=CARTESIAN_POINT ( 'NONE',  ( 51.10510889049552219, 3.800546900492662417, -76.46299428730267778 ) ) ;
#22203=ORIENTED_EDGE ( 'NONE', *, *, #4916, .T. ) ;
#22204=ORIENTED_EDGE ( 'NONE', *, *, #47452, .F. ) ;
#22206=FACE_OUTER_BOUND ( 'NONE', #48018, .T. ) ;
#22208=CARTESIAN_POINT ( 'NONE',  ( 52.75874701511860110, 18.42236751908479775, -48.21692926115490252 ) ) ;
#22209=CARTESIAN_POINT ( 'NONE',  ( 64.96436114686899543, -1.516193279748339950, -16.48292108836169945 ) ) ;
#22210=CARTESIAN_POINT ( 'NONE',  ( 51.30775034956070613, -48.70729205768719794, -76.60305689054860068 ) ) ;
#22212=CARTESIAN_POINT ( 'NONE',  ( 60.83826515012160030, -46.13970514846629811, -48.26656313140399845 ) ) ;
#22215=CARTESIAN_POINT ( 'NONE',  ( 52.67941827447170056, -49.73994065207379123, -27.56303321415330032 ) ) ;
#22216=CARTESIAN_POINT ( 'NONE',  ( 68.13393739769706769, 17.98087126524489321, -74.20351669811762463 ) ) ;
#22217=ORIENTED_EDGE ( 'NONE', *, *, #51277, .T. ) ;
#22220=VECTOR ( 'NONE', #19089, 1000.000000000000000 ) ;
#22222=AXIS2_PLACEMENT_3D ( 'NONE', #37407, #24546, #9631 ) ;
#22223=CARTESIAN_POINT ( 'NONE',  ( 14.07747898808480080, -51.04610731982879912, -22.00391413710600119 ) ) ;
#22224=CARTESIAN_POINT ( 'NONE',  ( 55.57043806660909979, 19.45794959307779592, -75.70375535085590002 ) ) ;
#22225=CARTESIAN_POINT ( 'NONE',  ( 47.36202133841670303, -54.21176582509019681, -75.36157798374209449 ) ) ;
#22226=CARTESIAN_POINT ( 'NONE',  ( 54.89464421352140278, 14.83598063949260037, -15.98485522678499926 ) ) ;
#22227=CARTESIAN_POINT ( 'NONE',  ( 47.67821675608059451, 23.28668618819479619, -55.12141599180650076 ) ) ;
#22228=CARTESIAN_POINT ( 'NONE',  ( 56.52293937326459883, -50.63229154223470374, -53.14906066081460523 ) ) ;
#22231=DIRECTION ( 'NONE',  ( 0.3294064756440925335, -0.9441882088883222224, -3.330669073875471100E-16 ) ) ;
#22232=ORIENTED_EDGE ( 'NONE', *, *, #3663, .T. ) ;
#22233=CARTESIAN_POINT ( 'NONE',  ( 47.54872616799120522, 23.22222337448880225, -74.81054825214430082 ) ) ;
#22237=CARTESIAN_POINT ( 'NONE',  ( 12.40751055747876919, -65.38681240857033572, -23.57252729928288915 ) ) ;
#22238=CARTESIAN_POINT ( 'NONE',  ( 59.13340102237120277, -15.61618894467929941, -15.65754737356207116 ) ) ;
#22239=DIRECTION ( 'NONE',  ( -1.000000000000000000, -7.683667316014053881E-33, 8.592609827796581962E-15 ) ) ;
#22241=CARTESIAN_POINT ( 'NONE',  ( 82.13853704237929776, 14.41284512186622102, -47.72712807259519963 ) ) ;
#22242=CARTESIAN_POINT ( 'NONE',  ( 7.853097003783789276, 29.28805065900050053, -20.86915960608759946 ) ) ;
#22245=CARTESIAN_POINT ( 'NONE',  ( 12.77400604982229915, 32.54918712825639915, -45.78449089158890217 ) ) ;
#22246=VERTEX_POINT ( 'NONE', #41700 ) ;
#22247=CARTESIAN_POINT ( 'NONE',  ( 53.00021633606750271, -49.57817710704839698, -48.89297489742170200 ) ) ;
#22248=ORIENTED_EDGE ( 'NONE', *, *, #33265, .T. ) ;
#22250=CARTESIAN_POINT ( 'NONE',  ( 17.54621496640162448, 20.94681317766335127, -75.92929758211226954 ) ) ;
#22253=CARTESIAN_POINT ( 'NONE',  ( 13.93865262801319993, 19.96876084912479854, -22.80126943285790020 ) ) ;
#22254=CARTESIAN_POINT ( 'NONE',  ( 55.98639049795390576, 14.70696325443280017, -25.73482700409929791 ) ) ;
#22256=FACE_OUTER_BOUND ( 'NONE', #13411, .T. ) ;
#22257=CARTESIAN_POINT ( 'NONE',  ( 53.11419542519070092, 18.31613794100389825, -49.05615257636990378 ) ) ;
#22258=CARTESIAN_POINT ( 'NONE',  ( 54.47258461985209976, -46.25235281383459807, -15.76423277873260176 ) ) ;
#22263=CARTESIAN_POINT ( 'NONE',  ( 59.03492131492150463, 15.32045715074029957, -47.92638814198690511 ) ) ;
#22266=CARTESIAN_POINT ( 'NONE',  ( 11.42280562904119989, -65.35797272322230356, -18.14299411099350223 ) ) ;
#22267=CARTESIAN_POINT ( 'NONE',  ( 52.63953642234348251, -49.80174121720273916, -48.69586908824972227 ) ) ;
#22272=VERTEX_POINT ( 'NONE', #41190 ) ;
#22273=CARTESIAN_POINT ( 'NONE',  ( 10.13539115020860137, -63.12861584496490508, -45.99741659280339690 ) ) ;
#22275=CARTESIAN_POINT ( 'NONE',  ( 58.92073396209919878, -28.11618894467929763, -18.64999999999999858 ) ) ;
#22276=EDGE_LOOP ( 'NONE', ( #24723, #6189, #30181, #43131, #40763, #25489, #29231, #12693 ) ) ;
#22278=CARTESIAN_POINT ( 'NONE',  ( 56.93701001012390606, 19.40825549115340110, -53.86363390784850225 ) ) ;
#22279=CARTESIAN_POINT ( 'NONE',  ( 53.07826437316199275, 19.12198495391469777, -77.22375576538830444 ) ) ;
#22280=( BOUNDED_CURVE ( )  B_SPLINE_CURVE ( 3, ( #29482, #25282, #29988, #34177 ),
 .UNSPECIFIED., .F., .T. ) 
 B_SPLINE_CURVE_WITH_KNOTS ( ( 4, 4 ),
 ( 4.787162522534349485, 4.797305365512180231 ),
 .UNSPECIFIED. ) 
 CURVE ( )  GEOMETRIC_REPRESENTATION_ITEM ( )  RATIONAL_B_SPLINE_CURVE ( ( 1.000000000000000000, 0.9999914269130683042, 0.9999914269130683042, 1.000000000000000000 ) ) 
 REPRESENTATION_ITEM ( '' )  );
#22281=ORIENTED_EDGE ( 'NONE', *, *, #51496, .F. ) ;
#22282=ADVANCED_FACE ( 'NONE', ( #30920, #35118 ), #10778, .T. ) ;
#22283=DIRECTION ( 'NONE',  ( 0.000000000000000000, 0.9319748226751540798, -0.3625230060280524302 ) ) ;
#22290=LINE ( 'NONE', #27005, #5451 ) ;
#22292=ORIENTED_EDGE ( 'NONE', *, *, #8769, .T. ) ;
#22293=CARTESIAN_POINT ( 'NONE',  ( 61.75019796695539753, -46.11618894467930119, -37.26101630944549470 ) ) ;
#22298=CARTESIAN_POINT ( 'NONE',  ( 14.00739969242919969, 20.40964180427139851, -75.33373089150879309 ) ) ;
#22299=EDGE_CURVE ( 'NONE', #25615, #47514, #15957, .T. ) ;
#22301=CARTESIAN_POINT ( 'NONE',  ( 43.41582131227239927, -45.06410286474709181, -6.498296231305429771 ) ) ;
#22305=CARTESIAN_POINT ( 'NONE',  ( 52.61201418140420571, -49.81418459234139817, -28.07267484291759985 ) ) ;
#22306=CARTESIAN_POINT ( 'NONE',  ( 56.35989604313040502, -50.72843546871860099, -74.81725475743600384 ) ) ;
#22307=CARTESIAN_POINT ( 'NONE',  ( -0.09053481959779700883, 22.39771088603180260, -9.857808184667490536 ) ) ;
#22309=CARTESIAN_POINT ( 'NONE',  ( 47.40880866017789685, -54.64074575612490037, -54.64987641489110359 ) ) ;
#22312=CARTESIAN_POINT ( 'NONE',  ( -3.306064913546559847, -48.27659316127069644, -4.296538301066338938 ) ) ;
#22313=CARTESIAN_POINT ( 'NONE',  ( 47.44230769974480211, 23.39977620147499948, -54.85721486140309366 ) ) ;
#22316=CARTESIAN_POINT ( 'NONE',  ( 45.82850501745777905, -45.11588806901219328, -7.494124676809759578 ) ) ;
#22318=CARTESIAN_POINT ( 'NONE',  ( 57.06431677472210140, 13.92418399160115428, -25.30300627412070114 ) ) ;
#22319=CARTESIAN_POINT ( 'NONE',  ( 11.38858895854670017, 33.99473195841849815, -17.28671580462109958 ) ) ;
#22320=CARTESIAN_POINT ( 'NONE',  ( 51.67588111593440203, 17.38380895277190064, -77.01364305260611332 ) ) ;
#22321=CARTESIAN_POINT ( 'NONE',  ( 53.37786163247539406, 18.14274543012349739, -48.82821703136220037 ) ) ;
#22322=DIRECTION ( 'NONE',  ( -0.3294064756441279496, -0.9441882088883098989, 0.000000000000000000 ) ) ;
#22323=CARTESIAN_POINT ( 'NONE',  ( 57.22510014093110442, -47.50321319438739920, -48.27967399149409999 ) ) ;
#22324=CARTESIAN_POINT ( 'NONE',  ( 52.81005723544840436, 18.43886315067999959, -28.15002577751260304 ) ) ;
#22326=CARTESIAN_POINT ( 'NONE',  ( 50.44957631477119975, 22.08479505950380073, -54.57514961256589459 ) ) ;
#22328=CARTESIAN_POINT ( 'NONE',  ( 53.05489977530229595, 18.36750851102400262, -49.10811586475909962 ) ) ;
#22329=DIRECTION ( 'NONE',  ( 0.000000000000000000, -1.000000000000000000, 0.000000000000000000 ) ) ;
#22331=CARTESIAN_POINT ( 'NONE',  ( 10.49154450428839880, 32.04238758567439760, -45.62559114465060617 ) ) ;
#22334=CYLINDRICAL_SURFACE ( 'NONE', #42706, 2.000000000000170530 ) ;
#22335=VERTEX_POINT ( 'NONE', #15478 ) ;
#22336=CARTESIAN_POINT ( 'NONE',  ( 12.71077838082760891, 24.23706720221435162, -75.54041227948643211 ) ) ;
#22339=CARTESIAN_POINT ( 'NONE',  ( 56.53399784873889899, 19.21501630139210093, -52.81205167924800037 ) ) ;
#22340=CARTESIAN_POINT ( 'NONE',  ( 76.50051362292605006, -2.884157946879440715, -13.22963151320726283 ) ) ;
#22341=ORIENTED_EDGE ( 'NONE', *, *, #41710, .T. ) ;
#22342=CARTESIAN_POINT ( 'NONE',  ( 12.89514957290669983, -65.50886968517070841, -47.53407047177050515 ) ) ;
#22343=CARTESIAN_POINT ( 'NONE',  ( 57.44551019405400183, -45.12993590191310034, -25.53739291223670094 ) ) ;
#22344=DIRECTION ( 'NONE',  ( 1.000000000000000000, 0.000000000000000000, 0.000000000000000000 ) ) ;
#22348=ORIENTED_EDGE ( 'NONE', *, *, #34531, .T. ) ;
#22349=CARTESIAN_POINT ( 'NONE',  ( 11.83411043809303465, 34.19861816370081442, -22.31001989919771944 ) ) ;
#22352=EDGE_CURVE ( 'NONE', #12686, #38024, #39548, .T. ) ;
#22354=CARTESIAN_POINT ( 'NONE',  ( 46.21902970698399571, -45.19874479850450655, -8.545594584115770331 ) ) ;
#22356=CARTESIAN_POINT ( 'NONE',  ( 16.49314696555249782, 19.88381105389379755, -20.88058500138470208 ) ) ;
#22357=DIRECTION ( 'NONE',  ( 0.000000000000000000, 0.000000000000000000, 1.000000000000000000 ) ) ;
#22360=CARTESIAN_POINT ( 'NONE',  ( 47.25417729284069424, -54.61827072552059548, -74.80726814568210159 ) ) ;
#22361=CARTESIAN_POINT ( 'NONE',  ( 45.09885310914830114, 13.74449180402419834, -6.429922486547810401 ) ) ;
#22362=CARTESIAN_POINT ( 'NONE',  ( 57.50723796702470025, 15.88381105532069704, -31.98003398807230369 ) ) ;
#22364=CARTESIAN_POINT ( 'NONE',  ( 51.93948715274890304, 19.85719722970700118, -76.10418646478689197 ) ) ;
#22366=CYLINDRICAL_SURFACE ( 'NONE', #44555, 2.000000000000058620 ) ;
#22370=CARTESIAN_POINT ( 'NONE',  ( 6.047473704414409568, -58.85581576903580014, -11.31522686691929991 ) ) ;
#22371=CARTESIAN_POINT ( 'NONE',  ( 76.39679632360071082, -12.51312258731159766, -12.78270703766589911 ) ) ;
#22372=CARTESIAN_POINT ( 'NONE',  ( 75.12449000029563706, 13.75696482515094310, -14.63746784062838913 ) ) ;
#22373=CARTESIAN_POINT ( 'NONE',  ( 16.65420337943509566, -51.11618894467930119, -15.67544740040250062 ) ) ;
#22374=CARTESIAN_POINT ( 'NONE',  ( 13.58714272597830686, -55.53442211211926605, -76.07915437886748578 ) ) ;
#22375=CARTESIAN_POINT ( 'NONE',  ( 14.74632770935266102, -16.62434639553314142, -170.7999095292539948 ) ) ;
#22377=CARTESIAN_POINT ( 'NONE',  ( 82.41472024409949881, -45.17082120583620508, -46.87528017089150012 ) ) ;
#22379=CARTESIAN_POINT ( 'NONE',  ( 42.37474662607149867, 12.16745287750829974, -4.189334837800680056 ) ) ;
#22382=CARTESIAN_POINT ( 'NONE',  ( 66.23540447448814916, -49.95860450174473044, -71.35146707679193412 ) ) ;
#22384=CARTESIAN_POINT ( 'NONE',  ( 75.98223876097091534, -43.32481619739640166, -13.62276456639723321 ) ) ;
#22385=CARTESIAN_POINT ( 'NONE',  ( 57.48324947012589803, 13.88381105532070059, -17.42702405245080044 ) ) ;
#22391=CARTESIAN_POINT ( 'NONE',  ( 53.29384558423090112, -50.54670888882439783, -48.47378032971909789 ) ) ;
#22392=CARTESIAN_POINT ( 'NONE',  ( 60.49059093688929778, -45.82073196953280814, -47.74858579941459880 ) ) ;
#22394=DIRECTION ( 'NONE',  ( -1.000000000000000000, 0.000000000000000000, 0.000000000000000000 ) ) ;
#22398=ORIENTED_EDGE ( 'NONE', *, *, #39645, .T. ) ;
#22399=ORIENTED_EDGE ( 'NONE', *, *, #20485, .F. ) ;
#22400=ORIENTED_EDGE ( 'NONE', *, *, #9370, .F. ) ;
#22401=DIRECTION ( 'NONE',  ( 0.5685928097855378338, 0.5944782866685498490, -0.5685928097855378338 ) ) ;
#22402=CARTESIAN_POINT ( 'NONE',  ( 61.16489974143080133, -45.30856623237389869, -46.97020373819919570 ) ) ;
#22403=CARTESIAN_POINT ( 'NONE',  ( 52.70547899565750072, -49.76225394339979857, -48.81521342827540622 ) ) ;
#22405=AXIS2_PLACEMENT_3D ( 'NONE', #48862, #40214, #32572 ) ;
#22406=ORIENTED_EDGE ( 'NONE', *, *, #8846, .F. ) ;
#22407=EDGE_CURVE ( 'NONE', #37013, #31554, #7619, .T. ) ;
#22414=CARTESIAN_POINT ( 'NONE',  ( 66.63393739769620083, -38.11618894467930119, -73.25000000000000000 ) ) ;
#22415=CARTESIAN_POINT ( 'NONE',  ( 51.98443728612009096, -51.36758245232200437, -75.98853294935470615 ) ) ;
#22416=CARTESIAN_POINT ( 'NONE',  ( 60.59271029648169105, 14.39476059538499975, -47.40213830669640060 ) ) ;
#22419=CARTESIAN_POINT ( 'NONE',  ( 42.34708436978809942, 14.06745345395279934, -6.529032511125610228 ) ) ;
#22420=CARTESIAN_POINT ( 'NONE',  ( 42.42181531931939986, -43.19228534352320281, -3.882827786889420096 ) ) ;
#22422=CARTESIAN_POINT ( 'NONE',  ( 66.72561048563099462, 1.883811055320649963, -20.64999999980150136 ) ) ;
#22424=LINE ( 'NONE', #50488, #11043 ) ;
#22427=CARTESIAN_POINT ( 'NONE',  ( 43.55793695338589799, 14.79940918324820132, -7.980363424730000155 ) ) ;
#22429=CARTESIAN_POINT ( 'NONE',  ( 27.86468381613284961, -7.093302786438550278, -6.928362978644219794 ) ) ;
#22431=CARTESIAN_POINT ( 'NONE',  ( 85.84022851002180232, 17.38381105532069881, -53.47585302082339354 ) ) ;
#22433=CARTESIAN_POINT ( 'NONE',  ( 47.84470410613830182, -54.42058614811499950, -54.90151223973010275 ) ) ;
#22436=CARTESIAN_POINT ( 'NONE',  ( 56.45679588454870412, 19.42305698160840066, -53.17273421675590583 ) ) ;
#22437=CARTESIAN_POINT ( 'NONE',  ( 41.40756759976829926, 13.53921337778190015, -5.393983492778530398 ) ) ;
#22438=CARTESIAN_POINT ( 'NONE',  ( 48.04015573092420510, 23.13167815216619871, -55.20742902216350245 ) ) ;
#22441=ORIENTED_EDGE ( 'NONE', *, *, #19397, .T. ) ;
#22444=CARTESIAN_POINT ( 'NONE',  ( 83.76204656006096627, 13.76116163493793820, -47.48603732758919449 ) ) ;
#22445=CARTESIAN_POINT ( 'NONE',  ( 16.13393739769620083, -15.61618894467929941, -15.65000000000000036 ) ) ;
#22446=CYLINDRICAL_SURFACE ( 'NONE', #28198, 1.999999999999997335 ) ;
#22447=CARTESIAN_POINT ( 'NONE',  ( 53.37088539291629985, 17.75190881940800125, -26.62991259020409984 ) ) ;
#22451=CARTESIAN_POINT ( 'NONE',  ( 55.92358841828349370, -45.89462731853816280, -25.40852269161388222 ) ) ;
#22452=ORIENTED_EDGE ( 'NONE', *, *, #19976, .T. ) ;
#22456=CARTESIAN_POINT ( 'NONE',  ( 12.09242720215750033, -64.92301394585230412, -16.23377612492940258 ) ) ;
#22459=CARTESIAN_POINT ( 'NONE',  ( 11.79211174348889912, 33.77432752955800055, -45.32950553571880192 ) ) ;
#22460=B_SPLINE_CURVE_WITH_KNOTS ( 'NONE', 3,
 ( #30746, #18704, #31514, #43598, #10600, #2986, #14778, #39407, #39150, #46769 ),
 .UNSPECIFIED., .F., .F.,
 ( 4, 1, 1, 1, 1, 1, 1, 4 ),
 ( 0.000000000000000000, 0.1428507730289225175, 0.2857076245177915252, 0.4285644760066605330, 0.5714213274955285415, 0.7142781789843976048, 0.8571350304732666681, 1.000000000000000000 ),
 .UNSPECIFIED. ) ;
#22461=CARTESIAN_POINT ( 'NONE',  ( 13.00893739769619906, -65.51843714052719747, -47.75434321273180416 ) ) ;
#22462=ORIENTED_EDGE ( 'NONE', *, *, #38951, .F. ) ;
#22467=CARTESIAN_POINT ( 'NONE',  ( 52.84041160373019608, 18.34707223868749892, -48.42032881049700421 ) ) ;
#22469=CARTESIAN_POINT ( 'NONE',  ( 62.29010619281529415, -1.891186742061369941, -16.10088301903060071 ) ) ;
#22470=CARTESIAN_POINT ( 'NONE',  ( 50.90450148898350591, -49.87900598378690376, -76.22583875105431162 ) ) ;
#22471=CARTESIAN_POINT ( 'NONE',  ( 58.20425128766380141, -49.07305351875690036, -51.45101314545409821 ) ) ;
#22472=ORIENTED_EDGE ( 'NONE', *, *, #31624, .F. ) ;
#22474=CARTESIAN_POINT ( 'NONE',  ( 68.13393739769819035, 19.47158195952109594, -72.59354914830207406 ) ) ;
#22478=CARTESIAN_POINT ( 'NONE',  ( 57.22322293371580315, -47.50141109488779989, -48.27531557238859961 ) ) ;
#22479=AXIS2_PLACEMENT_3D ( 'NONE', #35881, #7342, #3673 ) ;
#22481=CARTESIAN_POINT ( 'NONE',  ( 13.09367229119200005, -50.61305962739500330, -21.36973413670409983 ) ) ;
#22482=CARTESIAN_POINT ( 'NONE',  ( 54.08449847407359812, 19.43926436916860112, -76.52238400108929284 ) ) ;
#22484=CARTESIAN_POINT ( 'NONE',  ( 46.50380985604989803, -53.09853600777310589, -76.13981661584659832 ) ) ;
#22485=CARTESIAN_POINT ( 'NONE',  ( 56.73667514912609988, 14.03196534028450060, -17.72798751313560217 ) ) ;
#22487=CARTESIAN_POINT ( 'NONE',  ( 56.68249757891010177, -50.44500735585980067, -52.87688493394379918 ) ) ;
#22490=VERTEX_POINT ( 'NONE', #15991 ) ;
#22491=CARTESIAN_POINT ( 'NONE',  ( 47.64143405400400866, 23.30250925608780221, -74.14999581260518369 ) ) ;
#22494=CARTESIAN_POINT ( 'NONE',  ( 12.52565026941822168, -65.42862977055203544, -23.52286200862776511 ) ) ;
#22495=CARTESIAN_POINT ( 'NONE',  ( 46.03123730580679762, -45.11618894467689955, -7.582885969263020165 ) ) ;
#22498=CARTESIAN_POINT ( 'NONE',  ( 82.34924927927150407, 14.41608331847699986, -47.73066065071600406 ) ) ;
#22499=CARTESIAN_POINT ( 'NONE',  ( 16.13393739769620083, -15.61618894467929941, -11.23251175440650051 ) ) ;
#22502=ADVANCED_FACE ( 'NONE', ( #28020 ), #26381, .T. ) ;
#22504=CARTESIAN_POINT ( 'NONE',  ( -0.3561701380248140092, 32.06759910672769820, -50.35138997524130389 ) ) ;
#22507=CARTESIAN_POINT ( 'NONE',  ( 52.73800511975559857, -49.72354018477579274, -48.71590736184970183 ) ) ;
#22510=CARTESIAN_POINT ( 'NONE',  ( 14.34417029198830029, 19.88381105532299742, -22.49240188329279988 ) ) ;
#22512=CARTESIAN_POINT ( 'NONE',  ( 13.61938558558030010, 20.19483563532820014, -23.15000001641130112 ) ) ;
#22513=CARTESIAN_POINT ( 'NONE',  ( 57.57776213900729800, 13.88371113915540001, -25.40878180930539898 ) ) ;
#22516=AXIS2_PLACEMENT_3D ( 'NONE', #8698, #20730, #36990 ) ;
#22518=CARTESIAN_POINT ( 'NONE',  ( 52.65605176727499526, 18.54635246044519903, -48.59646220643460879 ) ) ;
#22519=CARTESIAN_POINT ( 'NONE',  ( 55.17090527502239894, -46.00774235025210146, -16.22561265231399830 ) ) ;
#22521=VERTEX_POINT ( 'NONE', #15730 ) ;
#22523=CARTESIAN_POINT ( 'NONE',  ( 11.35626914494079998, -65.29495917086049417, -17.73521909030350230 ) ) ;
#22524=CARTESIAN_POINT ( 'NONE',  ( 11.28331493908370042, 33.98248205784230436, -47.30875510506540138 ) ) ;
#22526=CARTESIAN_POINT ( 'NONE',  ( 10.72852875956099972, -64.94169572740939600, -18.17421237900510178 ) ) ;
#22527=CARTESIAN_POINT ( 'NONE',  ( 52.67198760255845968, -49.78119412946662692, -48.75777783608981508 ) ) ;
#22528=DIRECTION ( 'NONE',  ( -0.1686178020941689892, 0.6660492713794449182, 0.7265992051412129005 ) ) ;
#22534=CARTESIAN_POINT ( 'NONE',  ( 10.98008937475129976, -63.44096224164839981, -44.74889856825390666 ) ) ;
#22537=ADVANCED_FACE ( 'NONE', ( #31685 ), #10267, .T. ) ;
#22539=CARTESIAN_POINT ( 'NONE',  ( 57.32356178356099718, 19.18213064475359886, -53.00097363025420094 ) ) ;
#22540=CARTESIAN_POINT ( 'NONE',  ( 52.75996715995819386, 18.93637462048650022, -77.25935876731659846 ) ) ;
#22542=CARTESIAN_POINT ( 'NONE',  ( 34.38393739769620083, -15.61618894467929941, 7.849999999999999645 ) ) ;
#22548=ORIENTED_EDGE ( 'NONE', *, *, #36725, .T. ) ;
#22550=VECTOR ( 'NONE', #21767, 1000.000000000000000 ) ;
#22551=CYLINDRICAL_SURFACE ( 'NONE', #35082, 1.999999999999999112 ) ;
#22553=TOROIDAL_SURFACE ( 'NONE', #31745, 25.10000000000000142, 4.000000000000050626 ) ;
#22557=CARTESIAN_POINT ( 'NONE',  ( 13.76101378273559916, 20.06273318926150040, -74.35769860268439402 ) ) ;
#22558=DIRECTION ( 'NONE',  ( 0.000000000000000000, 0.000000000000000000, -1.000000000000000000 ) ) ;
#22559=CARTESIAN_POINT ( 'NONE',  ( 41.12782547105919662, -44.91524683664780326, -5.505761199517789528 ) ) ;
#22564=CARTESIAN_POINT ( 'NONE',  ( 56.25504298498950817, -50.77785272729379784, -74.74462238221099142 ) ) ;
#22565=CARTESIAN_POINT ( 'NONE',  ( -6.219785763107670284, 14.61265879496390063, -4.702705381378909699 ) ) ;
#22569=DIRECTION ( 'NONE',  ( 0.3445670372598628184, 0.6174735272333260472, -0.7071067811865442421 ) ) ;
#22573=CARTESIAN_POINT ( 'NONE',  ( 47.48084007132430173, 23.37089297048629888, -54.76237024660140662 ) ) ;
#22577=CARTESIAN_POINT ( 'NONE',  ( 11.84416398831050010, 33.85620967646509882, -16.58498012167680002 ) ) ;
#22580=CARTESIAN_POINT ( 'NONE',  ( 53.04797525238309674, 18.31477690342330078, -48.83268161531540130 ) ) ;
#22581=CARTESIAN_POINT ( 'NONE',  ( 61.13393739769620083, -43.11618894467930119, -84.38499399519520239 ) ) ;
#22583=CARTESIAN_POINT ( 'NONE',  ( 55.52913409436600034, 15.90026116505450027, -26.42135380471329853 ) ) ;
#22588=CARTESIAN_POINT ( 'NONE',  ( 46.23055864956999983, -45.11618894467940066, -7.629554990163329720 ) ) ;
#22590=CARTESIAN_POINT ( 'NONE',  ( 11.13393739769619906, 31.88305279702909800, -43.91250110351749925 ) ) ;
#22592=AXIS2_PLACEMENT_3D ( 'NONE', #43819, #11341, #23352 ) ;
#22593=CARTESIAN_POINT ( 'NONE',  ( 66.50409435687238613, -33.11595941302709889, -20.28080645395380088 ) ) ;
#22594=CARTESIAN_POINT ( 'NONE',  ( 18.66237858775300040, 20.19926697308340380, -74.35527526576579760 ) ) ;
#22598=CARTESIAN_POINT ( 'NONE',  ( 49.06135853991354168, -2.772563640123296924, -15.65933779184700647 ) ) ;
#22600=EDGE_CURVE ( 'NONE', #49606, #28015, #8579, .T. ) ;
#22601=CARTESIAN_POINT ( 'NONE',  ( 11.52518891765600095, -64.75101289998659126, -45.36825986196159732 ) ) ;
#22602=CARTESIAN_POINT ( 'NONE',  ( 55.99739780941779799, -45.92760302930049932, -25.73393128425269794 ) ) ;
#22603=DIRECTION ( 'NONE',  ( 0.000000000000000000, 0.000000000000000000, 1.000000000000000000 ) ) ;
#22604=DIRECTION ( 'NONE',  ( -0.8732394366197182567, 0.4872913772396111343, -1.665334536937735304E-16 ) ) ;
#22605=VERTEX_POINT ( 'NONE', #5741 ) ;
#22606=CARTESIAN_POINT ( 'NONE',  ( 11.63938621547738705, 34.14834037275974055, -22.50902133189791243 ) ) ;
#22608=CARTESIAN_POINT ( 'NONE',  ( 43.46647314489950276, -45.04259908834720250, -6.433232421327499395 ) ) ;
#22609=ORIENTED_EDGE ( 'NONE', *, *, #30208, .F. ) ;
#22613=B_SPLINE_CURVE_WITH_KNOTS ( 'NONE', 3,
 ( #6158, #25001, #5129, #21085, #37086 ),
 .UNSPECIFIED., .F., .F.,
 ( 4, 1, 4 ),
 ( 0.000000000000000000, 0.3333435241872368393, 0.5000152864445784884 ),
 .UNSPECIFIED. ) ;
#22616=CARTESIAN_POINT ( 'NONE',  ( 14.55219274796575313, 20.46959765477225091, -75.56421372419544014 ) ) ;
#22617=CARTESIAN_POINT ( 'NONE',  ( 46.72272053391589708, -53.55196115563460779, -76.01521976086429788 ) ) ;
#22618=CARTESIAN_POINT ( 'NONE',  ( 60.86286082204030379, 12.20400039278949933, -9.318368423349330243 ) ) ;
#22619=EDGE_CURVE ( 'NONE', #26354, #13074, #17027, .T. ) ;
#22620=DIRECTION ( 'NONE',  ( 0.000000000000000000, -1.000000000000000000, 0.000000000000000000 ) ) ;
#22621=AXIS2_PLACEMENT_3D ( 'NONE', #43646, #35253, #51254 ) ;
#22625=CARTESIAN_POINT ( 'NONE',  ( 60.51496306430259864, 13.88379478767680020, -26.40814067861359860 ) ) ;
#22629=B_SPLINE_SURFACE_WITH_KNOTS ( 'NONE', 3, 3, ( 
 ( #37395, #13555, #21641, #30288, #33702, #45523, #37914, #2007, #29763, #17989, #45783, #41842, #49971, #14063, #46048, #42101 ),
 ( #6206, #22160, #34733, #27901, #50993, #35524, #35782, #47589, #23186, #7490, #3820, #34993, #15614, #31569, #42886, #10915 ),
 ( #15096, #51260, #30798, #43653, #19793, #7754, #31058, #23703, #51516, #47083, #35263, #11683, #11432, #27650, #39717, #3564 ),
 ( #23443, #51766, #38696, #31312, #15865, #31825, #47841, #18759, #6980, #19535, #3045, #11945, #43143, #7238, #6724, #39202 ),
 ( #11173, #38954, #22680, #27138, #47337, #3298, #2788, #50737, #14836, #46826, #19280, #26877, #22934, #19017, #15356, #39465 ),
 ( #27394, #43395, #40482, #36541, #12194, #139, #37073, #48353, #1171, #8255, #32584, #48880, #23952, #49147, #12985, #16114 ),
 ( #41003, #44940, #391, #40232, #33119, #13244, #32077, #8522, #20289, #4067, #24987, #8779, #12718, #28672, #43906, #48095 ),
 ( #40744, #24469, #7999, #28935, #20546, #9041, #4322, #39975, #20033, #28154, #16375, #36031, #5119, #21071, #36280, #32332 ),
 ( #44158, #24203, #12446, #28413, #44420, #16906, #4574, #648, #32848, #16631, #48619, #44676, #24729, #20811, #36801, #911 ) ),
 .UNSPECIFIED., .F., .F., .F.,
 ( 4, 1, 1, 1, 1, 1, 4 ),
 ( 4, 2, 2, 2, 2, 2, 2, 4 ),
 ( 0.000000000000000000, 0.1666666666666670182, 0.3333333333333329818, 0.5000000000000000000, 0.6666666666666670737, 0.8333333333333330373, 1.000000003372510049 ),
 ( -11.88254149278500016, -9.803096731538550657, -7.426588432971120035, -5.941270746366480004, -5.198611903064159989, -4.010357753780449563, -2.109151114926509862, 3.424587999999999838E-09 ),
 .UNSPECIFIED. ) ;
#22630=ORIENTED_EDGE ( 'NONE', *, *, #37984, .F. ) ;
#22632=CARTESIAN_POINT ( 'NONE',  ( -8.120841049443690451, -43.88478719140770323, -4.398687954041819559 ) ) ;
#22633=CARTESIAN_POINT ( 'NONE',  ( 75.26680305930699433, -18.74898951345290143, -11.37374796283529932 ) ) ;
#22634=CARTESIAN_POINT ( 'NONE',  ( 75.11664760679863662, 13.76739462715691431, -14.66476025242160475 ) ) ;
#22635=CARTESIAN_POINT ( 'NONE',  ( 16.13393739769620083, -15.61618894467929941, -20.15000000000000213 ) ) ;
#22637=CARTESIAN_POINT ( 'NONE',  ( 82.13853704237929776, -45.12072225811939319, -46.53690974066719832 ) ) ;
#22638=CARTESIAN_POINT ( 'NONE',  ( 16.13393739769620083, -15.61618894467929941, -20.65000000000000213 ) ) ;
#22639=CARTESIAN_POINT ( 'NONE',  ( 42.63139190005710333, 11.62219417602310045, -3.312314667585950279 ) ) ;
#22643=CARTESIAN_POINT ( 'NONE',  ( 68.13393739769847457, -50.70395984888145335, -72.15645085170113759 ) ) ;
#22645=CARTESIAN_POINT ( 'NONE',  ( 17.93348425303889826, -51.26614876191910497, -74.93568190818520236 ) ) ;
#22646=CARTESIAN_POINT ( 'NONE',  ( 44.88192221582870189, -45.11618894467940066, -7.000245857760280188 ) ) ;
#22647=VERTEX_POINT ( 'NONE', #33505 ) ;
#22652=CARTESIAN_POINT ( 'NONE',  ( 60.62539537963969849, -45.77966094345969594, -47.75584023230200614 ) ) ;
#22656=CARTESIAN_POINT ( 'NONE',  ( 41.33278336659260077, -45.54329717826499291, -6.226146794320340128 ) ) ;
#22658=EDGE_LOOP ( 'NONE', ( #21045, #3535, #23843, #36577, #10120, #50654 ) ) ;
#22661=CARTESIAN_POINT ( 'NONE',  ( 61.34010690585019887, -45.20347833372960622, -46.45024392112279799 ) ) ;
#22662=CARTESIAN_POINT ( 'NONE',  ( 82.45630311851421368, -45.09271792554360303, -46.38988467804559690 ) ) ;
#22668=LINE ( 'NONE', #43645, #43663 ) ;
#22671=CARTESIAN_POINT ( 'NONE',  ( 31.10075179363273179, -4.742161777268546707, 7.849999999999997868 ) ) ;
#22672=CARTESIAN_POINT ( 'NONE',  ( 52.82839229275239745, -51.22091222732959892, -75.91621971673269798 ) ) ;
#22673=CARTESIAN_POINT ( 'NONE',  ( 60.95425169575680258, 14.19472640642180039, -47.19051797104440027 ) ) ;
#22675=EDGE_CURVE ( 'NONE', #38928, #21370, #20291, .T. ) ;
#22676=DIRECTION ( 'NONE',  ( 0.000000000000000000, 1.000000000000000000, 0.000000000000000000 ) ) ;
#22677=CARTESIAN_POINT ( 'NONE',  ( 40.75026606626570214, -44.57835314504790603, -4.220911785948969985 ) ) ;
#22680=CARTESIAN_POINT ( 'NONE',  ( -10.43316342469580071, 11.56352937203230091, -6.076102107692801013 ) ) ;
#22683=CARTESIAN_POINT ( 'NONE',  ( 17.92370450360863998, -51.11618894467903118, -74.34716300802168121 ) ) ;
#22686=CARTESIAN_POINT ( 'NONE',  ( 14.89313683410190059, -52.76520172820870158, -76.12661215459480957 ) ) ;
#22691=DIRECTION ( 'NONE',  ( 0.000000000000000000, 0.000000000000000000, -1.000000000000000000 ) ) ;
#22693=CARTESIAN_POINT ( 'NONE',  ( 11.13393739769619906, 32.28996932333459569, -43.76018303787720498 ) ) ;
#22695=EDGE_CURVE ( 'NONE', #8205, #18792, #9443, .T. ) ;
#22697=CARTESIAN_POINT ( 'NONE',  ( 47.83873146774000418, -54.45004056421520033, -55.16375355595400265 ) ) ;
#22698=FACE_OUTER_BOUND ( 'NONE', #37685, .T. ) ;
#22700=CARTESIAN_POINT ( 'NONE',  ( 47.71207051903009955, 23.26369402866030001, -54.98518041347200125 ) ) ;
#22707=DIRECTION ( 'NONE',  ( 0.05023550054956202326, 0.000000000000000000, 0.9987374001630934250 ) ) ;
#22708=CARTESIAN_POINT ( 'NONE',  ( 83.67079303953970282, 13.80909354995310068, -47.45584445533860674 ) ) ;
#22715=ORIENTED_EDGE ( 'NONE', *, *, #16241, .F. ) ;
#22717=CARTESIAN_POINT ( 'NONE',  ( 11.89829296289419958, -64.83233913608019350, -16.17105426249170108 ) ) ;
#22719=CARTESIAN_POINT ( 'NONE',  ( 76.45177665192957761, -25.09083072484978416, -13.01961666583026300 ) ) ;
#22720=CARTESIAN_POINT ( 'NONE',  ( 9.367149180512809536, -63.29633625153390142, -46.50590274669379909 ) ) ;
#22721=EDGE_LOOP ( 'NONE', ( #7678, #1218, #42922, #4449 ) ) ;
#22722=ORIENTED_EDGE ( 'NONE', *, *, #39030, .T. ) ;
#22724=CARTESIAN_POINT ( 'NONE',  ( 52.86576716034980450, 18.31963347231479844, -48.38645722914640146 ) ) ;
#22725=CARTESIAN_POINT ( 'NONE',  ( 61.27130757359800128, -0.5767551585763339705, -16.33740500793329886 ) ) ;
#22726=CARTESIAN_POINT ( 'NONE',  ( 51.79630867582309861, -49.28713043378009218, -76.98491571383419796 ) ) ;
#22727=CARTESIAN_POINT ( 'NONE',  ( 57.01128662093320543, -50.56557199667180669, -53.09478151126450030 ) ) ;
#22730=CARTESIAN_POINT ( 'NONE',  ( 52.61990787174079998, -49.80354421666690001, -27.74322489265389891 ) ) ;
#22736=AXIS2_PLACEMENT_3D ( 'NONE', #24003, #44988, #40280 ) ;
#22739=CARTESIAN_POINT ( 'NONE',  ( 13.67288539103119938, -51.17054487835680021, -22.23396216461150132 ) ) ;
#22740=CARTESIAN_POINT ( 'NONE',  ( 47.32111516514439842, -54.12775347911220081, -75.47461153638509757 ) ) ;
#22741=ADVANCED_FACE ( 'NONE', ( #45057 ), #29571, .F. ) ;
#22742=CARTESIAN_POINT ( 'NONE',  ( 56.17414541250489890, 14.05430885410310005, -16.17612370156109947 ) ) ;
#22747=ORIENTED_EDGE ( 'NONE', *, *, #25494, .T. ) ;
#22748=CARTESIAN_POINT ( 'NONE',  ( 47.57129143639170366, 23.33298354540060160, -74.19756735440549278 ) ) ;
#22756=CARTESIAN_POINT ( 'NONE',  ( 82.13853704237929776, 13.90869809199659990, -46.70066698695239893 ) ) ;
#22761=CARTESIAN_POINT ( 'NONE',  ( -29.08731580419370033, 4.375077605369980027, -55.16774717297709429 ) ) ;
#22762=VERTEX_POINT ( 'NONE', #46106 ) ;
#22764=CARTESIAN_POINT ( 'NONE',  ( 52.93241479646199821, -49.61258791452640082, -48.85493845497290266 ) ) ;
#22769=CARTESIAN_POINT ( 'NONE',  ( 14.13581725382830001, 19.88180066538970081, -22.31751565788919933 ) ) ;
#22772=CARTESIAN_POINT ( 'NONE',  ( 52.59421258935810073, 18.59942272400250118, -48.47378032971769812 ) ) ;
#22773=CARTESIAN_POINT ( 'NONE',  ( 55.82670324262860362, -45.92590652002289886, -17.31876773537310044 ) ) ;
#22774=CARTESIAN_POINT ( 'NONE',  ( 14.34417029198830029, 19.88381105532299742, -74.14999999999999147 ) ) ;
#22777=ORIENTED_EDGE ( 'NONE', *, *, #39766, .T. ) ;
#22778=CARTESIAN_POINT ( 'NONE',  ( 60.05889968639040433, 14.78467075934760011, -47.76686567462839861 ) ) ;
#22779=CARTESIAN_POINT ( 'NONE',  ( 10.97012820795380073, 33.88053142178789301, -47.22757037167239957 ) ) ;
#22781=CARTESIAN_POINT ( 'NONE',  ( 56.46551567295650642, 19.54378694285259854, -74.14999999999999147 ) ) ;
#22785=CARTESIAN_POINT ( 'NONE',  ( 49.40539548389180879, -53.49785366681999932, -54.15746054660920095 ) ) ;
#22786=ORIENTED_EDGE ( 'NONE', *, *, #12029, .F. ) ;
#22789=CARTESIAN_POINT ( 'NONE',  ( 10.77178238407419997, -63.25331191240289286, -45.20468163478559376 ) ) ;
#22793=CARTESIAN_POINT ( 'NONE',  ( 57.34583854495710398, 19.00625385608790197, -52.73888232642729434 ) ) ;
#22794=CARTESIAN_POINT ( 'NONE',  ( 52.84397956633110027, 19.27108008843849873, -76.72969847962329482 ) ) ;
#22795=ORIENTED_EDGE ( 'NONE', *, *, #22802, .T. ) ;
#22796=CARTESIAN_POINT ( 'NONE',  ( 9.374134760172621483, -64.20245714614587484, -46.81441715244631041 ) ) ;
#22797=B_SPLINE_SURFACE_WITH_KNOTS ( 'NONE', 3, 3, ( 
 ( #44402, #36011, #39958, #8239, #35511, #3806, #126, #27379, #16100, #15600, #24190, #7478, #375, #47574, #16356, #28397 ),
 ( #23427, #39450, #3550, #31553, #27634, #43639, #4824, #13482, #21569, #48858, #44922, #1415, #9023, #37565, #17401, #29440 ),
 ( #12700, #49129, #24967, #12965, #892, #40986, #5099, #5615, #21053, #41245, #20792, #48599, #36785, #49386, #16887, #13228 ),
 ( #1674, #9547, #37054, #25498, #21312, #41501, #33368, #1150, #32832, #45445, #17661, #28653, #33099, #16611, #17147, #5357 ),
 ( #29177, #37313, #45180, #28916, #32569, #44656, #8762, #24711, #25240, #40728, #9293, #12598, #19928, #7894, #20691, #32731 ),
 ( #28042, #39863, #280, #35920, #27537, #36681, #3965, #35, #20436, #31968, #785, #36423, #28560, #16516, #23588, #16264 ),
 ( #16010, #43793, #47989, #12088, #16784, #44047, #44301, #31708, #43543, #47732, #32465, #23840, #32217, #24615, #4726, #8660 ),
 ( #40626, #40369, #11575, #530, #8150, #11837, #48495, #7643, #39606, #20182, #44561, #24094, #28296, #40117, #4210, #8409 ),
 ( #24355, #36172, #3710, #19678, #27797, #35675, #4466, #48241, #51661, #12335, #15754, #48762, #44823, #29845, #29342, #49544 ),
 ( #12866, #6025, #13383, #5763, #13886, #36953, #45344, #49027, #21728, #1571, #25141, #49794, #9697, #21473, #29595, #13636 ),
 ( #17563, #45600, #33531, #25658, #9449, #9189, #21985, #25914, #45866, #9949, #20957, #41660, #41927, #37473, #37734, #18069 ) ),
 .UNSPECIFIED., .F., .F., .F.,
 ( 4, 1, 1, 1, 1, 1, 1, 1, 4 ),
 ( 4, 2, 2, 2, 2, 2, 2, 4 ),
 ( -1.411926611000000059E-06, 0.1250000000000000000, 0.2500000000000000000, 0.3750000000000000000, 0.5000000000000000000, 0.6250000000000000000, 0.7500000000000000000, 0.8750000000000000000, 1.000010174520270079 ),
 ( -0.5134457415475799369, -0.4235843427975279907, -0.3208972293920659968, -0.2567177835136529862, -0.2246280605744469805, -0.1732845038717159836, -0.09113481314734700467, 1.017452027400000023E-05 ),
 .UNSPECIFIED. ) ;
#22798=CARTESIAN_POINT ( 'NONE',  ( 50.97251424797730124, 19.73188950824126309, -76.14992187212315855 ) ) ;
#22799=DIRECTION ( 'NONE',  ( 1.000000000000000000, 0.000000000000000000, 0.000000000000000000 ) ) ;
#22800=CARTESIAN_POINT ( 'NONE',  ( 57.24929578232330130, -50.61618894764249887, -53.91492796143979405 ) ) ;
#22802=EDGE_CURVE ( 'NONE', #19884, #19952, #42234, .T. ) ;
#22807=EDGE_LOOP ( 'NONE', ( #49094, #22281, #5670, #30524 ) ) ;
#22810=TOROIDAL_SURFACE ( 'NONE', #29509, 32.00000000000000000, 1.000000000000000000 ) ;
#22811=CARTESIAN_POINT ( 'NONE',  ( 53.51283228710530437, -49.43204137189339775, -49.22146279461640006 ) ) ;
#22813=DIRECTION ( 'NONE',  ( 0.000000000000000000, 0.000000000000000000, -1.000000000000000000 ) ) ;
#22818=CARTESIAN_POINT ( 'NONE',  ( 53.00983118628400348, -49.38275580526859443, -27.01103834705430273 ) ) ;
#22819=AXIS2_PLACEMENT_3D ( 'NONE', #24892, #44064, #12352 ) ;
#22820=CARTESIAN_POINT ( 'NONE',  ( 55.56519842082970229, -50.87569675573109862, -75.15977926761300409 ) ) ;
#22821=CARTESIAN_POINT ( 'NONE',  ( -10.13547705207719929, 11.41357116503390046, -5.029204105224179600 ) ) ;
#22822=DIRECTION ( 'NONE',  ( -1.000000000000000000, 0.000000000000000000, 0.000000000000000000 ) ) ;
#22823=CARTESIAN_POINT ( 'NONE',  ( 47.61217947097659930, -54.50984741584490223, -54.68372563208449577 ) ) ;
#22824=EDGE_CURVE ( 'NONE', #1802, #40665, #4068, .T. ) ;
#22825=DIRECTION ( 'NONE',  ( 0.3294064756441309472, 0.9441882088883087887, 3.053113317719179500E-16 ) ) ;
#22826=ORIENTED_EDGE ( 'NONE', *, *, #34759, .T. ) ;
#22827=CARTESIAN_POINT ( 'NONE',  ( 52.83011299386760129, -49.66073358055960085, -48.49877547121819532 ) ) ;
#22828=CARTESIAN_POINT ( 'NONE',  ( 47.58649647341519540, 23.31928261732160124, -54.89219699614270098 ) ) ;
#22831=CARTESIAN_POINT ( 'NONE',  ( 61.22425882976509826, 14.43492084046710033, -47.75784053982390276 ) ) ;
#22832=CARTESIAN_POINT ( 'NONE',  ( 11.25424573356439950, 33.80288494388220499, -16.95782968490189901 ) ) ;
#22833=CARTESIAN_POINT ( 'NONE',  ( 52.19989370126119610, 18.55847580453720269, -77.09681678487270062 ) ) ;
#22834=CARTESIAN_POINT ( 'NONE',  ( 52.95585356374179042, 18.36289647769510225, -48.79473315328430516 ) ) ;
#22836=CARTESIAN_POINT ( 'NONE',  ( 55.68173555697770638, 17.70376283165290232, -53.85224183627919814 ) ) ;
#22837=CARTESIAN_POINT ( 'NONE',  ( 52.77991141011769827, 18.45283218612549803, -28.02125929211980093 ) ) ;
#22838=CARTESIAN_POINT ( 'NONE',  ( 49.72648160330989953, 22.41435850158119791, -55.11972614036179863 ) ) ;
#22839=VECTOR ( 'NONE', #4731, 1000.000000000000114 ) ;
#22840=CARTESIAN_POINT ( 'NONE',  ( 54.63655381128389621, -48.05296878824569973, -26.73577887340519865 ) ) ;
#22841=CARTESIAN_POINT ( 'NONE',  ( 52.84346299185870066, 18.45884386080550144, -48.96941050064629763 ) ) ;
#22844=CARTESIAN_POINT ( 'NONE',  ( 10.48773063397930017, 31.94422603044110076, -45.62697307978170613 ) ) ;
#22846=CARTESIAN_POINT ( 'NONE',  ( 17.49475172342960150, 19.88381105532299742, -15.67743212163030186 ) ) ;
#22847=CARTESIAN_POINT ( 'NONE',  ( 66.62839972533728883, -32.95476632565599573, -19.40718689916469941 ) ) ;
#22849=ORIENTED_EDGE ( 'NONE', *, *, #6985, .F. ) ;
#22850=VERTEX_POINT ( 'NONE', #42427 ) ;
#22851=CARTESIAN_POINT ( 'NONE',  ( 41.27829246776259708, 12.87545685813379848, -3.596739354799309840 ) ) ;
#22852=CARTESIAN_POINT ( 'NONE',  ( 76.57339177411788000, 0.8951608601394540621, -13.54367431337692729 ) ) ;
#22854=CARTESIAN_POINT ( 'NONE',  ( 11.36758345312349938, -64.52529782468211295, -45.06392959096150719 ) ) ;
#22855=CARTESIAN_POINT ( 'NONE',  ( 56.78246058254009654, -45.33631709052220060, -25.70543994511969998 ) ) ;
#22857=CARTESIAN_POINT ( 'NONE',  ( 12.08165187759344761, 24.17815767738823141, -22.62772784292297956 ) ) ;
#22859=CARTESIAN_POINT ( 'NONE',  ( 61.29923175484539399, -47.67319342919869740, -45.87705171400279625 ) ) ;
#22861=CARTESIAN_POINT ( 'NONE',  ( 11.73100068668170159, 32.29067168418070111, -24.74706328898560059 ) ) ;
#22863=CARTESIAN_POINT ( 'NONE',  ( 45.90332635223469993, -45.11618894461400231, -7.776724400097649870 ) ) ;
#22867=CARTESIAN_POINT ( 'NONE',  ( 16.44553025965459980, 19.88381305015400002, -20.85618808645970290 ) ) ;
#22869=EDGE_CURVE ( 'NONE', #17592, #11419, #23625, .T. ) ;
#22870=CARTESIAN_POINT ( 'NONE',  ( 60.15822031048740826, -28.97818250310960053, -15.79925957823600058 ) ) ;
#22873=CARTESIAN_POINT ( 'NONE',  ( 46.76359541693670252, -53.62286661502929519, -75.98188598372340152 ) ) ;
#22874=CARTESIAN_POINT ( 'NONE',  ( 44.96327775120639814, 13.88381306199719845, -7.018648154247789428 ) ) ;
#22879=CIRCLE ( 'NONE', #20367, 1.000000000000000888 ) ;
#22880=ADVANCED_FACE ( 'NONE', ( #8062 ), #22810, .T. ) ;
#22881=LINE ( 'NONE', #27339, #32347 ) ;
#22885=CARTESIAN_POINT ( 'NONE',  ( -6.046672580744979264, -47.40279481310589915, -7.123502465237989689 ) ) ;
#22886=CARTESIAN_POINT ( 'NONE',  ( 75.29396857310361213, -8.410730295738069628, -11.50483984771559953 ) ) ;
#22887=CARTESIAN_POINT ( 'NONE',  ( 75.09775766446816192, 13.79064084518985744, -14.73081397881156640 ) ) ;
#22888=EDGE_CURVE ( 'NONE', #9498, #49564, #8582, .T. ) ;
#22890=CARTESIAN_POINT ( 'NONE',  ( 59.13340102237120277, -3.116188944679349593, -15.65754737356207116 ) ) ;
#22892=CARTESIAN_POINT ( 'NONE',  ( 57.49008984609597661, 18.87413028802463089, -52.59398425856332437 ) ) ;
#22893=CARTESIAN_POINT ( 'NONE',  ( 9.633937397696209715, -15.61618894467929941, -22.64999999999999858 ) ) ;
#22894=CARTESIAN_POINT ( 'NONE',  ( 40.87457764023000095, 13.37883080456079909, -4.704571308414649877 ) ) ;
#22897=CARTESIAN_POINT ( 'NONE',  ( 68.13393739769745139, -49.21324915460503036, -70.54648330188275906 ) ) ;
#22899=CARTESIAN_POINT ( 'NONE',  ( 76.13000578349209491, -43.30572666886710209, -13.72134801843236218 ) ) ;
#22900=CARTESIAN_POINT ( 'NONE',  ( 18.09998078254310272, -52.35976395901120384, -75.83262351151699932 ) ) ;
#22901=CARTESIAN_POINT ( 'NONE',  ( 60.86356685786619636, -43.43553833881050252, -9.316062384177440592 ) ) ;
#22904=ORIENTED_EDGE ( 'NONE', *, *, #22675, .F. ) ;
#22908=EDGE_CURVE ( 'NONE', #45765, #46021, #12774, .T. ) ;
#22910=CARTESIAN_POINT ( 'NONE',  ( 43.28342787795109814, -45.55823673264939799, -7.371216836625280600 ) ) ;
#22914=LINE ( 'NONE', #47570, #42780 ) ;
#22916=CARTESIAN_POINT ( 'NONE',  ( 53.59226879024850376, -49.40789622861189656, -49.22934975135349589 ) ) ;
#22921=ORIENTED_EDGE ( 'NONE', *, *, #7682, .F. ) ;
#22925=EDGE_CURVE ( 'NONE', #19324, #7222, #12000, .T. ) ;
#22926=DIRECTION ( 'NONE',  ( 0.000000000000000000, 0.000000000000000000, 1.000000000000000000 ) ) ;
#22927=CARTESIAN_POINT ( 'NONE',  ( 53.43416304911610126, -51.19054688946549447, -75.78314156995350004 ) ) ;
#22928=CARTESIAN_POINT ( 'NONE',  ( 60.27616520369410580, 14.52716031431759980, -47.25859949951769323 ) ) ;
#22931=AXIS2_PLACEMENT_3D ( 'NONE', #21519, #37516, #49590 ) ;
#22932=CARTESIAN_POINT ( 'NONE',  ( 41.53965823250400291, -44.22865657591820110, -4.633657428418399782 ) ) ;
#22933=CARTESIAN_POINT ( 'NONE',  ( 65.10753607264098264, 0.7662848317789809904, -17.50331135171781227 ) ) ;
#22934=CARTESIAN_POINT ( 'NONE',  ( -4.852296971786230095, 16.18044332419180265, -5.030532656363839727 ) ) ;
#22938=CARTESIAN_POINT ( 'NONE',  ( 17.92370450339669929, -51.11618894467930119, -74.14999999999999147 ) ) ;
#22940=ORIENTED_EDGE ( 'NONE', *, *, #36645, .T. ) ;
#22941=DIRECTION ( 'NONE',  ( 0.3445670372598625963, -0.6174735272333260472, -0.7071067811865442421 ) ) ;
#22942=CARTESIAN_POINT ( 'NONE',  ( 57.31868460842820667, 19.28698455871409934, -53.29708888710140258 ) ) ;
#22947=CARTESIAN_POINT ( 'NONE',  ( 14.73074138134250077, 19.35333670681460205, -20.78918949795229665 ) ) ;
#22948=CARTESIAN_POINT ( 'NONE',  ( 46.74845599210109981, -53.81985652269789711, -75.90842213619210099 ) ) ;
#22950=CARTESIAN_POINT ( 'NONE',  ( 48.03526516117440082, -54.27886751425110390, -54.71370355240560457 ) ) ;
#22953=CARTESIAN_POINT ( 'NONE',  ( 47.84600491270340683, 23.14802384070760155, -54.72009433156399894 ) ) ;
#22956=EDGE_LOOP ( 'NONE', ( #26157, #35110, #31775, #37369, #191, #7272 ) ) ;
#22958=CARTESIAN_POINT ( 'NONE',  ( 60.60266389430760370, -45.58847639179440137, -47.13124125531790298 ) ) ;
#22959=CARTESIAN_POINT ( 'NONE',  ( 59.52869175205803032, 14.25746298374641441, -26.73578769780420572 ) ) ;
#22961=CARTESIAN_POINT ( 'NONE',  ( 57.50723798014340105, 13.88381064843590096, -25.33268340738889890 ) ) ;
#22964=CARTESIAN_POINT ( 'NONE',  ( 59.52869410915831594, -45.48984219772450643, -26.73579121603098585 ) ) ;
#22967=ORIENTED_EDGE ( 'NONE', *, *, #16556, .F. ) ;
#22973=CARTESIAN_POINT ( 'NONE',  ( 11.76101335022769945, -64.89508155409039603, -16.31614116036690021 ) ) ;
#22975=CARTESIAN_POINT ( 'NONE',  ( 76.42375628065715887, -22.57305820191152890, -12.89887670999500102 ) ) ;
#22976=CARTESIAN_POINT ( 'NONE',  ( 10.10021300068440020, -64.40744690142780371, -46.68963158283009562 ) ) ;
#22978=EDGE_LOOP ( 'NONE', ( #34535, #20169, #17915, #37428 ) ) ;
#22980=CARTESIAN_POINT ( 'NONE',  ( 56.87601579295709797, 14.74005962510780066, -26.24549083051520171 ) ) ;
#22981=DIRECTION ( 'NONE',  ( 0.5721078732755690011, 0.8201783838507971103, 0.000000000000000000 ) ) ;
#22983=CARTESIAN_POINT ( 'NONE',  ( 60.05814672930910092, -1.519238805058580111, -15.90733267895319969 ) ) ;
#22984=CARTESIAN_POINT ( 'NONE',  ( 51.62537655945009618, -49.19526475647730024, -76.81862610561158533 ) ) ;
#22985=CARTESIAN_POINT ( 'NONE',  ( 59.61233446001679681, -47.78174833862750148, -50.05788297521610275 ) ) ;
#22994=CARTESIAN_POINT ( 'NONE',  ( 13.61471636588469991, -51.00593421810309991, -21.87339661680830361 ) ) ;
#22997=CARTESIAN_POINT ( 'NONE',  ( 56.89868990065399856, 13.89633980461660023, -16.37351210530319889 ) ) ;
#22998=CARTESIAN_POINT ( 'NONE',  ( 61.12579551892830665, -45.35598161261900430, -47.14991131457540519 ) ) ;
#23004=CARTESIAN_POINT ( 'NONE',  ( 47.11719193978310471, 22.63726203342839582, -75.76637087395009473 ) ) ;
#23006=CARTESIAN_POINT ( 'NONE',  ( 44.02992521606390142, -46.06978035797460080, -8.311541264417458663 ) ) ;
#23008=CARTESIAN_POINT ( 'NONE',  ( 17.73211690492210479, 20.42331746234410161, -75.51793353176734058 ) ) ;
#23012=CARTESIAN_POINT ( 'NONE',  ( 82.34961391206009296, 14.41937359025589949, -47.73425003811119893 ) ) ;
#23016=CIRCLE ( 'NONE', #13840, 3.500000000000003109 ) ;
#23018=CARTESIAN_POINT ( 'NONE',  ( 48.90562224917519529, 22.57469039213979656, -54.45244080928650021 ) ) ;
#23019=ORIENTED_EDGE ( 'NONE', *, *, #31311, .F. ) ;
#23020=CARTESIAN_POINT ( 'NONE',  ( 53.45905338263879969, -49.36511705999589594, -49.00044516267050199 ) ) ;
#23024=CARTESIAN_POINT ( 'NONE',  ( 13.92801754442050033, 19.97389345108679848, -22.96894029843029728 ) ) ;
#23025=CARTESIAN_POINT ( 'NONE',  ( 51.68229386145609539, -48.76553798961150221, -77.01557736628760154 ) ) ;
#23027=CARTESIAN_POINT ( 'NONE',  ( 52.84810394027419989, 18.43930803410469821, -48.89993304137779973 ) ) ;
#23028=CARTESIAN_POINT ( 'NONE',  ( 54.79773977241499949, -46.08976703690969146, -15.91708512117589969 ) ) ;
#23030=EDGE_CURVE ( 'NONE', #12954, #22246, #8312, .T. ) ;
#23031=ORIENTED_EDGE ( 'NONE', *, *, #20069, .T. ) ;
#23034=EDGE_CURVE ( 'NONE', #46345, #38625, #16160, .T. ) ;
#23036=CARTESIAN_POINT ( 'NONE',  ( 10.22879563217340149, 33.47692832875780056, -46.94094174653320550 ) ) ;
#23039=CARTESIAN_POINT ( 'NONE',  ( 47.94507282302989637, -54.66591535502590204, -55.53467711414020158 ) ) ;
#23040=CARTESIAN_POINT ( 'NONE',  ( 53.05489980299899599, -49.59988638911212178, -49.10811587859365801 ) ) ;
#23043=CARTESIAN_POINT ( 'NONE',  ( 52.83236252576280378, -52.32374954317370452, -54.28770559089719683 ) ) ;
#23047=CARTESIAN_POINT ( 'NONE',  ( 10.77397357765519814, -63.36960133942959317, -45.20699438509760171 ) ) ;
#23048=CARTESIAN_POINT ( 'NONE',  ( 68.13393739769819035, 19.47158195952289717, -70.40645085170196182 ) ) ;
#23049=EDGE_LOOP ( 'NONE', ( #30975, #847, #10166, #41119, #16459 ) ) ;
#23051=CARTESIAN_POINT ( 'NONE',  ( 57.03355800488689908, 19.22800892903980241, -53.04057970399039590 ) ) ;
#23052=CARTESIAN_POINT ( 'NONE',  ( 52.23775048363239648, 18.59126050118990037, -77.10775523732289116 ) ) ;
#23053=ORIENTED_EDGE ( 'NONE', *, *, #50213, .T. ) ;
#23054=CARTESIAN_POINT ( 'NONE',  ( 10.13693647382719476, -64.73981908136153152, -47.01156320461868887 ) ) ;
#23056=CARTESIAN_POINT ( 'NONE',  ( 14.58506229057406678, 20.56215755416807056, -75.65677362359035385 ) ) ;
#23059=B_SPLINE_SURFACE_WITH_KNOTS ( 'NONE', 3, 3, ( 
 ( #34627, #50632, #22827, #48244, #48499, #8413, #7897, #284, #24358, #534, #4470, #28045, #36426, #23844, #36177, #39867, #12092, #16268, #3968, #39609, #35409, #12602, #16520, #20439, #51664, #44050, #4213, #32468, #27801, #15757 ),
 ( #15506, #28563, #40, #20186, #40120, #40372, #43798, #44564, #28301, #8665, #7648, #16015, #19684, #44304, #24098, #47736, #24620, #32221, #8154, #12339, #40630, #19429, #51410, #31460, #47484, #11579, #31972, #31711, #27541, #11842 ),
 ( #19931, #43547, #23592, #35679, #3713, #35923, #47992, #25917, #16788, #33007, #1576, #45870, #33787, #17815, #45349, #37225, #33534, #44827, #49030, #17311, #49798, #29346, #24878, #45083, #13889, #21477, #20960, #9453, #5767, #13137 ),
 ( #36685, #40888, #25661, #1058, #25402, #29848, #9953, #1836, #21214, #4730, #49551, #20696, #45603, #9193, #37477, #9700, #37739, #41664, #13387, #21732, #25144, #17567, #41148, #49289, #13639, #5263, #4999, #788, #32736, #48765 ),
 ( #41404, #5522, #12869, #29087, #17053, #28825, #8934, #36958, #1322, #33274, #29599, #6811, #14402, #42716, #46396, #22764, #10484, #38519, #22247, #21989, #26439, #31142, #46912, #34304, #37999, #14144, #30883, #10998, #11256, #26693 ),
 ( #18844, #2618, #2349, #26965, #50317, #38784, #19103, #2096, #18072, #42455, #42975, #34826, #41931, #39041, #50828, #51084, #3136, #50050, #30630, #10223, #47168, #42193, #38256, #14920, #6543, #18322, #46133, #7070, #23020, #35080 ),
 ( #2876, #6291, #46655, #15182, #30371, #6030, #34041, #30114, #22507, #10738, #26182, #18588, #34566, #50571, #14661, #15695, #36118, #47674, #473, #220, #44240, #32162, #39289, #15956, #31650, #19622, #7584, #11778, #27737, #36365 ),
 ( #35863, #43736, #16460, #48178, #35612, #23270, #51346, #16204, #12280, #48438, #12032, #32415, #43230, #11517, #28242, #8093, #19364, #7837, #47931, #23530, #31909, #51854, #27477, #35345, #8345, #27985, #27218, #3397, #3651, #24037 ),
 ( #47424, #7323, #43479, #39547, #20125, #23786, #51600, #31397, #24298, #40313, #4409, #20376, #15444, #39801, #3908, #43987, #19872, #4150, #40058, #37695, #42151, #50532, #33494, #30333, #25619, #42414, #41622, #34002, #2054, #14103 ),
 ( #26395, #10699, #38746, #45826, #6249, #37958, #41890, #10180, #8052, #30843, #48027, #7359, #19404, #24335, #4703, #1295, #36934, #41635, #26153, #47079, #643, #1167, #40935, #10268, #41978, #34350, #50094, #1622, #45913, #26227 ),
 ( #33321, #13685, #45650, #45131, #9243, #1365, #29393, #25705, #17613, #6078, #21781, #37787, #1884, #49846, #38047, #11562, #27521, #50361, #46701, #46439, #30417, #26485, #38567, #27013, #51135, #47214, #3440, #22811, #18634, #7367 ),
 ( #6859, #14706, #38830, #14964, #23067, #39087, #27263, #35392, #16502, #264, #16767, #12851, #40872, #44283, #32719, #36667, #35657, #31949, #11820, #51644, #43777, #48746, #32203, #515, #32454, #40611, #24598, #3952, #4710, #49780 ),
 ( #1303, #9169, #9435, #20944, #25126, #9681, #41385, #5502, #49270, #1556, #49529, #41643, #21708, #29829, #37718, #45849, #4882, #23993, #12488, #36580, #12232, #20586, #40524, #32114, #4101, #16947, #4615, #15907, #43943, #20330 ),
 ( #32892, #36071, #21113, #16415, #28978, #9079, #25027, #29497, #5409, #46287, #22403, #1211, #42082, #21367, #45501, #21620, #17969, #9599, #30002, #41556, #37624, #25808, #33681, #45761, #41815, #5922, #37895, #2506, #3027, #22916 ) ),
 .UNSPECIFIED., .F., .F., .F.,
 ( 4, 1, 1, 1, 1, 1, 1, 1, 3, 4 ),
 ( 4, 2, 2, 2, 2, 2, 2, 2, 2, 2, 2, 2, 2, 2, 4 ),
 ( 0.000000000000000000, 0.1250000000000000000, 0.2500000000000000000, 0.3750000000000000000, 0.5000000000000000000, 0.6250000000000000000, 0.7500000000000000000, 0.8750000000000000000, 1.000000000000000000, 1.010000000000000009 ),
 ( 0.000000000000000000, 0.03744778849575899904, 0.1081480782291359966, 0.1523357593124970155, 0.1872251531838270144, 0.2221145470551559864, 0.2911210082761750417, 0.3342500465393130060, 0.3773790848024499711, 0.4312903826313710387, 0.4852016804602920508, 0.5714597569865660365, 0.6485380782585299375, 0.7718633922936719571, 0.8625807652627420774 ),
 .UNSPECIFIED. ) ;
#23064=ORIENTED_EDGE ( 'NONE', *, *, #3726, .F. ) ;
#23067=CARTESIAN_POINT ( 'NONE',  ( 52.60226675332729940, -49.82835823082800175, -48.60906011901539614 ) ) ;
#23068=CARTESIAN_POINT ( 'NONE',  ( 51.75217146182449568, 13.88381105532070059, -11.53056162543830077 ) ) ;
#23072=CARTESIAN_POINT ( 'NONE',  ( 45.14276133008436886, -45.91161332868410483, -8.929567349377213858 ) ) ;
#23073=CARTESIAN_POINT ( 'NONE',  ( 68.13393739769847457, -50.70395984887981200, -74.34354914830335304 ) ) ;
#23074=CARTESIAN_POINT ( 'NONE',  ( 12.16231664502929988, 33.44509448364060233, -15.91745067705889838 ) ) ;
#23077=CARTESIAN_POINT ( 'NONE',  ( 54.75911359420950220, -47.36916784795560176, -25.73144026446449928 ) ) ;
#23079=CARTESIAN_POINT ( 'NONE',  ( 54.87218746053860485, -50.87499351157259753, -75.61051383423139782 ) ) ;
#23080=CARTESIAN_POINT ( 'NONE',  ( -3.348521525975739710, 18.94928180732459921, -7.645520396857000023 ) ) ;
#23081=CARTESIAN_POINT ( 'NONE',  ( 47.81335647225210295, 23.16511464041720103, -54.71582838624409817 ) ) ;
#23082=CARTESIAN_POINT ( 'NONE',  ( 47.42962603948429745, -54.62656463334229784, -54.65340493925440057 ) ) ;
#23086=CARTESIAN_POINT ( 'NONE',  ( 47.73137043576249994, 23.21653874435460096, -54.73785977659620272 ) ) ;
#23089=CARTESIAN_POINT ( 'NONE',  ( 61.06116337346599465, 14.20715986148650067, -47.36084287260779746 ) ) ;
#23091=CARTESIAN_POINT ( 'NONE',  ( 51.24580074018999198, 18.16659437971649993, -76.45613186000909423 ) ) ;
#23092=CARTESIAN_POINT ( 'NONE',  ( 52.87376177351259798, 18.40584817417369834, -48.72414004473989735 ) ) ;
#23093=CARTESIAN_POINT ( 'NONE',  ( 61.04001029137710077, -45.35933836075930259, -46.86320535112459851 ) ) ;
#23095=CARTESIAN_POINT ( 'NONE',  ( 56.02491708892659972, 15.50432384546050102, -26.35756105441370067 ) ) ;
#23096=EDGE_CURVE ( 'NONE', #15061, #38484, #11164, .T. ) ;
#23097=CARTESIAN_POINT ( 'NONE',  ( 49.53395860104499349, 22.37801950097359693, -54.45855173817810169 ) ) ;
#23099=CARTESIAN_POINT ( 'NONE',  ( 52.74562310603300119, 18.50712734077499988, -48.86764753959050012 ) ) ;
#23100=CARTESIAN_POINT ( 'NONE',  ( 59.85389437514099598, -29.73929060095769827, -15.91137588707199768 ) ) ;
#23102=CYLINDRICAL_SURFACE ( 'NONE', #32563, 1.999999999999998224 ) ;
#23105=DIRECTION ( 'NONE',  ( 1.000000000000000000, 8.008164437427536525E-27, -1.590235242698479852E-09 ) ) ;
#23108=ORIENTED_EDGE ( 'NONE', *, *, #39684, .T. ) ;
#23110=CARTESIAN_POINT ( 'NONE',  ( 41.83063930790589779, 12.37849180622510126, -3.362295849109719903 ) ) ;
#23113=CARTESIAN_POINT ( 'NONE',  ( 55.90097409207919554, -45.92300129936620579, -25.39712007592949661 ) ) ;
#23120=CARTESIAN_POINT ( 'NONE',  ( 41.33192604761929800, -44.75281548107679441, -5.349971310512899869 ) ) ;
#23122=EDGE_CURVE ( 'NONE', #6528, #7222, #41468, .T. ) ;
#23125=CYLINDRICAL_SURFACE ( 'NONE', #32991, 1.999999999999999112 ) ;
#23126=DIRECTION ( 'NONE',  ( 0.000000000000000000, 0.000000000000000000, -1.000000000000000000 ) ) ;
#23127=EDGE_CURVE ( 'NONE', #43345, #11471, #21653, .T. ) ;
#23129=CARTESIAN_POINT ( 'NONE',  ( 59.34396388824480084, -28.26380901204359830, -15.68000386546350100 ) ) ;
#23131=CARTESIAN_POINT ( 'NONE',  ( 47.21533240379599761, -54.54479670161060056, -75.00425604315580586 ) ) ;
#23132=CARTESIAN_POINT ( 'NONE',  ( 55.22142780376210425, 14.83850043050260048, -16.34787572981039716 ) ) ;
#23134=CARTESIAN_POINT ( 'NONE',  ( 83.66059785054299880, -44.84460576056169856, -47.23564833931240514 ) ) ;
#23139=CARTESIAN_POINT ( 'NONE',  ( 11.51160566532390028, -51.12796951774690513, -23.15000000000000213 ) ) ;
#23140=CARTESIAN_POINT ( 'NONE',  ( 9.416484201958351008, -63.56992309908239491, -16.81318693889570071 ) ) ;
#23141=CARTESIAN_POINT ( 'NONE',  ( 76.17746443069590612, -21.84911981489240063, -12.19081726112320041 ) ) ;
#23143=CARTESIAN_POINT ( 'NONE',  ( 75.40236786212628317, -44.30595597757749005, -13.67333791107008523 ) ) ;
#23144=CARTESIAN_POINT ( 'NONE',  ( 12.73487495346794240, -55.47150669537813883, -75.56421462368682285 ) ) ;
#23146=CARTESIAN_POINT ( 'NONE',  ( 82.34446664224419976, -45.60532208362960205, -47.68359978794560305 ) ) ;
#23147=CARTESIAN_POINT ( 'NONE',  ( 57.31173127953859847, -50.51960560014510548, -53.29728758193470384 ) ) ;
#23148=CARTESIAN_POINT ( 'NONE',  ( 43.01559835719159963, 11.40977387627630080, -3.897419375871189917 ) ) ;
#23150=CARTESIAN_POINT ( 'NONE',  ( 63.36072709640390599, -45.11618894467940066, -12.04575099730080012 ) ) ;
#23153=CARTESIAN_POINT ( 'NONE',  ( 66.70613787219339486, -1.460923002439210139, -17.03146698529479863 ) ) ;
#23154=CARTESIAN_POINT ( 'NONE',  ( 18.65170598449359929, -51.88814251562649815, -75.11575902015950135 ) ) ;
#23155=CARTESIAN_POINT ( 'NONE',  ( 41.36014816789919735, -44.98000569772389667, -5.614915768826699960 ) ) ;
#23159=CARTESIAN_POINT ( 'NONE',  ( 8.784728771152188642, 31.88305279702909800, -46.67204636145419983 ) ) ;
#23164=CARTESIAN_POINT ( 'NONE',  ( 45.18452560921219430, -45.82136313292339480, -8.866308695862619160 ) ) ;
#23165=ORIENTED_EDGE ( 'NONE', *, *, #36788, .T. ) ;
#23166=CARTESIAN_POINT ( 'NONE',  ( 17.21347160910339724, 21.88381105532300097, -76.14999999999999147 ) ) ;
#23167=ORIENTED_EDGE ( 'NONE', *, *, #32590, .F. ) ;
#23175=VERTEX_POINT ( 'NONE', #13800 ) ;
#23176=DIRECTION ( 'NONE',  ( 1.000000000000000000, 0.000000000000000000, 0.000000000000000000 ) ) ;
#23180=DIRECTION ( 'NONE',  ( -0.8857883891771971552, 0.4640893551880569956, 0.000000000000000000 ) ) ;
#23181=CARTESIAN_POINT ( 'NONE',  ( 53.19108586364980340, -51.21468528679280041, -75.83523861080040263 ) ) ;
#23182=CARTESIAN_POINT ( 'NONE',  ( 60.66118264286809847, 14.41976552486340069, -47.55100573580950396 ) ) ;
#23186=CARTESIAN_POINT ( 'NONE',  ( -6.917132356002309912, 14.81246362652350079, -5.581884250354890220 ) ) ;
#23187=CARTESIAN_POINT ( 'NONE',  ( 46.52115705324671779, 22.06631441008168792, -76.11314270329992837 ) ) ;
#23191=CARTESIAN_POINT ( 'NONE',  ( 56.82514455556469812, -50.66164335286360654, -53.84957932322389951 ) ) ;
#23192=CARTESIAN_POINT ( 'NONE',  ( 57.55751162087899786, 19.21837686176930049, -53.12582022096169965 ) ) ;
#23193=UNCERTAINTY_MEASURE_WITH_UNIT (LENGTH_MEASURE( 1.000000000000000082E-05 ), #24024, 'distance_accuracy_value', 'NONE');
#23196=CARTESIAN_POINT ( 'NONE',  ( 15.80830505657939966, 19.69806453318900097, -20.14990715359050100 ) ) ;
#23200=CARTESIAN_POINT ( 'NONE',  ( 75.13393739769618662, -43.11618894467930119, -84.38499399519520239 ) ) ;
#23201=CARTESIAN_POINT ( 'NONE',  ( 48.75008997992030402, -54.05277686579759688, -55.10220984819350321 ) ) ;
#23203=EDGE_CURVE ( 'NONE', #21823, #25078, #27029, .T. ) ;
#23205=DIRECTION ( 'NONE',  ( 0.3294064756441053565, -0.9441882088883176705, 9.436895709313929201E-16 ) ) ;
#23206=ORIENTED_EDGE ( 'NONE', *, *, #17049, .T. ) ;
#23208=ADVANCED_FACE ( 'NONE', ( #968 ), #28996, .T. ) ;
#23209=ORIENTED_EDGE ( 'NONE', *, *, #40756, .F. ) ;
#23210=CARTESIAN_POINT ( 'NONE',  ( 17.36506586026114363, 21.76199782478837008, -76.14999999999999147 ) ) ;
#23212=CARTESIAN_POINT ( 'NONE',  ( 49.20993668789943598, -53.61219117315735616, -54.26298610208210249 ) ) ;
#23213=COLOUR_RGB ( '', 0.72549020, 0.75294118, 0.79215686) ;
#23214=DIRECTION ( 'NONE',  ( 0.000000000000000000, 1.000000000000000000, 0.000000000000000000 ) ) ;
#23218=ADVANCED_FACE ( 'NONE', ( #21383 ), #6760, .T. ) ;
#23221=ORIENTED_EDGE ( 'NONE', *, *, #11130, .F. ) ;
#23223=EDGE_LOOP ( 'NONE', ( #33239, #13444, #5223, #23358 ) ) ;
#23224=VECTOR ( 'NONE', #21814, 1000.000000000000000 ) ;
#23228=CARTESIAN_POINT ( 'NONE',  ( 31.69621505835715070, -15.61618894406255187, -7.049999999955885777 ) ) ;
#23229=CARTESIAN_POINT ( 'NONE',  ( 10.21539763879230023, -64.50324338944329838, -46.72617082249710307 ) ) ;
#23233=CARTESIAN_POINT ( 'NONE',  ( 57.15892657999940241, -45.14675268583049927, -25.30896480302860141 ) ) ;
#23234=CARTESIAN_POINT ( 'NONE',  ( 56.45387226280909942, -50.77876243562330671, -53.73846350693940366 ) ) ;
#23236=CARTESIAN_POINT ( 'NONE',  ( 59.54599179390969965, -1.644003503891439788, -15.85381421209810071 ) ) ;
#23237=EDGE_CURVE ( 'NONE', #31153, #5028, #26170, .T. ) ;
#23238=CARTESIAN_POINT ( 'NONE',  ( 52.04690325057050160, -49.64260248550559851, -77.05403615378560289 ) ) ;
#23239=CARTESIAN_POINT ( 'NONE',  ( 59.16562437307299405, -48.30719178829460247, -50.63109401121659658 ) ) ;
#23243=DIRECTION ( 'NONE',  ( 0.000000000000000000, 0.000000000000000000, 1.000000000000000000 ) ) ;
#23246=CARTESIAN_POINT ( 'NONE',  ( 13.19554430041099913, -50.05398002221009790, -21.01912116497090111 ) ) ;
#23247=CARTESIAN_POINT ( 'NONE',  ( 54.26063908242769429, 19.39368898450049983, -76.71671800660969609 ) ) ;
#23249=CARTESIAN_POINT ( 'NONE',  ( 56.41668308765360251, 14.04457932355130012, -16.58850673112480223 ) ) ;
#23250=CARTESIAN_POINT ( 'NONE',  ( 61.09295143732159517, -45.56367091068960207, -47.61628434988689662 ) ) ;
#23251=CARTESIAN_POINT ( 'NONE',  ( 56.84933714557369910, -50.65633608292760215, -53.71862200040009583 ) ) ;
#23256=EDGE_LOOP ( 'NONE', ( #4607, #5055, #50141, #30466 ) ) ;
#23257=CARTESIAN_POINT ( 'NONE',  ( 46.37947015913910320, 21.71088129859489868, -76.14999999999999147 ) ) ;
#23260=CARTESIAN_POINT ( 'NONE',  ( 17.74774429082748384, 20.37931109195205792, -75.46937998419048199 ) ) ;
#23261=CARTESIAN_POINT ( 'NONE',  ( 64.36502057692270284, 13.88381105532070059, -12.32037188644589953 ) ) ;
#23262=CARTESIAN_POINT ( 'NONE',  ( 46.70520323956110076, -53.35084480228680093, -76.07728942632040514 ) ) ;
#23263=CARTESIAN_POINT ( 'NONE',  ( 82.55450662793859351, 14.39374320518479955, -47.70628961803360113 ) ) ;
#23267=CARTESIAN_POINT ( 'NONE',  ( 49.21898449315310131, 22.63053291997670158, -55.19912396961220225 ) ) ;
#23270=CARTESIAN_POINT ( 'NONE',  ( 52.67786065000549911, -49.76447174785660366, -48.65293559773409982 ) ) ;
#23271=EDGE_LOOP ( 'NONE', ( #22472, #48189, #25607, #42456 ) ) ;
#23274=CARTESIAN_POINT ( 'NONE',  ( 13.72891134303729999, 20.05318723622899668, -22.65898119229509788 ) ) ;
#23277=CARTESIAN_POINT ( 'NONE',  ( 52.62897435024740389, 18.57025500941220031, -48.60270736271959890 ) ) ;
#23278=EDGE_CURVE ( 'NONE', #39996, #16045, #37905, .T. ) ;
#23279=CARTESIAN_POINT ( 'NONE',  ( 55.96902840122019995, -45.83494316293919724, -17.93019966846399882 ) ) ;
#23280=CARTESIAN_POINT ( 'NONE',  ( 52.67986940689019804, 18.50721041040169723, -27.55370633776830047 ) ) ;
#23281=ORIENTED_EDGE ( 'NONE', *, *, #37866, .T. ) ;
#23284=CARTESIAN_POINT ( 'NONE',  ( 10.86720904402820054, -64.97138516849830125, -17.53558607436760042 ) ) ;
#23285=CARTESIAN_POINT ( 'NONE',  ( 8.892600493579569942, 32.33025239218060420, -46.69114580456879793 ) ) ;
#23287=CARTESIAN_POINT ( 'NONE',  ( 52.94422481404690473, -50.11505731177610556, -50.07963147481419952 ) ) ;
#23290=VECTOR ( 'NONE', #23180, 999.9999999999998863 ) ;
#23291=VECTOR ( 'NONE', #8113, 1000.000000000000000 ) ;
#23294=CARTESIAN_POINT ( 'NONE',  ( 10.48902586684800120, -63.20932193476740224, -45.62615988541170253 ) ) ;
#23295=CARTESIAN_POINT ( 'NONE',  ( 65.43393739769584272, 16.88381105532339532, -68.79999999999942872 ) ) ;
#23297=CARTESIAN_POINT ( 'NONE',  ( 68.38971107296249841, -30.11618894467929763, -18.15384911730639672 ) ) ;
#23298=CARTESIAN_POINT ( 'NONE',  ( 56.72454650675000210, 19.42863887235380105, -53.46416969237759531 ) ) ;
#23299=CARTESIAN_POINT ( 'NONE',  ( 52.28361328024040233, 18.56717822572520404, -77.20042836414900478 ) ) ;
#23302=CARTESIAN_POINT ( 'NONE',  ( -21.86606260230379917, -15.61618894467929408, 1.600000000000000089 ) ) ;
#23304=DIRECTION ( 'NONE',  ( 0.000000000000000000, 1.000000000000000000, 0.000000000000000000 ) ) ;
#23308=EDGE_LOOP ( 'NONE', ( #44604, #36215, #24536, #20921 ) ) ;
#23310=CARTESIAN_POINT ( 'NONE',  ( 47.26610112325450075, -54.05804861832230301, -75.56421356201970241 ) ) ;
#23316=CARTESIAN_POINT ( 'NONE',  ( 46.37248745885530354, 21.71508437276260040, -76.14999999999999147 ) ) ;
#23318=EDGE_CURVE ( 'NONE', #9892, #28507, #40999, .T. ) ;
#23320=CARTESIAN_POINT ( 'NONE',  ( 11.98171981665849906, 33.81671209943120004, -16.46086821534060007 ) ) ;
#23326=CARTESIAN_POINT ( 'NONE',  ( 55.54166167750689453, -50.64959640008070352, -75.92050756598530370 ) ) ;
#23327=CARTESIAN_POINT ( 'NONE',  ( 0.4348764806820569762, 21.36561379262120042, -7.218237925363110818 ) ) ;
#23331=LINE ( 'NONE', #8151, #13088 ) ;
#23335=CARTESIAN_POINT ( 'NONE',  ( 47.59457368048200721, 23.32277084168419989, -55.07961569987379846 ) ) ;
#23340=CARTESIAN_POINT ( 'NONE',  ( 51.34919120559619188, 18.37200898748080036, -76.46527063284669623 ) ) ;
#23341=CARTESIAN_POINT ( 'NONE',  ( 52.88990462379319979, 18.39739278198799965, -48.74279802066659784 ) ) ;
#23342=ADVANCED_FACE ( 'NONE', ( #21580 ), #29293, .T. ) ;
#23343=CARTESIAN_POINT ( 'NONE',  ( 78.22251691734010137, 1.883811055320649963, -20.65000000000000213 ) ) ;
#23344=CARTESIAN_POINT ( 'NONE',  ( 52.87578377016760101, -49.63680538124820885, -48.67531175415540190 ) ) ;
#23345=CARTESIAN_POINT ( 'NONE',  ( 51.04520179763379417, 21.63149099170350098, -53.86124592026170177 ) ) ;
#23347=CARTESIAN_POINT ( 'NONE',  ( 8.978915886419921222, -63.28580153388660534, -46.63388789120410394 ) ) ;
#23349=CARTESIAN_POINT ( 'NONE',  ( 63.76915202389999138, -31.63922660026030087, -17.09407974168160038 ) ) ;
#23352=DIRECTION ( 'NONE',  ( 0.000000000000000000, 0.000000000000000000, -1.000000000000000000 ) ) ;
#23355=VERTEX_POINT ( 'NONE', #10596 ) ;
#23358=ORIENTED_EDGE ( 'NONE', *, *, #23096, .T. ) ;
#23359=CARTESIAN_POINT ( 'NONE',  ( 57.22147638113349899, -45.13525055360219795, -25.38212350801009975 ) ) ;
#23361=TOROIDAL_SURFACE ( 'NONE', #42666, 23.00000000000000000, 1.000000000000000000 ) ;
#23362=ORIENTED_EDGE ( 'NONE', *, *, #22165, .F. ) ;
#23364=CIRCLE ( 'NONE', #4152, 1.999999999999419131 ) ;
#23366=CARTESIAN_POINT ( 'NONE',  ( 11.00351569080370062, 32.38571639576179706, -24.01957829310750014 ) ) ;
#23369=ORIENTED_EDGE ( 'NONE', *, *, #6699, .F. ) ;
#23371=FACE_OUTER_BOUND ( 'NONE', #44699, .T. ) ;
#23374=CARTESIAN_POINT ( 'NONE',  ( 62.88919424588500107, -30.09987604331610100, -16.25000278776590079 ) ) ;
#23375=CARTESIAN_POINT ( 'NONE',  ( 14.46046508473829739, 20.21129459968669906, -75.25166008039606425 ) ) ;
#23376=CARTESIAN_POINT ( 'NONE',  ( 46.58185961912909789, -53.30757753662899745, -76.10130133987269119 ) ) ;
#23379=CARTESIAN_POINT ( 'NONE',  ( 42.70760066071729710, 14.62349772956079974, -7.311903287840700649 ) ) ;
#23383=CARTESIAN_POINT ( 'NONE',  ( 83.68633570933860710, -44.57328881918749630, -46.84648411755270558 ) ) ;
#23384=CARTESIAN_POINT ( 'NONE',  ( 61.71847798149180164, 13.88380456764680027, -28.01475703387260197 ) ) ;
#23388=CARTESIAN_POINT ( 'NONE',  ( 13.95190178771889933, -50.80797314161940648, -21.48693983945890196 ) ) ;
#23389=CARTESIAN_POINT ( 'NONE',  ( 75.28448646084041229, -21.88343552876009923, -11.45926160344929912 ) ) ;
#23391=LINE ( 'NONE', #16070, #10599 ) ;
#23392=AXIS2_PLACEMENT_3D ( 'NONE', #29506, #34466, #45254 ) ;
#23393=AXIS2_PLACEMENT_3D ( 'NONE', #7806, #32646, #698 ) ;
#23396=CARTESIAN_POINT ( 'NONE',  ( 47.18324198357279897, 23.57489020266570279, -54.61058319554400242 ) ) ;
#23399=CARTESIAN_POINT ( 'NONE',  ( 57.33583209739280306, -50.39857923248089833, -53.00720873729819971 ) ) ;
#23401=CARTESIAN_POINT ( 'NONE',  ( 43.83393256038859676, 12.23250093112789827, -5.056952191481049574 ) ) ;
#23403=EDGE_CURVE ( 'NONE', #26843, #35884, #24470, .T. ) ;
#23405=CARTESIAN_POINT ( 'NONE',  ( 59.82327988359549664, -45.99681751185720202, -47.29966340866579344 ) ) ;
#23406=CARTESIAN_POINT ( 'NONE',  ( 68.13393739769649926, -48.11618894467630270, -70.54999999999999716 ) ) ;
#23407=AXIS2_PLACEMENT_3D ( 'NONE', #6051, #34322, #2113 ) ;
#23409=CARTESIAN_POINT ( 'NONE',  ( 18.14469253414399930, -51.80504026018019914, -75.54815173289030383 ) ) ;
#23411=CARTESIAN_POINT ( 'NONE',  ( 41.58072008512179707, -43.56399069942670366, -4.585251495889560047 ) ) ;
#23415=EDGE_LOOP ( 'NONE', ( #23221, #50787, #50358, #40914 ) ) ;
#23416=CARTESIAN_POINT ( 'NONE',  ( 45.64759345662743328, 13.96552997495392390, -8.164371371256416765 ) ) ;
#23422=CARTESIAN_POINT ( 'NONE',  ( 17.28335488448169954, 21.70396400196510100, -76.14999999999999147 ) ) ;
#23425=CARTESIAN_POINT ( 'NONE',  ( 57.48392795645190034, -45.11618894467940066, -17.43413289997389981 ) ) ;
#23427=CARTESIAN_POINT ( 'NONE',  ( 61.48313195732390568, 14.13204578777779830, -47.33728109067860146 ) ) ;
#23428=ORIENTED_EDGE ( 'NONE', *, *, #6922, .T. ) ;
#23433=VECTOR ( 'NONE', #17156, 1000.000000000000000 ) ;
#23434=AXIS2_PLACEMENT_3D ( 'NONE', #32436, #749, #36917 ) ;
#23437=CARTESIAN_POINT ( 'NONE',  ( 53.35840066752189870, -51.38288175838889771, -75.63634975937459615 ) ) ;
#23439=CARTESIAN_POINT ( 'NONE',  ( 60.55338150670809938, 14.46439363635230180, -47.56067349930459898 ) ) ;
#23440=CARTESIAN_POINT ( 'NONE',  ( 16.13393739769620083, -15.61618894467929941, -12.65000000000000036 ) ) ;
#23443=CARTESIAN_POINT ( 'NONE',  ( -11.32734370190460105, 10.64934056395049922, -6.430192534648650593 ) ) ;
#23449=CARTESIAN_POINT ( 'NONE',  ( 57.30647849094400215, 19.33005196432110040, -53.44855329768490293 ) ) ;
#23452=CARTESIAN_POINT ( 'NONE',  ( 14.30723785212189902, 19.48216086971750016, -21.19168582719050065 ) ) ;
#23455=CARTESIAN_POINT ( 'NONE',  ( 12.86222957544669931, 18.76465490122250301, -21.07385131904699804 ) ) ;
#23457=CARTESIAN_POINT ( 'NONE',  ( 48.31161565387870382, -54.20246409351659622, -54.89734529629400583 ) ) ;
#23458=CARTESIAN_POINT ( 'NONE',  ( 16.13393739769620083, -15.61618894467929941, -10.21818181818179916 ) ) ;
#23462=DIRECTION ( 'NONE',  ( 0.000000000000000000, 0.000000000000000000, 1.000000000000000000 ) ) ;
#23464=ORIENTED_EDGE ( 'NONE', *, *, #29071, .T. ) ;
#23469=CARTESIAN_POINT ( 'NONE',  ( 60.33296087198709756, -45.76927181686579615, -47.49787425318459810 ) ) ;
#23470=CARTESIAN_POINT ( 'NONE',  ( 47.88879426235697423, -54.35786135377512807, -54.72388424469790635 ) ) ;
#23471=CARTESIAN_POINT ( 'NONE',  ( 10.47385200046668707, 23.98129158042145548, -45.62050397739949403 ) ) ;
#23472=CARTESIAN_POINT ( 'NONE',  ( 84.42051485081360340, 12.29857348627670000, -47.44928677006510043 ) ) ;
#23473=CARTESIAN_POINT ( 'NONE',  ( 11.13393739769619906, 24.07008072128950005, -24.15000000000000213 ) ) ;
#23474=CIRCLE ( 'NONE', #34374, 2.000000000000002220 ) ;
#23478=ORIENTED_EDGE ( 'NONE', *, *, #43839, .T. ) ;
#23479=VERTEX_POINT ( 'NONE', #44806 ) ;
#23482=CARTESIAN_POINT ( 'NONE',  ( 76.42418064599820582, -22.61660856622344085, -12.90070511953996046 ) ) ;
#23483=CARTESIAN_POINT ( 'NONE',  ( 10.00488484307560100, -64.56416557920189803, -46.87927852444020260 ) ) ;
#23484=ORIENTED_EDGE ( 'NONE', *, *, #18736, .T. ) ;
#23488=CARTESIAN_POINT ( 'NONE',  ( 56.43927191853270386, -50.77432121216759953, -53.62502937860860186 ) ) ;
#23490=CARTESIAN_POINT ( 'NONE',  ( 59.77091825180480100, -2.116024841059339856, -15.76949253102769788 ) ) ;
#23491=CARTESIAN_POINT ( 'NONE',  ( 52.14531965947189462, -49.88997716300030305, -76.93285152251229420 ) ) ;
#23493=VERTEX_POINT ( 'NONE', #51455 ) ;
#23500=ADVANCED_FACE ( 'NONE', ( #15550 ), #768, .F. ) ;
#23502=CARTESIAN_POINT ( 'NONE',  ( 56.10889328822010214, 13.96147111367669957, -15.64994076471440110 ) ) ;
#23503=CARTESIAN_POINT ( 'NONE',  ( 61.10829104979099924, -45.34000981476349779, -47.03632675756029613 ) ) ;
#23504=ADVANCED_FACE ( 'NONE', ( #8910 ), #18452, .T. ) ;
#23506=EDGE_CURVE ( 'NONE', #51033, #40162, #37776, .T. ) ;
#23507=CARTESIAN_POINT ( 'NONE',  ( 68.13393739769620083, 11.88381105532070059, -71.50000000000000000 ) ) ;
#23510=LINE ( 'NONE', #39531, #41894 ) ;
#23512=EDGE_CURVE ( 'NONE', #25873, #18453, #38416, .T. ) ;
#23514=CARTESIAN_POINT ( 'NONE',  ( 12.13393739769600010, -55.41568642894409180, -74.14999999999999147 ) ) ;
#23516=CARTESIAN_POINT ( 'NONE',  ( 42.30370408490749412, -45.85561060964679569, -7.058032441766999732 ) ) ;
#23518=CARTESIAN_POINT ( 'NONE',  ( -8.966062602303901841, -15.61618894467929941, 8.449999999999979750 ) ) ;
#23522=FACE_OUTER_BOUND ( 'NONE', #15505, .T. ) ;
#23523=CARTESIAN_POINT ( 'NONE',  ( 64.31436383256627209, 0.8397385815152118571, -17.57630501671912526 ) ) ;
#23525=CARTESIAN_POINT ( 'NONE',  ( 8.049429273948879526, -62.14062887497920684, -15.83795189838459905 ) ) ;
#23527=EDGE_CURVE ( 'NONE', #4421, #45554, #8983, .T. ) ;
#23528=CYLINDRICAL_SURFACE ( 'NONE', #46561, 20.00000000000000355 ) ;
#23530=CARTESIAN_POINT ( 'NONE',  ( 53.03054974377609909, -49.58583241490480020, -49.02174586602249917 ) ) ;
#23531=VERTEX_POINT ( 'NONE', #20354 ) ;
#23534=FACE_OUTER_BOUND ( 'NONE', #15783, .T. ) ;
#23535=CARTESIAN_POINT ( 'NONE',  ( 51.80594959294069213, -49.19315472720849414, -77.05312857362879697 ) ) ;
#23537=CARTESIAN_POINT ( 'NONE',  ( 16.13393739769620083, -15.61618894467929941, -5.093415854460129566 ) ) ;
#23538=CARTESIAN_POINT ( 'NONE',  ( 56.28345034116380674, -45.19089576527889562, -15.87205044493469863 ) ) ;
#23539=CARTESIAN_POINT ( 'NONE',  ( 55.88720792914200075, 14.71003294998529931, -25.33276946690889986 ) ) ;
#23543=CARTESIAN_POINT ( 'NONE',  ( 11.31571027617879999, -65.02774978745999590, -16.86897512598950044 ) ) ;
#23544=CARTESIAN_POINT ( 'NONE',  ( 10.51008157369509988, 33.62871359210459588, -47.02029114578689928 ) ) ;
#23548=CARTESIAN_POINT ( 'NONE',  ( 8.815605938792600682, 32.05029769220720226, -46.67186391141279955 ) ) ;
#23551=ADVANCED_FACE ( 'NONE', ( #40549 ), #1943, .F. ) ;
#23553=EDGE_LOOP ( 'NONE', ( #47582, #20592, #44662, #16097 ) ) ;
#23555=CARTESIAN_POINT ( 'NONE',  ( 10.97938593161299892, -63.34067210474159282, -44.74408272625530003 ) ) ;
#23561=VERTEX_POINT ( 'NONE', #13298 ) ;
#23563=CARTESIAN_POINT ( 'NONE',  ( 62.88393739769619373, 11.88381105532070059, -84.94863984844531046 ) ) ;
#23565=CARTESIAN_POINT ( 'NONE',  ( 53.36310540583830431, 18.42371825317529854, -49.52410620756050008 ) ) ;
#23567=DIRECTION ( 'NONE',  ( 0.000000000000000000, 0.000000000000000000, -1.000000000000000000 ) ) ;
#23570=ORIENTED_EDGE ( 'NONE', *, *, #2678, .F. ) ;
#23575=EDGE_CURVE ( 'NONE', #43692, #13650, #29762, .T. ) ;
#23576=CARTESIAN_POINT ( 'NONE',  ( 47.24370950863509933, 23.52822492643439745, -74.14999583207030298 ) ) ;
#23581=CARTESIAN_POINT ( 'NONE',  ( 11.86340152622300081, 33.76504418661139795, -16.42027960339740034 ) ) ;
#23583=CARTESIAN_POINT ( 'NONE',  ( 53.09137791023449893, -49.29352759859440170, -26.91462423334489884 ) ) ;
#23584=CARTESIAN_POINT ( 'NONE',  ( 56.72911628704090248, -50.61618894563009263, -75.43431501713151022 ) ) ;
#23585=CARTESIAN_POINT ( 'NONE',  ( -0.5445768713979989295, 21.67700174432700067, -8.410206044792879254 ) ) ;
#23588=CARTESIAN_POINT ( 'NONE',  ( 61.51108537876409343, 13.91219412833640057, -46.41805243735920072 ) ) ;
#23590=CARTESIAN_POINT ( 'NONE',  ( 68.38971107296249841, -1.116188944679350037, -18.15384911730639672 ) ) ;
#23592=CARTESIAN_POINT ( 'NONE',  ( 52.79481824716010863, -49.67983215287559773, -48.50059634193729607 ) ) ;
#23593=CARTESIAN_POINT ( 'NONE',  ( 47.56952775046020321, 23.32449217223370042, -54.84171050377470635 ) ) ;
#23596=CARTESIAN_POINT ( 'NONE',  ( 61.07002009609450255, 14.12889903531000080, -47.07613370539880293 ) ) ;
#23598=CARTESIAN_POINT ( 'NONE',  ( 51.37232752684040094, 18.41177481517059888, -76.46732852243368939 ) ) ;
#23599=CARTESIAN_POINT ( 'NONE',  ( 52.75763158996860369, 18.47217075649399831, -48.62437232909790197 ) ) ;
#23601=CARTESIAN_POINT ( 'NONE',  ( 52.83531802359640039, -49.65800651964969603, -48.55820785178020316 ) ) ;
#23604=CARTESIAN_POINT ( 'NONE',  ( 47.68090551657530085, -54.49693150964059640, -54.85613361089130535 ) ) ;
#23605=CARTESIAN_POINT ( 'NONE',  ( 10.14913760601130122, -63.33847347462889843, -45.99399621147029649 ) ) ;
#23607=CARTESIAN_POINT ( 'NONE',  ( 60.77505974369530151, -30.37856211516960059, -16.18800847133800147 ) ) ;
#23616=ORIENTED_EDGE ( 'NONE', *, *, #4916, .F. ) ;
#23620=CARTESIAN_POINT ( 'NONE',  ( 12.31664131201799961, -65.34953315657870121, -46.39762439856330900 ) ) ;
#23624=EDGE_LOOP ( 'NONE', ( #22398, #6842, #37839, #12228 ) ) ;
#23625=CIRCLE ( 'NONE', #38739, 6.049999999999999822 ) ;
#23626=CARTESIAN_POINT ( 'NONE',  ( 11.21896018345050727, 33.88794933533077369, -22.95123051540872439 ) ) ;
#23628=CARTESIAN_POINT ( 'NONE',  ( 61.62036109055981115, 14.01986140997038888, -47.09707863094710945 ) ) ;
#23633=CARTESIAN_POINT ( 'NONE',  ( 60.09862518859029734, -29.13340823245889766, -15.80421788918070014 ) ) ;
#23636=CARTESIAN_POINT ( 'NONE',  ( 47.43599255125010217, -54.63612274721339901, -74.17395249489511855 ) ) ;
#23639=CARTESIAN_POINT ( 'NONE',  ( 44.72942195059490444, 14.16990783988029889, -7.990949946541189952 ) ) ;
#23642=( BOUNDED_CURVE ( )  B_SPLINE_CURVE ( 3, ( #39551, #49231, #21159, #32680 ),
 .UNSPECIFIED., .F., .T. ) 
 B_SPLINE_CURVE_WITH_KNOTS ( ( 4, 4 ),
 ( 4.712388980593789967, 6.283185307179586232 ),
 .UNSPECIFIED. ) 
 CURVE ( )  GEOMETRIC_REPRESENTATION_ITEM ( )  RATIONAL_B_SPLINE_CURVE ( ( 1.000000000000000000, 0.8047378541736504021, 0.8047378541736504021, 1.000000000000000000 ) ) 
 REPRESENTATION_ITEM ( '' )  );
#23643=CARTESIAN_POINT ( 'NONE',  ( 83.38337402972518930, -45.06848590938879795, -47.24826086172119233 ) ) ;
#23648=CARTESIAN_POINT ( 'NONE',  ( 14.14835400965569967, -50.34648095446409855, -20.86158003109909842 ) ) ;
#23649=CARTESIAN_POINT ( 'NONE',  ( 76.14068792729830193, 12.13509142339390046, -13.68365738061490156 ) ) ;
#23651=FACE_OUTER_BOUND ( 'NONE', #36272, .T. ) ;
#23652=VECTOR ( 'NONE', #32535, 1000.000000000000000 ) ;
#23654=CARTESIAN_POINT ( 'NONE',  ( -8.075504256637460188, -45.03553824879330847, -5.700448868517660195 ) ) ;
#23655=AXIS2_PLACEMENT_3D ( 'NONE', #16173, #3877, #12508 ) ;
#23657=CARTESIAN_POINT ( 'NONE',  ( 50.95939078474919626, 10.05946586878370042, -76.37902184192930122 ) ) ;
#23659=CARTESIAN_POINT ( 'NONE',  ( 13.02862176429879781, 19.08811602440689725, -21.18331087829950121 ) ) ;
#23660=CARTESIAN_POINT ( 'NONE',  ( 57.55751162052580128, -50.59130190800640747, -53.59933301306699605 ) ) ;
#23661=CARTESIAN_POINT ( 'NONE',  ( 43.52753934370100097, 12.39697735565209946, -5.023899789804930904 ) ) ;
#23663=CARTESIAN_POINT ( 'NONE',  ( 16.13393739769620083, -15.61618894467929941, 6.072546842075589701 ) ) ;
#23664=CARTESIAN_POINT ( 'NONE',  ( 56.95646850581400145, -47.49882031525390147, -47.91148979950029485 ) ) ;
#23667=CARTESIAN_POINT ( 'NONE',  ( 18.25826542137950170, -52.10962414010410271, -75.64877291256318870 ) ) ;
#23671=EDGE_LOOP ( 'NONE', ( #47463, #8370, #7333, #51673, #50274, #308, #3084 ) ) ;
#23672=CARTESIAN_POINT ( 'NONE',  ( 8.794764235947729603, 31.93474649087269768, -46.67042062406039804 ) ) ;
#23675=CARTESIAN_POINT ( 'NONE',  ( 52.68908936341578908, -49.75029824513269716, -28.15000000000000213 ) ) ;
#23678=CARTESIAN_POINT ( 'NONE',  ( 17.54620179519039880, 20.94680560585019791, -75.92929371827810314 ) ) ;
#23682=ORIENTED_EDGE ( 'NONE', *, *, #29794, .F. ) ;
#23685=ADVANCED_FACE ( 'NONE', ( #46565 ), #3044, .T. ) ;
#23689=B_SPLINE_CURVE_WITH_KNOTS ( 'NONE', 3,
 ( #13901, #33799, #7593, #47178, #23280, #3919, #12041, #31919, #15965, #7846, #11266, #27747, #19881, #35872, #39301, #39051, #8104, #51865, #15704, #27227, #43241, #43492, #23539, #16214 ),
 .UNSPECIFIED., .F., .F.,
 ( 4, 2, 2, 2, 2, 2, 2, 2, 2, 2, 2, 4 ),
 ( 0.000000000000000000, 0.2627958365207210267, 0.8013173561513319276, 1.332723478065980016, 1.850236617094970004, 2.367749756123960214, 3.156999674831939995, 3.551624634185940099, 4.183024569152329342, 5.193264465098549998, 6.167115316339319975, 6.313999209016010639 ),
 .UNSPECIFIED. ) ;
#23697=CARTESIAN_POINT ( 'NONE',  ( 41.40756759976829926, 13.53921337778190015, -5.393983492778530398 ) ) ;
#23698=CARTESIAN_POINT ( 'NONE',  ( 60.42383115829219520, 14.54589923391379891, -47.62650397435140093 ) ) ;
#23701=EDGE_CURVE ( 'NONE', #12879, #31811, #2127, .T. ) ;
#23703=CARTESIAN_POINT ( 'NONE',  ( -7.084120996664410086, 14.62350974809900173, -5.509165850239240214 ) ) ;
#23708=B_SPLINE_CURVE_WITH_KNOTS ( 'NONE', 3,
 ( #19400, #10777, #27002, #30919, #11550, #51380, #39324, #15728, #34602, #3428 ),
 .UNSPECIFIED., .F., .F.,
 ( 4, 2, 2, 2, 4 ),
 ( 0.5540946774305016698, 0.5625000000428368452, 0.6625000000401861655, 0.8225000000359454777, 1.000000000000000000 ),
 .UNSPECIFIED. ) ;
#23709=CARTESIAN_POINT ( 'NONE',  ( 87.61621807841599718, -48.61618894467930119, -61.12885639714370001 ) ) ;
#23714=CARTESIAN_POINT ( 'NONE',  ( 15.79694611016800287, 19.73115256075769963, -20.52360778208829828 ) ) ;
#23717=CARTESIAN_POINT ( 'NONE',  ( 61.37880583284824354, 14.09584805848855815, -47.24536948349046384 ) ) ;
#23718=CARTESIAN_POINT ( 'NONE',  ( 48.47831330238179959, -54.12362947456229989, -54.86665052696550049 ) ) ;
#23719=CARTESIAN_POINT ( 'NONE',  ( 52.08182543943776466, -33.08310422624513336, -19.98519270871916476 ) ) ;
#23722=CARTESIAN_POINT ( 'NONE',  ( 47.80730873599560482, 23.17301113850950145, -54.73352113644760664 ) ) ;
#23725=FACE_OUTER_BOUND ( 'NONE', #17143, .T. ) ;
#23726=ORIENTED_EDGE ( 'NONE', *, *, #45663, .T. ) ;
#23728=CARTESIAN_POINT ( 'NONE',  ( 60.75261223076579853, -45.51339453889590203, -47.16721473501090145 ) ) ;
#23729=CARTESIAN_POINT ( 'NONE',  ( 53.80794059781069194, -49.14842230199280237, -48.63343936029099979 ) ) ;
#23730=CARTESIAN_POINT ( 'NONE',  ( 83.23750471071477364, 13.58710101679191062, -46.42261246174885514 ) ) ;
#23733=CARTESIAN_POINT ( 'NONE',  ( 12.16981617636350066, 18.81688479155219795, -21.14999999999999858 ) ) ;
#23735=ORIENTED_EDGE ( 'NONE', *, *, #7504, .T. ) ;
#23738=EDGE_CURVE ( 'NONE', #34714, #23561, #43776, .T. ) ;
#23743=CARTESIAN_POINT ( 'NONE',  ( 47.18324198357289845, 23.57489020266570279, -74.14999999999999147 ) ) ;
#23744=CARTESIAN_POINT ( 'NONE',  ( 10.23176309419300090, -64.70699932978828883, -46.94201679684390172 ) ) ;
#23745=VERTEX_POINT ( 'NONE', #18504 ) ;
#23750=DIRECTION ( 'NONE',  ( 0.9529257800132618916, 0.000000000000000000, -0.3032036572769470362 ) ) ;
#23751=CARTESIAN_POINT ( 'NONE',  ( 64.18578493394871032, 0.2143848170464559832, -16.96023575528840155 ) ) ;
#23752=CARTESIAN_POINT ( 'NONE',  ( 51.51980101732179662, -49.43950574372139783, -76.63338017989070750 ) ) ;
#23754=EDGE_CURVE ( 'NONE', #12303, #29238, #25342, .T. ) ;
#23755=ORIENTED_EDGE ( 'NONE', *, *, #16902, .F. ) ;
#23757=CARTESIAN_POINT ( 'NONE',  ( 82.02429831058030629, 10.00628846694210061, -45.87976092105969883 ) ) ;
#23762=CARTESIAN_POINT ( 'NONE',  ( 13.77413875405740029, -50.62291444519870254, -21.29092247280310346 ) ) ;
#23763=CARTESIAN_POINT ( 'NONE',  ( 54.96007620141639904, 19.38381105532069881, -76.67894625151460275 ) ) ;
#23765=EDGE_CURVE ( 'NONE', #3407, #34403, #14317, .T. ) ;
#23766=DIRECTION ( 'NONE',  ( -0.5547001962252289253, 0.000000000000000000, -0.8320502943378439431 ) ) ;
#23767=CARTESIAN_POINT ( 'NONE',  ( 60.91034051199495281, -45.42727599127712779, -46.97125969418770097 ) ) ;
#23768=CARTESIAN_POINT ( 'NONE',  ( 61.24450422717950460, -45.36922733462990465, -47.29134737333090044 ) ) ;
#23772=VERTEX_POINT ( 'NONE', #30287 ) ;
#23773=CARTESIAN_POINT ( 'NONE',  ( 46.81019908455479595, 22.25026678784159984, -76.02856692477300271 ) ) ;
#23774=CARTESIAN_POINT ( 'NONE',  ( 47.24767689108010416, -54.75733057101270163, -54.63867562300049485 ) ) ;
#23779=CARTESIAN_POINT ( 'NONE',  ( 10.78192289011060012, -64.93864051461240194, -17.70651626566360193 ) ) ;
#23781=CYLINDRICAL_SURFACE ( 'NONE', #20114, 1.999999999999998890 ) ;
#23784=CARTESIAN_POINT ( 'NONE',  ( 49.08512682873279687, 22.68755118111490177, -55.26163594736860318 ) ) ;
#23786=CARTESIAN_POINT ( 'NONE',  ( 52.65273120535449891, -49.78633184267020084, -48.66233031291120170 ) ) ;
#23789=DIRECTION ( 'NONE',  ( 0.000000000000000000, 0.7071067811865521247, 0.7071067811865429098 ) ) ;
#23790=CARTESIAN_POINT ( 'NONE',  ( 83.92831008986510710, 12.99935617635409990, -46.72264359244289977 ) ) ;
#23792=CARTESIAN_POINT ( 'NONE',  ( 52.90434486281380799, 18.43107897257790029, -49.01850765170799917 ) ) ;
#23793=CARTESIAN_POINT ( 'NONE',  ( 56.96434502685580270, -45.17967511238569500, -17.49912984090079959 ) ) ;
#23795=ORIENTED_EDGE ( 'NONE', *, *, #33573, .F. ) ;
#23797=VECTOR ( 'NONE', #3891, 1000.000000000000000 ) ;
#23799=VERTEX_POINT ( 'NONE', #26349 ) ;
#23801=CARTESIAN_POINT ( 'NONE',  ( 11.38858907665120057, -65.22710982081629538, -17.28671555175889907 ) ) ;
#23802=CARTESIAN_POINT ( 'NONE',  ( 10.90497224517999975, 33.02336919903609669, -45.71389029108730284 ) ) ;
#23805=CARTESIAN_POINT ( 'NONE',  ( 11.31086268549694829, -65.19635327846651762, -22.85314699157382989 ) ) ;
#23808=CARTESIAN_POINT ( 'NONE',  ( 11.10552572835999996, -63.29074793436570445, -44.25199298686389682 ) ) ;
#23809=CARTESIAN_POINT ( 'NONE',  ( 66.23540447448930024, 18.72622661238580122, -71.50000000000139266 ) ) ;
#23810=ORIENTED_EDGE ( 'NONE', *, *, #23127, .T. ) ;
#23815=ORIENTED_EDGE ( 'NONE', *, *, #22869, .T. ) ;
#23821=AXIS2_PLACEMENT_3D ( 'NONE', #47968, #39329, #11815 ) ;
#23825=EDGE_CURVE ( 'NONE', #39, #679, #34129, .T. ) ;
#23830=CARTESIAN_POINT ( 'NONE',  ( 47.17278709481859522, 23.23193946581579894, -75.17206278554509424 ) ) ;
#23831=DIRECTION ( 'NONE',  ( 0.8229030450105319083, 0.000000000000000000, 0.5681818181818162339 ) ) ;
#23832=CARTESIAN_POINT ( 'NONE',  ( 11.13393739769619906, -65.36556080001030011, 8.349999999999999645 ) ) ;
#23833=CARTESIAN_POINT ( 'NONE',  ( 12.00051660606520088, 33.89238323676829623, -16.59289575485349744 ) ) ;
#23836=CARTESIAN_POINT ( 'NONE',  ( 56.61807468419900147, -50.61971398085310625, -75.33860262121818607 ) ) ;
#23838=CARTESIAN_POINT ( 'NONE',  ( 10.66853968524194762, -55.24094850124689771, -45.35057670835523425 ) ) ;
#23840=CARTESIAN_POINT ( 'NONE',  ( 61.43276948373569724, 13.94038599860599881, -46.57406651285639754 ) ) ;
#23843=ORIENTED_EDGE ( 'NONE', *, *, #33862, .T. ) ;
#23844=CARTESIAN_POINT ( 'NONE',  ( 52.93498292564289187, -49.60578928504740048, -48.74287988808979577 ) ) ;
#23845=CARTESIAN_POINT ( 'NONE',  ( 60.96737254747249324, -45.23440155981300137, -27.35231452095100124 ) ) ;
#23846=AXIS2_PLACEMENT_3D ( 'NONE', #23832, #47474, #3701 ) ;
#23847=FACE_OUTER_BOUND ( 'NONE', #16980, .T. ) ;
#23848=CARTESIAN_POINT ( 'NONE',  ( 56.66669568006840052, 14.87756128898679897, -26.25347649126269900 ) ) ;
#23850=CARTESIAN_POINT ( 'NONE',  ( 51.08268012532420244, 17.38380819494409835, -76.44192738162151102 ) ) ;
#23851=CARTESIAN_POINT ( 'NONE',  ( 53.49062365255090157, 18.11806236342570031, -48.99764540719110073 ) ) ;
#23856=EDGE_CURVE ( 'NONE', #36517, #15061, #18164, .T. ) ;
#23857=CYLINDRICAL_SURFACE ( 'NONE', #36343, 2.000000000000006217 ) ;
#23859=CARTESIAN_POINT ( 'NONE',  ( 47.58042881629169329, -54.55451462403799923, -54.88832507069039934 ) ) ;
#23862=CARTESIAN_POINT ( 'NONE',  ( 62.57089764215618999, -31.49364712873180139, -16.95369364430399983 ) ) ;
#23864=EDGE_CURVE ( 'NONE', #1009, #39844, #25232, .T. ) ;
#23865=CARTESIAN_POINT ( 'NONE',  ( 11.13393739769619906, 32.00863872204660510, -43.74499609563760316 ) ) ;
#23868=ADVANCED_FACE ( 'NONE', ( #37831 ), #25491, .T. ) ;
#23871=ORIENTED_EDGE ( 'NONE', *, *, #3394, .F. ) ;
#23878=ORIENTED_EDGE ( 'NONE', *, *, #46532, .T. ) ;
#23880=DIRECTION ( 'NONE',  ( -0.04251717301921900671, 0.000000000000000000, -0.9990957361526741076 ) ) ;
#23881=DIRECTION ( 'NONE',  ( 0.3805321250008310008, 0.000000000000000000, -0.9247677015566404535 ) ) ;
#23885=EDGE_CURVE ( 'NONE', #30115, #2811, #15858, .T. ) ;
#23886=CARTESIAN_POINT ( 'NONE',  ( 61.64370769382880155, -29.21250595235679981, -16.00854006375729810 ) ) ;
#23890=CARTESIAN_POINT ( 'NONE',  ( 41.26310204296880357, 14.16900014587270107, -6.071150992149259906 ) ) ;
#23892=CARTESIAN_POINT ( 'NONE',  ( 14.92425731419689861, 21.51730579194029858, -76.12465403027070465 ) ) ;
#23893=CARTESIAN_POINT ( 'NONE',  ( 83.33882225295539570, -44.99385703852960461, -47.09476873026769539 ) ) ;
#23895=EDGE_CURVE ( 'NONE', #15334, #29806, #16997, .T. ) ;
#23897=ORIENTED_EDGE ( 'NONE', *, *, #14660, .T. ) ;
#23898=CARTESIAN_POINT ( 'NONE',  ( 55.88979882644740371, -46.58799578511379735, -26.24141907459939915 ) ) ;
#23899=CARTESIAN_POINT ( 'NONE',  ( 12.63859970449419912, -64.82257329977309723, -16.00819051994519882 ) ) ;
#23902=CARTESIAN_POINT ( 'NONE',  ( 40.76017235305160114, -45.36108721241059527, -5.740519108723990627 ) ) ;
#23903=ORIENTED_EDGE ( 'NONE', *, *, #8920, .T. ) ;
#23904=CARTESIAN_POINT ( 'NONE',  ( -5.724976569056140718, -47.03139907360350236, -5.524370486448079376 ) ) ;
#23905=CYLINDRICAL_SURFACE ( 'NONE', #51624, 2.000000000000000444 ) ;
#23909=CARTESIAN_POINT ( 'NONE',  ( 57.32084457176560477, -50.51928695062449748, -53.29702802308130316 ) ) ;
#23910=CARTESIAN_POINT ( 'NONE',  ( 41.35617332069819696, 13.41895923659610013, -5.195208887928910002 ) ) ;
#23911=FACE_OUTER_BOUND ( 'NONE', #40145, .T. ) ;
#23913=CARTESIAN_POINT ( 'NONE',  ( 57.68257350692169894, -47.11839356109889820, -47.67368955113449402 ) ) ;
#23917=CARTESIAN_POINT ( 'NONE',  ( 17.54489239063250139, -52.26337343415740122, -75.96669286083250938 ) ) ;
#23918=PRODUCT ( 'Swivel Caster Main Housing', 'Swivel Caster Main Housing', '', ( #27517 ) ) ;
#23929=ORIENTED_EDGE ( 'NONE', *, *, #3071, .T. ) ;
#23930=CARTESIAN_POINT ( 'NONE',  ( 17.98857762822040129, 21.26099547410819923, -75.92929371827810314 ) ) ;
#23931=CIRCLE ( 'NONE', #1369, 20.29675463313339989 ) ;
#23932=VERTEX_POINT ( 'NONE', #45439 ) ;
#23934=CYLINDRICAL_SURFACE ( 'NONE', #30227, 2.000000000000058620 ) ;
#23940=LINE ( 'NONE', #37060, #29443 ) ;
#23942=CARTESIAN_POINT ( 'NONE',  ( 16.13393739769620083, -15.61618894467929941, 7.944363289481099599 ) ) ;
#23943=ORIENTED_EDGE ( 'NONE', *, *, #50562, .T. ) ;
#23946=LINE ( 'NONE', #7230, #46796 ) ;
#23948=CARTESIAN_POINT ( 'NONE',  ( 60.86422568982110448, 14.38054746056040045, -47.60180080821060500 ) ) ;
#23949=CIRCLE ( 'NONE', #31367, 1.000000000000000444 ) ;
#23952=CARTESIAN_POINT ( 'NONE',  ( -4.838091769851679658, 16.12562087950150058, -4.829461453175369456 ) ) ;
#23953=CARTESIAN_POINT ( 'NONE',  ( 46.36969437874859779, 21.71676560242570631, -76.14999999999999147 ) ) ;
#23954=CARTESIAN_POINT ( 'NONE',  ( 61.12152888756239832, 13.98644838521740041, -27.50614731511399924 ) ) ;
#23958=AXIS2_PLACEMENT_3D ( 'NONE', #29225, #45232, #25287 ) ;
#23960=EDGE_CURVE ( 'NONE', #17149, #14841, #4488, .T. ) ;
#23962=CARTESIAN_POINT ( 'NONE',  ( 53.75473964300852714, -50.98815654850967150, -75.91867185088533176 ) ) ;
#23966=CARTESIAN_POINT ( 'NONE',  ( 47.19189654124329536, 23.53431858022840117, -74.50357331166900110 ) ) ;
#23967=CARTESIAN_POINT ( 'NONE',  ( 48.76904876940009359, -54.05456627190059749, -55.30034376619679648 ) ) ;
#23968=LINE ( 'NONE', #7770, #27275 ) ;
#23974=CARTESIAN_POINT ( 'NONE',  ( 75.47966807050509885, 12.14072485751589880, -13.40512917118210012 ) ) ;
#23977=CARTESIAN_POINT ( 'NONE',  ( 60.66485807962820331, -45.57220713008260304, -47.29680594952690598 ) ) ;
#23979=CARTESIAN_POINT ( 'NONE',  ( 48.93508874961765542, -53.77152385436457394, -54.40024034726641844 ) ) ;
#23986=ORIENTED_EDGE ( 'NONE', *, *, #3416, .T. ) ;
#23987=DIRECTION ( 'NONE',  ( -0.5685928097855378338, 0.5944782866685498490, 0.5685928097855378338 ) ) ;
#23988=B_SPLINE_CURVE_WITH_KNOTS ( 'NONE', 3,
 ( #28456, #35819, #47883, #48133, #48658, #9080, #13024, #32893, #8564, #12489, #12757, #23994, #12233, #44457, #27939, #24505, #16156, #8296 ),
 .UNSPECIFIED., .F., .F.,
 ( 4, 2, 2, 2, 2, 2, 2, 2, 4 ),
 ( 0.000000000000000000, 0.01645352784434715721, 0.1775000000366272201, 0.3375000000696457003, 0.4375000000902801167, 0.5000000001031779107, 0.6250000001289733875, 0.7632226885852325671, 1.000000000000000000 ),
 .UNSPECIFIED. ) ;
#23990=B_SPLINE_CURVE_WITH_KNOTS ( 'NONE', 3,
 ( #10321, #22349, #37121, #2969, #18943, #34923, #26282, #9085, #22606, #2713, #5163, #21118, #33167, #13284, #3999, #47769, #31744, #51693, #32002, #30986, #23626, #15282, #47012, #73, #43830, #39387, #7679, #43578, #44084, #11875, #4248, #16046, #50922, #35954, #3491 ),
 .UNSPECIFIED., .F., .F.,
 ( 4, 2, 2, 1, 1, 2, 2, 2, 1, 1, 2, 2, 2, 2, 1, 1, 1, 2, 2, 2, 4 ),
 ( 0.000000000000000000, 0.06250000000003767819, 0.09375000000005774548, 0.1093750000000684730, 0.1171875000000714567, 0.1210937500000717759, 0.1250000000000721090, 0.1875000000000927036, 0.2187500000001041944, 0.2343750000001105227, 0.2421875000001139366, 0.2500000000001173506, 0.3750000000001291744, 0.4375000000001351141, 0.4687500000001366129, 0.4843750000001361133, 0.4921875000001392220, 0.4960937500001375566, 0.5000000000001357803, 0.7500000000000679456, 1.000000000000000000 ),
 .UNSPECIFIED. ) ;
#23993=CARTESIAN_POINT ( 'NONE',  ( 52.95041285254770003, -49.64391847752840192, -49.05228050339000134 ) ) ;
#23994=CARTESIAN_POINT ( 'NONE',  ( 53.23465407748010847, -50.42897142312819625, -77.19488661283054398 ) ) ;
#23995=CARTESIAN_POINT ( 'NONE',  ( 76.39397256973549588, -18.14611920900664188, -12.77057708294060490 ) ) ;
#23996=CARTESIAN_POINT ( 'NONE',  ( 52.41075892860209962, -52.38690917609680042, -53.79179071692110625 ) ) ;
#23999=ORIENTED_EDGE ( 'NONE', *, *, #8621, .T. ) ;
#24002=CARTESIAN_POINT ( 'NONE',  ( 56.35191260731789953, -50.54342274251170153, -52.86474260619870336 ) ) ;
#24003=CARTESIAN_POINT ( 'NONE',  ( 68.13393739769620083, -33.11618894467940066, -65.65000000000000568 ) ) ;
#24004=CARTESIAN_POINT ( 'NONE',  ( 63.16535863595050415, 0.3893935637993060084, -17.07704178728910094 ) ) ;
#24005=CARTESIAN_POINT ( 'NONE',  ( 51.80595388240210042, -49.19315315062009830, -77.05313553807228288 ) ) ;
#24007=DIRECTION ( 'NONE',  ( 1.000000000000000000, 0.000000000000000000, 0.000000000000000000 ) ) ;
#24012=CARTESIAN_POINT ( 'NONE',  ( 12.57902733935019945, -50.33803507323350601, -21.19240466621000252 ) ) ;
#24014=CARTESIAN_POINT ( 'NONE',  ( 65.43393739769584272, -48.11618894467441976, -75.95000000000109708 ) ) ;
#24015=FACE_OUTER_BOUND ( 'NONE', #10633, .T. ) ;
#24018=CARTESIAN_POINT ( 'NONE',  ( 18.34504066045640513, -52.20691909698821576, -75.61049359297886951 ) ) ;
#24019=B_SPLINE_SURFACE_WITH_KNOTS ( 'NONE', 3, 3, ( 
 ( #30481, #30740, #32913, #48940, #28995, #35964, #23886, #27327, #11619, #43333, #11881, #31244, #23129, #43078 ),
 ( #35192, #35716, #15546, #39398, #10849, #3235, #27840, #19211, #43838, #39650, #39142, #3498, #15793, #31502 ),
 ( #47522, #51195, #31757, #27582, #7939, #42822, #35455, #7171, #30995, #22870, #15290, #47020, #7689, #47274 ),
 ( #11362, #7425, #19967, #23374, #43586, #19469, #51451, #26811, #38891, #23633, #47776, #39910, #4006, #2979 ),
 ( #3757, #19724, #81, #51701, #16052, #32008, #18953, #6918, #34931, #50932, #15028, #11108, #27072, #44066 ),
 ( #8170, #15264, #39627, #3984, #30965, #4230, #24114, #57, #35427, #27555, #16031, #7401, #47247, #40134 ),
 ( #39118, #15522, #27301, #11080, #31987, #15772, #19702, #35694, #20204, #3212, #7664, #43814, #51426, #3473 ),
 ( #51171, #46995, #23349, #50905, #14997, #28063, #48007, #23607, #27048, #23100, #12106, #43052, #47498, #7913 ),
 ( #31726, #51678, #7148, #19183, #35164, #47752, #11859, #27814, #39372, #3730, #31474, #31220, #11337, #11596 ),
 ( #43563, #43309, #19444, #23862, #39885, #19947, #35937, #9210, #40907, #12888, #36191, #28581, #37242, #44581 ) ),
 .UNSPECIFIED., .F., .F., .F.,
 ( 4, 1, 1, 1, 1, 1, 1, 4 ),
 ( 4, 2, 2, 2, 2, 2, 4 ),
 ( -0.001640340358549000066, 0.1428571428571430157, 0.2857142857142860315, 0.4285714285714289917, 0.5714285714285709528, 0.7142857142857139685, 0.8571428571428569843, 1.000038638203759822 ),
 ( -0.9741865675133749569, -0.7931653508785260209, -0.6345322807028209722, -0.5552157456149680037, -0.4283092894744039980, -0.2252589596495010171, 0.001640340358549000066 ),
 .UNSPECIFIED. ) ;
#24020=VERTEX_POINT ( 'NONE', #35176 ) ;
#24021=CARTESIAN_POINT ( 'NONE',  ( 14.15391798052560013, -51.16362366046359966, -74.57010117179498820 ) ) ;
#24023=CARTESIAN_POINT ( 'NONE',  ( 47.39567005599690219, -54.65671969365300242, -54.74175872089709571 ) ) ;
#24024=( LENGTH_UNIT ( ) NAMED_UNIT ( * ) SI_UNIT ( .MILLI., .METRE. ) );
#24025=DIRECTION ( 'NONE',  ( 0.000000000000000000, 0.000000000000000000, -1.000000000000000000 ) ) ;
#24026=CARTESIAN_POINT ( 'NONE',  ( 74.17629866868290378, -43.11618894467930119, -65.34607522167520699 ) ) ;
#24029=CARTESIAN_POINT ( 'NONE',  ( 47.26610112325450075, -54.05804861832230301, -75.56421356201970241 ) ) ;
#24032=DIRECTION ( 'NONE',  ( 1.000000000000000000, -6.091302000000000065E-09, -6.644969000000000155E-09 ) ) ;
#24035=CARTESIAN_POINT ( 'NONE',  ( 49.29567348006049343, 22.45443271384029771, -54.47873722526050244 ) ) ;
#24037=CARTESIAN_POINT ( 'NONE',  ( 53.53746104731280298, -49.37100955498770105, -49.11443482729089993 ) ) ;
#24038=EDGE_LOOP ( 'NONE', ( #31868, #25846, #39754, #33031, #14080, #36366, #11146, #30012, #34399, #24554, #23878, #23064, #39641, #119, #28461, #27857, #38028, #49488 ) ) ;
#24041=DIRECTION ( 'NONE',  ( -1.000000000000000000, 0.000000000000000000, 0.000000000000000000 ) ) ;
#24042=CARTESIAN_POINT ( 'NONE',  ( 83.68633570933860710, 13.34091092982879978, -46.84648411755270558 ) ) ;
#24043=CARTESIAN_POINT ( 'NONE',  ( 55.90075151227409833, 15.08720832841919979, -26.05342630048340169 ) ) ;
#24045=CARTESIAN_POINT ( 'NONE',  ( 52.66873572145449600, 18.54828968354710028, -48.73460864874000009 ) ) ;
#24046=CARTESIAN_POINT ( 'NONE',  ( 56.50061855793390464, -45.38130615441500026, -17.93020122267619954 ) ) ;
#24048=CARTESIAN_POINT ( 'NONE',  ( 53.62552786343490396, 20.09834016026489678, -75.58099297212140755 ) ) ;
#24052=ADVANCED_FACE ( 'NONE', ( #6634 ), #19452, .F. ) ;
#24053=ORIENTED_EDGE ( 'NONE', *, *, #17789, .T. ) ;
#24054=CARTESIAN_POINT ( 'NONE',  ( 10.98135327145790008, -65.06876835564288797, -17.57575595872290108 ) ) ;
#24055=CARTESIAN_POINT ( 'NONE',  ( 11.31310665686720007, 33.54695633304280022, -46.14727449326090181 ) ) ;
#24057=CARTESIAN_POINT ( 'NONE',  ( 49.54367864761420037, -52.88831591555140221, -52.75219176336310056 ) ) ;
#24058=CARTESIAN_POINT ( 'NONE',  ( 10.83247370603695003, -64.53797486497589375, -23.38721072466407236 ) ) ;
#24062=CARTESIAN_POINT ( 'NONE',  ( 10.97767197991529997, -63.11543068638779630, -44.74312619248830458 ) ) ;
#24066=CARTESIAN_POINT ( 'NONE',  ( 56.39270784037419304, 19.29512405589720103, -52.86271187285759510 ) ) ;
#24072=CARTESIAN_POINT ( 'NONE',  ( 57.35590716831809743, -50.13655087819479661, -52.61987026682340485 ) ) ;
#24073=VECTOR ( 'NONE', #13883, 1000.000000000000000 ) ;
#24074=CARTESIAN_POINT ( 'NONE',  ( 50.51283422208840079, 21.26479333751330003, -52.94373263262310303 ) ) ;
#24077=CARTESIAN_POINT ( 'NONE',  ( 56.50064219191239800, 19.52881903142939635, -74.14937127320040133 ) ) ;
#24083=CARTESIAN_POINT ( 'NONE',  ( 46.54864319858230459, 22.04971653235029905, -76.11254988220410667 ) ) ;
#24084=EDGE_CURVE ( 'NONE', #10936, #9424, #50508, .T. ) ;
#24085=DIRECTION ( 'NONE',  ( -1.000000000000000000, 0.000000000000000000, 0.000000000000000000 ) ) ;
#24087=( BOUNDED_CURVE ( )  B_SPLINE_CURVE ( 2, ( #19669, #2666, #11309, #23073, #43025 ),
 .UNSPECIFIED., .F., .T. ) 
 B_SPLINE_CURVE_WITH_KNOTS ( ( 3, 2, 3 ),
 ( -0.003205554299145560102, 0.8238407534178779912, 1.650887061134900025 ),
 .UNSPECIFIED. ) 
 CURVE ( )  GEOMETRIC_REPRESENTATION_ITEM ( )  RATIONAL_B_SPLINE_CURVE ( ( 1.000000000000000000, 0.9157107718028779653, 1.000000000000000000, 0.9157107718028449916, 1.000000000000000000 ) ) 
 REPRESENTATION_ITEM ( '' )  );
#24088=CARTESIAN_POINT ( 'NONE',  ( 12.17681940038050037, 33.64169525760830481, -16.15032133962059646 ) ) ;
#24090=CARTESIAN_POINT ( 'NONE',  ( 54.86175947632980154, -50.65972080371189890, -76.24591593276051071 ) ) ;
#24094=CARTESIAN_POINT ( 'NONE',  ( 61.37578811247220045, 13.95917485428159921, -46.55532700619050246 ) ) ;
#24095=CARTESIAN_POINT ( 'NONE',  ( 76.87859684847769870, -43.11619168008749625, -14.85884840380859906 ) ) ;
#24096=DIRECTION ( 'NONE',  ( 0.000000000000000000, 0.000000000000000000, 1.000000000000000000 ) ) ;
#24097=ORIENTED_EDGE ( 'NONE', *, *, #47117, .F. ) ;
#24098=CARTESIAN_POINT ( 'NONE',  ( 52.94089229371839878, -49.60269320154350225, -48.75998159659980047 ) ) ;
#24100=CARTESIAN_POINT ( 'NONE',  ( 59.06502219811700627, -45.32330029555010498, -26.35699478639849858 ) ) ;
#24102=CARTESIAN_POINT ( 'NONE',  ( 56.59921044315609606, 14.68325417103389974, -26.17131425341809958 ) ) ;
#24104=CARTESIAN_POINT ( 'NONE',  ( 50.62459437698230147, 18.71911933297949915, -76.16377488163089993 ) ) ;
#24105=CARTESIAN_POINT ( 'NONE',  ( 52.75872642489079567, 18.46922250474269944, -48.48805342991609990 ) ) ;
#24107=CARTESIAN_POINT ( 'NONE',  ( 40.64814218619559938, -44.65225711300980294, -4.018323718197329697 ) ) ;
#24108=ORIENTED_EDGE ( 'NONE', *, *, #36414, .T. ) ;
#24109=CARTESIAN_POINT ( 'NONE',  ( 20.13393739083949896, -55.41568640430479320, -20.65000000000000213 ) ) ;
#24111=CARTESIAN_POINT ( 'NONE',  ( 47.78329665909949853, -54.43353293614439536, -54.80119951604820017 ) ) ;
#24112=CARTESIAN_POINT ( 'NONE',  ( -7.653322382745200159, 14.02129102307469921, -4.959142631146099767 ) ) ;
#24114=CARTESIAN_POINT ( 'NONE',  ( 61.41002981261989646, -30.19755464412979862, -16.14587537362810110 ) ) ;
#24121=ORIENTED_EDGE ( 'NONE', *, *, #17903, .T. ) ;
#24125=CARTESIAN_POINT ( 'NONE',  ( 55.82582291612180114, -46.03321360888129732, -25.33858244797220038 ) ) ;
#24126=CARTESIAN_POINT ( 'NONE',  ( 53.81599905896988645, 20.06114670800089428, -75.54047393059830995 ) ) ;
#24128=ORIENTED_EDGE ( 'NONE', *, *, #22352, .T. ) ;
#24129=DIRECTION ( 'NONE',  ( 1.000000000000000000, 0.000000000000000000, 0.000000000000000000 ) ) ;
#24138=CARTESIAN_POINT ( 'NONE',  ( 11.10346939884210116, -64.31936717124580127, -23.87841574096529840 ) ) ;
#24141=CARTESIAN_POINT ( 'NONE',  ( 41.02377769398490415, 13.92370008184540175, -5.717048413919049388 ) ) ;
#24143=EDGE_CURVE ( 'NONE', #30210, #17198, #25763, .T. ) ;
#24144=CARTESIAN_POINT ( 'NONE',  ( 14.27678794190400069, 20.53764257940400029, -75.58342519351550948 ) ) ;
#24146=EDGE_CURVE ( 'NONE', #24756, #32096, #45847, .T. ) ;
#24147=CARTESIAN_POINT ( 'NONE',  ( 83.20652121431659509, -45.06907107880329733, -47.10047235024320145 ) ) ;
#24148=CARTESIAN_POINT ( 'NONE',  ( 10.89208569013780448, 33.76849054883776802, -17.57297834644989720 ) ) ;
#24152=CARTESIAN_POINT ( 'NONE',  ( 52.72304479398140131, -49.72255302625990225, -28.01707846523380141 ) ) ;
#24153=CARTESIAN_POINT ( 'NONE',  ( 11.23965435610889863, -65.13936513006379414, -17.15438869215460116 ) ) ;
#24156=CARTESIAN_POINT ( 'NONE',  ( 75.45730910492666510, 12.50011331391788794, -13.48270834329013645 ) ) ;
#24157=CARTESIAN_POINT ( 'NONE',  ( 12.86227365712040083, -49.99703836812659574, -21.07384430750599691 ) ) ;
#24159=CARTESIAN_POINT ( 'NONE',  ( -6.571053818291229476, -46.36898988238050379, -5.603118524855751126 ) ) ;
#24160=CARTESIAN_POINT ( 'NONE',  ( 47.21165009223999931, 23.55238375380269744, -54.63209248662939643 ) ) ;
#24164=CARTESIAN_POINT ( 'NONE',  ( 57.30262416817789983, -50.51992209788300414, -53.29749893028549934 ) ) ;
#24165=CARTESIAN_POINT ( 'NONE',  ( 42.74124889056859899, 12.81040389201469942, -5.015693368315670142 ) ) ;
#24167=CYLINDRICAL_SURFACE ( 'NONE', #30816, 40.00000000000000711 ) ;
#24168=CARTESIAN_POINT ( 'NONE',  ( 53.80794059781069194, -49.14842230199280237, -48.63343936029099979 ) ) ;
#24171=CARTESIAN_POINT ( 'NONE',  ( 17.21347160910390173, -53.11618894467930119, -76.14999999999999147 ) ) ;
#24180=CARTESIAN_POINT ( 'NONE',  ( 68.13393739769620083, 18.13381105532069881, -71.50000000000000000 ) ) ;
#24185=CARTESIAN_POINT ( 'NONE',  ( 17.33622727253819917, 21.74151571116259873, -76.14999999999999147 ) ) ;
#24186=ORIENTED_EDGE ( 'NONE', *, *, #39971, .F. ) ;
#24187=ORIENTED_EDGE ( 'NONE', *, *, #7030, .F. ) ;
#24188=CARTESIAN_POINT ( 'NONE',  ( 57.42983846519040725, -45.73690961613799999, -26.26079255916740252 ) ) ;
#24190=CARTESIAN_POINT ( 'NONE',  ( 61.71598194884530386, 13.91966528094189925, -46.75058645329289675 ) ) ;
#24193=CARTESIAN_POINT ( 'NONE',  ( 12.09990269636916871, 34.01294328777810705, -16.83009735979323196 ) ) ;
#24195=PLANE ( 'NONE',  #34448 ) ;
#24199=CARTESIAN_POINT ( 'NONE',  ( 72.13393739769620083, -1.116188944679340045, -20.65000000000000213 ) ) ;
#24201=CARTESIAN_POINT ( 'NONE',  ( 61.16964974363649787, 14.21611140120430150, -47.43903885526910358 ) ) ;
#24202=CARTESIAN_POINT ( 'NONE',  ( 49.03396268060160423, 14.94209610719759951, -11.76399786255080038 ) ) ;
#24203=CARTESIAN_POINT ( 'NONE',  ( -10.89822638436359981, 11.09799366564529954, -6.199143116420779975 ) ) ;
#24205=VECTOR ( 'NONE', #25626, 1000.000000000000114 ) ;
#24208=CARTESIAN_POINT ( 'NONE',  ( 60.57156752678139355, 14.04241620716539884, -27.07292534466720113 ) ) ;
#24209=CIRCLE ( 'NONE', #45997, 40.00000000000000711 ) ;
#24210=EDGE_CURVE ( 'NONE', #21618, #28327, #22879, .T. ) ;
#24213=CARTESIAN_POINT ( 'NONE',  ( 53.41693480164789776, 18.12090330447900044, -48.75416851879769808 ) ) ;
#24215=CARTESIAN_POINT ( 'NONE',  ( 11.65854852791870044, 33.64587830465290352, -45.04862363297149841 ) ) ;
#24218=DIRECTION ( 'NONE',  ( 0.000000000000000000, 0.000000000000000000, -1.000000000000000000 ) ) ;
#24220=CARTESIAN_POINT ( 'NONE',  ( 47.20049209618989750, 23.55315852235050045, -74.36225199019699517 ) ) ;
#24221=CARTESIAN_POINT ( 'NONE',  ( 48.48681609642030566, -54.13994113942329278, -54.95545728264639962 ) ) ;
#24222=CARTESIAN_POINT ( 'NONE',  ( 51.51228236258946680, -32.18033297859199138, -17.73310860033575764 ) ) ;
#24231=CARTESIAN_POINT ( 'NONE',  ( 61.06210316266220417, -45.44419311714590748, -47.37017503401310137 ) ) ;
#24238=EDGE_LOOP ( 'NONE', ( #4555, #29943, #14702, #24186, #33888 ) ) ;
#24239=CARTESIAN_POINT ( 'NONE',  ( 83.87142430054410625, -44.85900700689950327, -47.47134017317799959 ) ) ;
#24240=ORIENTED_EDGE ( 'NONE', *, *, #25179, .T. ) ;
#24245=CARTESIAN_POINT ( 'NONE',  ( 11.53605495837543948, -55.35105376503654639, -21.73576846289474318 ) ) ;
#24247=CARTESIAN_POINT ( 'NONE',  ( 76.42290226885830862, -8.715687769802094920, -12.89519280475484209 ) ) ;
#24248=CARTESIAN_POINT ( 'NONE',  ( 49.80812477255949489, -53.32727295909180043, -54.05131971329959839 ) ) ;
#24254=VECTOR ( 'NONE', #23880, 1000.000000000000114 ) ;
#24256=B_SPLINE_CURVE_WITH_KNOTS ( 'NONE', 3,
 ( #27431, #11474, #35820, #43434, #50784, #14874, #35032, #3345, #19321, #26648, #7537, #42667, #6767, #22719, #42925, #51038, #47375, #35302, #51300, #7023, #23482, #22975, #3605, #19576, #44199, #28715, #28980, #40782, #40273, #28458, #11987, #24507, #8822, #48392, #44458, #20081, #8041, #44979, #4361, #9081, #16158, #4103, #12490, #32116, #23995, #15911, #40016, #47884, #51805, #31867, #48134, #27940, #43945, #36073, #32895, #32373, #685, #25029, #12234, #44716, #431, #41045, #179, #8565, #24773, #36320, #36582, #4884, #20332, #13026, #28196, #8297, #24247, #5158, #21827, #16417, #953, #40526, #4618, #20588, #48927, #16673, #32632, #48659, #12758, #16949, #20850, #36849, #17908, #26794, #30209, #10828, #38346, #38614, #38089, #14493, #7160, #42805, #2185, #18419, #22340, #6379, #50140, #18165, #33877, #10314, #6901, #42545, #30465, #46225, #14753, #15008, #22852, #26275, #46485, #49890, #10574, #46746 ),
 .UNSPECIFIED., .F., .F.,
 ( 4, 2, 1, 1, 1, 2, 2, 1, 2, 2, 2, 1, 1, 1, 1, 1, 1, 1, 2, 2, 2, 2, 2, 1, 1, 1, 1, 1, 2, 2, 2, 2, 1, 1, 2, 2, 2, 2, 1, 1, 2, 2, 1, 1, 1, 1, 2, 2, 1, 1, 1, 1, 2, 2, 1, 1, 2, 2, 2, 1, 1, 1, 1, 2, 2, 1, 1, 2, 2, 2, 1, 2, 2, 1, 1, 1, 1, 1, 2, 4 ),
 ( 0.000000000000000000, 0.2499999999972345455, 0.2812499999968888775, 0.2968749999967161268, 0.2988281249966943665, 0.2998046874966834863, 0.3007812499966726616, 0.3046874999966289188, 0.3124999999965417663, 0.3437499999961932118, 0.3593749999960189068, 0.3671874999959318098, 0.3710937499958883445, 0.3730468749958665287, 0.3740234374958556485, 0.3745117187458500418, 0.3747558593708472663, 0.3748779296833459895, 0.3749389648395953789, 0.3749999999958447683, 0.4062499999955537788, 0.4218749999954082286, 0.4296874999953354535, 0.4335937499952993157, 0.4355468749952812746, 0.4365234374952717822, 0.4370117187452666196, 0.4372558593702645102, 0.4373779296827634555, 0.4374999999952623453, 0.4687499999950052731, 0.4843749999948768759, 0.4921874999948127605, 0.4960937499947808416, 0.4980468749947649099, 0.4999999999947489782, 0.5312499999944939599, 0.5390624999944302331, 0.5429687499943983697, 0.5449218749943823825, 0.5458984374943743889, 0.5468749999943663953, 0.5624999999942384976, 0.5781249999941105999, 0.5859374999940466511, 0.5898437499940146767, 0.5917968749939988005, 0.5937499999939828133, 0.6249999999937280171, 0.6562499999934733319, 0.6601562499934414685, 0.6621093749934254813, 0.6630859374934174877, 0.6633300781184153783, 0.6635742187434133799, 0.6640624999934093831, 0.6718749999933307793, 0.6874999999931732386, 0.7187499999928583794, 0.7226562499928189665, 0.7236328124928091965, 0.7241210937428042005, 0.7243652343678017580, 0.7244873046803005368, 0.7245483398365499816, 0.7246093749927994265, 0.7265624999928507188, 0.7343749999930548888, 0.7499999999934631179, 0.7812499999942796869, 0.7851562499943818274, 0.7856445312443947060, 0.7858886718694010343, 0.7861328124944074736, 0.7871093749944330087, 0.7890624999944840789, 0.7968749999946883600, 0.8124999999950969221, 0.8749999999967311703, 1.000000000000000000 ),
 .UNSPECIFIED. ) ;
#24257=CARTESIAN_POINT ( 'NONE',  ( 57.20754666121199961, -45.13815381503769686, -25.31149905167690051 ) ) ;
#24259=CARTESIAN_POINT ( 'NONE',  ( 16.13393739769620083, -15.61618894467929941, -5.740514720465069942 ) ) ;
#24262=CARTESIAN_POINT ( 'NONE',  ( 52.15299206959110023, -49.68190268104039831, -77.15977264154089710 ) ) ;
#24263=EDGE_CURVE ( 'NONE', #19930, #19589, #3325, .T. ) ;
#24264=ORIENTED_EDGE ( 'NONE', *, *, #38951, .T. ) ;
#24266=CARTESIAN_POINT ( 'NONE',  ( 52.97782969051129953, -50.30123836914950175, -77.23919107196950051 ) ) ;
#24268=DIRECTION ( 'NONE',  ( 0.000000000000000000, 1.000000000000000000, 0.000000000000000000 ) ) ;
#24270=CARTESIAN_POINT ( 'NONE',  ( 13.39861581086750064, -50.35706945913049992, -21.14264498997030017 ) ) ;
#24274=CARTESIAN_POINT ( 'NONE',  ( 57.41961282339919848, 13.88381105532070059, -17.93020877507790090 ) ) ;
#24275=DIRECTION ( 'NONE',  ( 0.000000000000000000, 0.000000000000000000, 1.000000000000000000 ) ) ;
#24279=ADVANCED_FACE ( 'NONE', ( #9727 ), #14698, .T. ) ;
#24281=CARTESIAN_POINT ( 'NONE',  ( 14.34345188046069985, -51.57142019855179882, -75.41551559479479749 ) ) ;
#24282=CARTESIAN_POINT ( 'NONE',  ( 47.36437953800110279, -54.67829754402429643, -54.76347716479679661 ) ) ;
#24284=CARTESIAN_POINT ( 'NONE',  ( 12.82231730657736257, 34.27273057154334879, -47.70638112244893136 ) ) ;
#24286=CIRCLE ( 'NONE', #2548, 17.39999999999999503 ) ;
#24287=CARTESIAN_POINT ( 'NONE',  ( 60.92101825946003402, -45.44428967124540009, -47.19725562356851611 ) ) ;
#24290=DIRECTION ( 'NONE',  ( 0.000000000000000000, 0.000000000000000000, -1.000000000000000000 ) ) ;
#24292=CARTESIAN_POINT ( 'NONE',  ( 10.63085527536540020, 33.60671078422439706, -18.12439166827990178 ) ) ;
#24294=CARTESIAN_POINT ( 'NONE',  ( 12.35956436866795727, -50.22963602464601962, -21.15000000006194369 ) ) ;
#24296=CARTESIAN_POINT ( 'NONE',  ( 48.46943201930690037, 22.93089287882050087, -55.04752992213770568 ) ) ;
#24297=ORIENTED_EDGE ( 'NONE', *, *, #36750, .T. ) ;
#24298=CARTESIAN_POINT ( 'NONE',  ( 52.69326468654779205, -49.76107638029880320, -48.74393324173220066 ) ) ;
#24300=CARTESIAN_POINT ( 'NONE',  ( 18.67893569163094725, -51.93861847160620471, -75.09855816265704220 ) ) ;
#24303=CARTESIAN_POINT ( 'NONE',  ( 82.49223220840640636, 13.86914553491480007, -46.59234684980529551 ) ) ;
#24304=CARTESIAN_POINT ( 'NONE',  ( 54.31423360305029746, 16.85098597931899889, -26.53140032282190219 ) ) ;
#24306=CARTESIAN_POINT ( 'NONE',  ( 52.67899906575139113, 18.54202610784680161, -48.75316747057349431 ) ) ;
#24307=CARTESIAN_POINT ( 'NONE',  ( 56.44084032582000532, -45.18826010465620158, -16.10354642779179812 ) ) ;
#24309=ORIENTED_EDGE ( 'NONE', *, *, #10875, .F. ) ;
#24312=CARTESIAN_POINT ( 'NONE',  ( 11.27698470052689927, -65.16424334175378874, -17.25002958030430023 ) ) ;
#24313=CARTESIAN_POINT ( 'NONE',  ( 12.60445274137229887, 34.24115893967649527, -47.46978735726350607 ) ) ;
#24314=DIRECTION ( 'NONE',  ( 0.6911981449639439390, -0.7226652920947588266, 0.000000000000000000 ) ) ;
#24315=CARTESIAN_POINT ( 'NONE',  ( 51.63616101854069740, -50.90272864159400257, -50.31291621231439848 ) ) ;
#24316=CARTESIAN_POINT ( 'NONE',  ( 10.85712480788070167, -64.59421087333633693, -23.35787417042663705 ) ) ;
#24319=CARTESIAN_POINT ( 'NONE',  ( 52.27483174160517621, -50.84964383646082808, -50.96525577083021830 ) ) ;
#24320=CARTESIAN_POINT ( 'NONE',  ( 11.13393739769619906, -63.30396901272830945, -43.91553734765660266 ) ) ;
#24321=EDGE_CURVE ( 'NONE', #26727, #10857, #33769, .T. ) ;
#24325=CARTESIAN_POINT ( 'NONE',  ( 50.30621290460380379, -48.75259804172680589, -76.16272939178270462 ) ) ;
#24330=CYLINDRICAL_SURFACE ( 'NONE', #5814, 1.000000000000000444 ) ;
#24331=CARTESIAN_POINT ( 'NONE',  ( 56.93466175439829868, -50.26424374751940150, -52.70269902980160026 ) ) ;
#24332=CARTESIAN_POINT ( 'NONE',  ( 60.29341046574950269, 14.73091211308410031, -47.84808156045389893 ) ) ;
#24333=CIRCLE ( 'NONE', #1762, 20.29675463313339989 ) ;
#24335=CARTESIAN_POINT ( 'NONE',  ( 52.82750202116550042, -49.69555339446630171, -48.94276309583950280 ) ) ;
#24336=PLANE ( 'NONE',  #8777 ) ;
#24342=CARTESIAN_POINT ( 'NONE',  ( 12.48566319264315716, 34.18281312454822540, -23.53955123170710095 ) ) ;
#24345=CARTESIAN_POINT ( 'NONE',  ( 46.87775759358779482, 22.67357701198350028, -75.82248416561151316 ) ) ;
#24348=CARTESIAN_POINT ( 'NONE',  ( -2.623662905535780077, 17.43154064245049994, -4.296538310234220504 ) ) ;
#24349=CARTESIAN_POINT ( 'NONE',  ( 12.29766918194670033, 33.39812178576170254, -15.84900139484649984 ) ) ;
#24351=CARTESIAN_POINT ( 'NONE',  ( 56.30960098403389935, -50.61618702972189965, -75.76111591682739288 ) ) ;
#24355=CARTESIAN_POINT ( 'NONE',  ( 61.08966237208559846, 14.10374299845339863, -46.92975878837979309 ) ) ;
#24356=CARTESIAN_POINT ( 'NONE',  ( 6.312816564080409698, -63.12436966802319205, -47.22137548220880632 ) ) ;
#24357=ORIENTED_EDGE ( 'NONE', *, *, #33098, .T. ) ;
#24358=CARTESIAN_POINT ( 'NONE',  ( 52.86024057890890049, -49.64494889463909999, -48.64479820451980174 ) ) ;
#24360=CARTESIAN_POINT ( 'NONE',  ( 61.03683084929289748, -45.19175033160959742, -27.29275181042889997 ) ) ;
#24362=CARTESIAN_POINT ( 'NONE',  ( 13.08122484219290094, 19.68326368368759915, -21.57315878215120009 ) ) ;
#24363=CARTESIAN_POINT ( 'NONE',  ( 56.44602573759370046, 15.00063885377410067, -26.25485097157960013 ) ) ;
#24366=CARTESIAN_POINT ( 'NONE',  ( 50.38251483118710183, 18.64895037491550056, -76.14999999999999147 ) ) ;
#24367=CARTESIAN_POINT ( 'NONE',  ( 52.82298539538220439, 18.43416779221530177, -48.69818189231450134 ) ) ;
#24369=CARTESIAN_POINT ( 'NONE',  ( 40.92757250301959715, -44.41382921904099845, -3.805845460188720164 ) ) ;
#24370=CARTESIAN_POINT ( 'NONE',  ( 45.17943004775749927, -44.39222964805399840, -5.706577274949769851 ) ) ;
#24372=DIRECTION ( 'NONE',  ( -0.9200120562340469155, 0.3918900565005459247, -8.326672684688669123E-17 ) ) ;
#24373=CARTESIAN_POINT ( 'NONE',  ( 47.73667124825149699, -54.43832146008400485, -54.70375119057089819 ) ) ;
#24376=CARTESIAN_POINT ( 'NONE',  ( 60.85130585975760198, 14.27032567669020047, -47.46989369029309813 ) ) ;
#24378=DIRECTION ( 'NONE',  ( 0.000000000000000000, 0.000000000000000000, 1.000000000000000000 ) ) ;
#24383=ORIENTED_EDGE ( 'NONE', *, *, #51653, .T. ) ;
#24385=EDGE_CURVE ( 'NONE', #26354, #38464, #2021, .T. ) ;
#24386=DIRECTION ( 'NONE',  ( 0.000000000000000000, -1.000000000000000000, 0.000000000000000000 ) ) ;
#24388=CARTESIAN_POINT ( 'NONE',  ( 11.18784989604460023, -64.00854436587380292, -43.96560154067280024 ) ) ;
#24389=CARTESIAN_POINT ( 'NONE',  ( 12.39116026363089951, -65.38104286502799312, -46.54587326243779444 ) ) ;
#24392=TOROIDAL_SURFACE ( 'NONE', #30994, 47.00000000000000000, 3.000000000000000000 ) ;
#24395=CARTESIAN_POINT ( 'NONE',  ( 60.74502025776879321, 14.51238070346370002, -47.75426036517409756 ) ) ;
#24399=EDGE_LOOP ( 'NONE', ( #38347, #27179, #6648, #31997 ) ) ;
#24402=CARTESIAN_POINT ( 'NONE',  ( 12.65814259846169954, -65.49670600571860746, -22.98480981823819747 ) ) ;
#24407=CARTESIAN_POINT ( 'NONE',  ( 13.84625307261759986, 20.91303491124859804, -75.51792558472199346 ) ) ;
#24409=CARTESIAN_POINT ( 'NONE',  ( 17.71568183981793609, 20.46959823935371503, -75.56421430877649925 ) ) ;
#24413=CARTESIAN_POINT ( 'NONE',  ( 53.82042919933849845, -48.69340853470760067, -26.93473920014709933 ) ) ;
#24414=CARTESIAN_POINT ( 'NONE',  ( 15.93086454162260068, -51.01877534386230195, -20.59235730855489876 ) ) ;
#24419=ORIENTED_EDGE ( 'NONE', *, *, #5633, .T. ) ;
#24420=CARTESIAN_POINT ( 'NONE',  ( -9.066986571212598989, -44.13582524313829936, -5.880785460427049749 ) ) ;
#24421=CARTESIAN_POINT ( 'NONE',  ( 47.32718728057039925, 23.47016710949800000, -54.75130141235280234 ) ) ;
#24424=CARTESIAN_POINT ( 'NONE',  ( 56.55522360613520760, 14.97957722649010037, -26.26695323647559732 ) ) ;
#24425=CARTESIAN_POINT ( 'NONE',  ( 42.99451563395630416, 11.89542822664250110, -4.474847206224069396 ) ) ;
#24428=DIRECTION ( 'NONE',  ( 1.000000000000000000, 0.000000000000000000, 0.000000000000000000 ) ) ;
#24429=CARTESIAN_POINT ( 'NONE',  ( 57.08228080684060046, -47.57523781541689800, -48.30570546696120005 ) ) ;
#24432=CARTESIAN_POINT ( 'NONE',  ( 17.60467135870129951, -52.01451994755070274, -75.82251062550821530 ) ) ;
#24434=CARTESIAN_POINT ( 'NONE',  ( 54.44697901455320022, 13.88381105532070059, -13.49511142752179893 ) ) ;
#24437=CARTESIAN_POINT ( 'NONE',  ( 10.13821898889280071, 31.93693633726830328, -45.99533705415459650 ) ) ;
#24439=CARTESIAN_POINT ( 'NONE',  ( 43.46649277351350094, 13.81022299180570023, -6.433241829987640159 ) ) ;
#24440=CARTESIAN_POINT ( 'NONE',  ( 68.16054639260629244, -30.33163972796129926, -18.00105978623409797 ) ) ;
#24442=CARTESIAN_POINT ( 'NONE',  ( 17.79306446254500074, 20.39333564065439930, -75.48537863783369062 ) ) ;
#24443=ORIENTED_EDGE ( 'NONE', *, *, #39684, .F. ) ;
#24444=ORIENTED_EDGE ( 'NONE', *, *, #27186, .F. ) ;
#24446=B_SPLINE_CURVE_WITH_KNOTS ( 'NONE', 3,
 ( #2181, #30460, #6631, #33619, #10824, #33872, #46481, #18674, #10570, #45952, #22336, #26526, #2700, #42541 ),
 .UNSPECIFIED., .F., .F.,
 ( 4, 2, 2, 2, 1, 1, 2, 4 ),
 ( 0.000000000000000000, 0.2471173528950013354, 0.3706760293425083730, 0.4324553675662667906, 0.4633450366781509122, 0.4787898712340928897, 0.4865122885120643503, 0.4942347057900358109 ),
 .UNSPECIFIED. ) ;
#24448=CYLINDRICAL_SURFACE ( 'NONE', #37763, 1.999999999999997335 ) ;
#24451=CARTESIAN_POINT ( 'NONE',  ( 59.34499803081109803, -28.11618894467929763, -15.68015151901639825 ) ) ;
#24453=ORIENTED_EDGE ( 'NONE', *, *, #28727, .F. ) ;
#24456=B_SPLINE_SURFACE_WITH_KNOTS ( 'NONE', 3, 3, ( 
 ( #29667, #38071, #49104, #46208, #10293, #2167, #25472, #33606, #13205, #13461, #1390, #9268, #5335, #45420, #5592, #9525, #41476, #21546, #5842, #25729, #41737, #1648, #49620, #13713, #45676, #10812, #11073, #3204, #30706, #39364 ),
 ( #26256, #51419, #50389, #50639, #42262, #47238, #3466, #2688, #34634, #19437, #6361, #38327, #15513, #14473, #43302, #51163, #18660, #26771, #46988, #35417, #10555, #35155, #46467, #26512, #42789, #27039, #43044, #14990, #7140, #31467 ),
 ( #30956, #31211, #22321, #47491, #2417, #27293, #6884, #2944, #7393, #14735, #22580, #18398, #34377, #30446, #22834, #46728, #42528, #23341, #23092, #39111, #19176, #6616, #38597, #34898, #15256, #38855, #11329, #18915, #50898, #24626 ),
 ( #35929, #20703, #32744, #40637, #12608, #36183, #4736, #35685, #44570, #36694, #8162, #4476, #31978, #44310, #48251, #19693, #794, #16796, #12345, #28311, #24367, #19939, #16275, #44056, #11587, #27548, #28054, #8419, #24105, #28571 ),
 ( #40380, #46, #16023, #47998, #20445, #8671, #39617, #12098, #36433, #7656, #541, #3720, #51670, #40126, #15764, #27807, #16527, #4219, #32477, #20193, #48507, #31717, #32228, #43554, #23599, #47742, #11850, #43804, #7904, #290 ),
 ( #23851, #39875, #3974, #6039, #13394, #29607, #41156, #29093, #12875, #24884, #9460, #17822, #9964, #13898, #40896, #18080, #5269, #25669, #9199, #21220, #37484, #13144, #5777, #44836, #25409, #33796, #25151, #48771, #21996, #20966 ),
 ( #49805, #21485, #41939, #36967, #29856, #25924, #45358, #41671, #17317, #45610, #33542, #5006, #38006, #2104, #49560, #13647, #9709, #37232, #1585, #29352, #28831, #8941, #41412, #21739, #5530, #45877, #33281, #1329, #33013, #1064 ),
 ( #37746, #17060, #49036, #49297, #1844, #45092, #17573, #10232, #22257, #34574, #38264, #50325, #30892, #38527, #14927, #42464, #23027, #2357, #2883, #46919, #11005, #35090, #26973, #18333, #34312, #22518, #42724, #26703, #27225, #42982 ),
 ( #50579, #7077, #26448, #14411, #50058, #26190, #46663, #3143, #47175, #51091, #42201, #3404, #6551, #39049, #11264, #19111, #2626, #15189, #31150, #43239, #7330, #30639, #6818, #30379, #6299, #23277, #18598, #39299, #46404, #22772 ),
 ( #10492, #14669, #14154, #10746, #30122, #34048, #46141, #38791, #18851, #34834, #50835, #480, #51863, #20134, #48446, #15702, #48185, #19879, #4418, #27993, #47938, #24306, #24045, #31658, #11785, #32169, #32423, #36125, #16468, #51353 ),
 ( #20384, #12289, #3658, #19630, #7844, #43996, #12039, #12548, #16212, #24563, #36373, #19371, #28514, #23792, #229, #8102, #39808, #47682, #40066, #8356, #4159, #35353, #28250, #44511, #44248, #3916, #40323, #8615, #35620, #40576 ) ),
 .UNSPECIFIED., .F., .F., .F.,
 ( 4, 1, 1, 1, 1, 1, 1, 1, 4 ),
 ( 4, 2, 2, 2, 2, 2, 2, 2, 2, 2, 2, 2, 2, 2, 4 ),
 ( 0.000000000000000000, 0.1250000000000000000, 0.2500000000000000000, 0.3750000000000000000, 0.5000000000000000000, 0.6250000000000000000, 0.7500000000000000000, 0.8750000000000000000, 1.000000000000000000 ),
 ( -1.979714999999999961E-13, 0.09067117207851999039, 0.2140248969013430203, 0.2911209749156069559, 0.3773790415573270440, 0.4312903332084020436, 0.4852016248594769876, 0.5283306581803369761, 0.5714596915011970202, 0.6404661448145729796, 0.6753595992144020288, 0.7102530536142309670, 0.7544417240960439308, 0.8251435968669439402, 0.8625806664170020399 ),
 .UNSPECIFIED. ) ;
#24459=CARTESIAN_POINT ( 'NONE',  ( 11.66595244850846314, -64.88074487536820811, -23.89163317478661241 ) ) ;
#24463=DIRECTION ( 'NONE',  ( 1.000000000000000000, 0.000000000000000000, 0.000000000000000000 ) ) ;
#24464=CARTESIAN_POINT ( 'NONE',  ( 11.09249001376588240, -65.15264562256584213, -17.64371731244277441 ) ) ;
#24465=CARTESIAN_POINT ( 'NONE',  ( 60.91971420063490683, 14.46337360283989959, -47.74179738751160329 ) ) ;
#24466=CARTESIAN_POINT ( 'NONE',  ( 46.21098136784690524, 13.96635512142479918, -8.540225283467140827 ) ) ;
#24469=CARTESIAN_POINT ( 'NONE',  ( -10.89697165533940115, 11.09930551684650091, -6.204277548033930501 ) ) ;
#24470=CIRCLE ( 'NONE', #5298, 1.999999999999998668 ) ;
#24472=CARTESIAN_POINT ( 'NONE',  ( 57.58395499372409887, 14.48151100416250081, -26.27729977557869745 ) ) ;
#24475=CARTESIAN_POINT ( 'NONE',  ( 59.98335056725809977, 14.70517998043040109, -47.53560967005149962 ) ) ;
#24477=CARTESIAN_POINT ( 'NONE',  ( 52.56521937542130019, 18.62941943741099848, -48.47378147059570352 ) ) ;
#24481=EDGE_CURVE ( 'NONE', #45923, #28860, #13101, .T. ) ;
#24482=CARTESIAN_POINT ( 'NONE',  ( 46.37015983751390280, 21.71648543033839829, -76.14999999999999147 ) ) ;
#24483=CARTESIAN_POINT ( 'NONE',  ( 49.60483365582589954, -53.69855377821179587, -55.15230005116299594 ) ) ;
#24484=CARTESIAN_POINT ( 'NONE',  ( -10.41557261171689852, 11.58869671994870032, -6.169019698314530231 ) ) ;
#24488=CARTESIAN_POINT ( 'NONE',  ( 55.82175251386000525, 13.88381105532070059, -14.52096918537739967 ) ) ;
#24493=CARTESIAN_POINT ( 'NONE',  ( 60.86554014449199457, -45.45472802933989698, -47.11666279147539882 ) ) ;
#24495=CARTESIAN_POINT ( 'NONE',  ( 58.84616880385656401, -43.44694404977806812, -8.775629712027942730 ) ) ;
#24498=CARTESIAN_POINT ( 'NONE',  ( 68.13393739769630031, 16.88381105532069881, -71.50000000000000000 ) ) ;
#24501=CARTESIAN_POINT ( 'NONE',  ( 84.44784216359251161, -43.11618894467930119, -47.47585302082339354 ) ) ;
#24502=ORIENTED_EDGE ( 'NONE', *, *, #33917, .T. ) ;
#24504=CARTESIAN_POINT ( 'NONE',  ( 61.40055391219659953, -45.31037351547990255, -47.20955474051870482 ) ) ;
#24505=CARTESIAN_POINT ( 'NONE',  ( 53.82998062364706726, -50.59960046679898937, -77.06221267959426768 ) ) ;
#24507=CARTESIAN_POINT ( 'NONE',  ( 76.40158688816870836, -19.74821089629645243, -12.80337776394537030 ) ) ;
#24508=CARTESIAN_POINT ( 'NONE',  ( 51.29528453023580425, -52.95704580151759444, -54.37422039053849687 ) ) ;
#24509=EDGE_CURVE ( 'NONE', #16879, #38586, #47069, .T. ) ;
#24512=VERTEX_POINT ( 'NONE', #2838 ) ;
#24513=EDGE_CURVE ( 'NONE', #46034, #43570, #50791, .T. ) ;
#24519=LINE ( 'NONE', #36593, #25074 ) ;
#24522=CARTESIAN_POINT ( 'NONE',  ( 52.38386414254079426, -49.88582441666579825, -77.22931079715800706 ) ) ;
#24529=FACE_OUTER_BOUND ( 'NONE', #50381, .T. ) ;
#24530=EDGE_CURVE ( 'NONE', #5619, #49749, #11415, .T. ) ;
#24531=CARTESIAN_POINT ( 'NONE',  ( 41.60772359302610113, -44.62161519139999655, -5.233302501927670214 ) ) ;
#24532=CARTESIAN_POINT ( 'NONE',  ( 18.03855228839456970, -51.11618894468890062, -15.68043506693139832 ) ) ;
#24536=ORIENTED_EDGE ( 'NONE', *, *, #20255, .T. ) ;
#24537=CARTESIAN_POINT ( 'NONE',  ( 14.24806556045970041, -51.98087455372210286, -75.71853508996549920 ) ) ;
#24538=CARTESIAN_POINT ( 'NONE',  ( 47.35028767480929446, -54.68244725382609772, -54.65313065648980029 ) ) ;
#24544=CARTESIAN_POINT ( 'NONE',  ( 61.00027414223083611, -45.45014343267921930, -47.32927810435275262 ) ) ;
#24545=EDGE_CURVE ( 'NONE', #7985, #2432, #46612, .T. ) ;
#24546=DIRECTION ( 'NONE',  ( 0.000000000000000000, 0.000000000000000000, 1.000000000000000000 ) ) ;
#24547=CARTESIAN_POINT ( 'NONE',  ( 11.73422653530680115, 34.19011593798479964, -18.16216258077279733 ) ) ;
#24548=ADVANCED_FACE ( 'NONE', ( #22206 ), #46875, .T. ) ;
#24551=CARTESIAN_POINT ( 'NONE',  ( -11.32734370190460105, -41.88171845330919751, -6.430192534648670133 ) ) ;
#24552=CARTESIAN_POINT ( 'NONE',  ( 43.09344256680816443, 12.72802089079580412, -5.051331040473342249 ) ) ;
#24553=CARTESIAN_POINT ( 'NONE',  ( 48.40697635570069934, 22.96883648311629855, -55.14150811720919876 ) ) ;
#24554=ORIENTED_EDGE ( 'NONE', *, *, #7759, .F. ) ;
#24556=ORIENTED_EDGE ( 'NONE', *, *, #43902, .F. ) ;
#24557=CARTESIAN_POINT ( 'NONE',  ( 18.74892447570123366, -51.88237913653802735, -74.91995119709325479 ) ) ;
#24558=CARTESIAN_POINT ( 'NONE',  ( 53.41693480158270546, -49.35328119387190071, -48.75416851881869462 ) ) ;
#24559=DIRECTION ( 'NONE',  ( 0.000000000000000000, 0.000000000000000000, 1.000000000000000000 ) ) ;
#24560=CARTESIAN_POINT ( 'NONE',  ( 83.27189663703491362, 13.64797996652180068, -46.76788818508799750 ) ) ;
#24561=CARTESIAN_POINT ( 'NONE',  ( 53.01071900028409800, 18.17451771224559920, -27.28273396498699910 ) ) ;
#24563=CARTESIAN_POINT ( 'NONE',  ( 53.05489977530229595, 18.36750851102400262, -49.10811586475909962 ) ) ;
#24564=CARTESIAN_POINT ( 'NONE',  ( 56.73667420261889305, -45.26434326652640294, -17.93020191283299880 ) ) ;
#24567=VERTEX_POINT ( 'NONE', #38744 ) ;
#24568=ORIENTED_EDGE ( 'NONE', *, *, #7249, .F. ) ;
#24569=CARTESIAN_POINT ( 'NONE',  ( 11.98171981665329966, -65.04908998879550097, -16.46086821535179823 ) ) ;
#24570=CARTESIAN_POINT ( 'NONE',  ( 12.03939575523859951, 34.11084159468560273, -47.24132823177560425 ) ) ;
#24573=CARTESIAN_POINT ( 'NONE',  ( 52.60056159696439693, -50.12372689670589665, -49.79359568308569806 ) ) ;
#24578=CARTESIAN_POINT ( 'NONE',  ( 11.13393739769619906, -63.31057960318910460, -43.74730822310910128 ) ) ;
#24579=AXIS2_PLACEMENT_3D ( 'NONE', #30649, #2636, #15464 ) ;
#24581=CARTESIAN_POINT ( 'NONE',  ( 47.55940100909866430, 23.33745173926940453, -55.06178025467780657 ) ) ;
#24582=CARTESIAN_POINT ( 'NONE',  ( 50.93004497053770052, -50.92639964791920448, -76.14999999999999147 ) ) ;
#24585=VERTEX_POINT ( 'NONE', #42931 ) ;
#24588=CARTESIAN_POINT ( 'NONE',  ( 56.73072851771979686, -50.34974087631989903, -52.75329813171639870 ) ) ;
#24589=CARTESIAN_POINT ( 'NONE',  ( 54.24589373054839569, 17.44605741449650083, -48.34735630146840180 ) ) ;
#24591=CARTESIAN_POINT ( 'NONE',  ( 13.68997055383310091, -51.35827251140110405, -23.13969639952529889 ) ) ;
#24592=CARTESIAN_POINT ( 'NONE',  ( 53.64448049682719954, 20.03493786279390321, -75.63065916943469347 ) ) ;
#24594=CARTESIAN_POINT ( 'NONE',  ( 47.16864635708999742, -54.20974419499959396, -75.46775895608709561 ) ) ;
#24595=EDGE_LOOP ( 'NONE', ( #9219, #14947 ) ) ;
#24598=CARTESIAN_POINT ( 'NONE',  ( 53.42000044619080512, -49.46448084836430326, -49.21358545526090467 ) ) ;
#24599=DIRECTION ( 'NONE',  ( 1.000000000000000000, 0.000000000000000000, 0.000000000000000000 ) ) ;
#24600=CARTESIAN_POINT ( 'NONE',  ( 12.54176915115859181, 34.20132235598342874, -23.51595098417593022 ) ) ;
#24602=CARTESIAN_POINT ( 'NONE',  ( 47.24349440877020356, 23.09672500570559706, -75.29141078596350667 ) ) ;
#24603=CARTESIAN_POINT ( 'NONE',  ( 19.74336188031776373, -54.29616745937406108, -17.45721575027601347 ) ) ;
#24605=CARTESIAN_POINT ( 'NONE',  ( 12.30205595647769989, 33.50594860225369587, -15.96528926831930129 ) ) ;
#24609=EDGE_CURVE ( 'NONE', #3072, #19396, #8333, .T. ) ;
#24611=CARTESIAN_POINT ( 'NONE',  ( -10.74337798235499974, 10.09066047292260038, -4.376538325821149655 ) ) ;
#24612=LINE ( 'NONE', #16261, #3878 ) ;
#24613=AXIS2_PLACEMENT_3D ( 'NONE', #18344, #31928, #16225 ) ;
#24615=CARTESIAN_POINT ( 'NONE',  ( 61.45021783597690046, 13.92999906544429933, -46.45636237004219993 ) ) ;
#24617=CARTESIAN_POINT ( 'NONE',  ( -12.40573950840640016, -56.00019996439819892, -51.46982831076100240 ) ) ;
#24620=CARTESIAN_POINT ( 'NONE',  ( 52.97622290741030326, -49.58418250313399511, -48.78091471321639716 ) ) ;
#24621=LINE ( 'NONE', #24879, #22839 ) ;
#24623=CARTESIAN_POINT ( 'NONE',  ( 56.83722719842539561, 14.19618794446390098, -25.88848200734760141 ) ) ;
#24625=CARTESIAN_POINT ( 'NONE',  ( 50.48048356710739881, 18.85947689767530377, -76.14999999999999147 ) ) ;
#24626=CARTESIAN_POINT ( 'NONE',  ( 52.79307622657449883, 18.44841517198999625, -48.47378032971769812 ) ) ;
#24628=DIRECTION ( 'NONE',  ( 4.486507500526829843E-12, 3.054623595244970244E-12, -1.000000000000000000 ) ) ;
#24633=CARTESIAN_POINT ( 'NONE',  ( 47.73232013880370772, -54.44372343144849680, -54.71634908794329277 ) ) ;
#24636=CARTESIAN_POINT ( 'NONE',  ( 41.55663457306080488, 12.62725083537310056, -3.466044030332980252 ) ) ;
#24637=CARTESIAN_POINT ( 'NONE',  ( 60.80486542312029741, 14.95141560336979936, -48.31465950696279776 ) ) ;
#24647=CARTESIAN_POINT ( 'NONE',  ( 57.07894513400979974, 18.98008675654529753, -52.67137582195630330 ) ) ;
#24648=CARTESIAN_POINT ( 'NONE',  ( 16.15069521921704165, -51.05177107958204630, -15.66900421577824254 ) ) ;
#24649=ORIENTED_EDGE ( 'NONE', *, *, #45123, .T. ) ;
#24651=CARTESIAN_POINT ( 'NONE',  ( 60.23130391296999875, -45.78304229081430066, -47.24246919202539630 ) ) ;
#24652=CARTESIAN_POINT ( 'NONE',  ( 57.50723798014340105, 13.88381064843590096, -25.33268340738889890 ) ) ;
#24653=CARTESIAN_POINT ( 'NONE',  ( 51.30756405184769875, 19.59276739940289858, -76.17053259469020077 ) ) ;
#24654=ORIENTED_EDGE ( 'NONE', *, *, #40847, .F. ) ;
#24657=CARTESIAN_POINT ( 'NONE',  ( 60.41031540318880388, 14.61374793670090000, -47.73939764751050063 ) ) ;
#24660=CIRCLE ( 'NONE', #2091, 2.745152743487029756 ) ;
#24665=CARTESIAN_POINT ( 'NONE',  ( 40.82287771318460301, 14.16359845706069898, -5.804582292309759417 ) ) ;
#24666=CARTESIAN_POINT ( 'NONE',  ( 52.26504646883520167, 18.55116755685089913, -77.19463087837650050 ) ) ;
#24667=CARTESIAN_POINT ( 'NONE',  ( 13.39998208310050032, -51.78678246903520233, -74.14999999999999147 ) ) ;
#24668=CARTESIAN_POINT ( 'NONE',  ( 56.13393739769620083, -15.61618894467859953, -3.187564294433463008 ) ) ;
#24670=ORIENTED_EDGE ( 'NONE', *, *, #27044, .F. ) ;
#24671=CARTESIAN_POINT ( 'NONE',  ( 54.50086469845559378, -48.02103409330769779, -26.62677904963780051 ) ) ;
#24672=AXIS2_PLACEMENT_3D ( 'NONE', #516, #12324, #24599 ) ;
#24674=CARTESIAN_POINT ( 'NONE',  ( 14.56142577300950158, -51.11619481415970512, -22.31059544230570069 ) ) ;
#24675=CARTESIAN_POINT ( 'NONE',  ( 50.14053598161640224, -36.67694914693753105, -76.15143915218567372 ) ) ;
#24676=CARTESIAN_POINT ( 'NONE',  ( 16.13393739769620083, -15.61618894467929941, -6.721843382729280059 ) ) ;
#24677=CARTESIAN_POINT ( 'NONE',  ( 75.46929132602400614, 12.36451391831151270, -13.44110377523724509 ) ) ;
#24680=CARTESIAN_POINT ( 'NONE',  ( -3.546948566059239916, -48.75848200741000227, -5.665576563160169776 ) ) ;
#24681=CARTESIAN_POINT ( 'NONE',  ( 47.33041554461919986, 23.46292742803399989, -54.63195680419789824 ) ) ;
#24685=CARTESIAN_POINT ( 'NONE',  ( 11.93488809551230112, 34.20717902861789383, -17.90291664076359979 ) ) ;
#24687=CARTESIAN_POINT ( 'NONE',  ( 68.13393739769708191, 17.98087126524919555, -68.79648330188413752 ) ) ;
#24688=DIRECTION ( 'NONE',  ( -0.6911981449639438280, -0.7226652920947587155, -3.885780586188047891E-16 ) ) ;
#24689=CARTESIAN_POINT ( 'NONE',  ( 54.36584921719999386, -48.99915756198799954, -48.99053282728779379 ) ) ;
#24692=CARTESIAN_POINT ( 'NONE',  ( 17.63739037456999981, -52.51931604725010061, -76.04695140691811162 ) ) ;
#24697=CARTESIAN_POINT ( 'NONE',  ( 9.284658136444910781, 31.95765349661940036, -46.53066704864979641 ) ) ;
#24698=CARTESIAN_POINT ( 'NONE',  ( 41.84489819291530210, 13.62916984612999904, -5.635697468575719959 ) ) ;
#24699=CARTESIAN_POINT ( 'NONE',  ( 68.39017786503269747, -30.34043394131120408, -18.15414633457509908 ) ) ;
#24702=CARTESIAN_POINT ( 'NONE',  ( 18.39354190614909967, 20.87662390947729918, -75.53341961486960088 ) ) ;
#24707=CARTESIAN_POINT ( 'NONE',  ( 10.72704221230929988, -63.83388919140170259, -45.49767852026099746 ) ) ;
#24711=CARTESIAN_POINT ( 'NONE',  ( 61.51123563376980030, 13.94229735801039993, -46.77252351816970588 ) ) ;
#24712=ORIENTED_EDGE ( 'NONE', *, *, #24210, .T. ) ;
#24713=CARTESIAN_POINT ( 'NONE',  ( 75.24637618196231870, 2.935769708213510576, -12.27223567965690698 ) ) ;
#24715=CARTESIAN_POINT ( 'NONE',  ( 11.93488785502882799, 34.20717900760969599, -17.90291655963030237 ) ) ;
#24717=CARTESIAN_POINT ( 'NONE',  ( 48.60192464956850245, -46.16790854508710140, -11.45750858288359808 ) ) ;
#24718=CIRCLE ( 'NONE', #35638, 31.00000000000000000 ) ;
#24720=B_SPLINE_CURVE_WITH_KNOTS ( 'NONE', 3,
 ( #47586, #47335, #11430, #11681 ),
 .UNSPECIFIED., .F., .F.,
 ( 4, 4 ),
 ( 3.627924839442150162, 3.679879811498320219 ),
 .UNSPECIFIED. ) ;
#24723=ORIENTED_EDGE ( 'NONE', *, *, #16820, .F. ) ;
#24725=CARTESIAN_POINT ( 'NONE',  ( 11.78395124411410322, -65.42271807245853665, -17.88069317963548954 ) ) ;
#24726=CARTESIAN_POINT ( 'NONE',  ( 73.29566088972229920, 12.14852325496580043, -12.77663947542729872 ) ) ;
#24727=CARTESIAN_POINT ( 'NONE',  ( 49.66581511508110935, 14.35062369332880117, -11.70419715158129925 ) ) ;
#24728=CARTESIAN_POINT ( 'NONE',  ( 16.13393739769620083, -15.61618894467929941, -19.14999999999999858 ) ) ;
#24729=CARTESIAN_POINT ( 'NONE',  ( -4.848012345730049688, 16.07167109130610072, -4.416243733086949952 ) ) ;
#24732=CARTESIAN_POINT ( 'NONE',  ( 59.11062488304980178, 14.31961591063559958, -26.60245654262559967 ) ) ;
#24734=VERTEX_POINT ( 'NONE', #7283 ) ;
#24736=CARTESIAN_POINT ( 'NONE',  ( 60.05889968639040433, 14.78467075934760011, -47.76686567462839861 ) ) ;
#24737=B_SPLINE_CURVE_WITH_KNOTS ( 'NONE', 3,
 ( #7328, #27223, #18849, #46660, #27483, #11261 ),
 .UNSPECIFIED., .F., .F.,
 ( 4, 2, 4 ),
 ( 0.4942347057900358109, 0.7471173528950179055, 1.000000000000000000 ),
 .UNSPECIFIED. ) ;
#24740=CARTESIAN_POINT ( 'NONE',  ( 11.14366242735480128, 32.52627267133070177, -44.02655122816489808 ) ) ;
#24742=B_SPLINE_CURVE_WITH_KNOTS ( 'NONE', 3,
 ( #50230, #50486, #10394, #9871, #2267, #6465, #2529, #22422 ),
 .UNSPECIFIED., .F., .F.,
 ( 4, 2, 2, 4 ),
 ( 0.000000000000000000, 0.01259071533122118475, 0.6292267250244858445, 1.000000000000000000 ),
 .UNSPECIFIED. ) ;
#24744=CARTESIAN_POINT ( 'NONE',  ( 10.86720904402820054, -64.97138516849830125, -17.53558607436760042 ) ) ;
#24746=CARTESIAN_POINT ( 'NONE',  ( 47.18323847407950211, 23.57489298307800141, -74.14999581260398998 ) ) ;
#24747=CARTESIAN_POINT ( 'NONE',  ( 49.24139269240150441, -53.85336577086550136, -55.19402337003639758 ) ) ;
#24749=CARTESIAN_POINT ( 'NONE',  ( 16.13393739769620083, -15.61618894467929941, -13.15000000000000036 ) ) ;
#24750=CARTESIAN_POINT ( 'NONE',  ( 63.02123093760216221, 0.4193442080440759612, -17.11446765124405900 ) ) ;
#24752=CARTESIAN_POINT ( 'NONE',  ( 56.87728296015039575, 13.88381105532070059, -15.74456185640559980 ) ) ;
#24756=VERTEX_POINT ( 'NONE', #4624 ) ;
#24757=DIRECTION ( 'NONE',  ( 1.000000000000000000, 0.000000000000000000, 0.000000000000000000 ) ) ;
#24758=CARTESIAN_POINT ( 'NONE',  ( 61.34213663493839874, -45.56221510017259391, -47.63657398781079877 ) ) ;
#24760=CARTESIAN_POINT ( 'NONE',  ( 50.04022705241149538, 17.68250914423200015, -76.14999999999999147 ) ) ;
#24762=FACE_BOUND ( 'NONE', #45816, .T. ) ;
#24763=CARTESIAN_POINT ( 'NONE',  ( 51.76047954393799699, -51.31561834827489577, -76.04144536748918881 ) ) ;
#24766=CARTESIAN_POINT ( 'NONE',  ( 84.32109122769391263, -43.95295802218129921, -47.41657241682840151 ) ) ;
#24770=VERTEX_POINT ( 'NONE', #959 ) ;
#24771=CARTESIAN_POINT ( 'NONE',  ( 61.56767787646829504, -45.23020975912200470, -47.05004766648129788 ) ) ;
#24772=CARTESIAN_POINT ( 'NONE',  ( 60.83133136721959744, 14.23629320661039976, -47.01992809069390233 ) ) ;
#24773=CARTESIAN_POINT ( 'NONE',  ( 76.39788387924198787, -12.46578609194745013, -12.78738496680618120 ) ) ;
#24774=CARTESIAN_POINT ( 'NONE',  ( 55.74551679396239479, -51.08285690157870107, -53.82168174107410152 ) ) ;
#24775=ORIENTED_EDGE ( 'NONE', *, *, #15208, .T. ) ;
#24776=ORIENTED_EDGE ( 'NONE', *, *, #46584, .F. ) ;
#24777=CARTESIAN_POINT ( 'NONE',  ( 48.19306574706310897, 22.95973674188289948, -54.68274065309989851 ) ) ;
#24778=AXIS2_PLACEMENT_3D ( 'NONE', #21346, #34172, #17948 ) ;
#24786=CARTESIAN_POINT ( 'NONE',  ( -64.19449136036989501, -52.49048880573185016, -62.88965083512580634 ) ) ;
#24787=CARTESIAN_POINT ( 'NONE',  ( 53.89956272158779882, -50.63255278052579911, -76.79736712525030384 ) ) ;
#24789=CARTESIAN_POINT ( 'NONE',  ( 60.27298471930929225, 14.52882665919789851, -47.23662664135199662 ) ) ;
#24790=AXIS2_PLACEMENT_3D ( 'NONE', #22638, #13317, #6420 ) ;
#24794=CARTESIAN_POINT ( 'NONE',  ( 43.31938993087129575, -43.19129029557480237, -4.740111887245549660 ) ) ;
#24800=CARTESIAN_POINT ( 'NONE',  ( 65.14567254404629182, 0.9617428959510800901, -17.75426655703740053 ) ) ;
#24801=ORIENTED_EDGE ( 'NONE', *, *, #48629, .F. ) ;
#24802=CARTESIAN_POINT ( 'NONE',  ( 14.25022214270639864, -51.72416169445279621, -75.53980707817230211 ) ) ;
#24804=CARTESIAN_POINT ( 'NONE',  ( 47.39659154339189939, -54.65216982619919861, -54.68228600026159825 ) ) ;
#24806=CARTESIAN_POINT ( 'NONE',  ( 83.63329895952738013, 13.29802447021414658, -46.55718444776781695 ) ) ;
#24813=CARTESIAN_POINT ( 'NONE',  ( 11.53916947328389853, 34.14449583656730169, -17.79819407340969661 ) ) ;
#24815=CARTESIAN_POINT ( 'NONE',  ( 13.61938558719180037, -51.42721352359901488, -22.88820061572821274 ) ) ;
#24816=CARTESIAN_POINT ( 'NONE',  ( 19.17404118348583353, -55.50002796966285246, -75.86242720129490635 ) ) ;
#24817=CARTESIAN_POINT ( 'NONE',  ( 42.35079399692714475, 13.08996448747064001, -5.113119481343584738 ) ) ;
#24818=CARTESIAN_POINT ( 'NONE',  ( 48.70700827379929621, 22.78256351753950071, -54.80992293905860180 ) ) ;
#24819=VERTEX_POINT ( 'NONE', #16680 ) ;
#24822=CARTESIAN_POINT ( 'NONE',  ( 47.81335647225210295, 23.16511464041720103, -54.71582838624409817 ) ) ;
#24824=CARTESIAN_POINT ( 'NONE',  ( 17.70545290926953541, -14.47441609210117086, -7.393828452885189861 ) ) ;
#24826=CARTESIAN_POINT ( 'NONE',  ( 83.46510812583990457, 13.46894839930740062, -46.64393865386079341 ) ) ;
#24827=CARTESIAN_POINT ( 'NONE',  ( 55.29029958675930345, 15.78228302045550002, -26.18850085621529900 ) ) ;
#24829=CARTESIAN_POINT ( 'NONE',  ( 11.97330428935281432, 33.54929834488839901, -16.08313759590791037 ) ) ;
#24830=CARTESIAN_POINT ( 'NONE',  ( 56.75109370957429888, -45.11618894467940066, -15.55230934101470197 ) ) ;
#24832=VERTEX_POINT ( 'NONE', #44986 ) ;
#24834=VERTEX_POINT ( 'NONE', #48933 ) ;
#24835=CARTESIAN_POINT ( 'NONE',  ( 11.95767227753720086, -64.99278100762269617, -16.37738641795650096 ) ) ;
#24836=CARTESIAN_POINT ( 'NONE',  ( 12.90536311836260097, 34.27762790739640764, -47.59859303656190122 ) ) ;
#24837=CARTESIAN_POINT ( 'NONE',  ( 61.50409964634459925, -45.37406455498979341, -47.35437808299670337 ) ) ;
#24841=CARTESIAN_POINT ( 'NONE',  ( 52.95538414884752143, 18.32046719859912542, -27.75247099191258826 ) ) ;
#24843=CARTESIAN_POINT ( 'NONE',  ( 13.00893796619580023, 34.28605843179359880, -23.32157451048000141 ) ) ;
#24847=CARTESIAN_POINT ( 'NONE',  ( 56.61928438282120624, 14.09173444410579989, -25.29356196242219923 ) ) ;
#24853=CARTESIAN_POINT ( 'NONE',  ( 52.23246550063239368, -46.22135848195970453, -14.08618016001920026 ) ) ;
#24854=EDGE_CURVE ( 'NONE', #12469, #2875, #41054, .T. ) ;
#24856=CARTESIAN_POINT ( 'NONE',  ( 13.65323237260809996, -51.39160756126780427, -23.15000001653109862 ) ) ;
#24857=CYLINDRICAL_SURFACE ( 'NONE', #16675, 22.00000000000000355 ) ;
#24858=CARTESIAN_POINT ( 'NONE',  ( 46.95087536525909400, -53.78713274785700094, -75.86145147363799879 ) ) ;
#24859=EDGE_LOOP ( 'NONE', ( #34250, #24922, #45440, #46483, #15411 ) ) ;
#24860=CARTESIAN_POINT ( 'NONE',  ( 54.86086241772310501, 14.92554945543239953, -16.02041001650959728 ) ) ;
#24863=CARTESIAN_POINT ( 'NONE',  ( 12.85792267939620181, 34.27659983687792078, -23.38353926081359191 ) ) ;
#24864=CARTESIAN_POINT ( 'NONE',  ( 47.49951315049990086, 23.36196595494009998, -74.36100594765079563 ) ) ;
#24865=CARTESIAN_POINT ( 'NONE',  ( 19.88800963098302788, -54.71077588610068432, -18.05472786948379493 ) ) ;
#24870=ADVANCED_FACE ( 'NONE', ( #21969 ), #9235, .T. ) ;
#24875=DIRECTION ( 'NONE',  ( 0.000000000000000000, 0.000000000000000000, -1.000000000000000000 ) ) ;
#24876=CARTESIAN_POINT ( 'NONE',  ( -33.14628496358510290, -25.37751098170330266, -57.60188784292080300 ) ) ;
#24878=CARTESIAN_POINT ( 'NONE',  ( 53.13654541734729264, -49.50093312247239652, -48.84750851792770021 ) ) ;
#24879=CARTESIAN_POINT ( 'NONE',  ( 13.39998208309999939, 20.55440457967890211, -74.14999999999999147 ) ) ;
#24881=CARTESIAN_POINT ( 'NONE',  ( 56.08973322185949684, 14.74539909579659991, -25.91532893058719722 ) ) ;
#24883=CARTESIAN_POINT ( 'NONE',  ( 50.83387907959539831, 18.50773185315869895, -76.22448499212009665 ) ) ;
#24884=CARTESIAN_POINT ( 'NONE',  ( 53.05608040805520176, 18.32399154030060018, -48.95471305401200368 ) ) ;
#24886=DIRECTION ( 'NONE',  ( 0.1686178020941689892, -0.6660492713794449182, -0.7265992051412129005 ) ) ;
#24887=CARTESIAN_POINT ( 'NONE',  ( 73.35428046702240579, -45.11618894467940066, -14.85668780614170004 ) ) ;
#24891=CARTESIAN_POINT ( 'NONE',  ( 47.48995689174640233, -54.59520503108659994, -54.73871931135540336 ) ) ;
#24892=CARTESIAN_POINT ( 'NONE',  ( 16.13393739769620083, -15.61618894467929941, -6.928362978644219794 ) ) ;
#24894=CARTESIAN_POINT ( 'NONE',  ( 57.11681979626609973, 18.51971639153730109, -52.00830098209539898 ) ) ;
#24902=ORIENTED_EDGE ( 'NONE', *, *, #30844, .T. ) ;
#24903=CARTESIAN_POINT ( 'NONE',  ( 9.286271486682959875, -63.20121777444870048, -46.53040463691939976 ) ) ;
#24904=LINE ( 'NONE', #32500, #40262 ) ;
#24910=CARTESIAN_POINT ( 'NONE',  ( 53.07814259748259644, 19.64173092165989942, -76.24016859401959323 ) ) ;
#24911=ORIENTED_EDGE ( 'NONE', *, *, #7030, .T. ) ;
#24912=FACE_OUTER_BOUND ( 'NONE', #8986, .T. ) ;
#24914=CARTESIAN_POINT ( 'NONE',  ( 60.47553822975979898, 14.59310890814650108, -47.74689862192149548 ) ) ;
#24917=EDGE_CURVE ( 'NONE', #17232, #566, #44533, .T. ) ;
#24918=CARTESIAN_POINT ( 'NONE',  ( 55.91595717589819259, 14.67227259378030091, -25.32543214355489880 ) ) ;
#24920=B_SPLINE_CURVE_WITH_KNOTS ( 'NONE', 3,
 ( #48482, #24863, #29331, #24600, #24342, #45332, #12325, #20680, #29073, #32205, #9171, #28285, #40357, #36669, #36410 ),
 .UNSPECIFIED., .F., .F.,
 ( 4, 2, 2, 1, 1, 1, 2, 2, 4 ),
 ( 0.000000000000000000, 0.2500000000000059952, 0.3750000000000062172, 0.4375000000000073275, 0.4687500000000076050, 0.4843750000000044964, 0.4921875000000029976, 0.5000000000000014433, 1.000000000000000000 ),
 .UNSPECIFIED. ) ;
#24922=ORIENTED_EDGE ( 'NONE', *, *, #169, .T. ) ;
#24923=FACE_OUTER_BOUND ( 'NONE', #34965, .T. ) ;
#24926=CARTESIAN_POINT ( 'NONE',  ( 14.31317264139750023, 20.84016670874339638, -75.79682998878489286 ) ) ;
#24933=CARTESIAN_POINT ( 'NONE',  ( 54.01638715310450323, -48.57868330340730267, -26.93638457783499973 ) ) ;
#24934=CARTESIAN_POINT ( 'NONE',  ( 16.05893884861770005, -51.08980756358450037, -20.93640534643669682 ) ) ;
#24939=CARTESIAN_POINT ( 'NONE',  ( -6.533439702237169300, -46.24119595036209773, -5.313628346711630535 ) ) ;
#24940=CARTESIAN_POINT ( 'NONE',  ( 47.20857549670580511, 23.55481961561859805, -54.63975978072630113 ) ) ;
#24943=DIRECTION ( 'NONE',  ( 0.3294064756441428266, 0.9441882088883046809, -2.329877999999999163E-14 ) ) ;
#24944=CARTESIAN_POINT ( 'NONE',  ( 11.78860067047029858, 34.19036438400789280, -17.85348613431190046 ) ) ;
#24948=CARTESIAN_POINT ( 'NONE',  ( 59.53533088614899782, -46.29190482577769927, -47.84669194743329967 ) ) ;
#24950=CARTESIAN_POINT ( 'NONE',  ( 17.40399715363529864, -52.78596775754549952, -76.12812327221449493 ) ) ;
#24956=CARTESIAN_POINT ( 'NONE',  ( 8.953364294532669021, 31.90297171738869864, -46.63441339637809335 ) ) ;
#24959=ORIENTED_EDGE ( 'NONE', *, *, #30748, .F. ) ;
#24960=CARTESIAN_POINT ( 'NONE',  ( 18.68424525891759913, 20.62786770048280260, -75.03330975078269205 ) ) ;
#24962=VERTEX_POINT ( 'NONE', #4388 ) ;
#24964=CARTESIAN_POINT ( 'NONE',  ( 10.31171152940200031, -63.41871857732729723, -45.84829271550790253 ) ) ;
#24965=CARTESIAN_POINT ( 'NONE',  ( 56.92366313695160329, -45.73164766762909750, -26.16831549262139944 ) ) ;
#24967=CARTESIAN_POINT ( 'NONE',  ( 61.49572070650139466, 14.06442238722440052, -47.20084786350769690 ) ) ;
#24972=AXIS2_PLACEMENT_3D ( 'NONE', #33555, #46415, #6564 ) ;
#24973=CARTESIAN_POINT ( 'NONE',  ( 12.30205592777625334, 33.50594859046132257, -15.96528925779647601 ) ) ;
#24975=CARTESIAN_POINT ( 'NONE',  ( 11.13393739525318438, -63.64729783289567422, -24.14585929178920054 ) ) ;
#24983=CARTESIAN_POINT ( 'NONE',  ( 47.17210187534929844, -54.78212032244810104, -74.50474471063260751 ) ) ;
#24985=CARTESIAN_POINT ( 'NONE',  ( 46.42739470264289992, 14.32699058590440089, -9.432284590658529311 ) ) ;
#24986=CARTESIAN_POINT ( 'NONE',  ( 16.13393739769620083, -15.61618894467929941, -3.187564294433600232 ) ) ;
#24987=CARTESIAN_POINT ( 'NONE',  ( -6.123496779401830459, 15.19157518532879969, -4.783664570069790400 ) ) ;
#24989=CARTESIAN_POINT ( 'NONE',  ( 54.86087699991983868, 14.92551754678483711, -16.02040008515932712 ) ) ;
#24991=EDGE_CURVE ( 'NONE', #30210, #14297, #1164, .T. ) ;
#24993=CARTESIAN_POINT ( 'NONE',  ( 11.67620015026735203, -64.89165383396532150, -23.88711004025349283 ) ) ;
#24994=CARTESIAN_POINT ( 'NONE',  ( -8.601845089184939397, -44.24493450895539581, -5.161620436049600080 ) ) ;
#24995=CARTESIAN_POINT ( 'NONE',  ( 11.79211174369839910, 33.77432752974699781, -45.32950553526499959 ) ) ;
#24998=AXIS2_PLACEMENT_3D ( 'NONE', #50873, #14962, #30928 ) ;
#24999=CARTESIAN_POINT ( 'NONE',  ( 11.88460916115749910, -64.82510961609500555, -16.16716782998640056 ) ) ;
#25001=CARTESIAN_POINT ( 'NONE',  ( 11.73319001782157933, 34.19002770849662198, -18.17421237843034731 ) ) ;
#25003=CARTESIAN_POINT ( 'NONE',  ( 49.36631007174879926, -53.73686886467790202, -54.70819196421620489 ) ) ;
#25004=CARTESIAN_POINT ( 'NONE',  ( 42.53968774367980643, -44.23115725350800176, -5.088323970340629998 ) ) ;
#25005=CARTESIAN_POINT ( 'NONE',  ( 61.72540128749741228, -0.04346031282550247982, -16.65167021730934493 ) ) ;
#25008=EDGE_LOOP ( 'NONE', ( #39271, #16888, #50138, #41930, #14371 ) ) ;
#25010=( BOUNDED_CURVE ( )  B_SPLINE_CURVE ( 3, ( #15054, #34696, #18465, #14282 ),
 .UNSPECIFIED., .F., .T. ) 
 B_SPLINE_CURVE_WITH_KNOTS ( ( 4, 4 ),
 ( 3.293969860817171025, 3.377821128487717317 ),
 .UNSPECIFIED. ) 
 CURVE ( )  GEOMETRIC_REPRESENTATION_ITEM ( )  RATIONAL_B_SPLINE_CURVE ( ( 1.000000000000000000, 0.9994141662295833450, 0.9994141662295833450, 1.000000000000000000 ) ) 
 REPRESENTATION_ITEM ( '' )  );
#25013=CARTESIAN_POINT ( 'NONE',  ( 16.13393739769620083, -15.61618894467929941, 8.349999999999999645 ) ) ;
#25014=CARTESIAN_POINT ( 'NONE',  ( 60.71052973799270092, -45.66926968361909900, -47.62087077360929754 ) ) ;
#25015=CARTESIAN_POINT ( 'NONE',  ( 56.84932596551109185, -50.65659107673559447, -53.85230338955700091 ) ) ;
#25016=CARTESIAN_POINT ( 'NONE',  ( 61.62036109055981115, 14.01986140997038888, -47.09707863094710945 ) ) ;
#25018=FACE_OUTER_BOUND ( 'NONE', #40729, .T. ) ;
#25022=CARTESIAN_POINT ( 'NONE',  ( 84.05638291250160421, -44.46509440729400353, -47.35165316785450074 ) ) ;
#25025=EDGE_LOOP ( 'NONE', ( #29060, #18118, #40275, #37609, #7879 ) ) ;
#25026=FACE_OUTER_BOUND ( 'NONE', #883, .T. ) ;
#25027=CARTESIAN_POINT ( 'NONE',  ( 52.63768092904719964, -49.80353151416749569, -48.69670982295910022 ) ) ;
#25028=CARTESIAN_POINT ( 'NONE',  ( 55.94681035962474880, 14.65618203914781859, -25.53316267917964311 ) ) ;
#25029=CARTESIAN_POINT ( 'NONE',  ( 76.39306992833101617, -14.04342351347505513, -12.76664126219467121 ) ) ;
#25034=CARTESIAN_POINT ( 'NONE',  ( 56.84210776121830122, 19.42547441397019981, -53.85131221055259942 ) ) ;
#25036=FACE_OUTER_BOUND ( 'NONE', #47569, .T. ) ;
#25037=EDGE_CURVE ( 'NONE', #14960, #44411, #10376, .T. ) ;
#25038=CARTESIAN_POINT ( 'NONE',  ( 8.797781558458089179, -63.18317285479920997, -46.67022811708060459 ) ) ;
#25041=ORIENTED_EDGE ( 'NONE', *, *, #13510, .F. ) ;
#25042=DIRECTION ( 'NONE',  ( 0.3294064756441309472, 0.9441882088883087887, -3.053113317719179500E-16 ) ) ;
#25043=CARTESIAN_POINT ( 'NONE',  ( 83.89200044194980421, -48.61618894467930119, -53.92796738110899923 ) ) ;
#25046=CARTESIAN_POINT ( 'NONE',  ( 60.82575030619229750, 14.23921728079439930, -47.02326931679620259 ) ) ;
#25050=AXIS2_PLACEMENT_3D ( 'NONE', #44132, #15587, #35497 ) ;
#25051=CARTESIAN_POINT ( 'NONE',  ( 42.25512407184699981, -43.69544688865530446, -4.476913605124590134 ) ) ;
#25057=CARTESIAN_POINT ( 'NONE',  ( 67.08848200792850491, -0.1544538032429550178, -17.50642677597119956 ) ) ;
#25058=ORIENTED_EDGE ( 'NONE', *, *, #22600, .F. ) ;
#25059=CARTESIAN_POINT ( 'NONE',  ( 13.76720245349099869, -52.01740915708810320, -75.38689171750549178 ) ) ;
#25060=CARTESIAN_POINT ( 'NONE',  ( 57.37029956467470271, 18.93460159902399909, -52.65659740218330143 ) ) ;
#25062=CARTESIAN_POINT ( 'NONE',  ( 83.30738730474247689, 10.97725729733029532, -44.69194689374966600 ) ) ;
#25067=CARTESIAN_POINT ( 'NONE',  ( 47.71760965017880096, -54.49863051568969752, -55.05225816380090009 ) ) ;
#25070=AXIS2_PLACEMENT_3D ( 'NONE', #29775, #45792, #26104 ) ;
#25072=CARTESIAN_POINT ( 'NONE',  ( 2.918607032519620947, -25.21768847662068325, 5.856814007409659517 ) ) ;
#25073=CARTESIAN_POINT ( 'NONE',  ( 48.80215967364860319, 22.76357081333170029, -54.88693110859010460 ) ) ;
#25074=VECTOR ( 'NONE', #44728, 1000.000000000000000 ) ;
#25075=ORIENTED_EDGE ( 'NONE', *, *, #23512, .F. ) ;
#25078=VERTEX_POINT ( 'NONE', #43458 ) ;
#25079=TOROIDAL_SURFACE ( 'NONE', #15088, 34.99999974117479695, 4.999999999402000128 ) ;
#25083=CARTESIAN_POINT ( 'NONE',  ( 83.99291904213089310, 13.14199879970889917, -47.15152633430140838 ) ) ;
#25084=CARTESIAN_POINT ( 'NONE',  ( 56.05190775535580627, 14.68378006638939937, -25.80821134207000256 ) ) ;
#25085=AXIS2_PLACEMENT_3D ( 'NONE', #4623, #48397, #11990 ) ;
#25088=CARTESIAN_POINT ( 'NONE',  ( 82.34864690492774741, -45.64188066427791313, -47.72348187592566404 ) ) ;
#25092=ORIENTED_EDGE ( 'NONE', *, *, #48676, .F. ) ;
#25094=CARTESIAN_POINT ( 'NONE',  ( 12.12757547495970023, -65.18777574590600921, -16.69244762554430039 ) ) ;
#25095=CARTESIAN_POINT ( 'NONE',  ( 11.44396443873849911, 33.41480605604599674, -45.21635737664340127 ) ) ;
#25096=DIRECTION ( 'NONE',  ( -0.5685928097855377228, 0.5944782866685497380, 0.5685928097855377228 ) ) ;
#25097=CARTESIAN_POINT ( 'NONE',  ( 49.34600860551959300, -53.00476810193420363, -52.46789648595490263 ) ) ;
#25099=ORIENTED_EDGE ( 'NONE', *, *, #4655, .F. ) ;
#25100=CARTESIAN_POINT ( 'NONE',  ( 57.10963496851019272, 14.63735811038339918, -26.25116453996779953 ) ) ;
#25104=CARTESIAN_POINT ( 'NONE',  ( 50.12211799414340163, -48.76092583931080071, -76.14999999999999147 ) ) ;
#25107=FACE_OUTER_BOUND ( 'NONE', #4098, .T. ) ;
#25108=ORIENTED_EDGE ( 'NONE', *, *, #30689, .T. ) ;
#25111=DIRECTION ( 'NONE',  ( 0.000000000000000000, -1.000000000000000000, 0.000000000000000000 ) ) ;
#25112=EDGE_LOOP ( 'NONE', ( #9713, #35903, #12630, #13351, #46134, #15285, #1032, #14415, #20072 ) ) ;
#25115=EDGE_CURVE ( 'NONE', #37505, #51131, #7816, .T. ) ;
#25117=CARTESIAN_POINT ( 'NONE',  ( 68.13393739769630031, 16.88381105531836823, -74.20000000000023022 ) ) ;
#25118=FACE_OUTER_BOUND ( 'NONE', #14568, .T. ) ;
#25119=CARTESIAN_POINT ( 'NONE',  ( 47.45602544390119704, -54.53030583225749695, -74.72363872023309739 ) ) ;
#25122=CARTESIAN_POINT ( 'NONE',  ( 55.40887998857099461, 14.39935875450660063, -16.01783516407289909 ) ) ;
#25124=CARTESIAN_POINT ( 'NONE',  ( 57.24507234829509628, -50.61619228912019963, -53.91419826682510319 ) ) ;
#25126=CARTESIAN_POINT ( 'NONE',  ( 52.60158096327749888, -49.82903481347529606, -48.60922413768609829 ) ) ;
#25131=VECTOR ( 'NONE', #49132, 1000.000000000000000 ) ;
#25132=CARTESIAN_POINT ( 'NONE',  ( 47.34254393078440160, 23.13085423282609909, -75.17206278554509424 ) ) ;
#25134=EDGE_CURVE ( 'NONE', #28015, #1802, #7048, .T. ) ;
#25135=CARTESIAN_POINT ( 'NONE',  ( 61.14444386409353882, -45.63613486214893555, -47.70810082891851067 ) ) ;
#25136=CARTESIAN_POINT ( 'NONE',  ( 12.30638105235319912, 33.40191250400779666, -15.85198194120730086 ) ) ;
#25141=CARTESIAN_POINT ( 'NONE',  ( 61.26948014433400402, 14.00673465877100021, -46.56955475535669819 ) ) ;
#25142=CARTESIAN_POINT ( 'NONE',  ( -18.43754721997909840, -52.44194012997609633, -54.46408928706210162 ) ) ;
#25144=CARTESIAN_POINT ( 'NONE',  ( 53.06129598958289506, -49.54289835688069843, -48.87622692776139388 ) ) ;
#25146=CARTESIAN_POINT ( 'NONE',  ( 61.56839264358480079, -45.12835126257370177, -27.89781785035500050 ) ) ;
#25148=CARTESIAN_POINT ( 'NONE',  ( 56.79768778468150003, 14.70793938441589965, -26.22464504602800162 ) ) ;
#25150=CARTESIAN_POINT ( 'NONE',  ( 50.65222607392030341, 18.77326448281979765, -76.16386725149659753 ) ) ;
#25151=CARTESIAN_POINT ( 'NONE',  ( 52.70437010560439717, 18.50693821689120000, -48.55295696688259710 ) ) ;
#25154=CARTESIAN_POINT ( 'NONE',  ( 73.90096124267101629, -43.37807912905199714, -12.95075084354250095 ) ) ;
#25159=CARTESIAN_POINT ( 'NONE',  ( 47.43216622799359783, -54.63853425152050391, -54.88096955750960149 ) ) ;
#25169=ORIENTED_EDGE ( 'NONE', *, *, #7509, .F. ) ;
#25173=CARTESIAN_POINT ( 'NONE',  ( 9.273487956746848226, -63.11543068638779630, -46.53410025525219851 ) ) ;
#25174=LINE ( 'NONE', #13167, #30229 ) ;
#25177=CARTESIAN_POINT ( 'NONE',  ( 84.02702888049316243, 13.40383544920428172, -47.45289756459199992 ) ) ;
#25178=PLANE ( 'NONE',  #48752 ) ;
#25179=EDGE_CURVE ( 'NONE', #483, #32383, #22914, .T. ) ;
#25180=CARTESIAN_POINT ( 'NONE',  ( 53.39545258799459759, 19.65859595880879951, -76.18303073696110062 ) ) ;
#25185=ADVANCED_FACE ( 'NONE', ( #2767 ), #3547, .T. ) ;
#25190=CARTESIAN_POINT ( 'NONE',  ( 56.55522355860080097, -46.21195502513410247, -26.26695352263039851 ) ) ;
#25194=CARTESIAN_POINT ( 'NONE',  ( 14.54665750016330072, 20.57774151326000123, -75.67041253543301593 ) ) ;
#25196=CARTESIAN_POINT ( 'NONE',  ( 51.99247536373789558, 18.26518850788540149, -77.11022606388370093 ) ) ;
#25198=VECTOR ( 'NONE', #51369, 1000.000000000000000 ) ;
#25200=VERTEX_POINT ( 'NONE', #18998 ) ;
#25201=CARTESIAN_POINT ( 'NONE',  ( 55.83353943854869783, -46.18894462837869952, -25.84382037829299961 ) ) ;
#25202=CARTESIAN_POINT ( 'NONE',  ( 14.48916582606740100, -51.10390356942439638, -22.14433180932410039 ) ) ;
#25204=DIRECTION ( 'NONE',  ( 0.000000000000000000, 0.000000000000000000, 1.000000000000000000 ) ) ;
#25205=DIRECTION ( 'NONE',  ( 0.000000000000000000, 0.000000000000000000, -1.000000000000000000 ) ) ;
#25207=CARTESIAN_POINT ( 'NONE',  ( -5.145629218704510066, -47.11336362869789696, -4.652761024381289801 ) ) ;
#25208=CARTESIAN_POINT ( 'NONE',  ( 47.20789225325369642, 23.55536091824439637, -54.64146362385890399 ) ) ;
#25209=ADVANCED_FACE ( 'NONE', ( #6444 ), #18738, .T. ) ;
#25210=CARTESIAN_POINT ( 'NONE',  ( 55.91595722987329964, -45.90465052577939531, -25.32543029193989881 ) ) ;
#25213=CARTESIAN_POINT ( 'NONE',  ( 11.50291098922579991, 34.11720288171970594, -17.75618560011610114 ) ) ;
#25214=CARTESIAN_POINT ( 'NONE',  ( 16.13393739769620083, -15.61618894467929941, -7.139181489322110608 ) ) ;
#25217=CARTESIAN_POINT ( 'NONE',  ( 58.76768575440100051, -46.69271212826609485, -47.97336379875430623 ) ) ;
#25220=CARTESIAN_POINT ( 'NONE',  ( 52.78762917051419379, 21.08910179861619838, -54.06354383229390237 ) ) ;
#25225=CARTESIAN_POINT ( 'NONE',  ( 9.739018438830168378, 32.00108083321330099, -46.29762906764769781 ) ) ;
#25226=CARTESIAN_POINT ( 'NONE',  ( 66.10673863877181589, -29.76883965895079953, -16.72118890776879852 ) ) ;
#25228=VERTEX_POINT ( 'NONE', #51497 ) ;
#25229=CARTESIAN_POINT ( 'NONE',  ( 18.21797964295990013, 20.46947493835569887, -75.41867332334460627 ) ) ;
#25230=EDGE_LOOP ( 'NONE', ( #20591, #8374, #43260, #36623 ) ) ;
#25232=LINE ( 'NONE', #21825, #10305 ) ;
#25234=CARTESIAN_POINT ( 'NONE',  ( 12.33080418725089977, -65.41125055805170518, -47.27598567016929820 ) ) ;
#25235=CARTESIAN_POINT ( 'NONE',  ( 56.48760883520149889, -46.18664620669910192, -26.24751697164999698 ) ) ;
#25237=LINE ( 'NONE', #9801, #44042 ) ;
#25240=CARTESIAN_POINT ( 'NONE',  ( 61.51623078522280252, 13.93866689514799972, -46.75536389823849959 ) ) ;
#25248=CARTESIAN_POINT ( 'NONE',  ( 49.47280132910630357, -45.11618894461000195, -10.20974854288130018 ) ) ;
#25252=LINE ( 'NONE', #45193, #14113 ) ;
#25253=CARTESIAN_POINT ( 'NONE',  ( 47.19185019601420095, -54.76658792525179820, -74.50414561666529778 ) ) ;
#25255=CARTESIAN_POINT ( 'NONE',  ( 54.47259994055220034, 15.01996530865999979, -15.76423849626599960 ) ) ;
#25256=DIRECTION ( 'NONE',  ( 0.6911981449639427177, -0.7226652920947596037, 0.000000000000000000 ) ) ;
#25257=DIRECTION ( 'NONE',  ( 1.000000000000000000, 0.000000000000000000, 0.000000000000000000 ) ) ;
#25259=CARTESIAN_POINT ( 'NONE',  ( 57.71856222965350014, 13.89769183763849902, -25.57520695384850029 ) ) ;
#25262=CARTESIAN_POINT ( 'NONE',  ( 59.95384340470150164, 14.69603373565070115, -47.36701927546829438 ) ) ;
#25266=AXIS2_PLACEMENT_3D ( 'NONE', #49384, #22603, #22344 ) ;
#25268=AXIS2_PLACEMENT_3D ( 'NONE', #89, #32790, #3764 ) ;
#25272=CARTESIAN_POINT ( 'NONE',  ( 49.13043947778380272, -53.90062760971940037, -55.21565379135309826 ) ) ;
#25273=CARTESIAN_POINT ( 'NONE',  ( 51.19324896229723976, -31.68074559396569256, -17.14371393497826901 ) ) ;
#25281=ORIENTED_EDGE ( 'NONE', *, *, #6662, .F. ) ;
#25282=CARTESIAN_POINT ( 'NONE',  ( 10.97210468079044610, 32.23756417331421176, -23.98816728309424917 ) ) ;
#25283=CARTESIAN_POINT ( 'NONE',  ( 60.88289654404759688, -45.68840397722050284, -47.72275522894760513 ) ) ;
#25285=CARTESIAN_POINT ( 'NONE',  ( 12.89656437789989951, 18.76901986582059934, -21.06838189635490011 ) ) ;
#25287=DIRECTION ( 'NONE',  ( -1.000000000000000000, -1.040834085586084257E-16, 0.000000000000000000 ) ) ;
#25289=DIRECTION ( 'NONE',  ( 0.000000000000000000, 1.000000000000000000, 0.000000000000000000 ) ) ;
#25291=ORIENTED_EDGE ( 'NONE', *, *, #46926, .F. ) ;
#25293=ORIENTED_EDGE ( 'NONE', *, *, #36750, .F. ) ;
#25294=CARTESIAN_POINT ( 'NONE',  ( 61.50647473645999952, -45.22354326066130170, -47.00768424768439502 ) ) ;
#25295=DIRECTION ( 'NONE',  ( 0.000000000000000000, 0.000000000000000000, 1.000000000000000000 ) ) ;
#25296=CARTESIAN_POINT ( 'NONE',  ( 54.39599759010950208, -51.37714874329250136, -53.12073448206439963 ) ) ;
#25297=ORIENTED_EDGE ( 'NONE', *, *, #33775, .T. ) ;
#25301=ORIENTED_EDGE ( 'NONE', *, *, #42829, .F. ) ;
#25305=CARTESIAN_POINT ( 'NONE',  ( 56.46551779669420057, -50.77616595281960343, -53.85225392423020452 ) ) ;
#25306=CARTESIAN_POINT ( 'NONE',  ( 62.88393739769619373, 4.883811055320659733, -84.94863984844531046 ) ) ;
#25311=CARTESIAN_POINT ( 'NONE',  ( 53.51849515060609974, -51.02420518644899516, -75.95517920710381077 ) ) ;
#25313=CARTESIAN_POINT ( 'NONE',  ( 60.39786843514819736, 14.46339658146679952, -47.23199723846380493 ) ) ;
#25316=CARTESIAN_POINT ( 'NONE',  ( 41.74196416991780012, 13.83302381481709986, -5.934307256532159514 ) ) ;
#25317=CARTESIAN_POINT ( 'NONE',  ( 42.47447998003330127, -44.18050766653550454, -5.039225367523919807 ) ) ;
#25318=CARTESIAN_POINT ( 'NONE',  ( 69.22748654599971019, -50.70395984887900909, -74.34354914830332461 ) ) ;
#25319=CARTESIAN_POINT ( 'NONE',  ( 67.45368034285870351, 1.609458251574180432, -19.55784009146304214 ) ) ;
#25322=CARTESIAN_POINT ( 'NONE',  ( 65.36113773965780638, 1.378962859947149955, -18.37587875859610165 ) ) ;
#25324=CARTESIAN_POINT ( 'NONE',  ( 14.36865994475110142, -51.35369855970039765, -75.11575902016450357 ) ) ;
#25326=CARTESIAN_POINT ( 'NONE',  ( 47.21621394679169725, -54.78114590934789874, -54.62203065971809934 ) ) ;
#25329=( BOUNDED_SURFACE ( )  B_SPLINE_SURFACE ( 2, 2, ( 
 ( #7347, #11025, #19894, #23295, #3934, #31420, #31676, #31166, #7608 ),
 ( #35888, #47194, #11542, #15469, #31934, #3, #7861, #246, #19130 ),
 ( #30910, #43506, #23809, #35640, #43759, #26994, #39827, #7097, #35109 ),
 ( #51109, #11281, #27764, #46940, #23048, #3160, #43000, #15212, #51625 ),
 ( #15980, #8117, #47955, #19391, #11801, #12058, #28009, #44016, #27504 ) ),
 .UNSPECIFIED., .F., .T., .T. ) 
 B_SPLINE_SURFACE_WITH_KNOTS ( ( 3, 2, 3 ),
 ( 3, 2, 2, 2, 3 ),
 ( -0.003205554297748039981, 0.8238407534185530068, 1.650887061134849843 ),
 ( -3.141592653589790007, -1.570796326794899889, 0.000000000000000000, 1.570796326794899889, 3.141592653589790007 ),
 .UNSPECIFIED. ) 
 GEOMETRIC_REPRESENTATION_ITEM ( )  RATIONAL_B_SPLINE_SURFACE ( (
 ( 1.000000000000000000, 0.7071067811865480168, 1.000000000000000000, 0.7071067811865480168, 1.000000000000000000, 0.7071067811865480168, 1.000000000000000000, 0.7071067811865480168, 1.000000000000000000),
 ( 0.9157107718030679244, 0.6475052963475169676, 0.9157107718030679244, 0.6475052963475169676, 0.9157107718030679244, 0.6475052963475169676, 0.9157107718030679244, 0.6475052963475169676, 0.9157107718030679244),
 ( 1.000000000000000000, 0.7071067811865480168, 1.000000000000000000, 0.7071067811865480168, 1.000000000000000000, 0.7071067811865480168, 1.000000000000000000, 0.7071067811865480168, 1.000000000000000000),
 ( 0.9157107718030469412, 0.6475052963475019796, 0.9157107718030469412, 0.6475052963475019796, 0.9157107718030469412, 0.6475052963475019796, 0.9157107718030469412, 0.6475052963475019796, 0.9157107718030469412),
 ( 1.000000000000000000, 0.7071067811865480168, 1.000000000000000000, 0.7071067811865480168, 1.000000000000000000, 0.7071067811865480168, 1.000000000000000000, 0.7071067811865480168, 1.000000000000000000) ) ) 
 REPRESENTATION_ITEM ( '' )  SURFACE ( )  );
#25334=CARTESIAN_POINT ( 'NONE',  ( 16.65420337845429799, 19.88381105532299742, -20.15000000000000213 ) ) ;
#25336=CARTESIAN_POINT ( 'NONE',  ( 56.38082786511019862, 19.49268417552400123, -53.29063683202039670 ) ) ;
#25338=CARTESIAN_POINT ( 'NONE',  ( 48.55128749046469494, 22.77231967830010007, -54.59786143027240257 ) ) ;
#25342=CIRCLE ( 'NONE', #9490, 2.000000000000000000 ) ;
#25343=VERTEX_POINT ( 'NONE', #12176 ) ;
#25344=PLANE ( 'NONE',  #39589 ) ;
#25345=CARTESIAN_POINT ( 'NONE',  ( 53.55347996444381664, -49.37856166211688702, -49.15350056090469621 ) ) ;
#25346=DIRECTION ( 'NONE',  ( 0.3445670372598628184, 0.6174735272333260472, -0.7071067811865442421 ) ) ;
#25347=CARTESIAN_POINT ( 'NONE',  ( 84.44303304399450383, 12.08919773384380036, -47.45512980871949793 ) ) ;
#25348=CARTESIAN_POINT ( 'NONE',  ( 54.40762147712389663, 16.55776885928690234, -25.97561773943489882 ) ) ;
#25354=ORIENTED_EDGE ( 'NONE', *, *, #30300, .T. ) ;
#25355=CARTESIAN_POINT ( 'NONE',  ( 11.79921494304270091, -65.04093993986319333, -16.52202905013960077 ) ) ;
#25356=CARTESIAN_POINT ( 'NONE',  ( 11.13393739775729863, 32.27424679965390197, -43.95119008811450101 ) ) ;
#25360=CARTESIAN_POINT ( 'NONE',  ( 10.13693646489610067, -64.73981908445260558, -47.01156321116880576 ) ) ;
#25362=ADVANCED_FACE ( 'NONE', ( #372 ), #8760, .T. ) ;
#25364=CARTESIAN_POINT ( 'NONE',  ( 53.71518589158228707, 17.65496981945476662, -27.13660862535111562 ) ) ;
#25365=AXIS2_PLACEMENT_3D ( 'NONE', #41346, #13326, #8872 ) ;
#25367=ADVANCED_FACE ( 'NONE', ( #16353 ), #24448, .T. ) ;
#25369=CARTESIAN_POINT ( 'NONE',  ( 50.67690155642070238, -50.61106055578139973, -76.14999999999999147 ) ) ;
#25370=LINE ( 'NONE', #29565, #17094 ) ;
#25372=CARTESIAN_POINT ( 'NONE',  ( 53.55220836886790181, -48.78100643530040514, -26.47327747818699706 ) ) ;
#25373=CARTESIAN_POINT ( 'NONE',  ( 68.13393739769814772, 19.38381105532029736, -71.50000000000200373 ) ) ;
#25376=CARTESIAN_POINT ( 'NONE',  ( 47.27830536510050052, -46.14749639572039541, -10.52818769379789821 ) ) ;
#25379=CARTESIAN_POINT ( 'NONE',  ( 53.91674685403769729, 19.61716007771000037, -76.09466592280320185 ) ) ;
#25380=CARTESIAN_POINT ( 'NONE',  ( 47.40869509741950338, -54.46061727596239876, -74.94674070344109396 ) ) ;
#25381=ORIENTED_EDGE ( 'NONE', *, *, #38703, .F. ) ;
#25382=CARTESIAN_POINT ( 'NONE',  ( 55.98930672876529968, 14.33000371823360020, -16.77916391804700069 ) ) ;
#25383=CARTESIAN_POINT ( 'NONE',  ( 57.35856959117180054, -50.13596281943610222, -52.61941485247680106 ) ) ;
#25388=CARTESIAN_POINT ( 'NONE',  ( 46.76255008597159701, 22.27812416600520251, -76.02679354016848379 ) ) ;
#25390=CARTESIAN_POINT ( 'NONE',  ( 75.16204195899146612, -29.53650206104261500, -11.85619338644309551 ) ) ;
#25394=CARTESIAN_POINT ( 'NONE',  ( 84.44784216359251161, -43.11618894467930119, -47.47585302082339354 ) ) ;
#25395=CARTESIAN_POINT ( 'NONE',  ( 68.13393739769620083, -15.61618894467929941, -65.65000000000000568 ) ) ;
#25397=ADVANCED_FACE ( 'NONE', ( #43635 ), #23934, .F. ) ;
#25398=DIRECTION ( 'NONE',  ( -0.6676418852213052979, 0.2329255526947255628, -0.7071067811865461294 ) ) ;
#25399=CARTESIAN_POINT ( 'NONE',  ( 6.300025116801259983, -65.10110191454670314, -48.92608059699489331 ) ) ;
#25402=CARTESIAN_POINT ( 'NONE',  ( 52.77257543143819873, -49.69364411959510619, -48.57105728902469366 ) ) ;
#25404=CARTESIAN_POINT ( 'NONE',  ( 61.75043129679379916, -45.11618897208669665, -28.15142663286150437 ) ) ;
#25405=CARTESIAN_POINT ( 'NONE',  ( 49.60483365582589954, -53.69855377821169640, -55.15230005116299594 ) ) ;
#25408=CARTESIAN_POINT ( 'NONE',  ( 50.47459370284359892, 19.05485954424960227, -76.14999999999999147 ) ) ;
#25409=CARTESIAN_POINT ( 'NONE',  ( 52.73033965374710164, 18.49117935840850180, -48.63393906880330775 ) ) ;
#25410=CARTESIAN_POINT ( 'NONE',  ( 60.45746832332759624, -45.66454841953329691, -47.21482551237440362 ) ) ;
#25411=CARTESIAN_POINT ( 'NONE',  ( 46.61750669586271556, 22.00845647503780000, -76.11314270326337805 ) ) ;
#25413=VECTOR ( 'NONE', #46217, 999.9999999999998863 ) ;
#25417=CARTESIAN_POINT ( 'NONE',  ( 47.50476691646419880, -54.58925063325320082, -54.77393688460149690 ) ) ;
#25419=CARTESIAN_POINT ( 'NONE',  ( 11.53606103740170674, 24.11867657901759188, -21.73577486392030167 ) ) ;
#25420=CARTESIAN_POINT ( 'NONE',  ( 56.45552857517409961, 19.30196012738109701, -52.91205108279270775 ) ) ;
#25428=CARTESIAN_POINT ( 'NONE',  ( 9.291657151117041380, -63.23923423081338768, -46.52991438213880571 ) ) ;
#25431=ADVANCED_FACE ( 'NONE', ( #8499 ), #34342, .T. ) ;
#25435=CARTESIAN_POINT ( 'NONE',  ( 51.83018428346819206, 19.54284939159689927, -76.24313691477149746 ) ) ;
#25446=CARTESIAN_POINT ( 'NONE',  ( 18.59699486872473884, 20.77208395163040322, -75.25166008050844368 ) ) ;
#25450=CARTESIAN_POINT ( 'NONE',  ( 13.92353701934610122, 20.57110240350969832, -75.40982873507010709 ) ) ;
#25456=CARTESIAN_POINT ( 'NONE',  ( 52.77799953798270138, -49.65042343486720000, -27.64301666048340067 ) ) ;
#25457=CARTESIAN_POINT ( 'NONE',  ( 16.60579442219119883, -51.11619062814370551, -20.30246704093690013 ) ) ;
#25458=CARTESIAN_POINT ( 'NONE',  ( 3.953188568412389969, 25.49695625375460040, -9.854466049057851507 ) ) ;
#25459=ADVANCED_FACE ( 'NONE', ( #20468 ), #7675, .T. ) ;
#25460=DIRECTION ( 'NONE',  ( 0.000000000000000000, 0.000000000000000000, 1.000000000000000000 ) ) ;
#25462=ORIENTED_EDGE ( 'NONE', *, *, #2799, .T. ) ;
#25463=CARTESIAN_POINT ( 'NONE',  ( -6.527821822757669423, -46.15177778084200355, -5.007725705170800623 ) ) ;
#25464=EDGE_CURVE ( 'NONE', #19643, #45513, #10756, .T. ) ;
#25465=CARTESIAN_POINT ( 'NONE',  ( 47.41560371684850139, 23.41602560681479872, -54.88584520135799494 ) ) ;
#25468=CARTESIAN_POINT ( 'NONE',  ( 60.85038404897530029, 14.22631097275989909, -47.01191575018489743 ) ) ;
#25469=CARTESIAN_POINT ( 'NONE',  ( 43.27084646332170337, 12.63989574393310100, -5.051381114894940794 ) ) ;
#25471=CARTESIAN_POINT ( 'NONE',  ( 16.13393739769620083, -15.61618894467929941, 4.450000000000000178 ) ) ;
#25472=CARTESIAN_POINT ( 'NONE',  ( 53.18486760013709613, 18.24248981343010101, -48.80133335483809986 ) ) ;
#25473=LINE ( 'NONE', #17641, #27503 ) ;
#25474=CARTESIAN_POINT ( 'NONE',  ( 56.62774750731059470, -47.76694016067460069, -48.32660976114450335 ) ) ;
#25477=CARTESIAN_POINT ( 'NONE',  ( 54.26151850782470376, 20.26306358825659970, -53.24447792474390440 ) ) ;
#25482=EDGE_LOOP ( 'NONE', ( #50788, #21478, #44360, #28255 ) ) ;
#25484=CARTESIAN_POINT ( 'NONE',  ( 9.293570193019839110, 32.02070994195079834, -46.52994104399439834 ) ) ;
#25485=CARTESIAN_POINT ( 'NONE',  ( 45.93002705875483827, 13.88381105130597604, -7.538620839776520199 ) ) ;
#25487=CARTESIAN_POINT ( 'NONE',  ( 68.03809913820030886, -32.00255854605169503, -18.68243752497800259 ) ) ;
#25488=CARTESIAN_POINT ( 'NONE',  ( 17.99108685348040026, 20.53764257940400029, -75.58342519351550948 ) ) ;
#25489=ORIENTED_EDGE ( 'NONE', *, *, #21980, .F. ) ;
#25491=PLANE ( 'NONE',  #39591 ) ;
#25493=ORIENTED_EDGE ( 'NONE', *, *, #44254, .T. ) ;
#25494=EDGE_CURVE ( 'NONE', #16045, #31153, #11843, .T. ) ;
#25495=CARTESIAN_POINT ( 'NONE',  ( 10.66704074881489994, -63.38769094126030268, -45.39606956719949693 ) ) ;
#25496=CARTESIAN_POINT ( 'NONE',  ( 57.00815868861789681, -45.37048793376839484, -25.89347327989339931 ) ) ;
#25498=CARTESIAN_POINT ( 'NONE',  ( 61.48519961305099457, 14.00861713270729858, -47.04493765378530412 ) ) ;
#25500=ORIENTED_EDGE ( 'NONE', *, *, #35622, .F. ) ;
#25503=CARTESIAN_POINT ( 'NONE',  ( 54.56301516078890046, -45.21020833436829633, -14.51131706652730102 ) ) ;
#25506=ORIENTED_EDGE ( 'NONE', *, *, #43822, .F. ) ;
#25508=CARTESIAN_POINT ( 'NONE',  ( 47.02944151445359466, -54.40995658191120299, -75.36157798374209449 ) ) ;
#25509=CARTESIAN_POINT ( 'NONE',  ( 61.30950358004140099, 14.36220717851900019, -47.67188667985269745 ) ) ;
#25511=CARTESIAN_POINT ( 'NONE',  ( 50.30650830823179120, 13.88381105525040127, -10.79667524648609955 ) ) ;
#25512=AXIS2_PLACEMENT_3D ( 'NONE', #49460, #9615, #5431 ) ;
#25515=CARTESIAN_POINT ( 'NONE',  ( 57.89943171185210247, 14.04932663211479849, -25.97857316395900185 ) ) ;
#25517=B_SPLINE_SURFACE_WITH_KNOTS ( 'NONE', 3, 3, ( 
 ( #37148, #49472, #25582, #17488, #5697, #25835, #26102, #1246, #21650, #21910, #41077, #33961 ),
 ( #33195, #37655, #49214, #9382, #49977, #14069, #17740, #34217, #30031, #41329, #6213, #18248 ),
 ( #21400, #25060, #50238, #45009, #5190, #17234, #22942, #23449, #27146, #35534, #47345, #30296 ),
 ( #18769, #31065, #3054, #14584, #34740, #30550, #14844, #19024, #46314, #15103, #11442, #51005 ),
 ( #47091, #39473, #46574, #39209, #50493, #10662, #30806, #11180, #43149, #35000, #7245, #3574 ),
 ( #6471, #34488, #42895, #26619, #2535, #23192, #2796, #38961, #6990, #10404, #42634, #26356 ) ),
 .UNSPECIFIED., .F., .F., .F.,
 ( 4, 2, 4 ),
 ( 4, 1, 1, 1, 1, 1, 1, 1, 1, 4 ),
 ( -0.3078040425649150036, -0.2786161072492089885, 1.435456000000000037E-29 ),
 ( 0.000000000000000000, 0.1111111111111110078, 0.2222222222222219878, 0.3333333333333329818, 0.4444444444444439757, 0.5555555555555560243, 0.6666666666666670737, 0.7777777777777779011, 0.8888888888888889506, 1.000000000000000000 ),
 .UNSPECIFIED. ) ;
#25518=ORIENTED_EDGE ( 'NONE', *, *, #19976, .F. ) ;
#25525=EDGE_CURVE ( 'NONE', #8290, #5276, #28593, .T. ) ;
#25531=CARTESIAN_POINT ( 'NONE',  ( 48.94088206813629682, -53.97935211052140403, -55.17481584361439673 ) ) ;
#25533=CARTESIAN_POINT ( 'NONE',  ( 76.85544920018013215, -43.13137431541007061, -14.75910591941364380 ) ) ;
#25535=VERTEX_POINT ( 'NONE', #24651 ) ;
#25538=ORIENTED_EDGE ( 'NONE', *, *, #48697, .T. ) ;
#25540=CARTESIAN_POINT ( 'NONE',  ( 60.52868080801660255, -45.70706635237720405, -47.56219373738379375 ) ) ;
#25542=CARTESIAN_POINT ( 'NONE',  ( 50.23538082579219832, 18.53774256725959901, -76.14999999999999147 ) ) ;
#25546=DIRECTION ( 'NONE',  ( 0.000000000000000000, 0.000000000000000000, 1.000000000000000000 ) ) ;
#25552=CARTESIAN_POINT ( 'NONE',  ( 61.34009987415589649, -45.20348205694470067, -46.37197372483269930 ) ) ;
#25555=CARTESIAN_POINT ( 'NONE',  ( 54.86738137264109838, -51.34065982945939766, -53.37025816224030450 ) ) ;
#25560=CARTESIAN_POINT ( 'NONE',  ( 50.51702630346309775, -53.30999449162459314, -54.91376886094779763 ) ) ;
#25564=CARTESIAN_POINT ( 'NONE',  ( 52.30043102847849923, -50.70004990181330129, -76.35983844118280217 ) ) ;
#25565=DIRECTION ( 'NONE',  ( -0.3294064756440929220, 0.9441882088883218893, 0.000000000000000000 ) ) ;
#25570=CARTESIAN_POINT ( 'NONE',  ( 41.58741077758180182, 13.58021230090170128, -5.496105773154369878 ) ) ;
#25571=CARTESIAN_POINT ( 'NONE',  ( 41.99652581331089607, -44.42478526866589306, -5.118462684484269332 ) ) ;
#25572=EDGE_CURVE ( 'NONE', #29653, #20020, #9731, .T. ) ;
#25573=CARTESIAN_POINT ( 'NONE',  ( 68.13393739769840352, -50.61618894467879670, -73.25000000000220268 ) ) ;
#25578=CARTESIAN_POINT ( 'NONE',  ( 66.50410218238459947, 1.883581543589160079, -20.28081949647409843 ) ) ;
#25581=CARTESIAN_POINT ( 'NONE',  ( 14.74689323179859990, -52.86909850055779714, -76.12391999848780699 ) ) ;
#25582=CARTESIAN_POINT ( 'NONE',  ( 57.35071420090630312, 19.00220926952300005, -52.74072019877679907 ) ) ;
#25587=EDGE_CURVE ( 'NONE', #36317, #51255, #5098, .T. ) ;
#25588=CARTESIAN_POINT ( 'NONE',  ( 8.038038740883386879, -60.26370295294966439, -21.05410134318717041 ) ) ;
#25590=CARTESIAN_POINT ( 'NONE',  ( 56.48240791863720744, 19.53654756573429907, -53.80987478700529891 ) ) ;
#25591=CARTESIAN_POINT ( 'NONE',  ( 48.03280260593719930, 23.13580117559470040, -55.25606283016369957 ) ) ;
#25594=ORIENTED_EDGE ( 'NONE', *, *, #28778, .T. ) ;
#25595=CONICAL_SURFACE ( 'NONE', #13077, 14.87302494707580180, 1.249045772398249987 ) ;
#25596=DIRECTION ( 'NONE',  ( 0.5951849179585205762, 0.4324271549242467705, 0.6773194734531339245 ) ) ;
#25597=CARTESIAN_POINT ( 'NONE',  ( 57.24929578232330130, -50.61618894764249887, -53.91492796143979405 ) ) ;
#25598=CARTESIAN_POINT ( 'NONE',  ( 84.40405423732200063, 12.27453954208750098, -47.38850513265820297 ) ) ;
#25599=CARTESIAN_POINT ( 'NONE',  ( 52.61984545813539427, 18.57124442378099971, -27.71374801268460075 ) ) ;
#25602=CARTESIAN_POINT ( 'NONE',  ( 56.59132469845479818, -45.11618894467940066, -15.49288788266510153 ) ) ;
#25607=ORIENTED_EDGE ( 'NONE', *, *, #22888, .T. ) ;
#25608=CARTESIAN_POINT ( 'NONE',  ( 12.10371154477140010, -65.18136423378868471, -16.68259577209380140 ) ) ;
#25609=CARTESIAN_POINT ( 'NONE',  ( 12.11391230005439823, 34.07748982303999696, -46.92647627143619360 ) ) ;
#25612=B_SPLINE_CURVE_WITH_KNOTS ( 'NONE', 3,
 ( #15433, #7569, #11244, #7057, #31384, #36107, #35852, #23260, #23008, #3123 ),
 .UNSPECIFIED., .F., .F.,
 ( 4, 2, 2, 2, 4 ),
 ( 0.000000000000000000, 0.1775000000004226253, 0.3375000000003006706, 0.4375000000002248757, 0.5000003605123823913 ),
 .UNSPECIFIED. ) ;
#25613=DIRECTION ( 'NONE',  ( 0.9200120562340469155, -0.3918900565005459247, 0.000000000000000000 ) ) ;
#25615=VERTEX_POINT ( 'NONE', #9985 ) ;
#25618=CARTESIAN_POINT ( 'NONE',  ( 54.63655771189059607, 16.82059223505549994, -26.73578643762699869 ) ) ;
#25619=CARTESIAN_POINT ( 'NONE',  ( 53.26167791221869408, -49.50159509410539727, -49.13884078695329549 ) ) ;
#25620=CARTESIAN_POINT ( 'NONE',  ( 51.50035696899490034, 19.75281252459599912, -50.15572549081029052 ) ) ;
#25621=CARTESIAN_POINT ( 'NONE',  ( 59.83128115804950653, -2.247120905410399772, -15.76168587106839958 ) ) ;
#25622=CARTESIAN_POINT ( 'NONE',  ( 51.01140995548900037, -49.48507500592920394, -76.32135044086720654 ) ) ;
#25623=DIRECTION ( 'NONE',  ( 0.000000000000000000, -1.000000000000000000, 0.000000000000000000 ) ) ;
#25624=ORIENTED_EDGE ( 'NONE', *, *, #45984, .T. ) ;
#25626=DIRECTION ( 'NONE',  ( -0.5951849179585204652, -0.4324271549242469925, 0.6773194734531338135 ) ) ;
#25627=ORIENTED_EDGE ( 'NONE', *, *, #4317, .T. ) ;
#25632=CARTESIAN_POINT ( 'NONE',  ( 13.99297327411639991, -51.17866263145759831, -22.74640880580200175 ) ) ;
#25633=CARTESIAN_POINT ( 'NONE',  ( 54.34362824239659773, 19.58923895723300035, -75.97910198928759939 ) ) ;
#25634=CARTESIAN_POINT ( 'NONE',  ( 46.87137491217979601, -53.55967532393449915, -75.98463753095340678 ) ) ;
#25636=ADVANCED_FACE ( 'NONE', ( #45117 ), #49831, .F. ) ;
#25637=CARTESIAN_POINT ( 'NONE',  ( 56.26232872805620389, 14.29808925844480072, -17.58200819105400114 ) ) ;
#25640=CARTESIAN_POINT ( 'NONE',  ( 57.35094531453579947, -50.23772356244409565, -52.73804475687759918 ) ) ;
#25644=B_SPLINE_CURVE_WITH_KNOTS ( 'NONE', 3,
 ( #22373, #22113, #31011, #10085 ),
 .UNSPECIFIED., .F., .F.,
 ( 4, 4 ),
 ( 3.898674657257720000, 4.021955696373110456 ),
 .UNSPECIFIED. ) ;
#25646=CARTESIAN_POINT ( 'NONE',  ( 47.42191000389319555, 23.38128243525070360, -74.50100479479878857 ) ) ;
#25648=CARTESIAN_POINT ( 'NONE',  ( 75.16212372845173206, -29.54155010626721634, -11.85658773837712054 ) ) ;
#25650=DIRECTION ( 'NONE',  ( 0.2771081164311157696, -0.6505467637364703570, -0.7071067811865504593 ) ) ;
#25652=EDGE_CURVE ( 'NONE', #14404, #39471, #17594, .T. ) ;
#25658=CARTESIAN_POINT ( 'NONE',  ( 61.14427338081150509, 14.07233411761519903, -46.75185522880649813 ) ) ;
#25659=CARTESIAN_POINT ( 'NONE',  ( -33.14628496358510290, -5.854866907655339681, -57.60188784292080300 ) ) ;
#25661=CARTESIAN_POINT ( 'NONE',  ( 52.76045300953009587, -49.70056559441360378, -48.50241422118810419 ) ) ;
#25662=ORIENTED_EDGE ( 'NONE', *, *, #23960, .T. ) ;
#25663=CARTESIAN_POINT ( 'NONE',  ( 57.75416591588980708, -45.11614852472010284, -25.44313242021300070 ) ) ;
#25664=DIRECTION ( 'NONE',  ( 0.000000000000000000, -1.000000000000000000, 0.000000000000000000 ) ) ;
#25665=CARTESIAN_POINT ( 'NONE',  ( 13.61473149145860084, 19.77355128491650049, -21.87339239449909911 ) ) ;
#25666=CARTESIAN_POINT ( 'NONE',  ( 56.52876338304670156, 14.13686770687309924, -25.36325227249279735 ) ) ;
#25669=CARTESIAN_POINT ( 'NONE',  ( 52.83705229977910278, 18.43325409324560127, -48.81125896478140191 ) ) ;
#25671=CARTESIAN_POINT ( 'NONE',  ( 60.32392629779650406, -45.73451482830140691, -47.22595585683189512 ) ) ;
#25672=CARTESIAN_POINT ( 'NONE',  ( 64.81322693590129802, -44.32916768243990191, -10.69846699143639945 ) ) ;
#25673=ORIENTED_EDGE ( 'NONE', *, *, #41564, .T. ) ;
#25676=CARTESIAN_POINT ( 'NONE',  ( 47.39616816378460129, -54.65991725903980125, -54.86393396055039773 ) ) ;
#25679=CARTESIAN_POINT ( 'NONE',  ( 10.91841378337480073, -65.04619103187860674, -17.66395372721920154 ) ) ;
#25683=AXIS2_PLACEMENT_3D ( 'NONE', #853, #49350, #21276 ) ;
#25687=CARTESIAN_POINT ( 'NONE',  ( 8.802047646820330584, -63.20618355599279425, -46.67014429624759941 ) ) ;
#25693=CARTESIAN_POINT ( 'NONE',  ( 53.29069657418769879, 19.80760425434010230, -75.99878262601679069 ) ) ;
#25695=CARTESIAN_POINT ( 'NONE',  ( 61.31807987947320271, 14.40950277385760003, -47.72348187476750070 ) ) ;
#25699=EDGE_CURVE ( 'NONE', #9424, #44314, #41184, .T. ) ;
#25703=CARTESIAN_POINT ( 'NONE',  ( 57.25349264864389909, -45.82938052622620262, -26.26171515177349747 ) ) ;
#25705=CARTESIAN_POINT ( 'NONE',  ( 52.66149646884399971, -49.78765645775949622, -48.73888008360700042 ) ) ;
#25707=CARTESIAN_POINT ( 'NONE',  ( 14.04989515242449905, 20.46947493835569887, -75.41867332334470575 ) ) ;
#25709=CARTESIAN_POINT ( 'NONE',  ( 41.50830747127400144, -45.30505886361360268, -6.113803590135650445 ) ) ;
#25712=ORIENTED_EDGE ( 'NONE', *, *, #22925, .F. ) ;
#25713=CARTESIAN_POINT ( 'NONE',  ( 52.69755715977279920, -49.73393510400349982, -27.86573118051390097 ) ) ;
#25714=CARTESIAN_POINT ( 'NONE',  ( 16.50880182598979573, -51.11266520550329773, -20.14980157100569969 ) ) ;
#25715=CARTESIAN_POINT ( 'NONE',  ( 11.23966493344340023, 33.90699900300699454, -17.15436069251279605 ) ) ;
#25719=CARTESIAN_POINT ( 'NONE',  ( 47.38131247932619772, 14.91674438995409879, -10.59906179801200032 ) ) ;
#25720=ORIENTED_EDGE ( 'NONE', *, *, #15322, .F. ) ;
#25721=CARTESIAN_POINT ( 'NONE',  ( -10.88827818861070185, -42.34077264742860081, -6.211465758528559533 ) ) ;
#25722=CARTESIAN_POINT ( 'NONE',  ( 47.62712401335679857, 23.26915926184220140, -54.68830161141420376 ) ) ;
#25724=CARTESIAN_POINT ( 'NONE',  ( 56.46551779669420057, -50.77616595281960343, -53.85225392423020452 ) ) ;
#25726=CARTESIAN_POINT ( 'NONE',  ( 60.86520825975330240, 14.21854415338730071, -47.04175779766590182 ) ) ;
#25727=CARTESIAN_POINT ( 'NONE',  ( 42.80890084553470132, 12.86785355579670131, -5.063862466711140264 ) ) ;
#25728=CARTESIAN_POINT ( 'NONE',  ( 52.15298324570800048, 18.44951579869039904, -77.15976990859368811 ) ) ;
#25729=CARTESIAN_POINT ( 'NONE',  ( 52.87578304523380268, 18.40442787170260175, -48.67531064471670277 ) ) ;
#25730=CARTESIAN_POINT ( 'NONE',  ( 18.68073206901139471, 24.30204422277620324, -76.07915437898316213 ) ) ;
#25731=CARTESIAN_POINT ( 'NONE',  ( 60.34543612929479650, -45.86997884962860184, -47.73174601672569395 ) ) ;
#25734=CARTESIAN_POINT ( 'NONE',  ( 52.23074715003530599, 21.34763686467589849, -54.40819828980639983 ) ) ;
#25736=CARTESIAN_POINT ( 'NONE',  ( 63.88393739769619373, 4.883811055320659733, -61.34712802272770915 ) ) ;
#25738=ORIENTED_EDGE ( 'NONE', *, *, #328, .T. ) ;
#25740=CARTESIAN_POINT ( 'NONE',  ( 10.77396489004810043, 32.13674430547519734, -45.20697498780340595 ) ) ;
#25741=FACE_OUTER_BOUND ( 'NONE', #12101, .T. ) ;
#25742=CARTESIAN_POINT ( 'NONE',  ( 65.61159321741499184, -31.73702401370160331, -17.31747073895240163 ) ) ;
#25743=CARTESIAN_POINT ( 'NONE',  ( 18.12954445334329989, 19.89798265472740013, -74.14993923597710079 ) ) ;
#25744=VERTEX_POINT ( 'NONE', #1606 ) ;
#25746=CARTESIAN_POINT ( 'NONE',  ( 49.48559182206740559, 22.51696836342139818, -55.18124709514480486 ) ) ;
#25748=CARTESIAN_POINT ( 'NONE',  ( 12.56728399523450079, -65.44523288411160422, -46.96404464519110178 ) ) ;
#25749=CARTESIAN_POINT ( 'NONE',  ( 56.44632044434209917, -46.23264868926420235, -26.25478470813849796 ) ) ;
#25750=CARTESIAN_POINT ( 'NONE',  ( 76.21898748821377012, -48.61618894467930119, -83.94294850574455324 ) ) ;
#25756=CARTESIAN_POINT ( 'NONE',  ( 49.15516447654730570, -45.57934867088179942, -11.33945784234580145 ) ) ;
#25757=EDGE_CURVE ( 'NONE', #43986, #1848, #26030, .T. ) ;
#25761=ADVANCED_FACE ( 'NONE', ( #30913 ), #14691, .F. ) ;
#25762=ORIENTED_EDGE ( 'NONE', *, *, #1600, .T. ) ;
#25763=B_SPLINE_CURVE_WITH_KNOTS ( 'NONE', 3,
 ( #26793, #6900, #31483, #11604, #42544, #22851, #38871, #2434, #47507, #7157, #23110, #39128, #42280, #2960, #47004, #18933 ),
 .UNSPECIFIED., .F., .F.,
 ( 4, 2, 2, 2, 2, 2, 2, 4 ),
 ( -5.400124999999999671E-13, 0.7105627886305859731, 1.313424307618820119, 1.690212756986460008, 1.931671722270319913, 2.414589652838039946, 3.187258341746380008, 3.863343444541179839 ),
 .UNSPECIFIED. ) ;
#25764=ADVANCED_FACE ( 'NONE', ( #10513 ), #10521, .T. ) ;
#25766=CARTESIAN_POINT ( 'NONE',  ( 47.09611959407079951, -54.55650624126920434, -75.12137911381070410 ) ) ;
#25767=CARTESIAN_POINT ( 'NONE',  ( 49.79848667668909457, 12.57015533470270086, -6.517774395972690371 ) ) ;
#25770=CARTESIAN_POINT ( 'NONE',  ( 52.06789743720410257, 13.88381105532070059, -11.75767006276409887 ) ) ;
#25771=CARTESIAN_POINT ( 'NONE',  ( 51.97963026116360652, 21.17322201635790080, -53.55374510773989982 ) ) ;
#25772=CARTESIAN_POINT ( 'NONE',  ( 51.02815224725549825, 19.65062265738080072, -76.14999943445199904 ) ) ;
#25773=CARTESIAN_POINT ( 'NONE',  ( 57.74431620579319713, 13.88376939222820106, -25.44123524798349933 ) ) ;
#25775=VERTEX_POINT ( 'NONE', #21627 ) ;
#25777=CARTESIAN_POINT ( 'NONE',  ( -11.22462160640339945, -41.78302095251060422, -5.474790624452850807 ) ) ;
#25778=CARTESIAN_POINT ( 'NONE',  ( 76.75364055736000068, -40.92245084168380487, -14.31887545395620087 ) ) ;
#25779=CARTESIAN_POINT ( 'NONE',  ( 0.5716597380707004739, -15.61618894405949831, -8.050000000008262546 ) ) ;
#25780=ADVANCED_FACE ( 'NONE', ( #13794 ), #3459, .F. ) ;
#25781=( BOUNDED_CURVE ( )  B_SPLINE_CURVE ( 3, ( #9241, #1363, #49844, #33319 ),
 .UNSPECIFIED., .F., .T. ) 
 B_SPLINE_CURVE_WITH_KNOTS ( ( 4, 4 ),
 ( 2.269173848739415078, 2.375544669831940237 ),
 .UNSPECIFIED. ) 
 CURVE ( )  GEOMETRIC_REPRESENTATION_ITEM ( )  RATIONAL_B_SPLINE_CURVE ( ( 1.000000000000000000, 0.9990573262772525220, 0.9990573262772525220, 1.000000000000000000 ) ) 
 REPRESENTATION_ITEM ( '' )  );
#25785=CARTESIAN_POINT ( 'NONE',  ( 59.11308834892447805, 16.26059245213280136, -49.51867816856292137 ) ) ;
#25786=CARTESIAN_POINT ( 'NONE',  ( 43.60412366894710345, -43.70472620657429985, -5.064848484333539957 ) ) ;
#25793=CARTESIAN_POINT ( 'NONE',  ( -2.611048155534260395, 19.76244989865589829, -8.524257365257900787 ) ) ;
#25794=CARTESIAN_POINT ( 'NONE',  ( 60.78207366828240055, -45.60272865987860769, -47.53378783808489771 ) ) ;
#25801=CIRCLE ( 'NONE', #24972, 1.999999999999995115 ) ;
#25802=CARTESIAN_POINT ( 'NONE',  ( 56.84932592767829362, -50.65659099804129539, -63.99406948319280275 ) ) ;
#25803=CARTESIAN_POINT ( 'NONE',  ( 40.69061954106139467, -45.32287878058329511, -5.669818197142030058 ) ) ;
#25808=CARTESIAN_POINT ( 'NONE',  ( 53.12256372476250021, -49.57422361163540359, -49.14106871637599738 ) ) ;
#25809=DIRECTION ( 'NONE',  ( 0.000000000000000000, 0.000000000000000000, 1.000000000000000000 ) ) ;
#25810=CARTESIAN_POINT ( 'NONE',  ( 55.98862517971360120, -50.75900301025659900, -53.00668962061499911 ) ) ;
#25812=VERTEX_POINT ( 'NONE', #14047 ) ;
#25814=CARTESIAN_POINT ( 'NONE',  ( 50.12109376404330163, -53.47864665676979712, -55.01406006385839476 ) ) ;
#25815=CARTESIAN_POINT ( 'NONE',  ( 11.13393739769619906, -55.30245861064819479, -24.15000000000000213 ) ) ;
#25817=CARTESIAN_POINT ( 'NONE',  ( 56.84932592767840021, 19.42421310868259354, -74.14999999999999147 ) ) ;
#25818=CARTESIAN_POINT ( 'NONE',  ( 53.70323348958860521, -50.76982429470329805, -76.35188063097180589 ) ) ;
#25819=CARTESIAN_POINT ( 'NONE',  ( 60.23130391297029718, 14.55066440145539985, -47.24246919202519734 ) ) ;
#25820=EDGE_CURVE ( 'NONE', #41896, #12580, #32707, .T. ) ;
#25822=CARTESIAN_POINT ( 'NONE',  ( 1.027904703268269992, 11.45423359053189927, -15.65000000000000036 ) ) ;
#25823=CARTESIAN_POINT ( 'NONE',  ( 43.16865701737530259, 13.99521548782530012, -6.804304403661720180 ) ) ;
#25824=CARTESIAN_POINT ( 'NONE',  ( 42.30536707268809948, -43.16822450031050096, -3.349718967764970134 ) ) ;
#25826=CARTESIAN_POINT ( 'NONE',  ( 55.98228069898435422, 14.58868318825703092, -25.31776496031197610 ) ) ;
#25831=VECTOR ( 'NONE', #40852, 1000.000000000000000 ) ;
#25832=CARTESIAN_POINT ( 'NONE',  ( 67.98303682264749170, 0.1477386350055570063, -18.18688548989880260 ) ) ;
#25834=CARTESIAN_POINT ( 'NONE',  ( 15.05440318628160057, -53.11618894467930119, -76.14999999999999147 ) ) ;
#25835=CARTESIAN_POINT ( 'NONE',  ( 57.31533494679120366, 19.23294600587710335, -53.15033584403609979 ) ) ;
#25839=CARTESIAN_POINT ( 'NONE',  ( 46.97440434136990461, -54.33447984715540002, -75.47461153638509757 ) ) ;
#25841=CARTESIAN_POINT ( 'NONE',  ( 11.49998292432769986, 34.13930433918829976, -17.88621716035489939 ) ) ;
#25842=B_SPLINE_CURVE_WITH_KNOTS ( 'NONE', 3,
 ( #43893, #5104, #24973, #21059, #36526, #27887, #40731, #28921, #36268, #24193, #37058, #49133, #16103, #44406, #4308, #9027, #24715, #378 ),
 .UNSPECIFIED., .F., .F.,
 ( 4, 2, 2, 2, 2, 2, 2, 2, 4 ),
 ( 0.000000000000000000, 0.1774999104122986782, 0.3374998296571877221, 0.4374997791852425766, 0.4999997476402775476, 0.6249996845503474896, 0.7565686301423247828, 0.9670789430894899397, 1.000000000000000000 ),
 .UNSPECIFIED. ) ;
#25844=CARTESIAN_POINT ( 'NONE',  ( 56.43926849312130400, 19.54193581886750053, -53.62500735189280476 ) ) ;
#25845=CARTESIAN_POINT ( 'NONE',  ( 47.97791291234110389, 23.15825109668029924, -55.19708778542380401 ) ) ;
#25846=ORIENTED_EDGE ( 'NONE', *, *, #35887, .F. ) ;
#25850=CARTESIAN_POINT ( 'NONE',  ( 16.13393739769620083, -15.61618894467929941, 7.349999999999999645 ) ) ;
#25852=CARTESIAN_POINT ( 'NONE',  ( 84.43710458089100257, 12.07919292302930181, -47.42958317885469910 ) ) ;
#25853=DIRECTION ( 'NONE',  ( 0.3569024281753349626, 0.000000000000000000, 0.9341416684649872515 ) ) ;
#25856=CARTESIAN_POINT ( 'NONE',  ( 11.13393739769619906, -55.30245861064819479, -24.15000000000000213 ) ) ;
#25858=CARTESIAN_POINT ( 'NONE',  ( 56.18972397053033063, -45.98241309864640414, -26.01119422816448079 ) ) ;
#25863=ADVANCED_FACE ( 'NONE', ( #6969 ), #34983, .T. ) ;
#25865=CARTESIAN_POINT ( 'NONE',  ( 12.72020591613260088, 34.25200402611910278, -47.31888902628400473 ) ) ;
#25867=CIRCLE ( 'NONE', #3299, 2.999999999999997780 ) ;
#25869=LINE ( 'NONE', #17519, #9962 ) ;
#25870=AXIS2_PLACEMENT_3D ( 'NONE', #32583, #32331, #20810 ) ;
#25873=VERTEX_POINT ( 'NONE', #30530 ) ;
#25875=CARTESIAN_POINT ( 'NONE',  ( 57.33795248997969907, 14.58087673940109852, -26.27059240990359967 ) ) ;
#25877=CARTESIAN_POINT ( 'NONE',  ( 47.28886650904659206, 23.50118699693149793, -54.78430227607729819 ) ) ;
#25878=CARTESIAN_POINT ( 'NONE',  ( 59.89120361409349869, -2.379225728188540501, -15.76033884563189957 ) ) ;
#25879=CARTESIAN_POINT ( 'NONE',  ( 51.16024758163639774, -50.72509723359110012, -76.16561535978119934 ) ) ;
#25880=CARTESIAN_POINT ( 'NONE',  ( 60.25366577380279409, -46.63518866124190509, -48.78944481778400188 ) ) ;
#25881=EDGE_CURVE ( 'NONE', #50462, #25775, #47855, .T. ) ;
#25884=CARTESIAN_POINT ( 'NONE',  ( 68.13393739769814772, 19.38381105532029736, -71.50000000000200373 ) ) ;
#25886=CARTESIAN_POINT ( 'NONE',  ( 12.33745008528437026, -55.43540947936329388, -75.02879301533954504 ) ) ;
#25887=DIRECTION ( 'NONE',  ( -0.7956403955640117820, 0.6057692307692287281, 0.000000000000000000 ) ) ;
#25890=CARTESIAN_POINT ( 'NONE',  ( 13.32592044370020012, -50.85448151712510167, -21.60957454853980053 ) ) ;
#25891=CARTESIAN_POINT ( 'NONE',  ( 54.67606251842929765, 19.48951422470729966, -76.08857982990380719 ) ) ;
#25892=CARTESIAN_POINT ( 'NONE',  ( 47.48063017875849567, -54.33024059387050642, -75.12266286288350159 ) ) ;
#25894=CARTESIAN_POINT ( 'NONE',  ( 55.96902438450270978, 14.60256988625710051, -17.93020271988870107 ) ) ;
#25895=CARTESIAN_POINT ( 'NONE',  ( 47.66479567111289839, 23.29271780185170115, -55.15155557582939849 ) ) ;
#25896=CARTESIAN_POINT ( 'NONE',  ( 56.96867955654300175, -50.47610601613909864, -53.05103816245590309 ) ) ;
#25899=CARTESIAN_POINT ( 'NONE',  ( 47.07698750752110328, 22.65904192746489798, -75.76367654143750485 ) ) ;
#25902=CARTESIAN_POINT ( 'NONE',  ( 40.76017235305160114, -45.36108721241059527, -5.740519108723990627 ) ) ;
#25908=CARTESIAN_POINT ( 'NONE',  ( 18.86789271228450104, 20.55440457967890211, -74.14999999999999147 ) ) ;
#25914=CARTESIAN_POINT ( 'NONE',  ( 61.22873865439940033, 14.02808039422199826, -46.61559125704629736 ) ) ;
#25915=CARTESIAN_POINT ( 'NONE',  ( -26.90058206776729932, 10.62243301518619987, -56.03720707547429924 ) ) ;
#25917=CARTESIAN_POINT ( 'NONE',  ( 52.82947468502609922, -49.66147222709160047, -48.64744666514059901 ) ) ;
#25921=CARTESIAN_POINT ( 'NONE',  ( 57.05026703580490022, 13.94318891463120025, -25.51228499960440388 ) ) ;
#25924=CARTESIAN_POINT ( 'NONE',  ( 53.24078573210410070, 18.24730475180699685, -49.04425871532740189 ) ) ;
#25927=CARTESIAN_POINT ( 'NONE',  ( 55.68173555688790088, -48.93614072104979584, -53.85224183628929495 ) ) ;
#25931=EDGE_CURVE ( 'NONE', #51329, #30578, #22668, .T. ) ;
#25935=CARTESIAN_POINT ( 'NONE',  ( 11.01613591012540105, -65.16628805936319679, -18.04558894943079750 ) ) ;
#25936=CARTESIAN_POINT ( 'NONE',  ( 52.82975622904280755, 18.42854261028849905, -48.48625935290110078 ) ) ;
#25937=DIRECTION ( 'NONE',  ( 0.3569024281753415129, 0.000000000000000000, 0.9341416684649846980 ) ) ;
#25941=ORIENTED_EDGE ( 'NONE', *, *, #4974, .T. ) ;
#25942=CARTESIAN_POINT ( 'NONE',  ( 8.967302953424740153, -63.21494621409839709, -46.63268177960510030 ) ) ;
#25943=LINE ( 'NONE', #14946, #5957 ) ;
#25947=DIRECTION ( 'NONE',  ( 0.000000000000000000, 0.000000000000000000, -1.000000000000000000 ) ) ;
#25948=AXIS2_PLACEMENT_3D ( 'NONE', #21319, #18179, #1423 ) ;
#25949=CARTESIAN_POINT ( 'NONE',  ( 52.35198200795250045, 18.81557687444639981, -76.97988190764880301 ) ) ;
#25950=VECTOR ( 'NONE', #15978, 1000.000000000000114 ) ;
#25951=ORIENTED_EDGE ( 'NONE', *, *, #328, .F. ) ;
#25959=B_SPLINE_SURFACE_WITH_KNOTS ( 'NONE', 3, 3, ( 
 ( #13648, #42911, #25671, #27159, #29858, #45879, #29354, #9966, #22958, #37749, #9711, #45360, #41941, #18784, #6042, #38980 ),
 ( #1586, #9462, #1846, #51022, #25410, #31081, #38008, #43167, #41413, #17575, #33543, #2817, #34762, #29608, #41673, #5779 ),
 ( #46851, #31591, #4090, #20316, #47362, #20574, #36305, #39492, #415, #12474, #16402, #23728, #11713, #24493, #36567, #3590 ),
 ( #43678, #27416, #48377, #32101, #36058, #167, #40511, #19563, #23977, #32359, #28442, #44444, #20064, #39744, #8027, #43930 ),
 ( #47612, #11459, #15383, #43421, #8550, #47870, #16141, #4599, #27676, #44183, #15894, #31336, #40001, #7778, #3846, #12219 ),
 ( #7521, #23469, #48120, #35552, #19819, #51542, #15639, #35807, #51791, #31851, #11973, #27928, #28181, #8283, #24231, #40256 ),
 ( #4348, #40768, #17701, #25540, #28964, #21354, #13265, #17190, #25794, #1198, #1456, #938, #29221, #21874, #41544, #16934 ),
 ( #45488, #16659, #44701, #5144, #41028, #25014, #21098, #33411, #33669, #28699, #37101, #13526, #48644, #29483, #8806, #4869 ),
 ( #20836, #32878, #49429, #9586, #33147, #41803, #49174, #36834, #37357, #5660, #21607, #48912, #32616, #1717, #37611, #45228 ),
 ( #9336, #45748, #49684, #5909, #13778, #669, #29732, #25283, #17445, #41287, #13009, #5397, #44963, #9842, #12744, #24758 ),
 ( #9065, #6694, #22392, #22652, #47057, #22131, #46794, #6172, #38138, #38396, #38672, #2757, #26581, #18729, #31031, #34967 ) ),
 .UNSPECIFIED., .F., .F., .F.,
 ( 4, 1, 1, 1, 1, 1, 1, 1, 4 ),
 ( 4, 2, 2, 2, 2, 2, 2, 4 ),
 ( 0.000000000000000000, 0.1250000000000000000, 0.2500000000000000000, 0.3750000000000000000, 0.5000000000000000000, 0.6250000000000000000, 0.7500000000000000000, 0.8750000000000000000, 1.000000000000000000 ),
 ( 6.048176999999999513E-14, 0.1586790292817849835, 0.3005262815670050047, 0.4007017087559869850, 0.4507894223504779752, 0.5309297641016630376, 0.6591543109035590264, 0.8014034175119129078 ),
 .UNSPECIFIED. ) ;
#25961=B_SPLINE_CURVE_WITH_KNOTS ( 'NONE', 3,
 ( #24424, #5331, #40438, #4530, #17374, #33341, #20502, #36495, #599, #16584, #32537, #48571 ),
 .UNSPECIFIED., .F., .F.,
 ( 4, 2, 2, 2, 2, 4 ),
 ( 0.000000000000000000, 0.05115848177113838796, 0.3903315494385208306, 0.7421782045515662452, 0.9620823639972201358, 1.000000000000000000 ),
 .UNSPECIFIED. ) ;
#25966=CARTESIAN_POINT ( 'NONE',  ( 57.23048878589050048, -45.83455400380619693, -26.25958840414919848 ) ) ;
#25969=CARTESIAN_POINT ( 'NONE',  ( 13.42257066052990133, 20.48963383789619996, -74.34036667011370980 ) ) ;
#25970=CARTESIAN_POINT ( 'NONE',  ( 11.13393739769619906, 24.07008072128950005, -43.74348518090240390 ) ) ;
#25971=CARTESIAN_POINT ( 'NONE',  ( 41.13179987942019977, -45.04922869730629742, -5.658934828260900218 ) ) ;
#25975=CARTESIAN_POINT ( 'NONE',  ( 53.35940782512449942, -48.99705445778459278, -26.69012152621940359 ) ) ;
#25976=CARTESIAN_POINT ( 'NONE',  ( 54.76812893638570046, -50.71857552302670058, -76.05693996196100670 ) ) ;
#25978=CARTESIAN_POINT ( 'NONE',  ( 70.26204857723202224, 12.15939804013194880, -11.90373897417649829 ) ) ;
#25981=PLANE ( 'NONE',  #8880 ) ;
#25983=ORIENTED_EDGE ( 'NONE', *, *, #25881, .T. ) ;
#25984=CARTESIAN_POINT ( 'NONE',  ( -11.32734370190460105, -41.88171845330919751, -6.430192534648670133 ) ) ;
#25985=AXIS2_PLACEMENT_3D ( 'NONE', #49285, #24875, #40884 ) ;
#25986=CARTESIAN_POINT ( 'NONE',  ( 47.53188093336569864, 23.33481414632970186, -54.72542454593359906 ) ) ;
#25989=CARTESIAN_POINT ( 'NONE',  ( 12.99333467301740086, 19.39160263449290156, -21.36722376697930059 ) ) ;
#25991=CIRCLE ( 'NONE', #13498, 15.29999999999999716 ) ;
#25992=CARTESIAN_POINT ( 'NONE',  ( 11.62127288507080003, 34.09666180512939349, -17.36671666713459672 ) ) ;
#25996=CARTESIAN_POINT ( 'NONE',  ( 57.59125325346249724, -47.31051068446480201, -48.20109099143959952 ) ) ;
#25998=ADVANCED_FACE ( 'NONE', ( #39194, #43386 ), #15081, .T. ) ;
#25999=CARTESIAN_POINT ( 'NONE',  ( 54.45614327494340046, 20.39970296835699770, -54.11881936521780290 ) ) ;
#26003=CARTESIAN_POINT ( 'NONE',  ( 19.94077147091733337, 23.62963092878765536, -18.33136226284473125 ) ) ;
#26004=CARTESIAN_POINT ( 'NONE',  ( 10.77166614911110187, 32.01493747166969683, -45.20465578477089963 ) ) ;
#26006=B_SPLINE_CURVE_WITH_KNOTS ( 'NONE', 3,
 ( #19564, #39231, #7522, #43422, #30824, #47110, #10940, #46852, #42912, #8028, #11461, #47613, #4091, #27160, #23729, #15384 ),
 .UNSPECIFIED., .F., .F.,
 ( 4, 2, 2, 2, 2, 2, 2, 4 ),
 ( 0.000000000000000000, 1.392512724848399941, 2.647735462739909895, 3.432249673922110222, 3.922571055910980320, 4.903213819888729397, 6.472242242253120281, 7.845142111821970410 ),
 .UNSPECIFIED. ) ;
#26007=CARTESIAN_POINT ( 'NONE',  ( 66.14674587413610141, -31.04161172517479983, -17.02975172920780267 ) ) ;
#26010=ORIENTED_EDGE ( 'NONE', *, *, #27200, .F. ) ;
#26011=CARTESIAN_POINT ( 'NONE',  ( 49.60654698967459808, 22.46544607396180027, -55.15184126837920076 ) ) ;
#26012=CARTESIAN_POINT ( 'NONE',  ( 50.77833043287579073, -0.1940347697328212717, -16.58944421967073524 ) ) ;
#26014=CARTESIAN_POINT ( 'NONE',  ( 12.05814235705390125, -65.22170215249130365, -46.28435471616069918 ) ) ;
#26015=CARTESIAN_POINT ( 'NONE',  ( 56.86392865038990152, -45.57086430673709998, -26.04468540372219820 ) ) ;
#26022=CARTESIAN_POINT ( 'NONE',  ( 51.85399221484009757, -45.59830427757680127, -13.29383979432519958 ) ) ;
#26024=CARTESIAN_POINT ( 'NONE',  ( 14.56142577301880081, 19.88381692480329832, -22.31059544230340208 ) ) ;
#26025=EDGE_CURVE ( 'NONE', #42086, #13057, #31930, .T. ) ;
#26029=CARTESIAN_POINT ( 'NONE',  ( 46.74845599210109981, -53.81985652269789711, -75.90842213619210099 ) ) ;
#26030=CIRCLE ( 'NONE', #18519, 20.00000000000000355 ) ;
#26031=CARTESIAN_POINT ( 'NONE',  ( 49.73684662565250392, 13.14257322138860040, -6.768569892874900518 ) ) ;
#26033=CARTESIAN_POINT ( 'NONE',  ( 50.47459759387780309, -50.28724450852030259, -76.14999999999999147 ) ) ;
#26035=CARTESIAN_POINT ( 'NONE',  ( 51.42797782268849716, 19.97168430531710115, -76.10787250224271361 ) ) ;
#26036=CARTESIAN_POINT ( 'NONE',  ( 58.51605347960990144, 13.88377689860699959, -25.61130927043330274 ) ) ;
#26039=DIRECTION ( 'NONE',  ( 0.000000000000000000, 0.000000000000000000, 1.000000000000000000 ) ) ;
#26040=CARTESIAN_POINT ( 'NONE',  ( -9.207529314482119531, -42.75858213421489751, -4.288095148114170030 ) ) ;
#26044=CARTESIAN_POINT ( 'NONE',  ( 20.13393739768955726, -55.41568642894477392, -74.40622738393629731 ) ) ;
#26045=CARTESIAN_POINT ( 'NONE',  ( 7.523314408995540603, 29.85141564380720069, -20.29480228628009542 ) ) ;
#26047=CARTESIAN_POINT ( 'NONE',  ( 41.52331217820510290, 12.65721966367290108, -3.580227199495849888 ) ) ;
#26050=DIRECTION ( 'NONE',  ( 0.9486832980505123247, 0.000000000000000000, 0.3162277660168421045 ) ) ;
#26051=EDGE_CURVE ( 'NONE', #24834, #46021, #33751, .T. ) ;
#26053=CARTESIAN_POINT ( 'NONE',  ( 18.74893938429089957, -51.88241111309920228, -74.91994212300119216 ) ) ;
#26060=ORIENTED_EDGE ( 'NONE', *, *, #4133, .F. ) ;
#26062=AXIS2_PLACEMENT_3D ( 'NONE', #35252, #38942, #31557 ) ;
#26068=EDGE_CURVE ( 'NONE', #9489, #41896, #3236, .T. ) ;
#26070=DIRECTION ( 'NONE',  ( 0.7800418122827239564, 0.000000000000000000, -0.6257273935913973961 ) ) ;
#26071=ORIENTED_EDGE ( 'NONE', *, *, #1763, .F. ) ;
#26074=CARTESIAN_POINT ( 'NONE',  ( 61.18552659700819873, -45.29711232550319266, -46.94415545492860531 ) ) ;
#26075=CARTESIAN_POINT ( 'NONE',  ( 60.97477285130578650, 14.20885590850662261, -47.29314152441210695 ) ) ;
#26076=CARTESIAN_POINT ( 'NONE',  ( 82.75389963950320293, -45.59493862562369770, -47.67227237921210303 ) ) ;
#26082=ADVANCED_FACE ( 'NONE', ( #32064 ), #24195, .F. ) ;
#26086=CARTESIAN_POINT ( 'NONE',  ( 51.63598217325660045, -50.37061234098579376, -76.35349662556009775 ) ) ;
#26087=CARTESIAN_POINT ( 'NONE',  ( 60.77503050668930484, 14.28448999696009913, -47.26114755906990439 ) ) ;
#26089=DIRECTION ( 'NONE',  ( 0.000000000000000000, -1.000000000000000000, 0.000000000000000000 ) ) ;
#26090=CARTESIAN_POINT ( 'NONE',  ( 45.82863908892869631, 13.88351059623800055, -7.494183445420209644 ) ) ;
#26091=CARTESIAN_POINT ( 'NONE',  ( 42.33768682256320659, -43.16216139800930307, -3.566431340445090026 ) ) ;
#26092=CARTESIAN_POINT ( 'NONE',  ( 7.517033938252880354, 30.35161808146150264, -19.14999999999999858 ) ) ;
#26094=( BOUNDED_CURVE ( )  B_SPLINE_CURVE ( 3, ( #33205, #9389, #5960, #25334 ),
 .UNSPECIFIED., .F., .T. ) 
 B_SPLINE_CURVE_WITH_KNOTS ( ( 4, 4 ),
 ( 5.387239059104177663, 6.283185307179586232 ),
 .UNSPECIFIED. ) 
 CURVE ( )  GEOMETRIC_REPRESENTATION_ITEM ( )  RATIONAL_B_SPLINE_CURVE ( ( 1.000000000000000000, 0.9342179155433358861, 0.9342179155433358861, 1.000000000000000000 ) ) 
 REPRESENTATION_ITEM ( '' )  );
#26096=EDGE_CURVE ( 'NONE', #16045, #45245, #23940, .T. ) ;
#26100=EDGE_LOOP ( 'NONE', ( #32957, #27217, #42142, #1935 ) ) ;
#26101=DIRECTION ( 'NONE',  ( -0.8696770943991732894, 0.4936210606096660958, -7.688651000000001506E-17 ) ) ;
#26102=CARTESIAN_POINT ( 'NONE',  ( 57.30262419534599871, 19.28754421135300134, -53.29749903242779396 ) ) ;
#26103=CARTESIAN_POINT ( 'NONE',  ( 9.618181908336627117, 33.17626444789963358, -46.87734673171561184 ) ) ;
#26104=DIRECTION ( 'NONE',  ( 0.000000000000000000, -0.7371541403039566509, 0.6757246284047478957 ) ) ;
#26105=CARTESIAN_POINT ( 'NONE',  ( 46.44868656089280279, -53.13167745678150311, -76.13981661584659832 ) ) ;
#26107=CARTESIAN_POINT ( 'NONE',  ( 47.82090655655320433, -54.45843870253389696, -55.22757576880370323 ) ) ;
#26110=CARTESIAN_POINT ( 'NONE',  ( 48.17643508576089317, 23.07461921580190278, -55.27613280443460297 ) ) ;
#26111=ORIENTED_EDGE ( 'NONE', *, *, #23895, .T. ) ;
#26114=ADVANCED_FACE ( 'NONE', ( #4057 ), #1269, .T. ) ;
#26115=VERTEX_POINT ( 'NONE', #47518 ) ;
#26116=PRODUCT_DEFINITION_SHAPE ( 'NONE', 'NONE',  #45296 ) ;
#26119=CARTESIAN_POINT ( 'NONE',  ( 82.75389963950189554, 14.36256073625980001, -47.67227237920639737 ) ) ;
#26121=CARTESIAN_POINT ( 'NONE',  ( 83.78435757737699419, 13.39064817555830089, -47.11582429421620333 ) ) ;
#26123=LINE ( 'NONE', #42135, #13698 ) ;
#26126=DIRECTION ( 'NONE',  ( -1.000000000000000000, 0.000000000000000000, 0.000000000000000000 ) ) ;
#26127=EDGE_LOOP ( 'NONE', ( #43685, #38203, #12704, #32261 ) ) ;
#26129=ORIENTED_EDGE ( 'NONE', *, *, #51230, .F. ) ;
#26131=CARTESIAN_POINT ( 'NONE',  ( 12.36320305068320025, -64.54682834576858852, -15.76422791927960176 ) ) ;
#26135=CARTESIAN_POINT ( 'NONE',  ( 12.39246200226850014, -65.46010474692718617, -47.59569286893109563 ) ) ;
#26138=ORIENTED_EDGE ( 'NONE', *, *, #43117, .T. ) ;
#26141=CARTESIAN_POINT ( 'NONE',  ( 52.73337885104540135, 18.44966310541049737, -48.25078709180450431 ) ) ;
#26142=CARTESIAN_POINT ( 'NONE',  ( 65.47927597481400142, -1.466436190217940139, -16.55648068461299971 ) ) ;
#26144=CARTESIAN_POINT ( 'NONE',  ( 51.14620533116269741, -49.75767105349819985, -76.32769630694630791 ) ) ;
#26145=CARTESIAN_POINT ( 'NONE',  ( 59.38599522353990068, -47.70324967091819701, -49.95552091575579823 ) ) ;
#26146=VERTEX_POINT ( 'NONE', #25736 ) ;
#26148=CARTESIAN_POINT ( 'NONE',  ( 70.83393739769690001, 16.88381105531530579, -74.20000000000047180 ) ) ;
#26149=EDGE_LOOP ( 'NONE', ( #20776, #30250 ) ) ;
#26151=CARTESIAN_POINT ( 'NONE',  ( 55.64908854110159808, -48.32622745761450034, -48.64133301306080170 ) ) ;
#26153=CARTESIAN_POINT ( 'NONE',  ( 52.97768859602520308, -49.62760585955020076, -49.05519427004490041 ) ) ;
#26154=CARTESIAN_POINT ( 'NONE',  ( 14.04300386716569982, -50.94367055530580757, -21.72002249117950257 ) ) ;
#26155=CARTESIAN_POINT ( 'NONE',  ( 57.01957022279430021, 19.39593752494300105, -74.14897285927730763 ) ) ;
#26156=CARTESIAN_POINT ( 'NONE',  ( 46.69907961121389661, -53.35444326668270065, -76.07703971530399656 ) ) ;
#26157=ORIENTED_EDGE ( 'NONE', *, *, #3185, .F. ) ;
#26158=CARTESIAN_POINT ( 'NONE',  ( 55.95110166314709943, 14.60640795197440056, -17.62158316991920159 ) ) ;
#26160=CARTESIAN_POINT ( 'NONE',  ( 56.57206750191940614, -50.73353241686610460, -53.72158482581370009 ) ) ;
#26165=EDGE_CURVE ( 'NONE', #34653, #13586, #38222, .T. ) ;
#26166=CARTESIAN_POINT ( 'NONE',  ( 47.32559383855520707, 22.99766105135049798, -75.35927704317229825 ) ) ;
#26168=CARTESIAN_POINT ( 'NONE',  ( 75.16211347727251280, -29.54091756298097948, -11.85653830296175926 ) ) ;
#26170=CIRCLE ( 'NONE', #1092, 28.31678667024650409 ) ;
#26171=CARTESIAN_POINT ( 'NONE',  ( 57.50723795381379944, -45.11618894467940066, -25.33268388717609909 ) ) ;
#26172=DIRECTION ( 'NONE',  ( 0.3805321250008310008, 0.000000000000000000, -0.9247677015566404535 ) ) ;
#26173=CARTESIAN_POINT ( 'NONE',  ( 82.68210891836909582, 14.16981534136089849, -47.42732332448029808 ) ) ;
#26179=CARTESIAN_POINT ( 'NONE',  ( 12.76594342643739921, 33.07036822156479872, -45.89070534480030261 ) ) ;
#26182=CARTESIAN_POINT ( 'NONE',  ( 52.76604523481000086, -49.70803434126499809, -48.76247711586999856 ) ) ;
#26186=CARTESIAN_POINT ( 'NONE',  ( 13.79402747301139875, 19.88244612326230154, -22.16946263372249959 ) ) ;
#26187=CARTESIAN_POINT ( 'NONE',  ( 57.25554329504040396, 13.89079948325800018, -25.31272174971099886 ) ) ;
#26189=CARTESIAN_POINT ( 'NONE',  ( 36.93393739769619799, -15.61618894467929941, -12.65000000000000036 ) ) ;
#26190=CARTESIAN_POINT ( 'NONE',  ( 53.26169323521300214, 18.26921110352349942, -49.13884436845789594 ) ) ;
#26199=CARTESIAN_POINT ( 'NONE',  ( 11.89321892218980103, -65.43602743108449715, -18.17421237902440012 ) ) ;
#26205=ORIENTED_EDGE ( 'NONE', *, *, #453, .T. ) ;
#26206=CARTESIAN_POINT ( 'NONE',  ( 10.14016983710170017, -63.19813366497749030, -45.99431160738090085 ) ) ;
#26207=CIRCLE ( 'NONE', #42119, 21.50000000000000000 ) ;
#26208=LINE ( 'NONE', #5798, #42830 ) ;
#26211=CARTESIAN_POINT ( 'NONE',  ( 57.27159524557450254, 19.01963230153999973, -52.75109250000340211 ) ) ;
#26212=CARTESIAN_POINT ( 'NONE',  ( 53.83004547088629721, 19.36722000321880088, -77.06233108604320137 ) ) ;
#26215=VECTOR ( 'NONE', #14102, 1000.000000000000000 ) ;
#26216=CARTESIAN_POINT ( 'NONE',  ( 12.77233515538412512, -65.50098146119171361, -47.69352623444314787 ) ) ;
#26221=DIRECTION ( 'NONE',  ( 1.000000000000000000, 0.000000000000000000, 0.000000000000000000 ) ) ;
#26224=ORIENTED_EDGE ( 'NONE', *, *, #16379, .F. ) ;
#26225=CARTESIAN_POINT ( 'NONE',  ( 57.28506249589020172, -45.82228059267649911, -26.26463383974999743 ) ) ;
#26227=CARTESIAN_POINT ( 'NONE',  ( 53.58092488835709588, -49.39931725161739706, -49.20716744093340367 ) ) ;
#26230=ADVANCED_FACE ( 'NONE', ( #14481 ), #22068, .T. ) ;
#26232=DIRECTION ( 'NONE',  ( 0.000000000000000000, 0.000000000000000000, -1.000000000000000000 ) ) ;
#26233=CARTESIAN_POINT ( 'NONE',  ( 14.15215969969850107, 19.92749982851029955, -74.54610039094001195 ) ) ;
#26236=CARTESIAN_POINT ( 'NONE',  ( 44.72927470446840204, -45.40228777558419893, -7.990864045375530189 ) ) ;
#26240=CARTESIAN_POINT ( 'NONE',  ( 55.05504109302290061, -47.02930131300339411, -25.82589578894450000 ) ) ;
#26241=CARTESIAN_POINT ( 'NONE',  ( 55.16108428730660052, -50.93339917627999824, -75.32514449214200170 ) ) ;
#26242=CARTESIAN_POINT ( 'NONE',  ( 1.761208164887659855, 24.33375541177040091, -11.00324065032750021 ) ) ;
#26250=CARTESIAN_POINT ( 'NONE',  ( 47.38645038732749981, 23.43329625106930081, -54.85297834023369745 ) ) ;
#26254=CARTESIAN_POINT ( 'NONE',  ( 11.99500145082170022, 34.02547674131670163, -16.88883237367399914 ) ) ;
#26256=CARTESIAN_POINT ( 'NONE',  ( 53.42190059089289633, 18.11830158836169957, -48.77466594534000421 ) ) ;
#26257=EDGE_CURVE ( 'NONE', #22762, #33088, #9452, .T. ) ;
#26259=CARTESIAN_POINT ( 'NONE',  ( 57.81792062896100504, -47.19274128029930182, -48.15693251440850275 ) ) ;
#26260=CARTESIAN_POINT ( 'NONE',  ( 56.48924519203420402, 14.93416829053070138, -26.24160504693750084 ) ) ;
#26262=DIRECTION ( 'NONE',  ( -0.2517544074889990768, 0.9677911542837447367, 0.000000000000000000 ) ) ;
#26263=CARTESIAN_POINT ( 'NONE',  ( 12.30205595647329986, -64.73832649162540065, -15.96528926833489948 ) ) ;
#26265=CARTESIAN_POINT ( 'NONE',  ( 19.78696991733798427, 23.18878466699404939, -17.61868324447104328 ) ) ;
#26266=CARTESIAN_POINT ( 'NONE',  ( 10.77308341670910075, 32.08904557254610523, -45.20552704545990252 ) ) ;
#26268=CARTESIAN_POINT ( 'NONE',  ( 67.45418707017489623, -32.84195721915489941, -19.55846886189739919 ) ) ;
#26269=ORIENTED_EDGE ( 'NONE', *, *, #17049, .F. ) ;
#26270=CARTESIAN_POINT ( 'NONE',  ( 18.84530413485449785, 20.48963383789619996, -74.34036667011370980 ) ) ;
#26275=CARTESIAN_POINT ( 'NONE',  ( 76.60792998803806597, 2.469312492038889140, -13.69250461759032866 ) ) ;
#26277=CARTESIAN_POINT ( 'NONE',  ( 11.98107198743070079, -65.17237640307759250, -46.15866685343029729 ) ) ;
#26278=CARTESIAN_POINT ( 'NONE',  ( 57.57641373505710192, -45.19636825784430556, -25.75112877952900092 ) ) ;
#26279=DIRECTION ( 'NONE',  ( -1.000000000000000000, 0.000000000000000000, 0.000000000000000000 ) ) ;
#26281=ORIENTED_EDGE ( 'NONE', *, *, #22407, .T. ) ;
#26282=CARTESIAN_POINT ( 'NONE',  ( 11.65850508138839992, 34.15500248326146959, -22.48931345404534099 ) ) ;
#26286=CARTESIAN_POINT ( 'NONE',  ( 54.01992009194989919, -45.20950787019129535, -14.10456388246860016 ) ) ;
#26287=CARTESIAN_POINT ( 'NONE',  ( 51.94632098643839413, 1.634516250066370135, -19.08862713762362517 ) ) ;
#26288=AXIS2_PLACEMENT_3D ( 'NONE', #46931, #51364, #3154 ) ;
#26289=CARTESIAN_POINT ( 'NONE',  ( 16.50882131665489894, 19.88028741127540044, -20.29200666522829977 ) ) ;
#26290=CARTESIAN_POINT ( 'NONE',  ( 52.68908936341578908, 18.51792035577400242, -28.15000000000000213 ) ) ;
#26293=CARTESIAN_POINT ( 'NONE',  ( 47.11902681095349976, -54.23932985581029698, -75.46775895608709561 ) ) ;
#26294=CARTESIAN_POINT ( 'NONE',  ( 45.32018539748889907, 12.59810024214380064, -5.468941159389729911 ) ) ;
#26296=CARTESIAN_POINT ( 'NONE',  ( 50.95179065742699720, 19.71850122818939965, -76.14999999969789712 ) ) ;
#26297=CARTESIAN_POINT ( 'NONE',  ( 58.76638950021190055, 13.88377925009550040, -25.68003433735720265 ) ) ;
#26300=CARTESIAN_POINT ( 'NONE',  ( 50.15542239739440333, 21.61238791475396326, -53.37026996103012522 ) ) ;
#26301=AXIS2_PLACEMENT_3D ( 'NONE', #33108, #45708, #45188 ) ;
#26302=CARTESIAN_POINT ( 'NONE',  ( 7.077899642728071150, -59.90137670018390281, -12.08739966597480020 ) ) ;
#26307=CARTESIAN_POINT ( 'NONE',  ( 7.492845759203720313, 29.94784237631284896, -20.13893727953968948 ) ) ;
#26308=CARTESIAN_POINT ( 'NONE',  ( 82.27845038698740154, -45.17869114109299744, -46.87713570531570184 ) ) ;
#26309=DIRECTION ( 'NONE',  ( 0.000000000000000000, 0.000000000000000000, -1.000000000000000000 ) ) ;
#26310=CARTESIAN_POINT ( 'NONE',  ( 42.53933707111890783, 12.02846082064439948, -4.182107870958490459 ) ) ;
#26313=CARTESIAN_POINT ( 'NONE',  ( 57.79494562534669200, 17.81506593150905360, -51.23192195986732855 ) ) ;
#26320=ORIENTED_EDGE ( 'NONE', *, *, #15491, .F. ) ;
#26325=CARTESIAN_POINT ( 'NONE',  ( 57.50723796702470025, 13.88381105532070059, -17.93019253464870033 ) ) ;
#26330=FACE_OUTER_BOUND ( 'NONE', #33841, .T. ) ;
#26340=VERTEX_POINT ( 'NONE', #7912 ) ;
#26342=CARTESIAN_POINT ( 'NONE',  ( 51.82948403312330754, -50.48701590866159705, -76.37482631807910138 ) ) ;
#26343=CARTESIAN_POINT ( 'NONE',  ( 60.65208747370029840, 14.36635548808680163, -47.38958427977119925 ) ) ;
#26346=FACE_OUTER_BOUND ( 'NONE', #40268, .T. ) ;
#26348=CARTESIAN_POINT ( 'NONE',  ( 41.80294712679280167, -43.87265997789249639, -4.284453813682689294 ) ) ;
#26349=CARTESIAN_POINT ( 'NONE',  ( 74.93037156228848517, -45.11618894467250129, -15.31097063366330069 ) ) ;
#26350=CARTESIAN_POINT ( 'NONE',  ( 56.52818367932749766, 14.13713193161779991, -25.29323032974989971 ) ) ;
#26354=VERTEX_POINT ( 'NONE', #19946 ) ;
#26356=CARTESIAN_POINT ( 'NONE',  ( 57.55751162087899786, 19.38381105532060289, -53.92796738110899923 ) ) ;
#26361=CARTESIAN_POINT ( 'NONE',  ( 47.82833025861889809, -54.39460764734859310, -54.73692062665020330 ) ) ;
#26365=CARTESIAN_POINT ( 'NONE',  ( 41.53147733619440629, 13.48015055873413992, -5.331435673538858389 ) ) ;
#26366=ADVANCED_FACE ( 'NONE', ( #11858 ), #7663, .F. ) ;
#26367=CARTESIAN_POINT ( 'NONE',  ( 47.92670010532269487, 23.13728742016890294, -54.84775024399120014 ) ) ;
#26368=VERTEX_POINT ( 'NONE', #28062 ) ;
#26372=CARTESIAN_POINT ( 'NONE',  ( 60.34379258661509482, -45.86802437805019395, -47.72732609191810127 ) ) ;
#26376=CARTESIAN_POINT ( 'NONE',  ( 55.64728501505769742, 15.02354991311229959, -25.47826257345920098 ) ) ;
#26381=B_SPLINE_SURFACE_WITH_KNOTS ( 'NONE', 1, 3, ( 
 ( #32195, #27773, #7873, #48736, #4443, #12841, #24589, #23565, #28798, #47965, #44026, #24074, #39581, #40093, #3687, #8382 ),
 ( #35649, #24332, #40600, #40348, #4186, #505, #51635, #20162, #16494, #36153, #48215, #32446, #48473, #12574, #28537, #8637 ) ),
 .UNSPECIFIED., .F., .F., .F.,
 ( 2, 2 ),
 ( 4, 2, 2, 2, 2, 2, 2, 4 ),
 ( 0.1258684489467890022, 0.9339464778236650222 ),
 ( -9.143185466370150394, -8.666071118672251217, -5.863520046276620157, -3.060968973880999755, -0.2584179014853750234, 2.544133170910249930, 5.346684243305870332, 5.524684653693860525 ),
 .UNSPECIFIED. ) ;
#26384=ORIENTED_EDGE ( 'NONE', *, *, #12738, .T. ) ;
#26385=ORIENTED_EDGE ( 'NONE', *, *, #4717, .T. ) ;
#26386=CARTESIAN_POINT ( 'NONE',  ( 12.17681940037459931, -64.87407314697640004, -16.15032133963409677 ) ) ;
#26389=DIRECTION ( 'NONE',  ( 0.000000000000000000, 0.000000000000000000, -1.000000000000000000 ) ) ;
#26390=CIRCLE ( 'NONE', #27264, 1.999999999999996669 ) ;
#26391=VERTEX_POINT ( 'NONE', #8169 ) ;
#26395=CARTESIAN_POINT ( 'NONE',  ( 52.57474326386780206, -49.85166559037340761, -48.47378032971909789 ) ) ;
#26396=CARTESIAN_POINT ( 'NONE',  ( 52.79235666617839939, 18.38620345821869861, -48.27343973962159396 ) ) ;
#26397=CARTESIAN_POINT ( 'NONE',  ( 59.22263297176129981, -2.907530923697950076, -15.66492698287460072 ) ) ;
#26398=CARTESIAN_POINT ( 'NONE',  ( 51.09074886990410391, -48.81936691653330485, -76.44262319005039785 ) ) ;
#26399=CARTESIAN_POINT ( 'NONE',  ( 57.78985979110940008, -48.99901549808799928, -51.17840550953660284 ) ) ;
#26400=( BOUNDED_CURVE ( )  B_SPLINE_CURVE ( 3, ( #23590, #47482, #19929, #27799 ),
 .UNSPECIFIED., .F., .T. ) 
 B_SPLINE_CURVE_WITH_KNOTS ( ( 4, 4 ),
 ( 1.570796326794895004, 2.169041209213995014 ),
 .UNSPECIFIED. ) 
 CURVE ( )  GEOMETRIC_REPRESENTATION_ITEM ( )  RATIONAL_B_SPLINE_CURVE ( ( 1.000000000000000000, 0.9703969717270899409, 0.9703969717270899409, 1.000000000000000000 ) ) 
 REPRESENTATION_ITEM ( '' )  );
#26403=CARTESIAN_POINT ( 'NONE',  ( 68.13393739769769297, 18.72622661238300168, -73.39853292320978539 ) ) ;
#26405=CARTESIAN_POINT ( 'NONE',  ( 16.13393739769620083, -15.61618894467929941, -15.65000000000000036 ) ) ;
#26406=CARTESIAN_POINT ( 'NONE',  ( 55.20159258013029557, -48.56083622538359634, -48.75785604020860120 ) ) ;
#26408=CIRCLE ( 'NONE', #48201, 20.00000000000001421 ) ;
#26409=CARTESIAN_POINT ( 'NONE',  ( 14.13534289311499847, -51.11424938965239306, -22.31792951338179876 ) ) ;
#26410=CARTESIAN_POINT ( 'NONE',  ( 54.95426265229980345, 19.54999294923799980, -75.77179759279050586 ) ) ;
#26413=CARTESIAN_POINT ( 'NONE',  ( 47.57068389873440140, -54.44477986132550029, -74.81178025453719727 ) ) ;
#26414=CARTESIAN_POINT ( 'NONE',  ( 56.96608301822320186, 13.88381105532070059, -16.09650052231710404 ) ) ;
#26415=CARTESIAN_POINT ( 'NONE',  ( -11.32734370190460105, -41.88171845330919751, -6.430192534648659475 ) ) ;
#26420=EDGE_CURVE ( 'NONE', #49388, #41237, #21056, .T. ) ;
#26422=CARTESIAN_POINT ( 'NONE',  ( 47.39163994235539690, 23.01787381642170160, -75.29714945969119810 ) ) ;
#26426=CARTESIAN_POINT ( 'NONE',  ( 12.04795396861086942, -65.20652679592811296, -23.72527635874608265 ) ) ;
#26428=CIRCLE ( 'NONE', #37334, 2.000000000000000000 ) ;
#26430=CARTESIAN_POINT ( 'NONE',  ( 82.25188034893719191, 13.88444637376409929, -46.44925509022990440 ) ) ;
#26432=CARTESIAN_POINT ( 'NONE',  ( 52.26504646883520167, 18.55116755685089913, -77.19463087837650050 ) ) ;
#26437=CARTESIAN_POINT ( 'NONE',  ( -0.1608700869847050074, 30.41078316111070023, -48.65898601561190162 ) ) ;
#26438=ORIENTED_EDGE ( 'NONE', *, *, #26257, .T. ) ;
#26439=CARTESIAN_POINT ( 'NONE',  ( 53.05831035746550128, -49.54894111999600170, -48.91556382526960078 ) ) ;
#26440=VERTEX_POINT ( 'NONE', #300 ) ;
#26442=CIRCLE ( 'NONE', #10584, 20.00000000000001421 ) ;
#26444=CARTESIAN_POINT ( 'NONE',  ( 14.01810477701600099, 19.82185230895960260, -22.03884457292680210 ) ) ;
#26445=CARTESIAN_POINT ( 'NONE',  ( 57.04818975476379705, 14.01160997093949945, -25.71237456541479816 ) ) ;
#26447=CARTESIAN_POINT ( 'NONE',  ( 50.93003901630650176, 19.69401506034679983, -76.14999999999999147 ) ) ;
#26448=CARTESIAN_POINT ( 'NONE',  ( 53.48932715621429423, 18.18157440465409991, -49.16886947772060523 ) ) ;
#26449=CARTESIAN_POINT ( 'NONE',  ( 55.43335310247359615, -45.81514513605549865, -16.33642346105520105 ) ) ;
#26450=CARTESIAN_POINT ( 'NONE',  ( 16.15069188244332210, 19.81939201856824795, -15.66900176635303232 ) ) ;
#26454=CARTESIAN_POINT ( 'NONE',  ( 11.63826667102989987, -65.39198021057481469, -17.83149736357540149 ) ) ;
#26457=CARTESIAN_POINT ( 'NONE',  ( 10.98409431994489971, -65.15011576587480135, -18.15364188641290255 ) ) ;
#26459=CARTESIAN_POINT ( 'NONE',  ( 47.64143405400680109, 23.30250925609140111, -74.14999999999999147 ) ) ;
#26466=CARTESIAN_POINT ( 'NONE',  ( 10.48815925059109944, -63.18736884412081167, -45.62666951642670199 ) ) ;
#26470=CARTESIAN_POINT ( 'NONE',  ( 56.96867952315420069, 19.24372813523060088, -53.05103816797900151 ) ) ;
#26471=CARTESIAN_POINT ( 'NONE',  ( 52.91674791423729829, 19.03363345784520178, -77.24667101748759990 ) ) ;
#26472=EDGE_LOOP ( 'NONE', ( #28146, #26936, #15213 ) ) ;
#26473=FACE_OUTER_BOUND ( 'NONE', #4164, .T. ) ;
#26476=CARTESIAN_POINT ( 'NONE',  ( 14.92425238142254784, 21.51730928977700685, -76.12465453342672106 ) ) ;
#26479=CIRCLE ( 'NONE', #24778, 18.00000000000000355 ) ;
#26480=CARTESIAN_POINT ( 'NONE',  ( 16.13393739769620083, -15.61618894467929941, 6.349999999999999645 ) ) ;
#26482=ORIENTED_EDGE ( 'NONE', *, *, #24210, .F. ) ;
#26485=CARTESIAN_POINT ( 'NONE',  ( 53.12218299100999985, -49.57312743958999590, -49.13784299743709738 ) ) ;
#26486=AXIS2_PLACEMENT_3D ( 'NONE', #50120, #49869, #1905 ) ;
#26488=ADVANCED_FACE ( 'NONE', ( #20453 ), #21773, .T. ) ;
#26490=CARTESIAN_POINT ( 'NONE',  ( 13.76640160517550093, 20.38774172224130155, -75.08736963500949457 ) ) ;
#26492=CARTESIAN_POINT ( 'NONE',  ( 41.24359221735250003, -44.95166412314729598, -5.592253627833279950 ) ) ;
#26493=CARTESIAN_POINT ( 'NONE',  ( 54.47259832750690123, 15.01994964729280113, -15.76422791930239953 ) ) ;
#26495=ORIENTED_EDGE ( 'NONE', *, *, #28410, .F. ) ;
#26496=CARTESIAN_POINT ( 'NONE',  ( 52.72378859808819840, -49.69239786187580421, -27.46381703610870062 ) ) ;
#26498=CARTESIAN_POINT ( 'NONE',  ( 54.11678715959330077, -50.95118505024800015, -75.83232676159579455 ) ) ;
#26499=CARTESIAN_POINT ( 'NONE',  ( 9.593021974030840227, 30.53981953105449776, -13.35990672362370013 ) ) ;
#26501=CARTESIAN_POINT ( 'NONE',  ( 15.05440318628110141, 21.88381105532300097, -76.14999999999999147 ) ) ;
#26502=DIRECTION ( 'NONE',  ( -1.000000000000000000, 0.000000000000000000, 0.000000000000000000 ) ) ;
#26505=CARTESIAN_POINT ( 'NONE',  ( 47.52205594386720122, 23.34398621139530050, -54.75138854905920027 ) ) ;
#26506=AXIS2_PLACEMENT_3D ( 'NONE', #2679, #38584, #6095 ) ;
#26510=CARTESIAN_POINT ( 'NONE',  ( 11.70612132434609975, 33.78984264953350447, -16.54010580622759718 ) ) ;
#26511=CARTESIAN_POINT ( 'NONE',  ( 51.81004865379589575, 18.07991840855869725, -76.98867843095119667 ) ) ;
#26512=CARTESIAN_POINT ( 'NONE',  ( 52.83783336071989822, 18.42431077469710132, -48.61329614525410392 ) ) ;
#26513=CARTESIAN_POINT ( 'NONE',  ( 69.63393739769620083, 11.88381105532070059, -71.50000000000000000 ) ) ;
#26514=CARTESIAN_POINT ( 'NONE',  ( 57.34991680843397432, -50.61618894467929408, -53.92361874565386159 ) ) ;
#26515=CARTESIAN_POINT ( 'NONE',  ( 54.99095794367999446, 16.49186176109470026, -26.61809928030959682 ) ) ;
#26517=CARTESIAN_POINT ( 'NONE',  ( 11.13393739769619906, -63.50859000450320480, -43.92731420739779225 ) ) ;
#26519=CARTESIAN_POINT ( 'NONE',  ( 46.62909198040490111, -45.11618894467940066, -7.723523852232909270 ) ) ;
#26521=CARTESIAN_POINT ( 'NONE',  ( 10.97902921384109831, 32.05945366115350481, -44.74278564644669842 ) ) ;
#26524=ADVANCED_FACE ( 'NONE', ( #20503 ), #37261, .T. ) ;
#26525=FACE_OUTER_BOUND ( 'NONE', #25482, .T. ) ;
#26526=CARTESIAN_POINT ( 'NONE',  ( 12.72276870064157883, 24.23809552752231866, -75.55236793428871067 ) ) ;
#26530=CARTESIAN_POINT ( 'NONE',  ( -1.266062602478600141, -15.61618894541809865, -10.44999999990159623 ) ) ;
#26531=CARTESIAN_POINT ( 'NONE',  ( 49.34719147343828638, -2.352134976191016857, -15.70858444975636559 ) ) ;
#26532=EDGE_LOOP ( 'NONE', ( #40785, #37949, #49647, #34851 ) ) ;
#26533=CARTESIAN_POINT ( 'NONE',  ( 11.80055863122290027, -65.03891413853099834, -45.85802714334909780 ) ) ;
#26534=CARTESIAN_POINT ( 'NONE',  ( 56.53807458594769741, -45.58081011514489944, -25.88778928241779909 ) ) ;
#26535=DIRECTION ( 'NONE',  ( 0.9316796806450557966, 0.000000000000000000, 0.3632808454531109565 ) ) ;
#26537=DIRECTION ( 'NONE',  ( 9.341879000000000579E-17, -6.787273000000000785E-17, 1.000000000000000000 ) ) ;
#26539=CARTESIAN_POINT ( 'NONE',  ( 59.52869175205803032, 14.25746298374641441, -26.73578769780420572 ) ) ;
#26541=CARTESIAN_POINT ( 'NONE',  ( 12.18056949873179917, 33.83315300093070022, -24.20126506825790003 ) ) ;
#26543=CARTESIAN_POINT ( 'NONE',  ( 53.28808755247190021, -45.11618894467940066, -12.64220374931200119 ) ) ;
#26545=CARTESIAN_POINT ( 'NONE',  ( 16.33846296857170088, 19.88381105367919943, -21.13414048024790048 ) ) ;
#26546=CARTESIAN_POINT ( 'NONE',  ( 0.000000000000000000, 0.000000000000000000, 0.000000000000000000 ) ) ;
#26549=CARTESIAN_POINT ( 'NONE',  ( 47.36711723512720340, -54.66958679686550227, -74.36142533359220863 ) ) ;
#26550=CARTESIAN_POINT ( 'NONE',  ( 64.61729235537799809, 13.73161753659590012, -11.40814173470289994 ) ) ;
#26552=CARTESIAN_POINT ( 'NONE',  ( 68.13393739769620083, -38.11618894467930119, -73.25000000000000000 ) ) ;
#26553=B_SPLINE_SURFACE_WITH_KNOTS ( 'NONE', 3, 3, ( 
 ( #38068, #10290, #46205, #25468, #38324, #41473 ),
 ( #5589, #49617, #1645, #25726, #17635, #33603 ),
 ( #13710, #29664, #45672, #41734, #5839, #21804 ),
 ( #37811, #17884, #23596, #7390, #7137, #19936 ),
 ( #11846, #7901, #6881, #26768, #47235, #43041 ),
 ( #16019, #34895, #11326, #23089, #47739, #11584 ),
 ( #47488, #51159, #27545, #15253, #43299, #27036 ),
 ( #31206, #35926, #51667, #39108, #42784, #18912 ),
 ( #27290, #39871, #2941, #43, #10809, #30953 ),
 ( #43551, #3971, #50895, #46725, #3201, #51415 ),
 ( #46984, #38852, #19689, #3463, #22831, #14987 ) ),
 .UNSPECIFIED., .F., .F., .F.,
 ( 4, 1, 1, 1, 1, 1, 1, 1, 4 ),
 ( 4, 2, 4 ),
 ( 0.000000000000000000, 0.1250000000000000000, 0.2500000000000000000, 0.3750000000000000000, 0.5000000000000000000, 0.6250000000000000000, 0.7500000000000000000, 0.8750000000000000000, 1.000001242265009971 ),
 ( 0.5133021419581690337, 0.6217601802413029732, 0.8336663735762139815 ),
 .UNSPECIFIED. ) ;
#26556=CARTESIAN_POINT ( 'NONE',  ( 11.63826681150182374, 34.15960232215161341, -17.83149674234766380 ) ) ;
#26559=CARTESIAN_POINT ( 'NONE',  ( 52.92565939194879832, 18.90186872980919830, -50.10275203585430148 ) ) ;
#26560=CARTESIAN_POINT ( 'NONE',  ( 8.120607361937230095, -62.21505069536980415, -15.66636916474939767 ) ) ;
#26561=CARTESIAN_POINT ( 'NONE',  ( 75.47375904900299304, -35.00320737813580507, -12.36911740208540067 ) ) ;
#26564=DIRECTION ( 'NONE',  ( 1.000000000000000000, 0.000000000000000000, 0.000000000000000000 ) ) ;
#26566=CARTESIAN_POINT ( 'NONE',  ( 82.64666749252569389, -45.32231744321139644, -47.29311289609230329 ) ) ;
#26567=CARTESIAN_POINT ( 'NONE',  ( 12.76333982178410054, 19.08640070912930042, -21.19734824621640001 ) ) ;
#26568=CARTESIAN_POINT ( 'NONE',  ( 14.12259461928470117, 19.90775691817940185, -22.75706044212220291 ) ) ;
#26569=CARTESIAN_POINT ( 'NONE',  ( 41.30230023304270048, 12.85426430236040041, -3.681965864469090022 ) ) ;
#26570=DIRECTION ( 'NONE',  ( -1.000000000000000000, 0.000000000000000000, 0.000000000000000000 ) ) ;
#26572=CARTESIAN_POINT ( 'NONE',  ( 70.03247032090770574, -49.95860450174168221, -71.35146707679193412 ) ) ;
#26573=CARTESIAN_POINT ( 'NONE',  ( 75.55177307622278704, -43.36778670056347806, -13.42519430266176528 ) ) ;
#26574=CARTESIAN_POINT ( 'NONE',  ( 17.93421870997589807, -52.10138505899109873, -75.81674732426940011 ) ) ;
#26575=CARTESIAN_POINT ( 'NONE',  ( 58.41816864604760440, -45.11618894467940066, -10.37988043371890079 ) ) ;
#26576=EDGE_LOOP ( 'NONE', ( #4293, #45931, #21626, #22400, #4266, #35385 ) ) ;
#26579=ORIENTED_EDGE ( 'NONE', *, *, #19502, .T. ) ;
#26581=CARTESIAN_POINT ( 'NONE',  ( 61.14444386409360277, -45.63613486214899950, -47.70810082891859594 ) ) ;
#26588=ORIENTED_EDGE ( 'NONE', *, *, #2060, .F. ) ;
#26590=CARTESIAN_POINT ( 'NONE',  ( 55.94726098010619353, -45.11618894467940066, -14.63509752318040036 ) ) ;
#26591=CARTESIAN_POINT ( 'NONE',  ( 61.32820939606469324, -45.23504818669070460, -46.87279288174590164 ) ) ;
#26595=AXIS2_PLACEMENT_3D ( 'NONE', #43643, #50980, #39705 ) ;
#26599=CONICAL_SURFACE ( 'NONE', #4022, 55.50000000000000711, 1.262743545771120246 ) ;
#26603=CARTESIAN_POINT ( 'NONE',  ( 52.36927103260880045, -51.34176544043950230, -75.93037472320008874 ) ) ;
#26604=CARTESIAN_POINT ( 'NONE',  ( 60.82331437658589834, 14.26027801509150095, -47.24344971340510568 ) ) ;
#26605=EDGE_CURVE ( 'NONE', #34084, #7703, #5996, .T. ) ;
#26607=B_SPLINE_CURVE_WITH_KNOTS ( 'NONE', 3,
 ( #7075, #43485, #23025, #27743, #7589, #19627, #23535, #14666, #43236, #39047, #46917, #34832, #3141, #19109, #43741, #35086, #51351, #50833 ),
 .UNSPECIFIED., .F., .F.,
 ( 4, 2, 2, 2, 2, 2, 2, 2, 4 ),
 ( 0.000000000000000000, 0.4467108845949059881, 0.9572376098462268557, 1.276316813128300032, 1.435856414769340006, 1.633224234453040324, 1.949012745946970160, 2.454274364337259762, 2.552633626256600063 ),
 .UNSPECIFIED. ) ;
#26609=CARTESIAN_POINT ( 'NONE',  ( 41.82061695157300818, -44.02105789449079509, -4.552229691682260437 ) ) ;
#26611=CARTESIAN_POINT ( 'NONE',  ( 65.24498226310142002, 0.1269486509447112499, -16.97693471835480850 ) ) ;
#26612=CARTESIAN_POINT ( 'NONE',  ( 56.61789568001263007, 14.09242255766770491, -25.29355634365396099 ) ) ;
#26615=FACE_OUTER_BOUND ( 'NONE', #30642, .T. ) ;
#26618=CARTESIAN_POINT ( 'NONE',  ( 14.63048442081539946, -52.51931604725010061, -76.04695140691811162 ) ) ;
#26619=CARTESIAN_POINT ( 'NONE',  ( 57.55751162087899786, 19.06184008987549916, -52.83558909271580006 ) ) ;
#26622=CARTESIAN_POINT ( 'NONE',  ( 41.23393739769619515, -15.61618894467929408, 4.450000000000000178 ) ) ;
#26624=CARTESIAN_POINT ( 'NONE',  ( 47.03253577542010078, -54.46635581206609800, -75.29851419728690587 ) ) ;
#26626=CARTESIAN_POINT ( 'NONE',  ( 47.82811749538019797, -54.43775025877560836, -54.96145351061949924 ) ) ;
#26628=CARTESIAN_POINT ( 'NONE',  ( -9.553724527077868345, -43.62474080932184251, -5.594726726022510199 ) ) ;
#26629=CARTESIAN_POINT ( 'NONE',  ( 48.26465138126300758, 22.99219893776650281, -54.90320022043339776 ) ) ;
#26630=ORIENTED_EDGE ( 'NONE', *, *, #46935, .F. ) ;
#26635=CARTESIAN_POINT ( 'NONE',  ( 83.49396093841654931, 14.01989379893576881, -47.52772051671507114 ) ) ;
#26641=VERTEX_POINT ( 'NONE', #44554 ) ;
#26642=CARTESIAN_POINT ( 'NONE',  ( 51.67587649748470113, -33.96749857170579645, -77.01363636363508647 ) ) ;
#26643=VERTEX_POINT ( 'NONE', #44813 ) ;
#26646=CARTESIAN_POINT ( 'NONE',  ( 12.19720189295309964, -64.69332835163750417, -15.92873818751279913 ) ) ;
#26647=CARTESIAN_POINT ( 'NONE',  ( 56.39253198848358295, 14.87044060624309871, -26.18964637225387193 ) ) ;
#26648=CARTESIAN_POINT ( 'NONE',  ( 76.47316685153059268, -26.61964061097626555, -13.11179020515832150 ) ) ;
#26649=CARTESIAN_POINT ( 'NONE',  ( 9.013808781100760115, -63.78940033112238694, -46.72196778451930044 ) ) ;
#26651=B_SPLINE_CURVE_WITH_KNOTS ( 'NONE', 3,
 ( #19306, #3329, #35288, #51286, #11714, #22959 ),
 .UNSPECIFIED., .F., .F.,
 ( 4, 2, 4 ),
 ( 0.000000000000000000, 0.3218804212953693678, 0.6437608425907387355 ),
 .UNSPECIFIED. ) ;
#26654=CARTESIAN_POINT ( 'NONE',  ( 83.89200044194980421, -48.61618894467930119, -53.92796738110899923 ) ) ;
#26655=CARTESIAN_POINT ( 'NONE',  ( 48.94415371571059836, 22.39326048681330050, -54.05322516865759752 ) ) ;
#26656=CARTESIAN_POINT ( 'NONE',  ( 61.45969919439730234, -1.272705315759670164, -16.07655046430879864 ) ) ;
#26657=CARTESIAN_POINT ( 'NONE',  ( 51.61772101699829562, -50.35897448521090070, -76.35065455175050886 ) ) ;
#26658=CARTESIAN_POINT ( 'NONE',  ( 60.85130813898859969, -45.50269846729229783, -47.46988763436880276 ) ) ;
#26659=ORIENTED_EDGE ( 'NONE', *, *, #32784, .T. ) ;
#26661=CARTESIAN_POINT ( 'NONE',  ( 76.87859648677320479, 11.88381402801379849, -14.85884684523960075 ) ) ;
#26663=PLANE ( 'NONE',  #51124 ) ;
#26664=CIRCLE ( 'NONE', #30854, 50.00000000000000000 ) ;
#26665=CARTESIAN_POINT ( 'NONE',  ( 50.44516630505179933, -45.11618894467940066, -10.60027150234669868 ) ) ;
#26666=CIRCLE ( 'NONE', #16644, 39.39359268544610870 ) ;
#26668=CARTESIAN_POINT ( 'NONE',  ( 13.20471009389370032, -50.60438166373199920, -21.36609921343159968 ) ) ;
#26670=CARTESIAN_POINT ( 'NONE',  ( 47.02070054993090054, -53.74782267376620126, -75.86501933388160523 ) ) ;
#26671=CARTESIAN_POINT ( 'NONE',  ( 56.40060982945949775, 13.95655126064509943, -16.03711971019910010 ) ) ;
#26673=CARTESIAN_POINT ( 'NONE',  ( 56.76664445295860872, -50.67471734267469685, -53.84360320749780016 ) ) ;
#26677=CARTESIAN_POINT ( 'NONE',  ( 46.51664131682890257, 21.89886130434609868, -76.13722091169989881 ) ) ;
#26679=CARTESIAN_POINT ( 'NONE',  ( 44.88827463677240104, -46.10881073926530149, -8.898903786617220035 ) ) ;
#26681=CARTESIAN_POINT ( 'NONE',  ( 49.34439669087809932, 13.88381105532070059, -8.366249983091170961 ) ) ;
#26682=VECTOR ( 'NONE', #27516, 1000.000000000000000 ) ;
#26684=CARTESIAN_POINT ( 'NONE',  ( 82.13853704237929776, 13.88381105532070059, -46.42699167578030028 ) ) ;
#26685=CARTESIAN_POINT ( 'NONE',  ( 11.19961559249191652, 34.01497085325235759, -46.39999999999999858 ) ) ;
#26686=CARTESIAN_POINT ( 'NONE',  ( 47.62448409337466160, 23.28090871689746422, -74.50417146696477744 ) ) ;
#26691=CARTESIAN_POINT ( 'NONE',  ( 13.04555273158369921, 34.28832529259570094, -47.48197110827519651 ) ) ;
#26693=CARTESIAN_POINT ( 'NONE',  ( 53.46953806474559201, -49.34555379450520718, -48.93764703832670193 ) ) ;
#26698=CARTESIAN_POINT ( 'NONE',  ( 13.99298669291740183, 19.94627925521579925, -22.74639520659370007 ) ) ;
#26701=TOROIDAL_SURFACE ( 'NONE', #4988, 48.00000000000000000, 2.000000000000000000 ) ;
#26702=LINE ( 'NONE', #39741, #9859 ) ;
#26703=CARTESIAN_POINT ( 'NONE',  ( 52.63212352556610085, 18.56439172932729775, -48.50958596172849724 ) ) ;
#26704=CARTESIAN_POINT ( 'NONE',  ( 55.05621579753230321, -46.03286285214759488, -16.12183698155410028 ) ) ;
#26705=DIRECTION ( 'NONE',  ( 0.000000000000000000, 1.000000000000000000, 0.000000000000000000 ) ) ;
#26707=EDGE_CURVE ( 'NONE', #15849, #3072, #35456, .T. ) ;
#26713=CARTESIAN_POINT ( 'NONE',  ( 10.99340395496080092, 33.76106700544529815, -46.99437235894899345 ) ) ;
#26715=( BOUNDED_CURVE ( )  B_SPLINE_CURVE ( 3, ( #22137, #38403, #1462, #10109 ),
 .UNSPECIFIED., .F., .T. ) 
 B_SPLINE_CURVE_WITH_KNOTS ( ( 4, 4 ),
 ( 2.299782947909850161, 2.699475143822985146 ),
 .UNSPECIFIED. ) 
 CURVE ( )  GEOMETRIC_REPRESENTATION_ITEM ( )  RATIONAL_B_SPLINE_CURVE ( ( 1.000000000000000000, 0.9867314279001654365, 0.9867314279001654365, 1.000000000000000000 ) ) 
 REPRESENTATION_ITEM ( '' )  );
#26716=CARTESIAN_POINT ( 'NONE',  ( 11.49998292431379987, -65.37168222854499788, -17.88621716038850096 ) ) ;
#26721=EDGE_CURVE ( 'NONE', #24734, #39182, #39077, .T. ) ;
#26725=CARTESIAN_POINT ( 'NONE',  ( 10.77036614487909993, -63.18183448256370127, -45.20525045113869567 ) ) ;
#26727=VERTEX_POINT ( 'NONE', #50308 ) ;
#26729=CARTESIAN_POINT ( 'NONE',  ( 57.03340744182619915, 19.08153169885300215, -52.79504028237870017 ) ) ;
#26730=CARTESIAN_POINT ( 'NONE',  ( 53.45776890000269788, 19.34146221496600049, -76.87859199860160686 ) ) ;
#26731=ORIENTED_EDGE ( 'NONE', *, *, #20425, .F. ) ;
#26743=CIRCLE ( 'NONE', #29245, 21.96784688337769964 ) ;
#26749=DIRECTION ( 'NONE',  ( 0.8857883891771956009, -0.4640893551880597712, 2.775557561562888578E-17 ) ) ;
#26753=CARTESIAN_POINT ( 'NONE',  ( 41.35843174423229840, -44.86402911857589970, -5.517451181412050154 ) ) ;
#26758=CARTESIAN_POINT ( 'NONE',  ( 54.73608448560249684, -51.07312271709760410, -75.36140526845879606 ) ) ;
#26759=CARTESIAN_POINT ( 'NONE',  ( -8.972852706257611999, 12.24880239228480150, -4.689908045945220039 ) ) ;
#26763=ORIENTED_EDGE ( 'NONE', *, *, #44610, .F. ) ;
#26764=LINE ( 'NONE', #27286, #18949 ) ;
#26765=CARTESIAN_POINT ( 'NONE',  ( 47.82244534609320397, 23.17065945679449968, -54.75726970773219904 ) ) ;
#26768=CARTESIAN_POINT ( 'NONE',  ( 61.00282475136230431, 14.19724498751740072, -47.27680998975259996 ) ) ;
#26769=CARTESIAN_POINT ( 'NONE',  ( 11.94527157685780061, 34.17980222613059738, -17.48520199522390328 ) ) ;
#26770=CARTESIAN_POINT ( 'NONE',  ( 51.50850416226409578, 17.38380873894399770, -76.79363219169579224 ) ) ;
#26771=CARTESIAN_POINT ( 'NONE',  ( 52.90228695499589406, 18.39054173078930177, -48.72753549895890046 ) ) ;
#26772=PLANE ( 'NONE',  #6651 ) ;
#26774=CARTESIAN_POINT ( 'NONE',  ( 54.23599842029290130, 17.14189944890559758, -26.83793738065240220 ) ) ;
#26775=CARTESIAN_POINT ( 'NONE',  ( 50.90601119115756745, 4.155396614399425204, -76.35101117172904139 ) ) ;
#26777=EDGE_CURVE ( 'NONE', #38024, #41237, #14650, .T. ) ;
#26778=CARTESIAN_POINT ( 'NONE',  ( 54.44538087470321130, -48.22925714520665252, -26.80321430961254947 ) ) ;
#26783=CARTESIAN_POINT ( 'NONE',  ( 10.49286768590240015, 32.07784613589559797, -45.62589547488590114 ) ) ;
#26787=CARTESIAN_POINT ( 'NONE',  ( 66.72606212556679850, -33.11598147586919794, -20.65075273511109799 ) ) ;
#26788=EDGE_CURVE ( 'NONE', #30697, #5671, #17554, .T. ) ;
#26789=B_SPLINE_CURVE_WITH_KNOTS ( 'NONE', 3,
 ( #35947, #27824, #3742, #20213, #39897, #36201, #35177, #7923, #19712, #43318, #15275, #35704, #19955, #12366, #28329, #31230, #47257, #8961 ),
 .UNSPECIFIED., .F., .F.,
 ( 4, 2, 2, 2, 1, 1, 1, 1, 2, 2, 4 ),
 ( 0.4288339318601827599, 0.5716254488951695301, 0.6430212074126628874, 0.6787190866714091220, 0.6965680263007817397, 0.7054924961154681595, 0.7099547310228111474, 0.7121858484764826969, 0.7133014072033192488, 0.7144169659301558006, 1.000000000000000000 ),
 .UNSPECIFIED. ) ;
#26793=CARTESIAN_POINT ( 'NONE',  ( 40.36721523010790236, 13.65407319109839790, -4.296538310233780855 ) ) ;
#26794=CARTESIAN_POINT ( 'NONE',  ( 76.49291921988624665, -3.342101280679246056, -13.19690610020979982 ) ) ;
#26796=CARTESIAN_POINT ( 'NONE',  ( 13.00893739769619906, -65.51843714052719747, -47.75434321273180416 ) ) ;
#26797=CARTESIAN_POINT ( 'NONE',  ( 56.99279156800540136, -45.19728653190040291, -25.51108452758600009 ) ) ;
#26801=ORIENTED_EDGE ( 'NONE', *, *, #25134, .T. ) ;
#26802=DIRECTION ( 'NONE',  ( -1.000000000000000000, 0.000000000000000000, 0.000000000000000000 ) ) ;
#26804=CARTESIAN_POINT ( 'NONE',  ( 41.58742287076989896, -44.81259267420119841, -5.496112453488630756 ) ) ;
#26807=CARTESIAN_POINT ( 'NONE',  ( 51.18332209997665672, 0.4329010285075667874, -17.12802215458399857 ) ) ;
#26808=CARTESIAN_POINT ( 'NONE',  ( 16.05644225717160012, 19.79911103497629909, -20.34167354763550151 ) ) ;
#26809=ADVANCED_FACE ( 'NONE', ( #2085 ), #6020, .T. ) ;
#26811=CARTESIAN_POINT ( 'NONE',  ( 61.02197387602029721, -29.53831944543249932, -15.95139295748569985 ) ) ;
#26813=CARTESIAN_POINT ( 'NONE',  ( 47.37032927764639822, -54.67515752274410090, -74.14999999999999147 ) ) ;
#26814=CARTESIAN_POINT ( 'NONE',  ( 58.22650904342010136, 12.52539876674930142, -8.667039378196390587 ) ) ;
#26815=CARTESIAN_POINT ( 'NONE',  ( 15.05440318628110141, 21.88381105532300097, -76.14999999999999147 ) ) ;
#26818=AXIS2_PLACEMENT_3D ( 'NONE', #46026, #2769, #14561 ) ;
#26820=EDGE_CURVE ( 'NONE', #16107, #45923, #31512, .T. ) ;
#26824=B_SPLINE_SURFACE_WITH_KNOTS ( 'NONE', 3, 3, ( 
 ( #46510, #2461, #50167, #21849, #1952, #38641, #6405, #18703, #10598, #33645, #14264, #42045, #26035, #34153, #49664, #49911, #29708, #26296 ),
 ( #2209, #6660, #18446, #2730, #14519, #6148, #38369, #30487, #42569, #13752, #17929, #33900, #14005, #45719, #9820, #22103, #18186, #25772 ),
 ( #10338, #38114, #50430, #30232, #41779, #5883, #45983, #42306, #10076, #46249, #22364, #34419, #8701, #12637, #24653, #45635, #45119, #13420 ),
 ( #17597, #36993, #25693, #21511, #29632, #823, #9227, #12904, #37509, #17344, #40923, #13670, #25435, #37256, #45382, #33820, #5553, #49584 ),
 ( #33310, #41437, #25180, #24910, #41696, #49323, #5296, #21247, #40664, #44596, #13172, #9733, #1608, #28595, #5803, #33568, #21764, #37775 ),
 ( #1353, #32770, #17847, #28859, #8966, #29380, #9487, #1868, #4763, #1089, #20733, #17088, #16824, #36720, #48795, #49064, #44862, #5033 ),
 ( #20996, #33040, #29121, #41186, #13925, #14692, #29880, #22794, #45900, #50349, #2126, #18619, #10772, #46685, #14177, #9987, #50857, #42748 ),
 ( #18106, #34073, #43004, #26730, #3164, #14950, #49833, #6577, #18354, #38289, #10514, #19134, #30146, #25949, #34597, #41966, #6062, #30661 ),
 ( #50602, #34332, #6845, #7103, #50082, #38815, #26998, #2906, #2379, #18875, #34858, #30914, #46944, #46167, #10254, #42487, #23052, #14434 ),
 ( #11030, #30404, #26212, #22020, #39073, #38032, #42222, #6322, #22279, #46427, #26471, #22540, #38551, #2650, #4438, #23299, #51629, #11546 ) ),
 .UNSPECIFIED., .F., .F., .F.,
 ( 4, 1, 1, 1, 1, 1, 1, 4 ),
 ( 4, 2, 2, 2, 2, 2, 2, 2, 4 ),
 ( 0.000000000000000000, 0.1428571428571430157, 0.2857142857142860315, 0.4285714285714289917, 0.5714285714285709528, 0.7142857142857139685, 0.8571428571428569843, 1.000073332888519850 ),
 ( -7.333288851099999919E-05, 0.9295627158857400207, 1.472201184288379983, 1.962934912384509900, 2.208301776432569863, 2.600888758909470244, 3.229027930872510055, 3.861273708119669745, 3.925943157657540095 ),
 .UNSPECIFIED. ) ;
#26825=EDGE_LOOP ( 'NONE', ( #7857, #19407, #13232, #33569, #19817, #956 ) ) ;
#26827=ADVANCED_FACE ( 'NONE', ( #18313 ), #34288, .F. ) ;
#26828=CARTESIAN_POINT ( 'NONE',  ( -6.023628976439000304, -47.42688974637729871, -6.961268883118139961 ) ) ;
#26829=CARTESIAN_POINT ( 'NONE',  ( 76.57120089795539286, -34.85044501265049632, -13.53274818732839968 ) ) ;
#26830=CARTESIAN_POINT ( 'NONE',  ( 75.01492932893468435, 13.86426277530698492, -15.01926194450931362 ) ) ;
#26831=LINE ( 'NONE', #50947, #41559 ) ;
#26832=CARTESIAN_POINT ( 'NONE',  ( 14.19855276898620033, -55.56934008872499930, -76.14999999999999147 ) ) ;
#26833=CARTESIAN_POINT ( 'NONE',  ( 39.13393739769620083, -15.61618894467929941, -14.65000000000000036 ) ) ;
#26834=CARTESIAN_POINT ( 'NONE',  ( 82.13853704237929776, -45.28162313823070662, -47.17417977903829751 ) ) ;
#26835=DIRECTION ( 'NONE',  ( 0.000000000000000000, 0.000000000000000000, 1.000000000000000000 ) ) ;
#26836=CARTESIAN_POINT ( 'NONE',  ( 41.35854804407180296, 12.82120953887990034, -3.852418314459289839 ) ) ;
#26837=CARTESIAN_POINT ( 'NONE',  ( 61.28398356449380202, -45.60471458446119897, -47.68178229846480320 ) ) ;
#26839=CARTESIAN_POINT ( 'NONE',  ( 67.04038824939736685, -50.70395984888217811, -72.15645085170115181 ) ) ;
#26840=CARTESIAN_POINT ( 'NONE',  ( 75.47966807050509885, -43.37310274687460065, -13.40512917118210012 ) ) ;
#26841=CARTESIAN_POINT ( 'NONE',  ( 18.12479075550290020, -52.38392585211880714, -75.82251062550821530 ) ) ;
#26842=CARTESIAN_POINT ( 'NONE',  ( 52.59140206479120394, -52.14549427466430842, -53.43195377655929690 ) ) ;
#26843=VERTEX_POINT ( 'NONE', #43468 ) ;
#26844=EDGE_CURVE ( 'NONE', #10891, #35613, #20628, .T. ) ;
#26848=CARTESIAN_POINT ( 'NONE',  ( -11.32734372065470119, 10.64934054434680100, -6.430561461456250072 ) ) ;
#26853=CARTESIAN_POINT ( 'NONE',  ( 43.99490479527259623, -45.81249226280370124, -8.084108929775279506 ) ) ;
#26858=CARTESIAN_POINT ( 'NONE',  ( 57.12835595156409596, -45.11618894467940066, -16.21298877816359862 ) ) ;
#26862=AXIS2_PLACEMENT_3D ( 'NONE', #29630, #9485, #17086 ) ;
#26863=ORIENTED_EDGE ( 'NONE', *, *, #9214, .F. ) ;
#26866=ORIENTED_EDGE ( 'NONE', *, *, #42442, .F. ) ;
#26871=CARTESIAN_POINT ( 'NONE',  ( 51.62918029574790069, -50.98197525970820010, -76.14997290400350494 ) ) ;
#26872=CARTESIAN_POINT ( 'NONE',  ( 60.51088772352670020, 14.40667547550430072, -47.25398757032650110 ) ) ;
#26875=CARTESIAN_POINT ( 'NONE',  ( 41.67695036363830496, -43.85159771036679643, -4.028589966754839047 ) ) ;
#26876=CARTESIAN_POINT ( 'NONE',  ( 65.03603135454920903, 1.015437840524759938, -17.83403478221330118 ) ) ;
#26877=CARTESIAN_POINT ( 'NONE',  ( -5.339665001452960524, 15.83869399000049860, -5.053056987543070200 ) ) ;
#26880=CARTESIAN_POINT ( 'NONE',  ( 17.74855170510530300, -51.60941532113833574, -75.47165350121125016 ) ) ;
#26882=ORIENTED_EDGE ( 'NONE', *, *, #46527, .T. ) ;
#26885=CARTESIAN_POINT ( 'NONE',  ( 43.24982176573970349, 14.76832211732570244, -7.760834293533140027 ) ) ;
#26887=EDGE_CURVE ( 'NONE', #39996, #32099, #12271, .T. ) ;
#26889=CARTESIAN_POINT ( 'NONE',  ( 14.18385191393459976, 19.60157099775030076, -21.44137102719379939 ) ) ;
#26893=VECTOR ( 'NONE', #51688, 1000.000000000000114 ) ;
#26896=CARTESIAN_POINT ( 'NONE',  ( 48.08338613907370274, -54.27467684138100168, -54.77539264028180099 ) ) ;
#26897=CARTESIAN_POINT ( 'NONE',  ( 53.53273701459760048, 1.883811055320649963, -56.74709961107230782 ) ) ;
#26899=CARTESIAN_POINT ( 'NONE',  ( 47.73325073025490184, 23.25446252339419928, -54.99405306332750598 ) ) ;
#26902=VERTEX_POINT ( 'NONE', #46902 ) ;
#26905=CARTESIAN_POINT ( 'NONE',  ( 48.51115049231166410, -54.01384098269411282, -54.58190071400569110 ) ) ;
#26907=CARTESIAN_POINT ( 'NONE',  ( 84.09627682649329472, 13.28281544432810080, -47.44643906338429673 ) ) ;
#26909=LINE ( 'NONE', #43173, #43916 ) ;
#26913=VERTEX_POINT ( 'NONE', #3640 ) ;
#26917=CARTESIAN_POINT ( 'NONE',  ( 12.24959214048389811, -64.71630487127059439, -15.94651421640129740 ) ) ;
#26920=CARTESIAN_POINT ( 'NONE',  ( 9.002245833509869399, -63.28624783032829271, -46.62846273742899683 ) ) ;
#26928=CARTESIAN_POINT ( 'NONE',  ( 62.29142313821609633, -0.6939978288072199408, -16.33503342585539997 ) ) ;
#26929=CARTESIAN_POINT ( 'NONE',  ( 51.54546934694510441, -48.95615870297720562, -76.80150978122190963 ) ) ;
#26930=CARTESIAN_POINT ( 'NONE',  ( 59.09164618180179929, -48.27810260483980187, -50.59936035653869624 ) ) ;
#26936=ORIENTED_EDGE ( 'NONE', *, *, #29862, .F. ) ;
#26937=CARTESIAN_POINT ( 'NONE',  ( 17.92370450339619836, 19.88381105532299742, -76.14999999999999147 ) ) ;
#26940=CARTESIAN_POINT ( 'NONE',  ( 13.50717251036370037, -51.04402699075219374, -21.90150652010380128 ) ) ;
#26941=CARTESIAN_POINT ( 'NONE',  ( 57.24929532239860208, 19.38381105532069881, -74.14879648477479179 ) ) ;
#26943=CARTESIAN_POINT ( 'NONE',  ( 55.42167411747570327, 13.97341619388889988, -14.99504123111160148 ) ) ;
#26944=CARTESIAN_POINT ( 'NONE',  ( 61.07012975457860193, -45.36121598898729701, -47.07601971527900275 ) ) ;
#26945=CARTESIAN_POINT ( 'NONE',  ( 56.85513653747680252, -50.50737975057980123, -53.07093444070599730 ) ) ;
#26948=ORIENTED_EDGE ( 'NONE', *, *, #12013, .T. ) ;
#26949=CARTESIAN_POINT ( 'NONE',  ( 47.15730504846059290, 22.76836487247490126, -75.65554796064559184 ) ) ;
#26952=CARTESIAN_POINT ( 'NONE',  ( 47.64143405402000297, 23.30250925608569901, -55.14905519569659731 ) ) ;
#26955=CYLINDRICAL_SURFACE ( 'NONE', #30605, 1.999999999999995115 ) ;
#26956=CARTESIAN_POINT ( 'NONE',  ( 82.36129846001850296, 13.87672100883400006, -46.45437161147240346 ) ) ;
#26958=CARTESIAN_POINT ( 'NONE',  ( 52.91668457653215540, 19.03365523282223748, -77.24653539121042911 ) ) ;
#26961=CARTESIAN_POINT ( 'NONE',  ( 49.43322755553389669, 22.52438033512590110, -54.94234374367420060 ) ) ;
#26963=ORIENTED_EDGE ( 'NONE', *, *, #4174, .T. ) ;
#26965=CARTESIAN_POINT ( 'NONE',  ( 52.70437350293030221, -49.73931392293049925, -48.55297031683699771 ) ) ;
#26970=CARTESIAN_POINT ( 'NONE',  ( 13.85785670643420175, 19.97506034401209973, -22.56070333950139783 ) ) ;
#26973=CARTESIAN_POINT ( 'NONE',  ( 52.70623495221639843, 18.51481665853420111, -48.71311406155950152 ) ) ;
#26974=CARTESIAN_POINT ( 'NONE',  ( 56.26288285225719221, -45.53040306498559886, -17.58692621438209969 ) ) ;
#26976=DIRECTION ( 'NONE',  ( 0.000000000000000000, -1.000000000000000000, 0.000000000000000000 ) ) ;
#26977=VERTEX_POINT ( 'NONE', #45013 ) ;
#26983=CARTESIAN_POINT ( 'NONE',  ( 9.023714487127799444, 32.18236227648780101, -46.63240982052630557 ) ) ;
#26986=CARTESIAN_POINT ( 'NONE',  ( 53.52964967199919499, -49.40236756415160357, -49.18086210135690095 ) ) ;
#26987=CARTESIAN_POINT ( 'NONE',  ( 52.88388587306728539, -49.67261804826031835, -49.00306437247584768 ) ) ;
#26989=CARTESIAN_POINT ( 'NONE',  ( 50.33545347434720441, -53.26974486897529459, -54.25199063940150523 ) ) ;
#26991=CARTESIAN_POINT ( 'NONE',  ( 61.43314648866955707, 14.21603639159006427, -47.47826202051524547 ) ) ;
#26993=CARTESIAN_POINT ( 'NONE',  ( 10.48935662701619975, -63.21776614012360085, -45.62600156124040041 ) ) ;
#26994=CARTESIAN_POINT ( 'NONE',  ( 70.03247032090601465, 18.72622661238470343, -69.60146707679315625 ) ) ;
#26997=CARTESIAN_POINT ( 'NONE',  ( 57.34839258692319675, 19.00579764154129592, -52.73846305600119422 ) ) ;
#26998=CARTESIAN_POINT ( 'NONE',  ( 53.19378594384949821, 19.20558095012749789, -77.11066260656291149 ) ) ;
#26999=ORIENTED_EDGE ( 'NONE', *, *, #27532, .T. ) ;
#27000=CARTESIAN_POINT ( 'NONE',  ( 10.23245084088046220, -64.79111536330883325, -47.03631046558128759 ) ) ;
#27001=CARTESIAN_POINT ( 'NONE',  ( 11.67619942398430055, 33.65927571709689659, -45.08494251881550241 ) ) ;
#27002=CARTESIAN_POINT ( 'NONE',  ( 83.62039307877681438, -44.54160141935248163, -46.55140768024734399 ) ) ;
#27005=CARTESIAN_POINT ( 'NONE',  ( 57.55751162049570269, -50.61618894467930119, -53.92796738110899923 ) ) ;
#27007=ORIENTED_EDGE ( 'NONE', *, *, #21797, .F. ) ;
#27010=DIRECTION ( 'NONE',  ( 0.000000000000000000, 1.000000000000000000, 0.000000000000000000 ) ) ;
#27013=CARTESIAN_POINT ( 'NONE',  ( 53.23850466849069818, -49.52901910977939792, -49.17578823945770239 ) ) ;
#27014=CARTESIAN_POINT ( 'NONE',  ( 50.44542158146659716, 13.88381105532070059, -10.59990841316350085 ) ) ;
#27019=CARTESIAN_POINT ( 'NONE',  ( 12.14166061495670057, 33.87333292297899590, -16.52221827437060142 ) ) ;
#27021=CARTESIAN_POINT ( 'NONE',  ( 55.69969381902829753, -46.18869917138589898, -25.38063810554809763 ) ) ;
#27023=CARTESIAN_POINT ( 'NONE',  ( 53.82407901297139574, -51.23529577529289725, -75.59334556761540114 ) ) ;
#27024=CARTESIAN_POINT ( 'NONE',  ( -7.134180881003870489, 15.03340159476780080, -6.707190621226460259 ) ) ;
#27026=DIRECTION ( 'NONE',  ( 0.8732394366197160362, -0.4872913772396150756, 0.000000000000000000 ) ) ;
#27029=( BOUNDED_CURVE ( )  B_SPLINE_CURVE ( 3, ( #28732, #49710, #29251, #33179 ),
 .UNSPECIFIED., .F., .T. ) 
 B_SPLINE_CURVE_WITH_KNOTS ( ( 4, 4 ),
 ( 4.862900663153626013, 4.999863811009007009 ),
 .UNSPECIFIED. ) 
 CURVE ( )  GEOMETRIC_REPRESENTATION_ITEM ( )  RATIONAL_B_SPLINE_CURVE ( ( 1.000000000000000000, 0.9984373688466792185, 0.9984373688466792185, 1.000000000000000000 ) ) 
 REPRESENTATION_ITEM ( '' )  );
#27030=CARTESIAN_POINT ( 'NONE',  ( -9.553724527302819070, -43.62474080911430008, -5.594726724945660479 ) ) ;
#27031=B_SPLINE_CURVE_WITH_KNOTS ( 'NONE', 3,
 ( #24666, #48813, #582, #332, #48040, #25196, #41202, #17105, #44354, #40681, #16837, #13187, #4513, #8459, #5311, #1372, #20232, #48550 ),
 .UNSPECIFIED., .F., .F.,
 ( 4, 2, 2, 2, 2, 2, 2, 2, 4 ),
 ( -2.552633636494849867, -2.454247488323869852, -1.948999206626869984, -1.633219030566239960, -1.435856420528349942, -1.276316818247430041, -0.9572376136855691442, -0.4467108863865978385, 2.220446049250313081E-15 ),
 .UNSPECIFIED. ) ;
#27032=CARTESIAN_POINT ( 'NONE',  ( 47.62602275188279322, 23.28642693250159823, -54.79164112689819888 ) ) ;
#27033=EDGE_CURVE ( 'NONE', #45554, #40162, #46290, .T. ) ;
#27035=CARTESIAN_POINT ( 'NONE',  ( 84.44421850428412313, -43.32357619328593756, -47.46023813354324261 ) ) ;
#27036=CARTESIAN_POINT ( 'NONE',  ( 60.92599952699959687, 14.37113304530450009, -47.62103037817029616 ) ) ;
#27037=CARTESIAN_POINT ( 'NONE',  ( 11.41186166766810040, 33.90528444067879832, -17.00495033411830192 ) ) ;
#27038=CARTESIAN_POINT ( 'NONE',  ( 51.37477221945899686, 17.86423695781330068, -76.61256277725719599 ) ) ;
#27039=CARTESIAN_POINT ( 'NONE',  ( 52.82466266506040142, 18.43121127117079894, -48.56034107118879461 ) ) ;
#27042=CARTESIAN_POINT ( 'NONE',  ( 56.45717822463519298, 14.96703538239720110, -26.24611782501470003 ) ) ;
#27044=EDGE_CURVE ( 'NONE', #8290, #51304, #25644, .T. ) ;
#27045=CIRCLE ( 'NONE', #17848, 17.39999999999999503 ) ;
#27047=CARTESIAN_POINT ( 'NONE',  ( 52.97667581671070280, 18.39974466412820320, -49.06651679849090186 ) ) ;
#27048=CARTESIAN_POINT ( 'NONE',  ( 60.49441524024199879, -30.20409861275970087, -16.10365693432350298 ) ) ;
#27050=CARTESIAN_POINT ( 'NONE',  ( 11.13393739769619906, 32.06339680888989818, -43.91522882996569166 ) ) ;
#27052=CARTESIAN_POINT ( 'NONE',  ( 50.96897961697546009, -35.27620091889338028, -76.38407851794919168 ) ) ;
#27055=ORIENTED_EDGE ( 'NONE', *, *, #49812, .T. ) ;
#27056=CARTESIAN_POINT ( 'NONE',  ( 49.75284640906040323, 26.72485768586289723, -54.55457994667449384 ) ) ;
#27057=CARTESIAN_POINT ( 'NONE',  ( 50.02561910228128284, -1.340710577923809987, -15.97583675998615149 ) ) ;
#27058=ORIENTED_EDGE ( 'NONE', *, *, #41234, .F. ) ;
#27059=CARTESIAN_POINT ( 'NONE',  ( 55.93374749697019865, -46.01427663227649845, -25.74332633017289851 ) ) ;
#27060=FACE_OUTER_BOUND ( 'NONE', #20335, .T. ) ;
#27062=ORIENTED_EDGE ( 'NONE', *, *, #31393, .F. ) ;
#27065=CARTESIAN_POINT ( 'NONE',  ( 41.84490955069979634, -44.86154966424449952, -5.635703470643719903 ) ) ;
#27069=CARTESIAN_POINT ( 'NONE',  ( 52.10267379959660161, 1.883811054221469883, -20.65000000000000213 ) ) ;
#27072=CARTESIAN_POINT ( 'NONE',  ( 59.16200396169190157, -28.35957559346910273, -15.65933892576900099 ) ) ;
#27074=CARTESIAN_POINT ( 'NONE',  ( 47.15818641045569848, -54.58383002653739879, -75.00633330157590706 ) ) ;
#27076=EDGE_CURVE ( 'NONE', #4059, #46792, #36223, .T. ) ;
#27082=CARTESIAN_POINT ( 'NONE',  ( 84.43354761919439966, -43.30556812193899674, -47.41425570151039892 ) ) ;
#27083=CARTESIAN_POINT ( 'NONE',  ( 61.47394622263419706, 13.88380263855350094, -27.27040111922170240 ) ) ;
#27088=CARTESIAN_POINT ( 'NONE',  ( 10.81351130465269961, -63.69219886199940817, -15.12224224647750148 ) ) ;
#27089=CARTESIAN_POINT ( 'NONE',  ( 76.55459068199429851, 0.4406365421732439946, -13.46266660724949915 ) ) ;
#27090=CARTESIAN_POINT ( 'NONE',  ( 75.26896404091627346, 13.46709405488641309, -14.13654111410380665 ) ) ;
#27091=DIRECTION ( 'NONE',  ( 9.341879000000000579E-17, -6.787273000000000785E-17, 1.000000000000000000 ) ) ;
#27092=DIRECTION ( 'NONE',  ( 0.000000000000000000, 0.000000000000000000, -1.000000000000000000 ) ) ;
#27093=CARTESIAN_POINT ( 'NONE',  ( 12.84688943576596643, 20.36144273378011249, -21.73578643762688856 ) ) ;
#27095=CARTESIAN_POINT ( 'NONE',  ( 13.05742136612449933, 19.08961680411999851, -21.18088012638509809 ) ) ;
#27096=CARTESIAN_POINT ( 'NONE',  ( 57.29642382700900072, -50.59336727787100330, -53.60300200697109574 ) ) ;
#27097=CARTESIAN_POINT ( 'NONE',  ( 41.14792778566190634, 13.00557415106479908, -3.958129196103689296 ) ) ;
#27098=CARTESIAN_POINT ( 'NONE',  ( 18.86789271228509790, -51.78678246903520233, -74.14999999999999147 ) ) ;
#27101=CARTESIAN_POINT ( 'NONE',  ( 65.43393739769578588, -48.11618894467640217, -73.25000000000000000 ) ) ;
#27102=CIRCLE ( 'NONE', #27946, 1.000000000000000000 ) ;
#27103=CARTESIAN_POINT ( 'NONE',  ( 67.94624738391060248, -1.132776823338670136, -17.85820666156480030 ) ) ;
#27104=CARTESIAN_POINT ( 'NONE',  ( 17.77815508849479897, -51.52596624575240725, -75.36996982820370761 ) ) ;
#27105=CARTESIAN_POINT ( 'NONE',  ( 63.36072709640390599, -45.11618894467940066, -12.04575099730080012 ) ) ;
#27106=EDGE_CURVE ( 'NONE', #26902, #8993, #26831, .T. ) ;
#27109=ORIENTED_EDGE ( 'NONE', *, *, #14346, .T. ) ;
#27110=CARTESIAN_POINT ( 'NONE',  ( 8.949719927774120620, 31.88305279702909800, -46.63538165998269847 ) ) ;
#27115=CARTESIAN_POINT ( 'NONE',  ( 40.73312973959730243, -45.28955000209560211, -5.671162506903860034 ) ) ;
#27117=CARTESIAN_POINT ( 'NONE',  ( 17.72121729522119793, 20.57774151326000123, -75.67041253543310120 ) ) ;
#27123=AXIS2_PLACEMENT_3D ( 'NONE', #42972, #27982, #35609 ) ;
#27128=ORIENTED_EDGE ( 'NONE', *, *, #8795, .F. ) ;
#27132=CARTESIAN_POINT ( 'NONE',  ( 82.13853704237929776, 14.01986140997038888, -47.09707863094710945 ) ) ;
#27133=CARTESIAN_POINT ( 'NONE',  ( 51.42797784481540191, -51.20406220416529663, -76.10787249881708760 ) ) ;
#27134=CARTESIAN_POINT ( 'NONE',  ( 61.10834071495069963, 14.19179375509720131, -47.35406349611139376 ) ) ;
#27138=CARTESIAN_POINT ( 'NONE',  ( -9.434644029686850786, 12.51702915438919916, -5.750855165144660219 ) ) ;
#27139=EDGE_CURVE ( 'NONE', #23799, #30077, #38765, .T. ) ;
#27142=ADVANCED_FACE ( 'NONE', ( #50176 ), #28151, .F. ) ;
#27145=CARTESIAN_POINT ( 'NONE',  ( 58.45382029077139663, 15.48193787282010092, -47.52511337483100107 ) ) ;
#27146=CARTESIAN_POINT ( 'NONE',  ( 57.29403763066589761, 19.36100728100389645, -53.60293029200749970 ) ) ;
#27149=CARTESIAN_POINT ( 'NONE',  ( 15.00521638035900018, 19.40293989305209976, -20.65446309923339641 ) ) ;
#27151=CARTESIAN_POINT ( 'NONE',  ( 48.21519585597539503, -54.28409539510870019, -55.14684628828510427 ) ) ;
#27157=ORIENTED_EDGE ( 'NONE', *, *, #38361, .T. ) ;
#27159=CARTESIAN_POINT ( 'NONE',  ( 60.41042530350419781, -45.68919557567430445, -47.20254626644950235 ) ) ;
#27160=CARTESIAN_POINT ( 'NONE',  ( 54.20043578389000061, -48.94278307704069420, -48.51842787370119936 ) ) ;
#27161=CARTESIAN_POINT ( 'NONE',  ( 16.13393739769620083, -15.61618894467929941, 4.450000000000000178 ) ) ;
#27169=CIRCLE ( 'NONE', #23821, 0.9999999999999974465 ) ;
#27170=B_SPLINE_CURVE_WITH_KNOTS ( 'NONE', 3,
 ( #20757, #36744, #851, #16848, #48820, #38315, #25978, #30176 ),
 .UNSPECIFIED., .F., .F.,
 ( 4, 2, 2, 4 ),
 ( 0.000000000000000000, 0.2500000000000000000, 0.5000000000000000000, 1.000000000000000000 ),
 .UNSPECIFIED. ) ;
#27176=CARTESIAN_POINT ( 'NONE',  ( 9.374134746951858332, -64.20245714978280205, -46.81441715858309749 ) ) ;
#27179=ORIENTED_EDGE ( 'NONE', *, *, #26605, .T. ) ;
#27180=CARTESIAN_POINT ( 'NONE',  ( 56.46551611171859975, 19.54378718077660082, -53.85224439323700096 ) ) ;
#27182=CARTESIAN_POINT ( 'NONE',  ( 56.43758032280119608, -50.61865618686479706, -53.06658686592589902 ) ) ;
#27184=CARTESIAN_POINT ( 'NONE',  ( 64.74596444412888729, 0.01574119868441500175, -16.86735715512289957 ) ) ;
#27185=CARTESIAN_POINT ( 'NONE',  ( 51.81004866964649835, -49.31229632625730375, -76.98867843529478705 ) ) ;
#27186=EDGE_CURVE ( 'NONE', #22022, #4375, #20625, .T. ) ;
#27193=CARTESIAN_POINT ( 'NONE',  ( 12.89174309999000023, -50.31665465520150349, -21.19267362013180289 ) ) ;
#27195=CARTESIAN_POINT ( 'NONE',  ( 55.89391012728359698, 14.06573721227290008, -15.81894319212849886 ) ) ;
#27196=CARTESIAN_POINT ( 'NONE',  ( 61.08978236430399988, -45.33605757380430390, -46.92961198363219921 ) ) ;
#27197=CARTESIAN_POINT ( 'NONE',  ( 56.52076750121499771, -50.75359106364579986, -53.72896418895009418 ) ) ;
#27200=EDGE_CURVE ( 'NONE', #12954, #2493, #39409, .T. ) ;
#27203=CARTESIAN_POINT ( 'NONE',  ( 13.39996905094259994, -51.78681982904430470, -74.14993593045390696 ) ) ;
#27205=CARTESIAN_POINT ( 'NONE',  ( 44.79293918095169147, -46.10604169002750297, -8.834396361043069135 ) ) ;
#27206=CARTESIAN_POINT ( 'NONE',  ( 14.34417029198876037, -51.11618894467900986, -74.34716300801292732 ) ) ;
#27207=CARTESIAN_POINT ( 'NONE',  ( 14.22007340590318591, -50.37075074235775674, -20.84587593357120738 ) ) ;
#27209=CARTESIAN_POINT ( 'NONE',  ( 10.85466640530910176, -64.96697012893029921, -17.55961383758990024 ) ) ;
#27210=CARTESIAN_POINT ( 'NONE',  ( 82.43661600080049823, 13.98517417207279934, -47.02799317055919914 ) ) ;
#27212=DIRECTION ( 'NONE',  ( 0.000000000000000000, 1.000000000000000000, 0.000000000000000000 ) ) ;
#27213=CARTESIAN_POINT ( 'NONE',  ( 11.58723606553711960, 33.56456631676410041, -23.92637893903365764 ) ) ;
#27214=CIRCLE ( 'NONE', #22157, 1.999999999999996669 ) ;
#27216=CARTESIAN_POINT ( 'NONE',  ( 49.35532640881360322, 22.36582529078320292, -54.31909934291780218 ) ) ;
#27217=ORIENTED_EDGE ( 'NONE', *, *, #14346, .F. ) ;
#27218=CARTESIAN_POINT ( 'NONE',  ( 53.38243181765169965, -49.43430105679019704, -49.11031764516960152 ) ) ;
#27219=VERTEX_POINT ( 'NONE', #15811 ) ;
#27221=CARTESIAN_POINT ( 'NONE',  ( 55.91595717589669334, -45.90465048314089103, -17.93019253464870033 ) ) ;
#27222=CARTESIAN_POINT ( 'NONE',  ( 13.59495223564569955, 20.17160945779230019, -22.70120839867610130 ) ) ;
#27223=CARTESIAN_POINT ( 'NONE',  ( 12.89240665056879287, 24.25254711536716101, -75.71737149047099535 ) ) ;
#27225=CARTESIAN_POINT ( 'NONE',  ( 52.62812434242830051, 18.56774166479950239, -48.49159175247050513 ) ) ;
#27226=CARTESIAN_POINT ( 'NONE',  ( 55.98987895930139302, -45.71865684571069721, -17.27603967193159917 ) ) ;
#27227=CARTESIAN_POINT ( 'NONE',  ( 55.44576274181299880, 15.28165783319319893, -25.46131564888750276 ) ) ;
#27228=VERTEX_POINT ( 'NONE', #23902 ) ;
#27231=CARTESIAN_POINT ( 'NONE',  ( 10.99341273097670069, -65.07165995155320104, -17.55111636776990025 ) ) ;
#27232=CARTESIAN_POINT ( 'NONE',  ( 12.50062754218100025, 34.23954769984390367, -47.60354279947580380 ) ) ;
#27237=CARTESIAN_POINT ( 'NONE',  ( 50.49348186761249480, -53.32002352356300179, -54.80181514761489581 ) ) ;
#27240=CARTESIAN_POINT ( 'NONE',  ( 10.49445490244490031, -63.35389096203630999, -45.62690019722019485 ) ) ;
#27244=ORIENTED_EDGE ( 'NONE', *, *, #8220, .T. ) ;
#27245=CARTESIAN_POINT ( 'NONE',  ( 11.63780894515396902, -64.84990601410612499, -45.00312526891814002 ) ) ;
#27246=CARTESIAN_POINT ( 'NONE',  ( 57.18740753958720546, 19.19824428508539782, -53.01833411987959721 ) ) ;
#27251=CARTESIAN_POINT ( 'NONE',  ( 52.03944399862464110, 20.14552308598237573, -75.97489327919006996 ) ) ;
#27253=DIRECTION ( 'NONE',  ( 0.000000000000000000, 0.000000000000000000, -1.000000000000000000 ) ) ;
#27254=B_SPLINE_SURFACE_WITH_KNOTS ( 'NONE', 3, 3, ( 
 ( #39934, #51724, #11642, #19748, #3780, #4031, #7715, #35741, #23660, #15818, #51473, #51219 ),
 ( #16076, #19991, #104, #50951, #18971, #39422, #35988, #31783, #8218, #32034, #47800, #48057 ),
 ( #47041, #27607, #7192, #44119, #39164, #35216, #11906, #43356, #15313, #43100, #43862, #7960 ),
 ( #27862, #12157, #28112, #7449, #39674, #34951, #23909, #15049, #27096, #47298, #11128, #19492 ),
 ( #31016, #38910, #3000, #3522, #23399, #35482, #23147, #3257, #19234, #31265, #11388, #27350 ),
 ( #15572, #31528, #47546, #43612, #29413, #41217, #24164, #32806, #44629, #12674, #36753, #45417 ) ),
 .UNSPECIFIED., .F., .F., .F.,
 ( 4, 2, 4 ),
 ( 4, 1, 1, 1, 1, 1, 1, 1, 1, 4 ),
 ( -1.569668176790179892, -1.294976245851900076, -1.261864097015199970 ),
 ( 0.000000000000000000, 0.1111111111111110078, 0.2222222222222219878, 0.3333333333333329818, 0.4444444444444439757, 0.5555555555555560243, 0.6666666666666670737, 0.7777777777777779011, 0.8888888888888889506, 1.000000000000000000 ),
 .UNSPECIFIED. ) ;
#27261=CARTESIAN_POINT ( 'NONE',  ( 42.80890084010550112, -44.10023144781310123, -5.063862467037759885 ) ) ;
#27263=CARTESIAN_POINT ( 'NONE',  ( 52.63891792457810226, -49.80233798285760116, -48.69614933315279615 ) ) ;
#27264=AXIS2_PLACEMENT_3D ( 'NONE', #32425, #44775, #48448 ) ;
#27265=CARTESIAN_POINT ( 'NONE',  ( 53.41693480164780539, 18.12090330447910347, -48.75416851879779756 ) ) ;
#27269=CARTESIAN_POINT ( 'NONE',  ( 47.24090259303480366, 23.52242523391999640, -74.36162934055690243 ) ) ;
#27270=ADVANCED_FACE ( 'NONE', ( #23651 ), #48301, .T. ) ;
#27271=SPHERICAL_SURFACE ( 'NONE', #11686, 1.999999999999879874 ) ;
#27272=CARTESIAN_POINT ( 'NONE',  ( 41.64265090550289727, -46.42699119286240261, -4.296538310234230273 ) ) ;
#27274=CARTESIAN_POINT ( 'NONE',  ( 11.92574115022319958, 33.61414101779169528, -16.17905523990620154 ) ) ;
#27275=VECTOR ( 'NONE', #32349, 1000.000000000000000 ) ;
#27278=AXIS2_PLACEMENT_3D ( 'NONE', #35291, #19567, #38984 ) ;
#27279=CARTESIAN_POINT ( 'NONE',  ( 54.08208344327369588, -50.62656384555610600, -76.77976102529341063 ) ) ;
#27280=CARTESIAN_POINT ( 'NONE',  ( -5.732068215684789969, 16.49934381252809956, -7.265698657585460296 ) ) ;
#27286=CARTESIAN_POINT ( 'NONE',  ( 50.95182575631829991, 19.71852405838109945, -76.14999999999999147 ) ) ;
#27287=CARTESIAN_POINT ( 'NONE',  ( 47.61319252893540011, 23.29799037178950272, -54.82509320845959877 ) ) ;
#27288=CARTESIAN_POINT ( 'NONE',  ( 61.26731136653179988, -45.17707473731150003, -27.55258710780080378 ) ) ;
#27290=CARTESIAN_POINT ( 'NONE',  ( 61.44133208345009933, 14.11479117031280062, -47.30158650751790361 ) ) ;
#27292=CARTESIAN_POINT ( 'NONE',  ( 51.31527825151569999, 17.56656504245249906, -76.60412086039399071 ) ) ;
#27293=CARTESIAN_POINT ( 'NONE',  ( 53.21186570040269714, 18.22927129311189987, -48.84882494703119704 ) ) ;
#27297=CARTESIAN_POINT ( 'NONE',  ( 50.52370621751256152, 4.812620015576031918, -76.21186558187457649 ) ) ;
#27299=CARTESIAN_POINT ( 'NONE',  ( 65.03603135455020379, -32.24781572988710110, -17.83403478221860183 ) ) ;
#27301=CARTESIAN_POINT ( 'NONE',  ( 63.83689218472199656, -31.35186283222479631, -16.87006829021100174 ) ) ;
#27303=CARTESIAN_POINT ( 'NONE',  ( 12.06284766121009966, 32.21085600226960111, -46.39999999999999858 ) ) ;
#27305=VECTOR ( 'NONE', #10167, 1000.000000000000114 ) ;
#27312=EDGE_CURVE ( 'NONE', #23745, #44974, #23391, .T. ) ;
#27313=EDGE_LOOP ( 'NONE', ( #46936, #11951, #16380, #5919, #43385 ) ) ;
#27314=CARTESIAN_POINT ( 'NONE',  ( 56.76430699766049770, -45.27286064042839797, -25.50473296857350292 ) ) ;
#27317=CARTESIAN_POINT ( 'NONE',  ( 68.13393739769620083, -43.11618894467930119, -73.25000000000000000 ) ) ;
#27320=CARTESIAN_POINT ( 'NONE',  ( 10.64252135837869950, 32.35448059989499825, -23.65858396068249903 ) ) ;
#27325=CARTESIAN_POINT ( 'NONE',  ( 14.34417029198830029, 20.88381105532299742, -74.14999999999999147 ) ) ;
#27327=CARTESIAN_POINT ( 'NONE',  ( 61.13643316145629569, -29.09601468760619980, -15.93607196403809922 ) ) ;
#27329=CARTESIAN_POINT ( 'NONE',  ( 46.46443538989580446, -53.12220744445389897, -76.13964794981698958 ) ) ;
#27332=CARTESIAN_POINT ( 'NONE',  ( 40.80913032419420716, 13.98564897013269892, -5.659189743293089769 ) ) ;
#27333=CIRCLE ( 'NONE', #3063, 2.000000000000001332 ) ;
#27335=CARTESIAN_POINT ( 'NONE',  ( 10.47385200046668707, 23.98129158042145548, -45.62050397739949403 ) ) ;
#27336=( BOUNDED_CURVE ( )  B_SPLINE_CURVE ( 3, ( #25695, #6580, #34077, #10258 ),
 .UNSPECIFIED., .F., .T. ) 
 B_SPLINE_CURVE_WITH_KNOTS ( ( 4, 4 ),
 ( 2.239730981376319097, 2.341125871569534223 ),
 .UNSPECIFIED. ) 
 CURVE ( )  GEOMETRIC_REPRESENTATION_ITEM ( )  RATIONAL_B_SPLINE_CURVE ( ( 1.000000000000000000, 0.9991434398402569972, 0.9991434398402569972, 1.000000000000000000 ) ) 
 REPRESENTATION_ITEM ( '' )  );
#27337=CARTESIAN_POINT ( 'NONE',  ( 82.68714621053820224, -45.11135183450330288, -46.76937705306080062 ) ) ;
#27338=CIRCLE ( 'NONE', #4752, 0.9999999999999992228 ) ;
#27339=CARTESIAN_POINT ( 'NONE',  ( 15.67962062493570130, 19.63028992856250099, -20.15000000000000213 ) ) ;
#27342=DIRECTION ( 'NONE',  ( 0.000000000000000000, -1.000000000000000000, 0.000000000000000000 ) ) ;
#27343=CARTESIAN_POINT ( 'NONE',  ( 2.905851976713329954, -55.66614162501279850, -9.124290884277760583 ) ) ;
#27344=CARTESIAN_POINT ( 'NONE',  ( 76.46067994297268910, -29.90098307356280216, -13.05651891160819922 ) ) ;
#27345=CARTESIAN_POINT ( 'NONE',  ( 75.27756523070299011, 13.44262948222908527, -14.10653473551886883 ) ) ;
#27347=CARTESIAN_POINT ( 'NONE',  ( 12.95505628089291328, -55.48922089072598851, -75.75074683306100098 ) ) ;
#27348=AXIS2_PLACEMENT_3D ( 'NONE', #21678, #10435, #6242 ) ;
#27349=CARTESIAN_POINT ( 'NONE',  ( 82.13853704237929776, -45.22180057317820001, -47.02038781679129897 ) ) ;
#27350=CARTESIAN_POINT ( 'NONE',  ( 57.26033578974089977, -50.61618894467930119, -53.91588143635480179 ) ) ;
#27351=CARTESIAN_POINT ( 'NONE',  ( 42.08165257923059954, 13.00661616386149966, -4.969335771722079187 ) ) ;
#27354=CARTESIAN_POINT ( 'NONE',  ( 56.99484845788649778, -47.50308119450649968, -48.07762127917849426 ) ) ;
#27355=CARTESIAN_POINT ( 'NONE',  ( 65.43393739769584272, -48.11618894467441976, -75.95000000000109708 ) ) ;
#27357=CARTESIAN_POINT ( 'NONE',  ( 17.93795525508479827, -51.86173801737519540, -75.67066142420200947 ) ) ;
#27358=CARTESIAN_POINT ( 'NONE',  ( 45.01728387151260335, -44.97693402557090536, -6.411623703542949748 ) ) ;
#27363=CARTESIAN_POINT ( 'NONE',  ( 46.03122142033570441, 13.88381105532070059, -7.582879021622040305 ) ) ;
#27369=CIRCLE ( 'NONE', #15671, 38.00000000000000000 ) ;
#27370=CARTESIAN_POINT ( 'NONE',  ( 17.68156872138649760, 20.67960354982550086, -75.75221093576890041 ) ) ;
#27371=ORIENTED_EDGE ( 'NONE', *, *, #6462, .F. ) ;
#27375=CARTESIAN_POINT ( 'NONE',  ( 56.87513795754310308, -45.11618894467940066, -15.74603272341079929 ) ) ;
#27377=DIRECTION ( 'NONE',  ( -1.000000000000000000, 0.000000000000000000, 0.000000000000000000 ) ) ;
#27378=ADVANCED_FACE ( 'NONE', ( #11636 ), #39417, .F. ) ;
#27379=CARTESIAN_POINT ( 'NONE',  ( 61.69283295620359553, 13.94392212662380182, -46.85915540805209645 ) ) ;
#27389=CARTESIAN_POINT ( 'NONE',  ( 51.03828674417159306, -50.88950370325699879, -76.15016575943649002 ) ) ;
#27390=CARTESIAN_POINT ( 'NONE',  ( 60.82036937039629976, 14.47434740296430178, -47.72837797750310074 ) ) ;
#27392=EDGE_CURVE ( 'NONE', #42919, #38484, #8211, .T. ) ;
#27393=CARTESIAN_POINT ( 'NONE',  ( 41.57697697597580344, -43.84131550590989690, -3.558127429192100344 ) ) ;
#27394=CARTESIAN_POINT ( 'NONE',  ( -11.32734370190460105, 10.64934056395049922, -6.430192534648650593 ) ) ;
#27395=CARTESIAN_POINT ( 'NONE',  ( 46.84224739830732176, 22.80152007029589001, -75.76637087393561387 ) ) ;
#27399=CARTESIAN_POINT ( 'NONE',  ( 56.84932596551109185, -50.65659107673559447, -53.85230338955700091 ) ) ;
#27400=CARTESIAN_POINT ( 'NONE',  ( 44.79311949664099757, 14.87366903724590017, -8.834518368838249813 ) ) ;
#27403=CARTESIAN_POINT ( 'NONE',  ( 15.65801254756719807, 19.62299100880909819, -20.25518593351949903 ) ) ;
#27406=LINE ( 'NONE', #34748, #4581 ) ;
#27407=CARTESIAN_POINT ( 'NONE',  ( 48.85881101229590229, -54.00570711265250168, -55.08347352314449807 ) ) ;
#27408=CARTESIAN_POINT ( 'NONE',  ( -12.74484839418222748, -57.05697611480018594, -53.24848714985477471 ) ) ;
#27409=DIRECTION ( 'NONE',  ( -0.7286256507163790808, -0.6849121557675359462, 0.000000000000000000 ) ) ;
#27411=CARTESIAN_POINT ( 'NONE',  ( 47.73402016065340092, 23.24730430298579975, -54.93079182720639864 ) ) ;
#27412=ORIENTED_EDGE ( 'NONE', *, *, #32094, .T. ) ;
#27415=CARTESIAN_POINT ( 'NONE',  ( 18.38332385620206111, 20.94377882893676102, -75.56421372420827254 ) ) ;
#27416=CARTESIAN_POINT ( 'NONE',  ( 60.30125063334870106, -45.75567911012539923, -47.36809293580299851 ) ) ;
#27417=DIRECTION ( 'NONE',  ( -1.000000000000000000, 0.000000000000000000, 0.000000000000000000 ) ) ;
#27422=ORIENTED_EDGE ( 'NONE', *, *, #4649, .F. ) ;
#27423=DIRECTION ( 'NONE',  ( -0.8224686640529090820, -0.3976080002595601126, -0.4067593573362717763 ) ) ;
#27426=AXIS2_PLACEMENT_3D ( 'NONE', #17893, #42270, #45946 ) ;
#27431=CARTESIAN_POINT ( 'NONE',  ( 76.87859684847769870, -43.11619168008749625, -14.85884840380859906 ) ) ;
#27432=CARTESIAN_POINT ( 'NONE',  ( 12.77819848573380135, -65.50111593353840078, -47.68593301887450053 ) ) ;
#27433=VERTEX_POINT ( 'NONE', #33066 ) ;
#27434=ORIENTED_EDGE ( 'NONE', *, *, #16648, .F. ) ;
#27438=CARTESIAN_POINT ( 'NONE',  ( 56.39270784037439199, -50.52750194525579985, -52.86271187285759510 ) ) ;
#27439=DIRECTION ( 'NONE',  ( 0.9313175168446001795, -0.3616257875446830528, 0.04329517988293300756 ) ) ;
#27440=CARTESIAN_POINT ( 'NONE',  ( 62.98651954880020298, -0.7832202496777560530, -16.35632123205009947 ) ) ;
#27442=CARTESIAN_POINT ( 'NONE',  ( 51.31527825141329657, -48.79894293239630088, -76.60412086037939616 ) ) ;
#27443=CARTESIAN_POINT ( 'NONE',  ( 60.48885993748309886, -46.71224472025600249, -48.89115175517449785 ) ) ;
#27447=DIRECTION ( 'NONE',  ( 0.000000000000000000, 0.000000000000000000, -1.000000000000000000 ) ) ;
#27448=CARTESIAN_POINT ( 'NONE',  ( 83.36355414456373580, -45.34681625531927551, -47.55048134727741171 ) ) ;
#27450=CARTESIAN_POINT ( 'NONE',  ( 12.89658886673069915, -50.00140124964299559, -21.06837794024639976 ) ) ;
#27451=CARTESIAN_POINT ( 'NONE',  ( 56.53391597728690243, 19.38755390252309851, -75.43697629958880668 ) ) ;
#27452=EDGE_CURVE ( 'NONE', #29653, #37505, #27338, .T. ) ;
#27453=DIRECTION ( 'NONE',  ( -0.8320502943378438321, 0.000000000000000000, 0.5547001962252288143 ) ) ;
#27454=CARTESIAN_POINT ( 'NONE',  ( 56.00506715693309445, 13.88381105532070059, -14.82112848627589941 ) ) ;
#27455=CARTESIAN_POINT ( 'NONE',  ( 60.70258586536569823, -45.54124907573869763, -47.21990429565040159 ) ) ;
#27460=CARTESIAN_POINT ( 'NONE',  ( 46.90960455200850276, 22.37535576487919897, -75.96332490897151501 ) ) ;
#27462=LINE ( 'NONE', #26952, #22220 ) ;
#27463=LINE ( 'NONE', #43466, #13705 ) ;
#27464=CARTESIAN_POINT ( 'NONE',  ( 14.16187783161290170, -50.35113599914600258, -20.85710678118659800 ) ) ;
#27467=CARTESIAN_POINT ( 'NONE',  ( 10.64977475910500004, -64.85626261263139725, -18.05902683592860214 ) ) ;
#27468=CARTESIAN_POINT ( 'NONE',  ( 10.80633501409609920, 33.76396855927119844, -17.92671787883650225 ) ) ;
#27469=EDGE_CURVE ( 'NONE', #26913, #8932, #34058, .T. ) ;
#27470=CARTESIAN_POINT ( 'NONE',  ( 56.46551567295650642, -50.77616483221130750, -74.14999999999999147 ) ) ;
#27473=CARTESIAN_POINT ( 'NONE',  ( -0.2744272739026379915, -53.43782452381620374, -9.661128459681899372 ) ) ;
#27474=CARTESIAN_POINT ( 'NONE',  ( 49.06940219517189661, 22.69206583466019822, -55.15293681905570367 ) ) ;
#27475=EDGE_CURVE ( 'NONE', #20296, #45486, #14821, .T. ) ;
#27476=ORIENTED_EDGE ( 'NONE', *, *, #17913, .T. ) ;
#27477=CARTESIAN_POINT ( 'NONE',  ( 53.15063603407050152, -49.53259255823910223, -49.06766781164589730 ) ) ;
#27479=ORIENTED_EDGE ( 'NONE', *, *, #50840, .T. ) ;
#27482=FACE_OUTER_BOUND ( 'NONE', #26532, .T. ) ;
#27483=CARTESIAN_POINT ( 'NONE',  ( 13.87880486592528406, 24.32147317887789839, -76.14999999999997726 ) ) ;
#27485=CARTESIAN_POINT ( 'NONE',  ( 55.87801225299120489, -45.85446601339950234, -17.30532844135920101 ) ) ;
#27487=ORIENTED_EDGE ( 'NONE', *, *, #25115, .F. ) ;
#27490=CARTESIAN_POINT ( 'NONE',  ( 11.98643060099639968, -65.41791523794120167, -17.50083490704260214 ) ) ;
#27491=CARTESIAN_POINT ( 'NONE',  ( 10.13410506179149984, 33.50987130412710258, -47.01082059592499718 ) ) ;
#27495=FACE_OUTER_BOUND ( 'NONE', #40401, .T. ) ;
#27496=DIRECTION ( 'NONE',  ( 0.000000000000000000, -1.000000000000000000, 0.000000000000000000 ) ) ;
#27500=EDGE_CURVE ( 'NONE', #29825, #44194, #31857, .T. ) ;
#27502=CARTESIAN_POINT ( 'NONE',  ( 11.13393739769619906, -63.50859000450320480, -43.92731420739779225 ) ) ;
#27503=VECTOR ( 'NONE', #10029, 1000.000000000000000 ) ;
#27504=CARTESIAN_POINT ( 'NONE',  ( 68.13393739769810509, 19.38381105532030091, -71.50000000000198952 ) ) ;
#27516=DIRECTION ( 'NONE',  ( 0.000000000000000000, 1.000000000000000000, 0.000000000000000000 ) ) ;
#27517=PRODUCT_CONTEXT ( 'NONE', #22066, 'mechanical' ) ;
#27519=ORIENTED_EDGE ( 'NONE', *, *, #36141, .T. ) ;
#27521=CARTESIAN_POINT ( 'NONE',  ( 52.90434498377169348, -49.66345680823589959, -49.01850774012499556 ) ) ;
#27523=CARTESIAN_POINT ( 'NONE',  ( 47.07006461603479863, 23.03759314561689919, -75.46887108633461594 ) ) ;
#27524=DIRECTION ( 'NONE',  ( -0.2717754459342062168, -0.4033282527652566896, 0.8737645149058118621 ) ) ;
#27525=B_SPLINE_CURVE_WITH_KNOTS ( 'NONE', 3,
 ( #12871, #9456, #13139, #49292, #13389, #40633, #20962, #36689, #4732, #28827, #1840, #1325, #41407, #17818, #1060, #33537, #29348, #41667, #25405, #17055 ),
 .UNSPECIFIED., .F., .F.,
 ( 4, 2, 2, 2, 2, 2, 2, 2, 2, 4 ),
 ( 0.000000000000000000, 0.05535613038339300823, 0.2869944836127450438, 0.5186328368420959345, 0.8630971313986249838, 1.150796175198169902, 1.294645697097940085, 1.524804932137569846, 1.893059708200979907, 2.301592350396330033 ),
 .UNSPECIFIED. ) ;
#27526=DIRECTION ( 'NONE',  ( 0.000000000000000000, 1.000000000000000000, 0.000000000000000000 ) ) ;
#27527=CARTESIAN_POINT ( 'NONE',  ( 11.86574223145029983, 33.83900248408709643, -16.54426240393689795 ) ) ;
#27530=VECTOR ( 'NONE', #14690, 1000.000000000000000 ) ;
#27532=EDGE_CURVE ( 'NONE', #35884, #22335, #3944, .T. ) ;
#27533=CARTESIAN_POINT ( 'NONE',  ( 54.33632571825120294, -50.61618477685789941, -76.86293993265819324 ) ) ;
#27534=CARTESIAN_POINT ( 'NONE',  ( -2.912062977092380045, 18.91103907894019898, -6.721088743486959949 ) ) ;
#27535=CARTESIAN_POINT ( 'NONE',  ( 47.18325654339099628, 23.57487866773040253, -54.61058579560449289 ) ) ;
#27537=CARTESIAN_POINT ( 'NONE',  ( 61.38942555204300078, 13.99165690388499961, -46.90185059412529966 ) ) ;
#27540=ORIENTED_EDGE ( 'NONE', *, *, #3093, .T. ) ;
#27541=CARTESIAN_POINT ( 'NONE',  ( 53.39564317062880150, -49.36443647587950068, -48.78219654307289943 ) ) ;
#27542=CARTESIAN_POINT ( 'NONE',  ( 47.83453594094610395, 23.15510728029320120, -54.72216408865189408 ) ) ;
#27543=CARTESIAN_POINT ( 'NONE',  ( 57.83204157793740308, -45.68025036402679717, -26.31202219667439834 ) ) ;
#27545=CARTESIAN_POINT ( 'NONE',  ( 61.24439460628430254, 14.13692964258179963, -47.29149699898169956 ) ) ;
#27547=CARTESIAN_POINT ( 'NONE',  ( 51.34762213738049752, 17.76135683261760079, -76.60870781513519034 ) ) ;
#27548=CARTESIAN_POINT ( 'NONE',  ( 52.77257271998939814, 18.46126773324610326, -48.57104616786630658 ) ) ;
#27550=CARTESIAN_POINT ( 'NONE',  ( 52.86024057890899996, -49.64494889463909999, -48.64479820451980174 ) ) ;
#27552=CARTESIAN_POINT ( 'NONE',  ( 47.57920160075400418, -54.54378672726409860, -54.77372601769780402 ) ) ;
#27553=CARTESIAN_POINT ( 'NONE',  ( 63.63877703368444116, -31.87229146824659765, -17.33502983657059460 ) ) ;
#27555=CARTESIAN_POINT ( 'NONE',  ( 59.97735437335310138, -29.43971439818610136, -15.84040877096640187 ) ) ;
#27557=CARTESIAN_POINT ( 'NONE',  ( 11.13393739769619906, 32.10364385886999372, -43.74837338606149473 ) ) ;
#27559=CARTESIAN_POINT ( 'NONE',  ( 51.37212073277904523, -34.54336882558848743, -76.66706012796622360 ) ) ;
#27563=EDGE_LOOP ( 'NONE', ( #32658, #15532, #18824, #38240 ) ) ;
#27565=EDGE_CURVE ( 'NONE', #29281, #46345, #19002, .T. ) ;
#27567=EDGE_LOOP ( 'NONE', ( #9217, #42467, #8177, #25108 ) ) ;
#27570=TOROIDAL_SURFACE ( 'NONE', #44335, 34.99999963932619806, 4.999999999166930387 ) ;
#27576=CARTESIAN_POINT ( 'NONE',  ( 41.47581685013189912, -44.78873423027059886, -5.433834233955179727 ) ) ;
#27577=CIRCLE ( 'NONE', #42671, 1.000000000000000444 ) ;
#27578=AXIS2_PLACEMENT_3D ( 'NONE', #18463, #26570, #6680 ) ;
#27582=CARTESIAN_POINT ( 'NONE',  ( 62.94494383321469400, -29.78410970874689667, -16.20581832066559969 ) ) ;
#27583=CARTESIAN_POINT ( 'NONE',  ( 14.38797371179902385, 20.00716050925374390, -74.86151687917137565 ) ) ;
#27584=CARTESIAN_POINT ( 'NONE',  ( 47.29839800642639602, -54.29825318176240501, -75.29258675765889564 ) ) ;
#27586=CARTESIAN_POINT ( 'NONE',  ( 54.47257875656340076, 15.01998573668699954, -15.76423485725169904 ) ) ;
#27587=CARTESIAN_POINT ( 'NONE',  ( 42.77859928634750020, 14.48502410817190089, -7.241844954409731194 ) ) ;
#27588=CARTESIAN_POINT ( 'NONE',  ( 15.05440318628110141, 21.88381105532300097, -76.14999999999999147 ) ) ;
#27589=CARTESIAN_POINT ( 'NONE',  ( 84.44784216359251161, -43.11618894467930119, -47.47585302082339354 ) ) ;
#27590=DIRECTION ( 'NONE',  ( -1.000000000000000000, 0.000000000000000000, 0.000000000000000000 ) ) ;
#27593=CARTESIAN_POINT ( 'NONE',  ( 56.48923526673240048, -46.16653024775970238, -26.24159571999479823 ) ) ;
#27595=CARTESIAN_POINT ( 'NONE',  ( 15.03857555097549970, -50.67925693779799445, -20.69450120486489908 ) ) ;
#27596=CARTESIAN_POINT ( 'NONE',  ( 76.82820088796398750, 11.97361217437780034, -14.64015420985709959 ) ) ;
#27601=AXIS2_PLACEMENT_3D ( 'NONE', #3626, #36873, #20353 ) ;
#27602=CARTESIAN_POINT ( 'NONE',  ( -10.87300634462279980, -42.35673974988220181, -6.273959123267670357 ) ) ;
#27604=CARTESIAN_POINT ( 'NONE',  ( 9.127429636406475311, -55.01082058323148516, -22.14349223871027306 ) ) ;
#27607=CARTESIAN_POINT ( 'NONE',  ( 57.43802301110889630, -50.15325042756680318, -52.64491009731540316 ) ) ;
#27608=CARTESIAN_POINT ( 'NONE',  ( 42.52205268124630066, 12.26030094018719829, -4.456987777771080239 ) ) ;
#27610=CARTESIAN_POINT ( 'NONE',  ( 73.34727812780759848, -45.11618894467940066, -14.85468426629290128 ) ) ;
#27612=CARTESIAN_POINT ( 'NONE',  ( 68.13393739769840352, -50.61618894467879670, -73.25000000000220268 ) ) ;
#27614=CARTESIAN_POINT ( 'NONE',  ( 17.72038853882659737, -51.81226317974009987, -75.66803551354809088 ) ) ;
#27615=CARTESIAN_POINT ( 'NONE',  ( 16.13393739769620083, -15.61618894467929941, -6.928362978644219794 ) ) ;
#27626=EDGE_CURVE ( 'NONE', #26340, #13860, #37405, .T. ) ;
#27627=CARTESIAN_POINT ( 'NONE',  ( 18.22266512930399784, 21.07290090200189780, -75.74020909530109691 ) ) ;
#27629=ADVANCED_FACE ( 'NONE', ( #18904 ), #10546, .T. ) ;
#27632=B_SPLINE_CURVE_WITH_KNOTS ( 'NONE', 3,
 ( #16598, #32551, #48586, #12687, #44642, #45948, #49879, #21296, #42271, #18409, #13974, #29931, #26003, #21556, #17895, #45686, #38336, #26265, #29676, #10039, #10303, #22070, #38079, #49371, #17387 ),
 .UNSPECIFIED., .F., .F.,
 ( 4, 1, 1, 1, 2, 2, 1, 2, 2, 1, 2, 2, 2, 2, 4 ),
 ( 0.000000000000000000, 0.1250000000000037748, 0.1875000000000047184, 0.2187500000000053846, 0.2343750000000057176, 0.2500000000000060507, 0.3125000000000070499, 0.3437500000000067168, 0.3750000000000063838, 0.4375000000000049960, 0.4687500000000051070, 0.5000000000000052180, 0.6250000000000039968, 0.7500000000000027756, 1.000000000000000000 ),
 .UNSPECIFIED. ) ;
#27634=CARTESIAN_POINT ( 'NONE',  ( 61.61165453121049751, 14.00280548404949954, -47.05504859273239759 ) ) ;
#27636=CARTESIAN_POINT ( 'NONE',  ( 68.13393739769620083, -48.61618894467930119, -65.65000000000000568 ) ) ;
#27639=CARTESIAN_POINT ( 'NONE',  ( 57.24929578595760660, 19.38381105532069881, -74.14999999999999147 ) ) ;
#27645=CARTESIAN_POINT ( 'NONE',  ( 51.49462705094970261, -51.12905048845459532, -76.11693519191881308 ) ) ;
#27647=CARTESIAN_POINT ( 'NONE',  ( 61.29825847224779523, 14.29443508044710143, -47.59225652243549831 ) ) ;
#27650=CARTESIAN_POINT ( 'NONE',  ( -3.908839563797870120, 17.07291065422449705, -5.445805040184419354 ) ) ;
#27655=CARTESIAN_POINT ( 'NONE',  ( 56.83722671258179560, -50.65906061578299813, -53.85090158306050512 ) ) ;
#27657=CARTESIAN_POINT ( 'NONE',  ( 41.43966039318529937, 14.40677330313000049, -6.362507098331501076 ) ) ;
#27660=ADVANCED_FACE ( 'NONE', ( #50114 ), #50629, .T. ) ;
#27661=CARTESIAN_POINT ( 'NONE',  ( 14.22165922051550169, 19.31192048736480160, -21.01402899345969999 ) ) ;
#27662=ADVANCED_FACE ( 'NONE', ( #10019 ), #25981, .T. ) ;
#27663=CARTESIAN_POINT ( 'NONE',  ( 12.53549334626059952, 18.74519656086519959, -21.12176656462050062 ) ) ;
#27665=CARTESIAN_POINT ( 'NONE',  ( 48.74537093715300529, -53.89676824263879951, -54.52146652541890148 ) ) ;
#27666=DIRECTION ( 'NONE',  ( 1.000000000000000000, 0.000000000000000000, 0.000000000000000000 ) ) ;
#27670=ORIENTED_EDGE ( 'NONE', *, *, #33653, .F. ) ;
#27675=CIRCLE ( 'NONE', #47782, 2.000000000000001332 ) ;
#27676=CARTESIAN_POINT ( 'NONE',  ( 60.70114797779579874, -45.57531533405330748, -47.37795440859400031 ) ) ;
#27685=ORIENTED_EDGE ( 'NONE', *, *, #6922, .F. ) ;
#27687=ORIENTED_EDGE ( 'NONE', *, *, #18442, .T. ) ;
#27688=EDGE_CURVE ( 'NONE', #13415, #4297, #29758, .T. ) ;
#27689=EDGE_LOOP ( 'NONE', ( #27736, #33707, #34186, #42233, #30329 ) ) ;
#27692=CARTESIAN_POINT ( 'NONE',  ( 12.75847677693120197, 34.25788405235230272, -47.26854789455460093 ) ) ;
#27693=CARTESIAN_POINT ( 'NONE',  ( 12.19850843269619922, -65.41247318024639412, -47.44469434798769925 ) ) ;
#27696=CARTESIAN_POINT ( 'NONE',  ( 56.80588353391389944, -45.24242660625780132, -25.29585452565680015 ) ) ;
#27697=CARTESIAN_POINT ( 'NONE',  ( 56.46328325841249551, -50.76386906370840535, -53.62058756809589255 ) ) ;
#27699=CARTESIAN_POINT ( 'NONE',  ( 59.04067005502180621, -2.813652991295200412, -15.65184294716019942 ) ) ;
#27700=CARTESIAN_POINT ( 'NONE',  ( 51.85163801358509517, -49.58237482539740171, -76.86771389695809376 ) ) ;
#27702=ORIENTED_EDGE ( 'NONE', *, *, #12380, .T. ) ;
#27706=DIRECTION ( 'NONE',  ( 1.000000000000000000, 0.000000000000000000, 0.000000000000000000 ) ) ;
#27709=CARTESIAN_POINT ( 'NONE',  ( 55.87921360396619974, 19.38381105532069881, -76.16089020870099091 ) ) ;
#27711=CARTESIAN_POINT ( 'NONE',  ( 55.82174411980109596, 13.88381105532070059, -14.52096170695349997 ) ) ;
#27712=CARTESIAN_POINT ( 'NONE',  ( 60.67373791137799799, -45.55123872289310327, -47.14825100140640757 ) ) ;
#27713=VECTOR ( 'NONE', #14602, 1000.000000000000000 ) ;
#27717=AXIS2_PLACEMENT_3D ( 'NONE', #32765, #9482, #48790 ) ;
#27718=EDGE_LOOP ( 'NONE', ( #7736, #48922, #46719, #931, #45637 ) ) ;
#27720=ADVANCED_FACE ( 'NONE', ( #14726 ), #30179, .T. ) ;
#27723=EDGE_CURVE ( 'NONE', #17152, #28405, #48188, .T. ) ;
#27724=CARTESIAN_POINT ( 'NONE',  ( 14.39524263072926047, -51.26000751222474605, -74.91995119710422557 ) ) ;
#27729=CARTESIAN_POINT ( 'NONE',  ( 11.43830175784020042, 34.12894736269659290, -18.07704217307109928 ) ) ;
#27731=DIRECTION ( 'NONE',  ( 1.000000000000000000, 0.000000000000000000, 0.000000000000000000 ) ) ;
#27733=CARTESIAN_POINT ( 'NONE',  ( 82.13853704237929776, -45.11618894467940066, -46.37203261889099792 ) ) ;
#27735=CARTESIAN_POINT ( 'NONE',  ( 49.05097002867299949, 22.69010155233289794, -55.04456405487339765 ) ) ;
#27736=ORIENTED_EDGE ( 'NONE', *, *, #14477, .F. ) ;
#27737=CARTESIAN_POINT ( 'NONE',  ( 53.48011204154060039, -49.37340621726109902, -49.05829711586440567 ) ) ;
#27743=CARTESIAN_POINT ( 'NONE',  ( 51.70989020309399109, -48.92491896723970513, -77.02393701242800716 ) ) ;
#27745=DIRECTION ( 'NONE',  ( 1.000000000000000000, 0.000000000000000000, 0.000000000000000000 ) ) ;
#27746=CARTESIAN_POINT ( 'NONE',  ( 56.55503449515249770, -45.27146332001730400, -16.89072690454599979 ) ) ;
#27747=CARTESIAN_POINT ( 'NONE',  ( 53.72005416868749705, 17.35859260027000062, -26.34191669766330079 ) ) ;
#27748=VERTEX_POINT ( 'NONE', #34625 ) ;
#27750=EDGE_CURVE ( 'NONE', #14841, #33088, #40601, .T. ) ;
#27751=ORIENTED_EDGE ( 'NONE', *, *, #39030, .F. ) ;
#27752=CARTESIAN_POINT ( 'NONE',  ( 11.19833792948340090, -65.16806354647678745, -17.40716438213639705 ) ) ;
#27753=CARTESIAN_POINT ( 'NONE',  ( 12.52666257856989951, 34.23916454258710473, -47.57015704360200203 ) ) ;
#27756=CARTESIAN_POINT ( 'NONE',  ( 52.09592895031209991, -50.80234781981220493, -50.78436303379759664 ) ) ;
#27757=CARTESIAN_POINT ( 'NONE',  ( 8.803701492139829554, 31.98286322187070141, -46.67019247816079286 ) ) ;
#27763=CARTESIAN_POINT ( 'NONE',  ( 11.13393739769619906, -63.42417329230280387, -43.75301033632869263 ) ) ;
#27764=CARTESIAN_POINT ( 'NONE',  ( 67.04038824939814845, 19.47158195952278703, -71.50000000000200373 ) ) ;
#27767=CARTESIAN_POINT ( 'NONE',  ( 56.85513652204900126, 19.27500186593999842, -53.07093444364119961 ) ) ;
#27773=CARTESIAN_POINT ( 'NONE',  ( 56.44284150913800602, 14.76297046884359965, -45.11789043107459918 ) ) ;
#27780=ORIENTED_EDGE ( 'NONE', *, *, #8252, .T. ) ;
#27783=CARTESIAN_POINT ( 'NONE',  ( 47.22841302400619412, 23.19665601663579935, -75.17093853428211503 ) ) ;
#27785=DIRECTION ( 'NONE',  ( -0.6023772969742121619, -0.4987169684303940920, -0.6232358923310170606 ) ) ;
#27788=CARTESIAN_POINT ( 'NONE',  ( 11.60439326025529994, 33.70240003096060377, -16.46429631544720351 ) ) ;
#27789=AXIS2_PLACEMENT_3D ( 'NONE', #24668, #584, #35971 ) ;
#27793=CARTESIAN_POINT ( 'NONE',  ( 55.24960754175609878, -50.62333154088300091, -76.30022807136839447 ) ) ;
#27794=CARTESIAN_POINT ( 'NONE',  ( -6.938047273389929437, 15.02604475192799960, -5.910678614907980410 ) ) ;
#27797=CARTESIAN_POINT ( 'NONE',  ( 61.22003255449720172, 14.03468818129520024, -46.76603150336679704 ) ) ;
#27799=CARTESIAN_POINT ( 'NONE',  ( 66.70013194292150160, -1.463538230407920082, -17.02746303015019791 ) ) ;
#27801=CARTESIAN_POINT ( 'NONE',  ( 53.39109823518269593, -49.36681769490010652, -48.76214596301609561 ) ) ;
#27802=CARTESIAN_POINT ( 'NONE',  ( 58.98985417505780049, -45.56972936611299474, -26.56632039979439952 ) ) ;
#27804=CARTESIAN_POINT ( 'NONE',  ( 75.41048247916201319, -50.61618894467930119, -82.11365365517009707 ) ) ;
#27806=CARTESIAN_POINT ( 'NONE',  ( 51.63757600187660302, 18.40000253807760089, -76.65049568453349593 ) ) ;
#27807=CARTESIAN_POINT ( 'NONE',  ( 52.90334277911429695, 18.39508939093590101, -48.83356293938759762 ) ) ;
#27808=CARTESIAN_POINT ( 'NONE',  ( 52.83011299386760129, -49.66073358055960085, -48.49877547121819532 ) ) ;
#27811=CARTESIAN_POINT ( 'NONE',  ( 47.77031587149589598, -54.42339131114619732, -54.72319043475250311 ) ) ;
#27814=CARTESIAN_POINT ( 'NONE',  ( 60.73270329006090407, -30.50852859027810027, -16.25406692276280296 ) ) ;
#27818=CARTESIAN_POINT ( 'NONE',  ( 51.67587649748470113, -33.96749857170579645, -77.01363636363508647 ) ) ;
#27822=B_SPLINE_CURVE_WITH_KNOTS ( 'NONE', 3,
 ( #21407, #2477, #48965, #30501, #29022, #41086, #9388, #9118, #33461, #16990, #32938, #26568, #13069, #1510, #37409, #17494 ),
 .UNSPECIFIED., .F., .F.,
 ( 4, 2, 2, 2, 2, 2, 2, 4 ),
 ( -1.896558999999999901E-14, 0.4421500870759600410, 0.9474644723056518947, 1.263285963074209928, 1.421196708458489999, 1.673853901073330208, 2.078105409257089864, 2.526571926148439839 ),
 .UNSPECIFIED. ) ;
#27823=DIRECTION ( 'NONE',  ( -1.000000000000000000, 0.000000000000000000, 0.000000000000000000 ) ) ;
#27824=CARTESIAN_POINT ( 'NONE',  ( 51.01176328416968886, -31.39810158946774266, -16.86084553931457464 ) ) ;
#27826=CARTESIAN_POINT ( 'NONE',  ( 57.15402662460559924, -45.14613312479689711, -25.30846757484389897 ) ) ;
#27830=AXIS2_PLACEMENT_3D ( 'NONE', #11552, #23304, #14697 ) ;
#27833=CARTESIAN_POINT ( 'NONE',  ( 63.88393739769619373, 11.88381105532070059, -61.34712802272770915 ) ) ;
#27838=CARTESIAN_POINT ( 'NONE',  ( 59.49262858449159808, 17.38381105532069881, -53.92796738110899923 ) ) ;
#27839=ADVANCED_FACE ( 'NONE', ( #11839 ), #11577, .F. ) ;
#27840=CARTESIAN_POINT ( 'NONE',  ( 61.62576467234210043, -29.29680953590479930, -16.00589161936969873 ) ) ;
#27844=CARTESIAN_POINT ( 'NONE',  ( 40.74407095721729632, 14.06303216148480040, -5.682177862911860444 ) ) ;
#27845=CARTESIAN_POINT ( 'NONE',  ( 10.37023549284480595, 23.96649136636277078, -45.75009989963381685 ) ) ;
#27846=CARTESIAN_POINT ( 'NONE',  ( 82.61657258396949999, -45.26156352634939850, -47.17378930654930258 ) ) ;
#27851=CARTESIAN_POINT ( 'NONE',  ( 53.17105182305469668, -49.36586906142859732, -27.51403560245880087 ) ) ;
#27852=CARTESIAN_POINT ( 'NONE',  ( 16.08018489229460002, -51.03388179655710388, -20.24577016824899900 ) ) ;
#27855=CARTESIAN_POINT ( 'NONE',  ( 12.16981617636240109, -50.04926268091029584, -21.14999999999999858 ) ) ;
#27856=VECTOR ( 'NONE', #40890, 1000.000000000000114 ) ;
#27857=ORIENTED_EDGE ( 'NONE', *, *, #16854, .F. ) ;
#27862=CARTESIAN_POINT ( 'NONE',  ( 57.37515489807060476, -50.13231850399230183, -52.61654809435920299 ) ) ;
#27863=CARTESIAN_POINT ( 'NONE',  ( 41.99652641013659604, 13.19240707592760131, -5.118462553216080124 ) ) ;
#27866=DIRECTION ( 'NONE',  ( 0.000000000000000000, 0.000000000000000000, -1.000000000000000000 ) ) ;
#27869=CARTESIAN_POINT ( 'NONE',  ( 17.46613192265609982, -52.40466508994180117, -76.02664804518839503 ) ) ;
#27871=DIRECTION ( 'NONE',  ( 0.000000000000000000, -1.000000000000000000, 0.000000000000000000 ) ) ;
#27874=CARTESIAN_POINT ( 'NONE',  ( 8.798174420955659158, 31.95288804203559607, -46.67020513285999783 ) ) ;
#27875=DIRECTION ( 'NONE',  ( 0.000000000000000000, 1.000000000000000000, 0.000000000000000000 ) ) ;
#27878=CARTESIAN_POINT ( 'NONE',  ( 17.71569765418569986, 21.30155813473500004, -76.03742712147929694 ) ) ;
#27881=B_SPLINE_CURVE_WITH_KNOTS ( 'NONE', 3,
 ( #36018, #636, #8511, #4565 ),
 .UNSPECIFIED., .F., .F.,
 ( 4, 4 ),
 ( 1.172395546643479891, 1.281168487042899873 ),
 .UNSPECIFIED. ) ;
#27886=ORIENTED_EDGE ( 'NONE', *, *, #26887, .F. ) ;
#27887=CARTESIAN_POINT ( 'NONE',  ( 12.17742756452222963, 33.84218637042627620, -16.46016917631845544 ) ) ;
#27889=CARTESIAN_POINT ( 'NONE',  ( 72.38393739883420608, 20.38443354211860026, -61.44999999999999574 ) ) ;
#27890=EDGE_CURVE ( 'NONE', #40855, #10739, #3455, .T. ) ;
#27897=CARTESIAN_POINT ( 'NONE',  ( 46.44868656089280279, -53.13167745678150311, -76.13981661584659832 ) ) ;
#27898=CARTESIAN_POINT ( 'NONE',  ( 61.07726573414930016, 14.36074923854380003, -47.64481375401349794 ) ) ;
#27900=CARTESIAN_POINT ( 'NONE',  ( 41.73867462556020058, -43.69499173931319547, -3.496169911638010053 ) ) ;
#27901=CARTESIAN_POINT ( 'NONE',  ( -9.415595612123681235, 12.56745110274309951, -5.921523228984558962 ) ) ;
#27902=EDGE_CURVE ( 'NONE', #10739, #46034, #26400, .T. ) ;
#27904=CARTESIAN_POINT ( 'NONE',  ( 57.84059259261429986, 14.33091246258259943, -26.25095046041350244 ) ) ;
#27906=EDGE_CURVE ( 'NONE', #19736, #19697, #23331, .T. ) ;
#27907=ORIENTED_EDGE ( 'NONE', *, *, #31393, .T. ) ;
#27917=CARTESIAN_POINT ( 'NONE',  ( 47.18305960804269716, 23.57448916799839722, -74.19778952092750046 ) ) ;
#27918=CARTESIAN_POINT ( 'NONE',  ( 48.76647860316090544, -54.05566106471979992, -55.26728053078139880 ) ) ;
#27919=CARTESIAN_POINT ( 'NONE',  ( -11.32734372065470119, 10.64934054434680100, -6.430561461456250072 ) ) ;
#27920=DIRECTION ( 'NONE',  ( -0.7956403955640117820, 0.6057692307692287281, 0.000000000000000000 ) ) ;
#27921=DIRECTION ( 'NONE',  ( -0.8224686640529098591, 0.3976080002595605012, -0.4067593573362696113 ) ) ;
#27926=EDGE_LOOP ( 'NONE', ( #27687, #44983, #26320, #41554 ) ) ;
#27928=CARTESIAN_POINT ( 'NONE',  ( 60.88268456428720299, -45.52259370110750325, -47.42394128263550357 ) ) ;
#27929=CARTESIAN_POINT ( 'NONE',  ( 47.82353814990211305, -54.39218320395424655, -54.71742302521133894 ) ) ;
#27934=CARTESIAN_POINT ( 'NONE',  ( 56.76664444810730714, 19.44233945464240065, -53.84360320705440017 ) ) ;
#27939=CARTESIAN_POINT ( 'NONE',  ( 53.57529274648619122, -50.54592000773362059, -77.11805841020525065 ) ) ;
#27940=CARTESIAN_POINT ( 'NONE',  ( 76.39109092966590708, -16.43866963256245484, -12.75812042950594538 ) ) ;
#27941=ORIENTED_EDGE ( 'NONE', *, *, #3736, .T. ) ;
#27945=DIRECTION ( 'NONE',  ( 0.05355673487304404151, 0.9985648081870993620, 0.000000000000000000 ) ) ;
#27946=AXIS2_PLACEMENT_3D ( 'NONE', #13603, #25623, #28791 ) ;
#27947=ADVANCED_FACE ( 'NONE', ( #16266 ), #32219, .T. ) ;
#27949=CARTESIAN_POINT ( 'NONE',  ( 59.52540514537479766, -1.602101419350890010, -15.86601446510490021 ) ) ;
#27950=CARTESIAN_POINT ( 'NONE',  ( 51.96022949536530433, -49.99701410684310332, -76.69846579631709460 ) ) ;
#27951=ORIENTED_EDGE ( 'NONE', *, *, #41129, .F. ) ;
#27953=CARTESIAN_POINT ( 'NONE',  ( 52.24694037885000597, -49.83134711013449447, -77.11046193146449923 ) ) ;
#27957=CARTESIAN_POINT ( 'NONE',  ( 13.22847210400979812, -50.60300887283339932, -21.36464641127450292 ) ) ;
#27961=CARTESIAN_POINT ( 'NONE',  ( 65.43042069957888884, -49.21324915460513694, -73.25000000000119371 ) ) ;
#27962=DIRECTION ( 'NONE',  ( 0.000000000000000000, 0.000000000000000000, -1.000000000000000000 ) ) ;
#27963=DIRECTION ( 'NONE',  ( 1.000000000000000000, 0.000000000000000000, 0.000000000000000000 ) ) ;
#27966=ORIENTED_EDGE ( 'NONE', *, *, #51758, .F. ) ;
#27968=CARTESIAN_POINT ( 'NONE',  ( 13.76101294176279843, -51.29510989453670078, -74.37030622952929093 ) ) ;
#27969=CARTESIAN_POINT ( 'NONE',  ( 47.21794645697320192, -54.77977332054720705, -54.61771020034730384 ) ) ;
#27970=( NAMED_UNIT ( * ) SI_UNIT ( $, .STERADIAN. ) SOLID_ANGLE_UNIT ( ) );
#27972=CARTESIAN_POINT ( 'NONE',  ( 12.91569276136874578, 34.28022004554033941, -47.73039263111912334 ) ) ;
#27973=CARTESIAN_POINT ( 'NONE',  ( 14.55219295556159409, -51.70197612871098869, -75.56421430877743717 ) ) ;
#27974=CARTESIAN_POINT ( 'NONE',  ( 60.87387793921017476, -45.45198959003565875, -47.10856926084817786 ) ) ;
#27975=CARTESIAN_POINT ( 'NONE',  ( 10.69832412670059973, -64.89277703499729455, -17.91220997211459931 ) ) ;
#27976=CARTESIAN_POINT ( 'NONE',  ( 11.00562562894740104, 33.92899319167229777, -18.07900588225090033 ) ) ;
#27979=CARTESIAN_POINT ( 'NONE',  ( 62.09157612670949788, 1.883811055320649963, -65.34607522167520699 ) ) ;
#27980=CARTESIAN_POINT ( 'NONE',  ( 14.63258269449462823, -51.92835184173312513, -75.76245441609269449 ) ) ;
#27982=DIRECTION ( 'NONE',  ( 0.000000000000000000, -1.000000000000000000, 0.000000000000000000 ) ) ;
#27983=CARTESIAN_POINT ( 'NONE',  ( 49.60654698967459808, 22.46544607396180027, -55.15184126837920076 ) ) ;
#27985=CARTESIAN_POINT ( 'NONE',  ( 53.33273182090660214, -49.45495365240509500, -49.10545207584610239 ) ) ;
#27989=DIRECTION ( 'NONE',  ( 1.000000000000000000, 0.000000000000000000, 0.000000000000000000 ) ) ;
#27990=CARTESIAN_POINT ( 'NONE',  ( 82.84359872746441056, 13.83656922206100148, -46.75796921614900015 ) ) ;
#27991=CARTESIAN_POINT ( 'NONE',  ( 53.68517931677009614, 17.65142714004119995, -27.10739793169170042 ) ) ;
#27993=CARTESIAN_POINT ( 'NONE',  ( 52.71325193919590646, 18.52215315012190189, -48.80820480602550049 ) ) ;
#27994=CARTESIAN_POINT ( 'NONE',  ( 56.98602282141720110, -45.17932660430339808, -17.93020264185449975 ) ) ;
#27998=ORIENTED_EDGE ( 'NONE', *, *, #35846, .T. ) ;
#27999=CARTESIAN_POINT ( 'NONE',  ( 11.69717491040810131, -65.38668361297489184, -17.57872635863940403 ) ) ;
#28000=CARTESIAN_POINT ( 'NONE',  ( 10.66723504149939927, 32.23676291041770270, -45.40177853144560061 ) ) ;
#28001=CARTESIAN_POINT ( 'NONE',  ( -2.765096767708109748, -50.45527968746931435, -9.880994752627875855 ) ) ;
#28003=CARTESIAN_POINT ( 'NONE',  ( 11.22148308022864072, -65.11920307228105287, -22.94887291969233090 ) ) ;
#28004=CARTESIAN_POINT ( 'NONE',  ( 51.34655038886756273, 3.358464191959859679, -76.64437763193187436 ) ) ;
#28005=VERTEX_POINT ( 'NONE', #51149 ) ;
#28006=CARTESIAN_POINT ( 'NONE',  ( 13.58165716955151403, 20.15897125721314254, -22.62650420658231099 ) ) ;
#28007=CARTESIAN_POINT ( 'NONE',  ( 11.10564815319149901, -63.39283105347629999, -44.25602923368459329 ) ) ;
#28008=ADVANCED_FACE ( 'NONE', ( #15504 ), #19680, .T. ) ;
#28009=CARTESIAN_POINT ( 'NONE',  ( 68.13393739769810509, 19.38381105532030091, -71.50000000000198952 ) ) ;
#28011=CARTESIAN_POINT ( 'NONE',  ( 11.55362728243429160, -64.75226678741590547, -44.82234525104323097 ) ) ;
#28012=CARTESIAN_POINT ( 'NONE',  ( 56.52076750121499771, 19.52121317428709801, -53.72896418895009418 ) ) ;
#28013=CARTESIAN_POINT ( 'NONE',  ( 13.80798414608321067, -52.11463163829730405, -75.47165350121231597 ) ) ;
#28015=VERTEX_POINT ( 'NONE', #15755 ) ;
#28018=CARTESIAN_POINT ( 'NONE',  ( 68.13393739769620083, -50.61618894467930119, -65.65000000000000568 ) ) ;
#28020=FACE_OUTER_BOUND ( 'NONE', #15361, .T. ) ;
#28021=ADVANCED_FACE ( 'NONE', ( #31458 ), #31709, .F. ) ;
#28025=CARTESIAN_POINT ( 'NONE',  ( 56.43686078178020438, 19.54004972588730027, -74.42959766581059000 ) ) ;
#28027=EDGE_LOOP ( 'NONE', ( #33017, #20392, #27244, #42543, #26438 ) ) ;
#28029=ADVANCED_FACE ( 'NONE', ( #33005 ), #21332, .T. ) ;
#28032=CARTESIAN_POINT ( 'NONE',  ( 47.00520813701670164, 22.91485595127299746, -75.60950524211389734 ) ) ;
#28035=CARTESIAN_POINT ( 'NONE',  ( 57.26570439199549867, 16.10442508092609870, -47.75313496841199878 ) ) ;
#28036=CARTESIAN_POINT ( 'NONE',  ( 12.07459604305180001, 33.59801851824129670, -16.11467485432109825 ) ) ;
#28038=CARTESIAN_POINT ( 'NONE',  ( 56.07071590434600239, -50.62114172542430168, -75.80509802105420647 ) ) ;
#28039=CARTESIAN_POINT ( 'NONE',  ( -11.08670663458990013, 10.41904260857310049, -5.029111395560210696 ) ) ;
#28042=CARTESIAN_POINT ( 'NONE',  ( 61.25723346457989749, 14.07825924033359932, -47.12448165822169699 ) ) ;
#28044=EDGE_LOOP ( 'NONE', ( #17394, #42546, #31125, #5315 ) ) ;
#28045=CARTESIAN_POINT ( 'NONE',  ( 52.89416330280510437, -49.62717582914000047, -48.70339649242369973 ) ) ;
#28046=ADVANCED_FACE ( 'NONE', ( #11254 ), #23528, .T. ) ;
#28047=CARTESIAN_POINT ( 'NONE',  ( 60.27964521196050640, -45.35349871132130062, -26.98636702841220014 ) ) ;
#28050=CARTESIAN_POINT ( 'NONE',  ( 56.48064340649460746, 14.96064364930199986, -26.24823062834149923 ) ) ;
#28052=B_SPLINE_CURVE_WITH_KNOTS ( 'NONE', 3,
 ( #20058, #24488, #20568, #36049, #12213, #28174, #24752, #40762, #44177, #16928, #48904, #33916, #49933, #22385, #17437, #21867 ),
 .UNSPECIFIED., .F., .F.,
 ( 4, 2, 2, 2, 2, 2, 2, 4 ),
 ( -4.238728275518850452, -3.233993249338640297, -2.649205172199279978, -2.119364137759419897, -1.854443620539500071, -1.430570792987610140, -0.7523742689045951337, 0.000000000000000000 ),
 .UNSPECIFIED. ) ;
#28053=CARTESIAN_POINT ( 'NONE',  ( 50.58622399142209503, 17.63286775605750023, -76.21981748726690853 ) ) ;
#28054=CARTESIAN_POINT ( 'NONE',  ( 52.76678674812239933, 18.46451123677829997, -48.54390573034589806 ) ) ;
#28060=CARTESIAN_POINT ( 'NONE',  ( 47.61809482659410264, -54.54244161261100032, -55.01024658974859705 ) ) ;
#28061=CARTESIAN_POINT ( 'NONE',  ( 11.89321781986642002, -65.43603095096219135, -18.08603052201254968 ) ) ;
#28062=CARTESIAN_POINT ( 'NONE',  ( 61.50409964634459925, -45.37406455498979341, -47.35437808299670337 ) ) ;
#28063=CARTESIAN_POINT ( 'NONE',  ( 61.49111717500029783, -30.75662150461740296, -16.40374446335560066 ) ) ;
#28067=LINE ( 'NONE', #20208, #2517 ) ;
#28069=B_SPLINE_CURVE_WITH_KNOTS ( 'NONE', 3,
 ( #11048, #10790, #35135, #18639, #23072, #15235 ),
 .UNSPECIFIED., .F., .F.,
 ( 4, 1, 1, 4 ),
 ( 0.000000000000000000, 0.3333333141630762109, 0.6666666280596336147, 1.000000000000000000 ),
 .UNSPECIFIED. ) ;
#28071=ORIENTED_EDGE ( 'NONE', *, *, #42131, .F. ) ;
#28073=LINE ( 'NONE', #43825, #26893 ) ;
#28075=CARTESIAN_POINT ( 'NONE',  ( 57.00424200505899819, -45.17895554415359527, -25.30170080014089962 ) ) ;
#28076=CARTESIAN_POINT ( 'NONE',  ( 87.61621807841599718, -33.11618894467940066, -61.12885639714370001 ) ) ;
#28078=CARTESIAN_POINT ( 'NONE',  ( 51.67587649748470113, 2.735120682347050192, -77.01363636363508647 ) ) ;
#28082=ADVANCED_FACE ( 'NONE', ( #30881 ), #49409, .T. ) ;
#28084=AXIS2_PLACEMENT_3D ( 'NONE', #43796, #8662, #21475 ) ;
#28087=ORIENTED_EDGE ( 'NONE', *, *, #47600, .T. ) ;
#28091=CARTESIAN_POINT ( 'NONE',  ( 41.00662729433690146, 13.77143252834769882, -5.555595257260869779 ) ) ;
#28092=CIRCLE ( 'NONE', #3836, 2.000000000000000000 ) ;
#28093=CARTESIAN_POINT ( 'NONE',  ( 14.75122413114260134, 21.64019965034979975, -76.12465403027070465 ) ) ;
#28095=CARTESIAN_POINT ( 'NONE',  ( 84.44784216359251161, -43.11618894467930119, -47.47585302082339354 ) ) ;
#28098=ORIENTED_EDGE ( 'NONE', *, *, #23885, .T. ) ;
#28099=CARTESIAN_POINT ( 'NONE',  ( 54.98660006789570076, -47.35355536850440217, -26.27416394216670170 ) ) ;
#28100=CARTESIAN_POINT ( 'NONE',  ( 15.80830505657519680, -50.93044242254529763, -20.14990715359089890 ) ) ;
#28101=CARTESIAN_POINT ( 'NONE',  ( 50.89766658690811596, -35.40215446828276669, -76.34789914821418222 ) ) ;
#28104=CARTESIAN_POINT ( 'NONE',  ( 12.69633964705789886, -49.98156587680259832, -21.09933892968020075 ) ) ;
#28105=ORIENTED_EDGE ( 'NONE', *, *, #17837, .T. ) ;
#28107=CARTESIAN_POINT ( 'NONE',  ( 47.23649938924289415, 23.53374381085950162, -54.66384524898040098 ) ) ;
#28109=EDGE_CURVE ( 'NONE', #42834, #10465, #2810, .T. ) ;
#28110=DIRECTION ( 'NONE',  ( -1.000000000000000000, 0.000000000000000000, 0.000000000000000000 ) ) ;
#28112=CARTESIAN_POINT ( 'NONE',  ( 57.36541752560179930, -50.23213309141979721, -52.73855437091509657 ) ) ;
#28113=CARTESIAN_POINT ( 'NONE',  ( 43.19833518328499622, 12.57157279091759960, -5.006617643082219793 ) ) ;
#28114=CARTESIAN_POINT ( 'NONE',  ( 68.13393739769630031, 16.88381105532302939, -68.79999999999976978 ) ) ;
#28115=CARTESIAN_POINT ( 'NONE',  ( 70.17820777451849779, -45.11618894467940066, -13.95197280571250076 ) ) ;
#28116=DIRECTION ( 'NONE',  ( -1.000000000000000000, 0.000000000000000000, 0.000000000000000000 ) ) ;
#28118=EDGE_CURVE ( 'NONE', #19396, #49606, #11191, .T. ) ;
#28125=VERTEX_POINT ( 'NONE', #19298 ) ;
#28130=VERTEX_POINT ( 'NONE', #47357 ) ;
#28131=CARTESIAN_POINT ( 'NONE',  ( 17.81078732947910126, 21.37421319461290281, -76.02269426304029309 ) ) ;
#28132=VECTOR ( 'NONE', #15536, 1000.000000000000000 ) ;
#28133=ORIENTED_EDGE ( 'NONE', *, *, #12114, .T. ) ;
#28135=CARTESIAN_POINT ( 'NONE',  ( 56.52347729570519874, -46.24434533601050390, -26.27197595876690173 ) ) ;
#28144=AXIS2_PLACEMENT_3D ( 'NONE', #41529, #17686, #29975 ) ;
#28145=DIRECTION ( 'NONE',  ( -1.000000000000000000, 6.785502314117012559E-28, 1.822422554782380175E-11 ) ) ;
#28146=ORIENTED_EDGE ( 'NONE', *, *, #39645, .F. ) ;
#28149=CYLINDRICAL_SURFACE ( 'NONE', #21716, 1.999999999999998224 ) ;
#28150=CARTESIAN_POINT ( 'NONE',  ( 61.01489880521270237, 14.38000684155560016, -47.65651487079679782 ) ) ;
#28151=CONICAL_SURFACE ( 'NONE', #44071, 3.118521338338071214, 0.6364736820000767015 ) ;
#28154=CARTESIAN_POINT ( 'NONE',  ( -6.434752379702439740, 14.95818219322160125, -4.725866882124770463 ) ) ;
#28155=CARTESIAN_POINT ( 'NONE',  ( 47.14848705314030042, 23.49639263515488707, -74.72737448321004194 ) ) ;
#28157=CARTESIAN_POINT ( 'NONE',  ( 58.30601965111470264, 14.38410068486810012, -26.39168729330650010 ) ) ;
#28159=EDGE_LOOP ( 'NONE', ( #7541, #1604, #42974, #47015 ) ) ;
#28163=CARTESIAN_POINT ( 'NONE',  ( 12.04090198330849937, 33.96751094239839830, -45.84253678965290391 ) ) ;
#28167=CARTESIAN_POINT ( 'NONE',  ( 47.18323849499689970, 23.57489303030209982, -74.17387246174169491 ) ) ;
#28168=CARTESIAN_POINT ( 'NONE',  ( 48.59292341170780105, -54.12958895873340026, -55.31326040662610666 ) ) ;
#28169=DIRECTION ( 'NONE',  ( -1.000000000000000000, 0.000000000000000000, 0.000000000000000000 ) ) ;
#28172=FACE_OUTER_BOUND ( 'NONE', #26127, .T. ) ;
#28174=CARTESIAN_POINT ( 'NONE',  ( 56.78179639309170312, 13.88381105532070059, -15.59568127148800087 ) ) ;
#28176=ORIENTED_EDGE ( 'NONE', *, *, #12656, .F. ) ;
#28181=CARTESIAN_POINT ( 'NONE',  ( 60.92563286722050009, -45.50374237643139708, -47.41214175719230184 ) ) ;
#28183=CARTESIAN_POINT ( 'NONE',  ( 57.24929578234380045, 19.38381105828390361, -53.91492796160409284 ) ) ;
#28189=ORIENTED_EDGE ( 'NONE', *, *, #12918, .T. ) ;
#28190=CARTESIAN_POINT ( 'NONE',  ( 82.75388200178990417, -45.59495393102269389, -47.67228907607359645 ) ) ;
#28191=ORIENTED_EDGE ( 'NONE', *, *, #554, .F. ) ;
#28196=CARTESIAN_POINT ( 'NONE',  ( 76.40923666012143656, -10.47647217757513793, -12.83630549532472820 ) ) ;
#28197=CARTESIAN_POINT ( 'NONE',  ( 53.59017120079079888, -51.78138378941920195, -53.35603438827740064 ) ) ;
#28198=AXIS2_PLACEMENT_3D ( 'NONE', #18532, #34506, #50513 ) ;
#28203=CARTESIAN_POINT ( 'NONE',  ( 56.92280486547669938, -45.20348458963250238, -25.29907664449969928 ) ) ;
#28204=CARTESIAN_POINT ( 'NONE',  ( 56.28151583052680706, -50.59316951485450176, -52.90568346777400421 ) ) ;
#28205=CARTESIAN_POINT ( 'NONE',  ( 8.784728771177240603, -63.11543068614769680, -46.67204636144870022 ) ) ;
#28209=ORIENTED_EDGE ( 'NONE', *, *, #12829, .F. ) ;
#28211=CARTESIAN_POINT ( 'NONE',  ( 53.19378597440579881, -50.43795885268350787, -77.11066259967179803 ) ) ;
#28212=CARTESIAN_POINT ( 'NONE',  ( 60.27360767123090568, 14.56433066022204770, -47.49318409392830631 ) ) ;
#28215=CARTESIAN_POINT ( 'NONE',  ( 12.61047097489570135, -50.09335168391980631, -21.13759556400450279 ) ) ;
#28219=CARTESIAN_POINT ( 'NONE',  ( 57.39341912848639993, 13.88381105532070059, -16.95659913784360029 ) ) ;
#28221=B_SPLINE_CURVE_WITH_KNOTS ( 'NONE', 3,
 ( #27535, #16008, #51147, #23081 ),
 .UNSPECIFIED., .F., .F.,
 ( 4, 4 ),
 ( 0.000000000000000000, 1.000000000000000000 ),
 .UNSPECIFIED. ) ;
#28224=DIRECTION ( 'NONE',  ( 1.000000000000000000, 0.000000000000000000, 0.000000000000000000 ) ) ;
#28226=CARTESIAN_POINT ( 'NONE',  ( 47.23343139436899918, 22.78429295813339905, -75.61476957854540615 ) ) ;
#28227=CARTESIAN_POINT ( 'NONE',  ( 47.40958959913769633, -54.64515405761270017, -54.70637844396050298 ) ) ;
#28233=CARTESIAN_POINT ( 'NONE',  ( 21.78494278233659998, -33.82423023735729828, -74.14999999999999147 ) ) ;
#28234=DIRECTION ( 'NONE',  ( -1.878694634646244452E-12, -5.875576256101890322E-05, 0.9999999982738801974 ) ) ;
#28237=EDGE_CURVE ( 'NONE', #9060, #6692, #48637, .T. ) ;
#28238=CIRCLE ( 'NONE', #47538, 3.000000000000003109 ) ;
#28239=CARTESIAN_POINT ( 'NONE',  ( -4.193170025096960352, -49.34067901558599800, -7.780630217993570241 ) ) ;
#28240=CARTESIAN_POINT ( 'NONE',  ( 48.47823774206090519, 22.94606279175510011, -55.31601837894829998 ) ) ;
#28242=CARTESIAN_POINT ( 'NONE',  ( 52.86566477306229928, -49.66304969232309929, -48.91558077290370221 ) ) ;
#28246=CYLINDRICAL_SURFACE ( 'NONE', #47179, 40.00000000000000000 ) ;
#28247=CARTESIAN_POINT ( 'NONE',  ( 83.84636189228659475, 13.10553490620129935, -46.70679156566500012 ) ) ;
#28248=CARTESIAN_POINT ( 'NONE',  ( 56.12979400316489631, 14.82013761545010055, -26.01948386542559888 ) ) ;
#28250=CARTESIAN_POINT ( 'NONE',  ( 52.66149042093859123, 18.55528232251300125, -48.73886901161859697 ) ) ;
#28251=CARTESIAN_POINT ( 'NONE',  ( 56.87874324233769840, -45.12877571808259347, -16.32799602576229958 ) ) ;
#28252=DIRECTION ( 'NONE',  ( -0.1175431456444872985, -0.8277005620457519308, -0.5487215947100543278 ) ) ;
#28255=ORIENTED_EDGE ( 'NONE', *, *, #7759, .T. ) ;
#28256=CARTESIAN_POINT ( 'NONE',  ( 12.04669084400330092, -65.33956968768698914, -17.12210552323070090 ) ) ;
#28257=CARTESIAN_POINT ( 'NONE',  ( 11.70044915406800001, 33.92707456368980701, -46.82636340333009883 ) ) ;
#28259=CARTESIAN_POINT ( 'NONE',  ( 48.22648091640650136, -53.97280751374249519, -53.84476208330389824 ) ) ;
#28260=CARTESIAN_POINT ( 'NONE',  ( 8.784728771177219286, 31.88305279678909443, -46.67204636144870022 ) ) ;
#28262=ORIENTED_EDGE ( 'NONE', *, *, #11733, .T. ) ;
#28264=CARTESIAN_POINT ( 'NONE',  ( 11.13393739769619906, -63.34493739649700927, -43.91716459650320559 ) ) ;
#28269=CARTESIAN_POINT ( 'NONE',  ( 51.02818947082050016, -50.88302571328060253, -76.14999999999999147 ) ) ;
#28272=ORIENTED_EDGE ( 'NONE', *, *, #28237, .T. ) ;
#28280=DIRECTION ( 'NONE',  ( 0.000000000000000000, 0.000000000000000000, 1.000000000000000000 ) ) ;
#28282=EDGE_LOOP ( 'NONE', ( #30786, #46588, #43756, #8766 ) ) ;
#28285=CARTESIAN_POINT ( 'NONE',  ( 12.29223489819977821, 34.10423391560534156, -23.62127221463904547 ) ) ;
#28286=CARTESIAN_POINT ( 'NONE',  ( 47.13612099939350486, 23.16257524069679974, -75.29255935572381020 ) ) ;
#28288=DIRECTION ( 'NONE',  ( 0.000000000000000000, -1.000000000000000000, 0.000000000000000000 ) ) ;
#28291=CARTESIAN_POINT ( 'NONE',  ( 57.21097685450429537, -50.61618800939579899, -74.14879615022279324 ) ) ;
#28292=LINE ( 'NONE', #44819, #45806 ) ;
#28294=EDGE_CURVE ( 'NONE', #9275, #12303, #28052, .T. ) ;
#28296=CARTESIAN_POINT ( 'NONE',  ( 61.38286689828800036, 13.95525073026689888, -46.52105988975220185 ) ) ;
#28298=CARTESIAN_POINT ( 'NONE',  ( -0.2991137081908959994, -62.12324524158640315, -48.78634498590130164 ) ) ;
#28300=ORIENTED_EDGE ( 'NONE', *, *, #21617, .F. ) ;
#28301=CARTESIAN_POINT ( 'NONE',  ( 52.85165694913099799, -49.64944609877660042, -48.64955875961400267 ) ) ;
#28304=CARTESIAN_POINT ( 'NONE',  ( 61.14783123884740235, -45.23924466744810502, -27.62102214444609771 ) ) ;
#28305=CARTESIAN_POINT ( 'NONE',  ( 37.33393739769619657, -15.61618894467929941, -11.54999999999999893 ) ) ;
#28306=CARTESIAN_POINT ( 'NONE',  ( 56.33185943253500483, 14.93937505072510064, -26.19910003242920027 ) ) ;
#28307=VECTOR ( 'NONE', #14711, 1000.000000000000000 ) ;
#28310=CARTESIAN_POINT ( 'NONE',  ( 50.81500901600419695, 18.46718465057229963, -76.22412500802471413 ) ) ;
#28311=CARTESIAN_POINT ( 'NONE',  ( 52.83030979110780123, 18.43029764974290075, -48.71029753094079950 ) ) ;
#28313=DIRECTION ( 'NONE',  ( -0.000000000000000000, 1.000000000000000000, 0.000000000000000000 ) ) ;
#28316=CARTESIAN_POINT ( 'NONE',  ( 47.66097882627480686, -54.52613192741829096, -55.10530119525199666 ) ) ;
#28318=CARTESIAN_POINT ( 'NONE',  ( 58.92073396209919878, -28.11618894467929763, -18.64999999999999858 ) ) ;
#28319=CARTESIAN_POINT ( 'NONE',  ( 57.65805802474199737, 18.65029578125960086, -52.34980151920610325 ) ) ;
#28326=ORIENTED_EDGE ( 'NONE', *, *, #38814, .T. ) ;
#28327=VERTEX_POINT ( 'NONE', #29726 ) ;
#28329=CARTESIAN_POINT ( 'NONE',  ( 49.85658880370656476, -29.63768744850618475, -15.88711799670739921 ) ) ;
#28332=CARTESIAN_POINT ( 'NONE',  ( 57.22943158897479776, -45.13409722695310222, -25.31259632064490006 ) ) ;
#28335=DIRECTION ( 'NONE',  ( 0.000000000000000000, 0.000000000000000000, 1.000000000000000000 ) ) ;
#28342=CARTESIAN_POINT ( 'NONE',  ( 10.64252135837869950, -63.58685848925379958, -23.65858396068239955 ) ) ;
#28346=AXIS2_PLACEMENT_3D ( 'NONE', #18892, #37332, #17420 ) ;
#28348=CONICAL_SURFACE ( 'NONE', #22516, 1.587553672713209574, 1.249045772398249987 ) ;
#28350=CARTESIAN_POINT ( 'NONE',  ( 13.87433288923529950, 20.87662390947729918, -75.53341961486960088 ) ) ;
#28356=CARTESIAN_POINT ( 'NONE',  ( 56.05191282448750201, -45.91615162336719891, -25.80821051545110123 ) ) ;
#28357=B_SPLINE_CURVE_WITH_KNOTS ( 'NONE', 3,
 ( #8885, #17012, #45041, #29045, #36639, #9140, #44518, #28781, #40584, #4682, #24837 ),
 .UNSPECIFIED., .F., .F.,
 ( 4, 1, 1, 1, 1, 1, 1, 1, 4 ),
 ( 0.000000000000000000, 0.1249968820770194777, 0.2499966053408283206, 0.3749963286046372191, 0.4999960518684460342, 0.6249957751322549049, 0.7499954983960637200, 0.8749952216598726462, 1.000000000000000000 ),
 .UNSPECIFIED. ) ;
#28358=CARTESIAN_POINT ( 'NONE',  ( 15.80832228677149942, -50.93044681828930464, -20.21644471496500017 ) ) ;
#28359=CARTESIAN_POINT ( 'NONE',  ( 57.32828653034189870, 19.18168419026400073, -53.00038473087150237 ) ) ;
#28360=CARTESIAN_POINT ( 'NONE',  ( 75.47577596059235816, 12.24922386242644023, -13.41863335767928334 ) ) ;
#28361=CARTESIAN_POINT ( 'NONE',  ( 13.73527022026340028, -50.20735447812900532, -20.93080062776369843 ) ) ;
#28365=CARTESIAN_POINT ( 'NONE',  ( 47.32528955519509850, 23.46751979651900299, -54.64535935344500217 ) ) ;
#28369=CARTESIAN_POINT ( 'NONE',  ( 41.23309865046339695, 13.48886119783190018, -5.265645747893129780 ) ) ;
#28374=CARTESIAN_POINT ( 'NONE',  ( 58.40467996479630131, -46.88273201699870185, -48.03872346596099874 ) ) ;
#28377=CARTESIAN_POINT ( 'NONE',  ( 56.46551568209640237, 19.54378693895939989, -53.85224189773119718 ) ) ;
#28379=VECTOR ( 'NONE', #47203, 1000.000000000000227 ) ;
#28381=EDGE_LOOP ( 'NONE', ( #42048, #748, #3551, #26579 ) ) ;
#28383=CARTESIAN_POINT ( 'NONE',  ( 9.281825854502979922, 31.93825977863309973, -46.53126684085379594 ) ) ;
#28388=CARTESIAN_POINT ( 'NONE',  ( 17.78605519637239851, 20.27135023148479576, -75.33782839756391070 ) ) ;
#28393=EDGE_CURVE ( 'NONE', #10857, #4677, #26479, .T. ) ;
#28397=CARTESIAN_POINT ( 'NONE',  ( 61.75019864826120397, 13.88381105542450022, -46.37201226983719948 ) ) ;
#28405=VERTEX_POINT ( 'NONE', #37351 ) ;
#28408=CARTESIAN_POINT ( 'NONE',  ( 60.72740590574490227, 14.39261883701170142, -47.54234311855110207 ) ) ;
#28409=ADVANCED_FACE ( 'NONE', ( #6427 ), #5654, .F. ) ;
#28410=EDGE_CURVE ( 'NONE', #5215, #46792, #2489, .T. ) ;
#28411=CARTESIAN_POINT ( 'NONE',  ( 54.17079961804279975, 14.38146746993139935, -15.02185247389039979 ) ) ;
#28413=CARTESIAN_POINT ( 'NONE',  ( -9.468778084194710232, 12.47338336425449867, -5.557361635588190296 ) ) ;
#28417=CARTESIAN_POINT ( 'NONE',  ( 10.37125623313378497, 23.96744338674034935, -21.14999999999999858 ) ) ;
#28418=CARTESIAN_POINT ( 'NONE',  ( 59.47927764971650078, 14.15550012739879904, -26.60797151098220326 ) ) ;
#28419=CIRCLE ( 'NONE', #5855, 1.999999999999997558 ) ;
#28422=CARTESIAN_POINT ( 'NONE',  ( 55.13210266565960893, 17.31833316781790089, -48.68958776747170702 ) ) ;
#28423=CARTESIAN_POINT ( 'NONE',  ( 41.56838531616119781, 14.44787509676280024, -6.472129036803299762 ) ) ;
#28425=CARTESIAN_POINT ( 'NONE',  ( 54.08397353797261786, -50.62656311257075714, -76.77908082735504536 ) ) ;
#28428=ADVANCED_FACE ( 'NONE', ( #2231 ), #41537, .T. ) ;
#28429=DIRECTION ( 'NONE',  ( 0.000000000000000000, 0.000000000000000000, -1.000000000000000000 ) ) ;
#28430=EDGE_CURVE ( 'NONE', #25775, #17902, #18046, .T. ) ;
#28431=CARTESIAN_POINT ( 'NONE',  ( 46.46557555578730359, 21.92956842995989675, -76.13729948603509001 ) ) ;
#28432=CARTESIAN_POINT ( 'NONE',  ( 49.09311242517659934, -53.78968938430409708, -54.56531883649019932 ) ) ;
#28437=ORIENTED_EDGE ( 'NONE', *, *, #46645, .T. ) ;
#28442=CARTESIAN_POINT ( 'NONE',  ( 60.72928671769479791, -45.53983519128849622, -47.27644420220809707 ) ) ;
#28447=DIRECTION ( 'NONE',  ( -1.000000000000000000, 0.000000000000000000, 0.000000000000000000 ) ) ;
#28449=ORIENTED_EDGE ( 'NONE', *, *, #5914, .F. ) ;
#28450=CARTESIAN_POINT ( 'NONE',  ( 84.09627682649329472, -44.51519333368669606, -47.44643906338429673 ) ) ;
#28452=EDGE_LOOP ( 'NONE', ( #30029, #20126, #9850, #49498 ) ) ;
#28456=CARTESIAN_POINT ( 'NONE',  ( 52.26504646883520167, -49.78354544620959388, -77.19463087837650050 ) ) ;
#28457=VECTOR ( 'NONE', #42709, 1000.000000000000000 ) ;
#28458=CARTESIAN_POINT ( 'NONE',  ( 76.40827150342700236, -20.78360806407327743, -12.83216708051279653 ) ) ;
#28459=CARTESIAN_POINT ( 'NONE',  ( 50.25479149875150142, -53.19950294433710525, -54.04777103931960625 ) ) ;
#28460=VECTOR ( 'NONE', #31225, 1000.000000000000000 ) ;
#28461=ORIENTED_EDGE ( 'NONE', *, *, #22695, .F. ) ;
#28463=CIRCLE ( 'NONE', #48537, 15.56227766016840164 ) ;
#28464=AXIS2_PLACEMENT_3D ( 'NONE', #48214, #32444, #12314 ) ;
#28465=CARTESIAN_POINT ( 'NONE',  ( 48.03928511041160476, 23.04428228824039948, -54.71294081448219515 ) ) ;
#28468=DIRECTION ( 'NONE',  ( -0.000000000000000000, -0.000000000000000000, -1.000000000000000000 ) ) ;
#28471=B_SPLINE_CURVE_WITH_KNOTS ( 'NONE', 3,
 ( #29519, #14576, #25826, #30541, #37648, #10135, #26350, #1497, #26612, #42362 ),
 .UNSPECIFIED., .F., .F.,
 ( 4, 2, 2, 2, 4 ),
 ( 0.000000000000000000, 0.1746266369381154759, 0.6794498943083844278, 0.9949644301648022937, 1.000000000000000000 ),
 .UNSPECIFIED. ) ;
#28474=CARTESIAN_POINT ( 'NONE',  ( 52.26113438680789613, -49.98075224355449819, -76.96437239583239887 ) ) ;
#28480=CARTESIAN_POINT ( 'NONE',  ( 42.16594882433619773, -43.97269357279350288, -4.735301442609650024 ) ) ;
#28481=CARTESIAN_POINT ( 'NONE',  ( 18.40646359431065449, -51.24009245543214774, -15.69870911006933767 ) ) ;
#28482=EDGE_CURVE ( 'NONE', #48450, #18259, #21424, .T. ) ;
#28483=AXIS2_PLACEMENT_3D ( 'NONE', #17484, #34212, #41844 ) ;
#28484=CARTESIAN_POINT ( 'NONE',  ( 66.72561048563099462, 1.883811055320649963, -20.64999999980150136 ) ) ;
#28489=CARTESIAN_POINT ( 'NONE',  ( 14.47398509914520126, -51.62356816798740056, -75.48775473117470369 ) ) ;
#28490=CARTESIAN_POINT ( 'NONE',  ( 47.37754115064079485, -54.66825602412330198, -54.73097957181000339 ) ) ;
#28492=CIRCLE ( 'NONE', #22621, 15.24604989415149703 ) ;
#28493=CARTESIAN_POINT ( 'NONE',  ( 10.97012820822068058, 33.88053142170652166, -47.22757037140836189 ) ) ;
#28495=CARTESIAN_POINT ( 'NONE',  ( 60.98630419630155330, -45.44769370713505907, -47.30728599211079910 ) ) ;
#28496=CARTESIAN_POINT ( 'NONE',  ( 55.58073395081326851, -45.98461186095343578, -16.80393320440050076 ) ) ;
#28498=ADVANCED_FACE ( 'NONE', ( #50959 ), #41442, .T. ) ;
#28500=CYLINDRICAL_SURFACE ( 'NONE', #46608, 38.00000000000000711 ) ;
#28501=CARTESIAN_POINT ( 'NONE',  ( -4.162377065922562736, -48.30017088459130292, -5.617364974929863308 ) ) ;
#28502=CARTESIAN_POINT ( 'NONE',  ( 16.13393761331730047, -15.61618923485050026, -20.64999983909400072 ) ) ;
#28503=CARTESIAN_POINT ( 'NONE',  ( 48.81893253562370205, 22.77627760781700061, -54.98725303027700306 ) ) ;
#28504=ORIENTED_EDGE ( 'NONE', *, *, #51637, .T. ) ;
#28506=B_SPLINE_CURVE_WITH_KNOTS ( 'NONE', 3,
 ( #42775, #2156, #38844, #35143, #22823, #34624, #2933, #18136, #38317, #23082, #22309, #2405, #50628, #18903, #50887, #6874 ),
 .UNSPECIFIED., .F., .F.,
 ( 4, 2, 2, 2, 2, 2, 2, 4 ),
 ( 0.000000000000000000, 0.1750000000000006828, 0.3750000000000011102, 0.5000000000000003331, 0.5625000000000003331, 0.6625000000000006439, 0.8225000000000002309, 1.000000000000000000 ),
 .UNSPECIFIED. ) ;
#28507=VERTEX_POINT ( 'NONE', #797 ) ;
#28511=CARTESIAN_POINT ( 'NONE',  ( 83.45566905280598746, 13.44200627990649899, -46.48561260377739757 ) ) ;
#28512=CARTESIAN_POINT ( 'NONE',  ( 54.39595473835359485, 16.76334922740620215, -26.49617834758590007 ) ) ;
#28514=CARTESIAN_POINT ( 'NONE',  ( 52.95065142214180298, 18.41081157851500194, -49.05053735721260466 ) ) ;
#28515=CARTESIAN_POINT ( 'NONE',  ( 56.39822365214870104, -45.27769210685230661, -16.54940569508480053 ) ) ;
#28517=ORIENTED_EDGE ( 'NONE', *, *, #23237, .T. ) ;
#28519=CARTESIAN_POINT ( 'NONE',  ( 11.92234616936549862, -65.02420767682468750, -16.43998781665510123 ) ) ;
#28520=CARTESIAN_POINT ( 'NONE',  ( 10.63343953641030026, 32.99774508120760430, -46.06167227688830224 ) ) ;
#28521=CARTESIAN_POINT ( 'NONE',  ( 18.58015777933965751, 20.12863169291996712, -15.71908887857641623 ) ) ;
#28522=CARTESIAN_POINT ( 'NONE',  ( 51.93112808046510054, -50.81522873917079863, -50.63472941081700185 ) ) ;
#28523=CARTESIAN_POINT ( 'NONE',  ( 11.57443829055679352, -65.35522060805175215, -22.57612245162195208 ) ) ;
#28526=CARTESIAN_POINT ( 'NONE',  ( 66.63393739769620083, 11.88381105532070059, -71.50000000000000000 ) ) ;
#28527=CARTESIAN_POINT ( 'NONE',  ( 11.13393739769619906, -63.39706025650779253, -43.75139571400850258 ) ) ;
#28528=CARTESIAN_POINT ( 'NONE',  ( 13.67087992646597527, 20.77208395194776713, -75.25166008038891619 ) ) ;
#28530=CARTESIAN_POINT ( 'NONE',  ( 50.38251485953870201, -49.88132833114089948, -76.14999999999999147 ) ) ;
#28532=AXIS2_PLACEMENT_3D ( 'NONE', #3077, #6751, #14084 ) ;
#28533=EDGE_LOOP ( 'NONE', ( #47576, #24108, #48388, #20062 ) ) ;
#28537=CARTESIAN_POINT ( 'NONE',  ( 52.60283376768439467, 22.91519262962889769, -56.84002502892810327 ) ) ;
#28538=AXIS2_PLACEMENT_3D ( 'NONE', #44857, #29116, #1084 ) ;
#28540=EDGE_CURVE ( 'NONE', #34565, #12115, #45526, .T. ) ;
#28541=CARTESIAN_POINT ( 'NONE',  ( 10.62805030875319012, -55.23623230473515378, -21.20049831036011412 ) ) ;
#28542=CARTESIAN_POINT ( 'NONE',  ( 54.85910183373169247, 19.81893354343910119, -75.32013207243669228 ) ) ;
#28544=CARTESIAN_POINT ( 'NONE',  ( 47.19371938996459903, -54.14421669766970524, -75.51723258725520793 ) ) ;
#28545=ORIENTED_EDGE ( 'NONE', *, *, #31291, .F. ) ;
#28548=CARTESIAN_POINT ( 'NONE',  ( 66.10673863877181589, -1.463538230407920082, -16.72118890776879852 ) ) ;
#28549=CARTESIAN_POINT ( 'NONE',  ( 47.50309824425600169, 23.36724547216629944, -74.14999584438369595 ) ) ;
#28550=FACE_OUTER_BOUND ( 'NONE', #41766, .T. ) ;
#28552=CARTESIAN_POINT ( 'NONE',  ( 60.68762404489650919, -30.63429797783443931, -16.28103577270612590 ) ) ;
#28553=CARTESIAN_POINT ( 'NONE',  ( 12.36320305067610015, 33.31445045643330616, -15.76422791930239953 ) ) ;
#28556=B_SPLINE_CURVE_WITH_KNOTS ( 'NONE', 3,
 ( #46390, #3129, #34560, #30625, #26686, #42710, #19098, #35073, #51079, #15177, #8862, #12801, #32156, #28757, #44498, #44758 ),
 .UNSPECIFIED., .F., .F.,
 ( 4, 2, 2, 2, 2, 2, 2, 4 ),
 ( 0.000000000000000000, 0.04580887700494568754, 0.3154492010360799292, 0.4839744035555390567, 0.6054138568059892478, 0.7268533100564364968, 0.8786526266194979451, 1.000000000000000000 ),
 .UNSPECIFIED. ) ;
#28560=CARTESIAN_POINT ( 'NONE',  ( 61.49802603650289257, 13.92071365815219863, -46.55134034995590042 ) ) ;
#28561=CARTESIAN_POINT ( 'NONE',  ( 13.04555273158159956, -65.52070318195430332, -47.48197110827570100 ) ) ;
#28562=ORIENTED_EDGE ( 'NONE', *, *, #23403, .T. ) ;
#28563=CARTESIAN_POINT ( 'NONE',  ( 52.81767045377850422, -49.66725257592850085, -48.48656228474339969 ) ) ;
#28565=CARTESIAN_POINT ( 'NONE',  ( 57.76710182873919308, -45.11618912136610504, -25.37614636620249797 ) ) ;
#28567=CARTESIAN_POINT ( 'NONE',  ( 57.13943934813359959, 14.62469886311279943, -26.25200977877019781 ) ) ;
#28568=TOROIDAL_SURFACE ( 'NONE', #41985, 15.56227766016839986, 1.399999999999999911 ) ;
#28570=CARTESIAN_POINT ( 'NONE',  ( 50.72812903946289254, 18.91210722878299677, -76.16412222909750085 ) ) ;
#28571=CARTESIAN_POINT ( 'NONE',  ( 52.75740204447090065, 18.47005112969250007, -48.47378032971769812 ) ) ;
#28573=CARTESIAN_POINT ( 'NONE',  ( 41.83063930241069528, -43.61086970063350066, -3.362295850879169823 ) ) ;
#28577=CARTESIAN_POINT ( 'NONE',  ( 47.55278177603999978, -54.57312067195669414, -54.95467727275750747 ) ) ;
#28580=CARTESIAN_POINT ( 'NONE',  ( 41.36298005976649961, 12.80050257910570011, -3.553636961524439641 ) ) ;
#28581=CARTESIAN_POINT ( 'NONE',  ( 59.03790284062520044, -28.86438846994849783, -15.69185385446090031 ) ) ;
#28587=ORIENTED_EDGE ( 'NONE', *, *, #36658, .F. ) ;
#28589=CARTESIAN_POINT ( 'NONE',  ( 57.20288281111999851, 18.94155152855249824, -52.64687565416169690 ) ) ;
#28592=CARTESIAN_POINT ( 'NONE',  ( 11.32941480849519955, -64.39195845186381462, -44.31825940040779699 ) ) ;
#28593=LINE ( 'NONE', #39639, #31889 ) ;
#28595=CARTESIAN_POINT ( 'NONE',  ( 51.82948429423599634, 19.25463815188989969, -76.37482632157400531 ) ) ;
#28603=VERTEX_POINT ( 'NONE', #22774 ) ;
#28604=VECTOR ( 'NONE', #15905, 999.9999999999998863 ) ;
#28605=CARTESIAN_POINT ( 'NONE',  ( 11.39018864042530055, -63.93570751189418644, -24.36152679348629846 ) ) ;
#28610=CARTESIAN_POINT ( 'NONE',  ( 14.69599431308540005, 20.96156756881190120, -75.93682688742939035 ) ) ;
#28612=CARTESIAN_POINT ( 'NONE',  ( 83.23750369908759694, -44.81947700284720781, -46.42259446247490473 ) ) ;
#28616=CARTESIAN_POINT ( 'NONE',  ( 52.81789460724309748, -49.66430887009229878, -28.03531209662209989 ) ) ;
#28617=CARTESIAN_POINT ( 'NONE',  ( 15.00539844364359965, -50.92316721421990167, -21.20430891277609931 ) ) ;
#28618=CARTESIAN_POINT ( 'NONE',  ( 50.60551416901743238, -35.90772131913882248, -76.23178625769983796 ) ) ;
#28622=DIRECTION ( 'NONE',  ( -1.000000000000000000, 0.000000000000000000, 0.000000000000000000 ) ) ;
#28624=EDGE_LOOP ( 'NONE', ( #28903, #51872, #46007, #31045, #12187, #34974, #34458, #49140, #21883, #48375, #42749, #37021, #5868 ) ) ;
#28625=CARTESIAN_POINT ( 'NONE',  ( -5.256770087461370089, -47.44903047538170426, -5.577592548843699483 ) ) ;
#28626=CARTESIAN_POINT ( 'NONE',  ( 47.30384360797479815, 23.48520776747849936, -54.69971079365609512 ) ) ;
#28629=CARTESIAN_POINT ( 'NONE',  ( 10.85466582836039962, 33.73459203646100235, -17.55961494274570001 ) ) ;
#28633=CARTESIAN_POINT ( 'NONE',  ( 55.16746451318910260, -48.53221452072369857, -48.68584014076520106 ) ) ;
#28635=DIRECTION ( 'NONE',  ( -1.224646799147353207E-16, 1.000000000000000000, 0.000000000000000000 ) ) ;
#28641=CARTESIAN_POINT ( 'NONE',  ( 9.287871870417321318, 31.98002424137379762, -46.53019454594979720 ) ) ;
#28642=AXIS2_PLACEMENT_3D ( 'NONE', #17284, #49770, #13862 ) ;
#28643=CARTESIAN_POINT ( 'NONE',  ( 16.13393739769620083, -15.61618894467929941, -10.44999999999999929 ) ) ;
#28646=CARTESIAN_POINT ( 'NONE',  ( 18.63937188518799815, 20.22628383398659935, -74.56034069004439857 ) ) ;
#28648=ORIENTED_EDGE ( 'NONE', *, *, #15582, .T. ) ;
#28649=ORIENTED_EDGE ( 'NONE', *, *, #29390, .F. ) ;
#28650=CARTESIAN_POINT ( 'NONE',  ( 11.36715134725919896, -64.83549888376190040, -46.20270877207719451 ) ) ;
#28651=DIRECTION ( 'NONE',  ( 0.6676418852213051869, -0.2329255526947263677, -0.7071067811865459074 ) ) ;
#28653=CARTESIAN_POINT ( 'NONE',  ( 61.60982433611909670, 13.90674965645299821, -46.62866983784309838 ) ) ;
#28656=B_SPLINE_SURFACE_WITH_KNOTS ( 'NONE', 3, 3, ( 
 ( #44320, #29363, #40650, #45368, #550, #24894, #41169, #16283 ),
 ( #9472, #1340, #20715, #28844, #33293, #8685, #32488, #25420 ),
 ( #24376, #16807, #12621, #48260, #49309, #17073, #33024, #49049 ),
 ( #40391, #44847, #29105, #36705, #45104, #5281, #4748, #13404 ),
 ( #32237, #24637, #41423, #301, #12354, #28319, #8952, #8430 ),
 ( #20454, #21232, #48516, #4485, #32756, #36444, #16536, #38016 ) ),
 .UNSPECIFIED., .F., .F., .F.,
 ( 4, 1, 1, 4 ),
 ( 4, 2, 2, 4 ),
 ( 0.000000000000000000, 0.3333333333333329818, 0.6666666666666670737, 1.000000000000000000 ),
 ( -18.06426057213299785, -15.10764099038530084, -11.44518256847369919, -9.383697485516369952 ),
 .UNSPECIFIED. ) ;
#28659=CARTESIAN_POINT ( 'NONE',  ( 52.23246088134759901, -46.22137412629599851, -14.08618647836389925 ) ) ;
#28660=EDGE_CURVE ( 'NONE', #42919, #36517, #34816, .T. ) ;
#28664=ORIENTED_EDGE ( 'NONE', *, *, #32495, .F. ) ;
#28666=CARTESIAN_POINT ( 'NONE',  ( 72.13393739769617241, 0.6411703679100281272, -20.65000000000000924 ) ) ;
#28667=CARTESIAN_POINT ( 'NONE',  ( 73.38393739769610136, 4.883811055320659733, -84.94863984844540994 ) ) ;
#28668=DIRECTION ( 'NONE',  ( 0.000000000000000000, 0.000000000000000000, 1.000000000000000000 ) ) ;
#28670=CARTESIAN_POINT ( 'NONE',  ( 50.02872888617959291, 13.97177871515139991, -11.19014215844219962 ) ) ;
#28671=CARTESIAN_POINT ( 'NONE',  ( 12.63673238537484345, 34.26275087728654256, -22.96425606342529946 ) ) ;
#28672=CARTESIAN_POINT ( 'NONE',  ( -3.772792344368970152, 16.77021858688409850, -4.559953443787880367 ) ) ;
#28673=VECTOR ( 'NONE', #42100, 1000.000000000000000 ) ;
#28675=ADVANCED_FACE ( 'NONE', ( #50061 ), #10494, .F. ) ;
#28676=CARTESIAN_POINT ( 'NONE',  ( 55.89838737928348422, 14.67644932428170534, -17.62829472177295642 ) ) ;
#28681=CARTESIAN_POINT ( 'NONE',  ( 11.14789759608520114, 32.56083963058139830, -43.84340685660220061 ) ) ;
#28686=CARTESIAN_POINT ( 'NONE',  ( 46.38667117663079864, 21.75602067995220068, -76.14873014785041505 ) ) ;
#28687=CARTESIAN_POINT ( 'NONE',  ( 49.71697407881319464, -53.65078623385990397, -55.07777775019589939 ) ) ;
#28688=FACE_OUTER_BOUND ( 'NONE', #36790, .T. ) ;
#28690=CARTESIAN_POINT ( 'NONE',  ( 76.77796743388176992, -43.16487758388229423, -14.54547455625814045 ) ) ;
#28699=CARTESIAN_POINT ( 'NONE',  ( 60.87556493381669753, -45.60883372431879224, -47.59991427375260287 ) ) ;
#28705=DIRECTION ( 'NONE',  ( 0.000000000000000000, 0.000000000000000000, 1.000000000000000000 ) ) ;
#28707=ORIENTED_EDGE ( 'NONE', *, *, #40702, .F. ) ;
#28708=CARTESIAN_POINT ( 'NONE',  ( 82.73840718283260287, -45.54981251556409916, -47.62304481396609646 ) ) ;
#28709=VERTEX_POINT ( 'NONE', #6043 ) ;
#28710=ORIENTED_EDGE ( 'NONE', *, *, #49208, .T. ) ;
#28711=ORIENTED_EDGE ( 'NONE', *, *, #5097, .T. ) ;
#28714=CIRCLE ( 'NONE', #49662, 29.70020322226740106 ) ;
#28715=CARTESIAN_POINT ( 'NONE',  ( 76.42336834388106581, -22.53308218664625073, -12.89720526797597522 ) ) ;
#28716=CARTESIAN_POINT ( 'NONE',  ( 53.21998863634129151, -52.13732859160620592, -53.98245948904320812 ) ) ;
#28723=CARTESIAN_POINT ( 'NONE',  ( 49.72648160330889766, -53.64673639094029767, -55.11972614036120177 ) ) ;
#28727=EDGE_CURVE ( 'NONE', #29939, #50146, #48038, .T. ) ;
#28728=EDGE_LOOP ( 'NONE', ( #38473, #23019, #37108, #40793 ) ) ;
#28730=CARTESIAN_POINT ( 'NONE',  ( 52.22858155659860557, -49.81590603655720173, -77.10495058180190142 ) ) ;
#28731=CARTESIAN_POINT ( 'NONE',  ( 68.13393739769620083, 16.88381105532069881, -71.50000000000000000 ) ) ;
#28732=CARTESIAN_POINT ( 'NONE',  ( 47.40322300430410252, -54.65574458090419796, -54.88279555090289819 ) ) ;
#28733=EDGE_CURVE ( 'NONE', #14240, #30697, #36501, .T. ) ;
#28735=LINE ( 'NONE', #36871, #9632 ) ;
#28737=CARTESIAN_POINT ( 'NONE',  ( 54.17303629415799548, 19.38381105532069881, -77.01199944720809754 ) ) ;
#28738=B_SPLINE_CURVE_WITH_KNOTS ( 'NONE', 3,
 ( #14327, #30298, #17742, #33455, #18517, #46316, #10143, #1758, #13815, #10666 ),
 .UNSPECIFIED., .F., .F.,
 ( 4, 2, 2, 2, 4 ),
 ( 0.000000000000000000, 0.2538046189272509245, 0.5511430180573008153, 0.8049079287776087499, 1.000000000000000000 ),
 .UNSPECIFIED. ) ;
#28739=CARTESIAN_POINT ( 'NONE',  ( 41.40756461421400303, -44.77159006877079861, -5.393981499654329603 ) ) ;
#28741=VECTOR ( 'NONE', #40418, 1000.000000000000000 ) ;
#28742=CARTESIAN_POINT ( 'NONE',  ( 61.04001029137710077, -45.35933836075930259, -46.86320535112459851 ) ) ;
#28743=CARTESIAN_POINT ( 'NONE',  ( 61.41208173005990290, -45.43591354592849996, -47.45931927210430246 ) ) ;
#28746=CARTESIAN_POINT ( 'NONE',  ( 65.34027601680769237, 0.8063996746146668837, -17.56710917073600342 ) ) ;
#28748=CARTESIAN_POINT ( 'NONE',  ( 13.58892339565109886, -51.93864758878270038, -75.09854824053589084 ) ) ;
#28749=CARTESIAN_POINT ( 'NONE',  ( 47.38131715433139846, -54.66763248196649982, -54.77717321816150076 ) ) ;
#28751=CARTESIAN_POINT ( 'NONE',  ( 61.13393739769620083, 4.883811055320659733, -84.38499399519520239 ) ) ;
#28756=CARTESIAN_POINT ( 'NONE',  ( 47.74681726949440019, -54.47399125802040487, -54.93559451776580005 ) ) ;
#28757=CARTESIAN_POINT ( 'NONE',  ( 47.32200658827643025, 22.89650621548869225, -75.47293010799739932 ) ) ;
#28758=CARTESIAN_POINT ( 'NONE',  ( -6.924536278744959361, -46.06766666375389718, -5.623594431461650167 ) ) ;
#28760=CARTESIAN_POINT ( 'NONE',  ( 48.64758560217519801, 22.70397928459539827, -54.52813621919599996 ) ) ;
#28764=CARTESIAN_POINT ( 'NONE',  ( 72.38393739883420608, 4.883811055320659733, -61.34712802272770915 ) ) ;
#28767=CARTESIAN_POINT ( 'NONE',  ( 84.23484834998549786, 12.58064488669169911, -47.06355581890329631 ) ) ;
#28768=CARTESIAN_POINT ( 'NONE',  ( 52.92551367776950144, 18.26402201841269957, -27.38996126115440077 ) ) ;
#28769=EDGE_CURVE ( 'NONE', #39784, #25775, #9740, .T. ) ;
#28772=CARTESIAN_POINT ( 'NONE',  ( 57.30396242925620243, -45.11618894467940066, -16.63931852905170317 ) ) ;
#28776=ORIENTED_EDGE ( 'NONE', *, *, #26820, .T. ) ;
#28777=AXIS2_PLACEMENT_3D ( 'NONE', #8318, #4635, #20608 ) ;
#28778=EDGE_CURVE ( 'NONE', #1009, #42867, #23949, .T. ) ;
#28779=CARTESIAN_POINT ( 'NONE',  ( 12.12214211477839854, -65.05677813791820085, -16.43788246316010060 ) ) ;
#28780=CARTESIAN_POINT ( 'NONE',  ( 12.93642320027750081, 34.28151823598130221, -47.70347891814760288 ) ) ;
#28781=CARTESIAN_POINT ( 'NONE',  ( 61.37881371176925427, -45.32822124412814446, -47.24538866281226746 ) ) ;
#28782=CARTESIAN_POINT ( 'NONE',  ( 47.18323533445099827, -54.80730216070119809, -54.61058630203390152 ) ) ;
#28783=B_SPLINE_CURVE_WITH_KNOTS ( 'NONE', 3,
 ( #6019, #21976, #34286, #14131, #30099, #46124, #10208, #6279, #22494, #22237, #34554, #18312, #26426, #42444, #38503, #15941, #35067, #31129 ),
 .UNSPECIFIED., .F., .F.,
 ( 4, 2, 2, 2, 2, 2, 2, 2, 4 ),
 ( 0.000000000000000000, 0.06393429766015837346, 0.09590144649023724099, 0.1278685953203161085, 0.1918028929804706795, 0.2557371906406252227, 0.3836057859609320331, 0.4475400836210886024, 0.5114743812812451162 ),
 .UNSPECIFIED. ) ;
#28786=CARTESIAN_POINT ( 'NONE',  ( 16.13393739769620083, -15.61618894467929941, -10.90000000000000036 ) ) ;
#28790=CARTESIAN_POINT ( 'NONE',  ( 50.39203494574510245, -49.33609294867260076, -76.16300746230109553 ) ) ;
#28791=DIRECTION ( 'NONE',  ( 0.000000000000000000, 0.000000000000000000, -1.000000000000000000 ) ) ;
#28794=CARTESIAN_POINT ( 'NONE',  ( 55.01074116390070401, -47.06068843752009911, -25.62222821926219751 ) ) ;
#28795=CARTESIAN_POINT ( 'NONE',  ( 16.13393739769620083, -15.61618894467929941, -17.93019253464870033 ) ) ;
#28796=EDGE_LOOP ( 'NONE', ( #376, #21379, #562, #14170 ) ) ;
#28797=CARTESIAN_POINT ( 'NONE',  ( 57.07894516969589915, -50.21246463426640361, -52.67137581470450414 ) ) ;
#28798=CARTESIAN_POINT ( 'NONE',  ( 52.90945400079600347, 18.90700577772100033, -50.10580952084150397 ) ) ;
#28799=ADVANCED_FACE ( 'NONE', ( #42203 ), #6821, .F. ) ;
#28802=CARTESIAN_POINT ( 'NONE',  ( 53.79001371717119895, 20.06659692491659897, -75.54591657906719604 ) ) ;
#28803=CARTESIAN_POINT ( 'NONE',  ( 46.61193351516349992, -53.28955996511189852, -76.10144452841760199 ) ) ;
#28804=ORIENTED_EDGE ( 'NONE', *, *, #35846, .F. ) ;
#28810=CARTESIAN_POINT ( 'NONE',  ( 46.49861198364799719, 21.90968872996920069, -76.13710305591399674 ) ) ;
#28812=CARTESIAN_POINT ( 'NONE',  ( 12.32380480340579965, 33.40949394495549285, -15.85794303743209888 ) ) ;
#28813=VECTOR ( 'NONE', #16191, 1000.000000000000000 ) ;
#28814=DIRECTION ( 'NONE',  ( 0.000000000000000000, 0.000000000000000000, 1.000000000000000000 ) ) ;
#28817=CARTESIAN_POINT ( 'NONE',  ( 50.03007040746459921, 5.621799825072190337, -76.14999999999999147 ) ) ;
#28819=TOROIDAL_SURFACE ( 'NONE', #43911, 15.56227766016839986, 1.399999999999999911 ) ;
#28823=CARTESIAN_POINT ( 'NONE',  ( -32.29328640865499978, -20.30120719130589890, -55.80050612416169997 ) ) ;
#28824=EDGE_LOOP ( 'NONE', ( #3323, #26384, #11988, #35347 ) ) ;
#28825=CARTESIAN_POINT ( 'NONE',  ( 52.75763549665710173, -49.70454645220410583, -48.62438309228340216 ) ) ;
#28826=CARTESIAN_POINT ( 'NONE',  ( 58.79269946044950501, -45.11618907922949973, -25.61455272403410177 ) ) ;
#28827=CARTESIAN_POINT ( 'NONE',  ( 48.50471607674010244, -54.16716192014190057, -55.31622937648409533 ) ) ;
#28828=CARTESIAN_POINT ( 'NONE',  ( 57.35648317541490115, 14.51146209784109864, -26.25116064136519967 ) ) ;
#28830=CARTESIAN_POINT ( 'NONE',  ( 51.24890051900759858, 19.15053050095109910, -76.23258468917369157 ) ) ;
#28831=CARTESIAN_POINT ( 'NONE',  ( 52.75620127927579972, 18.48103312263130249, -48.74711883110850152 ) ) ;
#28833=PLANE ( 'NONE',  #8353 ) ;
#28834=CARTESIAN_POINT ( 'NONE',  ( 64.89116046657669301, -43.41583358990930464, -10.41655519546019981 ) ) ;
#28835=EDGE_CURVE ( 'NONE', #29183, #20094, #23689, .T. ) ;
#28836=ORIENTED_EDGE ( 'NONE', *, *, #3663, .F. ) ;
#28841=CARTESIAN_POINT ( 'NONE',  ( 47.42962603948429745, -54.62656463334229784, -54.65340493925440057 ) ) ;
#28844=CARTESIAN_POINT ( 'NONE',  ( 58.76033327212790169, 16.72714852453529844, -50.08083992869450185 ) ) ;
#28850=VERTEX_POINT ( 'NONE', #24048 ) ;
#28852=VECTOR ( 'NONE', #29000, 1000.000000000000000 ) ;
#28853=CARTESIAN_POINT ( 'NONE',  ( 9.283462026593010563, -63.18182653024980056, -46.53091203316120072 ) ) ;
#28855=ORIENTED_EDGE ( 'NONE', *, *, #34098, .F. ) ;
#28859=CARTESIAN_POINT ( 'NONE',  ( 53.20629916227129996, 19.50996791044699918, -76.43613545957519761 ) ) ;
#28860=VERTEX_POINT ( 'NONE', #3406 ) ;
#28865=B_SPLINE_SURFACE_WITH_KNOTS ( 'NONE', 3, 3, ( 
 ( #41013, #17174, #9826, #25777, #37340, #6153, #49412, #5125 ),
 ( #41784, #21855, #9319, #32858, #33905, #49919, #17426, #5643 ),
 ( #45989, #14011, #22110, #29971, #918, #10082, #13508, #1700 ),
 ( #37081, #45468, #1179, #21589, #37587, #48888, #17682, #26040 ),
 ( #12992, #28942, #44947, #9047, #24994, #21079, #6412, #22632 ),
 ( #22885, #26828, #38903, #31258, #35209, #14271, #42314, #50686 ),
 ( #10344, #42836, #10605, #30751, #14782, #38121, #18455, #34158 ),
 ( #50173, #19223, #18708, #2993, #15304, #34424, #15038, #38647 ),
 ( #46773, #50435, #30494, #34943, #34684, #27343, #43092, #39155 ),
 ( #10859, #18963, #6667, #14524, #2466, #22370, #7184, #47290 ),
 ( #46516, #11380, #2216, #30237, #43347, #26302, #3250, #11119 ),
 ( #50944, #26560, #51210, #31008, #42574, #6931, #47035, #7441 ),
 ( #18194, #23140, #38376, #46254, #2735, #27088, #31769, #19738 ),
 ( #19481, #4520, #4020, #24153, #588, #35731, #338, #23899 ) ),
 .UNSPECIFIED., .F., .F., .F.,
 ( 4, 2, 2, 2, 2, 2, 4 ),
 ( 4, 1, 1, 1, 1, 4 ),
 ( 3.901346948265469905, 4.407177605192729608, 8.834505823316810336, 16.99747883129379744, 26.70074659151990204, 31.55238047163300052, 38.13654360031040369 ),
 ( -1.140694639499999985E-05, 0.2000000000000000111, 0.4000000000000000222, 0.5999999999999999778, 0.8000000000000000444, 1.000037278610800051 ),
 .UNSPECIFIED. ) ;
#28868=CARTESIAN_POINT ( 'NONE',  ( 53.62552786343490396, 20.09834016026489678, -75.58099297212140755 ) ) ;
#28871=CARTESIAN_POINT ( 'NONE',  ( 11.62168671107460050, -64.72337088029789243, -24.07512666974249882 ) ) ;
#28874=CARTESIAN_POINT ( 'NONE',  ( 14.62118626177969993, 20.66382337739360153, -75.74020909530109691 ) ) ;
#28877=CARTESIAN_POINT ( 'NONE',  ( 84.37258452300260103, -43.45091051789750480, -47.24504068948050417 ) ) ;
#28880=CARTESIAN_POINT ( 'NONE',  ( 52.89242001099999868, -49.58003531765110239, -27.72111690325079891 ) ) ;
#28882=CARTESIAN_POINT ( 'NONE',  ( 15.85308752006570110, -51.11618894234659649, -21.66365682949659899 ) ) ;
#28883=FACE_OUTER_BOUND ( 'NONE', #26100, .T. ) ;
#28887=CARTESIAN_POINT ( 'NONE',  ( -9.076360731184159647, -44.08689318531880730, -5.731288650940340013 ) ) ;
#28888=CARTESIAN_POINT ( 'NONE',  ( 47.25362900639890285, 23.52000032359880066, -54.62089388818540669 ) ) ;
#28889=CARTESIAN_POINT ( 'NONE',  ( 56.42249722295453296, -45.43314942095580733, -25.29439854063558357 ) ) ;
#28892=CARTESIAN_POINT ( 'NONE',  ( 42.05805489943670494, 13.23020005123530041, -5.167112210102939862 ) ) ;
#28896=CARTESIAN_POINT ( 'NONE',  ( 53.97790768284939844, -49.20362396525460014, -49.10634432982389797 ) ) ;
#28898=EDGE_CURVE ( 'NONE', #5276, #19930, #41118, .T. ) ;
#28900=CARTESIAN_POINT ( 'NONE',  ( 17.43325189934310160, -52.80674074535590279, -76.12862656241330228 ) ) ;
#28903=ORIENTED_EDGE ( 'NONE', *, *, #26788, .F. ) ;
#28905=CARTESIAN_POINT ( 'NONE',  ( 9.729176998844950575, 31.90615194671379840, -46.30113559920939537 ) ) ;
#28906=CARTESIAN_POINT ( 'NONE',  ( 41.50322886078625828, 13.56217550620411672, -5.449103212913565031 ) ) ;
#28907=CARTESIAN_POINT ( 'NONE',  ( 13.13393739769619906, 32.28996932333459569, -46.39999999999999858 ) ) ;
#28909=CARTESIAN_POINT ( 'NONE',  ( 18.48574654752910007, 20.09246212084070038, -74.56515407679859209 ) ) ;
#28910=EDGE_LOOP ( 'NONE', ( #26482, #9018, #14351, #34040 ) ) ;
#28911=ORIENTED_EDGE ( 'NONE', *, *, #1727, .T. ) ;
#28913=CARTESIAN_POINT ( 'NONE',  ( 12.86012610505919973, -65.50554804669809528, -47.57962905350179739 ) ) ;
#28914=CARTESIAN_POINT ( 'NONE',  ( 57.38580998192630034, -45.30275844272679819, -25.91614474311650085 ) ) ;
#28916=CARTESIAN_POINT ( 'NONE',  ( 61.42450914986659427, 14.00539997787450019, -46.99871816792220613 ) ) ;
#28920=AXIS2_PLACEMENT_3D ( 'NONE', #6873, #11835, #22822 ) ;
#28921=CARTESIAN_POINT ( 'NONE',  ( 12.13696580915320311, 33.93507363936925003, -16.64705451129685443 ) ) ;
#28924=CIRCLE ( 'NONE', #22222, 0.9999999999999995559 ) ;
#28926=EDGE_CURVE ( 'NONE', #14552, #14297, #20594, .T. ) ;
#28927=CARTESIAN_POINT ( 'NONE',  ( 8.784728771152170879, -54.93525725209899235, -46.67204636145419983 ) ) ;
#28931=DIRECTION ( 'NONE',  ( 1.000000000000000000, 0.000000000000000000, 0.000000000000000000 ) ) ;
#28932=CARTESIAN_POINT ( 'NONE',  ( 60.47553822224839593, 14.59310891045189962, -47.74689862142960095 ) ) ;
#28933=CARTESIAN_POINT ( 'NONE',  ( 51.02726976822560090, 14.97164679345370075, -13.20165271163509857 ) ) ;
#28935=CARTESIAN_POINT ( 'NONE',  ( -9.464298943378709694, 12.47750318557470095, -5.578887212681300056 ) ) ;
#28936=CARTESIAN_POINT ( 'NONE',  ( -2.927979189508790103, -49.19984425798019601, -5.740620115512199639 ) ) ;
#28937=AXIS2_PLACEMENT_3D ( 'NONE', #1525, #8617, #32954 ) ;
#28938=CARTESIAN_POINT ( 'NONE',  ( 55.83253168230204011, 14.69212688956227986, -17.34603649656557778 ) ) ;
#28941=CARTESIAN_POINT ( 'NONE',  ( 57.37174218388170033, 16.14477099907140101, -48.15837671390720232 ) ) ;
#28942=CARTESIAN_POINT ( 'NONE',  ( -8.925905124820840086, -44.39248591613520034, -6.403223950166009537 ) ) ;
#28943=CARTESIAN_POINT ( 'NONE',  ( 11.39852503586600108, 33.29352875594079819, -44.68676662896000096 ) ) ;
#28945=CARTESIAN_POINT ( 'NONE',  ( 11.60439326024719975, -64.93477792032190621, -16.46429631545650096 ) ) ;
#28947=CARTESIAN_POINT ( 'NONE',  ( 16.65420337941059969, -49.11618894467930829, -17.90311212357429937 ) ) ;
#28948=CARTESIAN_POINT ( 'NONE',  ( 12.61030219803810049, 18.86097712249150149, -21.13761110129019727 ) ) ;
#28950=CARTESIAN_POINT ( 'NONE',  ( 49.54598800151290305, -53.61194117850519802, -54.50101998263480141 ) ) ;
#28952=CARTESIAN_POINT ( 'NONE',  ( 42.48652067527369525, -44.25687345361960467, -5.094659063150840161 ) ) ;
#28955=CARTESIAN_POINT ( 'NONE',  ( 12.06284766121009966, 32.21085600226960111, -22.25048313876769868 ) ) ;
#28960=EDGE_CURVE ( 'NONE', #4297, #37620, #15191, .T. ) ;
#28962=ORIENTED_EDGE ( 'NONE', *, *, #43077, .T. ) ;
#28963=CARTESIAN_POINT ( 'NONE',  ( 84.22672017746327811, -43.79043011566170662, -46.99906225576258834 ) ) ;
#28964=CARTESIAN_POINT ( 'NONE',  ( 60.58228858412009998, -45.68472658336609982, -47.55887949375219392 ) ) ;
#28966=CARTESIAN_POINT ( 'NONE',  ( 13.19614975339650087, 18.82172381217750257, -21.01902014737410340 ) ) ;
#28969=EDGE_CURVE ( 'NONE', #41896, #30141, #35623, .T. ) ;
#28971=CARTESIAN_POINT ( 'NONE',  ( 37.63393739769620083, -15.61618894467929941, -11.05000000000000071 ) ) ;
#28972=ORIENTED_EDGE ( 'NONE', *, *, #15303, .T. ) ;
#28973=CARTESIAN_POINT ( 'NONE',  ( 84.30744353797240365, -43.93553367712969759, -47.37637942009979497 ) ) ;
#28978=CARTESIAN_POINT ( 'NONE',  ( 52.60089517322759889, -49.82971139612260458, -48.60938815635680044 ) ) ;
#28980=CARTESIAN_POINT ( 'NONE',  ( 76.42335353787902363, -22.53155339109895650, -12.89714147592827942 ) ) ;
#28981=CARTESIAN_POINT ( 'NONE',  ( 54.97710707581860134, -51.41017014255020001, -53.92626239532030041 ) ) ;
#28985=AXIS2_PLACEMENT_3D ( 'NONE', #25927, #34314, #46143 ) ;
#28986=CARTESIAN_POINT ( 'NONE',  ( 56.72395159686060140, 19.45340621921160107, -53.71484871595450272 ) ) ;
#28994=CARTESIAN_POINT ( 'NONE',  ( 53.57535180181819356, -50.54591161070089811, -77.11818236577570929 ) ) ;
#28995=CARTESIAN_POINT ( 'NONE',  ( 62.50953355103300169, -29.38356811901130072, -16.13223000750240388 ) ) ;
#28996=PLANE ( 'NONE',  #50479 ) ;
#29000=DIRECTION ( 'NONE',  ( 0.000000000000000000, -1.000000000000000000, 0.000000000000000000 ) ) ;
#29002=CARTESIAN_POINT ( 'NONE',  ( 41.53147706019129970, -44.71252858122500129, -5.331435815133920286 ) ) ;
#29004=CARTESIAN_POINT ( 'NONE',  ( 69.22748654599975282, -50.70395984887971252, -73.25000000000218847 ) ) ;
#29009=CARTESIAN_POINT ( 'NONE',  ( 66.85053883392829732, 1.883667400092539967, -20.46403502974369815 ) ) ;
#29011=CARTESIAN_POINT ( 'NONE',  ( 13.94090093824480014, -51.82372487085179813, -75.44171726276898937 ) ) ;
#29013=CARTESIAN_POINT ( 'NONE',  ( 47.25382592556910311, -54.75228172359690149, -54.62311712267080566 ) ) ;
#29021=CARTESIAN_POINT ( 'NONE',  ( 11.93174526809839975, 34.20691394249479345, -17.93019253464870033 ) ) ;
#29022=CARTESIAN_POINT ( 'NONE',  ( 13.81950199196250040, 20.03075999784159933, -23.06529969907609967 ) ) ;
#29023=CARTESIAN_POINT ( 'NONE',  ( -10.86918838363719964, -42.36073152548370047, -6.289582464405770068 ) ) ;
#29024=CARTESIAN_POINT ( 'NONE',  ( 56.31131329977899469, 19.32763365105479636, -52.86805933726900264 ) ) ;
#29025=B_SPLINE_CURVE_WITH_KNOTS ( 'NONE', 3,
 ( #44572, #32230, #8421, #40898, #5008, #28573, #33283, #40640, #48253, #12877, #20968, #36969, #24369, #24107, #45094, #17062 ),
 .UNSPECIFIED., .F., .F.,
 ( 4, 2, 2, 2, 2, 2, 2, 4 ),
 ( -3.863343447353519977, -3.187258344066659976, -2.414589654595949764, -1.931671723676759989, -1.690212758217169764, -1.313423695611310116, -0.7105611954419281950, 0.000000000000000000 ),
 .UNSPECIFIED. ) ;
#29026=CARTESIAN_POINT ( 'NONE',  ( 48.62459252948669786, 22.87471263156120216, -55.12045204165480072 ) ) ;
#29029=EDGE_LOOP ( 'NONE', ( #46586, #20416, #1478, #17455, #50491, #49438 ) ) ;
#29030=CARTESIAN_POINT ( 'NONE',  ( 18.52891444416632538, -52.05916771839714841, -75.36997958377639861 ) ) ;
#29032=CARTESIAN_POINT ( 'NONE',  ( 57.55751162049570269, -50.09049722528730086, -52.57651812429949700 ) ) ;
#29034=CARTESIAN_POINT ( 'NONE',  ( 82.46791274550251671, 13.86095180792300141, -46.45744338702559872 ) ) ;
#29035=CARTESIAN_POINT ( 'NONE',  ( 54.44101168542169944, 16.53500074836000167, -26.08961774644910392 ) ) ;
#29041=ORIENTED_EDGE ( 'NONE', *, *, #10278, .T. ) ;
#29043=CARTESIAN_POINT ( 'NONE',  ( 11.73811129725980074, -65.16604538643500177, -16.79398347925659962 ) ) ;
#29044=CARTESIAN_POINT ( 'NONE',  ( 11.08014211953469896, 32.97560943143620449, -45.24939445730449705 ) ) ;
#29045=CARTESIAN_POINT ( 'NONE',  ( 61.14298689117413943, -45.32073797555708694, -46.99579994825386109 ) ) ;
#29046=CARTESIAN_POINT ( 'NONE',  ( 51.43602479376819758, -51.03778538747950222, -50.03115562382680537 ) ) ;
#29048=EDGE_CURVE ( 'NONE', #4830, #8473, #21423, .T. ) ;
#29049=ORIENTED_EDGE ( 'NONE', *, *, #40157, .T. ) ;
#29050=CARTESIAN_POINT ( 'NONE',  ( 10.57660162720581454, 23.99589349179882092, -45.49284114600560969 ) ) ;
#29052=CARTESIAN_POINT ( 'NONE',  ( 16.65420337941489848, 17.88381105532299742, -20.15000000000000213 ) ) ;
#29058=CARTESIAN_POINT ( 'NONE',  ( 68.13393739769620083, -49.36618894467930829, -73.25000000000000000 ) ) ;
#29060=ORIENTED_EDGE ( 'NONE', *, *, #18866, .F. ) ;
#29066=CARTESIAN_POINT ( 'NONE',  ( 47.26969180900909606, -54.15383702437160451, -75.47109442055590023 ) ) ;
#29068=CARTESIAN_POINT ( 'NONE',  ( 54.68760100489050302, 14.48868831793499901, -15.47702518080039980 ) ) ;
#29069=CARTESIAN_POINT ( 'NONE',  ( 57.20288283122350492, -50.17392941253179828, -52.64687565050539320 ) ) ;
#29071=EDGE_CURVE ( 'NONE', #998, #51191, #26390, .T. ) ;
#29073=CARTESIAN_POINT ( 'NONE',  ( 12.30798784977628735, 34.11147262445096828, -23.61458995968919083 ) ) ;
#29076=CARTESIAN_POINT ( 'NONE',  ( 47.39377455479480261, 23.20627220416080050, -75.00416199656089589 ) ) ;
#29079=CARTESIAN_POINT ( 'NONE',  ( 12.36320305067610015, 33.31445045643330616, -15.76422791930239953 ) ) ;
#29084=CARTESIAN_POINT ( 'NONE',  ( -26.15868020285170203, -41.19545595665919535, -54.51850539491499603 ) ) ;
#29086=EDGE_CURVE ( 'NONE', #31947, #48088, #37172, .T. ) ;
#29087=CARTESIAN_POINT ( 'NONE',  ( 52.73517777097259795, -49.71750526155659600, -48.54845401890089818 ) ) ;
#29088=CARTESIAN_POINT ( 'NONE',  ( 61.18381089449600552, -45.13403188722560344, -27.16748766345810040 ) ) ;
#29090=CARTESIAN_POINT ( 'NONE',  ( 56.55569464329139606, 14.33745061368849960, -25.88752018553109835 ) ) ;
#29092=CARTESIAN_POINT ( 'NONE',  ( 51.14620401246810388, 18.52529079830420145, -76.32769624451800894 ) ) ;
#29093=CARTESIAN_POINT ( 'NONE',  ( 53.14225946812250356, 18.28234889893970205, -48.98057205063000197 ) ) ;
#29096=LINE ( 'NONE', #8673, #10868 ) ;
#29098=ORIENTED_EDGE ( 'NONE', *, *, #43418, .T. ) ;
#29100=ORIENTED_EDGE ( 'NONE', *, *, #47661, .T. ) ;
#29102=CARTESIAN_POINT ( 'NONE',  ( 47.47677450096290386, -54.59520210331019285, -54.66133488802340423 ) ) ;
#29105=CARTESIAN_POINT ( 'NONE',  ( 60.18524539318269717, 15.49018248464509995, -48.88483521943319232 ) ) ;
#29106=CARTESIAN_POINT ( 'NONE',  ( 53.11114665040049942, 18.28111428451719789, -48.80212166739769941 ) ) ;
#29109=MECHANICAL_DESIGN_GEOMETRIC_PRESENTATION_REPRESENTATION('',(#13240),#49218);
#29113=VERTEX_POINT ( 'NONE', #17258 ) ;
#29114=CARTESIAN_POINT ( 'NONE',  ( 8.788636732660460638, -63.13527780971870129, -46.67124789091300130 ) ) ;
#29115=AXIS2_PLACEMENT_3D ( 'NONE', #44441, #3587, #20061 ) ;
#29116=DIRECTION ( 'NONE',  ( 0.000000000000000000, 0.000000000000000000, 1.000000000000000000 ) ) ;
#29118=CARTESIAN_POINT ( 'NONE',  ( 11.49293692653489884, -64.67039193628410487, -44.68941390596329910 ) ) ;
#29121=CARTESIAN_POINT ( 'NONE',  ( 53.61341609220770010, 19.44707778802039755, -76.60108244557071089 ) ) ;
#29122=ORIENTED_EDGE ( 'NONE', *, *, #34207, .F. ) ;
#29123=DIRECTION ( 'NONE',  ( 0.000000000000000000, -1.000000000000000000, 0.000000000000000000 ) ) ;
#29130=B_SPLINE_CURVE_WITH_KNOTS ( 'NONE', 3,
 ( #39498, #34769, #19569, #27934, #3596, #19313, #35558, #43936 ),
 .UNSPECIFIED., .F., .F.,
 ( 4, 2, 2, 4 ),
 ( 1.104809738474189951, 1.178746485095780061, 1.463424881496269814, 1.779239977503060066 ),
 .UNSPECIFIED. ) ;
#29131=CARTESIAN_POINT ( 'NONE',  ( 10.64863409883700029, -63.44323389162830296, -23.66469670114080159 ) ) ;
#29134=ADVANCED_FACE ( 'NONE', ( #13333 ), #48714, .F. ) ;
#29135=CARTESIAN_POINT ( 'NONE',  ( 14.58508199943239880, 20.56214955651219967, -75.65676662446099954 ) ) ;
#29138=CARTESIAN_POINT ( 'NONE',  ( 82.79586663885591236, -45.02293793585479875, -46.43485061813910164 ) ) ;
#29140=EDGE_LOOP ( 'NONE', ( #9890, #1300, #9083, #559, #28449 ) ) ;
#29141=CARTESIAN_POINT ( 'NONE',  ( 56.18973212658190164, -45.98240354813589903, -26.01119312686520146 ) ) ;
#29142=CARTESIAN_POINT ( 'NONE',  ( 16.33846296856719960, -51.11618894303549610, -21.13414048024940328 ) ) ;
#29145=CARTESIAN_POINT ( 'NONE',  ( 53.92601233233809666, 15.01256046956459933, -15.35059813110260052 ) ) ;
#29147=CARTESIAN_POINT ( 'NONE',  ( -8.078265854356109443, -44.94086578754730255, -5.419177366022879916 ) ) ;
#29148=CARTESIAN_POINT ( 'NONE',  ( 47.25108210846270396, 23.52211893725460001, -54.62737137215419381 ) ) ;
#29149=CARTESIAN_POINT ( 'NONE',  ( 56.59979300609889208, -45.33386959848365194, -25.29349730390593365 ) ) ;
#29152=CARTESIAN_POINT ( 'NONE',  ( 10.97564820803400032, 33.77114500669409836, -17.33480536923670101 ) ) ;
#29157=CARTESIAN_POINT ( 'NONE',  ( 56.66044069829109731, -47.79715243440499961, -48.40052123592339939 ) ) ;
#29158=CARTESIAN_POINT ( 'NONE',  ( 10.91612620756760066, 33.86326241729176445, -18.17421237796254019 ) ) ;
#29159=CARTESIAN_POINT ( 'NONE',  ( 52.62905305334270167, 20.95810661167350020, -53.53065356658779450 ) ) ;
#29165=CARTESIAN_POINT ( 'NONE',  ( 8.971085476333328756, 32.00512979024770033, -46.63277124569800236 ) ) ;
#29166=LINE ( 'NONE', #9014, #8394 ) ;
#29167=CARTESIAN_POINT ( 'NONE',  ( 66.65424818669949047, -29.91331004332360166, -16.99686723155519985 ) ) ;
#29169=CARTESIAN_POINT ( 'NONE',  ( 17.91441070958899928, 19.90988454773669858, -74.52171359303420672 ) ) ;
#29171=ORIENTED_EDGE ( 'NONE', *, *, #14967, .F. ) ;
#29172=CARTESIAN_POINT ( 'NONE',  ( 48.42521416700790127, -56.37491125791819968, -74.14999999999999147 ) ) ;
#29173=ORIENTED_EDGE ( 'NONE', *, *, #23960, .F. ) ;
#29174=CARTESIAN_POINT ( 'NONE',  ( 11.85109790645039851, -65.12712902498141432, -46.35237351896630287 ) ) ;
#29175=CARTESIAN_POINT ( 'NONE',  ( 56.57808279982729971, -46.09595787718389204, -26.23509901551880219 ) ) ;
#29177=CARTESIAN_POINT ( 'NONE',  ( 61.31732609679450263, 14.08360619472680142, -47.18614283445869972 ) ) ;
#29180=AXIS2_PLACEMENT_3D ( 'NONE', #42038, #13747, #38363 ) ;
#29181=ORIENTED_EDGE ( 'NONE', *, *, #24513, .F. ) ;
#29183=VERTEX_POINT ( 'NONE', #5213 ) ;
#29184=CARTESIAN_POINT ( 'NONE',  ( 54.31501561488440188, -45.11618894460480078, -13.70601682451409964 ) ) ;
#29186=DIRECTION ( 'NONE',  ( 1.000000000000000000, 0.000000000000000000, 0.000000000000000000 ) ) ;
#29189=CARTESIAN_POINT ( 'NONE',  ( 46.59543176902850092, -53.41648962811289891, -76.07661161287319374 ) ) ;
#29190=DIRECTION ( 'NONE',  ( 1.000000000000000000, 0.000000000000000000, 0.000000000000000000 ) ) ;
#29191=CARTESIAN_POINT ( 'NONE',  ( 51.09228874323290626, 14.75465462415100149, -13.11143323170220043 ) ) ;
#29193=DIRECTION ( 'NONE',  ( 0.000000000000000000, 0.000000000000000000, -1.000000000000000000 ) ) ;
#29194=CARTESIAN_POINT ( 'NONE',  ( 56.17779366879769753, 14.41653637947479893, -28.15000000000000213 ) ) ;
#29196=CARTESIAN_POINT ( 'NONE',  ( 61.26764236240780548, 13.92023311689909804, -27.40800516196399883 ) ) ;
#29199=DIRECTION ( 'NONE',  ( 0.000000000000000000, 0.000000000000000000, -1.000000000000000000 ) ) ;
#29201=CARTESIAN_POINT ( 'NONE',  ( 76.63910211808688189, -43.27582581740930578, -14.20153314710789871 ) ) ;
#29203=AXIS2_PLACEMENT_3D ( 'NONE', #36459, #16298, #8703 ) ;
#29210=CARTESIAN_POINT ( 'NONE',  ( 49.09930102447209777, -53.90153221160279884, -55.03246651661279998 ) ) ;
#29212=CARTESIAN_POINT ( 'NONE',  ( 59.36844839577301514, -1.819775244482397580, -15.80989836302429730 ) ) ;
#29213=CARTESIAN_POINT ( 'NONE',  ( 18.32671964139129983, -51.19324711185789312, -74.36773579015570590 ) ) ;
#29214=ADVANCED_FACE ( 'NONE', ( #34514 ), #30579, .T. ) ;
#29221=CARTESIAN_POINT ( 'NONE',  ( 60.97736607362909922, -45.52420556272499397, -47.49337238818740303 ) ) ;
#29225=CARTESIAN_POINT ( 'NONE',  ( 16.13393739769620083, -15.61618894467929941, -74.14999999999999147 ) ) ;
#29227=CARTESIAN_POINT ( 'NONE',  ( 87.61621807841599718, -48.61618894467930119, -61.12885639714370001 ) ) ;
#29231=ORIENTED_EDGE ( 'NONE', *, *, #23527, .F. ) ;
#29232=CARTESIAN_POINT ( 'NONE',  ( 61.61695481319249978, -45.18470336428949707, -46.90708922469920594 ) ) ;
#29234=CARTESIAN_POINT ( 'NONE',  ( 53.82348698186820002, -51.68201745328180152, -53.31677710839019824 ) ) ;
#29238=VERTEX_POINT ( 'NONE', #45815 ) ;
#29242=CARTESIAN_POINT ( 'NONE',  ( 8.815605938724019097, -63.28267558148569094, -46.67186391142220003 ) ) ;
#29244=AXIS2_PLACEMENT_3D ( 'NONE', #2532, #34483, #50489 ) ;
#29245=AXIS2_PLACEMENT_3D ( 'NONE', #38035, #2382, #13928 ) ;
#29248=CARTESIAN_POINT ( 'NONE',  ( 53.75480394220020486, -50.98814891280600392, -75.91868723642510020 ) ) ;
#29251=CARTESIAN_POINT ( 'NONE',  ( 47.55940288235914437, -54.56982865077419120, -55.06178236366046974 ) ) ;
#29256=CARTESIAN_POINT ( 'NONE',  ( 41.86538216647980448, 13.73410068919089966, -5.828812016449009370 ) ) ;
#29258=CARTESIAN_POINT ( 'NONE',  ( 43.27773194996530037, -42.90569250231440179, -4.515873930613719445 ) ) ;
#29260=CARTESIAN_POINT ( 'NONE',  ( 61.15824941542350501, -45.61002793583419646, -47.69140330884709300 ) ) ;
#29264=CARTESIAN_POINT ( 'NONE',  ( 65.46220881590400609, 1.315651889596580082, -18.25468295616219905 ) ) ;
#29266=CARTESIAN_POINT ( 'NONE',  ( 14.47068264623949929, -51.84692819978400280, -75.69083100613939052 ) ) ;
#29267=CARTESIAN_POINT ( 'NONE',  ( 47.18324198357289845, -54.80726809202429450, -54.61058319554170026 ) ) ;
#29272=CARTESIAN_POINT ( 'NONE',  ( 54.62220045163225279, -46.21585040664924549, -15.85440674217626977 ) ) ;
#29273=CARTESIAN_POINT ( 'NONE',  ( 47.79868757135139390, -54.43094906366430052, -54.82870257381310353 ) ) ;
#29275=DIRECTION ( 'NONE',  ( -0.3294064756442134922, -0.9441882088882800339, 8.551492847173809175E-14 ) ) ;
#29276=CARTESIAN_POINT ( 'NONE',  ( 19.37546814487692615, -55.48492500472980993, -75.71737149041572934 ) ) ;
#29277=DIRECTION ( 'NONE',  ( -0.5109955813515499878, -0.8595833385072046973, 0.000000000000000000 ) ) ;
#29278=EDGE_CURVE ( 'NONE', #17140, #22022, #43027, .T. ) ;
#29279=CARTESIAN_POINT ( 'NONE',  ( 48.76292579026059570, 22.72389827073419966, -54.68972791661200006 ) ) ;
#29281=VERTEX_POINT ( 'NONE', #30320 ) ;
#29285=CARTESIAN_POINT ( 'NONE',  ( 12.36320305029179956, 33.31445045633500257, -15.76422791923680045 ) ) ;
#29286=CARTESIAN_POINT ( 'NONE',  ( 53.59003930803689997, -49.40628012469949937, -49.22510501142529904 ) ) ;
#29288=CARTESIAN_POINT ( 'NONE',  ( 82.81544245083719602, 14.09548530567630031, -47.32222464724239330 ) ) ;
#29289=CARTESIAN_POINT ( 'NONE',  ( 55.45527622853430216, 15.26954464707670134, -25.53657833487140394 ) ) ;
#29293=B_SPLINE_SURFACE_WITH_KNOTS ( 'NONE', 3, 3, ( 
 ( #40479, #32845, #1428, #37579, #1685, #12980 ),
 ( #33642, #4570, #20542, #21068, #1166, #24726 ),
 ( #36537, #17163, #641, #20807, #16628, #48612 ),
 ( #12715, #36798, #33114, #2727, #45714, #29959 ),
 ( #42303, #14259, #26550, #30484, #1947, #2206 ),
 ( #6402, #18438, #5877, #22100, #42566, #34934 ),
 ( #50935, #45977, #42040, #38365, #6658, #22618 ),
 ( #34149, #18183, #30228, #38635, #26814, #21845 ),
 ( #18698, #41774, #34676, #37851, #33896, #46246 ),
 ( #10069, #50676, #14774, #30743, #46765, #46505 ),
 ( #14515, #10852, #42828, #26031, #25767, #6921 ),
 ( #17925, #22874, #22361, #10333, #26294, #2982 ),
 ( #38894, #50162, #2458, #49907, #18956, #6141 ),
 ( #15031, #9815, #14000, #38109, #34415, #50426 ) ),
 .UNSPECIFIED., .F., .F., .F.,
 ( 4, 2, 2, 2, 2, 2, 4 ),
 ( 4, 1, 1, 4 ),
 ( 11.91694619464080063, 18.73771508486100146, 24.98362011314799958, 28.10657262729149863, 33.10329664992109855, 41.09805508612850389, 46.81668623818470110 ),
 ( -4.801081116000000185E-06, 0.3333333333333329818, 0.6666666666666670737, 1.000005332741559894 ),
 .UNSPECIFIED. ) ;
#29294=DIRECTION ( 'NONE',  ( 0.000000000000000000, 0.000000000000000000, -1.000000000000000000 ) ) ;
#29297=CARTESIAN_POINT ( 'NONE',  ( 11.85902006004669929, -65.16986276887600127, -16.73665430629710116 ) ) ;
#29298=CARTESIAN_POINT ( 'NONE',  ( 12.03830950846760039, 34.00854491475119801, -46.58869671456609751 ) ) ;
#29301=CARTESIAN_POINT ( 'NONE',  ( 11.09843493734689979, -65.15652262471280665, -47.26083285670119949 ) ) ;
#29306=CARTESIAN_POINT ( 'NONE',  ( 52.26132335211670465, 19.59060111016600203, -50.93306148729159588 ) ) ;
#29308=CARTESIAN_POINT ( 'NONE',  ( 50.03007021624649298, -48.76508975269899793, -76.14999999999999147 ) ) ;
#29309=DIRECTION ( 'NONE',  ( -1.000000000000000000, 0.000000000000000000, 0.000000000000000000 ) ) ;
#29311=CARTESIAN_POINT ( 'NONE',  ( 53.95391475063919984, -48.32190372696410208, -26.18290555829399935 ) ) ;
#29312=CARTESIAN_POINT ( 'NONE',  ( 68.13393739769810509, 19.38381105532030091, -71.50000000000198952 ) ) ;
#29313=VERTEX_POINT ( 'NONE', #6762 ) ;
#29317=CARTESIAN_POINT ( 'NONE',  ( 13.99027006517380123, -51.18075678683580776, -22.90513384373820216 ) ) ;
#29318=CARTESIAN_POINT ( 'NONE',  ( 54.58684629315739301, 19.57352726647010144, -75.90306255601998942 ) ) ;
#29320=CARTESIAN_POINT ( 'NONE',  ( 47.34252490452630724, -54.36320411571839628, -75.17211772295890171 ) ) ;
#29321=VERTEX_POINT ( 'NONE', #49747 ) ;
#29322=AXIS2_PLACEMENT_3D ( 'NONE', #23942, #4058, #36531 ) ;
#29323=CARTESIAN_POINT ( 'NONE',  ( 55.94863681995290250, 14.49335208508280104, -17.16538366520289927 ) ) ;
#29326=( BOUNDED_CURVE ( )  B_SPLINE_CURVE ( 2, ( #28114, #24687, #40701, #18147, #37542 ),
 .UNSPECIFIED., .F., .T. ) 
 B_SPLINE_CURVE_WITH_KNOTS ( ( 3, 2, 3 ),
 ( -0.003205554297748039981, 0.8238407534185530068, 1.650887061134849843 ),
 .UNSPECIFIED. ) 
 CURVE ( )  GEOMETRIC_REPRESENTATION_ITEM ( )  RATIONAL_B_SPLINE_CURVE ( ( 1.000000000000000000, 0.9157107718030679244, 1.000000000000000000, 0.9157107718030469412, 1.000000000000000000 ) ) 
 REPRESENTATION_ITEM ( '' )  );
#29328=CARTESIAN_POINT ( 'NONE',  ( 56.93701003825890439, -50.64063337602780024, -53.86363391182649707 ) ) ;
#29331=CARTESIAN_POINT ( 'NONE',  ( 12.72191543439365979, 34.25104481395036515, -23.44039337806447065 ) ) ;
#29334=CARTESIAN_POINT ( 'NONE',  ( 46.98721080798319605, 22.60815134751159761, -75.82248416561151316 ) ) ;
#29336=CARTESIAN_POINT ( 'NONE',  ( 41.42082069171990355, -45.63313572307169608, -6.346463263985820724 ) ) ;
#29339=DIRECTION ( 'NONE',  ( 0.000000000000000000, 0.000000000000000000, -1.000000000000000000 ) ) ;
#29342=CARTESIAN_POINT ( 'NONE',  ( 61.34010671551649807, 13.97110126853510081, -46.40635191164569306 ) ) ;
#29344=CARTESIAN_POINT ( 'NONE',  ( -29.08731580419370033, -35.60745549472860461, -55.16774717297709429 ) ) ;
#29346=CARTESIAN_POINT ( 'NONE',  ( 53.10940566897379966, -49.51509250019670105, -48.84491346710589710 ) ) ;
#29347=CARTESIAN_POINT ( 'NONE',  ( 57.49269918002690360, -45.11614594041920157, -25.40091178144869843 ) ) ;
#29348=CARTESIAN_POINT ( 'NONE',  ( 49.24754892657740157, -53.85074344983969752, -55.23177050136099808 ) ) ;
#29349=CARTESIAN_POINT ( 'NONE',  ( 56.04577029392780219, 14.63406453562459930, -25.72783580284800209 ) ) ;
#29351=CARTESIAN_POINT ( 'NONE',  ( 50.31596464670999325, 18.73470065217860281, -76.14999999999999147 ) ) ;
#29352=CARTESIAN_POINT ( 'NONE',  ( 52.76604400197739864, 18.47565711339310113, -48.76247536867809629 ) ) ;
#29354=CARTESIAN_POINT ( 'NONE',  ( 60.54711305708200086, -45.61758103184519797, -47.15425142490470023 ) ) ;
#29355=CARTESIAN_POINT ( 'NONE',  ( 46.35275103504439898, 21.67755452994670406, -76.14999999999999147 ) ) ;
#29359=CARTESIAN_POINT ( 'NONE',  ( 47.42186964816270489, -54.64465214730000042, -54.90471645379279408 ) ) ;
#29363=CARTESIAN_POINT ( 'NONE',  ( 60.18629601137560314, 14.85053287620760010, -47.96423632185339869 ) ) ;
#29364=CARTESIAN_POINT ( 'NONE',  ( 52.83531650484950148, 18.42562942600509857, -48.55819829956829636 ) ) ;
#29371=ORIENTED_EDGE ( 'NONE', *, *, #51140, .T. ) ;
#29373=ORIENTED_EDGE ( 'NONE', *, *, #36551, .F. ) ;
#29374=CARTESIAN_POINT ( 'NONE',  ( 9.296350058830100238, -63.27348387625509929, -46.53013307742669724 ) ) ;
#29380=CARTESIAN_POINT ( 'NONE',  ( 52.90771571177940302, 19.45349931027849877, -76.48668076088111434 ) ) ;
#29387=CYLINDRICAL_SURFACE ( 'NONE', #356, 3.000000000000000444 ) ;
#29390=EDGE_CURVE ( 'NONE', #29313, #3712, #29795, .T. ) ;
#29391=CARTESIAN_POINT ( 'NONE',  ( 56.55820758832960138, -46.20897426240800598, -26.26650421730799678 ) ) ;
#29393=CARTESIAN_POINT ( 'NONE',  ( 52.63953642234350383, -49.80174121720269653, -48.69586908824970095 ) ) ;
#29396=CARTESIAN_POINT ( 'NONE',  ( 13.87643720199350028, 20.51618323985760028, -75.32473453343510528 ) ) ;
#29398=AXIS2_PLACEMENT_3D ( 'NONE', #29786, #5969, #38195 ) ;
#29403=ORIENTED_EDGE ( 'NONE', *, *, #28294, .F. ) ;
#29404=CARTESIAN_POINT ( 'NONE',  ( 52.61201418140420571, -49.81418459234139817, -28.15000000000000213 ) ) ;
#29405=CARTESIAN_POINT ( 'NONE',  ( 16.58032161480830169, -51.11619067739219702, -20.45514663783470155 ) ) ;
#29406=CARTESIAN_POINT ( 'NONE',  ( 10.35837886327420065, 33.32232037452499895, -17.68810962647529905 ) ) ;
#29407=DIRECTION ( 'NONE',  ( -0.2260571801428130634, -5.828670879282072626E-15, 0.9741140340359951688 ) ) ;
#29410=CARTESIAN_POINT ( 'NONE',  ( -11.32734370190460105, -41.88171845330919751, -6.430192534648670133 ) ) ;
#29411=CARTESIAN_POINT ( 'NONE',  ( 47.43185934795429404, 23.40577861522420022, -54.84779215339789715 ) ) ;
#29413=CARTESIAN_POINT ( 'NONE',  ( 57.32763708541499881, -50.39928489432909942, -53.00790317329960288 ) ) ;
#29414=CARTESIAN_POINT ( 'NONE',  ( 11.44080308043550076, 34.06382446123569707, -17.48917067575129991 ) ) ;
#29417=CARTESIAN_POINT ( 'NONE',  ( 8.784728771177219286, 31.88305279678909443, -46.67204636144870022 ) ) ;
#29418=CARTESIAN_POINT ( 'NONE',  ( 53.59007319635580302, -49.40623578145689976, -49.22505640097240587 ) ) ;
#29420=CARTESIAN_POINT ( 'NONE',  ( 52.93160674638770047, 21.02777951207980323, -54.03607036502950223 ) ) ;
#29425=CARTESIAN_POINT ( 'NONE',  ( 9.733202698440479139, 31.94412001969340054, -46.29921928092249317 ) ) ;
#29426=CARTESIAN_POINT ( 'NONE',  ( 43.87445613097960262, 13.83391143939489965, -6.621204841358950155 ) ) ;
#29427=ADVANCED_FACE ( 'NONE', ( #31090 ), #25595, .T. ) ;
#29428=CARTESIAN_POINT ( 'NONE',  ( 66.37091707294710830, -30.63654346061790079, -16.96663971210719879 ) ) ;
#29429=CARTESIAN_POINT ( 'NONE',  ( 18.50147319020889825, 20.38774172224130155, -75.08736963500949457 ) ) ;
#29435=CARTESIAN_POINT ( 'NONE',  ( 11.71313963123279933, -65.09861111722139526, -46.54370187508719425 ) ) ;
#29436=CARTESIAN_POINT ( 'NONE',  ( 57.06654200124710030, -45.67870534195919419, -26.17304345835309931 ) ) ;
#29440=CARTESIAN_POINT ( 'NONE',  ( 61.73008982643180076, 13.88381104171409852, -46.37201266034419689 ) ) ;
#29443=VECTOR ( 'NONE', #44148, 1000.000000000000114 ) ;
#29444=CARTESIAN_POINT ( 'NONE',  ( 75.04939620295748171, -15.61618894467929941, -11.30491871076499955 ) ) ;
#29446=CARTESIAN_POINT ( 'NONE',  ( 54.17850344129180229, -45.61389549855280023, -15.02769642854620002 ) ) ;
#29449=ORIENTED_EDGE ( 'NONE', *, *, #45844, .T. ) ;
#29450=DIRECTION ( 'NONE',  ( 0.4145156864928219997, -0.9100421669633689259, 0.000000000000000000 ) ) ;
#29451=CARTESIAN_POINT ( 'NONE',  ( 46.81364246026949871, -53.87014086992079598, -75.86283294038038605 ) ) ;
#29452=DIRECTION ( 'NONE',  ( 0.000000000000000000, 0.000000000000000000, 1.000000000000000000 ) ) ;
#29454=CARTESIAN_POINT ( 'NONE',  ( 50.78057069950819624, 14.75089828130050051, -12.88396743804300115 ) ) ;
#29455=CARTESIAN_POINT ( 'NONE',  ( 19.53299567489768407, -55.47150705052180086, -75.56421958049284626 ) ) ;
#29456=CARTESIAN_POINT ( 'NONE',  ( 41.64265090550289727, 15.19461330350370076, -4.296538310234210734 ) ) ;
#29458=CARTESIAN_POINT ( 'NONE',  ( 11.11660069372041804, -63.29819265419726548, -14.66254990259057855 ) ) ;
#29459=CARTESIAN_POINT ( 'NONE',  ( 57.45421615888909628, 13.89859616986070101, -25.53723535916439857 ) ) ;
#29461=EDGE_LOOP ( 'NONE', ( #22715, #10058, #30654, #25092, #45787 ) ) ;
#29464=CARTESIAN_POINT ( 'NONE',  ( 15.67962062535580081, -50.86266781815560023, -15.65622421709140077 ) ) ;
#29466=AXIS2_PLACEMENT_3D ( 'NONE', #13989, #21568, #38093 ) ;
#29468=CARTESIAN_POINT ( 'NONE',  ( 11.74347662706570006, -64.88511784619510081, -16.31133514117630057 ) ) ;
#29471=CARTESIAN_POINT ( 'NONE',  ( 48.92567656525680064, -53.97674872320250472, -55.07030108398770096 ) ) ;
#29472=B_SPLINE_CURVE_WITH_KNOTS ( 'NONE', 3,
 ( #40285, #4897, #8578, #5172, #4376, #41312, #48405, #965, #8835, #32645, #20865, #12504 ),
 .UNSPECIFIED., .F., .F.,
 ( 4, 2, 2, 2, 2, 4 ),
 ( 0.000000000000000000, 0.1250000000000001110, 0.2500000000000002220, 0.5000000000000001110, 0.7500000000000001110, 1.000000000000000000 ),
 .UNSPECIFIED. ) ;
#29475=CARTESIAN_POINT ( 'NONE',  ( 18.66237388361239624, -51.43165038652999499, -74.14992922886710858 ) ) ;
#29481=VERTEX_POINT ( 'NONE', #3855 ) ;
#29482=CARTESIAN_POINT ( 'NONE',  ( 11.13393739769619906, 32.24968758154479787, -24.15000000000000213 ) ) ;
#29483=CARTESIAN_POINT ( 'NONE',  ( 61.13062736222009619, -45.51825399203449507, -47.54701560607519895 ) ) ;
#29485=CARTESIAN_POINT ( 'NONE',  ( 12.16981617636350066, 18.81688479155219795, -21.14999999999999858 ) ) ;
#29489=CARTESIAN_POINT ( 'NONE',  ( 68.13393739769620083, -50.61618894467930119, -73.25000000000000000 ) ) ;
#29492=EDGE_CURVE ( 'NONE', #13640, #51441, #42356, .T. ) ;
#29497=CARTESIAN_POINT ( 'NONE',  ( 52.65975762845060615, -49.78933466291119458, -48.73990261843160710 ) ) ;
#29499=CARTESIAN_POINT ( 'NONE',  ( 68.13393739769620083, 1.883811055320649963, -65.65000000000000568 ) ) ;
#29501=VERTEX_POINT ( 'NONE', #8035 ) ;
#29506=CARTESIAN_POINT ( 'NONE',  ( 1.027904703268269992, 11.45423359053189927, -15.65000000000000036 ) ) ;
#29509=AXIS2_PLACEMENT_3D ( 'NONE', #7553, #3621, #15925 ) ;
#29510=CARTESIAN_POINT ( 'NONE',  ( 52.96554027761909822, -50.86173948047620286, -76.26079925769791146 ) ) ;
#29514=CARTESIAN_POINT ( 'NONE',  ( 47.18324198357289845, 23.57489020266570279, -74.14999999999999147 ) ) ;
#29515=CARTESIAN_POINT ( 'NONE',  ( 41.31713230452019303, 13.54959124757960076, -5.389667122562360468 ) ) ;
#29516=ADVANCED_FACE ( 'NONE', ( #10950 ), #31344, .T. ) ;
#29517=CARTESIAN_POINT ( 'NONE',  ( 43.52753934306360151, -43.62935524535279797, -5.023899789736471000 ) ) ;
#29519=CARTESIAN_POINT ( 'NONE',  ( 55.91596999402320023, 14.67228162054319895, -25.32543311652580087 ) ) ;
#29521=DIRECTION ( 'NONE',  ( -1.000000000000000000, 0.000000000000000000, 0.000000000000000000 ) ) ;
#29522=CARTESIAN_POINT ( 'NONE',  ( 67.87922885512119819, -0.5138706640943320192, -17.86501260203199948 ) ) ;
#29523=B_SPLINE_SURFACE_WITH_KNOTS ( 'NONE', 3, 3, ( 
 ( #14936, #23287, #15973, #30901, #47948, #12050, #47441, #46930 ),
 ( #26986, #7088, #3413, #15712, #15463, #39564, #19640, #23039 ),
 ( #47692, #11795, #27756, #43752, #3153, #44259, #20655, #13341 ),
 ( #8367, #24573, #28522, #45042, #32961, #20919, #44008, #32179 ),
 ( #8111, #4684, #36913, #48721, #4944, #40076, #1017, #20145 ),
 ( #44520, #48195, #24315, #40845, #24057, #36136, #16224, #4168 ),
 ( #12824, #17013, #48990, #9142, #13095, #28259, #40334, #32432 ),
 ( #36640, #37179, #29046, #49246, #25097, #239, #41109, #48454 ),
 ( #16741, #12559, #20396, #743, #5220, #32695, #12300, #28782 ) ),
 .UNSPECIFIED., .F., .F., .F.,
 ( 4, 1, 1, 1, 1, 1, 4 ),
 ( 4, 2, 2, 4 ),
 ( -1.933923635888309730E-05, 0.1666666666666670182, 0.3333333333333329818, 0.5000000000000000000, 0.6666666666666670737, 0.8333333333333330373, 1.000023964450169833 ),
 ( -10.25171765628389942, -6.367128310144029690, -2.534746465614240218, -0.1881082593979860051 ),
 .UNSPECIFIED. ) ;
#29525=CARTESIAN_POINT ( 'NONE',  ( 13.95043133595810048, -52.17403775882060302, -75.62474771911479365 ) ) ;
#29526=CIRCLE ( 'NONE', #44609, 2.000000000000002220 ) ;
#29527=CARTESIAN_POINT ( 'NONE',  ( 47.18324198357289845, -54.80726809202429450, -54.61058319554170026 ) ) ;
#29531=CARTESIAN_POINT ( 'NONE',  ( 13.00893739769619906, -65.51843714052719747, -23.32157302967710422 ) ) ;
#29532=CARTESIAN_POINT ( 'NONE',  ( 10.85466640526500015, 33.73459223953250330, -17.55961383757770022 ) ) ;
#29535=CARTESIAN_POINT ( 'NONE',  ( 48.36908225894410407, 22.86152331119799896, -54.63163985339289752 ) ) ;
#29537=AXIS2_PLACEMENT_3D ( 'NONE', #9395, #20378, #13576 ) ;
#29544=CARTESIAN_POINT ( 'NONE',  ( 83.51014914612841267, 13.55547819151079914, -46.95038033932869581 ) ) ;
#29545=CARTESIAN_POINT ( 'NONE',  ( 52.57331519483629734, 18.62081213560140114, -27.97396291639740085 ) ) ;
#29552=ORIENTED_EDGE ( 'NONE', *, *, #38044, .T. ) ;
#29553=CARTESIAN_POINT ( 'NONE',  ( 12.16177399482889854, -65.11171494345551025, -16.53048058985559976 ) ) ;
#29554=CARTESIAN_POINT ( 'NONE',  ( 11.13615425759000033, 32.70713249819939961, -44.52190971338829684 ) ) ;
#29556=CARTESIAN_POINT ( 'NONE',  ( 12.45971295103579912, 34.17435175697750083, -46.68166270225199810 ) ) ;
#29557=LINE ( 'NONE', #49247, #21646 ) ;
#29562=CARTESIAN_POINT ( 'NONE',  ( 49.63827221850689853, 21.52948366499370181, -52.16690606469470026 ) ) ;
#29563=DIRECTION ( 'NONE',  ( 1.000000000000000000, 0.000000000000000000, 0.000000000000000000 ) ) ;
#29564=CARTESIAN_POINT ( 'NONE',  ( 51.29313475710210213, -49.49861581368470098, -76.46030551791849916 ) ) ;
#29565=CARTESIAN_POINT ( 'NONE',  ( 10.61751707702999958, -64.82563018156609758, -18.17419295931939871 ) ) ;
#29566=ORIENTED_EDGE ( 'NONE', *, *, #16591, .T. ) ;
#29567=CARTESIAN_POINT ( 'NONE',  ( 52.87639532687909849, -49.52782412333860407, -27.19604750702719898 ) ) ;
#29568=LINE ( 'NONE', #45574, #24205 ) ;
#29569=ORIENTED_EDGE ( 'NONE', *, *, #26257, .F. ) ;
#29571=CYLINDRICAL_SURFACE ( 'NONE', #1883, 21.50000000000000000 ) ;
#29573=CARTESIAN_POINT ( 'NONE',  ( 68.13393739769769297, 18.72622661238300168, -73.39853292320978539 ) ) ;
#29574=CARTESIAN_POINT ( 'NONE',  ( 53.84012107995949492, 19.74703357530859904, -75.89928047384410092 ) ) ;
#29576=CARTESIAN_POINT ( 'NONE',  ( 47.51793463416109375, -54.37766850872819901, -75.00961804031550173 ) ) ;
#29578=CARTESIAN_POINT ( 'NONE',  ( 55.84963547784990112, 14.51039859417369904, -16.94429277193919958 ) ) ;
#29582=CARTESIAN_POINT ( 'NONE',  ( 57.04000892342570239, -50.62678238285099752, -53.73354994388930095 ) ) ;
#29584=DIRECTION ( 'NONE',  ( -0.6676418852213141797, -0.2329255526946994725, -0.7071067811865463515 ) ) ;
#29585=CARTESIAN_POINT ( 'NONE',  ( 47.03708331872790183, 22.68146662604199548, -75.76197391125640479 ) ) ;
#29587=CARTESIAN_POINT ( 'NONE',  ( 75.29711369228711249, -36.44373308530014555, -12.51629082861420983 ) ) ;
#29588=FACE_OUTER_BOUND ( 'NONE', #12217, .T. ) ;
#29592=CARTESIAN_POINT ( 'NONE',  ( 60.24058964203519650, -45.77817723718867171, -47.32689780713828753 ) ) ;
#29593=CARTESIAN_POINT ( 'NONE',  ( 88.13393739769620083, -48.61618894467930119, -65.65000000000000568 ) ) ;
#29595=CARTESIAN_POINT ( 'NONE',  ( 61.30391822008160574, 13.98869160185730109, -46.40371986329420650 ) ) ;
#29597=CARTESIAN_POINT ( 'NONE',  ( -28.48658230523989943, 4.086499779700029755, -54.95457219459440523 ) ) ;
#29599=CARTESIAN_POINT ( 'NONE',  ( 52.80835662174770562, -49.67696413664329924, -48.72774921968630224 ) ) ;
#29601=CARTESIAN_POINT ( 'NONE',  ( 61.72354181936940165, -45.11618267485779654, -28.15139908431080329 ) ) ;
#29603=CARTESIAN_POINT ( 'NONE',  ( 13.41560639233609997, 19.85270852858930013, -21.91538712361600005 ) ) ;
#29606=CARTESIAN_POINT ( 'NONE',  ( 50.04022686075009574, 17.68250774392249980, -76.14999999999999147 ) ) ;
#29607=CARTESIAN_POINT ( 'NONE',  ( 53.23191249145569515, 18.23954733812280082, -48.99600492437400590 ) ) ;
#29608=CARTESIAN_POINT ( 'NONE',  ( 60.83775786089130122, -45.46530407581749955, -47.05478991720049464 ) ) ;
#29609=CARTESIAN_POINT ( 'NONE',  ( 47.26610112325450075, 22.82567072896360116, -75.56421356201970241 ) ) ;
#29614=CARTESIAN_POINT ( 'NONE',  ( 47.42536334077440330, -54.63837742691509902, -54.75923846447550147 ) ) ;
#29617=CARTESIAN_POINT ( 'NONE',  ( 11.75767683379359951, -65.42451930117039183, -18.01774807210410145 ) ) ;
#29618=CARTESIAN_POINT ( 'NONE',  ( 53.26662649590710430, 18.19965403720820163, -48.79175420715159817 ) ) ;
#29619=ADVANCED_FACE ( 'NONE', ( #11207 ), #17606, .T. ) ;
#29622=CARTESIAN_POINT ( 'NONE',  ( 48.82567944655220060, -28.11618894467929763, -15.65000000000000036 ) ) ;
#29625=ORIENTED_EDGE ( 'NONE', *, *, #35181, .F. ) ;
#29626=CARTESIAN_POINT ( 'NONE',  ( 9.281183340106311519, -63.16631044210069490, -46.53144401359779891 ) ) ;
#29630=CARTESIAN_POINT ( 'NONE',  ( 67.56344246713349833, -30.11618894467929763, -21.20855465508889992 ) ) ;
#29632=CARTESIAN_POINT ( 'NONE',  ( 52.83096320285449821, 19.79380150020979912, -76.09006749206929499 ) ) ;
#29638=CARTESIAN_POINT ( 'NONE',  ( 16.13393739769620083, -15.61618894467929941, -10.90000000000000036 ) ) ;
#29642=CARTESIAN_POINT ( 'NONE',  ( 57.11003303655699881, -45.86943814250939511, -26.25113407850079739 ) ) ;
#29647=CARTESIAN_POINT ( 'NONE',  ( 14.13833034204109929, 19.89798265472740013, -74.14993923597710079 ) ) ;
#29648=CARTESIAN_POINT ( 'NONE',  ( 12.84688943576609788, -51.59382062313621020, -21.73578643762666474 ) ) ;
#29649=CARTESIAN_POINT ( 'NONE',  ( 43.56376642346300798, -45.24482142066580792, -7.028087995143840416 ) ) ;
#29653=VERTEX_POINT ( 'NONE', #24667 ) ;
#29654=CARTESIAN_POINT ( 'NONE',  ( 54.30624051828319665, -47.99265254736189945, -26.34811334082180068 ) ) ;
#29655=CARTESIAN_POINT ( 'NONE',  ( 15.24233146011200013, -51.07047254194969810, -21.55962016779339763 ) ) ;
#29656=CARTESIAN_POINT ( 'NONE',  ( 0.07122129016301401161, 22.52064049785749944, -9.361296192847889941 ) ) ;
#29657=CARTESIAN_POINT ( 'NONE',  ( 45.83414061996360545, -15.61618894467929586, 7.944363289481099599 ) ) ;
#29659=CARTESIAN_POINT ( 'NONE',  ( 8.784728771152170879, -54.93525725209899235, -46.67204636145419983 ) ) ;
#29661=CARTESIAN_POINT ( 'NONE',  ( -9.530397888691508612, -43.65111778182789948, -5.718006680799840424 ) ) ;
#29662=CARTESIAN_POINT ( 'NONE',  ( 47.42537234911539912, 23.41034979696710039, -54.89678846924610411 ) ) ;
#29664=CARTESIAN_POINT ( 'NONE',  ( 61.05528012745969590, 14.12195704883330194, -46.96576354475939752 ) ) ;
#29665=CARTESIAN_POINT ( 'NONE',  ( 43.91474985106849971, 12.31375205234749970, -5.093415854460159764 ) ) ;
#29666=CARTESIAN_POINT ( 'NONE',  ( 51.99247920141849733, 18.26518619690140000, -77.11023342130459923 ) ) ;
#29667=CARTESIAN_POINT ( 'NONE',  ( 53.41693480164800434, 18.12090330447900044, -48.75416851879799651 ) ) ;
#29668=DIRECTION ( 'NONE',  ( -0.6911981449639439390, -0.7226652920947588266, 0.000000000000000000 ) ) ;
#29672=CARTESIAN_POINT ( 'NONE',  ( 53.42290160909190178, 20.83982452118389972, -54.29362578891399949 ) ) ;
#29674=DIRECTION ( 'NONE',  ( 0.000000000000000000, 0.000000000000000000, -1.000000000000000000 ) ) ;
#29676=CARTESIAN_POINT ( 'NONE',  ( 19.71487976213365201, 22.98215037303318553, -17.34801211495729234 ) ) ;
#29677=CARTESIAN_POINT ( 'NONE',  ( 10.97982412035660005, 32.17011673400409677, -44.74671143413180374 ) ) ;
#29679=CARTESIAN_POINT ( 'NONE',  ( 66.39754877122931020, -33.04911773559199872, -19.74076586694979696 ) ) ;
#29685=CARTESIAN_POINT ( 'NONE',  ( 48.76908445385270596, 22.82217318232569880, -55.30112621652450144 ) ) ;
#29686=VECTOR ( 'NONE', #45467, 1000.000000000000000 ) ;
#29688=CARTESIAN_POINT ( 'NONE',  ( 12.11637196722969989, -65.28199310085939544, -46.68580356066069470 ) ) ;
#29689=CARTESIAN_POINT ( 'NONE',  ( 57.46694081946250066, -45.43955118043039931, -26.08166122527880049 ) ) ;
#29695=CARTESIAN_POINT ( 'NONE',  ( 48.64442696764240281, -45.11618894461089724, -9.632282537063208139 ) ) ;
#29697=CARTESIAN_POINT ( 'NONE',  ( 15.36633100621490122, 19.87547805676619816, -21.74512139206969863 ) ) ;
#29700=VERTEX_POINT ( 'NONE', #24409 ) ;
#29701=DIRECTION ( 'NONE',  ( 0.000000000000000000, 0.000000000000000000, -1.000000000000000000 ) ) ;
#29702=CARTESIAN_POINT ( 'NONE',  ( 46.89823403300989924, -54.16139584019150277, -75.66073271794819277 ) ) ;
#29703=DIRECTION ( 'NONE',  ( 1.000000000000000000, 0.000000000000000000, 0.000000000000000000 ) ) ;
#29704=CARTESIAN_POINT ( 'NONE',  ( 49.01168265687110193, 13.88381105532070059, -9.596379464110540880 ) ) ;
#29708=CARTESIAN_POINT ( 'NONE',  ( 50.96210802353969882, 19.72521229730620007, -76.15000017728949899 ) ) ;
#29709=CARTESIAN_POINT ( 'NONE',  ( 61.66992079451529918, 13.88595891104769997, -28.08578151254650024 ) ) ;
#29712=B_SPLINE_SURFACE_WITH_KNOTS ( 'NONE', 3, 3, ( 
 ( #19432, #11844, #31462, #39359, #19933, #39612, #43799, #27802, #51157, #47486, #11324, #15251 ),
 ( #32222, #31712, #41, #28304, #11582, #28047, #51665, #36178, #7899, #27543, #19687, #47993 ),
 ( #40373, #4214, #285, #12093, #23845, #31973, #35680, #15759, #15508, #35411, #35924, #44051 ),
 ( #47737, #44305, #31204, #27288, #24360, #51413, #16269, #24100, #39869, #16017, #8156, #40121 ),
 ( #20188, #48246, #12340, #8414, #4471, #20440, #43296, #7388, #37226, #33536, #12870, #45352 ),
 ( #20697, #40631, #25146, #44829, #29088, #8666, #21479, #49554, #37479, #8935, #1579, #13388 ),
 ( #13138, #41406, #41150, #5524, #17569, #33275, #17312, #1323, #13642, #16522, #9194, #9455 ),
 ( #29601, #48501, #36688, #49291, #32738, #45605, #20961, #36961, #9702, #1059, #25663, #29347 ),
 ( #25404, #41666, #48766, #5264, #5770, #36427, #12603, #535, #28826, #32470, #28565, #44565 ) ),
 .UNSPECIFIED., .F., .F., .F.,
 ( 4, 1, 1, 1, 1, 1, 4 ),
 ( 4, 2, 2, 2, 2, 4 ),
 ( -0.0004221351757990000008, 0.1666666666666670182, 0.3333333333333329818, 0.5000000000000000000, 0.6666666666666670737, 0.8333333333333330373, 1.000484995316600179 ),
 ( -0.0004754643611709999948, 0.1427389027784959907, 0.4935706371843600060, 0.8180431554277900474, 1.090724207237049992, 1.220493132826130145 ),
 .UNSPECIFIED. ) ;
#29713=ORIENTED_EDGE ( 'NONE', *, *, #10774, .F. ) ;
#29714=CARTESIAN_POINT ( 'NONE',  ( 49.40552051342540096, 22.26542118999089936, -54.15739458345379376 ) ) ;
#29720=DIRECTION ( 'NONE',  ( 0.2260571801428161443, 0.000000000000000000, -0.9741140340359945027 ) ) ;
#29725=CARTESIAN_POINT ( 'NONE',  ( 76.48559721756747365, -43.24489215890645966, -14.05942286515468709 ) ) ;
#29726=CARTESIAN_POINT ( 'NONE',  ( -6.866062602303800055, -15.61618894467929586, -15.65000000000000036 ) ) ;
#29731=CARTESIAN_POINT ( 'NONE',  ( 54.47259832750690123, -46.25232753665150653, -15.76422791930239953 ) ) ;
#29732=CARTESIAN_POINT ( 'NONE',  ( 60.82047572193099683, -45.70664521776530620, -47.72863310528089897 ) ) ;
#29736=DIRECTION ( 'NONE',  ( 0.000000000000000000, 1.000000000000000000, 0.000000000000000000 ) ) ;
#29739=CARTESIAN_POINT ( 'NONE',  ( 40.82288980517279953, -45.39598238709950095, -5.804594144209599627 ) ) ;
#29744=B_SPLINE_CURVE_WITH_KNOTS ( 'NONE', 3,
 ( #39140, #26807, #50928, #3232, #15287, #35189, #35451, #51193, #15024, #30992, #47270, #46239, #2975, #11358, #43330, #14251, #26287, #30220, #42296, #10327, #42819, #27069 ),
 .UNSPECIFIED., .F., .F.,
 ( 4, 2, 1, 1, 2, 2, 2, 2, 1, 1, 2, 2, 4 ),
 ( 0.5278395012772089112, 0.5352170090697533356, 0.5425945168622977599, 0.5573495324473857204, 0.5868595636175617525, 0.6458796259579139276, 0.7639197506386171677, 0.7712972584311608149, 0.7786747662237045731, 0.7934297818087913123, 0.8229398129789644578, 0.8819598753193100826, 1.000000000000000000 ),
 .UNSPECIFIED. ) ;
#29745=EDGE_LOOP ( 'NONE', ( #29098, #10448, #8465, #33223, #40723 ) ) ;
#29751=CARTESIAN_POINT ( 'NONE',  ( 7.853097003783789276, 29.28805065900050053, -20.86915960608759946 ) ) ;
#29755=CARTESIAN_POINT ( 'NONE',  ( 52.21153808996899670, -50.42173267543250148, -76.55085343181869462 ) ) ;
#29758=CIRCLE ( 'NONE', #9692, 2.999999999999999112 ) ;
#29760=CARTESIAN_POINT ( 'NONE',  ( 43.56381279507350257, 14.01244564278079885, -7.028114315100149945 ) ) ;
#29761=CARTESIAN_POINT ( 'NONE',  ( 42.15277068293529794, -43.77269754269769919, -4.489091470016449925 ) ) ;
#29762=LINE ( 'NONE', #37140, #17805 ) ;
#29763=CARTESIAN_POINT ( 'NONE',  ( -6.923935172077830380, 14.83398127567929947, -5.625849176739690094 ) ) ;
#29766=AXIS2_PLACEMENT_3D ( 'NONE', #23458, #34751, #2543 ) ;
#29768=CARTESIAN_POINT ( 'NONE',  ( 66.23675738725249573, 0.5074413136232309718, -17.49605282672580131 ) ) ;
#29770=CARTESIAN_POINT ( 'NONE',  ( 14.90064049178520023, -52.99263752172900155, -76.14999999999999147 ) ) ;
#29772=CARTESIAN_POINT ( 'NONE',  ( 47.18324198357289845, -54.80726809202429450, -54.61058319554170026 ) ) ;
#29773=ADVANCED_FACE ( 'NONE', ( #42244 ), #38308, .T. ) ;
#29775=CARTESIAN_POINT ( 'NONE',  ( 57.55751162049570269, -48.61618894467930119, -53.92796738110899923 ) ) ;
#29778=CARTESIAN_POINT ( 'NONE',  ( 47.68932896513950226, -54.51079220110009516, -55.03972088635050142 ) ) ;
#29779=CARTESIAN_POINT ( 'NONE',  ( 47.40322300430479885, 23.42336669154508755, -60.76348542011150045 ) ) ;
#29781=CARTESIAN_POINT ( 'NONE',  ( 48.05009841671569859, 23.12298604439770244, -55.13457781729299967 ) ) ;
#29786=CARTESIAN_POINT ( 'NONE',  ( 16.13393739769620083, -15.61618894467929941, 6.850000000000000533 ) ) ;
#29788=CARTESIAN_POINT ( 'NONE',  ( 83.30448183675929386, 14.00823756214430027, -47.41172112684520101 ) ) ;
#29789=CARTESIAN_POINT ( 'NONE',  ( 54.53415579258169998, 16.40665704925320156, -25.91141317301960001 ) ) ;
#29794=EDGE_CURVE ( 'NONE', #17232, #45765, #26428, .T. ) ;
#29795=LINE ( 'NONE', #18274, #27305 ) ;
#29800=CARTESIAN_POINT ( 'NONE',  ( 12.26707159644750078, -64.72375542069319465, -15.95265749177709935 ) ) ;
#29801=CARTESIAN_POINT ( 'NONE',  ( 11.09709394051290055, 32.24280216238350505, -44.33319920883189980 ) ) ;
#29806=VERTEX_POINT ( 'NONE', #41984 ) ;
#29810=CARTESIAN_POINT ( 'NONE',  ( 48.66127576079219352, 22.44898377099470110, -53.72649052181260032 ) ) ;
#29811=CARTESIAN_POINT ( 'NONE',  ( 59.28329934267080148, -2.939009483360070174, -15.67174078617610000 ) ) ;
#29812=CARTESIAN_POINT ( 'NONE',  ( 51.02429472136520161, -50.08032363113679963, -76.22815769145680065 ) ) ;
#29813=CARTESIAN_POINT ( 'NONE',  ( 57.23219029305369787, -49.86398702007070227, -52.24802155864789910 ) ) ;
#29816=CARTESIAN_POINT ( 'NONE',  ( 66.23540447448930024, 18.72622661238580122, -71.50000000000139266 ) ) ;
#29817=EDGE_LOOP ( 'NONE', ( #42759, #10892, #40468, #24187, #29181, #20515 ) ) ;
#29818=CARTESIAN_POINT ( 'NONE',  ( 12.40077350670613043, -55.44147723767447644, -75.14570525077779450 ) ) ;
#29821=CARTESIAN_POINT ( 'NONE',  ( 13.47931665894660114, -51.05589467822899508, -21.90688212588430162 ) ) ;
#29823=CARTESIAN_POINT ( 'NONE',  ( 56.90565801091290155, 19.41243383275969947, -74.14906031689440624 ) ) ;
#29824=CARTESIAN_POINT ( 'NONE',  ( 46.35275103504449845, -52.90993241930539881, -76.14999999999999147 ) ) ;
#29825=VERTEX_POINT ( 'NONE', #26493 ) ;
#29826=CARTESIAN_POINT ( 'NONE',  ( 55.52096773173170163, 14.56742854200139980, -16.43721700016279996 ) ) ;
#29828=CARTESIAN_POINT ( 'NONE',  ( 56.89013221634429840, -50.62054540486399645, -53.45144266526210686 ) ) ;
#29829=CARTESIAN_POINT ( 'NONE',  ( 52.82296810369110318, -49.70143565027870380, -48.95261578732520036 ) ) ;
#29830=AXIS2_PLACEMENT_3D ( 'NONE', #50558, #37989, #38245 ) ;
#29834=CARTESIAN_POINT ( 'NONE',  ( 46.89990028981509340, 22.38086965127029870, -75.96273535411170030 ) ) ;
#29837=CARTESIAN_POINT ( 'NONE',  ( 61.28085240419530066, -45.60177449860450594, -47.67834116410560341 ) ) ;
#29839=DIRECTION ( 'NONE',  ( 0.000000000000000000, 0.000000000000000000, 1.000000000000000000 ) ) ;
#29842=FACE_OUTER_BOUND ( 'NONE', #34128, .T. ) ;
#29845=CARTESIAN_POINT ( 'NONE',  ( 61.33741810518110071, 13.97252490929749946, -46.44068268147909606 ) ) ;
#29846=CARTESIAN_POINT ( 'NONE',  ( -29.85095995338080144, 4.820344610801059915, -56.22640780866669985 ) ) ;
#29847=ORIENTED_EDGE ( 'NONE', *, *, #23864, .T. ) ;
#29848=CARTESIAN_POINT ( 'NONE',  ( 52.78558355087229614, -49.68653575824099988, -48.61478092265500095 ) ) ;
#29852=CARTESIAN_POINT ( 'NONE',  ( 13.64707893708750142, 19.57323805727630273, -21.56006118760380019 ) ) ;
#29853=CARTESIAN_POINT ( 'NONE',  ( 56.70066228015040366, 14.05114599519139951, -25.36386621698419930 ) ) ;
#29855=CARTESIAN_POINT ( 'NONE',  ( 50.77827180918709615, 19.51522592562140090, -76.14999999999999147 ) ) ;
#29856=CARTESIAN_POINT ( 'NONE',  ( 53.31861474840820136, 18.21232818371930051, -49.05456087792640574 ) ) ;
#29858=CARTESIAN_POINT ( 'NONE',  ( 60.45089258339159954, -45.66799363392549793, -47.18958319368170606 ) ) ;
#29862=EDGE_CURVE ( 'NONE', #27228, #5608, #17248, .T. ) ;
#29866=CARTESIAN_POINT ( 'NONE',  ( 10.61751707702999958, -64.82563018156609758, -18.17421237900310160 ) ) ;
#29868=DIRECTION ( 'NONE',  ( 0.6415444970810870728, -0.4854844151940968522, 0.5939070136550171908 ) ) ;
#29874=CARTESIAN_POINT ( 'NONE',  ( 13.81959240480470008, -51.26308380621749450, -23.06522850035179673 ) ) ;
#29877=DIRECTION ( 'NONE',  ( -0.7226652920947592706, 0.6911981449639433839, 0.000000000000000000 ) ) ;
#29880=CARTESIAN_POINT ( 'NONE',  ( 52.96724627483459358, 19.31611233144339934, -76.71296415647860556 ) ) ;
#29891=ORIENTED_EDGE ( 'NONE', *, *, #28393, .T. ) ;
#29894=B_SPLINE_CURVE_WITH_KNOTS ( 'NONE', 3,
 ( #44387, #49369, #5598, #4809, #36765, #21554, #8488, #40449, #1655, #16596, #45428, #1396, #876, #24434, #17385, #16869 ),
 .UNSPECIFIED., .F., .F.,
 ( 4, 2, 2, 2, 2, 2, 2, 4 ),
 ( 0.000000000000000000, 2.041349754395100025, 4.374320902275210088, 5.832427869700280709, 6.561481353412809803, 7.727966927352870385, 9.594343845656959857, 11.66485573940060050 ),
 .UNSPECIFIED. ) ;
#29897=CARTESIAN_POINT ( 'NONE',  ( 14.41160410444349793, 20.07361457936550053, -75.01675372117850316 ) ) ;
#29901=CARTESIAN_POINT ( 'NONE',  ( 42.61259335559390138, -45.06347766768709562, -6.251417111687170625 ) ) ;
#29905=EDGE_LOOP ( 'NONE', ( #12417, #6960, #2680, #32357 ) ) ;
#29906=CARTESIAN_POINT ( 'NONE',  ( 55.70826441393730022, -46.17759071057790266, -25.46014295398670058 ) ) ;
#29907=CARTESIAN_POINT ( 'NONE',  ( 15.36633100619899928, -51.10785594612259786, -21.74512139207759986 ) ) ;
#29908=CARTESIAN_POINT ( 'NONE',  ( 4.370623416934749095, 25.31564308878670033, -9.528750125106599356 ) ) ;
#29911=DIRECTION ( 'NONE',  ( 0.000000000000000000, 0.000000000000000000, -1.000000000000000000 ) ) ;
#29913=CARTESIAN_POINT ( 'NONE',  ( -9.520856997028319668, -43.66653613195550321, -5.779509720377040694 ) ) ;
#29914=CARTESIAN_POINT ( 'NONE',  ( 47.47148429121339319, 23.37856424063020100, -54.78605424627399856 ) ) ;
#29916=DIRECTION ( 'NONE',  ( -0.8857883891771956009, -0.4640893551880597712, 0.000000000000000000 ) ) ;
#29919=CARTESIAN_POINT ( 'NONE',  ( 11.82286116601290082, 33.96844483572419904, -16.82382485988169663 ) ) ;
#29923=CARTESIAN_POINT ( 'NONE',  ( 10.61754762155600140, 33.59328422689429772, -18.17417937929459981 ) ) ;
#29925=CARTESIAN_POINT ( 'NONE',  ( 52.97539169126969938, 21.03044668291709840, -54.26108799293329810 ) ) ;
#29930=ORIENTED_EDGE ( 'NONE', *, *, #20225, .T. ) ;
#29931=CARTESIAN_POINT ( 'NONE',  ( 19.95098317553492251, 23.65890106099656620, -18.38988218853045709 ) ) ;
#29932=CARTESIAN_POINT ( 'NONE',  ( 10.48989095044620079, 31.99911048416310422, -45.62579085507780974 ) ) ;
#29934=CARTESIAN_POINT ( 'NONE',  ( 65.89614409097049474, -31.41618784131230413, -17.15307145949229906 ) ) ;
#29937=CARTESIAN_POINT ( 'NONE',  ( 14.34417029198879945, -52.11618894467940066, -21.14999999999999858 ) ) ;
#29939=VERTEX_POINT ( 'NONE', #10203 ) ;
#29940=CARTESIAN_POINT ( 'NONE',  ( 48.63696446388820505, 22.87845126040220123, -55.31022682284890379 ) ) ;
#29942=B_SPLINE_CURVE_WITH_KNOTS ( 'NONE', 3,
 ( #27299, #11078, #27553, #39625 ),
 .UNSPECIFIED., .F., .F.,
 ( 4, 4 ),
 ( 0.000000000000000000, 0.1924323111301881328 ),
 .UNSPECIFIED. ) ;
#29943=ORIENTED_EDGE ( 'NONE', *, *, #49162, .F. ) ;
#29944=CARTESIAN_POINT ( 'NONE',  ( 11.22793056427740055, -64.23882544888471102, -44.76071414201179977 ) ) ;
#29945=CARTESIAN_POINT ( 'NONE',  ( 57.18966657269059795, -45.47098121815820093, -26.05770951134740088 ) ) ;
#29949=EDGE_LOOP ( 'NONE', ( #40059, #4108, #10769, #21064, #14869, #44455, #50779 ) ) ;
#29952=ORIENTED_EDGE ( 'NONE', *, *, #37487, .F. ) ;
#29953=CARTESIAN_POINT ( 'NONE',  ( 45.70938948723410533, -45.91915171081740255, -9.310335717235579622 ) ) ;
#29955=CARTESIAN_POINT ( 'NONE',  ( 16.36412298844330238, 19.86444457474319947, -20.14982337726289785 ) ) ;
#29958=CARTESIAN_POINT ( 'NONE',  ( 46.67460823329760444, -53.58126690376659695, -76.01632185952030341 ) ) ;
#29959=CARTESIAN_POINT ( 'NONE',  ( 66.90311506357139137, 12.17475057385900072, -10.97232589725430074 ) ) ;
#29961=CARTESIAN_POINT ( 'NONE',  ( 50.52803994521560327, -50.37895321258069714, -76.14999999999999147 ) ) ;
#29964=EDGE_CURVE ( 'NONE', #24962, #35625, #44875, .T. ) ;
#29966=CARTESIAN_POINT ( 'NONE',  ( 59.52731112870050367, 14.05929059590050123, -26.49927307267730114 ) ) ;
#29970=CARTESIAN_POINT ( 'NONE',  ( -19.86606260230379917, -15.61618894467933671, -21.14999999999999858 ) ) ;
#29971=CARTESIAN_POINT ( 'NONE',  ( -10.98534442662180055, -42.03317511222970637, -5.475918862938390141 ) ) ;
#29974=CARTESIAN_POINT ( 'NONE',  ( 19.55709641456319403, -55.46944509157171410, -75.54041227948108883 ) ) ;
#29975=DIRECTION ( 'NONE',  ( 0.6676418852213139576, 0.2329255526947012489, -0.7071067811865460184 ) ) ;
#29977=CARTESIAN_POINT ( 'NONE',  ( 42.78269188002550294, 11.47418234317799879, -3.305184689555149991 ) ) ;
#29980=DIRECTION ( 'NONE',  ( 1.000000000000000000, 0.000000000000000000, 0.000000000000000000 ) ) ;
#29982=CARTESIAN_POINT ( 'NONE',  ( -1.120159439602289808, -49.66006368695019546, -9.067476037955330526 ) ) ;
#29988=CARTESIAN_POINT ( 'NONE',  ( 10.81033552764291272, 32.22462020258605264, -23.82639812994671402 ) ) ;
#29989=DIRECTION ( 'NONE',  ( 0.6888026391158250661, 0.7071067811865571207, 0.1598465650148950534 ) ) ;
#29992=DIRECTION ( 'NONE',  ( 0.000000000000000000, 0.000000000000000000, 1.000000000000000000 ) ) ;
#29999=ORIENTED_EDGE ( 'NONE', *, *, #21617, .T. ) ;
#30000=VERTEX_POINT ( 'NONE', #49531 ) ;
#30001=CARTESIAN_POINT ( 'NONE',  ( 61.21388880716399683, -45.26823853505940320, -46.65571761428090269 ) ) ;
#30002=CARTESIAN_POINT ( 'NONE',  ( 52.97643284592769675, -49.63320651957250362, -49.06923426146740042 ) ) ;
#30005=ADVANCED_FACE ( 'NONE', ( #34024 ), #2598, .T. ) ;
#30010=DIRECTION ( 'NONE',  ( 0.000000000000000000, 0.000000000000000000, -1.000000000000000000 ) ) ;
#30011=CYLINDRICAL_SURFACE ( 'NONE', #46897, 3.500000000000003109 ) ;
#30012=ORIENTED_EDGE ( 'NONE', *, *, #4174, .F. ) ;
#30014=CARTESIAN_POINT ( 'NONE',  ( 52.76002515207090937, -50.82837137994670229, -76.29651900278329890 ) ) ;
#30015=CARTESIAN_POINT ( 'NONE',  ( 61.06275439614230294, 14.21153323506290000, -47.36994811082230683 ) ) ;
#30017=PLANE ( 'NONE',  #7990 ) ;
#30018=CARTESIAN_POINT ( 'NONE',  ( 41.59981129736410566, 13.80564489721079902, -5.840260397566160222 ) ) ;
#30019=CARTESIAN_POINT ( 'NONE',  ( 41.15934782240720580, -44.50582977593190037, -4.800414935823390294 ) ) ;
#30023=CIRCLE ( 'NONE', #34210, 3.000000000000000000 ) ;
#30029=ORIENTED_EDGE ( 'NONE', *, *, #31022, .F. ) ;
#30030=CARTESIAN_POINT ( 'NONE',  ( 15.05440318628160057, -53.11618894467930119, -76.14999999999999147 ) ) ;
#30031=CARTESIAN_POINT ( 'NONE',  ( 57.28516360415049746, 19.36107379616109725, -53.60266086058560120 ) ) ;
#30037=CARTESIAN_POINT ( 'NONE',  ( 47.95926718124390220, -54.39950235201539641, -55.26638612347959878 ) ) ;
#30039=CARTESIAN_POINT ( 'NONE',  ( 56.48879402914250392, 19.47930851033790134, -53.39119800914449598 ) ) ;
#30040=CARTESIAN_POINT ( 'NONE',  ( 48.03761785762620207, 23.05233837423439880, -54.73540592323089982 ) ) ;
#30041=ORIENTED_EDGE ( 'NONE', *, *, #41194, .F. ) ;
#30045=CARTESIAN_POINT ( 'NONE',  ( 83.95017420394412966, 13.51629706050414370, -47.46180916972096497 ) ) ;
#30047=CARTESIAN_POINT ( 'NONE',  ( 83.58549413295790487, 13.67911557097859898, -47.23752224019400359 ) ) ;
#30048=CARTESIAN_POINT ( 'NONE',  ( 54.39509416807689490, 16.57266139559970242, -25.91861715551289791 ) ) ;
#30055=ORIENTED_EDGE ( 'NONE', *, *, #10133, .T. ) ;
#30057=CARTESIAN_POINT ( 'NONE',  ( 12.21895752911560074, -64.97095625756598736, -16.28177273609240316 ) ) ;
#30058=CARTESIAN_POINT ( 'NONE',  ( 54.71777383033455777, 14.38501790966102867, -15.43675659586341453 ) ) ;
#30061=CARTESIAN_POINT ( 'NONE',  ( 51.02533507254145206, 3.943601052197206247, -76.41499684325680164 ) ) ;
#30063=ORIENTED_EDGE ( 'NONE', *, *, #23506, .T. ) ;
#30066=ORIENTED_EDGE ( 'NONE', *, *, #27906, .T. ) ;
#30068=CARTESIAN_POINT ( 'NONE',  ( 56.91934464985369857, 14.71809440041320016, -26.24570009089640266 ) ) ;
#30070=AXIS2_PLACEMENT_3D ( 'NONE', #7915, #3986, #48009 ) ;
#30071=CARTESIAN_POINT ( 'NONE',  ( 52.58213039568269664, 18.91034102909139847, -49.81669729888150044 ) ) ;
#30072=CARTESIAN_POINT ( 'NONE',  ( 64.86720007709558899, -0.7199623700256880809, -16.56806548657110412 ) ) ;
#30073=CARTESIAN_POINT ( 'NONE',  ( 51.01628730930330136, -50.56319388302789974, -76.16510841824720046 ) ) ;
#30075=CARTESIAN_POINT ( 'NONE',  ( 58.34741903115999406, -49.12389367403579854, -51.52204152293429473 ) ) ;
#30077=VERTEX_POINT ( 'NONE', #50810 ) ;
#30080=ORIENTED_EDGE ( 'NONE', *, *, #21442, .T. ) ;
#30081=CARTESIAN_POINT ( 'NONE',  ( 56.46551567295650642, -50.77616483221130750, -74.14999999999999147 ) ) ;
#30082=CARTESIAN_POINT ( 'NONE',  ( 51.63377760598070410, -45.11618894467940066, -11.44539556650109979 ) ) ;
#30084=CARTESIAN_POINT ( 'NONE',  ( 14.18741021285519999, -51.10643937792600155, -22.27245518747690056 ) ) ;
#30085=CARTESIAN_POINT ( 'NONE',  ( 56.95199362970870283, 19.39688504427079963, -74.60677458063500467 ) ) ;
#30086=CARTESIAN_POINT ( 'NONE',  ( 47.46019987341419721, -54.30427659254309702, -75.17791912558919876 ) ) ;
#30088=CARTESIAN_POINT ( 'NONE',  ( 55.68942512253350685, 14.36557237263189890, -16.32472732305740237 ) ) ;
#30090=CARTESIAN_POINT ( 'NONE',  ( 57.34839258938159645, -50.23817553046570339, -52.73846305559919756 ) ) ;
#30094=CARTESIAN_POINT ( 'NONE',  ( 46.37667707902559755, 21.71256252826200139, -76.14999999999999147 ) ) ;
#30098=CARTESIAN_POINT ( 'NONE',  ( 75.27858690284780607, -35.61663803900331970, -12.42467591162693807 ) ) ;
#30099=CARTESIAN_POINT ( 'NONE',  ( 12.76222187884635240, -65.48774652861183654, -23.42344531452376799 ) ) ;
#30101=CARTESIAN_POINT ( 'NONE',  ( 41.29354830052630376, -44.77576227574429879, -5.375173069188550201 ) ) ;
#30106=CARTESIAN_POINT ( 'NONE',  ( 82.26799199803031115, 13.91172255425060023, -46.71841361690350425 ) ) ;
#30108=DIRECTION ( 'NONE',  ( 0.2260571801428161443, -2.775557561562891351E-17, -0.9741140340359945027 ) ) ;
#30112=CARTESIAN_POINT ( 'NONE',  ( -12.01951210174030038, 24.16090772189719971, -51.29522465964500100 ) ) ;
#30114=CARTESIAN_POINT ( 'NONE',  ( 52.72967167102660113, -49.72828118800889996, -48.70010208928940187 ) ) ;
#30115=VERTEX_POINT ( 'NONE', #31634 ) ;
#30117=CARTESIAN_POINT ( 'NONE',  ( 53.65234805279081343, -51.32547278899044585, -75.57542635131952125 ) ) ;
#30118=CARTESIAN_POINT ( 'NONE',  ( 13.86586360781780058, 20.00433391931990101, -22.87017487063610233 ) ) ;
#30119=CARTESIAN_POINT ( 'NONE',  ( 56.52818367932749766, 14.13713193161779991, -25.29323032974989971 ) ) ;
#30121=CARTESIAN_POINT ( 'NONE',  ( 50.90852063231859859, 19.66920620538740039, -76.14999999999999147 ) ) ;
#30122=CARTESIAN_POINT ( 'NONE',  ( 53.35900413950319887, 18.24539451609189911, -49.18808545514919217 ) ) ;
#30124=CARTESIAN_POINT ( 'NONE',  ( 16.65420337942459739, 19.88381105532299742, -15.67544741556190324 ) ) ;
#30126=EDGE_LOOP ( 'NONE', ( #40643, #49055, #5010, #37823 ) ) ;
#30129=CARTESIAN_POINT ( 'NONE',  ( 11.19961559249191652, 34.01497085325235759, -22.25048313876769868 ) ) ;
#30131=CARTESIAN_POINT ( 'NONE',  ( 11.75081654933170050, -65.42392464281880393, -18.04875625368890013 ) ) ;
#30135=LINE ( 'NONE', #46158, #30183 ) ;
#30138=CARTESIAN_POINT ( 'NONE',  ( 9.737942574377051130, -63.22272823571240252, -46.29781469063039623 ) ) ;
#30139=EDGE_CURVE ( 'NONE', #45765, #22075, #23510, .T. ) ;
#30141=VERTEX_POINT ( 'NONE', #47653 ) ;
#30143=DIRECTION ( 'NONE',  ( 0.000000000000000000, 0.000000000000000000, -1.000000000000000000 ) ) ;
#30146=CARTESIAN_POINT ( 'NONE',  ( 52.53691732766219502, 18.94171105001880306, -76.99573695378890648 ) ) ;
#30147=VECTOR ( 'NONE', #44525, 1000.000000000000000 ) ;
#30148=ORIENTED_EDGE ( 'NONE', *, *, #3623, .F. ) ;
#30154=AXIS2_PLACEMENT_3D ( 'NONE', #22859, #46233, #10582 ) ;
#30155=B_SPLINE_SURFACE_WITH_KNOTS ( 'NONE', 3, 3, ( 
 ( #32870, #37877, #17436, #29475, #2487, #46005, #33140, #30248, #49165 ),
 ( #45480, #5653, #9579, #13259, #21600, #29213, #17947, #33915, #45220 ),
 ( #9328, #14023, #49678, #10094, #41280, #37601, #42063, #13769, #45740 ),
 ( #26053, #22123, #18206, #5390, #21345, #15580, #46531, #22645, #31024 ),
 ( #42589, #23154, #42851, #11135, #47048, #18467, #50701, #14539, #34440 ),
 ( #51481, #50958, #19241, #47553, #14799, #47306, #18980, #3529, #27104 ),
 ( #10878, #15320, #15057, #7722, #23409, #19500, #31274, #43108, #51227 ),
 ( #7200, #11395, #23667, #50450, #2750, #27357, #39429, #43364, #7456 ),
 ( #38662, #39171, #35490, #31535, #34700, #30508, #11649, #27614, #3265 ),
 ( #18722, #43620, #39683, #10620, #26574, #6685, #30765, #46787, #6948 ),
 ( #26841, #22900, #38917, #35223, #3008, #34959, #40447, #36762, #24432 ),
 ( #44126, #36504, #8744, #873, #40708, #358, #48318, #23917, #11913 ),
 ( #8224, #12944, #19998, #44384, #24692, #35748, #9007, #4806, #27869 ),
 ( #16867, #20773, #12164, #112, #28900, #24950, #43870, #20257, #32042 ),
 ( #32814, #20511, #4538, #607, #44901, #7968, #12413, #48840, #3787 ),
 ( #44637, #19757, #48065, #51731, #39942, #24171, #4038, #16340, #16593 ) ),
 .UNSPECIFIED., .F., .F., .F.,
 ( 4, 2, 2, 2, 2, 2, 2, 4 ),
 ( 4, 1, 1, 1, 1, 1, 4 ),
 ( -3.203522274700000420E-05, 0.2957445120129499894, 0.5890486225480859872, 0.7853981633974479459, 0.8835729338221289808, 1.040652566501619969, 1.291979978788799999, 1.570796326794899889 ),
 ( -3.203522273900000163E-05, 0.1666666666666670182, 0.3333333333333329818, 0.5000000000000000000, 0.6666666666666670737, 0.8333333333333330373, 1.000032035222750082 ),
 .UNSPECIFIED. ) ;
#30166=ADVANCED_FACE ( 'NONE', ( #36606 ), #24392, .T. ) ;
#30167=CARTESIAN_POINT ( 'NONE',  ( 13.42257523142330200, 20.48963776793129909, -74.14994161014911356 ) ) ;
#30170=CARTESIAN_POINT ( 'NONE',  ( 42.05084668997409381, -45.26056779962699750, -6.331743932908059591 ) ) ;
#30174=CARTESIAN_POINT ( 'NONE',  ( 53.05686867825300368, -49.33660682032460443, -27.09038418901580059 ) ) ;
#30175=CARTESIAN_POINT ( 'NONE',  ( 55.22131878237419755, -50.98712927677730278, -75.19523011523990874 ) ) ;
#30176=CARTESIAN_POINT ( 'NONE',  ( 75.47966807050509885, 12.14072485751589880, -13.40512917118210012 ) ) ;
#30178=CARTESIAN_POINT ( 'NONE',  ( 14.34417029198869820, -49.11618894467930829, -22.49240188329099865 ) ) ;
#30179=CYLINDRICAL_SURFACE ( 'NONE', #39001, 1.999999999999997335 ) ;
#30180=PRODUCT_DEFINITION_FORMATION_WITH_SPECIFIED_SOURCE ( 'ANY', '', #23918, .NOT_KNOWN. ) ;
#30181=ORIENTED_EDGE ( 'NONE', *, *, #41812, .F. ) ;
#30182=CARTESIAN_POINT ( 'NONE',  ( -6.918095167487591013, -45.82906477882070106, -4.824152819064210895 ) ) ;
#30183=VECTOR ( 'NONE', #5793, 1000.000000000000000 ) ;
#30184=CARTESIAN_POINT ( 'NONE',  ( 47.50894761223599261, 23.34495395406939977, -54.68833697881660072 ) ) ;
#30185=DIRECTION ( 'NONE',  ( 0.000000000000000000, -1.000000000000000000, 0.000000000000000000 ) ) ;
#30187=CARTESIAN_POINT ( 'NONE',  ( 13.20467960049900036, 19.37200555191600060, -21.36610105499189771 ) ) ;
#30188=CARTESIAN_POINT ( 'NONE',  ( 57.50723798014340105, 13.88381064843590096, -25.33268340738889890 ) ) ;
#30190=CARTESIAN_POINT ( 'NONE',  ( 12.01906023897140052, 33.99185434501800529, -16.79721265541349950 ) ) ;
#30192=FACE_OUTER_BOUND ( 'NONE', #28027, .T. ) ;
#30193=DIRECTION ( 'NONE',  ( 1.000000000000000000, 0.000000000000000000, 0.000000000000000000 ) ) ;
#30194=CARTESIAN_POINT ( 'NONE',  ( 63.88393739769619373, 4.883811055320659733, -61.44999999999999574 ) ) ;
#30195=CARTESIAN_POINT ( 'NONE',  ( 56.32938366548789588, 14.88341733999840066, -26.17484211198950206 ) ) ;
#30196=CARTESIAN_POINT ( 'NONE',  ( 53.40578033982649941, 20.84711752906830284, -54.18098735754220030 ) ) ;
#30201=CARTESIAN_POINT ( 'NONE',  ( 11.10570036673579963, 32.20550737558679799, -44.25861501678190280 ) ) ;
#30204=CARTESIAN_POINT ( 'NONE',  ( 17.92366930135129977, 19.88381105676229765, -74.14994299942661371 ) ) ;
#30205=ORIENTED_EDGE ( 'NONE', *, *, #20197, .F. ) ;
#30207=CARTESIAN_POINT ( 'NONE',  ( 48.59288953467110161, 22.89722549970059617, -55.31247818475549849 ) ) ;
#30208=EDGE_CURVE ( 'NONE', #8932, #37620, #37142, .T. ) ;
#30209=CARTESIAN_POINT ( 'NONE',  ( 76.49393950927560581, -3.279981714206201993, -13.20130267904146848 ) ) ;
#30210=VERTEX_POINT ( 'NONE', #4390 ) ;
#30211=CARTESIAN_POINT ( 'NONE',  ( 11.13305467742809896, -63.61067243011080308, -43.97199255920600081 ) ) ;
#30212=CARTESIAN_POINT ( 'NONE',  ( 56.50520158204290055, -45.38268761669329621, -25.36340749954939966 ) ) ;
#30216=CYLINDRICAL_SURFACE ( 'NONE', #50259, 2.000000000000000444 ) ;
#30219=CARTESIAN_POINT ( 'NONE',  ( 52.29741850497030242, -46.00137683757239415, -13.99733621933699901 ) ) ;
#30220=CARTESIAN_POINT ( 'NONE',  ( 51.99322682244601168, 1.709311056957359520, -19.32981441259133604 ) ) ;
#30221=CARTESIAN_POINT ( 'NONE',  ( 14.83504272151670023, 19.88381105148139838, -22.28508381815080241 ) ) ;
#30224=AXIS2_PLACEMENT_3D ( 'NONE', #40317, #19625, #43234 ) ;
#30226=CARTESIAN_POINT ( 'NONE',  ( 47.09676272639379846, -54.20071801015340185, -75.51614565244940991 ) ) ;
#30227=AXIS2_PLACEMENT_3D ( 'NONE', #39700, #12428, #48332 ) ;
#30228=CARTESIAN_POINT ( 'NONE',  ( 57.97374689176790241, 13.73536417335439985, -9.618885821366971456 ) ) ;
#30229=VECTOR ( 'NONE', #36987, 1000.000000000000114 ) ;
#30230=ADVANCED_FACE ( 'NONE', ( #9107 ), #1823, .F. ) ;
#30232=CARTESIAN_POINT ( 'NONE',  ( 52.82838949928990502, 19.98853424248689947, -75.91622035586969730 ) ) ;
#30233=CARTESIAN_POINT ( 'NONE',  ( 61.36905519990600055, 13.93820976684110136, -27.72184371702499917 ) ) ;
#30235=ORIENTED_EDGE ( 'NONE', *, *, #44062, .F. ) ;
#30237=CARTESIAN_POINT ( 'NONE',  ( 6.289752778132990052, -60.00340137394460527, -12.93848582979680018 ) ) ;
#30238=FACE_OUTER_BOUND ( 'NONE', #51870, .T. ) ;
#30240=CARTESIAN_POINT ( 'NONE',  ( 19.53299567489768407, -55.47150705052180086, -75.56421958049284626 ) ) ;
#30243=LINE ( 'NONE', #18715, #13126 ) ;
#30244=CARTESIAN_POINT ( 'NONE',  ( 40.60804131356049851, 13.51331262618320039, -4.641941792357469510 ) ) ;
#30248=CARTESIAN_POINT ( 'NONE',  ( 17.99229598226500215, -51.11618622139260282, -74.14993436883820266 ) ) ;
#30250=ORIENTED_EDGE ( 'NONE', *, *, #45125, .T. ) ;
#30251=VECTOR ( 'NONE', #22707, 1000.000000000000000 ) ;
#30255=CARTESIAN_POINT ( 'NONE',  ( -9.494463584530519640, 12.56566348097149977, -6.502759410847990473 ) ) ;
#30259=CARTESIAN_POINT ( 'NONE',  ( 47.80851828325950237, -54.40380972823489714, -54.72998258637920799 ) ) ;
#30261=CIRCLE ( 'NONE', #21879, 2.000000000000000888 ) ;
#30262=DIRECTION ( 'NONE',  ( 0.000000000000000000, 1.000000000000000000, 0.000000000000000000 ) ) ;
#30263=CYLINDRICAL_SURFACE ( 'NONE', #49597, 3.000000000000000444 ) ;
#30266=EDGE_CURVE ( 'NONE', #5215, #42606, #1705, .T. ) ;
#30267=ORIENTED_EDGE ( 'NONE', *, *, #17254, .F. ) ;
#30273=ORIENTED_EDGE ( 'NONE', *, *, #14293, .F. ) ;
#30279=CARTESIAN_POINT ( 'NONE',  ( 53.20630144999590527, -50.74234614952320044, -76.43613505561189925 ) ) ;
#30280=CARTESIAN_POINT ( 'NONE',  ( 60.94474915215740651, 14.18121638299069964, -47.07753893340860429 ) ) ;
#30283=DIRECTION ( 'NONE',  ( 0.9741140340359945027, 0.000000000000000000, 0.2260571801428156169 ) ) ;
#30284=CARTESIAN_POINT ( 'NONE',  ( 42.75215489670460300, 13.74995302045830137, -6.093637046069630081 ) ) ;
#30286=CARTESIAN_POINT ( 'NONE',  ( 40.60988568039630309, -44.69613999932960269, -4.337423926737489666 ) ) ;
#30287=CARTESIAN_POINT ( 'NONE',  ( -13.56626582457120023, -15.61618894467929941, 7.944363289481099599 ) ) ;
#30288=CARTESIAN_POINT ( 'NONE',  ( -9.414006712227710238, 12.57454005906549988, -5.942694572982400558 ) ) ;
#30290=AXIS2_PLACEMENT_3D ( 'NONE', #2500, #6438, #13784 ) ;
#30294=ORIENTED_EDGE ( 'NONE', *, *, #48025, .F. ) ;
#30295=CARTESIAN_POINT ( 'NONE',  ( 14.38860766206780184, -52.17875626651990473, -75.87012052777591009 ) ) ;
#30296=CARTESIAN_POINT ( 'NONE',  ( 57.26876238482499559, 19.38381105532069881, -53.91656696360529821 ) ) ;
#30298=CARTESIAN_POINT ( 'NONE',  ( 11.13393739769250068, 32.42518242043740884, -43.78800781015315380 ) ) ;
#30300=EDGE_CURVE ( 'NONE', #17232, #10891, #22424, .T. ) ;
#30302=CARTESIAN_POINT ( 'NONE',  ( 47.97259836220649731, -54.39289801412169822, -55.19635314194069764 ) ) ;
#30304=CARTESIAN_POINT ( 'NONE',  ( 82.13853704237929776, -45.11618894467940066, -46.37203261889099792 ) ) ;
#30306=CARTESIAN_POINT ( 'NONE',  ( 47.78181927210629709, 23.24271050597710087, -55.19076979248089998 ) ) ;
#30309=ORIENTED_EDGE ( 'NONE', *, *, #46802, .F. ) ;
#30314=CARTESIAN_POINT ( 'NONE',  ( 83.86237639949339950, 13.50615999911470055, -47.35515635286719771 ) ) ;
#30315=CARTESIAN_POINT ( 'NONE',  ( 53.48305084018470268, 17.62635399826340077, -26.58258335482339874 ) ) ;
#30319=ORIENTED_EDGE ( 'NONE', *, *, #43530, .F. ) ;
#30320=CARTESIAN_POINT ( 'NONE',  ( 57.55751162087899786, 19.38381105532069881, -53.92796738110899923 ) ) ;
#30323=CARTESIAN_POINT ( 'NONE',  ( 12.30638105235980007, -64.63429039334658910, -15.85198194118579984 ) ) ;
#30325=CARTESIAN_POINT ( 'NONE',  ( 6.293131413230796056, 33.86298889378740995, -49.18705164837358268 ) ) ;
#30328=ORIENTED_EDGE ( 'NONE', *, *, #27890, .T. ) ;
#30329=ORIENTED_EDGE ( 'NONE', *, *, #32834, .T. ) ;
#30332=DIRECTION ( 'NONE',  ( 0.000000000000000000, 1.000000000000000000, 0.000000000000000000 ) ) ;
#30333=CARTESIAN_POINT ( 'NONE',  ( 53.22811123321509541, -49.51495811786340084, -49.13101390776430577 ) ) ;
#30334=CARTESIAN_POINT ( 'NONE',  ( 53.11054108117379258, 18.20428406185990156, -48.75085142486800294 ) ) ;
#30335=CARTESIAN_POINT ( 'NONE',  ( 60.30051528721210019, -2.182703807405690366, -15.82000114403490265 ) ) ;
#30336=CARTESIAN_POINT ( 'NONE',  ( 50.91412666581710056, -49.20888781110259202, -76.31682797935179963 ) ) ;
#30337=CARTESIAN_POINT ( 'NONE',  ( 58.51614409837979736, -48.15979427076100450, -50.25351394005609507 ) ) ;
#30340=CARTESIAN_POINT ( 'NONE',  ( 70.83745409581372598, 17.98087126524719892, -68.79648330188406646 ) ) ;
#30343=CARTESIAN_POINT ( 'NONE',  ( 51.23833939979579100, -45.11618894467940066, -11.16259862828139937 ) ) ;
#30345=CARTESIAN_POINT ( 'NONE',  ( 13.34067758125200065, -51.12402484803250502, -21.90730111293149918 ) ) ;
#30346=CARTESIAN_POINT ( 'NONE',  ( 55.18354902960369657, 19.47151978655200111, -75.88390424252150979 ) ) ;
#30347=CARTESIAN_POINT ( 'NONE',  ( 47.61801185652239354, -54.54486410850540068, -74.14999999999999147 ) ) ;
#30348=CARTESIAN_POINT ( 'NONE',  ( 56.70491206796489791, 13.95151597528120035, -16.59608766374520172 ) ) ;
#30353=CARTESIAN_POINT ( 'NONE',  ( 47.30391968620829601, 22.90394248747499617, -75.47331621149830028 ) ) ;
#30354=CARTESIAN_POINT ( 'NONE',  ( 19.91788182092076553, -54.79639948975857067, -18.20736960311763397 ) ) ;
#30355=CARTESIAN_POINT ( 'NONE',  ( 75.20727607192908692, -32.15526784732785615, -12.07513152916334498 ) ) ;
#30362=CARTESIAN_POINT ( 'NONE',  ( 82.13853704237929776, 14.04924524887199944, -47.17417977903829751 ) ) ;
#30368=CARTESIAN_POINT ( 'NONE',  ( -17.48391069661260033, 19.73109819378510110, -52.50953498851649925 ) ) ;
#30369=EDGE_CURVE ( 'NONE', #10642, #23531, #38534, .T. ) ;
#30370=EDGE_LOOP ( 'NONE', ( #42311, #51386, #39191, #50452 ) ) ;
#30371=CARTESIAN_POINT ( 'NONE',  ( 52.68399239296920200, -49.75584776967829725, -48.59017835746970349 ) ) ;
#30372=ORIENTED_EDGE ( 'NONE', *, *, #15158, .F. ) ;
#30373=CARTESIAN_POINT ( 'NONE',  ( 17.34362241395794868, 21.51730928977416468, -76.12465453342632316 ) ) ;
#30375=CARTESIAN_POINT ( 'NONE',  ( 14.04181524467029973, 19.90302481765870013, -22.40049071566960137 ) ) ;
#30376=CARTESIAN_POINT ( 'NONE',  ( 55.88898274229019592, 14.70399348244479931, -25.39814755123949652 ) ) ;
#30378=CARTESIAN_POINT ( 'NONE',  ( 50.67689124139590007, 19.37866773268710219, -76.14999999999999147 ) ) ;
#30379=CARTESIAN_POINT ( 'NONE',  ( 52.66298057413799683, 18.54726979422290256, -48.68531361618759945 ) ) ;
#30380=CARTESIAN_POINT ( 'NONE',  ( 55.72979527423980528, -45.76347876835659889, -16.72772322675590218 ) ) ;
#30382=CIRCLE ( 'NONE', #7811, 1.999999999999998224 ) ;
#30383=ORIENTED_EDGE ( 'NONE', *, *, #13130, .F. ) ;
#30387=CARTESIAN_POINT ( 'NONE',  ( 9.367149215637390114, 32.06395859284570804, -46.50590274904199362 ) ) ;
#30390=CARTESIAN_POINT ( 'NONE',  ( 10.80633501404929930, -64.99634644860429944, -17.92671787896209779 ) ) ;
#30391=DIRECTION ( 'NONE',  ( -7.539420000000001133E-18, 1.452687000000000165E-17, 1.000000000000000000 ) ) ;
#30399=CARTESIAN_POINT ( 'NONE',  ( 9.738771746928540196, -63.23098275344089814, -46.29766285214619614 ) ) ;
#30400=AXIS2_PLACEMENT_3D ( 'NONE', #10945, #42916, #7014 ) ;
#30403=CARTESIAN_POINT ( 'NONE',  ( 57.32592487606110154, 19.18190549473660056, -53.00067887316149751 ) ) ;
#30404=CARTESIAN_POINT ( 'NONE',  ( 53.99792397698860213, 19.38381073495739670, -77.02993432047880162 ) ) ;
#30407=CYLINDRICAL_SURFACE ( 'NONE', #3198, 21.19999999999999929 ) ;
#30408=LINE ( 'NONE', #18623, #22550 ) ;
#30409=CARTESIAN_POINT ( 'NONE',  ( -23.86606260230380272, -15.61618894467908092, -76.14999999999999147 ) ) ;
#30417=CARTESIAN_POINT ( 'NONE',  ( 53.05489980299899599, -49.59988638911210046, -49.10811587859359406 ) ) ;
#30420=CARTESIAN_POINT ( 'NONE',  ( 63.88393739769619373, 11.88381105532070059, -61.34712802272770915 ) ) ;
#30421=CARTESIAN_POINT ( 'NONE',  ( 13.58922753005830053, 20.47004600267149854, -74.90176971618339508 ) ) ;
#30422=CARTESIAN_POINT ( 'NONE',  ( 16.13393739769620083, -15.61618894467929941, -6.649999999999999467 ) ) ;
#30423=CARTESIAN_POINT ( 'NONE',  ( 44.42514528531739870, -45.25992823897050243, -7.504186993430459474 ) ) ;
#30426=ORIENTED_EDGE ( 'NONE', *, *, #41417, .T. ) ;
#30427=CARTESIAN_POINT ( 'NONE',  ( 52.89134886112609735, -49.51162219831950040, -27.21802740595560266 ) ) ;
#30429=CARTESIAN_POINT ( 'NONE',  ( 54.46275104342129936, -51.12164165988440345, -75.43974601459740370 ) ) ;
#30430=CARTESIAN_POINT ( 'NONE',  ( 9.118782003106261413, 30.73934052534850281, -13.66830718943320022 ) ) ;
#30433=CARTESIAN_POINT ( 'NONE',  ( -23.86606260230380272, -15.61618894467908092, -53.92777777777782688 ) ) ;
#30438=CARTESIAN_POINT ( 'NONE',  ( 13.96111746457373215, 21.00530369382216023, -75.65677362358476898 ) ) ;
#30439=CARTESIAN_POINT ( 'NONE',  ( 47.53131359496729402, 23.34191863293520086, -54.78660750946839642 ) ) ;
#30441=CARTESIAN_POINT ( 'NONE',  ( 84.32823744787019393, -43.96174957359315982, -47.43651528332460288 ) ) ;
#30442=CARTESIAN_POINT ( 'NONE',  ( 13.33369300875940056, 19.36669572017150287, -21.35583564802480083 ) ) ;
#30444=CARTESIAN_POINT ( 'NONE',  ( 11.59391792477759964, 33.72622688432610261, -16.50763286606089864 ) ) ;
#30445=CARTESIAN_POINT ( 'NONE',  ( 51.73429015981039925, 17.92666341930739904, -76.96796945729541051 ) ) ;
#30446=CARTESIAN_POINT ( 'NONE',  ( 52.96856317127399905, 18.35625398511779949, -48.80184351055599734 ) ) ;
#30448=CARTESIAN_POINT ( 'NONE',  ( 55.65109705446129595, -48.32796235437900378, -48.64566203011980150 ) ) ;
#30449=CARTESIAN_POINT ( 'NONE',  ( 52.83394450884049576, 18.38007605328469651, -27.67493365076309786 ) ) ;
#30450=CARTESIAN_POINT ( 'NONE',  ( 51.27175184527400376, 21.75613229864340070, -54.61634031474230255 ) ) ;
#30452=CARTESIAN_POINT ( 'NONE',  ( 52.56949877374420055, 18.62486692341260053, -48.49331013451849515 ) ) ;
#30455=CARTESIAN_POINT ( 'NONE',  ( 10.76935003792520007, 31.89982618482420307, -45.20657243697100114 ) ) ;
#30459=EDGE_CURVE ( 'NONE', #4756, #14500, #51097, .T. ) ;
#30460=CARTESIAN_POINT ( 'NONE',  ( 12.13393739769644419, 24.18330853958552851, -74.40622738399734715 ) ) ;
#30461=ORIENTED_EDGE ( 'NONE', *, *, #48697, .F. ) ;
#30462=VERTEX_POINT ( 'NONE', #33448 ) ;
#30465=CARTESIAN_POINT ( 'NONE',  ( 76.55776859562905656, 0.1525228172217792388, -13.47635171202204241 ) ) ;
#30466=ORIENTED_EDGE ( 'NONE', *, *, #19457, .F. ) ;
#30467=CARTESIAN_POINT ( 'NONE',  ( 12.31664178984540037, -65.34953336804649382, -46.39762368350670130 ) ) ;
#30468=CARTESIAN_POINT ( 'NONE',  ( 57.59886637785189833, -45.11801559808479567, -25.34084472867580118 ) ) ;
#30474=CARTESIAN_POINT ( 'NONE',  ( 12.43092062477990112, 34.07680541178370248, -23.93571342080350206 ) ) ;
#30476=CARTESIAN_POINT ( 'NONE',  ( 54.46259150374739733, -45.11618894467940066, -13.50670530417659876 ) ) ;
#30479=CARTESIAN_POINT ( 'NONE',  ( 16.08018489229900183, 19.80150390720080011, -20.24577016824859754 ) ) ;
#30481=CARTESIAN_POINT ( 'NONE',  ( 65.47973875042168856, -29.76586224471849818, -16.55654698053239926 ) ) ;
#30483=CARTESIAN_POINT ( 'NONE',  ( 47.04916798186049931, -54.23042865507689925, -75.51723258725520793 ) ) ;
#30484=CARTESIAN_POINT ( 'NONE',  ( 64.81411238528559693, 13.09683274588459945, -10.69644402401159944 ) ) ;
#30485=B_SPLINE_CURVE_WITH_KNOTS ( 'NONE', 3,
 ( #48175, #11514, #44237, #27980, #19360, #31394, #47668, #16201, #8602, #48434 ),
 .UNSPECIFIED., .F., .F.,
 ( 4, 2, 2, 2, 4 ),
 ( 0.5000003605116074556, 0.5624999999994833022, 0.6624999999996041833, 0.8224999999997919531, 1.000000000000000000 ),
 .UNSPECIFIED. ) ;
#30486=CARTESIAN_POINT ( 'NONE',  ( 55.53286968820209779, 19.65994446513209937, -52.96077464608250551 ) ) ;
#30487=CARTESIAN_POINT ( 'NONE',  ( 52.09209162650440561, 20.06877058433559924, -75.99731153404469808 ) ) ;
#30488=CARTESIAN_POINT ( 'NONE',  ( 58.01877172845900077, 13.88381123105269843, -25.42745524943100222 ) ) ;
#30490=ORIENTED_EDGE ( 'NONE', *, *, #32751, .T. ) ;
#30492=TOROIDAL_SURFACE ( 'NONE', #2042, 36.00000000000000000, 2.000000000000000000 ) ;
#30494=CARTESIAN_POINT ( 'NONE',  ( 1.958201230952900218, -55.72338255999500234, -10.46106927051559943 ) ) ;
#30495=CARTESIAN_POINT ( 'NONE',  ( 75.92152012689510343, 4.541771151542360663, -12.68757564883900102 ) ) ;
#30496=CARTESIAN_POINT ( 'NONE',  ( 82.81464131963001307, -43.11618894467930119, -49.28546657628889704 ) ) ;
#30498=CARTESIAN_POINT ( 'NONE',  ( 66.63393739769620083, -43.11618894467930119, -73.25000000000000000 ) ) ;
#30501=CARTESIAN_POINT ( 'NONE',  ( 13.77293537813399915, 20.06110665059810216, -23.09858807645749934 ) ) ;
#30502=CARTESIAN_POINT ( 'NONE',  ( 42.00588769599519878, 12.47412117931249931, -4.238533581052370103 ) ) ;
#30504=CARTESIAN_POINT ( 'NONE',  ( 50.95940558857264335, 4.060833044306336070, -76.37898308257572921 ) ) ;
#30505=CARTESIAN_POINT ( 'NONE',  ( 70.03247032090770574, -49.95860450173900347, -75.14853292321149070 ) ) ;
#30506=AXIS2_PLACEMENT_3D ( 'NONE', #46053, #26101, #42106 ) ;
#30507=CARTESIAN_POINT ( 'NONE',  ( 76.59130978626896535, -43.22129931671369008, -14.19826186240517174 ) ) ;
#30508=CARTESIAN_POINT ( 'NONE',  ( 17.91044080450719989, -51.90926368007729508, -75.71157996061791096 ) ) ;
#30510=ORIENTED_EDGE ( 'NONE', *, *, #46802, .T. ) ;
#30514=ORIENTED_EDGE ( 'NONE', *, *, #45844, .F. ) ;
#30515=CARTESIAN_POINT ( 'NONE',  ( 73.38393739769610136, 11.88381105532070059, -84.94863984844540994 ) ) ;
#30520=CARTESIAN_POINT ( 'NONE',  ( 44.34202791315729542, -46.09297532313080126, -8.529314961685768637 ) ) ;
#30522=ORIENTED_EDGE ( 'NONE', *, *, #37598, .T. ) ;
#30524=ORIENTED_EDGE ( 'NONE', *, *, #31369, .F. ) ;
#30526=CARTESIAN_POINT ( 'NONE',  ( 61.38641268662350114, -45.22597443312260168, -46.91882270677900379 ) ) ;
#30527=CARTESIAN_POINT ( 'NONE',  ( 82.51389170711580334, -45.11867408937381896, -46.70334177319745805 ) ) ;
#30529=ORIENTED_EDGE ( 'NONE', *, *, #13276, .T. ) ;
#30530=CARTESIAN_POINT ( 'NONE',  ( 10.61752692138360032, -64.82564047392860118, -18.17418372802830007 ) ) ;
#30534=LINE ( 'NONE', #21894, #45920 ) ;
#30535=CARTESIAN_POINT ( 'NONE',  ( 53.62559109365889753, -51.33070570257169862, -75.58097986874130925 ) ) ;
#30536=CARTESIAN_POINT ( 'NONE',  ( 60.91286535189659901, 14.21542966090570204, -47.20799383203969768 ) ) ;
#30539=CARTESIAN_POINT ( 'NONE',  ( 42.00047115104329976, -43.88691491351350038, -4.514521081582199891 ) ) ;
#30541=CARTESIAN_POINT ( 'NONE',  ( 56.12094024660369485, 14.43398220991280034, -25.30520633357740223 ) ) ;
#30544=DIRECTION ( 'NONE',  ( 0.000000000000000000, 0.000000000000000000, -1.000000000000000000 ) ) ;
#30545=LINE ( 'NONE', #18763, #36802 ) ;
#30547=ORIENTED_EDGE ( 'NONE', *, *, #49978, .T. ) ;
#30548=CARTESIAN_POINT ( 'NONE',  ( 14.60528279563649967, -52.33797002293529488, -75.98739629952659413 ) ) ;
#30550=CARTESIAN_POINT ( 'NONE',  ( 57.41104239909219586, 19.22742992429120079, -53.14439825748630142 ) ) ;
#30556=CARTESIAN_POINT ( 'NONE',  ( 83.89200044194980421, 17.38381105532069881, -53.92796738110899923 ) ) ;
#30557=AXIS2_PLACEMENT_3D ( 'NONE', #5401, #29736, #21358 ) ;
#30558=EDGE_CURVE ( 'NONE', #31153, #31690, #35571, .T. ) ;
#30562=CARTESIAN_POINT ( 'NONE',  ( 56.43758032280099712, 19.38627829750620180, -53.06658686592589902 ) ) ;
#30564=CARTESIAN_POINT ( 'NONE',  ( 48.18646040924789986, 23.06412321552320321, -55.14499207586399621 ) ) ;
#30569=CARTESIAN_POINT ( 'NONE',  ( 14.34417029198879945, -51.11618894467930119, -22.49240188329099865 ) ) ;
#30578=VERTEX_POINT ( 'NONE', #46569 ) ;
#30579=CYLINDRICAL_SURFACE ( 'NONE', #50692, 1.999999999999997780 ) ;
#30581=VERTEX_POINT ( 'NONE', #15358 ) ;
#30584=CARTESIAN_POINT ( 'NONE',  ( 11.97330428934050062, -64.78167623425329680, -16.08313759591939984 ) ) ;
#30585=CARTESIAN_POINT ( 'NONE',  ( 7.635415421591210894, -60.86027260432054931, -20.56421356237310150 ) ) ;
#30587=CARTESIAN_POINT ( 'NONE',  ( 11.78948683875339931, -65.25723971847149585, -47.10950715352170448 ) ) ;
#30592=CARTESIAN_POINT ( 'NONE',  ( 52.42687975140989209, 18.94760833839670155, -49.65940143135599527 ) ) ;
#30593=CARTESIAN_POINT ( 'NONE',  ( 59.34569085193420079, -3.119383829553379783, -15.68025057170479819 ) ) ;
#30594=CARTESIAN_POINT ( 'NONE',  ( 51.24891283041849732, -50.38292309881020969, -76.23258493454248708 ) ) ;
#30595=CARTESIAN_POINT ( 'NONE',  ( 60.21881437948049864, -46.03921328867149754, -47.91605915182169895 ) ) ;
#30600=DIRECTION ( 'NONE',  ( 1.000000000000000000, 0.000000000000000000, 0.000000000000000000 ) ) ;
#30601=CARTESIAN_POINT ( 'NONE',  ( 56.37863599685000082, -47.94388181700620066, -48.46423989679689726 ) ) ;
#30605=AXIS2_PLACEMENT_3D ( 'NONE', #33779, #6021, #14394 ) ;
#30606=CARTESIAN_POINT ( 'NONE',  ( 13.48893846581560041, -50.82346698513120486, -21.59024777398839845 ) ) ;
#30607=CARTESIAN_POINT ( 'NONE',  ( 47.40090504849130326, -54.33275752599000441, -75.17436503908771783 ) ) ;
#30608=CARTESIAN_POINT ( 'NONE',  ( 56.08896608865399713, 14.05775919982069944, -16.05802721449649795 ) ) ;
#30609=CARTESIAN_POINT ( 'NONE',  ( 9.746758075853771075, 32.08108121953329572, -46.29788637164419640 ) ) ;
#30614=CARTESIAN_POINT ( 'NONE',  ( 47.58828887377080719, 23.23481553981489967, -74.72737448322331488 ) ) ;
#30616=CARTESIAN_POINT ( 'NONE',  ( 42.86742020280579624, -45.95034697033790394, -7.481776181590609198 ) ) ;
#30618=CARTESIAN_POINT ( 'NONE',  ( 15.00527039807065144, -50.63538892808460901, -20.65452793192670100 ) ) ;
#30621=CARTESIAN_POINT ( 'NONE',  ( 46.42817262113109678, -53.00400577820990122, -76.14999999999999147 ) ) ;
#30623=CARTESIAN_POINT ( 'NONE',  ( 82.75411604745001171, 14.36250171077709936, -47.67220798777069746 ) ) ;
#30625=CARTESIAN_POINT ( 'NONE',  ( 47.63737926530004785, 23.29734256229923872, -74.36261479904801774 ) ) ;
#30626=CARTESIAN_POINT ( 'NONE',  ( 68.13393739769620083, 6.883811055320649963, -71.50000000000000000 ) ) ;
#30628=CARTESIAN_POINT ( 'NONE',  ( -12.74467463197259853, 25.82472242301949805, -53.24963421316469692 ) ) ;
#30630=CARTESIAN_POINT ( 'NONE',  ( 52.99414832248270812, -49.58664987881770259, -48.92816831207029793 ) ) ;
#30635=CARTESIAN_POINT ( 'NONE',  ( 13.64779416524800126, 19.95252045979090028, -22.24581330589570172 ) ) ;
#30639=CARTESIAN_POINT ( 'NONE',  ( 52.69325989587510151, 18.52870131071809823, -48.74392489991350175 ) ) ;
#30640=CARTESIAN_POINT ( 'NONE',  ( 55.96902894741660361, -45.83494304597260083, -17.77854326869700330 ) ) ;
#30641=CARTESIAN_POINT ( 'NONE',  ( 16.23919312834854622, 19.84040911589776357, -15.67087998636921498 ) ) ;
#30642=EDGE_LOOP ( 'NONE', ( #11151, #30273, #8634, #15036 ) ) ;
#30644=EDGE_CURVE ( 'NONE', #19736, #44974, #39204, .T. ) ;
#30646=CARTESIAN_POINT ( 'NONE',  ( 9.864589264534901147, 32.95178484568349830, -46.61883043024580076 ) ) ;
#30648=CARTESIAN_POINT ( 'NONE',  ( 10.83005342329749787, -65.00892210386099634, -17.86451960242310122 ) ) ;
#30649=CARTESIAN_POINT ( 'NONE',  ( 16.65420337941059969, -49.11618894467930829, -20.15000000000000213 ) ) ;
#30652=ORIENTED_EDGE ( 'NONE', *, *, #8824, .T. ) ;
#30654=ORIENTED_EDGE ( 'NONE', *, *, #15582, .F. ) ;
#30655=CARTESIAN_POINT ( 'NONE',  ( 10.48988994695839949, -63.23148834558760001, -45.62580560565609744 ) ) ;
#30660=CARTESIAN_POINT ( 'NONE',  ( 57.32828653034189870, 19.18168419026400073, -53.00038473087150237 ) ) ;
#30661=CARTESIAN_POINT ( 'NONE',  ( 52.14531167014489910, 18.65755136352539978, -76.93287919559629984 ) ) ;
#30664=CARTESIAN_POINT ( 'NONE',  ( 12.36324357420019915, -64.54680782163349306, -15.76420532458509882 ) ) ;
#30674=ORIENTED_EDGE ( 'NONE', *, *, #4580, .T. ) ;
#30677=AXIS2_PLACEMENT_3D ( 'NONE', #43981, #7833, #12532 ) ;
#30681=CARTESIAN_POINT ( 'NONE',  ( 14.53093143839820911, 9.901543998477746911, -75.56421356237308373 ) ) ;
#30684=CARTESIAN_POINT ( 'NONE',  ( 16.13393739769620083, -15.61618894467929941, -21.14999999999999858 ) ) ;
#30686=CARTESIAN_POINT ( 'NONE',  ( 41.86539284521009563, -44.96648031818330082, -5.828818289935889574 ) ) ;
#30687=DIRECTION ( 'NONE',  ( 0.000000000000000000, -1.000000000000000000, 0.000000000000000000 ) ) ;
#30689=EDGE_CURVE ( 'NONE', #3281, #44314, #35604, .T. ) ;
#30692=CARTESIAN_POINT ( 'NONE',  ( 56.46547357425270519, -50.77622842041579787, -74.28536251387168932 ) ) ;
#30693=CARTESIAN_POINT ( 'NONE',  ( -2.018330718851010008, 19.83360531021549988, -7.106613257804940353 ) ) ;
#30695=LINE ( 'NONE', #7380, #11306 ) ;
#30697=VERTEX_POINT ( 'NONE', #3570 ) ;
#30699=CARTESIAN_POINT ( 'NONE',  ( -3.978056048070269579, -47.86712544008820203, -4.331835806862760485 ) ) ;
#30700=CARTESIAN_POINT ( 'NONE',  ( 47.62947969218000566, 23.30723700853820191, -55.11574735166309580 ) ) ;
#30704=CARTESIAN_POINT ( 'NONE',  ( 12.12757547496249977, 33.95539785654250409, -16.69244762553350014 ) ) ;
#30705=CARTESIAN_POINT ( 'NONE',  ( 51.73306672719670019, 17.77684044143289910, -77.03096706391420412 ) ) ;
#30706=CARTESIAN_POINT ( 'NONE',  ( 52.82975622904280755, 18.42854261028849905, -48.48625935290110078 ) ) ;
#30707=CARTESIAN_POINT ( 'NONE',  ( 61.75019796695539753, -46.11618894467930119, -46.37203261889099792 ) ) ;
#30708=CARTESIAN_POINT ( 'NONE',  ( 54.36797223100090548, -49.00084403992370596, -48.99483916641750625 ) ) ;
#30709=CARTESIAN_POINT ( 'NONE',  ( 54.41698384653929566, 16.87217916612360114, -26.66137050635050088 ) ) ;
#30710=CARTESIAN_POINT ( 'NONE',  ( 50.26586832373690328, 21.96242454341640027, -54.04500157025010054 ) ) ;
#30712=CARTESIAN_POINT ( 'NONE',  ( 52.63952980978569940, 18.56936772728549911, -48.69585515676859444 ) ) ;
#30715=CARTESIAN_POINT ( 'NONE',  ( 10.77242972425730017, 32.05451349809659689, -45.20492820379810439 ) ) ;
#30723=CARTESIAN_POINT ( 'NONE',  ( 49.38368952090034725, -2.298263431363495535, -15.71712813759418026 ) ) ;
#30724=ORIENTED_EDGE ( 'NONE', *, *, #45974, .F. ) ;
#30725=CARTESIAN_POINT ( 'NONE',  ( 11.14030921647079886, -63.71572269098970054, -44.01013735364150392 ) ) ;
#30726=CARTESIAN_POINT ( 'NONE',  ( 57.36258065022549602, -45.13425998825839969, -25.53108703577100158 ) ) ;
#30732=CARTESIAN_POINT ( 'NONE',  ( 11.44079479683260026, 33.77516212222609937, -23.47454584385869936 ) ) ;
#30733=VERTEX_POINT ( 'NONE', #47591 ) ;
#30735=EDGE_CURVE ( 'NONE', #18008, #36317, #6983, .T. ) ;
#30739=ADVANCED_FACE ( 'NONE', ( #3048 ), #19019, .F. ) ;
#30740=CARTESIAN_POINT ( 'NONE',  ( 64.78100246958599939, -29.69834437706749952, -16.45672703461520214 ) ) ;
#30742=CARTESIAN_POINT ( 'NONE',  ( 46.93451352784899910, -54.01342379717689823, -75.73967526752529977 ) ) ;
#30743=CARTESIAN_POINT ( 'NONE',  ( 52.33571454780909704, 13.13344079467719894, -7.409926258573939606 ) ) ;
#30745=B_SPLINE_SURFACE_WITH_KNOTS ( 'NONE', 3, 3, ( 
 ( #17020, #29308, #44270, #21181, #17277, #44530, #33237, #13104, #45310, #8896, #499, #9419, #20404, #25369, #5484, #12568, #24582, #9153 ),
 ( #36147, #25104, #249, #16233, #48207, #40853, #4693, #28530, #8632, #20663, #36648, #32189, #753, #32971, #16750, #12310, #32702, #28269 ),
 ( #4956, #24325, #48729, #12833, #28790, #44791, #20926, #36922, #1026, #48997, #21692, #10445, #46615, #49510, #30073, #38479, #25879, #38220 ),
 ( #14106, #2315, #41893, #41625, #37440, #50535, #18553, #45829, #33497, #1795, #22470, #2579, #29812, #17778, #30594, #42679, #9663, #37962 ),
 ( #17529, #1541, #10703, #2059, #30336, #34529, #25622, #18037, #37699, #46359, #26144, #49763, #14627, #34259, #46098, #18287, #50282, #26657 ),
 ( #14368, #42154, #26398, #34006, #33748, #21441, #13601, #29564, #45570, #5733, #42418, #13855, #10183, #6510, #9916, #5991, #21951, #50016 ),
 ( #6253, #22210, #27442, #35577, #19331, #19068, #31875, #35830, #23752, #19840, #30847, #51562, #7802, #47388, #15663, #27950, #3870, #31616 ),
 ( #51814, #14882, #11484, #26929, #11995, #22984, #3103, #47634, #11222, #35042, #42935, #11742, #27700, #39768, #43698, #15920, #39006, #23491 ),
 ( #2842, #47892, #34788, #51051, #15148, #31107, #39254, #22726, #27185, #35311, #6775, #43192, #7287, #23238, #18808, #50794, #3357, #51312 ),
 ( #15407, #31360, #43445, #7547, #3615, #19587, #24005, #9090, #40025, #694, #12501, #48403, #20599, #4115, #24262, #20092, #12769, #36083 ) ),
 .UNSPECIFIED., .F., .F., .F.,
 ( 4, 1, 1, 1, 1, 1, 1, 4 ),
 ( 4, 2, 2, 2, 2, 2, 2, 2, 4 ),
 ( 0.000000000000000000, 0.1428571428571430157, 0.2857142857142860315, 0.4285714285714289917, 0.5714285714285709528, 0.7142857142857139685, 0.8571428571428569843, 1.000004205110210043 ),
 ( -4.205110215000000084E-06, 0.4467108845949059881, 0.9572376098462269667, 1.276316813128300032, 1.435856414769340006, 1.633224234453040102, 1.949012745946970160, 2.454274364337259762, 2.552637831366810328 ),
 .UNSPECIFIED. ) ;
#30746=CARTESIAN_POINT ( 'NONE',  ( 65.46029542295769943, -29.76883965895079953, -16.55376543218019947 ) ) ;
#30748=EDGE_CURVE ( 'NONE', #39800, #29825, #33130, .T. ) ;
#30750=CARTESIAN_POINT ( 'NONE',  ( 54.57977433850850701, -48.05032713420980173, -26.70386303289920349 ) ) ;
#30751=CARTESIAN_POINT ( 'NONE',  ( -3.898789279713819944, -49.42317546875409562, -6.816182948762260274 ) ) ;
#30752=CARTESIAN_POINT ( 'NONE',  ( 75.27130359675959426, 4.589503367956900171, -12.40984670276689883 ) ) ;
#30754=CARTESIAN_POINT ( 'NONE',  ( 75.29154419428947165, 13.40016185298322782, -14.05786387858811182 ) ) ;
#30756=DIRECTION ( 'NONE',  ( -1.000000000000000000, 0.000000000000000000, 0.000000000000000000 ) ) ;
#30757=CARTESIAN_POINT ( 'NONE',  ( 16.13393739769620083, -15.61618894467929941, -6.721843382729280059 ) ) ;
#30758=CARTESIAN_POINT ( 'NONE',  ( 82.37380189745128689, -45.11495191480410227, -46.56083452486799956 ) ) ;
#30759=DIRECTION ( 'NONE',  ( -1.000000000000000000, 0.000000000000000000, 0.000000000000000000 ) ) ;
#30760=CARTESIAN_POINT ( 'NONE',  ( 40.40277276999439948, 13.62463458412210038, -4.354462746277430796 ) ) ;
#30764=CYLINDRICAL_SURFACE ( 'NONE', #20862, 1.000000000000001110 ) ;
#30765=CARTESIAN_POINT ( 'NONE',  ( 17.73673790147540075, -51.97808261890140358, -75.79330468503940210 ) ) ;
#30776=CARTESIAN_POINT ( 'NONE',  ( 41.75079782317220634, -45.66965496456020190, -6.577253294032040287 ) ) ;
#30777=ORIENTED_EDGE ( 'NONE', *, *, #3829, .T. ) ;
#30781=CARTESIAN_POINT ( 'NONE',  ( 61.08961532041769971, -45.33614436321569485, -46.92979171198570043 ) ) ;
#30786=ORIENTED_EDGE ( 'NONE', *, *, #6269, .T. ) ;
#30787=CARTESIAN_POINT ( 'NONE',  ( 68.13393739769620083, -33.11618894467940066, -65.65000000000000568 ) ) ;
#30791=VERTEX_POINT ( 'NONE', #41008 ) ;
#30792=CARTESIAN_POINT ( 'NONE',  ( 61.55415490858696614, -29.38851365205942656, -15.99574535869865599 ) ) ;
#30793=CARTESIAN_POINT ( 'NONE',  ( 52.36416846730020325, -50.95050588212149734, -76.17671309931749590 ) ) ;
#30794=CARTESIAN_POINT ( 'NONE',  ( 60.73370194276889578, 14.32741777250609871, -47.36977307575320140 ) ) ;
#30795=CARTESIAN_POINT ( 'NONE',  ( 50.95939078474921047, -48.61618894467930119, -76.37902184192927280 ) ) ;
#30796=CARTESIAN_POINT ( 'NONE',  ( 41.85352072865990181, -43.83138081351579984, -4.272019245294999656 ) ) ;
#30798=CARTESIAN_POINT ( 'NONE',  ( -10.42111060954870005, 11.57999969675590002, -6.138047689998500367 ) ) ;
#30801=DIRECTION ( 'NONE',  ( -0.2260571801428030714, 0.000000000000000000, 0.9741140340359972782 ) ) ;
#30803=ADVANCED_FACE ( 'NONE', ( #20294 ), #9649, .T. ) ;
#30804=EDGE_LOOP ( 'NONE', ( #48716, #36199, #19856, #30080, #39380, #40518 ) ) ;
#30805=DIRECTION ( 'NONE',  ( 0.000000000000000000, 0.000000000000000000, -1.000000000000000000 ) ) ;
#30806=CARTESIAN_POINT ( 'NONE',  ( 57.48053633206980351, 19.28116340013579944, -53.28847060521069778 ) ) ;
#30810=CARTESIAN_POINT ( 'NONE',  ( 15.94238461914910054, 19.75473507481530078, -20.23090583108210083 ) ) ;
#30814=CARTESIAN_POINT ( 'NONE',  ( 48.04058133588620194, -54.36387450899209739, -55.20769835483399390 ) ) ;
#30816=AXIS2_PLACEMENT_3D ( 'NONE', #4281, #36244, #24428 ) ;
#30817=CARTESIAN_POINT ( 'NONE',  ( -3.978056047869968914, -47.86712544021135329, -4.331835810920249052 ) ) ;
#30818=CARTESIAN_POINT ( 'NONE',  ( 47.90025853917680365, 23.12498366852580034, -54.74357571739309947 ) ) ;
#30821=ORIENTED_EDGE ( 'NONE', *, *, #12089, .F. ) ;
#30824=CARTESIAN_POINT ( 'NONE',  ( 58.27624582431690214, -46.80735200045160127, -47.55852830428500511 ) ) ;
#30833=ORIENTED_EDGE ( 'NONE', *, *, #25572, .F. ) ;
#30834=EDGE_LOOP ( 'NONE', ( #6729, #13321, #48705, #10370, #16368, #10156 ) ) ;
#30835=CARTESIAN_POINT ( 'NONE',  ( 12.36320305068320025, -64.54682834576858852, -15.76422791927960176 ) ) ;
#30838=CARTESIAN_POINT ( 'NONE',  ( 12.40793752380340109, -65.45934900383400645, -47.57600753193199949 ) ) ;
#30839=EDGE_LOOP ( 'NONE', ( #17654, #30915, #19779, #16480, #34422 ) ) ;
#30842=CARTESIAN_POINT ( 'NONE',  ( 82.45630311851421368, -45.09271792554360303, -46.38988467804559690 ) ) ;
#30843=CARTESIAN_POINT ( 'NONE',  ( 52.70127459758040089, -49.76132437923789809, -48.79000188394560666 ) ) ;
#30844=EDGE_CURVE ( 'NONE', #34917, #5766, #2731, .T. ) ;
#30846=CARTESIAN_POINT ( 'NONE',  ( 58.94098116141569932, -3.123968702424910315, -15.65000564697079710 ) ) ;
#30847=CARTESIAN_POINT ( 'NONE',  ( 51.57818415910379883, -49.54080979270530349, -76.64184137469480618 ) ) ;
#30848=CARTESIAN_POINT ( 'NONE',  ( 57.43655318892930239, -49.91794914532149363, -52.37342405164899617 ) ) ;
#30854=AXIS2_PLACEMENT_3D ( 'NONE', #13494, #14257, #29450 ) ;
#30855=CARTESIAN_POINT ( 'NONE',  ( 68.13393739769620083, 4.883811055320659733, -65.65000000000000568 ) ) ;
#30858=CARTESIAN_POINT ( 'NONE',  ( 13.50106232664160011, -51.29021222096099564, -22.28116776360520035 ) ) ;
#30861=CARTESIAN_POINT ( 'NONE',  ( 57.30711608794669587, 13.88381105532070059, -16.97812376854340144 ) ) ;
#30868=CARTESIAN_POINT ( 'NONE',  ( 47.26969180900800183, 22.92145913501139987, -75.47109442055808870 ) ) ;
#30870=EDGE_CURVE ( 'NONE', #47619, #15485, #22460, .T. ) ;
#30873=DIRECTION ( 'NONE',  ( 4.809214325624639985E-31, -1.000000000000000000, -6.060292087350920604E-16 ) ) ;
#30874=FACE_OUTER_BOUND ( 'NONE', #10881, .T. ) ;
#30875=CARTESIAN_POINT ( 'NONE',  ( 82.45926474365251124, 14.04402909200689997, -47.17634237573840039 ) ) ;
#30877=CARTESIAN_POINT ( 'NONE',  ( 68.13393739769620083, 17.38381105532069881, -65.65000000000000568 ) ) ;
#30881=FACE_OUTER_BOUND ( 'NONE', #50211, .T. ) ;
#30883=CARTESIAN_POINT ( 'NONE',  ( 53.33637666853859827, -49.41089065994679430, -48.94981449663340101 ) ) ;
#30888=CARTESIAN_POINT ( 'NONE',  ( 13.81950199472360019, 20.03075999611900215, -23.06529971393420198 ) ) ;
#30889=DIRECTION ( 'NONE',  ( 1.000000000000000000, 0.000000000000000000, 0.000000000000000000 ) ) ;
#30892=CARTESIAN_POINT ( 'NONE',  ( 52.96080964268509916, 18.38537766553690034, -48.98458843674050200 ) ) ;
#30893=CARTESIAN_POINT ( 'NONE',  ( 56.28192814617099771, -45.52819751003289639, -17.93020058329020117 ) ) ;
#30894=CARTESIAN_POINT ( 'NONE',  ( 68.13393739769620083, -50.61618894467930119, -73.25000000000000000 ) ) ;
#30898=CARTESIAN_POINT ( 'NONE',  ( 61.13393739769620083, 4.883811055320659733, -84.38499399519520239 ) ) ;
#30899=CARTESIAN_POINT ( 'NONE',  ( 9.383988014790560328, 32.17454221883009780, -46.50702848791099342 ) ) ;
#30901=CARTESIAN_POINT ( 'NONE',  ( 50.87650205437540052, -52.17794571071839727, -52.56647976602120309 ) ) ;
#30902=CARTESIAN_POINT ( 'NONE',  ( 53.30280620372429468, 18.18069847459639732, -48.78464136231010428 ) ) ;
#30904=CARTESIAN_POINT ( 'NONE',  ( 51.65923706648989366, -52.70673387297149759, -53.94592918870640119 ) ) ;
#30908=CARTESIAN_POINT ( 'NONE',  ( 10.14486239315709959, -63.26972435890289148, -45.99310794422409998 ) ) ;
#30910=CARTESIAN_POINT ( 'NONE',  ( 68.13393739769769297, 18.72622661238300168, -73.39853292320978539 ) ) ;
#30912=CARTESIAN_POINT ( 'NONE',  ( 11.38042644497720701, -64.49026688052417455, -44.43662027715303964 ) ) ;
#30913=FACE_OUTER_BOUND ( 'NONE', #5549, .T. ) ;
#30914=CARTESIAN_POINT ( 'NONE',  ( 52.71937669323779829, 18.95387029200830042, -77.16972201513189589 ) ) ;
#30915=ORIENTED_EDGE ( 'NONE', *, *, #30266, .T. ) ;
#30919=CARTESIAN_POINT ( 'NONE',  ( 83.53665348986312722, -44.61316859376488253, -46.51478504062129105 ) ) ;
#30920=FACE_BOUND ( 'NONE', #41295, .T. ) ;
#30927=AXIS2_PLACEMENT_3D ( 'NONE', #23757, #10708, #50798 ) ;
#30928=DIRECTION ( 'NONE',  ( 1.000000000000000000, 0.000000000000000000, 0.000000000000000000 ) ) ;
#30930=AXIS2_PLACEMENT_3D ( 'NONE', #34936, #51204, #19973 ) ;
#30931=EDGE_CURVE ( 'NONE', #31554, #18021, #22881, .T. ) ;
#30932=CARTESIAN_POINT ( 'NONE',  ( 46.59919755282350451, 13.88381105532070059, -7.957589888115209398 ) ) ;
#30935=CARTESIAN_POINT ( 'NONE',  ( 13.13393739769619906, -63.52234721269329754, -46.39999999999999858 ) ) ;
#30938=EDGE_CURVE ( 'NONE', #2407, #32428, #27369, .T. ) ;
#30939=CYLINDRICAL_SURFACE ( 'NONE', #49121, 2.000000000000000888 ) ;
#30942=CARTESIAN_POINT ( 'NONE',  ( 55.82040737148000176, -50.78110051580220130, -75.19538818979980022 ) ) ;
#30943=CARTESIAN_POINT ( 'NONE',  ( -2.275804916070590433, 19.87795878944950090, -7.555165436777629751 ) ) ;
#30944=DIRECTION ( 'NONE',  ( -0.9987374001630935361, 0.000000000000000000, -0.05023550054955997629 ) ) ;
#30947=VERTEX_POINT ( 'NONE', #11115 ) ;
#30949=CARTESIAN_POINT ( 'NONE',  ( 47.72868234502399787, 23.24232774156940096, -54.87766230676579937 ) ) ;
#30950=ADVANCED_FACE ( 'NONE', ( #50431 ), #22366, .F. ) ;
#30953=CARTESIAN_POINT ( 'NONE',  ( 61.05708818547999783, 14.47205664048929918, -47.78546709072629994 ) ) ;
#30954=CARTESIAN_POINT ( 'NONE',  ( 11.84787507268790030, 34.05753326919850110, -17.04454487390190209 ) ) ;
#30955=CARTESIAN_POINT ( 'NONE',  ( 51.96022074122749501, 18.76462827808190070, -76.69846447276000845 ) ) ;
#30956=CARTESIAN_POINT ( 'NONE',  ( 53.43246109071290562, 18.11429855641319975, -48.81566079190549345 ) ) ;
#30959=CARTESIAN_POINT ( 'NONE',  ( 54.84972377084940121, 16.62358603453460049, -26.66243130723649912 ) ) ;
#30962=LINE ( 'NONE', #40389, #16133 ) ;
#30964=CARTESIAN_POINT ( 'NONE',  ( 53.02879948416539690, 18.37809327181799901, -49.09530617495999394 ) ) ;
#30965=CARTESIAN_POINT ( 'NONE',  ( 62.27952691711369937, -30.53997204947359734, -16.33238526922729861 ) ) ;
#30967=CARTESIAN_POINT ( 'NONE',  ( 11.13393739769619906, 32.22978334998650496, -43.92380911455280312 ) ) ;
#30969=VECTOR ( 'NONE', #3735, 1000.000000000000000 ) ;
#30970=AXIS2_PLACEMENT_3D ( 'NONE', #24180, #16090, #11656 ) ;
#30972=CARTESIAN_POINT ( 'NONE',  ( 51.13861002788090104, -34.97236549711250575, -76.48487255855283706 ) ) ;
#30974=ORIENTED_EDGE ( 'NONE', *, *, #31501, .T. ) ;
#30975=ORIENTED_EDGE ( 'NONE', *, *, #44228, .F. ) ;
#30980=CARTESIAN_POINT ( 'NONE',  ( 11.13393758244130005, -63.50662458344459793, -43.95118814396819573 ) ) ;
#30981=CARTESIAN_POINT ( 'NONE',  ( 56.99918881514469859, -45.18030430956060428, -25.37149625033120159 ) ) ;
#30983=EDGE_CURVE ( 'NONE', #43431, #47622, #46260, .T. ) ;
#30985=VERTEX_POINT ( 'NONE', #12659 ) ;
#30986=CARTESIAN_POINT ( 'NONE',  ( 11.29751794088404360, 33.95857977818198492, -22.86704619065415756 ) ) ;
#30988=CARTESIAN_POINT ( 'NONE',  ( 42.75216321632269967, -44.98233172091430276, -6.093641062779489914 ) ) ;
#30992=CARTESIAN_POINT ( 'NONE',  ( 51.68174538021649767, 1.214832132191203673, -18.13120047747256436 ) ) ;
#30994=AXIS2_PLACEMENT_3D ( 'NONE', #977, #43969, #28224 ) ;
#30995=CARTESIAN_POINT ( 'NONE',  ( 60.79941944348659888, -29.22537550237669990, -15.89275653899559870 ) ) ;
#30997=CARTESIAN_POINT ( 'NONE',  ( 47.19472346965950038, -54.65936592792999704, -74.80901628187270092 ) ) ;
#30998=CARTESIAN_POINT ( 'NONE',  ( 55.69411755635510275, 14.72515888537330042, -17.00763503960670064 ) ) ;
#30999=CARTESIAN_POINT ( 'NONE',  ( 15.05440318628110141, 21.88381105532300097, -76.14999999999999147 ) ) ;
#31000=( BOUNDED_CURVE ( )  B_SPLINE_CURVE ( 3, ( #14530, #50950, #22892, #47040 ),
 .UNSPECIFIED., .F., .F. ) 
 B_SPLINE_CURVE_WITH_KNOTS ( ( 4, 4 ),
 ( 3.802771094680959862, 3.909080582966734774 ),
 .UNSPECIFIED. ) 
 CURVE ( )  GEOMETRIC_REPRESENTATION_ITEM ( )  RATIONAL_B_SPLINE_CURVE ( ( 1.000000000000000000, 0.9990584127885050458, 0.9990584127885050458, 1.000000000000000000 ) ) 
 REPRESENTATION_ITEM ( '' )  );
#31002=CARTESIAN_POINT ( 'NONE',  ( 61.74535513545370691, 13.88381108448669998, -28.01209385561339715 ) ) ;
#31005=B_SPLINE_SURFACE_WITH_KNOTS ( 'NONE', 3, 3, ( 
 ( #33127, #49155, #29201, #45211, #33652, #37588 ),
 ( #9320, #1701, #17936, #21337, #37341, #45469 ),
 ( #9569, #25778, #17683, #49670, #41785, #5892 ),
 ( #45990, #26829, #11120, #51466, #26561, #51211 ),
 ( #10606, #27344, #19224, #38648, #46774, #47537 ),
 ( #2994, #50687, #23141, #6932, #23389, #19482 ),
 ( #2736, #11634, #35474, #42315, #22633, #18964 ),
 ( #47036, #43348, #15305, #15565, #31259, #43093 ),
 ( #22371, #15039, #47291, #7442, #11381, #2467 ),
 ( #18456, #39415, #34944, #42837, #22886, #31519 ),
 ( #39156, #42575, #38377, #6668, #3515, #18709 ),
 ( #27089, #6413, #34425, #3251, #50436, #7185 ),
 ( #35210, #14525, #34685, #30495, #14783, #30752 ),
 ( #46517, #10860, #38904, #50945, #31009, #40174 ),
 ( #8468, #44109, #8725, #4788, #12665, #39925 ),
 ( #20756, #27596, #7950, #23649, #43603, #39665 ) ),
 .UNSPECIFIED., .F., .F., .F.,
 ( 4, 2, 2, 2, 2, 2, 2, 4 ),
 ( 4, 1, 1, 4 ),
 ( 9.575042469628741060, 13.03139574839190118, 27.92441946083980042, 37.23255928111969837, 41.88662919125970063, 49.33314104748369999, 61.24756001744199807, 64.89007609261069831 ),
 ( -0.001356146170799000074, 0.3333333333333329818, 0.6666666666666670737, 1.001373499198290107 ),
 .UNSPECIFIED. ) ;
#31008=CARTESIAN_POINT ( 'NONE',  ( 8.625847590987680391, -62.42720030092139893, -14.82880704068799993 ) ) ;
#31009=CARTESIAN_POINT ( 'NONE',  ( 75.63587938996879245, 9.758298940360759843, -13.13773444762449927 ) ) ;
#31010=CARTESIAN_POINT ( 'NONE',  ( 75.42809886163706778, 12.76391134240307679, -13.58404645785000220 ) ) ;
#31011=CARTESIAN_POINT ( 'NONE',  ( 17.49475137708000005, -51.11618894467930119, -15.67743210564179890 ) ) ;
#31013=CARTESIAN_POINT ( 'NONE',  ( 47.21773113835070035, 23.54756601831279639, -54.61692783540039642 ) ) ;
#31015=CARTESIAN_POINT ( 'NONE',  ( 82.57809707948020161, -45.19656880909330710, -47.00698240636869940 ) ) ;
#31016=CARTESIAN_POINT ( 'NONE',  ( 57.36818733098329659, -50.13385377957740019, -52.61777321114799832 ) ) ;
#31017=CARTESIAN_POINT ( 'NONE',  ( 42.93197233849409855, 11.32569894967160096, -3.307825584507050110 ) ) ;
#31018=CARTESIAN_POINT ( 'NONE',  ( 47.58822566456690595, -54.46711296473307584, -74.72768729673299504 ) ) ;
#31019=CARTESIAN_POINT ( 'NONE',  ( 68.57574012094990223, -45.11618894467940066, -13.49754435276109987 ) ) ;
#31020=CARTESIAN_POINT ( 'NONE',  ( 58.65392622551220114, -46.60947465638219711, -47.57606315241160644 ) ) ;
#31021=CARTESIAN_POINT ( 'NONE',  ( 56.55522360613520760, 14.97957722649010037, -26.26695323647559732 ) ) ;
#31022=EDGE_CURVE ( 'NONE', #22850, #40057, #3568, .T. ) ;
#31023=CARTESIAN_POINT ( 'NONE',  ( 67.02526494145590163, -1.318240963702770108, -17.24421836522840223 ) ) ;
#31024=CARTESIAN_POINT ( 'NONE',  ( 17.87259706178020124, -51.26000396899109290, -74.91994212300129163 ) ) ;
#31025=CARTESIAN_POINT ( 'NONE',  ( 58.83289924021099893, -43.75437917904619667, -8.825342791311319601 ) ) ;
#31029=ORIENTED_EDGE ( 'NONE', *, *, #23856, .F. ) ;
#31031=CARTESIAN_POINT ( 'NONE',  ( 61.30872397726910350, -45.59477435387500321, -47.67209317366800292 ) ) ;
#31035=CARTESIAN_POINT ( 'NONE',  ( 45.32091058997599475, -45.57449214110749836, -8.659579893190318955 ) ) ;
#31036=ORIENTED_EDGE ( 'NONE', *, *, #5224, .T. ) ;
#31037=CARTESIAN_POINT ( 'NONE',  ( 17.95470215398700375, 20.84016670874339638, -75.79682998878489286 ) ) ;
#31038=ORIENTED_EDGE ( 'NONE', *, *, #44423, .T. ) ;
#31040=DIRECTION ( 'NONE',  ( 0.9441882088883221114, 0.3294064756440929775, 0.000000000000000000 ) ) ;
#31043=CARTESIAN_POINT ( 'NONE',  ( 16.13393739769620083, -15.61618894467929941, -11.54999999999999893 ) ) ;
#31045=ORIENTED_EDGE ( 'NONE', *, *, #43594, .F. ) ;
#31047=DIRECTION ( 'NONE',  ( 0.000000000000000000, 0.000000000000000000, -1.000000000000000000 ) ) ;
#31051=CARTESIAN_POINT ( 'NONE',  ( 57.24929578595760660, -50.61618894467930119, -74.14999999999999147 ) ) ;
#31054=CARTESIAN_POINT ( 'NONE',  ( 52.71259601604019451, -51.43286903184419856, -75.79898490202970152 ) ) ;
#31055=CARTESIAN_POINT ( 'NONE',  ( 60.49619678835889403, 14.44108935951489947, -47.41857351171270096 ) ) ;
#31057=DIRECTION ( 'NONE',  ( 0.000000000000000000, -1.000000000000000000, 0.000000000000000000 ) ) ;
#31058=CARTESIAN_POINT ( 'NONE',  ( -7.616907281497659277, 14.17406059737050050, -5.566654447284809848 ) ) ;
#31065=CARTESIAN_POINT ( 'NONE',  ( 57.43631978869650112, 18.92123149693339812, -52.64527532753600525 ) ) ;
#31068=CARTESIAN_POINT ( 'NONE',  ( 14.01533392343269924, 19.26065124468200196, -21.05253849812200073 ) ) ;
#31069=AXIS2_PLACEMENT_3D ( 'NONE', #25471, #21029, #37030 ) ;
#31071=CARTESIAN_POINT ( 'NONE',  ( 48.02285049171399578, -54.32307516229949584, -54.84930373619759791 ) ) ;
#31073=ADVANCED_FACE ( 'NONE', ( #29588 ), #32018, .T. ) ;
#31074=CARTESIAN_POINT ( 'NONE',  ( 56.39270784037419304, 19.29512405589720103, -52.86271187285759510 ) ) ;
#31075=CARTESIAN_POINT ( 'NONE',  ( 47.64143405403320486, 23.30250925608009993, -55.14905519569659731 ) ) ;
#31077=ORIENTED_EDGE ( 'NONE', *, *, #12652, .T. ) ;
#31079=ORIENTED_EDGE ( 'NONE', *, *, #44488, .F. ) ;
#31081=CARTESIAN_POINT ( 'NONE',  ( 60.52694424712060339, -45.62814803647550121, -47.19145984235160540 ) ) ;
#31083=CARTESIAN_POINT ( 'NONE',  ( 50.03007040746459921, 17.38381105532069881, -76.14999999999999147 ) ) ;
#31084=FACE_OUTER_BOUND ( 'NONE', #48955, .T. ) ;
#31085=CARTESIAN_POINT ( 'NONE',  ( 61.75019796695539753, -45.11618894467940066, -46.37203261889099792 ) ) ;
#31089=EDGE_LOOP ( 'NONE', ( #3857, #15068, #25941, #25500, #5160 ) ) ;
#31090=FACE_OUTER_BOUND ( 'NONE', #18281, .T. ) ;
#31091=ORIENTED_EDGE ( 'NONE', *, *, #47568, .T. ) ;
#31094=DIRECTION ( 'NONE',  ( 0.9858858899415445798, 2.580012592456886595E-12, -0.1674186728360041176 ) ) ;
#31095=CARTESIAN_POINT ( 'NONE',  ( 12.91917450909959975, 34.27891870249889905, -47.58062843006289455 ) ) ;
#31096=CARTESIAN_POINT ( 'NONE',  ( 10.32255761268189964, -64.75990130589950411, -46.96739154628469493 ) ) ;
#31100=EDGE_CURVE ( 'NONE', #5359, #2490, #2783, .T. ) ;
#31102=DIRECTION ( 'NONE',  ( 1.000000000000000000, 0.000000000000000000, 0.000000000000000000 ) ) ;
#31106=CARTESIAN_POINT ( 'NONE',  ( 64.31467946070409880, -0.4499903462937720477, -16.60140817515059908 ) ) ;
#31107=CARTESIAN_POINT ( 'NONE',  ( 51.73429016900899313, -49.15904133096110229, -76.96796945980311477 ) ) ;
#31115=CARTESIAN_POINT ( 'NONE',  ( 59.53476406250169362, -46.29126728519970158, -47.84522406268589378 ) ) ;
#31117=CARTESIAN_POINT ( 'NONE',  ( 12.44378448573739959, -49.98269638858799624, -21.13285771745299968 ) ) ;
#31118=CARTESIAN_POINT ( 'NONE',  ( 54.32114520510300082, 19.38381105532069881, -76.86722889149370985 ) ) ;
#31120=CARTESIAN_POINT ( 'NONE',  ( 56.88018964337059913, 13.94865836461010034, -17.08460512071569681 ) ) ;
#31121=CARTESIAN_POINT ( 'NONE',  ( 61.02921381188160410, -45.52723101486190416, -47.53466998951989808 ) ) ;
#31122=CARTESIAN_POINT ( 'NONE',  ( 56.77563393664169666, -50.64689510413649742, -53.45922468511930248 ) ) ;
#31125=ORIENTED_EDGE ( 'NONE', *, *, #39261, .F. ) ;
#31126=CARTESIAN_POINT ( 'NONE',  ( 13.42256853332840016, -51.72201361531850239, -74.35192203308750436 ) ) ;
#31129=CARTESIAN_POINT ( 'NONE',  ( 11.67620015026735203, -64.89165383396532150, -23.88711004025349283 ) ) ;
#31130=CARTESIAN_POINT ( 'NONE',  ( 70.56223753246619879, 13.88381105532070059, -14.05824725777380024 ) ) ;
#31132=CARTESIAN_POINT ( 'NONE',  ( 82.39375047534959151, 13.90419211000809874, -46.71925512375379697 ) ) ;
#31134=CARTESIAN_POINT ( 'NONE',  ( 53.23465404654513122, 19.19659352034578959, -77.19488661914444094 ) ) ;
#31135=DIRECTION ( 'NONE',  ( 0.000000000000000000, -1.000000000000000000, 0.000000000000000000 ) ) ;
#31138=CARTESIAN_POINT ( 'NONE',  ( 49.47908289717140207, 22.45249353912830159, -54.66541287124849902 ) ) ;
#31140=CIRCLE ( 'NONE', #25266, 22.00000000000000355 ) ;
#31142=CARTESIAN_POINT ( 'NONE',  ( 53.10876379251020296, -49.52367567955289474, -48.93018545852340395 ) ) ;
#31147=CARTESIAN_POINT ( 'NONE',  ( 13.91186867058490151, 19.84412712960480007, -22.10133442523809677 ) ) ;
#31150=CARTESIAN_POINT ( 'NONE',  ( 52.76221410082400354, 18.49020305563599820, -48.84748657229020097 ) ) ;
#31151=CARTESIAN_POINT ( 'NONE',  ( 55.80275820535209874, -45.58445552780170118, -16.47843131335860178 ) ) ;
#31152=CARTESIAN_POINT ( 'NONE',  ( 8.784728771152179760, 31.88305279685639704, -46.67204636145419983 ) ) ;
#31153=VERTEX_POINT ( 'NONE', #6800 ) ;
#31155=ORIENTED_EDGE ( 'NONE', *, *, #3182, .F. ) ;
#31156=CARTESIAN_POINT ( 'NONE',  ( 11.71337184211249927, -65.28004931318540116, -17.10636605765209950 ) ) ;
#31157=CARTESIAN_POINT ( 'NONE',  ( 11.14532849681570070, 33.83291464669790116, -47.04966230858290288 ) ) ;
#31160=CARTESIAN_POINT ( 'NONE',  ( 52.56949981068906652, -49.85724369911663700, -48.49331493222930334 ) ) ;
#31161=CARTESIAN_POINT ( 'NONE',  ( 82.45630311851421368, -45.09271792554360303, -46.38988467804559690 ) ) ;
#31162=CARTESIAN_POINT ( 'NONE',  ( 51.75362667781039505, -52.76185628017049822, -54.27263750760450023 ) ) ;
#31165=CARTESIAN_POINT ( 'NONE',  ( 9.732699106784480136, -63.17170994995979783, -46.29943774989700245 ) ) ;
#31166=CARTESIAN_POINT ( 'NONE',  ( 70.83393739769690001, 16.88381105531530579, -74.20000000000047180 ) ) ;
#31170=CARTESIAN_POINT ( 'NONE',  ( 57.19702054503510169, 19.38356614133159894, -53.75054411148590106 ) ) ;
#31171=CARTESIAN_POINT ( 'NONE',  ( 12.13393739769649926, 24.18330853958550364, -23.15000000000000213 ) ) ;
#31177=CARTESIAN_POINT ( 'NONE',  ( 1.633937397696199056, -15.61618894467930119, -7.349999999999999645 ) ) ;
#31181=CARTESIAN_POINT ( 'NONE',  ( 43.27084646103560317, -43.87227363443550132, -5.051381114840269859 ) ) ;
#31184=CARTESIAN_POINT ( 'NONE',  ( 50.93004313118130000, -50.92639752731179925, -76.14999999999999147 ) ) ;
#31186=CARTESIAN_POINT ( 'NONE',  ( 47.24352027743620397, 23.52783393649020027, -74.19756735715161255 ) ) ;
#31188=CARTESIAN_POINT ( 'NONE',  ( 0.1542402430813090142, -50.99248106341759978, -19.14999999999999858 ) ) ;
#31189=CARTESIAN_POINT ( 'NONE',  ( 11.66836325772959881, 33.74040207072849995, -16.48189043737649939 ) ) ;
#31191=CARTESIAN_POINT ( 'NONE',  ( 52.58769281011270635, -49.83788694981130618, -27.98708932276760208 ) ) ;
#31193=CARTESIAN_POINT ( 'NONE',  ( 57.21119120591109208, -50.61618800962469322, -74.41418816113228729 ) ) ;
#31194=CARTESIAN_POINT ( 'NONE',  ( -7.152478658582400506, 15.01426846172460117, -6.869100105340580242 ) ) ;
#31198=DIRECTION ( 'NONE',  ( 1.000000000000000000, 0.000000000000000000, 0.000000000000000000 ) ) ;
#31199=EDGE_CURVE ( 'NONE', #9596, #9489, #28783, .T. ) ;
#31201=CARTESIAN_POINT ( 'NONE',  ( 14.43858045676712720, 21.38896804172114230, -76.01806011802842988 ) ) ;
#31202=EDGE_CURVE ( 'NONE', #47320, #12485, #27463, .T. ) ;
#31203=CARTESIAN_POINT ( 'NONE',  ( 47.53404130184800636, 23.35181273068509711, -55.01564180042830543 ) ) ;
#31204=CARTESIAN_POINT ( 'NONE',  ( 61.41267152474549817, -45.16781038087659539, -27.92979456378700220 ) ) ;
#31206=CARTESIAN_POINT ( 'NONE',  ( 61.37892440507240366, 14.09575071485549991, -47.24517396406390191 ) ) ;
#31210=CARTESIAN_POINT ( 'NONE',  ( 51.30775049128980214, 17.38380848247659571, -76.60305691058019306 ) ) ;
#31211=CARTESIAN_POINT ( 'NONE',  ( 53.40534283797200032, 18.12842647251899919, -48.82229431740969972 ) ) ;
#31212=FACE_OUTER_BOUND ( 'NONE', #3149, .T. ) ;
#31214=CARTESIAN_POINT ( 'NONE',  ( 55.35735860040240652, 16.14714136825730151, -26.51181232951169875 ) ) ;
#31215=CARTESIAN_POINT ( 'NONE',  ( 50.52790554252050015, 22.07298246124570085, -54.91101322106079863 ) ) ;
#31216=AXIS2_PLACEMENT_3D ( 'NONE', #35480, #31526, #43860 ) ;
#31218=CARTESIAN_POINT ( 'NONE',  ( 10.49497832658790131, -63.36864664907449196, -45.62743361653370044 ) ) ;
#31219=CARTESIAN_POINT ( 'NONE',  ( 42.62644315548480023, 11.62703185229469938, -3.197525305353840608 ) ) ;
#31220=CARTESIAN_POINT ( 'NONE',  ( 59.05823500560009620, -28.84314769625699881, -15.68946708767219711 ) ) ;
#31222=CARTESIAN_POINT ( 'NONE',  ( 11.13393739769619906, 32.09516374018799922, -43.74800381802249660 ) ) ;
#31223=VECTOR ( 'NONE', #46095, 1000.000000000000000 ) ;
#31225=DIRECTION ( 'NONE',  ( -1.000000000000000000, 0.000000000000000000, 0.000000000000000000 ) ) ;
#31226=DIRECTION ( 'NONE',  ( 0.2313469967918511672, -0.8455706941739528082, 0.4811327968758425389 ) ) ;
#31227=ORIENTED_EDGE ( 'NONE', *, *, #3724, .F. ) ;
#31228=ORIENTED_EDGE ( 'NONE', *, *, #35597, .F. ) ;
#31229=CARTESIAN_POINT ( 'NONE',  ( 56.73072851102580216, 19.11736299019269936, -52.75329813363410381 ) ) ;
#31230=CARTESIAN_POINT ( 'NONE',  ( 49.58944174246663295, -29.23728716619012857, -15.75935478527375189 ) ) ;
#31233=CARTESIAN_POINT ( 'NONE',  ( 56.07552736419609829, -45.72903556735669639, -25.51839513193560194 ) ) ;
#31238=CARTESIAN_POINT ( 'NONE',  ( 12.64456732695109942, 34.26332736361320030, -22.97177317294229937 ) ) ;
#31240=CARTESIAN_POINT ( 'NONE',  ( 46.03121482517249774, -45.11618894467940066, -7.582874669927740285 ) ) ;
#31242=CARTESIAN_POINT ( 'NONE',  ( 57.50723796702470025, -47.11618894467930119, -31.98003398042899903 ) ) ;
#31244=CARTESIAN_POINT ( 'NONE',  ( 59.46287080461119956, -28.41472307337230063, -15.69699063629330027 ) ) ;
#31246=CARTESIAN_POINT ( 'NONE',  ( 46.41240425002109760, -53.01349718276490108, -76.14999999999999147 ) ) ;
#31250=CARTESIAN_POINT ( 'NONE',  ( 45.01575386057460548, 14.77919493983159960, -8.915118302820459917 ) ) ;
#31253=CARTESIAN_POINT ( 'NONE',  ( 84.39650841167420481, -43.49490765828570460, -47.35795223498069362 ) ) ;
#31256=ORIENTED_EDGE ( 'NONE', *, *, #1875, .T. ) ;
#31257=CARTESIAN_POINT ( 'NONE',  ( 54.79698325214220489, -47.90516110802800398, -26.67907444486039736 ) ) ;
#31258=CARTESIAN_POINT ( 'NONE',  ( -5.802364285079610440, -47.44218980195390145, -6.163383152730290249 ) ) ;
#31259=CARTESIAN_POINT ( 'NONE',  ( 75.26680305930699433, -14.04978866029259876, -11.37374796283529932 ) ) ;
#31261=CARTESIAN_POINT ( 'NONE',  ( 12.89658887244659979, -50.00140126166379417, -21.06837794357040039 ) ) ;
#31262=CARTESIAN_POINT ( 'NONE',  ( 13.87894895853409416, -55.55385804827719909, -76.14999999999999147 ) ) ;
#31263=CARTESIAN_POINT ( 'NONE',  ( 47.21691115651439929, 23.54821565252409954, -54.61897267083390517 ) ) ;
#31264=CARTESIAN_POINT ( 'NONE',  ( 82.26799080613189119, -45.14410041576280008, -46.71841345350929942 ) ) ;
#31265=CARTESIAN_POINT ( 'NONE',  ( 57.27338646566600033, -50.61204626796450157, -53.75880438950069617 ) ) ;
#31266=CARTESIAN_POINT ( 'NONE',  ( 42.25512407695530470, 12.46306899543039926, -4.476913604614050080 ) ) ;
#31270=CARTESIAN_POINT ( 'NONE',  ( 56.23228709081130461, -47.87823924875339543, -47.98841366488070292 ) ) ;
#31273=CARTESIAN_POINT ( 'NONE',  ( 66.66723128061150305, -1.312581826788029815, -17.00552257602960182 ) ) ;
#31274=CARTESIAN_POINT ( 'NONE',  ( 17.88460903198290097, -51.65751396603660339, -75.51495726157199329 ) ) ;
#31275=CARTESIAN_POINT ( 'NONE',  ( 44.81421300434149657, -45.11618894467940066, -7.294680430930359449 ) ) ;
#31280=CARTESIAN_POINT ( 'NONE',  ( 8.792634198315560923, 31.92357537073090157, -46.67064936031920297 ) ) ;
#31285=CARTESIAN_POINT ( 'NONE',  ( 40.72222851082409534, -45.28361251854680347, -5.660115265888800096 ) ) ;
#31287=CARTESIAN_POINT ( 'NONE',  ( 17.77507174714839877, 21.09308431968760189, -75.96462645239850531 ) ) ;
#31288=ORIENTED_EDGE ( 'NONE', *, *, #80, .T. ) ;
#31289=CIRCLE ( 'NONE', #36338, 2.000000000000004441 ) ;
#31290=ORIENTED_EDGE ( 'NONE', *, *, #31576, .F. ) ;
#31291=EDGE_CURVE ( 'NONE', #48131, #26643, #43723, .T. ) ;
#31292=CARTESIAN_POINT ( 'NONE',  ( 57.38548500607309677, -45.11618894467940066, -16.91114573195289950 ) ) ;
#31294=AXIS2_PLACEMENT_3D ( 'NONE', #28955, #39994, #27921 ) ;
#31297=DIRECTION ( 'NONE',  ( 0.4872913772396111898, 0.8732394366197182567, 0.000000000000000000 ) ) ;
#31304=CARTESIAN_POINT ( 'NONE',  ( 51.81953057646069993, -51.23881869680439394, -76.05779032467960121 ) ) ;
#31305=CARTESIAN_POINT ( 'NONE',  ( 61.23361899263159813, 14.35831534285940059, -47.66404968818600452 ) ) ;
#31306=EDGE_CURVE ( 'NONE', #1545, #29700, #25612, .T. ) ;
#31310=CARTESIAN_POINT ( 'NONE',  ( 12.26481034824478478, 34.23527980536555759, -22.60721090778044484 ) ) ;
#31311=EDGE_CURVE ( 'NONE', #37505, #38543, #622, .T. ) ;
#31312=CARTESIAN_POINT ( 'NONE',  ( -9.426225745850960180, 12.53465503246489909, -5.815077069593810322 ) ) ;
#31313=CARTESIAN_POINT ( 'NONE',  ( 47.18058889863803529, 23.56890040466754499, -74.36261479959277665 ) ) ;
#31320=DIRECTION ( 'NONE',  ( 1.000000000000000000, 0.000000000000000000, 0.000000000000000000 ) ) ;
#31323=CARTESIAN_POINT ( 'NONE',  ( 15.33884134720609893, 19.72557400333539945, -21.05298682722020231 ) ) ;
#31324=EDGE_CURVE ( 'NONE', #47971, #9060, #51586, .T. ) ;
#31325=CARTESIAN_POINT ( 'NONE',  ( 12.22498195829099998, 18.79317371135340053, -21.14999999988710400 ) ) ;
#31328=CARTESIAN_POINT ( 'NONE',  ( 48.66886125943680952, -54.03308671629140036, -54.81979436189590160 ) ) ;
#31329=DIRECTION ( 'NONE',  ( 0.000000000000000000, 0.000000000000000000, -1.000000000000000000 ) ) ;
#31332=ORIENTED_EDGE ( 'NONE', *, *, #51496, .T. ) ;
#31335=CARTESIAN_POINT ( 'NONE',  ( 17.98856614016580480, 21.26098553207546971, -75.92929758216462233 ) ) ;
#31336=CARTESIAN_POINT ( 'NONE',  ( 60.83600080046799974, -45.51118010285600235, -47.34051533470169915 ) ) ;
#31337=CARTESIAN_POINT ( 'NONE',  ( 48.64767879017822594, -53.93625458155253938, -54.52761353198754080 ) ) ;
#31339=CARTESIAN_POINT ( 'NONE',  ( 83.05638573198190500, 14.23020891227059970, -47.55746740334460299 ) ) ;
#31342=DIRECTION ( 'NONE',  ( 0.000000000000000000, 0.000000000000000000, -1.000000000000000000 ) ) ;
#31344=CYLINDRICAL_SURFACE ( 'NONE', #31478, 2.000000000000001776 ) ;
#31345=AXIS2_PLACEMENT_3D ( 'NONE', #6720, #33949, #42358 ) ;
#31347=ORIENTED_EDGE ( 'NONE', *, *, #45860, .T. ) ;
#31351=CARTESIAN_POINT ( 'NONE',  ( 9.056254019423489510, -63.50214810053400782, -46.63926694421989794 ) ) ;
#31352=EDGE_LOOP ( 'NONE', ( #25506, #47454, #44407, #31673, #40509 ) ) ;
#31356=CARTESIAN_POINT ( 'NONE',  ( 56.31131641729229642, -50.56001720853080172, -52.86807145390460505 ) ) ;
#31359=CARTESIAN_POINT ( 'NONE',  ( 59.10309117834729875, -3.122143041457199786, -15.65534436044210054 ) ) ;
#31360=CARTESIAN_POINT ( 'NONE',  ( 51.67588099511449684, -48.69063913976710012, -77.01364301606309937 ) ) ;
#31361=CARTESIAN_POINT ( 'NONE',  ( 13.96299814188780175, -52.23919279717198094, -75.65449996341371275 ) ) ;
#31362=ORIENTED_EDGE ( 'NONE', *, *, #46395, .T. ) ;
#31363=CARTESIAN_POINT ( 'NONE',  ( -7.894031745507627207, -33.07353038881739593, 7.944363289481099599 ) ) ;
#31364=FACE_OUTER_BOUND ( 'NONE', #32562, .T. ) ;
#31365=DIRECTION ( 'NONE',  ( 1.000000000000000000, 0.000000000000000000, 0.000000000000000000 ) ) ;
#31367=AXIS2_PLACEMENT_3D ( 'NONE', #49808, #10234, #18336 ) ;
#31369=EDGE_CURVE ( 'NONE', #32627, #31681, #6304, .T. ) ;
#31370=CARTESIAN_POINT ( 'NONE',  ( 13.33362440043809904, -50.59907500154410087, -21.35584257635559879 ) ) ;
#31371=CARTESIAN_POINT ( 'NONE',  ( 57.14246561268299729, 19.38381105532069881, -74.67211522426370607 ) ) ;
#31374=CARTESIAN_POINT ( 'NONE',  ( 56.58040397675829780, 14.03809001566030012, -16.97035855063799659 ) ) ;
#31375=CARTESIAN_POINT ( 'NONE',  ( 60.96921016464919774, -45.39643253083639962, -46.92502502242910367 ) ) ;
#31376=CARTESIAN_POINT ( 'NONE',  ( 56.74347696462359636, -50.41867359881469923, -52.86071028780529701 ) ) ;
#31384=CARTESIAN_POINT ( 'NONE',  ( 17.85630073056284672, 20.07361857726406384, -75.01676221294343350 ) ) ;
#31385=CARTESIAN_POINT ( 'NONE',  ( 56.12351168987260763, 13.88381105532070059, -10.09719779148739960 ) ) ;
#31387=EDGE_CURVE ( 'NONE', #17917, #14173, #463, .T. ) ;
#31388=CARTESIAN_POINT ( 'NONE',  ( 11.01613591017130034, 33.93391017002509358, -18.04558894928910107 ) ) ;
#31389=CARTESIAN_POINT ( 'NONE',  ( 61.75019796695539753, 14.88381105532069881, -46.37203261889099792 ) ) ;
#31390=CARTESIAN_POINT ( 'NONE',  ( 53.57529076486616049, 19.31354156546077405, -77.11805887586452002 ) ) ;
#31392=AXIS2_PLACEMENT_3D ( 'NONE', #47788, #2991, #27342 ) ;
#31393=EDGE_CURVE ( 'NONE', #3425, #29321, #17941, .T. ) ;
#31394=CARTESIAN_POINT ( 'NONE',  ( 14.74660166870041955, -52.24942673173599417, -75.96019247805895702 ) ) ;
#31395=CARTESIAN_POINT ( 'NONE',  ( 49.21269661613270330, 22.37820248916990096, -54.26152208607290106 ) ) ;
#31396=ORIENTED_EDGE ( 'NONE', *, *, #51417, .T. ) ;
#31397=CARTESIAN_POINT ( 'NONE',  ( 52.68346768350169640, -49.76694581559849695, -48.72606083504529551 ) ) ;
#31398=ORIENTED_EDGE ( 'NONE', *, *, #46935, .T. ) ;
#31405=CARTESIAN_POINT ( 'NONE',  ( 55.13249787720189943, -46.09229425796829815, -16.25834332036090046 ) ) ;
#31406=DIRECTION ( 'NONE',  ( 0.6668512999106339656, 0.3436531272335545117, -0.6612199875609449107 ) ) ;
#31410=CARTESIAN_POINT ( 'NONE',  ( 11.78860069758130003, -65.42274227350759475, -17.85348597566460072 ) ) ;
#31411=CARTESIAN_POINT ( 'NONE',  ( 11.71414166034919901, 34.09778695716270391, -47.42034454235100327 ) ) ;
#31413=DIRECTION ( 'NONE',  ( 0.000000000000000000, 1.000000000000000000, 0.000000000000000000 ) ) ;
#31417=CARTESIAN_POINT ( 'NONE',  ( 57.24929578595760660, 19.38381105532069881, -74.14999999999999147 ) ) ;
#31419=CARTESIAN_POINT ( 'NONE',  ( 11.10530294771309912, -63.11543068638779630, -44.25053028539870326 ) ) ;
#31420=CARTESIAN_POINT ( 'NONE',  ( 70.83393739769690001, 16.88381105531960458, -68.79999999999942872 ) ) ;
#31423=CARTESIAN_POINT ( 'NONE',  ( 56.62412426277949606, 19.48324289140059662, -53.71767670195740152 ) ) ;
#31425=ORIENTED_EDGE ( 'NONE', *, *, #23825, .T. ) ;
#31427=CARTESIAN_POINT ( 'NONE',  ( 0.5406133260286609676, 12.32747302715160131, -21.14999999999999858 ) ) ;
#31429=CARTESIAN_POINT ( 'NONE',  ( 57.26283657379369885, -50.61618895537380070, -53.75815476539319349 ) ) ;
#31440=DIRECTION ( 'NONE',  ( -0.4412403921323043154, 0.5329539830277481016, -0.7219882051154223879 ) ) ;
#31442=CARTESIAN_POINT ( 'NONE',  ( 46.73672019546049938, 22.47805634369839822, -75.96172454647880556 ) ) ;
#31446=CARTESIAN_POINT ( 'NONE',  ( 41.80336364839079266, -44.88664980482889888, -5.672379628686790021 ) ) ;
#31447=CARTESIAN_POINT ( 'NONE',  ( 12.04070883443819895, 33.58235188910439462, -16.10368401051540133 ) ) ;
#31448=VECTOR ( 'NONE', #24032, 1000.000000000000000 ) ;
#31451=CARTESIAN_POINT ( 'NONE',  ( 54.34775236769140605, -47.86158002624129892, -25.94360105443890063 ) ) ;
#31452=AXIS2_PLACEMENT_3D ( 'NONE', #9897, #18015, #25853 ) ;
#31453=CARTESIAN_POINT ( 'NONE',  ( 56.90586760780780651, -50.64480473018880247, -74.36144200333770016 ) ) ;
#31454=CARTESIAN_POINT ( 'NONE',  ( 0.06538248623146999949, 21.54194279676389812, -7.555612708363120156 ) ) ;
#31458=FACE_OUTER_BOUND ( 'NONE', #11980, .T. ) ;
#31460=CARTESIAN_POINT ( 'NONE',  ( 53.18570859912749427, -49.47442707985450028, -48.81732526230189961 ) ) ;
#31461=CARTESIAN_POINT ( 'NONE',  ( 47.55693705089040435, 23.33414435787860342, -54.87298417455060218 ) ) ;
#31462=CARTESIAN_POINT ( 'NONE',  ( 61.26565493546950592, -45.23349057862129996, -27.96003281282710162 ) ) ;
#31464=CARTESIAN_POINT ( 'NONE',  ( 61.58449942664206844, -45.28981909799563255, -47.18862349895694308 ) ) ;
#31466=CARTESIAN_POINT ( 'NONE',  ( 51.08267997340979605, 17.48509555023420248, -76.44192736852110670 ) ) ;
#31467=CARTESIAN_POINT ( 'NONE',  ( 52.81743982411089888, 18.43499551991449792, -48.47378032971769812 ) ) ;
#31469=CARTESIAN_POINT ( 'NONE',  ( 53.11114670112049652, -49.51349214730240078, -48.80212167156650338 ) ) ;
#31470=CARTESIAN_POINT ( 'NONE',  ( 50.27626388677308000, 5.227946323752799884, -76.15207597994086086 ) ) ;
#31472=CARTESIAN_POINT ( 'NONE',  ( 53.88536905793235121, -48.73596811206648738, -27.04541679508261254 ) ) ;
#31474=CARTESIAN_POINT ( 'NONE',  ( 59.50660854669460065, -29.52284063487349997, -15.84052005884069914 ) ) ;
#31476=DIRECTION ( 'NONE',  ( -0.4316160343590924597, 0.9020574254913767964, 0.000000000000000000 ) ) ;
#31478=AXIS2_PLACEMENT_3D ( 'NONE', #11469, #23987, #27423 ) ;
#31479=CARTESIAN_POINT ( 'NONE',  ( 51.29176893202588872, -34.69240276036310888, -76.59668289401075469 ) ) ;
#31480=CARTESIAN_POINT ( 'NONE',  ( 43.91474985151640453, 12.31375205243809923, -5.093415854581109237 ) ) ;
#31482=ORIENTED_EDGE ( 'NONE', *, *, #50483, .F. ) ;
#31483=CARTESIAN_POINT ( 'NONE',  ( 40.64814283787870153, 13.41987867678509971, -4.018323132419280519 ) ) ;
#31486=CARTESIAN_POINT ( 'NONE',  ( 55.85894235177089939, -45.98179482937800344, -25.33296393815039949 ) ) ;
#31488=FACE_BOUND ( 'NONE', #26149, .T. ) ;
#31489=EDGE_LOOP ( 'NONE', ( #42617, #16297, #43988, #23810 ) ) ;
#31493=DIRECTION ( 'NONE',  ( 0.000000000000000000, 0.000000000000000000, 1.000000000000000000 ) ) ;
#31497=DIRECTION ( 'NONE',  ( -1.000000000000000000, 0.000000000000000000, 0.000000000000000000 ) ) ;
#31498=DIRECTION ( 'NONE',  ( 0.000000000000000000, -1.000000000000000000, 0.000000000000000000 ) ) ;
#31501=EDGE_CURVE ( 'NONE', #17172, #45555, #44750, .T. ) ;
#31502=CARTESIAN_POINT ( 'NONE',  ( 59.32541119420320541, -28.11267854137589595, -15.67734865989629789 ) ) ;
#31503=EDGE_CURVE ( 'NONE', #9786, #36317, #21866, .T. ) ;
#31505=CARTESIAN_POINT ( 'NONE',  ( 46.65019242837639979, -53.38344801646140070, -76.07596939981860373 ) ) ;
#31508=CARTESIAN_POINT ( 'NONE',  ( 41.75078909917250058, 14.43727496473849925, -6.577246330791240325 ) ) ;
#31510=CARTESIAN_POINT ( 'NONE',  ( 15.05440318628110141, 21.88381105532300097, -76.14999999999999147 ) ) ;
#31511=CARTESIAN_POINT ( 'NONE',  ( 83.25229294592290330, -45.14839585538909716, -47.26064541804080221 ) ) ;
#31512=CIRCLE ( 'NONE', #29830, 1.999999999999998668 ) ;
#31514=CARTESIAN_POINT ( 'NONE',  ( 65.41765814209475138, -30.18662511381366187, -16.56748189521639247 ) ) ;
#31517=CARTESIAN_POINT ( 'NONE',  ( 53.00356549828499908, -49.51115989585530741, -27.69254757381720111 ) ) ;
#31518=CARTESIAN_POINT ( 'NONE',  ( 16.22100018021849976, -51.07051512547269567, -20.14984494908150126 ) ) ;
#31519=CARTESIAN_POINT ( 'NONE',  ( 75.07324054225550469, -8.405693818634281556, -11.43558758117930019 ) ) ;
#31521=EDGE_CURVE ( 'NONE', #47619, #12694, #19629, .T. ) ;
#31526=DIRECTION ( 'NONE',  ( -0.2260571801428161165, -2.775557561562891043E-17, 0.9741140340359943917 ) ) ;
#31527=CARTESIAN_POINT ( 'NONE',  ( 82.31238480745950881, -45.35763125051939681, -47.32928030304829292 ) ) ;
#31528=CARTESIAN_POINT ( 'NONE',  ( 57.35780229286250176, -50.16949399769480067, -52.65865520802150002 ) ) ;
#31529=CARTESIAN_POINT ( 'NONE',  ( 41.49029383318099917, 13.34306788730399873, -5.136314537161009497 ) ) ;
#31530=CARTESIAN_POINT ( 'NONE',  ( 47.63732207932127238, -54.52964753594648784, -74.36335264234261899 ) ) ;
#31532=CARTESIAN_POINT ( 'NONE',  ( 54.20043578388980166, -48.94278307704079367, -48.51842787370119936 ) ) ;
#31534=CARTESIAN_POINT ( 'NONE',  ( 68.16055449185739690, -0.9007378807446890789, -18.00106518090050045 ) ) ;
#31535=CARTESIAN_POINT ( 'NONE',  ( 18.12345004666019932, -52.06054985064280061, -75.71157996061791096 ) ) ;
#31536=CARTESIAN_POINT ( 'NONE',  ( 51.54415332628170177, -52.59067900109340599, -53.64346124582210251 ) ) ;
#31539=CARTESIAN_POINT ( 'NONE',  ( 56.51051770571049815, -45.90816165454779707, -45.01386504879189943 ) ) ;
#31544=DIRECTION ( 'NONE',  ( 0.000000000000000000, 1.000000000000000000, 0.000000000000000000 ) ) ;
#31547=VERTEX_POINT ( 'NONE', #34220 ) ;
#31548=CARTESIAN_POINT ( 'NONE',  ( 17.69970719370899914, 21.04130707244170040, -75.96082109999758814 ) ) ;
#31549=VERTEX_POINT ( 'NONE', #9881 ) ;
#31553=CARTESIAN_POINT ( 'NONE',  ( 61.58777976395109732, 14.02680365743669988, -47.11785714435669803 ) ) ;
#31554=VERTEX_POINT ( 'NONE', #1505 ) ;
#31555=CARTESIAN_POINT ( 'NONE',  ( 63.88393739769619373, 4.883811055320659733, -61.34712802272770915 ) ) ;
#31556=ORIENTED_EDGE ( 'NONE', *, *, #19502, .F. ) ;
#31557=DIRECTION ( 'NONE',  ( -0.2720339695306771000, 0.4031695913578095536, 0.8737572889686010535 ) ) ;
#31562=CARTESIAN_POINT ( 'NONE',  ( 59.34499803081109803, -28.11618894467929763, -15.68015151901639825 ) ) ;
#31563=CARTESIAN_POINT ( 'NONE',  ( 52.20740540343859237, -51.40483972235690402, -75.93239679552310406 ) ) ;
#31564=CARTESIAN_POINT ( 'NONE',  ( 61.19258921585740296, 14.32575781460780107, -47.61960278887369924 ) ) ;
#31565=AXIS2_PLACEMENT_3D ( 'NONE', #5410, #25809, #13538 ) ;
#31568=CARTESIAN_POINT ( 'NONE',  ( 42.93197233849409855, -42.55807683903029925, -3.187564294433600232 ) ) ;
#31569=CARTESIAN_POINT ( 'NONE',  ( -3.954343448002319850, 17.15822905836070333, -5.572179413950920868 ) ) ;
#31576=EDGE_CURVE ( 'NONE', #2407, #42744, #20075, .T. ) ;
#31578=CARTESIAN_POINT ( 'NONE',  ( 15.54393737248530094, 19.58453728325200061, -20.39348321914659934 ) ) ;
#31579=CYLINDRICAL_SURFACE ( 'NONE', #46515, 1.999999999999970246 ) ;
#31581=CARTESIAN_POINT ( 'NONE',  ( 48.66936276473360579, -53.96730371771859325, -54.61968686218679636 ) ) ;
#31585=CARTESIAN_POINT ( 'NONE',  ( 47.67338561975220301, 23.28889910737600033, -55.14318275608980002 ) ) ;
#31589=ORIENTED_EDGE ( 'NONE', *, *, #31656, .T. ) ;
#31591=CARTESIAN_POINT ( 'NONE',  ( 60.28833275760250388, -45.75485330741069845, -47.30217035591910246 ) ) ;
#31592=CARTESIAN_POINT ( 'NONE',  ( 48.29537619369078527, -54.13523159705017207, -54.65524445810790866 ) ) ;
#31594=CARTESIAN_POINT ( 'NONE',  ( 82.62219371776291155, 13.83471874997871964, -46.37145547400888290 ) ) ;
#31595=DIRECTION ( 'NONE',  ( -1.180619220495489865E-10, 8.141548257237140630E-09, 1.000000000000000000 ) ) ;
#31597=EDGE_CURVE ( 'NONE', #9855, #13869, #28738, .T. ) ;
#31605=EDGE_LOOP ( 'NONE', ( #16819, #9222, #32247, #24309, #32943 ) ) ;
#31609=CARTESIAN_POINT ( 'NONE',  ( 8.835310923510441228, -63.39783216344699213, -46.67672964034989747 ) ) ;
#31613=CARTESIAN_POINT ( 'NONE',  ( 56.51188083447159727, -50.74428706468020067, -53.61551639950389614 ) ) ;
#31615=CARTESIAN_POINT ( 'NONE',  ( 58.98154412302919525, -3.123513370137979805, -15.65041568119880289 ) ) ;
#31616=CARTESIAN_POINT ( 'NONE',  ( 51.99246080072099829, -50.02585771624480060, -76.70334503327950415 ) ) ;
#31617=CARTESIAN_POINT ( 'NONE',  ( 13.88455093916192951, -52.17615671833033275, -75.56421372420085447 ) ) ;
#31619=EDGE_LOOP ( 'NONE', ( #3087, #36843 ) ) ;
#31624=EDGE_CURVE ( 'NONE', #42867, #39634, #49475, .T. ) ;
#31626=CARTESIAN_POINT ( 'NONE',  ( 13.58580407945710000, -50.38962722024810148, -21.11665590476469845 ) ) ;
#31627=CARTESIAN_POINT ( 'NONE',  ( 55.77509494401380152, 19.38954758360430120, -76.00676941660189812 ) ) ;
#31628=CARTESIAN_POINT ( 'NONE',  ( 62.09157612670949788, 4.883811055320659733, -65.34607522167520699 ) ) ;
#31629=CARTESIAN_POINT ( 'NONE',  ( 10.61752692138360032, -64.82564047392860118, -18.17418372802830007 ) ) ;
#31630=CARTESIAN_POINT ( 'NONE',  ( 60.92599963243960559, -45.60351086516099883, -47.62103043570899530 ) ) ;
#31632=CIRCLE ( 'NONE', #9067, 21.50000000000000000 ) ;
#31634=CARTESIAN_POINT ( 'NONE',  ( 49.72648160330989953, 22.41435850158119791, -55.11972614036179863 ) ) ;
#31636=CARTESIAN_POINT ( 'NONE',  ( 47.41053033963120100, 23.00881195654629607, -75.29848680172570141 ) ) ;
#31638=CARTESIAN_POINT ( 'NONE',  ( 41.74231633223259763, -45.72926218777020324, -6.615723881723910793 ) ) ;
#31640=CARTESIAN_POINT ( 'NONE',  ( 14.27688375769564999, -50.38989777066024800, -20.83437850749841047 ) ) ;
#31642=CARTESIAN_POINT ( 'NONE',  ( 10.63085818559157048, -64.83909131530428738, -18.12438161376036660 ) ) ;
#31643=CARTESIAN_POINT ( 'NONE',  ( 11.89948726635009812, 34.20418277686660247, -18.06739951299479685 ) ) ;
#31648=CARTESIAN_POINT ( 'NONE',  ( 49.00556831830410687, 22.49847617784580223, -54.36652964084350259 ) ) ;
#31649=VERTEX_POINT ( 'NONE', #22429 ) ;
#31650=CARTESIAN_POINT ( 'NONE',  ( 53.24077194809640190, -49.47968887696829654, -49.04425631192140145 ) ) ;
#31651=ORIENTED_EDGE ( 'NONE', *, *, #2309, .T. ) ;
#31655=CARTESIAN_POINT ( 'NONE',  ( 84.22671941158239406, 12.55804992541220066, -46.99905560746370270 ) ) ;
#31656=EDGE_CURVE ( 'NONE', #45923, #51745, #40143, .T. ) ;
#31658=CARTESIAN_POINT ( 'NONE',  ( 52.64726118030579727, 18.56190800186159962, -48.69235233590459444 ) ) ;
#31659=CARTESIAN_POINT ( 'NONE',  ( 56.48065915063589415, -45.38274434046520156, -17.55965706255600267 ) ) ;
#31661=ORIENTED_EDGE ( 'NONE', *, *, #18197, .F. ) ;
#31663=ORIENTED_EDGE ( 'NONE', *, *, #453, .F. ) ;
#31665=CARTESIAN_POINT ( 'NONE',  ( 11.96242383438930013, -65.43598681641390158, -17.67418089159339800 ) ) ;
#31666=CARTESIAN_POINT ( 'NONE',  ( 10.84460789103059852, 32.90608426506580031, -45.64388948703140159 ) ) ;
#31669=CARTESIAN_POINT ( 'NONE',  ( 8.792634198315560923, 31.92357537073090157, -46.67064936031920297 ) ) ;
#31671=AXIS2_PLACEMENT_3D ( 'NONE', #36595, #13290, #697 ) ;
#31672=AXIS2_PLACEMENT_3D ( 'NONE', #45888, #9975, #25937 ) ;
#31673=ORIENTED_EDGE ( 'NONE', *, *, #27565, .F. ) ;
#31675=CARTESIAN_POINT ( 'NONE',  ( 11.10570106179580030, -63.43849378863360045, -44.25865445854999791 ) ) ;
#31676=CARTESIAN_POINT ( 'NONE',  ( 70.83393739769690001, 16.88381105531749782, -71.50000000000000000 ) ) ;
#31677=ORIENTED_EDGE ( 'NONE', *, *, #4399, .T. ) ;
#31678=CARTESIAN_POINT ( 'NONE',  ( 67.09900444977570544, -33.06551488220966917, -20.08988936614202103 ) ) ;
#31679=CARTESIAN_POINT ( 'NONE',  ( 56.53399784873889899, 19.21501630139210093, -52.81205167924800037 ) ) ;
#31680=CARTESIAN_POINT ( 'NONE',  ( 31.69621505786460247, -15.61618894467929763, -6.649999999999999467 ) ) ;
#31681=VERTEX_POINT ( 'NONE', #45533 ) ;
#31684=CARTESIAN_POINT ( 'NONE',  ( 57.35856957771729725, -50.13596282240779800, -52.61941485477820635 ) ) ;
#31685=FACE_OUTER_BOUND ( 'NONE', #45327, .T. ) ;
#31690=VERTEX_POINT ( 'NONE', #26622 ) ;
#31695=CARTESIAN_POINT ( 'NONE',  ( 47.04916798185949744, 22.99805076571630025, -75.51723258725729693 ) ) ;
#31696=FACE_OUTER_BOUND ( 'NONE', #18073, .T. ) ;
#31703=CARTESIAN_POINT ( 'NONE',  ( 56.57655762862680149, -50.65586698240579722, -74.96720691208240339 ) ) ;
#31704=CARTESIAN_POINT ( 'NONE',  ( -4.807165379747050160, 16.23227173892630049, -5.209035753736800167 ) ) ;
#31706=AXIS2_PLACEMENT_3D ( 'NONE', #30707, #46729, #10813 ) ;
#31708=CARTESIAN_POINT ( 'NONE',  ( 61.39380661293360220, 13.96359161412859962, -46.71089551414399921 ) ) ;
#31709=CYLINDRICAL_SURFACE ( 'NONE', #28084, 3.000000000000000444 ) ;
#31711=CARTESIAN_POINT ( 'NONE',  ( 53.36905185836059928, -49.37836840941449168, -48.78905575734700051 ) ) ;
#31712=CARTESIAN_POINT ( 'NONE',  ( 61.30987170295029642, -45.21799793180310445, -28.05306858404509995 ) ) ;
#31714=CARTESIAN_POINT ( 'NONE',  ( 56.53685690055910129, 14.99694011007190220, -26.26932896201929779 ) ) ;
#31716=CARTESIAN_POINT ( 'NONE',  ( 51.50420584715260475, 18.17752645460259942, -76.63112831200879782 ) ) ;
#31717=CARTESIAN_POINT ( 'NONE',  ( 52.78519658503790168, 18.45700756790349928, -48.68757693859610214 ) ) ;
#31718=DIRECTION ( 'NONE',  ( 1.000000000000000000, 0.000000000000000000, 0.000000000000000000 ) ) ;
#31719=CARTESIAN_POINT ( 'NONE',  ( 53.20760851556250515, -49.46295310004039436, -48.79936141347000245 ) ) ;
#31723=CARTESIAN_POINT ( 'NONE',  ( 47.60135642093380426, -54.55175135494879868, -55.04890805189040037 ) ) ;
#31726=CARTESIAN_POINT ( 'NONE',  ( 65.07885343532089450, -32.17484660787989981, -17.72663174665169805 ) ) ;
#31730=FACE_BOUND ( 'NONE', #20636, .T. ) ;
#31740=AXIS2_PLACEMENT_3D ( 'NONE', #11452, #7255, #27409 ) ;
#31741=ADVANCED_FACE ( 'NONE', ( #19545 ), #7766, .F. ) ;
#31744=CARTESIAN_POINT ( 'NONE',  ( 11.40398156086318160, 34.03074001837894969, -22.75443495787784798 ) ) ;
#31745=AXIS2_PLACEMENT_3D ( 'NONE', #14969, #6863, #7632 ) ;
#31747=FACE_OUTER_BOUND ( 'NONE', #32762, .T. ) ;
#31748=AXIS2_PLACEMENT_3D ( 'NONE', #40382, #24628, #33015 ) ;
#31750=ADVANCED_FACE ( 'NONE', ( #51011 ), #18881, .T. ) ;
#31753=AXIS2_PLACEMENT_3D ( 'NONE', #21353, #8549, #668 ) ;
#31757=CARTESIAN_POINT ( 'NONE',  ( 64.07783773375270187, -29.99138570131350434, -16.37128087021990197 ) ) ;
#31762=CARTESIAN_POINT ( 'NONE',  ( 45.28528579602679116, 14.15028987964289975, -8.309926139390320543 ) ) ;
#31763=CARTESIAN_POINT ( 'NONE',  ( 14.90280646933509878, 21.76199957607230218, -76.14999999999999147 ) ) ;
#31764=CARTESIAN_POINT ( 'NONE',  ( 83.62075525755088279, -44.78170833223440184, -47.10035895585609467 ) ) ;
#31768=CARTESIAN_POINT ( 'NONE',  ( 53.59175609322679890, -48.99677226645609096, -27.20769021208899829 ) ) ;
#31769=CARTESIAN_POINT ( 'NONE',  ( 11.13902037554059987, -63.56347337547460796, -14.91063010085480123 ) ) ;
#31775=ORIENTED_EDGE ( 'NONE', *, *, #25820, .T. ) ;
#31778=CIRCLE ( 'NONE', #43526, 2.700000000000230216 ) ;
#31779=CARTESIAN_POINT ( 'NONE',  ( 47.18324198357279897, 23.57489020266570279, -54.61058319554400242 ) ) ;
#31783=CARTESIAN_POINT ( 'NONE',  ( 57.47779638733530305, -50.55916219015709601, -53.44452029295939610 ) ) ;
#31784=CARTESIAN_POINT ( 'NONE',  ( 43.31938993097590185, 11.95891240614390050, -4.740111887263790180 ) ) ;
#31787=DIRECTION ( 'NONE',  ( -2.565320000000000120E-13, 1.000000000000000000, -8.628712999999999808E-13 ) ) ;
#31793=LINE ( 'NONE', #14343, #48853 ) ;
#31802=CARTESIAN_POINT ( 'NONE',  ( 17.21347160910339724, 21.88381105532300097, -76.14999999999999147 ) ) ;
#31805=CARTESIAN_POINT ( 'NONE',  ( 56.82261506997360101, -46.00315760091039152, -26.24626569297650036 ) ) ;
#31809=ORIENTED_EDGE ( 'NONE', *, *, #26051, .F. ) ;
#31810=CARTESIAN_POINT ( 'NONE',  ( 61.31807987960689843, -45.64188066342459393, -47.72348187499480332 ) ) ;
#31811=VERTEX_POINT ( 'NONE', #3497 ) ;
#31812=CARTESIAN_POINT ( 'NONE',  ( 11.26605718498006681, -64.23738894431306790, -24.07455686696101438 ) ) ;
#31813=EDGE_CURVE ( 'NONE', #31549, #47622, #42505, .T. ) ;
#31814=CARTESIAN_POINT ( 'NONE',  ( 59.43561021697854585, -45.50358387466955179, -26.70526119467472981 ) ) ;
#31816=AXIS2_PLACEMENT_3D ( 'NONE', #34912, #64, #31226 ) ;
#31817=EDGE_LOOP ( 'NONE', ( #26138, #51642, #22203, #21170 ) ) ;
#31819=FACE_OUTER_BOUND ( 'NONE', #17904, .T. ) ;
#31821=CARTESIAN_POINT ( 'NONE',  ( 61.07324514817819505, 14.25386249272230010, -47.46813279917520134 ) ) ;
#31822=AXIS2_PLACEMENT_3D ( 'NONE', #50605, #7107, #22799 ) ;
#31825=CARTESIAN_POINT ( 'NONE',  ( -7.968494235580870111, 13.83148165310410072, -5.506078144787959872 ) ) ;
#31826=CARTESIAN_POINT ( 'NONE',  ( 17.92370450339619836, 20.88381105532299742, -74.14999999999999147 ) ) ;
#31827=CARTESIAN_POINT ( 'NONE',  ( 58.53215119733189908, 14.40509552366270007, -26.46582177025860005 ) ) ;
#31831=CARTESIAN_POINT ( 'NONE',  ( 41.03169806305130152, 14.25711695494940123, -6.001447860943059709 ) ) ;
#31832=CARTESIAN_POINT ( 'NONE',  ( -5.066062602303800233, -15.61618894467930119, -12.65000000000000036 ) ) ;
#31835=CARTESIAN_POINT ( 'NONE',  ( 46.35275103504449845, -52.90993241930539881, -76.14999999999999147 ) ) ;
#31838=CARTESIAN_POINT ( 'NONE',  ( 48.62042966150410450, -53.96634867048729234, -54.57170596908269999 ) ) ;
#31839=CARTESIAN_POINT ( 'NONE',  ( 51.87293486654318286, -32.75009382961766136, -18.77186997386058209 ) ) ;
#31840=ADVANCED_FACE ( 'NONE', ( #4004 ), #19209, .T. ) ;
#31844=CIRCLE ( 'NONE', #8428, 1.999999999999998224 ) ;
#31849=CARTESIAN_POINT ( 'NONE',  ( 18.22265159334490292, 21.07288667571724616, -75.74021525124661025 ) ) ;
#31851=CARTESIAN_POINT ( 'NONE',  ( 60.78493093637079880, -45.56573178202909702, -47.44768458244219289 ) ) ;
#31852=CARTESIAN_POINT ( 'NONE',  ( 37.11786083938510217, -15.61618894467929941, 6.789625226207629538 ) ) ;
#31853=CARTESIAN_POINT ( 'NONE',  ( 7.492845759203720313, 29.94784237631284896, -20.13893727953968948 ) ) ;
#31857=B_SPLINE_CURVE_WITH_KNOTS ( 'NONE', 3,
 ( #17627, #29145, #5321, #33597, #592, #45146, #13449, #45665, #41465, #16577, #5582, #12668, #25719, #49093, #21021, #37020 ),
 .UNSPECIFIED., .F., .F.,
 ( 4, 2, 2, 2, 2, 2, 2, 4 ),
 ( 0.000000000000000000, 2.070511893743590015, 3.936888812047690145, 5.103374385987740069, 5.832427869700280709, 7.290534837125340673, 9.623505985005449404, 11.66485573940060050 ),
 .UNSPECIFIED. ) ;
#31858=EDGE_CURVE ( 'NONE', #28603, #34738, #35600, .T. ) ;
#31861=EDGE_LOOP ( 'NONE', ( #8292, #28962, #39445, #9281, #42085 ) ) ;
#31867=CARTESIAN_POINT ( 'NONE',  ( 76.39112045134315565, -16.55782844447705315, -12.75825074068906240 ) ) ;
#31868=ORIENTED_EDGE ( 'NONE', *, *, #43962, .F. ) ;
#31871=CARTESIAN_POINT ( 'NONE',  ( 56.64799623678120355, -45.30988597762969761, -25.29367807365969867 ) ) ;
#31872=CARTESIAN_POINT ( 'NONE',  ( 56.32100277383929665, -50.57626126597089922, -52.90110794044780107 ) ) ;
#31873=CARTESIAN_POINT ( 'NONE',  ( 60.18087665363530192, -1.847621400935020031, -15.84374030865019733 ) ) ;
#31875=CARTESIAN_POINT ( 'NONE',  ( 51.46000099094769809, -49.32027946797799700, -76.62475863447160407 ) ) ;
#31876=B_SPLINE_SURFACE_WITH_KNOTS ( 'NONE', 3, 3, ( 
 ( #33464, #8864, #32940, #17243, #9887, #25336, #993, #9120, #25844, #36620, #41088, #20632 ),
 ( #29024, #16992, #5200, #37158, #1256, #33206, #49225, #41339, #17496, #13571, #25590, #41595 ),
 ( #14078, #15114, #11190, #2544, #18005, #18778, #33970, #14853, #50503, #41856, #2026, #18257 ),
 ( #31074, #19036, #3065, #30562, #22436, #34753, #30039, #34226, #18525, #35011, #14593, #10152 ) ),
 .UNSPECIFIED., .F., .F., .F.,
 ( 4, 4 ),
 ( 4, 1, 1, 1, 1, 1, 1, 1, 1, 4 ),
 ( -0.1293119798323739966, 3.989325000000000270E-14 ),
 ( 0.000000000000000000, 0.1111111111111110078, 0.2222222222222219878, 0.3333333333333329818, 0.4444444444444439757, 0.5555555555555560243, 0.6666666666666670737, 0.7777777777777779011, 0.8888888888888889506, 1.000000000000000000 ),
 .UNSPECIFIED. ) ;
#31879=CARTESIAN_POINT ( 'NONE',  ( 53.07826439650979466, -50.35436285572949089, -77.22375575988948526 ) ) ;
#31881=CARTESIAN_POINT ( 'NONE',  ( 52.56521993351449851, -49.86179673305689874, -28.15000000000000213 ) ) ;
#31883=CARTESIAN_POINT ( 'NONE',  ( 12.76120696353130057, -49.98606220861660177, -21.08963177777529907 ) ) ;
#31885=CARTESIAN_POINT ( 'NONE',  ( 68.13393739769649926, -48.11618894467630270, -70.54999999999999716 ) ) ;
#31886=CARTESIAN_POINT ( 'NONE',  ( 60.85051643030340074, -45.45861950383179817, -47.01183782209979967 ) ) ;
#31889=VECTOR ( 'NONE', #3744, 1000.000000000000000 ) ;
#31893=CIRCLE ( 'NONE', #8463, 1.999999999999998224 ) ;
#31894=ORIENTED_EDGE ( 'NONE', *, *, #45631, .F. ) ;
#31895=CARTESIAN_POINT ( 'NONE',  ( 13.60550091177310073, -51.43165038652990262, -74.14992922886710858 ) ) ;
#31896=CARTESIAN_POINT ( 'NONE',  ( 47.30522570423300266, -54.71767344092400265, -54.76519543323880157 ) ) ;
#31897=FILL_AREA_STYLE_COLOUR ( '', #23213 ) ;
#31900=CARTESIAN_POINT ( 'NONE',  ( 61.35257968416159713, 13.88381105532070059, -11.49663005730239895 ) ) ;
#31902=CARTESIAN_POINT ( 'NONE',  ( 11.41950678101309968, 34.12481452477189947, -18.15863199430730290 ) ) ;
#31905=CARTESIAN_POINT ( 'NONE',  ( -8.077363885194191795, -45.04970852165219952, -5.734713034113010366 ) ) ;
#31906=CARTESIAN_POINT ( 'NONE',  ( -8.936452451236569061, -44.38145624430249825, -6.564714805037400680 ) ) ;
#31907=CARTESIAN_POINT ( 'NONE',  ( 49.59785998471309654, 22.46914640684560283, -55.11090114299469889 ) ) ;
#31908=ORIENTED_EDGE ( 'NONE', *, *, #41330, .F. ) ;
#31909=CARTESIAN_POINT ( 'NONE',  ( 53.05390111010630250, -49.57533313438899825, -49.03220058437089790 ) ) ;
#31914=CARTESIAN_POINT ( 'NONE',  ( 83.73251846585449698, 13.29777256131780128, -46.86010343433790126 ) ) ;
#31917=EDGE_CURVE ( 'NONE', #28850, #35503, #17999, .T. ) ;
#31918=CARTESIAN_POINT ( 'NONE',  ( 55.95983537943720165, -45.42096113467239604, -16.30775385143880030 ) ) ;
#31919=CARTESIAN_POINT ( 'NONE',  ( 53.08725068471199648, 18.06569830069809868, -26.91751262120149590 ) ) ;
#31923=CARTESIAN_POINT ( 'NONE',  ( 11.92291171973240083, -65.34405718864840651, -17.18421396917739941 ) ) ;
#31924=CARTESIAN_POINT ( 'NONE',  ( 10.89794792890609898, 33.54155821960309680, -46.64989010007410286 ) ) ;
#31928=DIRECTION ( 'NONE',  ( 0.000000000000000000, 1.000000000000000000, 0.000000000000000000 ) ) ;
#31929=CARTESIAN_POINT ( 'NONE',  ( 51.37210604755092191, 3.311019760866724226, -76.66704681122699583 ) ) ;
#31930=CIRCLE ( 'NONE', #16889, 6.049999999999999822 ) ;
#31932=CARTESIAN_POINT ( 'NONE',  ( 11.13393739769620616, 24.07008072128959597, -44.08754088842374586 ) ) ;
#31933=CARTESIAN_POINT ( 'NONE',  ( 11.13393739769619906, -63.11543068638779630, -43.74348518090240390 ) ) ;
#31934=CARTESIAN_POINT ( 'NONE',  ( 68.13393739769706769, 17.98087126524919555, -68.79648330188412331 ) ) ;
#31937=CARTESIAN_POINT ( 'NONE',  ( 56.62432785583700223, 19.48323104976229914, -53.83726655423080132 ) ) ;
#31938=CARTESIAN_POINT ( 'NONE',  ( 65.46029542295769943, -29.76883965895079953, -16.55376543218019947 ) ) ;
#31947=VERTEX_POINT ( 'NONE', #21003 ) ;
#31949=CARTESIAN_POINT ( 'NONE',  ( 52.95053218911250781, -49.64355395051840247, -49.05140896314050281 ) ) ;
#31954=CARTESIAN_POINT ( 'NONE',  ( 46.91913817000130393, 22.75192970925369806, -75.76197391125640479 ) ) ;
#31959=VECTOR ( 'NONE', #36573, 1000.000000000000000 ) ;
#31960=CARTESIAN_POINT ( 'NONE',  ( 12.01222358505770060, 33.78335047254940093, -16.39655052252450318 ) ) ;
#31963=CARTESIAN_POINT ( 'NONE',  ( 56.83675909612700394, -50.64711008564240302, -74.57384771777940102 ) ) ;
#31967=B_SPLINE_CURVE_WITH_KNOTS ( 'NONE', 3,
 ( #43297, #18656, #18910, #18394 ),
 .UNSPECIFIED., .F., .F.,
 ( 4, 4 ),
 ( 0.4993904256265703223, 1.000000000000000000 ),
 .UNSPECIFIED. ) ;
#31968=CARTESIAN_POINT ( 'NONE',  ( 61.46917948669830167, 13.93954126835109975, -46.68479815709330438 ) ) ;
#31972=CARTESIAN_POINT ( 'NONE',  ( 53.30581663188380048, -49.41149911629590008, -48.80307694725580347 ) ) ;
#31973=CARTESIAN_POINT ( 'NONE',  ( 60.31615391617089728, -45.30095148067049848, -26.93200975326800162 ) ) ;
#31975=CARTESIAN_POINT ( 'NONE',  ( 57.36674151108839936, 14.38237697927210057, -26.19522064574950093 ) ) ;
#31977=CARTESIAN_POINT ( 'NONE',  ( 50.83757486290169680, 17.38380788181660108, -76.31330845207050118 ) ) ;
#31978=CARTESIAN_POINT ( 'NONE',  ( 52.98906683290070418, 18.34770546868389829, -48.84983105046850227 ) ) ;
#31979=EDGE_CURVE ( 'NONE', #28709, #26641, #33067, .T. ) ;
#31981=DIRECTION ( 'NONE',  ( 0.2946419978043516297, 0.8205364433225794674, 0.4898020399195900931 ) ) ;
#31984=CARTESIAN_POINT ( 'NONE',  ( 47.63102691442649927, -54.53857517529880283, -55.07721006389790119 ) ) ;
#31987=CARTESIAN_POINT ( 'NONE',  ( 62.21566394024790725, -30.80684386566390032, -16.45443897629299812 ) ) ;
#31992=CARTESIAN_POINT ( 'NONE',  ( 59.94131200797997394, -45.42892869204277417, -26.87338874175082992 ) ) ;
#31997=ORIENTED_EDGE ( 'NONE', *, *, #31979, .F. ) ;
#32002=CARTESIAN_POINT ( 'NONE',  ( 11.39201708760626630, 34.02281520799220971, -22.76707769548407256 ) ) ;
#32007=CARTESIAN_POINT ( 'NONE',  ( 10.69832412674970001, 33.66039914567009816, -17.91220997198119846 ) ) ;
#32008=CARTESIAN_POINT ( 'NONE',  ( 61.68013916707700162, -30.03519813877060329, -16.11687714886729950 ) ) ;
#32011=CARTESIAN_POINT ( 'NONE',  ( 40.88927357473509971, 13.86719357938189923, -5.596100048965730878 ) ) ;
#32012=EDGE_CURVE ( 'NONE', #14545, #4756, #42758, .T. ) ;
#32013=AXIS2_PLACEMENT_3D ( 'NONE', #21590, #38122, #34159 ) ;
#32014=CARTESIAN_POINT ( 'NONE',  ( 14.78004722010049932, 21.61970083732919790, -76.12726769927830617 ) ) ;
#32017=CARTESIAN_POINT ( 'NONE',  ( 84.42999065749789622, -43.29956543148999515, -47.39892822416609874 ) ) ;
#32018=PLANE ( 'NONE',  #25268 ) ;
#32021=CARTESIAN_POINT ( 'NONE',  ( 53.43229558763829345, -49.00751707029830584, -27.03092591272499945 ) ) ;
#32022=CARTESIAN_POINT ( 'NONE',  ( 13.86889551668869913, -50.63824991484180060, -21.27403962367300139 ) ) ;
#32026=CARTESIAN_POINT ( 'NONE',  ( 82.02429831058030629, 10.00628846694210061, -45.87976092105969883 ) ) ;
#32034=CARTESIAN_POINT ( 'NONE',  ( 57.46993325851799739, -50.61178216551700615, -53.76538998729250096 ) ) ;
#32035=CARTESIAN_POINT ( 'NONE',  ( 41.57868469450720283, 13.12802241111150003, -4.871763367457619509 ) ) ;
#32038=CARTESIAN_POINT ( 'NONE',  ( 16.13393739769620083, -15.61618894467929941, -7.139181489322110608 ) ) ;
#32039=CARTESIAN_POINT ( 'NONE',  ( 54.21899510283260071, -48.93305932984999629, -48.60061331225900005 ) ) ;
#32042=CARTESIAN_POINT ( 'NONE',  ( 17.34547572264069970, -52.74444847917729362, -76.12391999848780699 ) ) ;
#32051=ORIENTED_EDGE ( 'NONE', *, *, #41171, .T. ) ;
#32052=CARTESIAN_POINT ( 'NONE',  ( 17.64668853360479872, 20.66382337739360153, -75.74020909530109691 ) ) ;
#32057=CARTESIAN_POINT ( 'NONE',  ( 57.39016325515699180, -45.80620285074159881, -26.27722981911719913 ) ) ;
#32060=FACE_OUTER_BOUND ( 'NONE', #11711, .T. ) ;
#32061=CARTESIAN_POINT ( 'NONE',  ( 75.47966807050509885, 12.14072485751589880, -13.40512917118210012 ) ) ;
#32062=CARTESIAN_POINT ( 'NONE',  ( 12.26481002496320016, -65.46765766720608326, -22.60721059743012873 ) ) ;
#32063=ORIENTED_EDGE ( 'NONE', *, *, #17043, .F. ) ;
#32064=FACE_OUTER_BOUND ( 'NONE', #36594, .T. ) ;
#32066=CARTESIAN_POINT ( 'NONE',  ( 58.98993200268654391, -45.56937796336901414, -26.56610208028315867 ) ) ;
#32070=DIRECTION ( 'NONE',  ( 2.020486089517491233E-31, -1.000000000000000000, 2.054487543405499690E-16 ) ) ;
#32072=DIRECTION ( 'NONE',  ( 0.000000000000000000, 0.000000000000000000, -1.000000000000000000 ) ) ;
#32073=CARTESIAN_POINT ( 'NONE',  ( 60.66741122180980028, 14.45296748104540008, -47.62419456964220643 ) ) ;
#32075=EDGE_CURVE ( 'NONE', #46034, #32635, #51806, .T. ) ;
#32077=CARTESIAN_POINT ( 'NONE',  ( -7.635283139872090175, 14.03913662587130062, -5.082544383023049228 ) ) ;
#32078=CARTESIAN_POINT ( 'NONE',  ( 47.10256183579443245, 23.39255389708953459, -75.00952367219578321 ) ) ;
#32079=CARTESIAN_POINT ( 'NONE',  ( 57.82240384458129512, 14.50996769876100068, -26.33560015361079820 ) ) ;
#32082=CARTESIAN_POINT ( 'NONE',  ( 55.16626882053050451, 17.34692063200439804, -48.76159087390789892 ) ) ;
#32084=CARTESIAN_POINT ( 'NONE',  ( 40.76017233408010298, 14.12870932884110076, -5.740519046195230679 ) ) ;
#32085=CARTESIAN_POINT ( 'NONE',  ( 11.57631367792649968, 33.55102097998219790, -44.87215126223550499 ) ) ;
#32089=CARTESIAN_POINT ( 'NONE',  ( 46.84224516425109641, 22.80152155003670345, -75.76637104849140769 ) ) ;
#32090=CARTESIAN_POINT ( 'NONE',  ( 48.87228429941779950, -54.00865885737479744, -55.18590764587609954 ) ) ;
#32091=CARTESIAN_POINT ( 'NONE',  ( -7.625877374285919608, 14.22289747138790084, -5.682500641286110543 ) ) ;
#32094=EDGE_CURVE ( 'NONE', #11209, #4421, #6994, .T. ) ;
#32096=VERTEX_POINT ( 'NONE', #19910 ) ;
#32099=VERTEX_POINT ( 'NONE', #21191 ) ;
#32100=DIRECTION ( 'NONE',  ( 0.000000000000000000, 0.000000000000000000, -1.000000000000000000 ) ) ;
#32101=CARTESIAN_POINT ( 'NONE',  ( 60.45022673394080215, -45.68032972807930037, -47.34936493783050793 ) ) ;
#32102=DIRECTION ( 'NONE',  ( 0.000000000000000000, 0.000000000000000000, -1.000000000000000000 ) ) ;
#32103=DIRECTION ( 'NONE',  ( 0.000000000000000000, -1.000000000000000000, 0.000000000000000000 ) ) ;
#32105=DIRECTION ( 'NONE',  ( 0.3918900564939547526, 0.9200120562368543364, 0.000000000000000000 ) ) ;
#32106=CARTESIAN_POINT ( 'NONE',  ( 58.91398403652545568, 14.34820724552367288, -26.53092679127404452 ) ) ;
#32109=CARTESIAN_POINT ( 'NONE',  ( 83.07525583555450055, -45.50440358686140030, -47.60489434516649965 ) ) ;
#32111=ORIENTED_EDGE ( 'NONE', *, *, #23765, .F. ) ;
#32113=DIRECTION ( 'NONE',  ( -0.9990957361526744407, 0.000000000000000000, -0.04251717301921301845 ) ) ;
#32114=CARTESIAN_POINT ( 'NONE',  ( 53.23907584153930372, -49.52980310945599740, -49.17816088826820220 ) ) ;
#32116=CARTESIAN_POINT ( 'NONE',  ( 76.39589878011133806, -18.67680352252259013, -12.77887956925968993 ) ) ;
#32117=CARTESIAN_POINT ( 'NONE',  ( 53.02870100497279537, -51.95943102007580450, -53.35088539576909739 ) ) ;
#32122=CARTESIAN_POINT ( 'NONE',  ( 56.44840739252509820, -50.75241255283049924, -53.50789655320240001 ) ) ;
#32124=CARTESIAN_POINT ( 'NONE',  ( 16.13393739769620083, -15.61618894467929941, -8.050000000000000711 ) ) ;
#32129=CARTESIAN_POINT ( 'NONE',  ( 52.84793105771459665, -50.35222278663569284, -76.98160984018271336 ) ) ;
#32133=CARTESIAN_POINT ( 'NONE',  ( 12.69305026481350041, -50.32355431075080077, -21.19712586183110048 ) ) ;
#32134=ADVANCED_FACE ( 'NONE', ( #25118 ), #24857, .F. ) ;
#32136=CARTESIAN_POINT ( 'NONE',  ( 18.68046040379451611, -51.42830650673013082, -15.73013301310943035 ) ) ;
#32137=CARTESIAN_POINT ( 'NONE',  ( 55.55363803660430477, 13.88381105532070059, -14.32024155674050014 ) ) ;
#32138=CARTESIAN_POINT ( 'NONE',  ( 61.12445724983340511, -45.77187651496940646, -47.85281658922149717 ) ) ;
#32143=CARTESIAN_POINT ( 'NONE',  ( 17.52097594613490728, -52.86909450412152722, -76.12392058102736314 ) ) ;
#32147=CARTESIAN_POINT ( 'NONE',  ( 47.34065738921189848, -54.69081672572639974, -54.67801390606140188 ) ) ;
#32148=FILL_AREA_STYLE ('',( #31897 ) ) ;
#32151=CARTESIAN_POINT ( 'NONE',  ( 60.83133137330749918, -45.46867109277970087, -47.01992810568810199 ) ) ;
#32154=CARTESIAN_POINT ( 'NONE',  ( 10.72852875961880059, 33.70931783810110005, -18.17421237878960127 ) ) ;
#32155=CIRCLE ( 'NONE', #39753, 40.00000000000000711 ) ;
#32156=CARTESIAN_POINT ( 'NONE',  ( 47.38034238265840514, 22.97049270074940708, -75.36289877198294107 ) ) ;
#32158=CARTESIAN_POINT ( 'NONE',  ( 10.61752692138360032, -64.82564047392860118, -18.17418372802830007 ) ) ;
#32160=CARTESIAN_POINT ( 'NONE',  ( 48.59256985241970028, 22.83699819754599858, -54.83953650029820182 ) ) ;
#32162=CARTESIAN_POINT ( 'NONE',  ( 53.11153479641689756, -49.53865774820230428, -49.01452490533140605 ) ) ;
#32167=CARTESIAN_POINT ( 'NONE',  ( 84.44784216359251161, 11.88381105532070059, -47.47585302082339354 ) ) ;
#32169=CARTESIAN_POINT ( 'NONE',  ( 52.61151938036640274, 18.58685067986549910, -48.60683035550010089 ) ) ;
#32170=CARTESIAN_POINT ( 'NONE',  ( 55.46022005097690055, -45.45871768700150284, -15.74543532541669855 ) ) ;
#32176=CARTESIAN_POINT ( 'NONE',  ( 11.86319498458860089, -65.39781150395960196, -17.45437997871620084 ) ) ;
#32177=CARTESIAN_POINT ( 'NONE',  ( 10.30800062017689989, 32.11819526227149879, -45.84700176684360429 ) ) ;
#32178=CARTESIAN_POINT ( 'NONE',  ( 18.52830607121394380, 20.08717197157803369, -15.71177323601433429 ) ) ;
#32179=CARTESIAN_POINT ( 'NONE',  ( 47.68700795962210037, -54.63828844795879291, -55.28492161652850001 ) ) ;
#32180=CARTESIAN_POINT ( 'NONE',  ( 8.802044555037090490, 31.97380483823370056, -46.67015369154350424 ) ) ;
#32182=ADVANCED_FACE ( 'NONE', ( #17031 ), #19314, .T. ) ;
#32184=CARTESIAN_POINT ( 'NONE',  ( 10.47385200046668707, 23.98129158042145548, -45.62050397739949403 ) ) ;
#32185=CARTESIAN_POINT ( 'NONE',  ( 11.10561945692110086, -63.36846315954289111, -44.25483350269709604 ) ) ;
#32189=CARTESIAN_POINT ( 'NONE',  ( 50.55910954965799675, -50.23966005774419585, -76.14999999999999147 ) ) ;
#32195=CARTESIAN_POINT ( 'NONE',  ( 56.50924534995709791, 14.67579805743599941, -45.01296638903539815 ) ) ;
#32198=CARTESIAN_POINT ( 'NONE',  ( 83.89200044194980421, 19.24776070067099099, -53.20292136905285929 ) ) ;
#32199=CARTESIAN_POINT ( 'NONE',  ( 55.41789900912189637, 19.74853478895110115, -75.07114006131348560 ) ) ;
#32203=CARTESIAN_POINT ( 'NONE',  ( 53.16292395753290378, -49.55788399721789972, -49.15366685756480081 ) ) ;
#32205=CARTESIAN_POINT ( 'NONE',  ( 12.29949449227315661, 34.10758153282596794, -23.61819227765068163 ) ) ;
#32207=CARTESIAN_POINT ( 'NONE',  ( 47.19475760687539889, 23.42706180971210017, -74.80880246430230329 ) ) ;
#32208=CIRCLE ( 'NONE', #38120, 1.999999999999998224 ) ;
#32213=CARTESIAN_POINT ( 'NONE',  ( 55.02244667203229511, -50.61618557942939844, -76.57012733959869877 ) ) ;
#32217=CARTESIAN_POINT ( 'NONE',  ( 61.43987658220769532, 13.93615501258799938, -46.53628776920029964 ) ) ;
#32219=CYLINDRICAL_SURFACE ( 'NONE', #12199, 50.00000000000000000 ) ;
#32221=CARTESIAN_POINT ( 'NONE',  ( 53.00383630090699683, -49.56971507260659848, -48.79311475622040462 ) ) ;
#32222=CARTESIAN_POINT ( 'NONE',  ( 61.30973436904390184, -45.21801592863619845, -28.15097513424300146 ) ) ;
#32224=CARTESIAN_POINT ( 'NONE',  ( -6.774824244623153469, -32.26037854176222197, 6.072546842075589701 ) ) ;
#32225=CARTESIAN_POINT ( 'NONE',  ( 56.52597820759500280, 14.74085777827989929, -26.17543599240089947 ) ) ;
#32227=CARTESIAN_POINT ( 'NONE',  ( 50.32395455581429644, 18.50520907444330021, -76.14999999999999147 ) ) ;
#32228=CARTESIAN_POINT ( 'NONE',  ( 52.77840648010259628, 18.46069720204630116, -48.67385165654339829 ) ) ;
#32230=CARTESIAN_POINT ( 'NONE',  ( 42.78018059632900361, -42.70905810753740184, -3.187564294433600232 ) ) ;
#32234=CARTESIAN_POINT ( 'NONE',  ( 47.50536557026320139, -54.59832931019789726, -54.95512628287880119 ) ) ;
#32237=CARTESIAN_POINT ( 'NONE',  ( 61.25350246668320153, 14.35920381295040116, -47.66861028105059717 ) ) ;
#32245=EDGE_LOOP ( 'NONE', ( #42247, #25281, #41026, #1924 ) ) ;
#32246=ADVANCED_FACE ( 'NONE', ( #24529 ), #44217, .T. ) ;
#32247=ORIENTED_EDGE ( 'NONE', *, *, #34873, .T. ) ;
#32248=CARTESIAN_POINT ( 'NONE',  ( 14.29753604904800035, -51.11618894467939356, -22.54695280101919863 ) ) ;
#32250=ORIENTED_EDGE ( 'NONE', *, *, #38749, .F. ) ;
#32251=CARTESIAN_POINT ( 'NONE',  ( 12.71291094188550019, -65.48164260791450886, -47.17969016435449703 ) ) ;
#32254=DIRECTION ( 'NONE',  ( 0.000000000000000000, 0.000000000000000000, 1.000000000000000000 ) ) ;
#32261=ORIENTED_EDGE ( 'NONE', *, *, #12918, .F. ) ;
#32262=ADVANCED_FACE ( 'NONE', ( #26346 ), #11377, .T. ) ;
#32266=CARTESIAN_POINT ( 'NONE',  ( 43.99501267352869860, 14.58011966584659902, -8.084181983217140655 ) ) ;
#32269=CARTESIAN_POINT ( 'NONE',  ( 14.64464131216699805, 20.99223335001410007, -75.94942944171690158 ) ) ;
#32271=CARTESIAN_POINT ( 'NONE',  ( 82.78852321480370335, -45.02051732207199564, -46.36931865296660504 ) ) ;
#32275=CARTESIAN_POINT ( 'NONE',  ( 52.77900411135830439, -49.68605478194980662, -28.02809848489370026 ) ) ;
#32276=CARTESIAN_POINT ( 'NONE',  ( 15.00521638035020189, -50.63531778240700021, -20.65446309923529711 ) ) ;
#32282=FACE_OUTER_BOUND ( 'NONE', #35299, .T. ) ;
#32283=CARTESIAN_POINT ( 'NONE',  ( 47.40969209871759915, 23.41413369233859854, -54.72755864828499739 ) ) ;
#32288=CARTESIAN_POINT ( 'NONE',  ( 42.42176422072400044, 12.97522254370229966, -5.045468646584310157 ) ) ;
#32289=CARTESIAN_POINT ( 'NONE',  ( 57.50723795381379944, -45.11618894467940066, -25.33268388717609909 ) ) ;
#32291=DIRECTION ( 'NONE',  ( 0.000000000000000000, 1.000000000000000000, 0.000000000000000000 ) ) ;
#32292=CARTESIAN_POINT ( 'NONE',  ( 57.50472949952089863, -47.23595428949509767, -47.96958150051639791 ) ) ;
#32294=CARTESIAN_POINT ( 'NONE',  ( 67.04038824939736685, -50.70395984888064334, -74.34354914830332461 ) ) ;
#32296=FACE_OUTER_BOUND ( 'NONE', #20327, .T. ) ;
#32298=CARTESIAN_POINT ( 'NONE',  ( 58.73736653739000246, -47.92991618810659560, -50.00877492792809420 ) ) ;
#32299=ORIENTED_EDGE ( 'NONE', *, *, #39411, .T. ) ;
#32301=CARTESIAN_POINT ( 'NONE',  ( 9.726666662871059188, 31.88305279702909800, -46.30264950036470140 ) ) ;
#32303=AXIS2_PLACEMENT_3D ( 'NONE', #50183, #33204, #45019 ) ;
#32306=CARTESIAN_POINT ( 'NONE',  ( 18.11374027727429947, 20.61624280354930150, -75.59143512441710300 ) ) ;
#32310=ORIENTED_EDGE ( 'NONE', *, *, #2011, .T. ) ;
#32311=EDGE_LOOP ( 'NONE', ( #28562, #25538, #48331, #36925 ) ) ;
#32313=CARTESIAN_POINT ( 'NONE',  ( -8.719958794165998839, 10.48190171173589924, -1.467676683391609949 ) ) ;
#32319=EDGE_LOOP ( 'NONE', ( #44785, #30514, #32299, #12143, #38680, #41562 ) ) ;
#32325=CARTESIAN_POINT ( 'NONE',  ( 61.75019796695539753, -45.11618894467940066, -46.37203261889099792 ) ) ;
#32326=CARTESIAN_POINT ( 'NONE',  ( 11.88236613209306825, -65.43512710276252164, -17.91369326119161087 ) ) ;
#32327=CARTESIAN_POINT ( 'NONE',  ( 60.74922417162630239, 14.42261168151119932, -47.61677699820549492 ) ) ;
#32329=EDGE_CURVE ( 'NONE', #6692, #42086, #13185, .T. ) ;
#32330=CARTESIAN_POINT ( 'NONE',  ( 52.07929282054270459, 14.36745883135820101, -13.46056141404780071 ) ) ;
#32331=DIRECTION ( 'NONE',  ( -0.8696770943981948498, -0.4936210606113898836, 1.887379141852609535E-15 ) ) ;
#32332=CARTESIAN_POINT ( 'NONE',  ( -2.623662902638759675, 17.43154064381609913, -4.386168478789810088 ) ) ;
#32335=CARTESIAN_POINT ( 'NONE',  ( 60.16078383215049996, 14.16442556805120034, -26.96501188446990227 ) ) ;
#32339=CARTESIAN_POINT ( 'NONE',  ( 59.66729930240479263, 14.84616221926219914, -47.40987971772899812 ) ) ;
#32341=CARTESIAN_POINT ( 'NONE',  ( 11.96163130544649889, 33.91328095727600811, -45.68067242497239278 ) ) ;
#32345=CARTESIAN_POINT ( 'NONE',  ( 12.52587677871439986, 18.86565027817080065, -21.14436856220130423 ) ) ;
#32346=CARTESIAN_POINT ( 'NONE',  ( 46.64446819860030757, 22.34959245454500021, -76.02856699519020367 ) ) ;
#32347=VECTOR ( 'NONE', #47532, 1000.000000000000000 ) ;
#32348=CARTESIAN_POINT ( 'NONE',  ( 48.55442280000429633, -54.08752141328759677, -54.84940790413600098 ) ) ;
#32349=DIRECTION ( 'NONE',  ( 0.04251717301921600217, 0.000000000000000000, -0.9990957361526742186 ) ) ;
#32356=CARTESIAN_POINT ( 'NONE',  ( 16.13393739769620083, -15.61618894467929941, -10.21818181818179916 ) ) ;
#32357=ORIENTED_EDGE ( 'NONE', *, *, #48211, .T. ) ;
#32359=CARTESIAN_POINT ( 'NONE',  ( 60.70483243996059741, -45.55211676233259510, -47.28445363277229774 ) ) ;
#32361=CARTESIAN_POINT ( 'NONE',  ( 50.20000624151330015, 18.43678156217400144, -76.14999999999999147 ) ) ;
#32367=CARTESIAN_POINT ( 'NONE',  ( 83.70743316420070812, -44.91498932721609805, -47.36488538498209522 ) ) ;
#32370=ORIENTED_EDGE ( 'NONE', *, *, #36012, .F. ) ;
#32371=CARTESIAN_POINT ( 'NONE',  ( 61.48309262502669981, -45.36446491065829889, -47.33735133955730134 ) ) ;
#32372=CARTESIAN_POINT ( 'NONE',  ( 55.91596999402320023, 14.67228162054319895, -25.32543311652580087 ) ) ;
#32373=CARTESIAN_POINT ( 'NONE',  ( 76.39209740234862522, -14.56176142460520317, -12.76245032130310264 ) ) ;
#32374=CARTESIAN_POINT ( 'NONE',  ( 52.70023876989939993, -52.26368731436640047, -53.73525348785970124 ) ) ;
#32376=EDGE_LOOP ( 'NONE', ( #34781, #472, #22001, #47378, #26224 ) ) ;
#32378=CARTESIAN_POINT ( 'NONE',  ( 48.42313109053679909, 22.83113193936399909, -54.61340708730690352 ) ) ;
#32380=CARTESIAN_POINT ( 'NONE',  ( 56.42219321547700162, -50.76386628334259399, -53.51233868223550161 ) ) ;
#32382=CARTESIAN_POINT ( 'NONE',  ( 65.05449253170610291, 1.020160266966620100, -17.84100813038880062 ) ) ;
#32383=VERTEX_POINT ( 'NONE', #45397 ) ;
#32384=CARTESIAN_POINT ( 'NONE',  ( 8.784728771177219286, 31.88305279678909443, -46.67204636144870022 ) ) ;
#32385=CARTESIAN_POINT ( 'NONE',  ( 52.43830835031209858, -49.98684424990290154, -77.15472072683439819 ) ) ;
#32390=CARTESIAN_POINT ( 'NONE',  ( 84.44784216359251161, 11.88381105532070059, -47.47585302082339354 ) ) ;
#32392=CARTESIAN_POINT ( 'NONE',  ( 42.69362901904169405, -43.61869170235599569, -4.694965688641879353 ) ) ;
#32393=CARTESIAN_POINT ( 'NONE',  ( 16.13393739769620083, -15.61618894467929941, -12.65000000000000036 ) ) ;
#32394=CARTESIAN_POINT ( 'NONE',  ( 65.43042069957887463, -49.21324915460321137, -75.95351669811965678 ) ) ;
#32398=CARTESIAN_POINT ( 'NONE',  ( 17.93046645737056011, -52.54004929531408408, -75.96019247805895702 ) ) ;
#32400=CARTESIAN_POINT ( 'NONE',  ( 14.33365608540959890, -52.10138505899109873, -75.81674732426940011 ) ) ;
#32401=CARTESIAN_POINT ( 'NONE',  ( 47.25178503846339595, -54.75397576815099399, -54.62830328906390065 ) ) ;
#32403=DIRECTION ( 'NONE',  ( 0.000000000000000000, 1.000000000000000000, 0.000000000000000000 ) ) ;
#32407=B_SPLINE_CURVE_WITH_KNOTS ( 'NONE', 3,
 ( #11085, #15002, #27052, #48012, #11600, #15776, #43056, #30972, #4237, #31479, #35940, #12111, #3216, #27559, #15269, #16035, #19707, #7405, #36195, #27818 ),
 .UNSPECIFIED., .F., .F.,
 ( 4, 2, 1, 1, 1, 2, 2, 2, 1, 1, 1, 2, 4 ),
 ( 0.5244055620448262456, 0.5318367251378740557, 0.5392678882309219768, 0.5541302144170151545, 0.5838548667892086153, 0.6433041715336005328, 0.7622027810223866995, 0.7696339441154360639, 0.7770651072084853173, 0.7919274333945859334, 0.8216520857667848343, 0.8811013905111874100, 1.000000000000000000 ),
 .UNSPECIFIED. ) ;
#32413=CARTESIAN_POINT ( 'NONE',  ( 48.52740815778420114, 22.81021699678759873, -54.66898914902790096 ) ) ;
#32415=CARTESIAN_POINT ( 'NONE',  ( 52.77947507452280007, -49.70653929005730021, -48.82716071996740226 ) ) ;
#32418=DIRECTION ( 'NONE',  ( -1.000000000000000000, -0.000000000000000000, -0.000000000000000000 ) ) ;
#32420=CARTESIAN_POINT ( 'NONE',  ( 84.25787305080559975, 12.62791954601209987, -47.19072229952409714 ) ) ;
#32421=CARTESIAN_POINT ( 'NONE',  ( 53.90944104900800227, 17.28048702971980077, -26.72631102452049845 ) ) ;
#32423=CARTESIAN_POINT ( 'NONE',  ( 52.59913543871140007, 18.59668918921780190, -48.56922736988880018 ) ) ;
#32424=CARTESIAN_POINT ( 'NONE',  ( 57.04817660294939685, -45.12828403733969651, -16.72517180066030207 ) ) ;
#32425=CARTESIAN_POINT ( 'NONE',  ( 12.06284766121009966, -63.44323389162830296, -22.25048313876769868 ) ) ;
#32426=EDGE_LOOP ( 'NONE', ( #30461, #26999, #42254, #7092 ) ) ;
#32428=VERTEX_POINT ( 'NONE', #19915 ) ;
#32429=CARTESIAN_POINT ( 'NONE',  ( 12.00051660606130177, -65.12476112613200030, -16.59289575486429769 ) ) ;
#32430=CARTESIAN_POINT ( 'NONE',  ( 11.91762376145129743, 34.07103531667779350, -47.17701748307580090 ) ) ;
#32431=CARTESIAN_POINT ( 'NONE',  ( 39.13393739769620083, -15.61618894467929941, -15.65000000000000036 ) ) ;
#32432=CARTESIAN_POINT ( 'NONE',  ( 47.28894142370269549, -54.73349313190560395, -54.78420696420580072 ) ) ;
#32433=CARTESIAN_POINT ( 'NONE',  ( 11.18482555203581441, -65.08283002702597742, -22.98856200317182896 ) ) ;
#32436=CARTESIAN_POINT ( 'NONE',  ( 0.5716597375277996385, -15.61618894467929941, -8.050000000000000711 ) ) ;
#32437=CARTESIAN_POINT ( 'NONE',  ( 11.13393739769619906, -63.16199138576410377, -43.91250325741290084 ) ) ;
#32438=CARTESIAN_POINT ( 'NONE',  ( 47.99879017111000223, 23.44647020611570198, -55.58088518830679448 ) ) ;
#32444=DIRECTION ( 'NONE',  ( -0.2260571801428161165, 1.249000902703300368E-16, 0.9741140340359943917 ) ) ;
#32446=CARTESIAN_POINT ( 'NONE',  ( 53.79693027462740673, 21.85383143305579878, -55.67392376200250226 ) ) ;
#32449=CARTESIAN_POINT ( 'NONE',  ( 53.70843326355630154, 20.08253603804340059, -75.56345715548110320 ) ) ;
#32451=CARTESIAN_POINT ( 'NONE',  ( 47.09661774331770090, -53.91811590987600056, -75.74144252524291687 ) ) ;
#32452=ORIENTED_EDGE ( 'NONE', *, *, #7096, .T. ) ;
#32454=CARTESIAN_POINT ( 'NONE',  ( 53.27415667070290084, -49.51643490155070282, -49.18599851058429806 ) ) ;
#32456=CARTESIAN_POINT ( 'NONE',  ( 47.33320835756340017, 23.23980503609559634, -75.00312280669810150 ) ) ;
#32457=CARTESIAN_POINT ( 'NONE',  ( 19.44419974378226712, -53.43866955709284383, -16.61603860993866633 ) ) ;
#32459=CARTESIAN_POINT ( 'NONE',  ( 12.36320305067610015, 33.31445045643330616, -15.76422791930239953 ) ) ;
#32462=CARTESIAN_POINT ( 'NONE',  ( -10.65907218400529999, 10.01002500177520105, -4.264802379178179947 ) ) ;
#32465=CARTESIAN_POINT ( 'NONE',  ( 61.41767410373359581, 13.94937499305689954, -46.63511954085710443 ) ) ;
#32466=CARTESIAN_POINT ( 'NONE',  ( -18.46117119615139757, -52.29887744895199830, -53.76231701354959824 ) ) ;
#32467=ORIENTED_EDGE ( 'NONE', *, *, #3416, .F. ) ;
#32468=CARTESIAN_POINT ( 'NONE',  ( 53.36494266454960211, -49.38052133118390685, -48.76947209987829979 ) ) ;
#32470=CARTESIAN_POINT ( 'NONE',  ( 58.02351487609760028, -45.11618911064800841, -25.42861971957569622 ) ) ;
#32472=CARTESIAN_POINT ( 'NONE',  ( 13.11803317904709942, 19.67693774826710040, -21.59044394916249843 ) ) ;
#32473=CARTESIAN_POINT ( 'NONE',  ( 56.68398579694790129, 14.78090256954719983, -26.22808307489359692 ) ) ;
#32476=CARTESIAN_POINT ( 'NONE',  ( 51.59928859560229597, 19.10878590974600044, -76.34973321511711220 ) ) ;
#32477=CARTESIAN_POINT ( 'NONE',  ( 52.83452149259679942, 18.43073975597890168, -48.76554741659339953 ) ) ;
#32480=CARTESIAN_POINT ( 'NONE',  ( 75.41292065207370854, -44.30578118641259522, -13.67617913553320186 ) ) ;
#32481=ORIENTED_EDGE ( 'NONE', *, *, #27532, .F. ) ;
#32485=CARTESIAN_POINT ( 'NONE',  ( 47.60675842126480006, -54.53351696772000423, -54.82215150501349399 ) ) ;
#32486=CARTESIAN_POINT ( 'NONE',  ( -5.346827492203339638, 15.73560381608349701, -4.480328059553770004 ) ) ;
#32487=CARTESIAN_POINT ( 'NONE',  ( 40.50275707922880031, 13.54185611314979987, -4.148922232357650230 ) ) ;
#32488=CARTESIAN_POINT ( 'NONE',  ( 56.82230906587010111, 18.91528989288639906, -52.48692337665460173 ) ) ;
#32495=EDGE_CURVE ( 'NONE', #27228, #40081, #29526, .T. ) ;
#32500=CARTESIAN_POINT ( 'NONE',  ( 58.92073396209919878, -28.11618894467929763, -15.65000000000000036 ) ) ;
#32502=CARTESIAN_POINT ( 'NONE',  ( 56.42249722292559966, -45.43314942097339326, -25.29439853946469796 ) ) ;
#32514=CARTESIAN_POINT ( 'NONE',  ( 10.73251648177490125, -64.28497866039579378, -23.50916409409489916 ) ) ;
#32520=CARTESIAN_POINT ( 'NONE',  ( 14.00623127734409934, 20.66741474030959935, -75.53710645103448940 ) ) ;
#32522=CARTESIAN_POINT ( 'NONE',  ( 84.44784216359251161, -43.11618894467930119, -47.47585302082339354 ) ) ;
#32523=CARTESIAN_POINT ( 'NONE',  ( 48.42521416700790127, 25.14253336855949783, -74.14999999999999147 ) ) ;
#32527=CARTESIAN_POINT ( 'NONE',  ( 53.50804305007959982, -48.99566724766310699, -27.12258064042100258 ) ) ;
#32528=CARTESIAN_POINT ( 'NONE',  ( 15.54393737248089913, -50.81691517260839674, -20.39348321914689777 ) ) ;
#32529=CARTESIAN_POINT ( 'NONE',  ( 50.45285235388368505, -36.16382338628016413, -76.19501922796175108 ) ) ;
#32532=ORIENTED_EDGE ( 'NONE', *, *, #17285, .T. ) ;
#32533=CARTESIAN_POINT ( 'NONE',  ( -6.562477110335280805, -46.34503278340989141, -5.556459679399529783 ) ) ;
#32534=CARTESIAN_POINT ( 'NONE',  ( 47.38009481930370015, 23.43661158662580135, -54.80057124748829978 ) ) ;
#32535=DIRECTION ( 'NONE',  ( 0.000000000000000000, -1.000000000000000000, 0.000000000000000000 ) ) ;
#32537=CARTESIAN_POINT ( 'NONE',  ( 54.66073981893745071, 16.79829358645031334, -26.72725689915946745 ) ) ;
#32538=CARTESIAN_POINT ( 'NONE',  ( 11.35626914493999884, 34.06258128150169995, -17.73521909030590038 ) ) ;
#32541=FACE_OUTER_BOUND ( 'NONE', #16670, .T. ) ;
#32542=CARTESIAN_POINT ( 'NONE',  ( 59.86299467440079525, -46.00059797876070178, -47.55238746115900028 ) ) ;
#32547=DIRECTION ( 'NONE',  ( 0.000000000000000000, 1.000000000000000000, 0.000000000000000000 ) ) ;
#32548=AXIS2_PLACEMENT_3D ( 'NONE', #43009, #19137, #35116 ) ;
#32551=CARTESIAN_POINT ( 'NONE',  ( 20.13393739009281447, 24.18330851781475488, -20.36976997827363434 ) ) ;
#32552=CARTESIAN_POINT ( 'NONE',  ( 10.14239080937649895, 31.99922782709920099, -45.99351196094749383 ) ) ;
#32559=ORIENTED_EDGE ( 'NONE', *, *, #51762, .F. ) ;
#32560=CARTESIAN_POINT ( 'NONE',  ( 18.82294826520599784, 20.50885532556510071, -74.53071772762450564 ) ) ;
#32562=EDGE_LOOP ( 'NONE', ( #13787, #50593, #19572, #28437 ) ) ;
#32563=AXIS2_PLACEMENT_3D ( 'NONE', #27303, #11598, #31476 ) ;
#32564=EDGE_LOOP ( 'NONE', ( #10439, #26659, #22777, #19086, #5720, #4729 ) ) ;
#32565=CARTESIAN_POINT ( 'NONE',  ( 12.39616473040790012, -65.41581959449560202, -47.19115183429629923 ) ) ;
#32566=CARTESIAN_POINT ( 'NONE',  ( 57.42036092767180122, -45.80331578673570192, -26.28157325255090271 ) ) ;
#32569=CARTESIAN_POINT ( 'NONE',  ( 61.44894565603249958, 13.98760630883520051, -46.94547993154250065 ) ) ;
#32570=ORIENTED_EDGE ( 'NONE', *, *, #38437, .T. ) ;
#32571=ORIENTED_EDGE ( 'NONE', *, *, #40387, .F. ) ;
#32572=DIRECTION ( 'NONE',  ( 1.000000000000000000, 0.000000000000000000, 0.000000000000000000 ) ) ;
#32574=CARTESIAN_POINT ( 'NONE',  ( 11.14568262985824276, -63.77342232876421946, -24.13735806910611004 ) ) ;
#32579=CYLINDRICAL_SURFACE ( 'NONE', #11624, 3.000000000000000444 ) ;
#32580=DIRECTION ( 'NONE',  ( -2.565320000000000120E-13, -1.000000000000000000, 8.628712999999999808E-13 ) ) ;
#32581=CARTESIAN_POINT ( 'NONE',  ( 61.36407574442390001, 14.34895716591110038, -47.65743212064409562 ) ) ;
#32582=CARTESIAN_POINT ( 'NONE',  ( 52.33303711461739738, 14.99040022374890135, -14.16117149841140055 ) ) ;
#32583=CARTESIAN_POINT ( 'NONE',  ( -3.610905026759430037, 19.17089483124840044, -4.296538310234230273 ) ) ;
#32584=CARTESIAN_POINT ( 'NONE',  ( -6.116815533026069396, 15.22351030921669945, -4.952229201496230360 ) ) ;
#32585=CONICAL_SURFACE ( 'NONE', #1688, 3.118521338338071214, 0.6364736820000767015 ) ;
#32587=CIRCLE ( 'NONE', #50178, 1.500000000000001332 ) ;
#32589=CARTESIAN_POINT ( 'NONE',  ( 55.65312842910222457, 14.73492698990839322, -16.92919021100515309 ) ) ;
#32590=EDGE_CURVE ( 'NONE', #38460, #49655, #24920, .T. ) ;
#32593=B_SPLINE_SURFACE_WITH_KNOTS ( 'NONE', 3, 3, ( 
 ( #1567, #17558, #47160, #51077 ),
 ( #15175, #26956, #26430, #26684 ),
 ( #2867, #3127, #19096, #46905 ),
 ( #50821, #31132, #30106, #22756 ),
 ( #11248, #35071, #10212, #34294 ),
 ( #46387, #27210, #34558, #50561 ),
 ( #14653, #30875, #42448, #30362 ),
 ( #38510, #38777, #18580, #42966 ),
 ( #26173, #19356, #6535, #7061 ),
 ( #39033, #2609, #10991, #43223 ),
 ( #7314, #46647, #42708, #18315 ),
 ( #30623, #23263, #14395, #18833 ),
 ( #46126, #3389, #39281, #22241 ),
 ( #50043, #14136, #22498, #10475 ),
 ( #42183, #38248, #23012, #6283 ) ),
 .UNSPECIFIED., .F., .F., .F.,
 ( 4, 1, 1, 1, 1, 1, 1, 1, 1, 3, 4 ),
 ( 4, 4 ),
 ( 0.000000000000000000, 0.1111111111111110078, 0.2222222222222219878, 0.3333333333333329818, 0.4444444444444439757, 0.5555555555555560243, 0.6666666666666670737, 0.7777777777777779011, 0.8888888888888889506, 1.000000000000000000, 1.010000000000000009 ),
 ( 0.05091673086865800002, 0.2043272503186320255 ),
 .UNSPECIFIED. ) ;
#32594=ORIENTED_EDGE ( 'NONE', *, *, #45123, .F. ) ;
#32595=CARTESIAN_POINT ( 'NONE',  ( 56.59159595385349917, 16.48196327652579996, -48.16094229791880110 ) ) ;
#32599=CARTESIAN_POINT ( 'NONE',  ( 11.89321892211240161, 34.20364954171930094, -18.17421237891140251 ) ) ;
#32605=CARTESIAN_POINT ( 'NONE',  ( 49.45769129680230236, -53.75852492999699450, -55.06250210633439934 ) ) ;
#32608=DIRECTION ( 'NONE',  ( -1.000000000000000000, 0.000000000000000000, 0.000000000000000000 ) ) ;
#32609=CARTESIAN_POINT ( 'NONE',  ( 65.04224801900546993, -32.25487679741158331, -17.84439582078725550 ) ) ;
#32614=ORIENTED_EDGE ( 'NONE', *, *, #5646, .T. ) ;
#32616=CARTESIAN_POINT ( 'NONE',  ( 61.08724268487739550, -45.59010680718600383, -47.64259283952999624 ) ) ;
#32621=CARTESIAN_POINT ( 'NONE',  ( 53.62552786343490396, -51.33071804962359153, -75.58099297212140755 ) ) ;
#32625=CARTESIAN_POINT ( 'NONE',  ( 83.94526921706011535, -44.52752621732469862, -47.24461768887499602 ) ) ;
#32626=ORIENTED_EDGE ( 'NONE', *, *, #31624, .T. ) ;
#32627=VERTEX_POINT ( 'NONE', #4712 ) ;
#32630=CARTESIAN_POINT ( 'NONE',  ( 11.72609483531606323, -55.37304398355237822, -21.92220830349348049 ) ) ;
#32631=CIRCLE ( 'NONE', #10074, 1.000000000000000888 ) ;
#32632=CARTESIAN_POINT ( 'NONE',  ( 76.44668319880682361, -6.578471008536523001, -12.99766820392643574 ) ) ;
#32633=CARTESIAN_POINT ( 'NONE',  ( 53.73900786348829683, -51.91625817396269582, -53.89034489052589549 ) ) ;
#32634=VECTOR ( 'NONE', #28705, 1000.000000000000000 ) ;
#32635=VERTEX_POINT ( 'NONE', #28548 ) ;
#32636=ORIENTED_EDGE ( 'NONE', *, *, #46381, .T. ) ;
#32641=CARTESIAN_POINT ( 'NONE',  ( 8.806603807574589382, -63.23125877106109982, -46.67034945549170288 ) ) ;
#32645=CARTESIAN_POINT ( 'NONE',  ( 9.986016378432044149, 30.93468997499846296, -13.71124846808129050 ) ) ;
#32646=DIRECTION ( 'NONE',  ( 0.2260571801428161165, -2.775557561562891043E-17, -0.9741140340359943917 ) ) ;
#32648=CARTESIAN_POINT ( 'NONE',  ( 60.64009084818329853, 14.33648947266850016, -47.14749194313639435 ) ) ;
#32651=CARTESIAN_POINT ( 'NONE',  ( 42.11495618085190529, -44.00662160972859738, -4.742906900993289376 ) ) ;
#32653=CARTESIAN_POINT ( 'NONE',  ( 70.83745409581581498, -49.21324915459896943, -75.95351669811965678 ) ) ;
#32654=CARTESIAN_POINT ( 'NONE',  ( 67.09900448097283743, 1.833136996312119571, -20.08988941315463705 ) ) ;
#32657=CARTESIAN_POINT ( 'NONE',  ( 65.66434943752820175, 1.163675854572349788, -18.02570572091639889 ) ) ;
#32658=ORIENTED_EDGE ( 'NONE', *, *, #27723, .F. ) ;
#32659=CARTESIAN_POINT ( 'NONE',  ( 14.47836920878520139, -52.11833314967490338, -75.86497326479759806 ) ) ;
#32660=EDGE_CURVE ( 'NONE', #26727, #28850, #30382, .T. ) ;
#32661=CARTESIAN_POINT ( 'NONE',  ( 47.39033437818570604, -54.65766784492359420, -54.69850838941369631 ) ) ;
#32665=CARTESIAN_POINT ( 'NONE',  ( 60.86245460095720716, -45.45535556830957802, -47.08538195706119467 ) ) ;
#32668=DIRECTION ( 'NONE',  ( 0.000000000000000000, 1.000000000000000000, 0.000000000000000000 ) ) ;
#32670=CARTESIAN_POINT ( 'NONE',  ( 11.75767683380609796, 34.19214141181279842, -18.01774807205339712 ) ) ;
#32671=DIRECTION ( 'NONE',  ( 1.000000000000000000, 0.000000000000000000, 0.000000000000000000 ) ) ;
#32675=CARTESIAN_POINT ( 'NONE',  ( 48.38771979903820153, 22.91125108602309979, -54.79794912714500299 ) ) ;
#32678=ORIENTED_EDGE ( 'NONE', *, *, #39970, .T. ) ;
#32680=CARTESIAN_POINT ( 'NONE',  ( 72.13393739769620083, -30.11618894467929763, -20.65000000000000213 ) ) ;
#32682=CARTESIAN_POINT ( 'NONE',  ( 82.63159810076149370, 13.83598294973969978, -46.43844420537269713 ) ) ;
#32683=CARTESIAN_POINT ( 'NONE',  ( 53.64943959690070585, 17.55132301322400323, -26.88176027460789896 ) ) ;
#32685=CARTESIAN_POINT ( 'NONE',  ( 10.86720897088954807, 33.73900725339473894, -17.53558621447852062 ) ) ;
#32686=CARTESIAN_POINT ( 'NONE',  ( 55.00845962336969563, -45.68083797646840338, -15.68178826579010021 ) ) ;
#32689=ORIENTED_EDGE ( 'NONE', *, *, #7096, .F. ) ;
#32690=ADVANCED_FACE ( 'NONE', ( #51424 ), #43561, .T. ) ;
#32692=CARTESIAN_POINT ( 'NONE',  ( 11.70209409419700108, -65.10125953154968670, -16.68277806566640109 ) ) ;
#32693=CARTESIAN_POINT ( 'NONE',  ( 11.35901696209509915, 33.72246011924219289, -46.58143593047419984 ) ) ;
#32695=CARTESIAN_POINT ( 'NONE',  ( 48.12000955664969837, -54.05113525397209884, -53.67196250754390974 ) ) ;
#32699=CARTESIAN_POINT ( 'NONE',  ( 57.13928881360590140, 14.62761254858610016, -26.25285887909490157 ) ) ;
#32702=CARTESIAN_POINT ( 'NONE',  ( 51.00677944403759767, -50.85929860725079266, -76.14999999999999147 ) ) ;
#32704=AXIS2_PLACEMENT_3D ( 'NONE', #10158, #42129, #18012 ) ;
#32706=CARTESIAN_POINT ( 'NONE',  ( 55.69968854544299575, -46.18870594509260741, -25.38063974465979911 ) ) ;
#32707=CIRCLE ( 'NONE', #33557, 1.416232040419838523 ) ;
#32709=ORIENTED_EDGE ( 'NONE', *, *, #5914, .T. ) ;
#32710=FACE_OUTER_BOUND ( 'NONE', #4055, .T. ) ;
#32713=CARTESIAN_POINT ( 'NONE',  ( 14.21286514218139807, -51.12296065175440418, -22.50824227891619955 ) ) ;
#32714=CARTESIAN_POINT ( 'NONE',  ( 55.50650517420189800, 19.65167480108070208, -75.18850971831560059 ) ) ;
#32715=CARTESIAN_POINT ( 'NONE',  ( 47.50309824425850280, -54.59962336152860019, -74.14999999999999147 ) ) ;
#32719=CARTESIAN_POINT ( 'NONE',  ( 52.84318129818419862, -49.69161783228769735, -48.97012305832240031 ) ) ;
#32722=CARTESIAN_POINT ( 'NONE',  ( 47.43599255124780001, 23.40374485785099878, -74.14999585054489728 ) ) ;
#32724=DIRECTION ( 'NONE',  ( 0.8933039976646232061, -0.3805134419104956311, 0.2392017731577900652 ) ) ;
#32725=CARTESIAN_POINT ( 'NONE',  ( 56.53717807884549984, 16.48612042830059821, -47.91220710008310135 ) ) ;
#32726=DIRECTION ( 'NONE',  ( -1.000000000000000000, 0.000000000000000000, 0.000000000000000000 ) ) ;
#32731=CARTESIAN_POINT ( 'NONE',  ( 61.57009771359940231, 13.89954599885069975, -46.37201592743719658 ) ) ;
#32733=CARTESIAN_POINT ( 'NONE',  ( 12.78938691692110119, -63.51980981231629642, -45.78213823142910854 ) ) ;
#32734=ORIENTED_EDGE ( 'NONE', *, *, #37738, .T. ) ;
#32735=AXIS2_PLACEMENT_3D ( 'NONE', #51268, #15365, #31320 ) ;
#32736=CARTESIAN_POINT ( 'NONE',  ( 53.42159007590120012, -49.35880756780849765, -48.88221812793829457 ) ) ;
#32737=AXIS2_PLACEMENT_3D ( 'NONE', #43813, #20203, #16030 ) ;
#32738=CARTESIAN_POINT ( 'NONE',  ( 61.31134020973939869, -45.11617949509319203, -27.05924974616770129 ) ) ;
#32740=CARTESIAN_POINT ( 'NONE',  ( 56.83358511926749657, 14.76423303200390080, -26.24603876820060222 ) ) ;
#32743=CARTESIAN_POINT ( 'NONE',  ( 50.72974176855199602, 18.26067442992610168, -76.22250671056579563 ) ) ;
#32744=CARTESIAN_POINT ( 'NONE',  ( 53.39267832350149945, 18.14114278012100101, -48.88675587074509821 ) ) ;
#32746=CARTESIAN_POINT ( 'NONE',  ( 83.89200044194980421, -48.61618894467930119, -53.92796738110899923 ) ) ;
#32747=CARTESIAN_POINT ( 'NONE',  ( 47.26511634744682766, 22.82442341443599432, -75.56574704403116982 ) ) ;
#32748=ORIENTED_EDGE ( 'NONE', *, *, #2973, .T. ) ;
#32749=DIRECTION ( 'NONE',  ( 1.000000000000000000, 0.000000000000000000, 0.000000000000000000 ) ) ;
#32751=EDGE_CURVE ( 'NONE', #25200, #30141, #17428, .T. ) ;
#32753=CARTESIAN_POINT ( 'NONE',  ( 47.60151701969190441, -54.52169367247979892, -54.71364311436219907 ) ) ;
#32756=CARTESIAN_POINT ( 'NONE',  ( 58.72865206045799624, 17.58198988844250010, -51.18437690886020164 ) ) ;
#32762=EDGE_LOOP ( 'NONE', ( #18039, #21521, #4422, #31396 ) ) ;
#32763=ORIENTED_EDGE ( 'NONE', *, *, #36955, .F. ) ;
#32765=CARTESIAN_POINT ( 'NONE',  ( 57.77564497937559906, -3.116188944679349593, -20.65000000000000213 ) ) ;
#32767=CARTESIAN_POINT ( 'NONE',  ( 11.83663345274839962, -65.04952236550880684, -45.42313153075849641 ) ) ;
#32769=CARTESIAN_POINT ( 'NONE',  ( 54.35208312152495580, 19.95646783507805111, -75.41447387695721716 ) ) ;
#32770=CARTESIAN_POINT ( 'NONE',  ( 53.70323219070949960, 19.53744653144449828, -76.35188078170320125 ) ) ;
#32771=ORIENTED_EDGE ( 'NONE', *, *, #33887, .F. ) ;
#32772=CARTESIAN_POINT ( 'NONE',  ( 84.44784216359251161, 11.88381105532070059, -47.47585302082339354 ) ) ;
#32779=AXIS2_PLACEMENT_3D ( 'NONE', #32313, #12429, #44400 ) ;
#32782=AXIS2_PLACEMENT_3D ( 'NONE', #16940, #25289, #37107 ) ;
#32784=EDGE_CURVE ( 'NONE', #15485, #5505, #29942, .T. ) ;
#32785=CARTESIAN_POINT ( 'NONE',  ( 14.67008335555839871, 21.21781726285519909, -76.03742712147929694 ) ) ;
#32788=EDGE_CURVE ( 'NONE', #1009, #32627, #8711, .T. ) ;
#32790=DIRECTION ( 'NONE',  ( -0.7071067811865475727, 0.000000000000000000, -0.7071067811865475727 ) ) ;
#32794=CARTESIAN_POINT ( 'NONE',  ( 54.07078989395569835, -48.34239437814039775, -26.64548683062099954 ) ) ;
#32795=CARTESIAN_POINT ( 'NONE',  ( 16.49314696554849746, -51.11618894325009421, -20.88058500138570039 ) ) ;
#32796=CARTESIAN_POINT ( 'NONE',  ( 50.95939809116894992, -35.29322421015848477, -76.37898009206955408 ) ) ;
#32801=CARTESIAN_POINT ( 'NONE',  ( -10.86918838363719964, -42.36073152548370047, -6.289582464405770068 ) ) ;
#32802=CARTESIAN_POINT ( 'NONE',  ( 47.46312990717009228, 23.37191056432249781, -54.66046005970299859 ) ) ;
#32803=FACE_OUTER_BOUND ( 'NONE', #5161, .T. ) ;
#32805=CARTESIAN_POINT ( 'NONE',  ( 13.39951981361199884, 19.12481834425529925, -21.14252705510070030 ) ) ;
#32806=CARTESIAN_POINT ( 'NONE',  ( 57.28958346807240787, -50.56274171085619429, -53.44848221258419585 ) ) ;
#32807=CARTESIAN_POINT ( 'NONE',  ( 10.96947337815019985, 33.83317461693680173, -17.60046538709029917 ) ) ;
#32808=CYLINDRICAL_SURFACE ( 'NONE', #7696, 14.50000000000000178 ) ;
#32811=CARTESIAN_POINT ( 'NONE',  ( 56.34619344238320338, -47.91446257689889165, -48.39186534203880541 ) ) ;
#32814=CARTESIAN_POINT ( 'NONE',  ( 17.36723430360029852, -52.99263752172900155, -76.14999999999999147 ) ) ;
#32815=EDGE_CURVE ( 'NONE', #26843, #24834, #30962, .T. ) ;
#32816=CARTESIAN_POINT ( 'NONE',  ( 33.53393739769619231, -15.61618894467929763, -6.649999999999999467 ) ) ;
#32818=ORIENTED_EDGE ( 'NONE', *, *, #15458, .F. ) ;
#32820=CARTESIAN_POINT ( 'NONE',  ( 9.296310069140089283, 32.04080841894100473, -46.53012790981569680 ) ) ;
#32823=CARTESIAN_POINT ( 'NONE',  ( 66.70613048662919198, -29.77145157328190095, -17.03146206158359988 ) ) ;
#32824=ORIENTED_EDGE ( 'NONE', *, *, #15741, .T. ) ;
#32825=CARTESIAN_POINT ( 'NONE',  ( 18.59700916488480260, 20.77210737664869811, -75.25165125838280744 ) ) ;
#32829=CARTESIAN_POINT ( 'NONE',  ( 9.896201805643420002, -63.47691444275439920, -46.22391251453240102 ) ) ;
#32830=CARTESIAN_POINT ( 'NONE',  ( 57.33492022655319431, -45.81309998369609815, -26.26997405205120018 ) ) ;
#32832=CARTESIAN_POINT ( 'NONE',  ( 61.57627151792929965, 13.93414709175500121, -46.78392464288939578 ) ) ;
#32834=EDGE_CURVE ( 'NONE', #51359, #34653, #46186, .T. ) ;
#32838=DIRECTION ( 'NONE',  ( 0.000000000000000000, 0.000000000000000000, -1.000000000000000000 ) ) ;
#32839=CARTESIAN_POINT ( 'NONE',  ( 60.91814615750740103, -46.16813708928359716, -48.29757979411370883 ) ) ;
#32840=CARTESIAN_POINT ( 'NONE',  ( 10.01860311628955813, -55.14667356096284578, -46.10193818995475112 ) ) ;
#32841=ORIENTED_EDGE ( 'NONE', *, *, #47809, .F. ) ;
#32845=CARTESIAN_POINT ( 'NONE',  ( 75.02341226432500321, 13.88381331661629936, -15.00428186426339927 ) ) ;
#32846=CARTESIAN_POINT ( 'NONE',  ( 50.07777262096480086, 14.74234056921910074, -12.37452011861049961 ) ) ;
#32847=DIRECTION ( 'NONE',  ( 0.000000000000000000, 0.000000000000000000, -1.000000000000000000 ) ) ;
#32848=CARTESIAN_POINT ( 'NONE',  ( -6.923399356429929874, 14.58998759983630045, -4.778090145611190387 ) ) ;
#32849=AXIS2_PLACEMENT_3D ( 'NONE', #4666, #37415, #8348 ) ;
#32850=VECTOR ( 'NONE', #37308, 999.9999999999998863 ) ;
#32852=CARTESIAN_POINT ( 'NONE',  ( 55.54885310752610650, 14.75987100490110393, -16.75765343292357201 ) ) ;
#32853=B_SPLINE_CURVE_WITH_KNOTS ( 'NONE', 3,
 ( #27464, #27207, #31640, #47659, #30618, #42961, #35853, #46901, #7827, #46642 ),
 .UNSPECIFIED., .F., .F.,
 ( 4, 2, 2, 2, 4 ),
 ( 0.000000000000000000, 0.06066521036188608773, 0.4651142842241269282, 0.7990341870335844199, 1.000000000000000000 ),
 .UNSPECIFIED. ) ;
#32858=CARTESIAN_POINT ( 'NONE',  ( -11.10497851609540021, -41.90811128427360188, -5.474771920946119863 ) ) ;
#32859=CARTESIAN_POINT ( 'NONE',  ( 12.36078803208969923, 34.13639577542789993, -46.58647024651509838 ) ) ;
#32862=CARTESIAN_POINT ( 'NONE',  ( 18.86789271272390067, -51.78678247029300508, -15.81497036395479761 ) ) ;
#32864=CARTESIAN_POINT ( 'NONE',  ( 46.97440157803860217, 23.10210390193510221, -75.47461176419869844 ) ) ;
#32865=CARTESIAN_POINT ( 'NONE',  ( 49.62716556310680005, -53.64958197259959860, -54.74430167493650146 ) ) ;
#32866=CYLINDRICAL_SURFACE ( 'NONE', #50711, 22.00000000000000355 ) ;
#32867=AXIS2_PLACEMENT_3D ( 'NONE', #5644, #10345, #10083 ) ;
#32868=B_SPLINE_CURVE_WITH_KNOTS ( 'NONE', 3,
 ( #7865, #47959, #22857, #14499, #15984, #18425 ),
 .UNSPECIFIED., .F., .F.,
 ( 4, 2, 4 ),
 ( 0.000000000000000000, 0.2487259972468401914, 0.4974519944936803828 ),
 .UNSPECIFIED. ) ;
#32870=CARTESIAN_POINT ( 'NONE',  ( 18.86790574444290058, -51.78681982904430470, -74.14993593045390696 ) ) ;
#32878=CARTESIAN_POINT ( 'NONE',  ( 60.39410434858780263, -45.81892262575509989, -47.68307256904559921 ) ) ;
#32879=CARTESIAN_POINT ( 'NONE',  ( 56.88339341544950400, 19.41749060555369866, -53.85640383776300411 ) ) ;
#32885=ORIENTED_EDGE ( 'NONE', *, *, #46932, .T. ) ;
#32886=CARTESIAN_POINT ( 'NONE',  ( 83.67079303953970282, -45.04147143931179187, -47.45584445533860674 ) ) ;
#32891=CARTESIAN_POINT ( 'NONE',  ( 61.57009771103250273, -45.13192389007129890, -46.37194711517049228 ) ) ;
#32892=CARTESIAN_POINT ( 'NONE',  ( 52.56293433422980144, -49.86422820730079764, -48.47378032971909789 ) ) ;
#32893=CARTESIAN_POINT ( 'NONE',  ( 52.91668460176483535, -50.26603313699760633, -77.24653538837539202 ) ) ;
#32894=AXIS2_PLACEMENT_3D ( 'NONE', #50458, #14548, #13779 ) ;
#32895=CARTESIAN_POINT ( 'NONE',  ( 76.39087184172302614, -15.49781190055006519, -12.75716859379809343 ) ) ;
#32896=CARTESIAN_POINT ( 'NONE',  ( 54.60804605940690237, -51.56737606348759329, -53.98096760914360459 ) ) ;
#32902=CARTESIAN_POINT ( 'NONE',  ( 56.84933713246299902, 19.42395819629489750, -53.71862199975780072 ) ) ;
#32906=CARTESIAN_POINT ( 'NONE',  ( 8.793990757808609615, -63.16307462209709911, -46.67050766270720175 ) ) ;
#32907=CARTESIAN_POINT ( 'NONE',  ( 62.72656151416200743, 0.3176618421485369881, -17.00947622673330173 ) ) ;
#32912=CARTESIAN_POINT ( 'NONE',  ( 53.83004757226819947, -50.59959810400789593, -77.06233067710800810 ) ) ;
#32913=CARTESIAN_POINT ( 'NONE',  ( 64.12516823571120028, -29.62180181437879867, -16.36303599707800061 ) ) ;
#32914=CARTESIAN_POINT ( 'NONE',  ( 60.86304203775009825, 14.21967909778819994, -47.00282332578510847 ) ) ;
#32916=LINE ( 'NONE', #48945, #28852 ) ;
#32917=AXIS2_PLACEMENT_3D ( 'NONE', #44903, #8487, #32547 ) ;
#32918=CARTESIAN_POINT ( 'NONE',  ( 41.06416708622129619, -44.69533140685900463, -5.123099498004579644 ) ) ;
#32919=DIRECTION ( 'NONE',  ( 1.000000000000000000, 0.000000000000000000, 0.000000000000000000 ) ) ;
#32921=CARTESIAN_POINT ( 'NONE',  ( 66.85007720623511318, 1.883639210398676989, -20.46329710072452812 ) ) ;
#32922=EDGE_CURVE ( 'NONE', #7985, #48450, #21178, .T. ) ;
#32925=CARTESIAN_POINT ( 'NONE',  ( 65.89616026620871025, 0.1838254176425679898, -17.15308774369420064 ) ) ;
#32926=EDGE_CURVE ( 'NONE', #43692, #39834, #9904, .T. ) ;
#32928=CARTESIAN_POINT ( 'NONE',  ( 13.67954409772299940, -51.79024427787750540, -75.14498753492070193 ) ) ;
#32929=CARTESIAN_POINT ( 'NONE',  ( 47.40680130986410745, -54.64269092349360335, -54.65527420080069732 ) ) ;
#32930=CARTESIAN_POINT ( 'NONE',  ( 8.892600494392757682, 32.33025239210895307, -46.69114580434834494 ) ) ;
#32936=CARTESIAN_POINT ( 'NONE',  ( 57.47203281493852955, 13.89859585196675873, -25.53999618909873348 ) ) ;
#32937=CARTESIAN_POINT ( 'NONE',  ( 47.67211062985429493, -54.52182009381669303, -55.16489596303849652 ) ) ;
#32938=CARTESIAN_POINT ( 'NONE',  ( 14.05648280823140084, 19.92572429986999794, -22.83284003973019693 ) ) ;
#32939=CARTESIAN_POINT ( 'NONE',  ( -11.32734370190460105, -41.88171845330919751, -6.430192534648670133 ) ) ;
#32940=CARTESIAN_POINT ( 'NONE',  ( 56.30184842130790202, 19.39087536565910241, -52.97276602642149612 ) ) ;
#32942=CARTESIAN_POINT ( 'NONE',  ( 48.40807908919139635, 22.97456863626519663, -55.22863709201329385 ) ) ;
#32943=ORIENTED_EDGE ( 'NONE', *, *, #41452, .F. ) ;
#32949=CARTESIAN_POINT ( 'NONE',  ( 82.79586663885601183, 13.79056004649610045, -46.43485061813930059 ) ) ;
#32950=CARTESIAN_POINT ( 'NONE',  ( 54.23595886153059809, 16.77554233507499859, -26.19545990100650101 ) ) ;
#32952=CYLINDRICAL_SURFACE ( 'NONE', #2807, 2.999999999999999112 ) ;
#32954=DIRECTION ( 'NONE',  ( 1.000000000000000000, 0.000000000000000000, 0.000000000000000000 ) ) ;
#32956=ORIENTED_EDGE ( 'NONE', *, *, #16508, .T. ) ;
#32957=ORIENTED_EDGE ( 'NONE', *, *, #23825, .F. ) ;
#32958=CARTESIAN_POINT ( 'NONE',  ( 11.84964338387410088, -64.94214987232159331, -16.34215248990359726 ) ) ;
#32959=CARTESIAN_POINT ( 'NONE',  ( 11.09465806800830023, 32.35066555307069791, -44.35269109309979996 ) ) ;
#32960=CARTESIAN_POINT ( 'NONE',  ( 18.15361292478090860, 19.88381105533058246, -15.68107046463052257 ) ) ;
#32961=CARTESIAN_POINT ( 'NONE',  ( 49.83032669135840109, -52.82339107842129522, -53.07740273290610133 ) ) ;
#32964=LINE ( 'NONE', #4950, #25950 ) ;
#32971=CARTESIAN_POINT ( 'NONE',  ( 50.75796709625730330, -50.55377401516400226, -76.14999999999999147 ) ) ;
#32972=EDGE_CURVE ( 'NONE', #35688, #1476, #18646, .T. ) ;
#32974=ORIENTED_EDGE ( 'NONE', *, *, #17837, .F. ) ;
#32978=CARTESIAN_POINT ( 'NONE',  ( 12.71214975072897779, -55.46957087202495984, -75.54211829845161219 ) ) ;
#32979=CARTESIAN_POINT ( 'NONE',  ( 54.47259832750690123, -46.25232753665150653, -15.76422791930239953 ) ) ;
#32981=CARTESIAN_POINT ( 'NONE',  ( 13.63913686917599932, -51.36033930440640205, -22.70105461358259902 ) ) ;
#32982=CARTESIAN_POINT ( 'NONE',  ( 56.40190446271180491, 19.55626960565449934, -74.41752554396340713 ) ) ;
#32983=CARTESIAN_POINT ( 'NONE',  ( 47.15880624984559688, -54.00277375082009712, -75.65761316843601492 ) ) ;
#32985=CARTESIAN_POINT ( 'NONE',  ( 55.59479635141730114, 14.68315623537079873, -16.73302166087749754 ) ) ;
#32986=( BOUNDED_CURVE ( )  B_SPLINE_CURVE ( 3, ( #31853, #35289, #51024, #20066 ),
 .UNSPECIFIED., .F., .T. ) 
 B_SPLINE_CURVE_WITH_KNOTS ( ( 4, 4 ),
 ( 1.053572925743754274, 1.570796326794900999 ),
 .UNSPECIFIED. ) 
 CURVE ( )  GEOMETRIC_REPRESENTATION_ITEM ( )  RATIONAL_B_SPLINE_CURVE ( ( 1.000000000000000000, 0.9778306343446276916, 0.9778306343446276916, 1.000000000000000000 ) ) 
 REPRESENTATION_ITEM ( '' )  );
#32987=CARTESIAN_POINT ( 'NONE',  ( 56.94040705048700346, -50.34429464441200253, -52.81451654216659364 ) ) ;
#32991=AXIS2_PLACEMENT_3D ( 'NONE', #31242, #2451, #10846 ) ;
#32992=CARTESIAN_POINT ( 'NONE',  ( 46.35275103504439898, 21.67755452994670406, -76.14999999999999147 ) ) ;
#32993=ADVANCED_FACE ( 'NONE', ( #22005, #34056 ), #33804, .T. ) ;
#32995=B_SPLINE_CURVE_WITH_KNOTS ( 'NONE', 3,
 ( #47590, #23953, #43144, #4069, #23187, #35264, #43654, #51263, #27395, #20037, #7239, #36032, #39203, #7756, #15357, #15869, #16117, #32078, #43396, #19282, #28155, #3821, #31313, #47339, #40233, #44159 ),
 .UNSPECIFIED., .F., .F.,
 ( 4, 2, 2, 2, 2, 2, 2, 2, 2, 2, 2, 2, 4 ),
 ( 0.000000000000000000, 0.03967672352634984967, 0.1774997633214195625, 0.3374995499773481011, 0.4374994166373029070, 0.4999993332997746398, 0.5624992499622464281, 0.6380835170998415684, 0.6985509308099168146, 0.7590183445199933931, 0.8429308035155282930, 0.9771907379083839551, 1.000000000000000000 ),
 .UNSPECIFIED. ) ;
#33000=CARTESIAN_POINT ( 'NONE',  ( 16.13393739769620083, -15.61618894467929941, -6.928362978644219794 ) ) ;
#33001=CARTESIAN_POINT ( 'NONE',  ( -10.89882054044000093, 10.23933580255000031, -4.618747568469349751 ) ) ;
#33003=CIRCLE ( 'NONE', #10442, 1.999999999999998668 ) ;
#33005=FACE_OUTER_BOUND ( 'NONE', #36076, .T. ) ;
#33007=CARTESIAN_POINT ( 'NONE',  ( 52.84630519521279979, -49.65262790780239754, -48.68178424806700377 ) ) ;
#33010=CARTESIAN_POINT ( 'NONE',  ( 57.48863382328549676, 14.20681801447659964, -26.08418812544719856 ) ) ;
#33012=CARTESIAN_POINT ( 'NONE',  ( 51.16024193372230400, 19.49271328425620098, -76.16561533977029796 ) ) ;
#33013=CARTESIAN_POINT ( 'NONE',  ( 52.65923532209550473, 18.54112759137870015, -48.49071726774990054 ) ) ;
#33015=DIRECTION ( 'NONE',  ( -1.000000000000000000, -1.791661345120054866E-29, -4.486507500526829843E-12 ) ) ;
#33016=CARTESIAN_POINT ( 'NONE',  ( 69.11293209371449109, -43.39700965238730390, -11.59160171341740053 ) ) ;
#33017=ORIENTED_EDGE ( 'NONE', *, *, #50037, .T. ) ;
#33021=CARTESIAN_POINT ( 'NONE',  ( 47.45236065713989859, -54.62711186455120327, -54.90161485602320113 ) ) ;
#33024=CARTESIAN_POINT ( 'NONE',  ( 56.95284895653189494, 18.93591985592150095, -52.58138290995459840 ) ) ;
#33025=CARTESIAN_POINT ( 'NONE',  ( 52.94585586128479093, 18.36771476006709847, -48.75076952771310346 ) ) ;
#33030=VERTEX_POINT ( 'NONE', #30129 ) ;
#33031=ORIENTED_EDGE ( 'NONE', *, *, #2055, .F. ) ;
#33033=CARTESIAN_POINT ( 'NONE',  ( 8.975750908825888885, -63.26599253637061082, -46.63326651989199689 ) ) ;
#33035=FACE_OUTER_BOUND ( 'NONE', #16606, .T. ) ;
#33038=CARTESIAN_POINT ( 'NONE',  ( 68.38971107317580334, -30.11618894467929763, -18.15384911698640025 ) ) ;
#33039=CARTESIAN_POINT ( 'NONE',  ( 55.20064104123608928, 19.79077351844777510, -75.15544575098610380 ) ) ;
#33040=CARTESIAN_POINT ( 'NONE',  ( 53.80070914189850129, 19.45344997228420070, -76.57022543143750681 ) ) ;
#33041=ORIENTED_EDGE ( 'NONE', *, *, #41812, .T. ) ;
#33042=CARTESIAN_POINT ( 'NONE',  ( 59.34499803081109803, -3.116188944679349593, -15.68015151901639825 ) ) ;
#33045=B_SPLINE_SURFACE_WITH_KNOTS ( 'NONE', 3, 3, ( 
 ( #21533, #21017, #9253, #41208, #37278, #13446, #37530, #1634, #17624, #33594, #49608, #14722, #30692, #34621 ),
 ( #46714, #27023, #10799, #30429, #26758, #3190, #30175, #2929, #14205, #46195, #46454, #42771, #6871, #50625 ),
 ( #39097, #43030, #22045, #50110, #6603, #26241, #18133, #22820, #18384, #38580, #22564, #45925, #42249, #41990 ),
 ( #6091, #7127, #26498, #38841, #23079, #6348, #18900, #10542, #30942, #2674, #22306, #38314, #34884, #42514 ),
 ( #50884, #46973, #14976, #18647, #11056, #14460, #2400, #10279, #34359, #19163, #35140, #50376, #51145, #15243 ),
 ( #38058, #10015, #34095, #25976, #2153, #7639, #16006, #43789, #47728, #4462, #31703, #31963, #31453, #7890 ),
 ( #4206, #47479, #11833, #24090, #47224, #23326, #35671, #19673, #3705, #51655, #12084, #12331, #7377, #15749 ),
 ( #27279, #8145, #39351, #19423, #27793, #35403, #11571, #28038, #44043, #23836, #20431, #39858, #51399, #47984 ),
 ( #40112, #27533, #11314, #32213, #20178, #3962, #19923, #35916, #24351, #36168, #36419, #48237, #31193, #28291 ),
 ( #276, #44295, #527, #43539, #43288, #3450, #15499, #8403, #40365, #23584, #39602, #49282, #49541, #44557 ) ),
 .UNSPECIFIED., .F., .F., .F.,
 ( 4, 1, 1, 1, 1, 1, 1, 4 ),
 ( 4, 2, 2, 2, 2, 2, 4 ),
 ( -0.0003239663523781590088, 0.1428571428571430157, 0.2857142857142860315, 0.4285714285714289917, 0.5714285714285709528, 0.7142857142857139685, 0.8571428571428569843, 1.000060558257379828 ),
 ( -0.7975921375522809775, -0.7173344096180139795, -0.5738675276944109616, -0.5021340867326099522, -0.3873605811937279597, -0.2037229723315160113, 0.0003085036975347379886 ),
 .UNSPECIFIED. ) ;
#33047=DIRECTION ( 'NONE',  ( -2.027310999999999893E-13, 2.567767000000000059E-13, 1.000000000000000000 ) ) ;
#33051=CARTESIAN_POINT ( 'NONE',  ( 11.01003601656879916, -63.61865847005719843, -24.02609861887260223 ) ) ;
#33053=CARTESIAN_POINT ( 'NONE',  ( 41.16398077517839482, 14.31303017726370008, -6.123772754722979883 ) ) ;
#33055=ADVANCED_FACE ( 'NONE', ( #11272 ), #50682, .T. ) ;
#33056=CARTESIAN_POINT ( 'NONE',  ( 14.34756424442590017, 21.20322725566390076, -75.94942944171690158 ) ) ;
#33058=CARTESIAN_POINT ( 'NONE',  ( 82.45627759125989087, -45.09272112584100256, -46.38986626917129996 ) ) ;
#33062=CARTESIAN_POINT ( 'NONE',  ( 54.24920814692630699, -48.27160202174960091, -26.73053837092809815 ) ) ;
#33063=FACE_OUTER_BOUND ( 'NONE', #13248, .T. ) ;
#33066=CARTESIAN_POINT ( 'NONE',  ( -8.866062602303800944, -15.61618894467929586, 4.450000000000000178 ) ) ;
#33067=CIRCLE ( 'NONE', #13825, 3.799999999999999378 ) ;
#33069=CARTESIAN_POINT ( 'NONE',  ( -8.369583062334038814, -44.67542189550749754, -5.381608453275170234 ) ) ;
#33070=CARTESIAN_POINT ( 'NONE',  ( 47.24879073443120348, 23.52399838237280250, -54.63316666300269731 ) ) ;
#33074=CARTESIAN_POINT ( 'NONE',  ( 11.56756857248330128, 34.11390478956230510, -17.53311478114069999 ) ) ;
#33078=CARTESIAN_POINT ( 'NONE',  ( 55.61561331844040268, -48.29731251153899763, -48.56918272874399634 ) ) ;
#33081=CARTESIAN_POINT ( 'NONE',  ( 53.50274481840529717, 20.58623994349600039, -53.37071925176099541 ) ) ;
#33083=VERTEX_POINT ( 'NONE', #31832 ) ;
#33085=CARTESIAN_POINT ( 'NONE',  ( 10.14913760601130122, 32.10609558527020369, -45.99399621147029649 ) ) ;
#33087=CARTESIAN_POINT ( 'NONE',  ( 66.55656304324030259, -30.20673539474010028, -16.96067054740260005 ) ) ;
#33088=VERTEX_POINT ( 'NONE', #24477 ) ;
#33089=CARTESIAN_POINT ( 'NONE',  ( 17.77572303879259863, 20.43782862716600235, -75.53341961486960088 ) ) ;
#33091=VERTEX_POINT ( 'NONE', #32599 ) ;
#33092=CARTESIAN_POINT ( 'NONE',  ( 47.77526208095149940, 23.24550361938759835, -55.21131733320120105 ) ) ;
#33095=CARTESIAN_POINT ( 'NONE',  ( 12.11535881846170071, -65.31089811698159053, -46.92786770476139679 ) ) ;
#33096=CARTESIAN_POINT ( 'NONE',  ( 56.47981878976860060, -46.01152027889720131, -26.17847996949780054 ) ) ;
#33098=EDGE_CURVE ( 'NONE', #45437, #814, #4331, .T. ) ;
#33099=CARTESIAN_POINT ( 'NONE',  ( 61.61685004883869965, 13.90101642484820132, -46.58069093359240043 ) ) ;
#33100=EDGE_CURVE ( 'NONE', #37257, #22022, #20554, .T. ) ;
#33103=LINE ( 'NONE', #8505, #25131 ) ;
#33106=CARTESIAN_POINT ( 'NONE',  ( 45.64758691443690708, -45.19790785473080064, -8.164367006753829870 ) ) ;
#33108=CARTESIAN_POINT ( 'NONE',  ( 16.13393739769620083, -15.61618894467929941, -10.44999999999999929 ) ) ;
#33109=DIRECTION ( 'NONE',  ( 0.000000000000000000, 0.000000000000000000, -1.000000000000000000 ) ) ;
#33112=LINE ( 'NONE', #32325, #49290 ) ;
#33113=CARTESIAN_POINT ( 'NONE',  ( 46.75888556483590008, -53.81317836377680663, -75.90771320283761270 ) ) ;
#33114=CARTESIAN_POINT ( 'NONE',  ( 66.62633200496509289, 13.73060551161930043, -11.96361206954319911 ) ) ;
#33115=CARTESIAN_POINT ( 'NONE',  ( 46.25788900357310496, 14.69397481452669929, -9.684285679222321974 ) ) ;
#33117=EDGE_CURVE ( 'NONE', #22647, #33533, #48811, .T. ) ;
#33118=DIRECTION ( 'NONE',  ( -0.8224686640529098591, 0.3976080002595605012, -0.4067593573362696113 ) ) ;
#33119=CARTESIAN_POINT ( 'NONE',  ( -8.908994694087390087, 12.97547407152449850, -5.435440242544679279 ) ) ;
#33121=CARTESIAN_POINT ( 'NONE',  ( 59.58068192400040175, 13.98218772109100172, -26.37874264201060015 ) ) ;
#33125=CARTESIAN_POINT ( 'NONE',  ( 53.55347996450739601, 18.14618377272470084, -49.15350056088400521 ) ) ;
#33127=CARTESIAN_POINT ( 'NONE',  ( 76.88109178265870014, -43.17103650464989784, -14.86960880489979964 ) ) ;
#33130=B_SPLINE_CURVE_WITH_KNOTS ( 'NONE', 3,
 ( #16377, #48883, #28676, #28938, #40747, #40234, #32589, #4846, #32852, #36806, #20039, #16118, #44422, #24989, #4324, #8524 ),
 .UNSPECIFIED., .F., .F.,
 ( 4, 2, 2, 2, 2, 2, 2, 4 ),
 ( 0.000000000000000000, 0.1775032223223184658, 0.3375025954872091227, 0.4375022037152671017, 0.5000019588578006324, 0.6250014691428724678, 0.7629640249125425600, 1.000000000000000000 ),
 .UNSPECIFIED. ) ;
#33132=CIRCLE ( 'NONE', #14763, 1.500000000000001332 ) ;
#33133=CARTESIAN_POINT ( 'NONE',  ( 82.13853704237929776, -45.11618894467940066, -46.37203261889099792 ) ) ;
#33135=CARTESIAN_POINT ( 'NONE',  ( 48.79180034249609577, -53.85388452497259948, -54.46585069627389686 ) ) ;
#33138=CARTESIAN_POINT ( 'NONE',  ( 51.17464648325179155, -31.65168256193422280, -17.11447666815010749 ) ) ;
#33139=CARTESIAN_POINT ( 'NONE',  ( 59.63596466869476131, -1.505138099722426848, -15.90544011693026683 ) ) ;
#33140=CARTESIAN_POINT ( 'NONE',  ( 18.12954305947619815, -51.13036009974659635, -74.14993170018701107 ) ) ;
#33147=CARTESIAN_POINT ( 'NONE',  ( 60.65080933879319502, -45.73000258907639903, -47.69371751895570100 ) ) ;
#33149=CARTESIAN_POINT ( 'NONE',  ( 50.31596464670999325, 18.73470065217860281, -76.14999999999999147 ) ) ;
#33160=CARTESIAN_POINT ( 'NONE',  ( 50.02331077270184068, -52.39130121342888913, -51.61203677770532749 ) ) ;
#33167=CARTESIAN_POINT ( 'NONE',  ( 11.54049066802846291, 34.10846995014738781, -22.61126967411468769 ) ) ;
#33170=CARTESIAN_POINT ( 'NONE',  ( 56.45963719500260680, 19.43072222330619780, -53.16982888481129521 ) ) ;
#33173=CARTESIAN_POINT ( 'NONE',  ( 8.813944282408009201, -63.27296482252339871, -46.67145360045340396 ) ) ;
#33177=CARTESIAN_POINT ( 'NONE',  ( 51.82414462793709475, -50.18944315258300293, -76.50963453239940293 ) ) ;
#33179=CARTESIAN_POINT ( 'NONE',  ( 47.64143405402000297, -54.53488714544439375, -55.14905519569939685 ) ) ;
#33180=AXIS2_PLACEMENT_3D ( 'NONE', #18144, #45936, #13962 ) ;
#33184=CARTESIAN_POINT ( 'NONE',  ( 45.24668088971260005, 13.87996455531310147, -7.238505014500240087 ) ) ;
#33186=CARTESIAN_POINT ( 'NONE',  ( 42.48652067527369525, -44.25687345361960467, -5.094659063150840161 ) ) ;
#33187=CARTESIAN_POINT ( 'NONE',  ( 70.03247032090770574, -49.95860450174030376, -73.25000000000169109 ) ) ;
#33188=CARTESIAN_POINT ( 'NONE',  ( 61.24959635998759921, -45.52506596813110207, -47.58791272468889844 ) ) ;
#33190=CARTESIAN_POINT ( 'NONE',  ( 18.19606299423181284, -52.32662977634584678, -75.76245441609270870 ) ) ;
#33191=CARTESIAN_POINT ( 'NONE',  ( 65.04200595171910493, 1.022226219316999973, -17.84399244536480111 ) ) ;
#33193=ORIENTED_EDGE ( 'NONE', *, *, #48230, .F. ) ;
#33194=CARTESIAN_POINT ( 'NONE',  ( 14.52849062202900043, -51.76348103900169662, -75.62474771911489313 ) ) ;
#33195=CARTESIAN_POINT ( 'NONE',  ( 57.36736290859560938, 18.90165667866860133, -52.61791395480889832 ) ) ;
#33202=CARTESIAN_POINT ( 'NONE',  ( 12.06284766121009966, 32.21085600226960111, -22.25048313876769868 ) ) ;
#33203=CARTESIAN_POINT ( 'NONE',  ( 47.77967683121789833, -54.45042155320719957, -54.88424258904849751 ) ) ;
#33204=DIRECTION ( 'NONE',  ( 0.3294064756440921449, -0.9441882088883224444, 0.000000000000000000 ) ) ;
#33205=CARTESIAN_POINT ( 'NONE',  ( 14.34417029198830029, 19.88381105532299742, -22.49240188329279988 ) ) ;
#33206=CARTESIAN_POINT ( 'NONE',  ( 56.41160328492299669, 19.47925591966880177, -53.28618851948499469 ) ) ;
#33208=CARTESIAN_POINT ( 'NONE',  ( 48.65500193615349644, 22.71479567191139992, -54.55862777695219989 ) ) ;
#33215=FACE_OUTER_BOUND ( 'NONE', #6428, .T. ) ;
#33216=CARTESIAN_POINT ( 'NONE',  ( 82.70745875113269108, 14.23235930836570162, -47.51979026979370246 ) ) ;
#33217=CARTESIAN_POINT ( 'NONE',  ( 52.77845664521150582, 18.41768890413229798, -27.63491308911480004 ) ) ;
#33220=CARTESIAN_POINT ( 'NONE',  ( 56.07056193865970073, -45.13118964431610181, -15.17735046330640181 ) ) ;
#33223=ORIENTED_EDGE ( 'NONE', *, *, #37738, .F. ) ;
#33224=CARTESIAN_POINT ( 'NONE',  ( 12.11414304660010188, -65.16113420147659951, -16.63763903707940273 ) ) ;
#33225=CARTESIAN_POINT ( 'NONE',  ( 12.37952141923769922, 34.14838032032060511, -46.79454185349629824 ) ) ;
#33230=ORIENTED_EDGE ( 'NONE', *, *, #51754, .T. ) ;
#33231=ADVANCED_FACE ( 'NONE', ( #30238 ), #6134, .F. ) ;
#33233=CARTESIAN_POINT ( 'NONE',  ( 52.88960523627919486, 18.37708893635865692, -27.85916541547489800 ) ) ;
#33237=CARTESIAN_POINT ( 'NONE',  ( 50.23538084491700317, -49.77012050973760182, -76.14999999999999147 ) ) ;
#33239=ORIENTED_EDGE ( 'NONE', *, *, #27392, .F. ) ;
#33240=B_SPLINE_CURVE_WITH_KNOTS ( 'NONE', 3,
 ( #25902, #17551, #5250, #33523, #14130, #37211, #1311, #33260, #29336, #49535, #3380, #31638, #7567, #19352, #19608, #23516, #18576, #51071, #30616, #15684, #10726, #39274, #50556, #38770, #23006, #39536, #35066, #46640, #50814, #35599, #27205, #26679, #15171, #11505 ),
 .UNSPECIFIED., .F., .F.,
 ( 4, 3, 3, 3, 3, 3, 3, 3, 3, 3, 3, 4 ),
 ( 3.231192999999999801E-12, 0.3998525513778730112, 0.8924049053485588745, 0.9695310320484800126, 1.582190098185180194, 2.108887993389690241, 2.822382364412600264, 3.535876735435510287, 4.252742048685130172, 4.968682683331829608, 5.179452103612369740, 5.526958877413330029 ),
 .UNSPECIFIED. ) ;
#33245=DIRECTION ( 'NONE',  ( 0.000000000000000000, 0.000000000000000000, -1.000000000000000000 ) ) ;
#33247=CARTESIAN_POINT ( 'NONE',  ( 13.86591929268250034, -51.23668186105609834, -22.87012482983299932 ) ) ;
#33250=CARTESIAN_POINT ( 'NONE',  ( 47.01491813235679729, -53.96463636605060543, -75.73879140141839628 ) ) ;
#33252=CARTESIAN_POINT ( 'NONE',  ( 56.19404819212199698, 14.17124906888450120, -16.68782110614939995 ) ) ;
#33253=CARTESIAN_POINT ( 'NONE',  ( 57.28774565251580242, -50.57888888196889354, -53.44461253009320245 ) ) ;
#33257=ORIENTED_EDGE ( 'NONE', *, *, #25699, .T. ) ;
#33258=CARTESIAN_POINT ( 'NONE',  ( 47.21888195866730342, 22.94886078616289993, -75.46887108633461594 ) ) ;
#33259=LINE ( 'NONE', #18060, #15868 ) ;
#33260=CARTESIAN_POINT ( 'NONE',  ( 41.40202236619799692, -45.62702843439980427, -6.330381766430189572 ) ) ;
#33264=CARTESIAN_POINT ( 'NONE',  ( 60.40020840339374075, 14.46217060654146280, -47.21880793596233872 ) ) ;
#33265=EDGE_CURVE ( 'NONE', #9653, #34462, #3042, .T. ) ;
#33266=DIRECTION ( 'NONE',  ( 1.000000000000000000, 0.000000000000000000, 0.000000000000000000 ) ) ;
#33267=FACE_OUTER_BOUND ( 'NONE', #34648, .T. ) ;
#33271=CARTESIAN_POINT ( 'NONE',  ( -26.88697088543599989, -41.87816877422690709, -56.26659592162470602 ) ) ;
#33272=ADVANCED_FACE ( 'NONE', ( #1180 ), #31005, .T. ) ;
#33274=CARTESIAN_POINT ( 'NONE',  ( 52.80018231237879434, -49.68132406852449634, -48.71455220968519484 ) ) ;
#33275=CARTESIAN_POINT ( 'NONE',  ( 60.57693621588790478, -45.12131271250889597, -26.54673895663080074 ) ) ;
#33277=CARTESIAN_POINT ( 'NONE',  ( 13.32586770901309947, 19.62211552346140309, -21.60957827883089877 ) ) ;
#33278=CARTESIAN_POINT ( 'NONE',  ( 57.06431677564219740, 13.92418399135899953, -25.30300626299959887 ) ) ;
#33280=CARTESIAN_POINT ( 'NONE',  ( 51.02428974428540442, 18.84793802927210038, -76.22815759457780871 ) ) ;
#33281=CARTESIAN_POINT ( 'NONE',  ( 52.67441652328110280, 18.52990734569499764, -48.55744554217059772 ) ) ;
#33283=CARTESIAN_POINT ( 'NONE',  ( 41.72053737372340265, -43.71151935359279861, -3.400228435618770195 ) ) ;
#33284=CARTESIAN_POINT ( 'NONE',  ( 73.44245504306711325, -45.11618894467940066, -14.54927509218509840 ) ) ;
#33290=CARTESIAN_POINT ( 'NONE',  ( 47.44513431003649373, -54.62464540978789529, -54.74498770855480245 ) ) ;
#33293=CARTESIAN_POINT ( 'NONE',  ( 58.15863228698849952, 17.43447541518139943, -50.85867504786170201 ) ) ;
#33294=CARTESIAN_POINT ( 'NONE',  ( 17.92370450339669929, -51.11618894467930119, -74.14999999999999147 ) ) ;
#33300=EDGE_CURVE ( 'NONE', #10111, #24567, #51228, .T. ) ;
#33303=CARTESIAN_POINT ( 'NONE',  ( 8.813944282408009201, -63.27296482252339871, -46.67145360045340396 ) ) ;
#33304=AXIS2_PLACEMENT_3D ( 'NONE', #12416, #16086, #7460 ) ;
#33305=DIRECTION ( 'NONE',  ( 1.000000000000000000, 0.000000000000000000, 0.000000000000000000 ) ) ;
#33310=CARTESIAN_POINT ( 'NONE',  ( 53.83039865298910343, 19.62284230666540097, -76.11625649682230232 ) ) ;
#33312=FACE_OUTER_BOUND ( 'NONE', #20970, .T. ) ;
#33313=CARTESIAN_POINT ( 'NONE',  ( -14.86606260230379917, -15.61618894467933139, -17.89999999999999858 ) ) ;
#33319=CARTESIAN_POINT ( 'NONE',  ( 56.39270784227079503, -50.52750194671250483, -52.86271187454359932 ) ) ;
#33321=CARTESIAN_POINT ( 'NONE',  ( 52.56521993351460509, -49.86179673305679927, -48.47378032971909789 ) ) ;
#33322=CARTESIAN_POINT ( 'NONE',  ( 42.67456719961179346, 14.69556074203230089, -7.343022369310959974 ) ) ;
#33323=CARTESIAN_POINT ( 'NONE',  ( 13.74871818702220061, 20.76921105827980085, -75.35480091913980516 ) ) ;
#33324=DIRECTION ( 'NONE',  ( -0.1999849291395982553, -0.9797989733190325401, 0.000000000000000000 ) ) ;
#33325=CARTESIAN_POINT ( 'NONE',  ( 83.46510812583990457, -44.70132628866610247, -46.64393865386079341 ) ) ;
#33329=CARTESIAN_POINT ( 'NONE',  ( 52.77069811684319944, -49.64525113236509668, -27.51082437244179957 ) ) ;
#33331=CARTESIAN_POINT ( 'NONE',  ( 14.34399776555519956, -51.11618894007569480, -22.49261467888789667 ) ) ;
#33333=CARTESIAN_POINT ( 'NONE',  ( 11.76847557413320189, 32.96418959114749470, -15.47533549984080103 ) ) ;
#33337=CARTESIAN_POINT ( 'NONE',  ( -11.32734370190460105, -41.88171845330919751, -6.430192534648670133 ) ) ;
#33338=CARTESIAN_POINT ( 'NONE',  ( 47.48053164517749991, 23.37705619533080181, -54.85557598631709908 ) ) ;
#33339=CARTESIAN_POINT ( 'NONE',  ( 16.13393739769620083, -15.61618894467929941, -7.049999999999999822 ) ) ;
#33341=CARTESIAN_POINT ( 'NONE',  ( 55.58236959119586373, 15.93246778660674323, -26.45502009950325473 ) ) ;
#33342=CARTESIAN_POINT ( 'NONE',  ( 11.91784406111709949, 34.19847404269119551, -17.65794013793280115 ) ) ;
#33345=CARTESIAN_POINT ( 'NONE',  ( -11.07640030671909948, 8.018182000708311108, -19.14999999999999858 ) ) ;
#33346=CARTESIAN_POINT ( 'NONE',  ( 55.20227514146910153, -48.56140865947679686, -48.75929635819750274 ) ) ;
#33348=CARTESIAN_POINT ( 'NONE',  ( 53.17432493994039788, 20.66509266784749954, -53.32388713517680401 ) ) ;
#33354=CARTESIAN_POINT ( 'NONE',  ( 9.289247614019680910, 31.98971538174660267, -46.53005782715530358 ) ) ;
#33356=CARTESIAN_POINT ( 'NONE',  ( 66.56327834958220535, -30.21069703426200093, -16.96525396667280106 ) ) ;
#33358=CARTESIAN_POINT ( 'NONE',  ( 17.73209452681750165, 20.42331001517590394, -75.51792558472199346 ) ) ;
#33362=B_SPLINE_CURVE_WITH_KNOTS ( 'NONE', 3,
 ( #4921, #1251, #44496, #45276, #8598, #20892, #32936, #13066, #9386 ),
 .UNSPECIFIED., .F., .F.,
 ( 4, 1, 1, 1, 1, 1, 4 ),
 ( 0.000000000000000000, 0.1666541203251306613, 0.3333161082673998243, 0.4999780962096700421, 0.6666400841519403153, 0.8333020720942094783, 1.000000000000000000 ),
 .UNSPECIFIED. ) ;
#33364=ORIENTED_EDGE ( 'NONE', *, *, #2540, .T. ) ;
#33365=CARTESIAN_POINT ( 'NONE',  ( 12.91702256450149910, -65.51268121040151016, -47.68987055332590330 ) ) ;
#33366=CARTESIAN_POINT ( 'NONE',  ( 56.17575110250020032, -46.09713117230519686, -26.07745160796680040 ) ) ;
#33368=CARTESIAN_POINT ( 'NONE',  ( 61.55546069326469905, 13.95115017060379969, -46.85742263993579115 ) ) ;
#33370=ORIENTED_EDGE ( 'NONE', *, *, #8054, .T. ) ;
#33372=CARTESIAN_POINT ( 'NONE',  ( 75.17996938839529264, -0.5297985755353621373, -11.94677486813695388 ) ) ;
#33374=ORIENTED_EDGE ( 'NONE', *, *, #33749, .F. ) ;
#33375=CARTESIAN_POINT ( 'NONE',  ( 50.66367948673760679, -45.98186837715630304, -12.79866758418470063 ) ) ;
#33378=CARTESIAN_POINT ( 'NONE',  ( 68.13393739769810509, 19.38381105532030091, -71.50000000000198952 ) ) ;
#33381=CARTESIAN_POINT ( 'NONE',  ( 46.91224408115239441, -54.15189901127720162, -75.65958371907380808 ) ) ;
#33383=CARTESIAN_POINT ( 'NONE',  ( 50.25339681658829960, 14.35477854232929928, -12.12767580573030024 ) ) ;
#33385=B_SPLINE_CURVE_WITH_KNOTS ( 'NONE', 3,
 ( #48138, #8569, #12495, #51809, #4109, #28465, #36078, #24777, #40530, #12239, #32378, #8301, #3864, #40787, #44203, #44463, #4888, #20087, #36587, #689 ),
 .UNSPECIFIED., .F., .F.,
 ( 4, 2, 2, 2, 2, 2, 2, 2, 2, 4 ),
 ( 0.000000000000000000, 0.03794172797384393753, 0.1301135039818921146, 0.2222852799899402987, 0.3374999999999994116, 0.4374999999999988898, 0.5000000000000018874, 0.6250000000000007772, 0.8250000000000001776, 1.000000000000000000 ),
 .UNSPECIFIED. ) ;
#33386=DIRECTION ( 'NONE',  ( -0.6023772969742139383, 0.4987169684303948691, -0.6232358923310148402 ) ) ;
#33388=CARTESIAN_POINT ( 'NONE',  ( 58.43730894494089512, 13.94609765837119930, -25.90344854066760050 ) ) ;
#33396=AXIS2_PLACEMENT_3D ( 'NONE', #28018, #51120, #35647 ) ;
#33398=CARTESIAN_POINT ( 'NONE',  ( 11.41271396217149992, -64.98654470182599141, -16.69425700586020156 ) ) ;
#33401=CARTESIAN_POINT ( 'NONE',  ( 47.46019986771550236, -54.30427659521456718, -75.17791912521337849 ) ) ;
#33402=CARTESIAN_POINT ( 'NONE',  ( 48.80109316716579571, -53.86560520698500198, -54.49771944612560048 ) ) ;
#33405=CARTESIAN_POINT ( 'NONE',  ( 61.75019796695539753, 14.88381105532069881, -37.26101630944549470 ) ) ;
#33411=CARTESIAN_POINT ( 'NONE',  ( 60.80694905565239594, -45.63379593877770901, -47.60985284215269786 ) ) ;
#33413=CARTESIAN_POINT ( 'NONE',  ( 50.36549662992289456, 18.84323467693539911, -76.14999999999999147 ) ) ;
#33418=ORIENTED_EDGE ( 'NONE', *, *, #47379, .T. ) ;
#33419=ORIENTED_EDGE ( 'NONE', *, *, #8769, .F. ) ;
#33422=ORIENTED_EDGE ( 'NONE', *, *, #36414, .F. ) ;
#33423=CARTESIAN_POINT ( 'NONE',  ( 61.49601566777620576, -45.18573077412970207, -46.83864831159979758 ) ) ;
#33425=CARTESIAN_POINT ( 'NONE',  ( 54.80487992904060235, -51.26385116109580053, -53.16356012067550552 ) ) ;
#33432=CARTESIAN_POINT ( 'NONE',  ( 55.72786029574290012, -51.09037789658940909, -53.93924188563359934 ) ) ;
#33433=DIRECTION ( 'NONE',  ( 0.000000000000000000, 0.000000000000000000, 1.000000000000000000 ) ) ;
#33438=CARTESIAN_POINT ( 'NONE',  ( 52.10718084980409515, -50.10817224434760675, -76.73077500979640320 ) ) ;
#33440=CARTESIAN_POINT ( 'NONE',  ( 60.70166025825290035, 14.30423153367579836, -47.08674219091739843 ) ) ;
#33444=CARTESIAN_POINT ( 'NONE',  ( 41.80335235802419902, 13.65426996821039829, -5.672373394308329431 ) ) ;
#33445=CARTESIAN_POINT ( 'NONE',  ( 43.68128689207919990, -43.54714580617979891, -5.037759820094009910 ) ) ;
#33448=CARTESIAN_POINT ( 'NONE',  ( 13.73527022026379996, 18.97497658877130178, -20.93080062776429884 ) ) ;
#33449=CARTESIAN_POINT ( 'NONE',  ( 65.70575104159891566, 1.626048249155310099, -18.95023426183129800 ) ) ;
#33450=ORIENTED_EDGE ( 'NONE', *, *, #8795, .T. ) ;
#33451=CARTESIAN_POINT ( 'NONE',  ( 13.80796782207779927, -52.11465364279959545, -75.47164421335219231 ) ) ;
#33452=ADVANCED_FACE ( 'NONE', ( #47858 ), #42755, .T. ) ;
#33453=CARTESIAN_POINT ( 'NONE',  ( 47.21413493457389876, -54.78279301590860229, -54.62721521096310084 ) ) ;
#33455=CARTESIAN_POINT ( 'NONE',  ( 11.20590614225525350, 32.84406522011376239, -44.01467685474590752 ) ) ;
#33458=CARTESIAN_POINT ( 'NONE',  ( 54.76549986477987630, -46.18104396004290635, -15.95313387964988472 ) ) ;
#33461=CARTESIAN_POINT ( 'NONE',  ( 13.99025901349430079, 19.94838289624579986, -22.90514568906469961 ) ) ;
#33463=VECTOR ( 'NONE', #22691, 1000.000000000000000 ) ;
#33464=CARTESIAN_POINT ( 'NONE',  ( 56.27102116988059777, 19.34483839479189982, -52.87264356866189985 ) ) ;
#33466=CARTESIAN_POINT ( 'NONE',  ( 48.03928511041160476, 23.04428228824039948, -54.71294081448219515 ) ) ;
#33468=ORIENTED_EDGE ( 'NONE', *, *, #42227, .F. ) ;
#33474=CARTESIAN_POINT ( 'NONE',  ( 83.73985275199801492, 13.43641148183490053, -47.11072319708490141 ) ) ;
#33475=CARTESIAN_POINT ( 'NONE',  ( 53.08725068471199648, 18.06569830069809868, -26.91751262120149590 ) ) ;
#33478=CIRCLE ( 'NONE', #19275, 2.000000000000070166 ) ;
#33479=CARTESIAN_POINT ( 'NONE',  ( 11.06646955189524029, 33.78253783233923713, -17.18453609578202190 ) ) ;
#33481=B_SPLINE_SURFACE_WITH_KNOTS ( 'NONE', 3, 3, ( 
 ( #27438, #43695, #4112, #27182, #3353, #15660, #51559, #35573, #31613, #43951, #44205, #39251 ),
 ( #24002, #7284, #40022, #19327, #51308, #11738, #15402, #43441, #8051, #20089, #47631, #437 ),
 ( #31356, #31872, #36080, #185, #7544, #43189, #12241, #32122, #27697, #19837, #3867, #4369 ),
 ( #16425, #28204, #11218, #19582, #7798, #48140, #8303, #32380, #23488, #23234, #47889, #51811 ) ),
 .UNSPECIFIED., .F., .F., .F.,
 ( 4, 4 ),
 ( 4, 1, 1, 1, 1, 1, 1, 1, 1, 4 ),
 ( -5.132488013533590632, -5.003182328417289604 ),
 ( 0.000000000000000000, 0.1111111111111110078, 0.2222222222222219878, 0.3333333333333329818, 0.4444444444444439757, 0.5555555555555560243, 0.6666666666666670737, 0.7777777777777779011, 0.8888888888888889506, 1.000000000000000000 ),
 .UNSPECIFIED. ) ;
#33486=CARTESIAN_POINT ( 'NONE',  ( 11.91426296010549990, -65.11770545154290346, -16.60966417101620252 ) ) ;
#33487=CARTESIAN_POINT ( 'NONE',  ( 12.64317103172330015, 34.24372746930500000, -47.41952126075570106 ) ) ;
#33489=CARTESIAN_POINT ( 'NONE',  ( 12.04090198311089921, 33.96751094227059298, -45.84253678999650106 ) ) ;
#33490=CARTESIAN_POINT ( 'NONE',  ( 12.89074585038019904, -65.51103569873420440, -47.72398483063609831 ) ) ;
#33493=CARTESIAN_POINT ( 'NONE',  ( 53.50527167498405845, 17.84081837129114234, -27.26089937317538769 ) ) ;
#33494=CARTESIAN_POINT ( 'NONE',  ( 53.15617301329960043, -49.54407833428120256, -49.11047178172640315 ) ) ;
#33495=CARTESIAN_POINT ( 'NONE',  ( 48.46496422664660031, 22.55782414888539833, -53.44104536398719318 ) ) ;
#33496=CARTESIAN_POINT ( 'NONE',  ( 61.57715961643649649, -1.766643160980349903, -16.00619826694699910 ) ) ;
#33497=CARTESIAN_POINT ( 'NONE',  ( 50.83387910135749621, -49.74010978817180018, -76.22448499253579257 ) ) ;
#33501=CARTESIAN_POINT ( 'NONE',  ( 53.00983118628400348, -49.38275580526859443, -27.01103834705430273 ) ) ;
#33503=EDGE_LOOP ( 'NONE', ( #35373, #26882, #26129, #17202, #48115, #10934 ) ) ;
#33505=CARTESIAN_POINT ( 'NONE',  ( -8.766062602303849260, -15.61618894467929941, 4.449999999999981526 ) ) ;
#33506=ADVANCED_FACE ( 'NONE', ( #8350 ), #20642, .F. ) ;
#33509=CARTESIAN_POINT ( 'NONE',  ( 55.37640121169410179, 19.59244258161170293, -75.41624985117930180 ) ) ;
#33510=CARTESIAN_POINT ( 'NONE',  ( 46.64206449348299799, -53.27165255397410704, -76.10218428122850298 ) ) ;
#33513=CARTESIAN_POINT ( 'NONE',  ( 56.13905073043380156, 14.31243755683419927, -17.10657833413849715 ) ) ;
#33515=CARTESIAN_POINT ( 'NONE',  ( 56.95883376355960337, -50.25507440355580258, -52.69722347720740174 ) ) ;
#33516=TOROIDAL_SURFACE ( 'NONE', #10938, 19.56371635397779940, 1.000000000000000000 ) ;
#33521=CARTESIAN_POINT ( 'NONE',  ( 46.95813824399459691, 22.72792253046040400, -75.76112237679920725 ) ) ;
#33523=CARTESIAN_POINT ( 'NONE',  ( 41.03170894472499697, -45.48949944206719920, -6.001457922227690034 ) ) ;
#33524=CARTESIAN_POINT ( 'NONE',  ( 53.35699421374690132, -49.92639189236809472, -74.14999999999999147 ) ) ;
#33526=ADVANCED_FACE ( 'NONE', ( #27482 ), #43834, .T. ) ;
#33527=CARTESIAN_POINT ( 'NONE',  ( 68.13393739769630031, -48.11618894467930119, -73.25000000000000000 ) ) ;
#33529=DIRECTION ( 'NONE',  ( -1.000000000000000000, -1.004313591354993529E-15, 0.000000000000000000 ) ) ;
#33531=CARTESIAN_POINT ( 'NONE',  ( 61.09392091072469810, 14.09871518747650043, -46.81036500987260496 ) ) ;
#33532=CARTESIAN_POINT ( 'NONE',  ( -33.78933650424870194, -20.47497671886300097, -57.07866011716559740 ) ) ;
#33533=VERTEX_POINT ( 'NONE', #12285 ) ;
#33534=CARTESIAN_POINT ( 'NONE',  ( 52.96856324676929262, -49.58863183502440108, -48.80184355050319311 ) ) ;
#33535=EDGE_LOOP ( 'NONE', ( #25518, #43807, #20236, #41496, #14932 ) ) ;
#33536=CARTESIAN_POINT ( 'NONE',  ( 57.90400457952389957, -45.28151604584450496, -25.97936526911970034 ) ) ;
#33537=CARTESIAN_POINT ( 'NONE',  ( 49.13578581667099598, -53.89835027320579997, -55.25235944000660027 ) ) ;
#33538=CARTESIAN_POINT ( 'NONE',  ( 13.48899612010369964, 19.59108034571840307, -21.59023847590369982 ) ) ;
#33539=CARTESIAN_POINT ( 'NONE',  ( 56.70205649827579464, 14.05047582634010084, -25.29386163676009858 ) ) ;
#33542=CARTESIAN_POINT ( 'NONE',  ( 53.03258583333429499, 18.34312913753139895, -48.98438925658670229 ) ) ;
#33543=CARTESIAN_POINT ( 'NONE',  ( 60.67083030670429622, -45.55276209844719659, -47.13425158708550100 ) ) ;
#33544=CARTESIAN_POINT ( 'NONE',  ( 47.20214428756302283, 22.74469374127451360, -75.65864031409697077 ) ) ;
#33545=ORIENTED_EDGE ( 'NONE', *, *, #38966, .F. ) ;
#33550=CARTESIAN_POINT ( 'NONE',  ( 47.41106868612380509, -54.65034373980500249, -54.82892287975980139 ) ) ;
#33553=CARTESIAN_POINT ( 'NONE',  ( 11.45636326040439990, -65.36476201173780964, -18.01147071083120110 ) ) ;
#33554=CARTESIAN_POINT ( 'NONE',  ( 53.20761889774500020, 18.23056977116540267, -48.79936051936330443 ) ) ;
#33555=CARTESIAN_POINT ( 'NONE',  ( 50.03007040746459921, 17.38381105532069881, -78.14999999999999147 ) ) ;
#33557=AXIS2_PLACEMENT_3D ( 'NONE', #41823, #46292, #1737 ) ;
#33562=CARTESIAN_POINT ( 'NONE',  ( 8.972284714083951229, -63.24474060077910309, -46.63284625306040709 ) ) ;
#33568=CARTESIAN_POINT ( 'NONE',  ( 51.63598265732919401, 19.13823475874330171, -76.35349669905959047 ) ) ;
#33569=ORIENTED_EDGE ( 'NONE', *, *, #20132, .T. ) ;
#33573=EDGE_CURVE ( 'NONE', #43431, #33091, #44482, .T. ) ;
#33576=CARTESIAN_POINT ( 'NONE',  ( 16.13393739769620083, -15.61618894467929941, -15.65000000000000036 ) ) ;
#33580=DIRECTION ( 'NONE',  ( 0.000000000000000000, 1.000000000000000000, 0.000000000000000000 ) ) ;
#33583=B_SPLINE_CURVE_WITH_KNOTS ( 'NONE', 3,
 ( #6162, #46907, #6805, #31390, #47162, #2871, #31134, #34819, #11250, #50823, #26958, #10732, #10477, #14913, #19615, #35339, #38779, #26432 ),
 .UNSPECIFIED., .F., .F.,
 ( 4, 2, 2, 2, 2, 2, 2, 2, 4 ),
 ( 0.000000000000000000, 0.2367787920637725030, 0.3749999997961399045, 0.4999999998369116239, 0.5624999998572962623, 0.6624999998899127052, 0.8224999999420987695, 0.9835460370430810784, 1.000000000000000000 ),
 .UNSPECIFIED. ) ;
#33584=CARTESIAN_POINT ( 'NONE',  ( 13.76193600395860095, 20.63771170940629673, -75.29799846200430125 ) ) ;
#33586=CARTESIAN_POINT ( 'NONE',  ( 44.89309739530899179, -45.25428046396859827, -7.755542271532889664 ) ) ;
#33592=VERTEX_POINT ( 'NONE', #43484 ) ;
#33593=CARTESIAN_POINT ( 'NONE',  ( 54.46658371067870519, -47.81044456346369742, -26.27512462187450026 ) ) ;
#33594=CARTESIAN_POINT ( 'NONE',  ( 55.98501704304129589, -50.87010798429000147, -74.79194691214389934 ) ) ;
#33595=CARTESIAN_POINT ( 'NONE',  ( 5.995642857577959894, 28.70634236700130160, -13.38692505553090051 ) ) ;
#33597=CARTESIAN_POINT ( 'NONE',  ( 52.33304160529149840, 14.99038499564479920, -14.16116536265050030 ) ) ;
#33599=CARTESIAN_POINT ( 'NONE',  ( -10.88446022757939957, -42.34476442307779820, -6.227089099853370335 ) ) ;
#33600=CARTESIAN_POINT ( 'NONE',  ( 47.43324995648460174, 23.39942513964739845, -54.73919042832569914 ) ) ;
#33601=DIRECTION ( 'NONE',  ( 0.000000000000000000, 0.000000000000000000, -1.000000000000000000 ) ) ;
#33603=CARTESIAN_POINT ( 'NONE',  ( 60.67373779709330250, 14.31886089341139900, -47.14825094286950247 ) ) ;
#33604=CARTESIAN_POINT ( 'NONE',  ( 11.93174564592089837, 34.20691397436080194, -17.93019396377509977 ) ) ;
#33605=CARTESIAN_POINT ( 'NONE',  ( 51.95832322464790565, 18.21933309198920270, -77.09973926587740323 ) ) ;
#33606=CARTESIAN_POINT ( 'NONE',  ( 53.13663690894949809, 18.26775922387509965, -48.80285956119419666 ) ) ;
#33608=DIRECTION ( 'NONE',  ( 0.000000000000000000, 0.000000000000000000, 1.000000000000000000 ) ) ;
#33609=CARTESIAN_POINT ( 'NONE',  ( 54.27276165828439503, 17.15419499903419975, -26.87182491303840237 ) ) ;
#33610=CARTESIAN_POINT ( 'NONE',  ( 52.83203762323750396, 21.09151004990239997, -54.28847891111020374 ) ) ;
#33612=CARTESIAN_POINT ( 'NONE',  ( 12.04669084400330092, -65.33956968768698914, -17.12210552323070090 ) ) ;
#33614=VERTEX_POINT ( 'NONE', #47429 ) ;
#33615=DIRECTION ( 'NONE',  ( -1.224646936193269808E-16, 1.000000000000000000, 3.054623595244969840E-12 ) ) ;
#33616=CARTESIAN_POINT ( 'NONE',  ( 10.77143137424659969, 32.00294380475830280, -45.20466975612399807 ) ) ;
#33619=CARTESIAN_POINT ( 'NONE',  ( 12.33744638055669363, 24.20302978297883811, -75.02878472494597872 ) ) ;
#33624=CARTESIAN_POINT ( 'NONE',  ( 11.90135363455309836, -65.25553501546980328, -46.97006170066550368 ) ) ;
#33625=CARTESIAN_POINT ( 'NONE',  ( 57.47999491983949838, -45.29966141242730515, -25.92515611446150103 ) ) ;
#33628=LINE ( 'NONE', #42028, #4192 ) ;
#33631=CARTESIAN_POINT ( 'NONE',  ( 75.08786029787904681, -6.316746508337682364, -11.49520958555957328 ) ) ;
#33632=ORIENTED_EDGE ( 'NONE', *, *, #8384, .T. ) ;
#33633=CARTESIAN_POINT ( 'NONE',  ( 48.66686317495700109, -45.95722105086829856, -11.36446868152489920 ) ) ;
#33636=CARTESIAN_POINT ( 'NONE',  ( 14.04279605691050037, 19.71127979334969993, -21.72007173762010268 ) ) ;
#33637=LINE ( 'NONE', #49654, #23433 ) ;
#33641=CARTESIAN_POINT ( 'NONE',  ( 46.40452006446609801, -53.01824288504249694, -76.14999999999999147 ) ) ;
#33642=CARTESIAN_POINT ( 'NONE',  ( 72.75000907364700709, 13.88381105527210124, -14.68250626227150057 ) ) ;
#33643=CARTESIAN_POINT ( 'NONE',  ( 46.46977925592499759, 13.88381105525470005, -8.151821053502690262 ) ) ;
#33645=CARTESIAN_POINT ( 'NONE',  ( 51.84413674030060548, 20.10506014047289725, -76.02231598272810231 ) ) ;
#33646=CARTESIAN_POINT ( 'NONE',  ( 61.60313986292270272, 13.88613617178600101, -27.62773227502630391 ) ) ;
#33648=ADVANCED_FACE ( 'NONE', ( #23534 ), #28246, .F. ) ;
#33649=ORIENTED_EDGE ( 'NONE', *, *, #51576, .F. ) ;
#33650=CARTESIAN_POINT ( 'NONE',  ( 68.13393739769620083, 18.13381105532069881, -75.00000000000000000 ) ) ;
#33652=CARTESIAN_POINT ( 'NONE',  ( 75.70738240145129794, -43.41214489997439330, -13.47559953613099992 ) ) ;
#33653=EDGE_CURVE ( 'NONE', #20243, #25615, #34301, .T. ) ;
#33657=FACE_OUTER_BOUND ( 'NONE', #34608, .T. ) ;
#33658=DIRECTION ( 'NONE',  ( -1.397030999999999991E-10, 0.000000000000000000, 1.000000000000000000 ) ) ;
#33660=CARTESIAN_POINT ( 'NONE',  ( 49.47431290566419904, -53.75415064111020058, -55.14222552823530776 ) ) ;
#33663=CARTESIAN_POINT ( 'NONE',  ( 54.39599759010950208, -51.37714874329260084, -53.12073448206449910 ) ) ;
#33669=CARTESIAN_POINT ( 'NONE',  ( 60.82607126368439765, -45.62681756021819979, -47.60724346531519302 ) ) ;
#33670=DIRECTION ( 'NONE',  ( -1.000000000000000000, 0.000000000000000000, 0.000000000000000000 ) ) ;
#33674=DIRECTION ( 'NONE',  ( 0.000000000000000000, 0.000000000000000000, -1.000000000000000000 ) ) ;
#33675=CYLINDRICAL_SURFACE ( 'NONE', #17734, 2.000000000000000888 ) ;
#33676=EDGE_LOOP ( 'NONE', ( #10247, #40538, #11103, #9421 ) ) ;
#33677=ORIENTED_EDGE ( 'NONE', *, *, #32075, .F. ) ;
#33681=CARTESIAN_POINT ( 'NONE',  ( 53.16328977476479878, -49.55862968577820027, -49.15589875833449440 ) ) ;
#33682=CARTESIAN_POINT ( 'NONE',  ( 49.31207000326343604, -53.03483995837590470, -52.41064504672193891 ) ) ;
#33683=CARTESIAN_POINT ( 'NONE',  ( 56.54475643210220426, -50.74241129021329755, -53.72841466469270699 ) ) ;
#33690=AXIS2_PLACEMENT_3D ( 'NONE', #41695, #25947, #22981 ) ;
#33694=CARTESIAN_POINT ( 'NONE',  ( 52.02578741164499831, -50.58705193961559843, -76.37778590614399832 ) ) ;
#33697=B_SPLINE_CURVE_WITH_KNOTS ( 'NONE', 3,
 ( #12060, #47196, #27245, #28011, #34856, #30912, #44018, #7099, #35890, #43761, #11283, #50855 ),
 .UNSPECIFIED., .F., .F.,
 ( 4, 2, 2, 2, 2, 4 ),
 ( 0.000000000000000000, 0.06094059512925743827, 0.2755827044638499701, 0.4977784882754372475, 0.7891864372720736043, 1.000000000000000000 ),
 .UNSPECIFIED. ) ;
#33699=CARTESIAN_POINT ( 'NONE',  ( 44.42525669626399321, 14.02755080800340082, -7.504247777814939901 ) ) ;
#33700=CARTESIAN_POINT ( 'NONE',  ( 41.14792718230170010, -44.23795256543909460, -3.958129521531580597 ) ) ;
#33701=CARTESIAN_POINT ( 'NONE',  ( 68.13393739769841773, -50.61618894467878960, -73.25000000000220268 ) ) ;
#33702=CARTESIAN_POINT ( 'NONE',  ( -8.870287765918970280, 13.09110620826400151, -5.844096418666690163 ) ) ;
#33705=CARTESIAN_POINT ( 'NONE',  ( 67.52398157331388973, 0.6199779298166340213, -18.22677178226010142 ) ) ;
#33706=B_SPLINE_SURFACE_WITH_KNOTS ( 'NONE', 3, 3, ( 
 ( #22320, #2416, #46207, #50388, #30705, #46727, #17638, #9777, #2166, #1907, #13712, #33605, #29666, #49619, #25728, #5841, #49871, #22060 ),
 ( #38070, #34111, #50122, #14472, #10292, #30445, #46466, #10554, #26511, #42527, #39110, #19175, #15512, #43043, #35684, #22833, #3465, #11849 ),
 ( #26770, #45, #50897, #51162, #42788, #47741, #3973, #3203, #35154, #19938, #6883, #38854, #16022, #14989, #43803, #51669, #15255, #2943 ),
 ( #31210, #15763, #27292, #27547, #27038, #19436, #47997, #31716, #7139, #7392, #11328, #27806, #7903, #3719, #18914, #30955, #19692, #34897 ),
 ( #23850, #31466, #39616, #46987, #39874, #11072, #23091, #43301, #47237, #23340, #23598, #39363, #35416, #51418, #47490, #11586, #43553, #35928 ),
 ( #31977, #7655, #48250, #12344, #540, #20702, #4735, #5268, #8940, #17316, #29092, #12097, #49035, #16526, #12874, #36693, #32476, #40378 ),
 ( #1063, #793, #28053, #48770, #45091, #32743, #48506, #28310, #24883, #44055, #4218, #36182, #33280, #16274, #28830, #40895, #5005, #13143 ),
 ( #44309, #8418, #12607, #16795, #44835, #21219, #20965, #8161, #9198, #24104, #25150, #28570, #36966, #17059, #44569, #4475, #33012, #41155 ),
 ( #40125, #37231, #1328, #20192, #8670, #289, #32227, #24366, #20444, #36432, #24625, #40636, #50057, #34047, #38005, #14153, #42463, #46403 ),
 ( #1584, #9963, #29606, #21484, #13393, #37483, #45357, #49296, #29351, #45609, #9459, #25408, #41411, #30378, #29855, #30121, #26447, #9708 ) ),
 .UNSPECIFIED., .F., .F., .F.,
 ( 4, 1, 1, 1, 1, 1, 1, 4 ),
 ( 4, 2, 2, 2, 2, 2, 2, 2, 4 ),
 ( -4.205109691999999775E-06, 0.1428571428571430157, 0.2857142857142860315, 0.4285714285714289917, 0.5714285714285709528, 0.7142857142857139685, 0.8571428571428569843, 1.000000000000000000 ),
 ( -2.552637841604540103, -2.105922750108249808, -1.595396022809280057, -1.276316818247430041, -1.116777215966499925, -0.9194146059286070205, -0.6036344298679829912, -0.09838614817098499665, 4.205109683999999746E-06 ),
 .UNSPECIFIED. ) ;
#33707=ORIENTED_EDGE ( 'NONE', *, *, #37649, .T. ) ;
#33708=CARTESIAN_POINT ( 'NONE',  ( 14.80174287272940070, -52.40466508994170169, -76.02664804518829555 ) ) ;
#33710=CARTESIAN_POINT ( 'NONE',  ( 47.21309542846500307, -54.78361656918900024, -54.62980748658569752 ) ) ;
#33711=EDGE_CURVE ( 'NONE', #41267, #260, #13830, .T. ) ;
#33714=CARTESIAN_POINT ( 'NONE',  ( 47.11354740527600171, -54.64978104499210332, -74.95188530402140259 ) ) ;
#33716=CARTESIAN_POINT ( 'NONE',  ( 8.133937397696209715, -59.33545798990849818, -21.14999999999999858 ) ) ;
#33718=CARTESIAN_POINT ( 'NONE',  ( 19.53299567489768407, -55.47150705052180086, -75.56421958049284626 ) ) ;
#33719=CARTESIAN_POINT ( 'NONE',  ( 48.25578050111359829, 22.93468281862570279, -54.69245131324669984 ) ) ;
#33721=TOROIDAL_SURFACE ( 'NONE', #7791, 30.50439988982899564, 1.000000000000000000 ) ;
#33725=CARTESIAN_POINT ( 'NONE',  ( 10.85466640530910176, -64.96697012893029921, -17.55961383758990024 ) ) ;
#33726=CARTESIAN_POINT ( 'NONE',  ( 82.91593256401816348, 14.33042927951009915, -47.63721988092869708 ) ) ;
#33728=CARTESIAN_POINT ( 'NONE',  ( 83.70962855682149950, 13.38540545388440073, -46.98048264170719790 ) ) ;
#33729=CARTESIAN_POINT ( 'NONE',  ( 52.82512926767439865, 18.35096675686759937, -27.26906326477469733 ) ) ;
#33731=CARTESIAN_POINT ( 'NONE',  ( 11.22384627824543557, 33.78040140241473921, -16.94931753701081334 ) ) ;
#33735=ORIENTED_EDGE ( 'NONE', *, *, #34452, .T. ) ;
#33736=ORIENTED_EDGE ( 'NONE', *, *, #10875, .T. ) ;
#33737=CARTESIAN_POINT ( 'NONE',  ( 12.26282170032640195, -64.61533680211610431, -15.83707920938230096 ) ) ;
#33738=CARTESIAN_POINT ( 'NONE',  ( 12.87771366368730064, 34.27547457673040299, -47.63452228340280215 ) ) ;
#33741=CARTESIAN_POINT ( 'NONE',  ( 12.13162406932769954, -65.41884435375050089, -47.52833373221270108 ) ) ;
#33746=CARTESIAN_POINT ( 'NONE',  ( 52.28488250037529639, 19.00519928096659683, -49.49583856337359578 ) ) ;
#33747=CARTESIAN_POINT ( 'NONE',  ( 63.46371119967039931, -1.000585159038779981, -16.34221528051200067 ) ) ;
#33748=CARTESIAN_POINT ( 'NONE',  ( 51.15450547264799752, -49.15030747453590010, -76.44814621741299732 ) ) ;
#33749=EDGE_CURVE ( 'NONE', #43574, #30462, #39143, .T. ) ;
#33750=CARTESIAN_POINT ( 'NONE',  ( 59.53688790405669806, -47.75280472282830146, -50.02630812161699936 ) ) ;
#33751=( BOUNDED_CURVE ( )  B_SPLINE_CURVE ( 3, ( #39456, #3554, #19524, #51504 ),
 .UNSPECIFIED., .F., .T. ) 
 B_SPLINE_CURVE_WITH_KNOTS ( ( 4, 4 ),
 ( 0.05097448463362189847, 0.2043272503186140121 ),
 .UNSPECIFIED. ) 
 CURVE ( )  GEOMETRIC_REPRESENTATION_ITEM ( )  RATIONAL_B_SPLINE_CURVE ( ( 1.000000000000000000, 0.9980412040773742888, 0.9980412040773742888, 1.000000000000000000 ) ) 
 REPRESENTATION_ITEM ( '' )  );
#33753=ADVANCED_FACE ( 'NONE', ( #33215 ), #9397, .T. ) ;
#33761=CARTESIAN_POINT ( 'NONE',  ( 68.13393739769708191, 17.98087126524488610, -74.20351669811759621 ) ) ;
#33762=CARTESIAN_POINT ( 'NONE',  ( 54.42316715427640617, 19.80705547073500128, -75.56251559860999123 ) ) ;
#33763=CARTESIAN_POINT ( 'NONE',  ( 47.49696547520699852, -54.38722354157379613, -75.00840848463889188 ) ) ;
#33765=CARTESIAN_POINT ( 'NONE',  ( 55.88393979655880628, 14.62082033763359945, -17.33319607435739940 ) ) ;
#33768=CARTESIAN_POINT ( 'NONE',  ( 56.87160283908409752, -50.28903218254829710, -52.71743054463500044 ) ) ;
#33769=CIRCLE ( 'NONE', #49700, 18.00000000000000355 ) ;
#33773=CARTESIAN_POINT ( 'NONE',  ( 46.60371894209130517, 22.01667934560690298, -76.11277936203079264 ) ) ;
#33774=DIRECTION ( 'NONE',  ( 0.000000000000000000, -1.000000000000000000, 0.000000000000000000 ) ) ;
#33775=EDGE_CURVE ( 'NONE', #24020, #10985, #21207, .T. ) ;
#33776=CARTESIAN_POINT ( 'NONE',  ( 75.29541660774471268, -36.36885601039063687, -12.50788449865524044 ) ) ;
#33779=CARTESIAN_POINT ( 'NONE',  ( 82.02429831058030629, -41.23866635630079713, -45.87976092105969883 ) ) ;
#33785=CARTESIAN_POINT ( 'NONE',  ( -33.45614285200539939, -10.80293933298100129, -56.47882598457800185 ) ) ;
#33786=VERTEX_POINT ( 'NONE', #21666 ) ;
#33787=CARTESIAN_POINT ( 'NONE',  ( 52.88990466204330687, -49.62977065132299970, -48.74279805905700158 ) ) ;
#33788=B_SPLINE_CURVE_WITH_KNOTS ( 'NONE', 3,
 ( #20622, #27972, #24284, #40304, #4396, #36883, #7824, #11764, #19859, #28493, #44493, #8595, #3895, #14070, #10142, #26103, #41589, #49979, #33962, #32930, #13309, #42110 ),
 .UNSPECIFIED., .F., .F.,
 ( 4, 2, 2, 2, 2, 2, 2, 2, 2, 2, 4 ),
 ( 0.000000000000000000, 0.04949999999865291322, 0.1774999999951696883, 0.2574999999929937777, 0.3374999999908167014, 0.4374999999880958557, 0.4999999999863959932, 0.6249999999829938258, 0.7432269898313242917, 0.8817545104238473375, 1.000000000000000000 ),
 .UNSPECIFIED. ) ;
#33793=CARTESIAN_POINT ( 'NONE',  ( 57.21713864038489561, 13.97813355815990022, -25.72061388221139921 ) ) ;
#33796=CARTESIAN_POINT ( 'NONE',  ( 52.71274604433429545, 18.50164618420620144, -48.58382401692190200 ) ) ;
#33799=CARTESIAN_POINT ( 'NONE',  ( 52.56521993351449851, 18.62941884369810097, -28.06240138782640159 ) ) ;
#33803=CARTESIAN_POINT ( 'NONE',  ( 47.42839689129279890, -54.63796168553609789, -54.78693215226149960 ) ) ;
#33804=PLANE ( 'NONE',  #41251 ) ;
#33806=CARTESIAN_POINT ( 'NONE',  ( 11.53916947328389853, -65.37687372592600354, -17.79819407340969661 ) ) ;
#33812=ORIENTED_EDGE ( 'NONE', *, *, #5224, .F. ) ;
#33813=CARTESIAN_POINT ( 'NONE',  ( 8.784728771152170879, -63.11543068638779630, -46.67204636145419983 ) ) ;
#33814=DIRECTION ( 'NONE',  ( 0.3918900565005459247, 0.9200120562340468044, 0.000000000000000000 ) ) ;
#33815=ORIENTED_EDGE ( 'NONE', *, *, #49, .T. ) ;
#33816=CARTESIAN_POINT ( 'NONE',  ( 63.88393739769619373, 11.88381105532070059, -61.44999999999999574 ) ) ;
#33817=CARTESIAN_POINT ( 'NONE',  ( 84.42051414645781904, 12.29857250479571107, -47.44928429649780810 ) ) ;
#33820=CARTESIAN_POINT ( 'NONE',  ( 51.42345381486639866, 19.32773741137469869, -76.23764488133839734 ) ) ;
#33821=ORIENTED_EDGE ( 'NONE', *, *, #41194, .T. ) ;
#33831=CARTESIAN_POINT ( 'NONE',  ( 56.60227008640750057, -46.16578870400680046, -26.26017074143819841 ) ) ;
#33834=CIRCLE ( 'NONE', #21262, 38.00000000000000000 ) ;
#33835=CARTESIAN_POINT ( 'NONE',  ( 14.15113475208380045, 20.32108400380180058, -75.32473453343510528 ) ) ;
#33838=CARTESIAN_POINT ( 'NONE',  ( 42.34709230781079725, -45.29983228306050336, -6.529037730685770313 ) ) ;
#33841=EDGE_LOOP ( 'NONE', ( #41146, #28133, #283, #4171 ) ) ;
#33842=CARTESIAN_POINT ( 'NONE',  ( 55.74091017665890035, -46.16737070784190422, -25.61914745244379787 ) ) ;
#33843=CARTESIAN_POINT ( 'NONE',  ( 15.72113303933780237, -51.10937407131510213, -21.50711442615979863 ) ) ;
#33844=CARTESIAN_POINT ( 'NONE',  ( 7.548220943605030264, 28.49602621674689829, -11.72997927153680031 ) ) ;
#33846=DIRECTION ( 'NONE',  ( 0.6888026391158372785, -0.7071067811865469066, 0.1598465650148877537 ) ) ;
#33847=DIRECTION ( 'NONE',  ( 0.6676418852213051869, -0.2329255526947263677, -0.7071067811865459074 ) ) ;
#33848=ORIENTED_EDGE ( 'NONE', *, *, #10313, .T. ) ;
#33849=CARTESIAN_POINT ( 'NONE',  ( -5.667588108579429296, -46.74622128715009950, -4.590257091596729566 ) ) ;
#33850=CARTESIAN_POINT ( 'NONE',  ( 47.49000820423450620, 23.36292359865809942, -54.73871130077979785 ) ) ;
#33852=DIRECTION ( 'NONE',  ( 0.000000000000000000, 0.000000000000000000, -1.000000000000000000 ) ) ;
#33854=CARTESIAN_POINT ( 'NONE',  ( 12.94102190407009978, 19.39887560817320278, -21.36191267119590265 ) ) ;
#33856=CARTESIAN_POINT ( 'NONE',  ( 11.31612274021629894, 33.84606982840180223, -16.97569932836579909 ) ) ;
#33859=CARTESIAN_POINT ( 'NONE',  ( 19.50973947245583773, 24.24110967164852681, -75.58682750963716046 ) ) ;
#33862=EDGE_CURVE ( 'NONE', #31554, #43574, #16773, .T. ) ;
#33864=CARTESIAN_POINT ( 'NONE',  ( 51.65752907925219972, 21.59180590640119846, -54.64640228080419604 ) ) ;
#33869=CARTESIAN_POINT ( 'NONE',  ( 11.10562983879290044, 32.14491805377860345, -44.25527573442839468 ) ) ;
#33871=CARTESIAN_POINT ( 'NONE',  ( 65.13280827392949845, -32.17956496334240057, -17.73393099564480124 ) ) ;
#33872=CARTESIAN_POINT ( 'NONE',  ( 12.51334738397835800, 24.21952903020473613, -75.31104072287740792 ) ) ;
#33873=ORIENTED_EDGE ( 'NONE', *, *, #19580, .T. ) ;
#33877=CARTESIAN_POINT ( 'NONE',  ( 76.55364060230128587, -0.04733056874654922169, -13.45856357439038575 ) ) ;
#33879=CARTESIAN_POINT ( 'NONE',  ( 11.26949083597030032, -64.33764097384030833, -44.85617399231739455 ) ) ;
#33880=CARTESIAN_POINT ( 'NONE',  ( 57.17215292315320596, -45.78104736118029905, -26.23432769010419818 ) ) ;
#33887=EDGE_CURVE ( 'NONE', #42086, #47971, #31793, .T. ) ;
#33888=ORIENTED_EDGE ( 'NONE', *, *, #23885, .F. ) ;
#33889=CARTESIAN_POINT ( 'NONE',  ( 48.84046368175200570, -45.57708435644870093, -11.11574200907650045 ) ) ;
#33891=CARTESIAN_POINT ( 'NONE',  ( 16.20840964857710276, 19.86086910830300312, -20.73468313311569844 ) ) ;
#33895=CARTESIAN_POINT ( 'NONE',  ( 47.10254288570079950, -54.62488891218850284, -75.00961804031550173 ) ) ;
#33896=CARTESIAN_POINT ( 'NONE',  ( 56.60991603741530298, 12.53331740833790064, -8.242952450017121180 ) ) ;
#33900=CARTESIAN_POINT ( 'NONE',  ( 51.61430880713380276, 19.94292765148920310, -76.09751503388891081 ) ) ;
#33901=CARTESIAN_POINT ( 'NONE',  ( 57.86705690550169834, 14.17621725492490015, -26.12831864294430062 ) ) ;
#33903=ORIENTED_EDGE ( 'NONE', *, *, #31199, .T. ) ;
#33904=CARTESIAN_POINT ( 'NONE',  ( 18.06932202639930196, -55.56934008872529773, -76.14999999999999147 ) ) ;
#33905=CARTESIAN_POINT ( 'NONE',  ( -10.96582629949129917, -41.77786732616849719, -5.028156413135709712 ) ) ;
#33906=CARTESIAN_POINT ( 'NONE',  ( 15.52232235369950075, -50.77489110054699495, -15.65194195389930165 ) ) ;
#33912=CARTESIAN_POINT ( 'NONE',  ( 19.75452607920933090, 24.21953045971935126, -75.31104306443889129 ) ) ;
#33914=CARTESIAN_POINT ( 'NONE',  ( 76.44596060521568859, -43.25290919633437881, -14.01301206241809183 ) ) ;
#33915=CARTESIAN_POINT ( 'NONE',  ( 17.99229861434620048, -51.11617952483079108, -74.35192203308130843 ) ) ;
#33916=CARTESIAN_POINT ( 'NONE',  ( 57.33235504379430125, 13.88381105532070059, -16.73838572529449920 ) ) ;
#33917=EDGE_CURVE ( 'NONE', #24512, #37059, #34612, .T. ) ;
#33924=DIRECTION ( 'NONE',  ( 0.000000000000000000, 1.000000000000000000, 0.000000000000000000 ) ) ;
#33928=VECTOR ( 'NONE', #17741, 1000.000000000000114 ) ;
#33930=CARTESIAN_POINT ( 'NONE',  ( 44.37469554261519988, -46.00068073351109632, -8.485651053198388638 ) ) ;
#33932=AXIS2_PLACEMENT_3D ( 'NONE', #15688, #24290, #35336 ) ;
#33935=CARTESIAN_POINT ( 'NONE',  ( 61.16510488283689995, -45.29379779991980115, -46.73120355716090302 ) ) ;
#33936=CARTESIAN_POINT ( 'NONE',  ( 51.96920254651271165, -50.49588334902367848, -49.26033372652806008 ) ) ;
#33937=CARTESIAN_POINT ( 'NONE',  ( 54.94181551684279441, -51.40389681108650421, -53.69988726361309972 ) ) ;
#33946=CARTESIAN_POINT ( 'NONE',  ( 53.61341843579059940, -50.67945576140650132, -76.60108205910400159 ) ) ;
#33947=CARTESIAN_POINT ( 'NONE',  ( 60.26025110216900060, 14.55536647234960057, -47.43140372362420010 ) ) ;
#33949=DIRECTION ( 'NONE',  ( 0.000000000000000000, 0.000000000000000000, -1.000000000000000000 ) ) ;
#33950=CARTESIAN_POINT ( 'NONE',  ( 41.24357956626280242, 13.71928266329340040, -5.592244466849718876 ) ) ;
#33951=CARTESIAN_POINT ( 'NONE',  ( 42.16710579205339826, -43.32203614284970428, -3.592545294820050472 ) ) ;
#33955=AXIS2_PLACEMENT_3D ( 'NONE', #26897, #15631, #31329 ) ;
#33957=CARTESIAN_POINT ( 'NONE',  ( 57.24929578595760660, -50.61618894467929408, -75.24227954305044364 ) ) ;
#33960=CARTESIAN_POINT ( 'NONE',  ( 15.05440318628160057, -53.11618894467930119, -76.14999999999999147 ) ) ;
#33961=CARTESIAN_POINT ( 'NONE',  ( 57.24929575387970004, 19.38381105532069881, -53.91492787281829635 ) ) ;
#33962=CARTESIAN_POINT ( 'NONE',  ( 9.063308985759819691, 32.62929763576821074, -46.73460937115434888 ) ) ;
#33964=DIRECTION ( 'NONE',  ( 0.6415444970810866288, 0.4854844151940982400, 0.5939070136550167467 ) ) ;
#33966=CARTESIAN_POINT ( 'NONE',  ( 47.92547496200619861, -54.35536316263760170, -54.78476778173359918 ) ) ;
#33970=CARTESIAN_POINT ( 'NONE',  ( 56.45988843467819862, 19.49067611367820163, -53.39311502846720003 ) ) ;
#33972=CARTESIAN_POINT ( 'NONE',  ( 48.03391530370259943, 23.06771420177449983, -54.78057301038420235 ) ) ;
#33975=VERTEX_POINT ( 'NONE', #4807 ) ;
#33977=CARTESIAN_POINT ( 'NONE',  ( 82.75389222264627165, 14.36253673539014919, -47.67224619643947392 ) ) ;
#33980=CARTESIAN_POINT ( 'NONE',  ( 83.63395638909621255, 13.75389496877540019, -47.37153147893519645 ) ) ;
#33984=CARTESIAN_POINT ( 'NONE',  ( 56.87513795754310308, -45.11618894467940066, -15.74603272341079929 ) ) ;
#33991=CARTESIAN_POINT ( 'NONE',  ( 12.07459604304269973, -64.83039640760800637, -16.11467485433340130 ) ) ;
#33992=CARTESIAN_POINT ( 'NONE',  ( 54.47259832750690123, 15.01994964729280113, -15.76422791930239953 ) ) ;
#33994=CARTESIAN_POINT ( 'NONE',  ( 10.23245083239389963, -64.79111536624868961, -47.03631047207230154 ) ) ;
#33996=VERTEX_POINT ( 'NONE', #36505 ) ;
#34000=AXIS2_PLACEMENT_3D ( 'NONE', #40260, #44188, #32105 ) ;
#34002=CARTESIAN_POINT ( 'NONE',  ( 53.48928929932589682, -49.41396641409689749, -49.16886795839930357 ) ) ;
#34003=CARTESIAN_POINT ( 'NONE',  ( 49.97469255755120088, 21.36656799640790183, -52.61615532409420126 ) ) ;
#34006=CARTESIAN_POINT ( 'NONE',  ( 51.12541109982870324, -49.03592882882020376, -76.44562399636079419 ) ) ;
#34007=CARTESIAN_POINT ( 'NONE',  ( 56.54805895952080164, -50.43678705299419818, -52.80479669090900785 ) ) ;
#34010=CARTESIAN_POINT ( 'NONE',  ( 68.13393739769630031, 16.88381105532149817, -68.79999999999999716 ) ) ;
#34015=CARTESIAN_POINT ( 'NONE',  ( 13.11803215473759998, -50.90931609213659925, -21.59044441884969956 ) ) ;
#34016=CARTESIAN_POINT ( 'NONE',  ( 56.83869077455450025, 19.41466794163520149, -74.56788156747980167 ) ) ;
#34017=CARTESIAN_POINT ( 'NONE',  ( 47.39162735359639811, -54.25023534817900384, -75.29717685666371096 ) ) ;
#34019=CARTESIAN_POINT ( 'NONE',  ( 55.89836899175390528, 14.67647375536889953, -17.62829706286229836 ) ) ;
#34022=AXIS2_PLACEMENT_3D ( 'NONE', #4025, #44111, #12398 ) ;
#34024=FACE_OUTER_BOUND ( 'NONE', #28381, .T. ) ;
#34027=CARTESIAN_POINT ( 'NONE',  ( 47.53482544724619885, 23.16677569099900325, -74.95177798121650881 ) ) ;
#34029=CARTESIAN_POINT ( 'NONE',  ( 75.16169728866853461, -29.51520510724298063, -11.85453094363455406 ) ) ;
#34031=CARTESIAN_POINT ( 'NONE',  ( 60.14258131274579000, -45.11618894467940066, -25.78020576970689959 ) ) ;
#34033=FACE_OUTER_BOUND ( 'NONE', #28452, .T. ) ;
#34035=CARTESIAN_POINT ( 'NONE',  ( 84.19224659786166853, -44.53040250705239345, -48.96577344625911365 ) ) ;
#34039=CARTESIAN_POINT ( 'NONE',  ( -32.29328640865499978, -10.93117069805279939, -55.80050612416169997 ) ) ;
#34040=ORIENTED_EDGE ( 'NONE', *, *, #13028, .T. ) ;
#34041=CARTESIAN_POINT ( 'NONE',  ( 52.71234499349689884, -49.73836072086629656, -48.66396021830070140 ) ) ;
#34042=ORIENTED_EDGE ( 'NONE', *, *, #2728, .T. ) ;
#34043=CARTESIAN_POINT ( 'NONE',  ( 17.27855009702555122, 21.70055148386360244, -76.14999999999999147 ) ) ;
#34045=CARTESIAN_POINT ( 'NONE',  ( 57.64963559888369815, 13.88883635462039834, -25.41607447946719844 ) ) ;
#34047=CARTESIAN_POINT ( 'NONE',  ( 50.75795695721529910, 19.32138164550209680, -76.14999999999999147 ) ) ;
#34048=CARTESIAN_POINT ( 'NONE',  ( 53.26968212669260083, 18.27860782879199775, -49.16957734417170656 ) ) ;
#34055=CARTESIAN_POINT ( 'NONE',  ( 54.37486050126969417, 17.76197798406979800, -48.98148910212459839 ) ) ;
#34056=FACE_OUTER_BOUND ( 'NONE', #3348, .T. ) ;
#34058=( BOUNDED_CURVE ( )  B_SPLINE_CURVE ( 3, ( #29659, #1380, #9767, #1638 ),
 .UNSPECIFIED., .F., .T. ) 
 B_SPLINE_CURVE_WITH_KNOTS ( ( 4, 4 ),
 ( 1.755576258187430128, 3.141592653589798445 ),
 .UNSPECIFIED. ) 
 CURVE ( )  GEOMETRIC_REPRESENTATION_ITEM ( )  RATIONAL_B_SPLINE_CURVE ( ( 1.000000000000000000, 0.8462184657327374016, 0.8462184657327374016, 1.000000000000000000 ) ) 
 REPRESENTATION_ITEM ( '' )  );
#34059=CARTESIAN_POINT ( 'NONE',  ( 10.75976506911110064, -64.96659187203999863, -18.06526995554730064 ) ) ;
#34060=CARTESIAN_POINT ( 'NONE',  ( 52.84731125486479897, 18.41934504040209930, -48.60966020774090168 ) ) ;
#34063=FACE_OUTER_BOUND ( 'NONE', #28044, .T. ) ;
#34066=CARTESIAN_POINT ( 'NONE',  ( 9.288932741751329658, -63.21985741985628948, -46.53007890215199893 ) ) ;
#34067=DIRECTION ( 'NONE',  ( 0.3294064756440890918, -0.9441882088883233326, 0.000000000000000000 ) ) ;
#34068=ORIENTED_EDGE ( 'NONE', *, *, #37487, .T. ) ;
#34071=CARTESIAN_POINT ( 'NONE',  ( 57.05931827775219745, 19.36066449068759709, -53.44572518222490487 ) ) ;
#34073=CARTESIAN_POINT ( 'NONE',  ( 53.89956157026149697, 19.40017492853139913, -76.79736723946669485 ) ) ;
#34075=CARTESIAN_POINT ( 'NONE',  ( 11.09843494245553330, -65.15652262322491595, -47.26083285147826984 ) ) ;
#34077=CARTESIAN_POINT ( 'NONE',  ( 58.88690644461912882, 17.44024477555941743, -51.02974587662403394 ) ) ;
#34084=VERTEX_POINT ( 'NONE', #32816 ) ;
#34085=CARTESIAN_POINT ( 'NONE',  ( 56.78239028773929675, -46.02921025412519640, -26.24769687010520158 ) ) ;
#34088=CARTESIAN_POINT ( 'NONE',  ( 13.64650866220840086, 20.52576179366219833, -75.06145659859170394 ) ) ;
#34090=CARTESIAN_POINT ( 'NONE',  ( 41.21726802631610553, -44.82489126183570249, -5.423354306796420055 ) ) ;
#34094=CARTESIAN_POINT ( 'NONE',  ( 54.00053677488939741, -48.28078295432670330, -26.32878014593650207 ) ) ;
#34095=CARTESIAN_POINT ( 'NONE',  ( 54.28170228800039609, -50.73610625031639643, -76.21973480364219711 ) ) ;
#34096=CARTESIAN_POINT ( 'NONE',  ( 7.952424752720789414, 30.74922443327189825, -15.01216219166649957 ) ) ;
#34098=EDGE_CURVE ( 'NONE', #51131, #41037, #12861, .T. ) ;
#34099=B_SPLINE_CURVE_WITH_KNOTS ( 'NONE', 3,
 ( #41776, #31184, #5878, #43278, #22101, #29961, #26033, #3441, #42041, #7368, #21847, #37852, #1948, #19412, #17927, #34151, #51390, #45458 ),
 .UNSPECIFIED., .F., .F.,
 ( 4, 2, 2, 2, 2, 2, 2, 2, 4 ),
 ( 0.000000000000000000, 0.09835926191934898921, 0.6036208803096320130, 0.9194093918035598501, 1.116777211487260058, 1.276316813128300032, 1.595396016410379980, 2.105922741661700126, 2.552633626256600063 ),
 .UNSPECIFIED. ) ;
#34103=CARTESIAN_POINT ( 'NONE',  ( -7.464592885573059888, -45.40146952839990035, -4.956245330965249885 ) ) ;
#34104=ADVANCED_FACE ( 'NONE', ( #48582 ), #8745, .F. ) ;
#34105=CARTESIAN_POINT ( 'NONE',  ( 47.44105247587240370, 23.39273938256710039, -54.71914698481260331 ) ) ;
#34108=CARTESIAN_POINT ( 'NONE',  ( 84.25370905176697534, -44.18318147193002687, -47.43624044261927963 ) ) ;
#34109=CARTESIAN_POINT ( 'NONE',  ( 12.08205748224539988, 34.04687831868819359, -16.92411159752879968 ) ) ;
#34111=CARTESIAN_POINT ( 'NONE',  ( 51.62357988847060142, 17.46062716628840050, -76.93789418233430411 ) ) ;
#34113=LINE ( 'NONE', #26513, #37599 ) ;
#34115=CARTESIAN_POINT ( 'NONE',  ( 55.42636091632299866, 15.84296872918980092, -26.34129395571439858 ) ) ;
#34116=VECTOR ( 'NONE', #20775, 1000.000000000000000 ) ;
#34117=CARTESIAN_POINT ( 'NONE',  ( 54.40370209750609831, 20.40074845781530044, -53.77986364435489719 ) ) ;
#34119=CARTESIAN_POINT ( 'NONE',  ( 53.51287195967390176, 18.19965013284789990, -49.22146522496750265 ) ) ;
#34120=CARTESIAN_POINT ( 'NONE',  ( 10.10517893431099878, 23.92687708958460036, -21.14999999999999858 ) ) ;
#34122=CARTESIAN_POINT ( 'NONE',  ( 10.97956612247109831, 32.13351753698560032, -44.74505020633399965 ) ) ;
#34123=DIRECTION ( 'NONE',  ( 0.07088902009066748444, 0.000000000000000000, 0.9974842088126432138 ) ) ;
#34125=CARTESIAN_POINT ( 'NONE',  ( 65.88922314972060690, -31.40957022853389802, -17.14610387725419827 ) ) ;
#34127=EDGE_LOOP ( 'NONE', ( #45893, #19105, #15874, #9931 ) ) ;
#34128=EDGE_LOOP ( 'NONE', ( #19633, #14296, #29552, #19061, #38226, #49212 ) ) ;
#34129=LINE ( 'NONE', #2184, #32850 ) ;
#34131=ORIENTED_EDGE ( 'NONE', *, *, #12996, .F. ) ;
#34133=CARTESIAN_POINT ( 'NONE',  ( 12.94913857733849838, -65.51469239313858850, -47.64817528796799451 ) ) ;
#34134=CARTESIAN_POINT ( 'NONE',  ( 56.65742313423940146, -46.03143560913069621, -26.22917644616859789 ) ) ;
#34138=ORIENTED_EDGE ( 'NONE', *, *, #25572, .T. ) ;
#34139=DIRECTION ( 'NONE',  ( 0.000000000000000000, 0.000000000000000000, -1.000000000000000000 ) ) ;
#34141=ORIENTED_EDGE ( 'NONE', *, *, #13335, .T. ) ;
#34142=CARTESIAN_POINT ( 'NONE',  ( 48.98108981356519820, -45.96115812557660973, -11.58776272563040166 ) ) ;
#34144=CARTESIAN_POINT ( 'NONE',  ( 14.79734571144840061, 19.88381641708039993, -22.20703854454670179 ) ) ;
#34145=DIRECTION ( 'NONE',  ( 0.000000000000000000, -1.000000000000000000, 0.000000000000000000 ) ) ;
#34148=CARTESIAN_POINT ( 'NONE',  ( 46.35275103504449845, -52.90993241930539881, -76.14999999999999147 ) ) ;
#34149=CARTESIAN_POINT ( 'NONE',  ( 57.73378796211289909, 13.88381105527449932, -10.52255156732080010 ) ) ;
#34151=CARTESIAN_POINT ( 'NONE',  ( 50.04022705227350087, -48.91488703454379561, -76.14999999999999147 ) ) ;
#34152=FACE_OUTER_BOUND ( 'NONE', #13334, .T. ) ;
#34153=CARTESIAN_POINT ( 'NONE',  ( 51.19516202202900246, 19.86383965925769957, -76.13919812682919996 ) ) ;
#34154=CARTESIAN_POINT ( 'NONE',  ( 61.66480336386660355, 13.88597247968120030, -28.02007549380890339 ) ) ;
#34158=CARTESIAN_POINT ( 'NONE',  ( -3.057385712928159638, -49.07295275241269650, -5.614604985102389811 ) ) ;
#34159=DIRECTION ( 'NONE',  ( 1.000000000000000000, 0.000000000000000000, 0.000000000000000000 ) ) ;
#34166=CARTESIAN_POINT ( 'NONE',  ( 42.80229243930720173, 11.48401673206149987, -3.540423289874710111 ) ) ;
#34169=CARTESIAN_POINT ( 'NONE',  ( 60.34379259250669492, 14.63564649040839960, -47.72732609510669732 ) ) ;
#34171=CARTESIAN_POINT ( 'NONE',  ( 76.04613871463565999, -43.31687852089314816, -13.66319593086862305 ) ) ;
#34172=DIRECTION ( 'NONE',  ( 0.000000000000000000, -1.000000000000000000, 0.000000000000000000 ) ) ;
#34173=ORIENTED_EDGE ( 'NONE', *, *, #15430, .T. ) ;
#34177=CARTESIAN_POINT ( 'NONE',  ( 10.64863409883700029, 32.21085600226960111, -23.66469670114080159 ) ) ;
#34178=DIRECTION ( 'NONE',  ( 0.000000000000000000, 0.000000000000000000, -1.000000000000000000 ) ) ;
#34179=DIRECTION ( 'NONE',  ( 0.000000000000000000, 0.000000000000000000, 1.000000000000000000 ) ) ;
#34180=AXIS2_PLACEMENT_3D ( 'NONE', #51703, #15794, #11109 ) ;
#34186=ORIENTED_EDGE ( 'NONE', *, *, #23512, .T. ) ;
#34189=ORIENTED_EDGE ( 'NONE', *, *, #46584, .T. ) ;
#34190=CARTESIAN_POINT ( 'NONE',  ( 61.43875230760810524, -45.16919861524459634, -46.56425532763250175 ) ) ;
#34191=CARTESIAN_POINT ( 'NONE',  ( 28.36591740443274290, -6.729135268073950904, -6.721843382729280059 ) ) ;
#34192=EDGE_LOOP ( 'NONE', ( #25720, #17438, #45409, #9555, #12956 ) ) ;
#34194=DIRECTION ( 'NONE',  ( 0.9999999999999997780, 2.292180684128748550E-25, 1.129617809262089834E-08 ) ) ;
#34198=CARTESIAN_POINT ( 'NONE',  ( 16.15069188244332210, 19.81939201856824795, -15.66900176635303232 ) ) ;
#34199=CARTESIAN_POINT ( 'NONE',  ( 52.01032223484130412, -50.03877910798939865, -76.70782219912229039 ) ) ;
#34200=CARTESIAN_POINT ( 'NONE',  ( 60.96305650301830070, 14.21870589704430010, -47.29791441411810382 ) ) ;
#34201=EDGE_CURVE ( 'NONE', #12115, #36299, #32995, .T. ) ;
#34205=CARTESIAN_POINT ( 'NONE',  ( 41.72083574932489825, 13.70929892781999904, -5.743067283000420353 ) ) ;
#34206=CARTESIAN_POINT ( 'NONE',  ( 42.84544925522080661, -42.99895311139940191, -4.190148907760479879 ) ) ;
#34207=EDGE_CURVE ( 'NONE', #37478, #1545, #37959, .T. ) ;
#34210=AXIS2_PLACEMENT_3D ( 'NONE', #390, #32847, #41259 ) ;
#34212=DIRECTION ( 'NONE',  ( 0.000000000000000000, 1.000000000000000000, 0.000000000000000000 ) ) ;
#34213=AXIS2_PLACEMENT_3D ( 'NONE', #19393, #8120, #35374 ) ;
#34217=CARTESIAN_POINT ( 'NONE',  ( 57.29802881897539635, 19.33020836189830050, -53.44853715813179917 ) ) ;
#34220=CARTESIAN_POINT ( 'NONE',  ( 0.5716597377992500562, -15.61618894406255365, -7.050000000025706370 ) ) ;
#34221=CARTESIAN_POINT ( 'NONE',  ( 46.95605112289660354, -54.29280230291429632, -75.52284329973289800 ) ) ;
#34224=CARTESIAN_POINT ( 'NONE',  ( 48.22078997057410277, -54.22619954268040487, -54.83130601189450459 ) ) ;
#34226=CARTESIAN_POINT ( 'NONE',  ( 56.50147281689449841, 19.49859888707450040, -53.50280580149869536 ) ) ;
#34227=CARTESIAN_POINT ( 'NONE',  ( 47.94837612362730539, 23.09355010960259946, -54.72220175608870107 ) ) ;
#34234=CARTESIAN_POINT ( 'NONE',  ( 83.54413676250729281, 13.61283532876010050, -47.09683803678880309 ) ) ;
#34235=CARTESIAN_POINT ( 'NONE',  ( 55.95580150607140268, 14.65510410099619953, -25.57470036468859931 ) ) ;
#34239=CARTESIAN_POINT ( 'NONE',  ( 56.55522355860080097, -46.21195502513410247, -26.26695352263039851 ) ) ;
#34240=ORIENTED_EDGE ( 'NONE', *, *, #45715, .F. ) ;
#34242=ORIENTED_EDGE ( 'NONE', *, *, #48882, .T. ) ;
#34243=ORIENTED_EDGE ( 'NONE', *, *, #13315, .T. ) ;
#34244=CARTESIAN_POINT ( 'NONE',  ( 12.27153357073309969, -64.61912752036219842, -15.84005975574299896 ) ) ;
#34247=CARTESIAN_POINT ( 'NONE',  ( -33.14629235451220524, -5.854914153751970218, -57.60079496986291048 ) ) ;
#34250=ORIENTED_EDGE ( 'NONE', *, *, #14293, .T. ) ;
#34252=VECTOR ( 'NONE', #11390, 1000.000000000000000 ) ;
#34253=ORIENTED_EDGE ( 'NONE', *, *, #22299, .F. ) ;
#34255=CARTESIAN_POINT ( 'NONE',  ( 82.24885320877977790, -45.11618894467940066, -46.39516212021803909 ) ) ;
#34256=CIRCLE ( 'NONE', #25050, 1.399999999999998579 ) ;
#34258=FACE_OUTER_BOUND ( 'NONE', #33503, .T. ) ;
#34259=CARTESIAN_POINT ( 'NONE',  ( 51.38511839723819463, -50.11055703386340099, -76.33916260165409540 ) ) ;
#34260=CARTESIAN_POINT ( 'NONE',  ( 57.45637359078290274, -50.19905859961199468, -52.69494871447199813 ) ) ;
#34261=EDGE_LOOP ( 'NONE', ( #32748, #32310 ) ) ;
#34263=CARTESIAN_POINT ( 'NONE',  ( 65.43393739769584272, 16.88381105532339532, -68.79999999999942872 ) ) ;
#34266=CARTESIAN_POINT ( 'NONE',  ( 53.97718803714800373, -49.20306630607990428, -49.10491108831829621 ) ) ;
#34269=CARTESIAN_POINT ( 'NONE',  ( 13.08122484219250126, -50.91564157304479465, -21.57315878215120009 ) ) ;
#34270=CARTESIAN_POINT ( 'NONE',  ( 55.69862941132319634, 19.50294859112689849, -75.44272654099910369 ) ) ;
#34271=CARTESIAN_POINT ( 'NONE',  ( 47.61398272666360043, -54.53961310099680304, -74.36298856109941369 ) ) ;
#34273=CARTESIAN_POINT ( 'NONE',  ( 56.92544927513679909, 13.88381105532070059, -16.01979077684439901 ) ) ;
#34280=CARTESIAN_POINT ( 'NONE',  ( 47.36202810124689933, 22.97939671731930034, -75.36156497780129371 ) ) ;
#34282=CARTESIAN_POINT ( 'NONE',  ( 20.03604369380067851, -55.13509060654741489, -18.97520576177407037 ) ) ;
#34283=B_SPLINE_CURVE_WITH_KNOTS ( 'NONE', 3,
 ( #31083, #11200, #24760, #49176, #21356, #32361, #25542, #48646, #33149, #33413, #45230, #44703, #37103, #9338, #37359, #41289, #940, #48914 ),
 .UNSPECIFIED., .F., .F.,
 ( 4, 2, 2, 2, 2, 2, 2, 2, 4 ),
 ( -2.552633636494849867, -2.105922750108249808, -1.595396022809280279, -1.276316818247430041, -1.116777215966499925, -0.9194146059286070205, -0.6036344298679827691, -0.09838614817098489951, 2.220446049250313081E-15 ),
 .UNSPECIFIED. ) ;
#34285=CARTESIAN_POINT ( 'NONE',  ( 75.14303606280716963, -28.31058215067825756, -11.76413862553087952 ) ) ;
#34286=CARTESIAN_POINT ( 'NONE',  ( 12.88498222292095008, -65.50776629007216911, -23.37250852991978078 ) ) ;
#34287=CIRCLE ( 'NONE', #10035, 1.999999999999997113 ) ;
#34288=CYLINDRICAL_SURFACE ( 'NONE', #8082, 2.000000000000001776 ) ;
#34289=CIRCLE ( 'NONE', #11732, 21.50000000000000000 ) ;
#34290=AXIS2_PLACEMENT_3D ( 'NONE', #15143, #11479, #3610 ) ;
#34294=CARTESIAN_POINT ( 'NONE',  ( 82.13853704237929776, 13.94246732026510038, -46.86219204859769860 ) ) ;
#34296=FACE_OUTER_BOUND ( 'NONE', #7304, .T. ) ;
#34301=B_SPLINE_CURVE_WITH_KNOTS ( 'NONE', 3,
 ( #43992, #44244, #40318, #36369, #4414, #40572, #477, #17756, #40833, #49232, #1001, #25597 ),
 .UNSPECIFIED., .F., .F.,
 ( 4, 2, 2, 2, 2, 4 ),
 ( -1.480557223830589963, -1.376569949160200146, -1.265367455784349948, -1.042962469032639783, -0.6871144902299088919, -0.6744302025021630120 ),
 .UNSPECIFIED. ) ;
#34302=CARTESIAN_POINT ( 'NONE',  ( -31.82194261889170050, -6.201200042654750000, -55.69495912570319973 ) ) ;
#34304=CARTESIAN_POINT ( 'NONE',  ( 53.19708396731179789, -49.47972728580509738, -48.94481821072159278 ) ) ;
#34308=CARTESIAN_POINT ( 'NONE',  ( 13.99922743840360084, 19.91584326097130031, -22.43849254327080089 ) ) ;
#34309=CARTESIAN_POINT ( 'NONE',  ( 55.93328256272239685, 14.78258593416649980, -25.74340590685439878 ) ) ;
#34311=DIRECTION ( 'NONE',  ( -0.6047562208151086027, -0.7964106436916998932, 0.000000000000000000 ) ) ;
#34312=CARTESIAN_POINT ( 'NONE',  ( 52.67785519474879408, 18.53209731767190149, -48.65292259172070288 ) ) ;
#34313=CARTESIAN_POINT ( 'NONE',  ( 56.06628350373850367, -45.70557515080610500, -17.61155996636929899 ) ) ;
#34314=DIRECTION ( 'NONE',  ( -0.9151634328772870752, -0.3898247278253974546, -0.1025308378007029897 ) ) ;
#34317=CARTESIAN_POINT ( 'NONE',  ( 11.88236604821880071, -65.43512709907859914, -17.91369388827580167 ) ) ;
#34318=CARTESIAN_POINT ( 'NONE',  ( 10.05382147007509985, 33.36697451426490346, -46.89254338722109594 ) ) ;
#34320=CARTESIAN_POINT ( 'NONE',  ( 10.62398834541929915, -64.83239605773999870, -18.14938726570430205 ) ) ;
#34322=DIRECTION ( 'NONE',  ( 0.000000000000000000, 0.000000000000000000, -1.000000000000000000 ) ) ;
#34326=ORIENTED_EDGE ( 'NONE', *, *, #10474, .T. ) ;
#34327=CARTESIAN_POINT ( 'NONE',  ( 10.14754812987370158, -63.31247221493028832, -45.99341560559020081 ) ) ;
#34331=CARTESIAN_POINT ( 'NONE',  ( 57.24929579703050564, 19.38381106717350022, -53.91492794795360055 ) ) ;
#34332=CARTESIAN_POINT ( 'NONE',  ( 53.96532849294369782, 19.38571653099999992, -76.95223800223610056 ) ) ;
#34333=AXIS2_PLACEMENT_3D ( 'NONE', #32393, #12782, #32919 ) ;
#34337=AXIS2_PLACEMENT_3D ( 'NONE', #31043, #629, #19519 ) ;
#34340=VECTOR ( 'NONE', #34139, 1000.000000000000000 ) ;
#34342=B_SPLINE_SURFACE_WITH_KNOTS ( 'NONE', 3, 3, ( 
 ( #32566, #40461, #32057, #32830, #625, #48856, #7738, #3804, #35763, #51746, #8237, #15844, #31805, #4298, #48078, #39956, #28135, #44141 ),
 ( #24188, #20270, #1929, #5355, #49383, #37311, #33880, #49893, #38092, #42026, #37052, #17659, #49127, #34134, #29175, #25235, #21567, #25749 ),
 ( #50143, #17398, #1411, #13479, #9799, #10053, #5095, #29436, #41757, #24965, #5863, #21049, #17145, #45442, #33096, #45177, #21829, #13988 ),
 ( #37835, #29689, #13226, #49642, #17911, #29945, #9289, #9021, #45959, #26015, #13733, #9544, #45699, #2188, #41242, #6126, #21309, #33366 ),
 ( #22082, #18168, #33625, #28914, #44919, #40983, #1148, #25496, #41498, #5612, #37562, #1671, #26534, #19455, #43320, #14242, #46488, #10317 ),
 ( #26278, #47259, #46749, #15011, #7414, #10578, #43063, #14756, #51182, #22855, #42548, #6638, #14496, #39132, #18938, #22602, #15277, #27059 ),
 ( #47008, #35179, #3223, #22343, #30726, #34919, #7162, #26797, #38617, #27314, #50917, #6903, #38876, #2439, #31233, #19194, #2707, #34655 ),
 ( #2964, #42285, #18682, #11093, #3486, #23359, #39384, #30981, #10831, #38349, #11349, #30212, #46228, #50409, #18422, #23113, #50662, #35441 ),
 ( #6382, #34397, #30468, #42809, #16550, #28332, #27826, #28075, #4498, #4245, #47766, #20731, #32502, #8184, #313, #48529, #31486, #24125 ) ),
 .UNSPECIFIED., .F., .F., .F.,
 ( 4, 1, 1, 1, 1, 1, 4 ),
 ( 4, 2, 2, 2, 2, 2, 2, 2, 4 ),
 ( 0.000000000000000000, 0.1666666666666670182, 0.3333333333333329818, 0.5000000000000000000, 0.6666666666666670737, 0.8333333333333330373, 1.000000000000000000 ),
 ( -0.9973706374895159321, -0.9474515228500450803, -0.8167403652454939822, -0.7016502394537249554, -0.5865601136619560396, -0.4426974564222450059, -0.2988347991825339722, -0.01347842800242600100, 0.07936656096996599907 ),
 .UNSPECIFIED. ) ;
#34345=DIRECTION ( 'NONE',  ( 0.000000000000000000, 0.000000000000000000, 1.000000000000000000 ) ) ;
#34348=CARTESIAN_POINT ( 'NONE',  ( 56.94970255497029399, -45.93464052491829364, -26.24572100487180037 ) ) ;
#34350=CARTESIAN_POINT ( 'NONE',  ( 53.35896811852089883, -49.47778564188549666, -49.18807904032110656 ) ) ;
#34352=DIRECTION ( 'NONE',  ( -0.1175431456444907818, -0.8277005620457529300, -0.5487215947100521074 ) ) ;
#34354=CARTESIAN_POINT ( 'NONE',  ( 41.62258892463700022, -45.17860157138659360, -6.029592982722220107 ) ) ;
#34358=CARTESIAN_POINT ( 'NONE',  ( 54.77076828691379973, -47.35498126536249686, -25.79499481954439943 ) ) ;
#34359=CARTESIAN_POINT ( 'NONE',  ( 55.92110024521279854, -50.72146136133119398, -75.31187564150310720 ) ) ;
#34360=CARTESIAN_POINT ( 'NONE',  ( 7.395348223008199717, 28.56816484056830063, -11.82605492805729952 ) ) ;
#34365=CARTESIAN_POINT ( 'NONE',  ( 13.00893739769619906, 34.28605925116850273, -47.75434321273180416 ) ) ;
#34368=CARTESIAN_POINT ( 'NONE',  ( -5.159222269507229619, -47.09623647360059806, -4.453993761141310515 ) ) ;
#34370=CARTESIAN_POINT ( 'NONE',  ( 47.46960547804090425, 23.38441036786990068, -54.88167812123789702 ) ) ;
#34372=LINE ( 'NONE', #46204, #43595 ) ;
#34374=AXIS2_PLACEMENT_3D ( 'NONE', #4427, #36383, #44782 ) ;
#34375=CARTESIAN_POINT ( 'NONE',  ( 12.09990282912600001, 34.01294332033750578, -16.83009741454110042 ) ) ;
#34377=CARTESIAN_POINT ( 'NONE',  ( 52.99768777340029402, 18.34103694310250177, -48.81581853631149670 ) ) ;
#34378=CARTESIAN_POINT ( 'NONE',  ( 19.42743748307076501, 24.24785769981644634, -75.66007724762421560 ) ) ;
#34380=CARTESIAN_POINT ( 'NONE',  ( 52.72392628394530334, 18.48930238429770156, -28.00962051878589776 ) ) ;
#34381=CARTESIAN_POINT ( 'NONE',  ( 49.40539548389270408, 22.26547577746099904, -54.15746054661040176 ) ) ;
#34383=CARTESIAN_POINT ( 'NONE',  ( 52.69474333003019950, 18.53535902989789719, -48.79529474154600166 ) ) ;
#34384=CARTESIAN_POINT ( 'NONE',  ( 46.42984739191849997, -45.11618894467940066, -7.676443726158701075 ) ) ;
#34386=CARTESIAN_POINT ( 'NONE',  ( 10.97797437399790077, 31.92103424516269783, -44.74231727136250214 ) ) ;
#34388=CARTESIAN_POINT ( 'NONE',  ( 65.04835540476229028, -32.26176030518409732, -17.85457486710349784 ) ) ;
#34393=CARTESIAN_POINT ( 'NONE',  ( 56.87160281683760132, 19.05665430235150026, -52.71743055004790790 ) ) ;
#34394=CARTESIAN_POINT ( 'NONE',  ( 49.96674047072312419, -1.429328268333673213, -15.94298744783530175 ) ) ;
#34396=CARTESIAN_POINT ( 'NONE',  ( 11.35027784094959991, -64.43558176466569876, -44.57647092392380017 ) ) ;
#34397=CARTESIAN_POINT ( 'NONE',  ( 57.63180676903699862, -45.11980367247790014, -25.34401879820149617 ) ) ;
#34399=ORIENTED_EDGE ( 'NONE', *, *, #49812, .F. ) ;
#34403=VERTEX_POINT ( 'NONE', #9314 ) ;
#34404=CARTESIAN_POINT ( 'NONE',  ( 55.55365765569959535, -45.11618894467940066, -14.32025624407079967 ) ) ;
#34407=CARTESIAN_POINT ( 'NONE',  ( 15.59055465919079886, 19.84640421423560142, -21.35214379961290021 ) ) ;
#34411=CIRCLE ( 'NONE', #28532, 0.9999999999999974465 ) ;
#34414=CARTESIAN_POINT ( 'NONE',  ( 47.28690122458660028, -54.53046819659620326, -74.94574354657768822 ) ) ;
#34415=CARTESIAN_POINT ( 'NONE',  ( 41.56665882477770424, 12.62342850819730167, -4.650889749848269084 ) ) ;
#34418=CARTESIAN_POINT ( 'NONE',  ( 49.40552051342540096, 22.26542118999089936, -54.15739458345379376 ) ) ;
#34419=CARTESIAN_POINT ( 'NONE',  ( 51.74354725780179365, 19.79449691764480335, -76.13548132539280289 ) ) ;
#34420=CARTESIAN_POINT ( 'NONE',  ( 61.75051681185560426, 13.88381108430350075, -28.08183634978059828 ) ) ;
#34422=ORIENTED_EDGE ( 'NONE', *, *, #34098, .T. ) ;
#34424=CARTESIAN_POINT ( 'NONE',  ( 0.7492974541592680726, -53.47458583507350482, -7.830755312676159541 ) ) ;
#34425=CARTESIAN_POINT ( 'NONE',  ( 76.31778600806960355, 0.5058489486935060508, -12.80249019458479864 ) ) ;
#34426=CARTESIAN_POINT ( 'NONE',  ( 75.28698268395557136, 13.41427130635144493, -14.07372847826834672 ) ) ;
#34427=EDGE_CURVE ( 'NONE', #42834, #3712, #49921, .T. ) ;
#34429=CARTESIAN_POINT ( 'NONE',  ( 19.86710470927560834, -55.44147536898664441, -75.14569893017471713 ) ) ;
#34431=CARTESIAN_POINT ( 'NONE',  ( 57.09195614716849576, -47.42783454384350250, -46.39999999999999858 ) ) ;
#34434=DIRECTION ( 'NONE',  ( 0.000000000000000000, 0.000000000000000000, 1.000000000000000000 ) ) ;
#34435=CARTESIAN_POINT ( 'NONE',  ( 41.08683620002359760, 13.04363067530499976, -3.799113739079239771 ) ) ;
#34436=CARTESIAN_POINT ( 'NONE',  ( 61.35893852378349322, -45.52617362054395755, -47.58679445246438888 ) ) ;
#34437=CARTESIAN_POINT ( 'NONE',  ( 20.13393739768846302, 24.18330853958629234, -74.40623532124070039 ) ) ;
#34439=CARTESIAN_POINT ( 'NONE',  ( 76.02169335355060298, -43.31998441844365288, -13.64721484880164937 ) ) ;
#34440=CARTESIAN_POINT ( 'NONE',  ( 17.84255373986179904, -51.34461045802749624, -75.09854824053090283 ) ) ;
#34441=DIRECTION ( 'NONE',  ( -0.8224686640529090820, -0.3976080002595601126, -0.4067593573362717763 ) ) ;
#34446=ORIENTED_EDGE ( 'NONE', *, *, #43332, .F. ) ;
#34447=CARTESIAN_POINT ( 'NONE',  ( -0.09052647982827211059, 22.39771960572409881, -9.857778326383000334 ) ) ;
#34448=AXIS2_PLACEMENT_3D ( 'NONE', #27889, #39962, #32838 ) ;
#34449=CARTESIAN_POINT ( 'NONE',  ( 16.13393739769620083, -15.61618894467929941, -7.049999999999999822 ) ) ;
#34451=CARTESIAN_POINT ( 'NONE',  ( 7.523314408995544156, -61.08379353316595228, -20.29480228628006699 ) ) ;
#34452=EDGE_CURVE ( 'NONE', #13586, #43378, #43604, .T. ) ;
#34458=ORIENTED_EDGE ( 'NONE', *, *, #16508, .F. ) ;
#34459=DIRECTION ( 'NONE',  ( -0.8224686640529097481, 0.3976080002595595575, -0.4067593573362710546 ) ) ;
#34460=CARTESIAN_POINT ( 'NONE',  ( 61.06128757285269870, -45.34819059754200765, -46.84339011699150035 ) ) ;
#34462=VERTEX_POINT ( 'NONE', #649 ) ;
#34463=VERTEX_POINT ( 'NONE', #44941 ) ;
#34465=APPLICATION_CONTEXT ( 'automotive_design' ) ;
#34466=DIRECTION ( 'NONE',  ( 0.4872913772396111898, -0.8732394366197182567, 0.000000000000000000 ) ) ;
#34469=CARTESIAN_POINT ( 'NONE',  ( 15.67962062511290000, 19.63028992866140143, -15.65622423491010196 ) ) ;
#34470=CARTESIAN_POINT ( 'NONE',  ( 52.12109123451309500, -50.88362419310729479, -76.21339085482510711 ) ) ;
#34471=CARTESIAN_POINT ( 'NONE',  ( 60.91700494128750165, 14.27513245742689918, -47.41475498393460697 ) ) ;
#34475=CARTESIAN_POINT ( 'NONE',  ( 41.44023858514859882, -43.98147948091650505, -3.815737768197240420 ) ) ;
#34479=AXIS2_PLACEMENT_3D ( 'NONE', #2039, #49746, #26126 ) ;
#34483=DIRECTION ( 'NONE',  ( 0.000000000000000000, 1.000000000000000000, 0.000000000000000000 ) ) ;
#34487=CARTESIAN_POINT ( 'NONE',  ( 14.83462289604239892, -52.80674074535599516, -76.12862656241330228 ) ) ;
#34488=CARTESIAN_POINT ( 'NONE',  ( 57.55751162087899786, 18.89525652402230094, -52.61703142040180126 ) ) ;
#34490=ADVANCED_FACE ( 'NONE', ( #17677 ), #26824, .T. ) ;
#34491=B_SPLINE_CURVE_WITH_KNOTS ( 'NONE', 3,
 ( #8368, #489, #36137, #36384, #7603, #24058, #24316, #4428, #40335, #39565, #47693, #20397, #43753, #16478, #47949, #12051, #32433, #28003, #48455, #23805, #7855, #40077, #7612, #3929, #8112, #12561, #20146, #43501, #28523, #44521, #19641, #44009, #35633, #11796, #19889, #47346, #6733 ),
 .UNSPECIFIED., .F., .F.,
 ( 4, 2, 2, 2, 1, 1, 1, 2, 2, 2, 2, 1, 1, 2, 2, 2, 2, 1, 1, 2, 2, 4 ),
 ( 0.000000000000000000, 0.2499999999998844258, 0.3749999999998271383, 0.4374999999997926659, 0.4687499999997803424, 0.4843749999997737921, 0.4921874999997742361, 0.4960937499997697397, 0.4999999999997651878, 0.6249999999998444578, 0.6874999999998867573, 0.7187499999999088507, 0.7343749999999165112, 0.7421874999999231726, 0.7499999999999297229, 0.8124999999999729106, 0.8437499999999933387, 0.8593750000000016653, 0.8671875000000058842, 0.8710937500000075495, 0.8750000000000091038, 1.000000000000000000 ),
 .UNSPECIFIED. ) ;
#34493=CARTESIAN_POINT ( 'NONE',  ( -9.882013117715120032, -40.49932216338130075, -19.14999999999999858 ) ) ;
#34496=CARTESIAN_POINT ( 'NONE',  ( 47.99585623154239755, -54.37189248632540028, -55.05664384648260068 ) ) ;
#34499=CARTESIAN_POINT ( 'NONE',  ( 47.85506559290410422, 23.21069065499990103, -55.16819991544539903 ) ) ;
#34500=ORIENTED_EDGE ( 'NONE', *, *, #11252, .F. ) ;
#34504=CARTESIAN_POINT ( 'NONE',  ( 88.13393739769620083, -15.61618894467929941, -65.65000000000000568 ) ) ;
#34505=LINE ( 'NONE', #10681, #30251 ) ;
#34506=DIRECTION ( 'NONE',  ( -0.8857883891771956009, -0.4640893551880597712, 0.000000000000000000 ) ) ;
#34507=CARTESIAN_POINT ( 'NONE',  ( 55.92723414887319677, 14.69231210900940177, -25.58060912393079533 ) ) ;
#34514=FACE_OUTER_BOUND ( 'NONE', #40966, .T. ) ;
#34516=VERTEX_POINT ( 'NONE', #31171 ) ;
#34518=CARTESIAN_POINT ( 'NONE',  ( 12.14266246861669885, -64.86007294939740575, -16.13799733648500023 ) ) ;
#34521=CARTESIAN_POINT ( 'NONE',  ( 12.15396043383179858, -65.41633662578259134, -47.50051160094690772 ) ) ;
#34527=CARTESIAN_POINT ( 'NONE',  ( 53.52853389627100000, 18.17118327204569894, -49.18229249838620376 ) ) ;
#34528=CARTESIAN_POINT ( 'NONE',  ( 61.24042730829579995, -2.108457229618950546, -15.95092827701309979 ) ) ;
#34529=CARTESIAN_POINT ( 'NONE',  ( 50.98146090960219823, -49.40936669674759685, -76.31995468972489505 ) ) ;
#34530=CARTESIAN_POINT ( 'NONE',  ( 57.99287681093679936, -49.02125455608680227, -51.32482328972750452 ) ) ;
#34531=EDGE_CURVE ( 'NONE', #28005, #37478, #7613, .T. ) ;
#34532=ORIENTED_EDGE ( 'NONE', *, *, #14598, .T. ) ;
#34534=CARTESIAN_POINT ( 'NONE',  ( 68.13393739769814772, 19.38381105532029736, -71.50000000000200373 ) ) ;
#34535=ORIENTED_EDGE ( 'NONE', *, *, #11675, .T. ) ;
#34536=FACE_OUTER_BOUND ( 'NONE', #11040, .T. ) ;
#34540=CARTESIAN_POINT ( 'NONE',  ( 13.13600760831069891, -50.60910559520539920, -21.36925334575990121 ) ) ;
#34541=AXIS2_PLACEMENT_3D ( 'NONE', #9470, #13907, #6306 ) ;
#34542=CARTESIAN_POINT ( 'NONE',  ( 56.60748237810329897, 19.38381105532069881, -75.50618570370070870 ) ) ;
#34543=CARTESIAN_POINT ( 'NONE',  ( 47.35405898648330236, -54.26885648339170842, -75.29488275581999801 ) ) ;
#34544=CARTESIAN_POINT ( 'NONE',  ( 57.24676268689880487, 13.88381105532070059, -16.76478824873209916 ) ) ;
#34545=DIRECTION ( 'NONE',  ( 0.000000000000000000, 0.000000000000000000, -1.000000000000000000 ) ) ;
#34546=CARTESIAN_POINT ( 'NONE',  ( 56.66762828736870006, -50.37953306433199430, -52.77094437832339935 ) ) ;
#34550=CARTESIAN_POINT ( 'NONE',  ( 46.35275103504439898, 21.67755452994670406, -76.14999999999999147 ) ) ;
#34553=VECTOR ( 'NONE', #48706, 1000.000000000000000 ) ;
#34554=CARTESIAN_POINT ( 'NONE',  ( 12.34963117160209833, -65.36344979145191303, -23.59691445115834796 ) ) ;
#34556=DIRECTION ( 'NONE',  ( 0.000000000000000000, 0.000000000000000000, 1.000000000000000000 ) ) ;
#34557=FACE_OUTER_BOUND ( 'NONE', #23256, .T. ) ;
#34558=CARTESIAN_POINT ( 'NONE',  ( 82.28938727573759593, 13.99365337418919886, -47.03253095781639814 ) ) ;
#34560=CARTESIAN_POINT ( 'NONE',  ( 47.64116066081108158, 23.30216094288792661, -74.19778950641801885 ) ) ;
#34564=CARTESIAN_POINT ( 'NONE',  ( 12.93945173866060117, 34.17938410075420563, -46.97472070025120416 ) ) ;
#34565=VERTEX_POINT ( 'NONE', #39320 ) ;
#34566=CARTESIAN_POINT ( 'NONE',  ( 52.82044787969120136, -49.67922433927950010, -48.83393259163720046 ) ) ;
#34567=ORIENTED_EDGE ( 'NONE', *, *, #22147, .T. ) ;
#34570=CARTESIAN_POINT ( 'NONE',  ( 14.24102869631679802, 19.87035360122330019, -22.22788221432290001 ) ) ;
#34574=CARTESIAN_POINT ( 'NONE',  ( 53.05390108533369897, 18.34295525618989942, -49.03220057305669854 ) ) ;
#34575=FACE_OUTER_BOUND ( 'NONE', #35980, .T. ) ;
#34576=CARTESIAN_POINT ( 'NONE',  ( 16.49542438326771787, 19.87930237151499924, -15.67473697716815373 ) ) ;
#34582=CARTESIAN_POINT ( 'NONE',  ( 12.82231730655639979, 34.27273057154270219, -47.70638112247609541 ) ) ;
#34584=CARTESIAN_POINT ( 'NONE',  ( 10.88578148292680048, -65.03392828768018319, -17.73314437552549805 ) ) ;
#34585=CARTESIAN_POINT ( 'NONE',  ( 53.39111139338680090, 18.13443291158960236, -48.76214190021520523 ) ) ;
#34587=LINE ( 'NONE', #29622, #21801 ) ;
#34588=VERTEX_POINT ( 'NONE', #31680 ) ;
#34590=VERTEX_POINT ( 'NONE', #51374 ) ;
#34591=CARTESIAN_POINT ( 'NONE',  ( 9.740906203438708388, -63.25244105705341013, -46.29739040527410054 ) ) ;
#34596=CARTESIAN_POINT ( 'NONE',  ( 57.27851913721940491, 18.92138913705230152, -52.63313635947250191 ) ) ;
#34597=CARTESIAN_POINT ( 'NONE',  ( 52.26113487638559718, 18.74837471589070148, -76.96437248003098830 ) ) ;
#34602=CARTESIAN_POINT ( 'NONE',  ( 82.62219371760957642, -45.06709663929255072, -46.37145547250047173 ) ) ;
#34608=EDGE_LOOP ( 'NONE', ( #26495, #37686, #12662, #5859 ) ) ;
#34609=DIRECTION ( 'NONE',  ( 0.000000000000000000, 1.000000000000000000, 0.000000000000000000 ) ) ;
#34612=CIRCLE ( 'NONE', #3661, 30.99999999999999645 ) ;
#34614=CARTESIAN_POINT ( 'NONE',  ( 57.36123081458359962, -50.13537923174280309, -52.61896056486340001 ) ) ;
#34616=CARTESIAN_POINT ( 'NONE',  ( 44.59157399860669813, -45.15507410885789596, -7.270416675856879785 ) ) ;
#34617=DIRECTION ( 'NONE',  ( 0.000000000000000000, -1.000000000000000000, 0.000000000000000000 ) ) ;
#34620=CARTESIAN_POINT ( 'NONE',  ( 52.59996064233959601, -49.82480704385319825, -27.82108120899960113 ) ) ;
#34621=CARTESIAN_POINT ( 'NONE',  ( 56.46527518672509416, -50.77626718493720404, -74.14938318154928254 ) ) ;
#34622=CARTESIAN_POINT ( 'NONE',  ( -6.505945840192179475, 14.80671025396210005, -5.054061883099680408 ) ) ;
#34624=CARTESIAN_POINT ( 'NONE',  ( 47.54281612864539852, -54.55267448867429891, -54.67232832126270381 ) ) ;
#34625=CARTESIAN_POINT ( 'NONE',  ( -10.90401617485183294, 10.24444606491774579, -20.56421356237309794 ) ) ;
#34626=ORIENTED_EDGE ( 'NONE', *, *, #44465, .T. ) ;
#34627=CARTESIAN_POINT ( 'NONE',  ( 52.82975622904280755, -49.66092049964720445, -48.47378032971909789 ) ) ;
#34628=CARTESIAN_POINT ( 'NONE',  ( 47.52904197842820366, 23.35432397247770098, -55.02687474755870056 ) ) ;
#34629=DIRECTION ( 'NONE',  ( 0.000000000000000000, 0.000000000000000000, -1.000000000000000000 ) ) ;
#34632=CARTESIAN_POINT ( 'NONE',  ( 11.61081905484630106, 34.00625395061120315, -17.07039315353630116 ) ) ;
#34634=CARTESIAN_POINT ( 'NONE',  ( 53.11047200542400049, 18.28146774992270451, -48.81638559825469770 ) ) ;
#34637=CARTESIAN_POINT ( 'NONE',  ( 53.13638922289359812, 18.11798713974379993, -27.41642391186969974 ) ) ;
#34640=CARTESIAN_POINT ( 'NONE',  ( 53.19546650609449756, -49.34483516088236854, -27.47723033151208938 ) ) ;
#34641=CARTESIAN_POINT ( 'NONE',  ( 53.27384017177119802, 18.28364788282440045, -49.18478595043859514 ) ) ;
#34644=CARTESIAN_POINT ( 'NONE',  ( 10.49070242014079923, 32.02022178723940016, -45.62562209983570227 ) ) ;
#34646=CARTESIAN_POINT ( 'NONE',  ( 65.62514207164689140, -31.75125826519879624, -17.33363148726699876 ) ) ;
#34647=DIRECTION ( 'NONE',  ( 0.000000000000000000, 0.000000000000000000, -1.000000000000000000 ) ) ;
#34648=EDGE_LOOP ( 'NONE', ( #11196, #37550, #13727, #27007 ) ) ;
#34652=CARTESIAN_POINT ( 'NONE',  ( 50.06027333097009091, -1.288484637660672227, -15.99592958142435961 ) ) ;
#34653=VERTEX_POINT ( 'NONE', #500 ) ;
#34654=CARTESIAN_POINT ( 'NONE',  ( 12.30224470026469952, -65.34897662448399558, -46.67366121987959815 ) ) ;
#34655=CARTESIAN_POINT ( 'NONE',  ( 55.85886099614570099, -46.00927082832929926, -25.54551749004689754 ) ) ;
#34662=CARTESIAN_POINT ( 'NONE',  ( 28.51189741163311098, -6.623074584604310644, -6.649999999999999467 ) ) ;
#34668=CARTESIAN_POINT ( 'NONE',  ( 15.45006552729070037, 19.88381503651260118, -21.87030236028560282 ) ) ;
#34669=B_SPLINE_CURVE_WITH_KNOTS ( 'NONE', 3,
 ( #14651, #30621, #46646, #43726, #23262, #8335, #3387, #51337, #47920, #7574, #15435, #7313, #8083, #24029 ),
 .UNSPECIFIED., .F., .F.,
 ( 4, 2, 2, 2, 2, 2, 4 ),
 ( 0.000000000000000000, 0.2230684146599339335, 0.4157015722607838581, 0.5812982619188552524, 0.7468949515769266467, 0.9958599354359034539, 1.000000000000000000 ),
 .UNSPECIFIED. ) ;
#34675=CARTESIAN_POINT ( 'NONE',  ( 47.26708353449659938, -54.64268123122759846, -74.72363872023309739 ) ) ;
#34676=CARTESIAN_POINT ( 'NONE',  ( 56.35995331962240584, 13.73636655591429978, -9.195822556514428925 ) ) ;
#34678=( BOUNDED_CURVE ( )  B_SPLINE_CURVE ( 3, ( #51216, #27604, #35479, #11126 ),
 .UNSPECIFIED., .F., .T. ) 
 B_SPLINE_CURVE_WITH_KNOTS ( ( 4, 4 ),
 ( 4.511031059594358794, 4.587061149216624223 ),
 .UNSPECIFIED. ) 
 CURVE ( )  GEOMETRIC_REPRESENTATION_ITEM ( )  RATIONAL_B_SPLINE_CURVE ( ( 1.000000000000000000, 0.9995183434654335564, 0.9995183434654335564, 1.000000000000000000 ) ) 
 REPRESENTATION_ITEM ( '' )  );
#34679=CARTESIAN_POINT ( 'NONE',  ( 60.53822230144759686, 13.88381112845349996, -26.37179243457269706 ) ) ;
#34682=FACE_OUTER_BOUND ( 'NONE', #9297, .T. ) ;
#34684=CARTESIAN_POINT ( 'NONE',  ( 2.539252561488040350, -55.76083552616880468, -9.526912277943489826 ) ) ;
#34685=CARTESIAN_POINT ( 'NONE',  ( 76.41006197761831231, 4.471648996623030392, -13.20456822250660167 ) ) ;
#34686=CARTESIAN_POINT ( 'NONE',  ( 75.19566803704495328, 13.64401423318863849, -14.39133821584264972 ) ) ;
#34690=CARTESIAN_POINT ( 'NONE',  ( 82.13853704237929776, -45.53381088318579373, -47.59887875144359981 ) ) ;
#34691=CARTESIAN_POINT ( 'NONE',  ( 12.89164060295139969, 19.08427617359420125, -21.19267904405079861 ) ) ;
#34692=CARTESIAN_POINT ( 'NONE',  ( 11.13393741218609989, -63.52234717531779751, -24.14942545402350049 ) ) ;
#34693=CARTESIAN_POINT ( 'NONE',  ( 41.67343726859200359, 12.74555918370619878, -4.319880481587650145 ) ) ;
#34694=CARTESIAN_POINT ( 'NONE',  ( 66.70013194292150160, -29.76883965895079953, -17.02746303015019791 ) ) ;
#34696=CARTESIAN_POINT ( 'NONE',  ( 56.50531572827331672, 19.52721310988098224, -53.84464530972960716 ) ) ;
#34698=TOROIDAL_SURFACE ( 'NONE', #22121, 32.00000000000000000, 1.000000000000000000 ) ;
#34700=CARTESIAN_POINT ( 'NONE',  ( 18.01980923492579834, -51.98087455372210286, -75.71853508996549920 ) ) ;
#34701=CARTESIAN_POINT ( 'NONE',  ( 60.43008559674330371, -45.11618894467940066, -10.91951671383950107 ) ) ;
#34703=EDGE_CURVE ( 'NONE', #18021, #4326, #21253, .T. ) ;
#34712=CARTESIAN_POINT ( 'NONE',  ( 40.78718624821470229, -45.20719311071780311, -5.637855430988819805 ) ) ;
#34713=ORIENTED_EDGE ( 'NONE', *, *, #43332, .T. ) ;
#34714=VERTEX_POINT ( 'NONE', #13350 ) ;
#34716=CARTESIAN_POINT ( 'NONE',  ( 57.30396242925620243, -45.11618894467940066, -16.63931852905170317 ) ) ;
#34717=CARTESIAN_POINT ( 'NONE',  ( 61.30391243981929961, -45.22107206010090152, -46.44424457753540736 ) ) ;
#34728=CARTESIAN_POINT ( 'NONE',  ( 50.97250182500789606, -50.96425953204839487, -76.14992205317840046 ) ) ;
#34729=CARTESIAN_POINT ( 'NONE',  ( 60.81754538871109617, 14.28754699922989957, -47.34637945857710406 ) ) ;
#34731=CARTESIAN_POINT ( 'NONE',  ( 42.73119093455760265, -42.90850753387979921, -3.876063987003000033 ) ) ;
#34733=CARTESIAN_POINT ( 'NONE',  ( -10.41738590414109922, 11.58576686758640051, -6.158695775020420093 ) ) ;
#34736=CARTESIAN_POINT ( 'NONE',  ( 56.16732778809232229, -50.61618894467929408, -76.24890161720091442 ) ) ;
#34738=VERTEX_POINT ( 'NONE', #754 ) ;
#34739=CARTESIAN_POINT ( 'NONE',  ( 14.86387764175020010, -52.78596775754549952, -76.12812327221449493 ) ) ;
#34740=CARTESIAN_POINT ( 'NONE',  ( 57.41838965642980241, 19.15902291818160208, -52.99946191110650062 ) ) ;
#34741=PRODUCT_DEFINITION_CONTEXT ( 'detailed design', #34465, 'design' ) ;
#34744=CARTESIAN_POINT ( 'NONE',  ( 15.72190426420170084, 19.65388757372259931, -20.14992017774509847 ) ) ;
#34745=CARTESIAN_POINT ( 'NONE',  ( 47.10254288570079950, -54.62488891218850284, -75.00961804031550173 ) ) ;
#34748=CARTESIAN_POINT ( 'NONE',  ( 72.38393739883420608, 20.38443354211860026, -61.34712802272770915 ) ) ;
#34749=CARTESIAN_POINT ( 'NONE',  ( 47.96382216759450046, -54.39756210150869720, -55.24304179605790210 ) ) ;
#34751=DIRECTION ( 'NONE',  ( 0.000000000000000000, 0.000000000000000000, -1.000000000000000000 ) ) ;
#34752=EDGE_CURVE ( 'NONE', #25873, #8693, #25370, .T. ) ;
#34753=CARTESIAN_POINT ( 'NONE',  ( 56.47388559847279765, 19.45410061890109787, -53.28105505440650091 ) ) ;
#34759=EDGE_CURVE ( 'NONE', #17323, #15326, #17278, .T. ) ;
#34762=CARTESIAN_POINT ( 'NONE',  ( 60.76394125543679792, -45.50397866361529964, -47.09160526915939471 ) ) ;
#34763=CARTESIAN_POINT ( 'NONE',  ( 82.74185698189259597, 14.32742998458173389, -47.63394792283020962 ) ) ;
#34767=EDGE_CURVE ( 'NONE', #35735, #23493, #27102, .T. ) ;
#34769=CARTESIAN_POINT ( 'NONE',  ( 56.83722670948610300, 19.42668272705650168, -53.85090158270489979 ) ) ;
#34770=ORIENTED_EDGE ( 'NONE', *, *, #42141, .F. ) ;
#34772=VECTOR ( 'NONE', #34995, 1000.000000000000000 ) ;
#34774=ORIENTED_EDGE ( 'NONE', *, *, #43527, .F. ) ;
#34775=CARTESIAN_POINT ( 'NONE',  ( 12.17667205660399965, -64.95597786680379215, -16.26506704565129979 ) ) ;
#34778=CARTESIAN_POINT ( 'NONE',  ( 10.97075952977539970, -64.83014200044789277, -46.68587730848879858 ) ) ;
#34780=VERTEX_POINT ( 'NONE', #24847 ) ;
#34781=ORIENTED_EDGE ( 'NONE', *, *, #11357, .F. ) ;
#34784=CARTESIAN_POINT ( 'NONE',  ( 56.68140060072190067, 14.86855146348369949, -26.25318016425800138 ) ) ;
#34786=CARTESIAN_POINT ( 'NONE',  ( 63.21052810172120218, 0.2212761650789459855, -16.92427711443150073 ) ) ;
#34788=CARTESIAN_POINT ( 'NONE',  ( 51.63018455908149917, -48.77028295090120480, -76.93968096216320873 ) ) ;
#34789=CARTESIAN_POINT ( 'NONE',  ( 57.10007285306519975, -49.84413130755979893, -52.15317371639780220 ) ) ;
#34790=EDGE_LOOP ( 'NONE', ( #46093, #4096, #43883, #1156 ) ) ;
#34794=DIRECTION ( 'NONE',  ( 1.000000000000000000, 0.000000000000000000, 0.000000000000000000 ) ) ;
#34795=CARTESIAN_POINT ( 'NONE',  ( 50.64365103579869754, -45.11618894467940066, -10.74058096729739908 ) ) ;
#34796=AXIS2_PLACEMENT_3D ( 'NONE', #14334, #18256, #13318 ) ;
#34799=CARTESIAN_POINT ( 'NONE',  ( 13.72891830083070097, -51.14266425624079915, -22.20512176267040161 ) ) ;
#34800=CARTESIAN_POINT ( 'NONE',  ( 54.17308252196429663, 19.39393527511609605, -76.74823974466679033 ) ) ;
#34802=CARTESIAN_POINT ( 'NONE',  ( 55.75423648348099448, 13.88381105532070059, -14.60095162971360061 ) ) ;
#34804=CARTESIAN_POINT ( 'NONE',  ( 56.46340970796750014, -50.48601309047270291, -52.83593731299979623 ) ) ;
#34805=ADVANCED_FACE ( 'NONE', ( #25107 ), #10948, .T. ) ;
#34809=CARTESIAN_POINT ( 'NONE',  ( 47.56593113937609729, 23.24463118434199771, -74.72646171873358867 ) ) ;
#34816=CIRCLE ( 'NONE', #18929, 3.500000000000003109 ) ;
#34817=CARTESIAN_POINT ( 'NONE',  ( 53.91121044660913242, -51.22748541984103809, -75.56421356237309794 ) ) ;
#34819=CARTESIAN_POINT ( 'NONE',  ( 53.11711210633388447, 19.14144468090594842, -77.21690156005293204 ) ) ;
#34822=CARTESIAN_POINT ( 'NONE',  ( 49.46107350807110237, 22.52470162032749812, -55.06157209291070131 ) ) ;
#34823=ORIENTED_EDGE ( 'NONE', *, *, #1995, .F. ) ;
#34825=( BOUNDED_CURVE ( )  B_SPLINE_CURVE ( 3, ( #20345, #1227, #36331, #17216 ),
 .UNSPECIFIED., .F., .T. ) 
 B_SPLINE_CURVE_WITH_KNOTS ( ( 4, 4 ),
 ( 2.369247656320500273, 2.476279911527849986 ),
 .UNSPECIFIED. ) 
 CURVE ( )  GEOMETRIC_REPRESENTATION_ITEM ( )  RATIONAL_B_SPLINE_CURVE ( ( 1.000000000000000000, 0.9990455691836308549, 0.9990455691836308549, 1.000000000000000000 ) ) 
 REPRESENTATION_ITEM ( '' )  );
#34826=CARTESIAN_POINT ( 'NONE',  ( 52.81564609458730075, -49.67679338445299919, -48.78617142090899961 ) ) ;
#34831=CARTESIAN_POINT ( 'NONE',  ( 13.97461707658050045, 19.95444906452859968, -22.92155397991069776 ) ) ;
#34832=CARTESIAN_POINT ( 'NONE',  ( 51.95832179060779765, -49.45171672659990492, -77.09973274272179822 ) ) ;
#34834=CARTESIAN_POINT ( 'NONE',  ( 53.05450032218360690, 18.36301419135650193, -49.09560402782900468 ) ) ;
#34835=EDGE_CURVE ( 'NONE', #4255, #9060, #48887, .T. ) ;
#34836=CARTESIAN_POINT ( 'NONE',  ( 54.62219313239500451, -46.21587333935030273, -15.85441571428080110 ) ) ;
#34838=VECTOR ( 'NONE', #27377, 1000.000000000000000 ) ;
#34839=ORIENTED_EDGE ( 'NONE', *, *, #35145, .T. ) ;
#34842=CARTESIAN_POINT ( 'NONE',  ( 10.96947337815119994, -65.06555250629570253, -17.60046538708800057 ) ) ;
#34843=CARTESIAN_POINT ( 'NONE',  ( 9.227644565586000880, 32.59853923576839918, -46.67822069845360033 ) ) ;
#34848=CARTESIAN_POINT ( 'NONE',  ( 50.03996090745119574, -53.49158772749100166, -54.67836234838419784 ) ) ;
#34851=ORIENTED_EDGE ( 'NONE', *, *, #44814, .F. ) ;
#34852=CARTESIAN_POINT ( 'NONE',  ( 9.734484948842229812, -63.18888116458209936, -46.29877033112669693 ) ) ;
#34856=CARTESIAN_POINT ( 'NONE',  ( 11.49293641769672547, -64.67039120822151688, -44.68941564908284647 ) ) ;
#34857=CARTESIAN_POINT ( 'NONE',  ( 57.07894513400979974, 18.98008675654529753, -52.67137582195630330 ) ) ;
#34858=CARTESIAN_POINT ( 'NONE',  ( 52.87559984714759764, 19.04777732598209994, -77.15855498664130607 ) ) ;
#34859=ORIENTED_EDGE ( 'NONE', *, *, #76, .T. ) ;
#34860=CARTESIAN_POINT ( 'NONE',  ( 16.13393739769620083, -15.61618894467929941, -11.54999999999999893 ) ) ;
#34861=CARTESIAN_POINT ( 'NONE',  ( 51.76047950956269261, 20.08324044957887722, -76.04144537520551239 ) ) ;
#34862=FACE_OUTER_BOUND ( 'NONE', #50091, .T. ) ;
#34870=DIRECTION ( 'NONE',  ( 1.000000000000000000, 0.000000000000000000, 0.000000000000000000 ) ) ;
#34873=EDGE_CURVE ( 'NONE', #32383, #6259, #43446, .T. ) ;
#34875=AXIS2_PLACEMENT_3D ( 'NONE', #41032, #40772, #16406 ) ;
#34877=CARTESIAN_POINT ( 'NONE',  ( 63.88393739769619373, 20.38443354211860026, -61.34712802272770915 ) ) ;
#34878=DIRECTION ( 'NONE',  ( 0.2992932829740320710, 0.8274908255099422405, 0.4750604850579560612 ) ) ;
#34881=CARTESIAN_POINT ( 'NONE',  ( 11.89829296290529825, 33.59996124671599915, -16.17105426248049937 ) ) ;
#34884=CARTESIAN_POINT ( 'NONE',  ( 56.68182224158719862, -50.69727463636530018, -74.32273727118189299 ) ) ;
#34885=CARTESIAN_POINT ( 'NONE',  ( 0.9417307494557060066, 22.43464593454210032, -8.026335962152479908 ) ) ;
#34886=DIRECTION ( 'NONE',  ( 1.000000000000000000, 0.000000000000000000, 0.000000000000000000 ) ) ;
#34887=DIRECTION ( 'NONE',  ( -1.000000000000000000, 0.000000000000000000, 0.000000000000000000 ) ) ;
#34890=CARTESIAN_POINT ( 'NONE',  ( -9.115847631259869743, -44.02029276258719648, -5.453298411520159483 ) ) ;
#34891=CARTESIAN_POINT ( 'NONE',  ( 47.63955984696239909, 23.29747590340559782, -54.97543810062130376 ) ) ;
#34892=AXIS2_PLACEMENT_3D ( 'NONE', #2157, #2934, #26502 ) ;
#34893=CARTESIAN_POINT ( 'NONE',  ( 42.75216321632269967, -44.98233172091430276, -6.093641062779489914 ) ) ;
#34895=CARTESIAN_POINT ( 'NONE',  ( 61.22235620690700131, 14.10114171156870100, -47.17370879253629568 ) ) ;
#34896=CARTESIAN_POINT ( 'NONE',  ( 11.71337180106040066, 34.04767145060470313, -17.10636616733519944 ) ) ;
#34897=CARTESIAN_POINT ( 'NONE',  ( 51.99246080072069986, 18.79347982688590335, -76.70334503327950415 ) ) ;
#34898=CARTESIAN_POINT ( 'NONE',  ( 52.81905492317230255, 18.43458074482090225, -48.62056802018800283 ) ) ;
#34901=CARTESIAN_POINT ( 'NONE',  ( 53.30277398520820498, -49.41309324413840187, -48.78464791978760218 ) ) ;
#34902=CARTESIAN_POINT ( 'NONE',  ( 54.50135132931570325, 16.78773581522769831, -26.62868989851730106 ) ) ;
#34903=CARTESIAN_POINT ( 'NONE',  ( 51.22043009712629669, 21.75654279735209684, -54.39216491918590179 ) ) ;
#34904=CARTESIAN_POINT ( 'NONE',  ( 54.25582316535073346, -48.40199966990474678, -26.87775820864355936 ) ) ;
#34908=CARTESIAN_POINT ( 'NONE',  ( 11.13393739769619906, 32.08797975232909749, -43.91615438303840335 ) ) ;
#34911=CARTESIAN_POINT ( 'NONE',  ( 65.66432530626940434, -32.39603305783209919, -18.02567142080080131 ) ) ;
#34912=CARTESIAN_POINT ( 'NONE',  ( 48.94270149030809591, -51.80671227847209792, -55.11972614036100282 ) ) ;
#34916=CARTESIAN_POINT ( 'NONE',  ( 51.07460838780723122, 0.2638179241706318234, -16.96543469932025872 ) ) ;
#34917=VERTEX_POINT ( 'NONE', #4833 ) ;
#34918=CARTESIAN_POINT ( 'NONE',  ( 12.66783529652720119, -65.47373773509440298, -47.23930563553710726 ) ) ;
#34919=CARTESIAN_POINT ( 'NONE',  ( 57.20761488960310004, -45.15217172719249561, -25.52117527002110009 ) ) ;
#34921=CARTESIAN_POINT ( 'NONE',  ( 6.531828926332683416, -46.09336100234546763, -20.85710678118654471 ) ) ;
#34923=CARTESIAN_POINT ( 'NONE',  ( 11.67118088809841403, 34.15913531565607286, -22.47626263540971436 ) ) ;
#34925=CARTESIAN_POINT ( 'NONE',  ( 11.31451853429699916, 33.98448577272930038, -22.84783898345410336 ) ) ;
#34931=CARTESIAN_POINT ( 'NONE',  ( 60.68061620254660227, -29.62692640763259888, -15.93463980944039982 ) ) ;
#34933=CARTESIAN_POINT ( 'NONE',  ( 46.88182844640049751, -53.82794794302169805, -75.86076060431129520 ) ) ;
#34934=CARTESIAN_POINT ( 'NONE',  ( 61.87076928723249836, 12.19882557268090117, -9.590776207249099627 ) ) ;
#34936=CARTESIAN_POINT ( 'NONE',  ( 74.17629866868290378, -15.61618894467929941, -65.34607522167520699 ) ) ;
#34938=AXIS2_PLACEMENT_3D ( 'NONE', #47374, #39504, #11728 ) ;
#34939=CARTESIAN_POINT ( 'NONE',  ( 59.76051743928839954, 13.88381115859199966, -25.97343284354310100 ) ) ;
#34942=CARTESIAN_POINT ( 'NONE',  ( 56.31078303086230363, -46.45614404618829951, -26.30376438173910358 ) ) ;
#34943=CARTESIAN_POINT ( 'NONE',  ( 2.219830629761540219, -55.78013387361319531, -9.977522010426989496 ) ) ;
#34944=CARTESIAN_POINT ( 'NONE',  ( 76.18788946429619102, -8.449960703364579828, -12.23626020543570014 ) ) ;
#34945=AXIS2_PLACEMENT_3D ( 'NONE', #164, #47867, #412 ) ;
#34946=DIRECTION ( 'NONE',  ( 1.370459167135278883E-23, -1.000000000000000000, -3.054623595244970244E-12 ) ) ;
#34949=CARTESIAN_POINT ( 'NONE',  ( 47.18324198357279897, 23.57489020266570279, -54.61058319554400242 ) ) ;
#34950=CARTESIAN_POINT ( 'NONE',  ( 57.24929578595760660, 21.38381105532069881, -74.14999999999999147 ) ) ;
#34951=CARTESIAN_POINT ( 'NONE',  ( 57.33263043794990210, -50.46433321893989898, -53.14935904668140410 ) ) ;
#34952=CARTESIAN_POINT ( 'NONE',  ( 41.38588548186360327, 12.78016087411839941, -3.641004086722789523 ) ) ;
#34954=EDGE_CURVE ( 'NONE', #15334, #21823, #51052, .T. ) ;
#34959=CARTESIAN_POINT ( 'NONE',  ( 17.78950558660029913, -52.11833314967490338, -75.86497326479759806 ) ) ;
#34965=EDGE_LOOP ( 'NONE', ( #8045, #36547, #40011, #49189, #13541, #5903 ) ) ;
#34966=CARTESIAN_POINT ( 'NONE',  ( -5.732063824511490324, 16.49934840382849899, -7.265669357055710265 ) ) ;
#34967=CARTESIAN_POINT ( 'NONE',  ( 61.36407574442370105, -45.58133505526990348, -47.65743212064420220 ) ) ;
#34971=CARTESIAN_POINT ( 'NONE',  ( 40.74407843658939754, -45.29541405632470230, -5.682185392553109615 ) ) ;
#34973=CARTESIAN_POINT ( 'NONE',  ( 17.40131324658650058, 21.55824172761710145, -76.12873484255680978 ) ) ;
#34974=ORIENTED_EDGE ( 'NONE', *, *, #44946, .F. ) ;
#34977=CARTESIAN_POINT ( 'NONE',  ( 11.13393739769619906, -55.30245861064819479, -43.74348518090240390 ) ) ;
#34978=FACE_OUTER_BOUND ( 'NONE', #27567, .T. ) ;
#34983=CYLINDRICAL_SURFACE ( 'NONE', #6867, 1.500000000000001332 ) ;
#34985=ORIENTED_EDGE ( 'NONE', *, *, #15848, .F. ) ;
#34987=CARTESIAN_POINT ( 'NONE',  ( 51.40458829746259539, -50.54838093730629822, -76.23573209381319771 ) ) ;
#34988=CARTESIAN_POINT ( 'NONE',  ( 60.47109295822400554, 14.43742118176249889, -47.34531703895609667 ) ) ;
#34990=EDGE_CURVE ( 'NONE', #11477, #6439, #21019, .T. ) ;
#34991=DIRECTION ( 'NONE',  ( -0.2260571801428161443, 0.000000000000000000, 0.9741140340359945027 ) ) ;
#34992=DIRECTION ( 'NONE',  ( 0.4872913772396113563, 0.8732394366197181457, 0.000000000000000000 ) ) ;
#34993=CARTESIAN_POINT ( 'NONE',  ( -5.416793657864619860, 16.04363467761240258, -5.522478245015279619 ) ) ;
#34995=DIRECTION ( 'NONE',  ( 0.000000000000000000, 1.000000000000000000, 0.000000000000000000 ) ) ;
#34999=CARTESIAN_POINT ( 'NONE',  ( 60.23130391297029718, 14.55066440145539985, -47.24246919202539630 ) ) ;
#35000=CARTESIAN_POINT ( 'NONE',  ( 57.46868213755980292, 19.37940608379300045, -53.76542284059749477 ) ) ;
#35003=CARTESIAN_POINT ( 'NONE',  ( 15.72192118514110071, 19.65389280997749921, -20.20712476364060350 ) ) ;
#35006=CIRCLE ( 'NONE', #41717, 1.999999999999999112 ) ;
#35009=CARTESIAN_POINT ( 'NONE',  ( 48.20668737594320419, -54.29411078304290328, -55.27999763446919701 ) ) ;
#35010=CARTESIAN_POINT ( 'NONE',  ( -0.3347231778644786937, -63.30338805799588897, -50.60099389661421299 ) ) ;
#35011=CARTESIAN_POINT ( 'NONE',  ( 56.51998432061879640, 19.51919619937510220, -53.72896419663989320 ) ) ;
#35013=CARTESIAN_POINT ( 'NONE',  ( 56.61928439928507828, -45.32411236664518839, -31.98003398042899903 ) ) ;
#35014=ORIENTED_EDGE ( 'NONE', *, *, #24854, .T. ) ;
#35020=LINE ( 'NONE', #15125, #41982 ) ;
#35022=CARTESIAN_POINT ( 'NONE',  ( 10.12791152504586378, 23.94333337502630243, -23.14397412734966508 ) ) ;
#35027=DIRECTION ( 'NONE',  ( 0.000000000000000000, 0.000000000000000000, 1.000000000000000000 ) ) ;
#35032=CARTESIAN_POINT ( 'NONE',  ( 76.47487835096482911, -26.73510161258535334, -13.11916531094834149 ) ) ;
#35033=CARTESIAN_POINT ( 'NONE',  ( 9.628276464716538641, -64.27089026540051009, -46.77858652811859486 ) ) ;
#35035=EDGE_LOOP ( 'NONE', ( #30148, #3218, #21093, #26866, #34626 ) ) ;
#35036=CARTESIAN_POINT ( 'NONE',  ( 52.25041881653689302, 21.33925748481389917, -54.52050471625830141 ) ) ;
#35037=B_SPLINE_CURVE_WITH_KNOTS ( 'NONE', 3,
 ( #22616, #18696, #3758, #3237, #23375, #11620, #27583, #47022, #35717, #43587 ),
 .UNSPECIFIED., .F., .F.,
 ( 4, 2, 2, 2, 4 ),
 ( 0.4999999271553960956, 0.5624999999993647304, 0.6624999999993823607, 0.8224999999994107025, 1.000000000000000000 ),
 .UNSPECIFIED. ) ;
#35038=CARTESIAN_POINT ( 'NONE',  ( 82.13853704237929776, -45.11618894467940066, -46.37203261889099792 ) ) ;
#35041=CARTESIAN_POINT ( 'NONE',  ( 59.05492726919700175, -2.399412892946870102, -15.68836725989760161 ) ) ;
#35042=CARTESIAN_POINT ( 'NONE',  ( 51.73941937002660296, -49.41743988675749222, -76.84325757996180073 ) ) ;
#35047=FACE_BOUND ( 'NONE', #31619, .T. ) ;
#35052=CARTESIAN_POINT ( 'NONE',  ( 13.90103794227359835, -50.94889596342950000, -21.77365670817500032 ) ) ;
#35054=CARTESIAN_POINT ( 'NONE',  ( 0.5406133260286609676, 12.32747302715160131, -21.14999999999999858 ) ) ;
#35055=CARTESIAN_POINT ( 'NONE',  ( 55.99298997062209793, 13.96345059265260069, -15.51995950838309923 ) ) ;
#35056=CARTESIAN_POINT ( 'NONE',  ( 60.96779371467680164, -45.50112736404290104, -47.44752493507809987 ) ) ;
#35059=CARTESIAN_POINT ( 'NONE',  ( 82.35517963119028195, 13.87593746180422905, -46.40109284526622702 ) ) ;
#35064=CARTESIAN_POINT ( 'NONE',  ( 14.21262892652819865, -51.28949470891959805, -74.96248001587449039 ) ) ;
#35066=CARTESIAN_POINT ( 'NONE',  ( 44.42281161027170100, -46.09301635695339883, -8.582928211182331069 ) ) ;
#35067=CARTESIAN_POINT ( 'NONE',  ( 11.71911513826172957, -64.93734084241999938, -23.86816772916239415 ) ) ;
#35070=DIRECTION ( 'NONE',  ( -0.6676418852213052979, 0.2329255526947255628, -0.7071067811865461294 ) ) ;
#35071=CARTESIAN_POINT ( 'NONE',  ( 82.41473067501779326, 13.93846136199109864, -46.87530260006650451 ) ) ;
#35073=CARTESIAN_POINT ( 'NONE',  ( 47.53482541495846903, 23.16677570558394095, -74.95177797945758869 ) ) ;
#35077=DIRECTION ( 'NONE',  ( 1.000000000000000000, 0.000000000000000000, 0.000000000000000000 ) ) ;
#35080=CARTESIAN_POINT ( 'NONE',  ( 53.49062365247959860, -49.35044025281749924, -48.99764540719809958 ) ) ;
#35081=ORIENTED_EDGE ( 'NONE', *, *, #14477, .T. ) ;
#35082=AXIS2_PLACEMENT_3D ( 'NONE', #39336, #38565, #3438 ) ;
#35085=CARTESIAN_POINT ( 'NONE',  ( 14.04300386716560034, 19.71129266594920182, -21.72002249118050088 ) ) ;
#35086=CARTESIAN_POINT ( 'NONE',  ( 52.23706462883279755, -49.75889276274740070, -77.18591504236948708 ) ) ;
#35090=CARTESIAN_POINT ( 'NONE',  ( 52.71531171373420221, 18.50951998324639902, -48.72995709875519310 ) ) ;
#35091=CARTESIAN_POINT ( 'NONE',  ( 55.63792462483650070, -45.97095330521690215, -16.89987564799369935 ) ) ;
#35094=AXIS2_PLACEMENT_3D ( 'NONE', #552, #36193, #5283 ) ;
#35098=CARTESIAN_POINT ( 'NONE',  ( 8.839329446722729244, 32.18893842050779597, -46.67772192990729252 ) ) ;
#35102=CARTESIAN_POINT ( 'NONE',  ( 53.16274104891702024, -49.55751115293774234, -49.15255090718006414 ) ) ;
#35105=CARTESIAN_POINT ( 'NONE',  ( 50.43862210052599693, -53.32183726795299350, -54.57790968970819989 ) ) ;
#35108=CARTESIAN_POINT ( 'NONE',  ( 10.13445450645889956, -63.11543068638779630, -45.99826666626069738 ) ) ;
#35109=CARTESIAN_POINT ( 'NONE',  ( 68.13393739769769297, 18.72622661238300168, -73.39853292320978539 ) ) ;
#35110=ORIENTED_EDGE ( 'NONE', *, *, #28969, .F. ) ;
#35111=CARTESIAN_POINT ( 'NONE',  ( 51.17464648325179155, -31.65168256193422280, -17.11447666815010749 ) ) ;
#35112=CARTESIAN_POINT ( 'NONE',  ( 57.26283657379340042, 19.38381106601499937, -53.75815476539330007 ) ) ;
#35115=CARTESIAN_POINT ( 'NONE',  ( 9.496404732828242601, -64.31007825828744728, -46.84592557098148546 ) ) ;
#35116=DIRECTION ( 'NONE',  ( -1.000000000000000000, 0.000000000000000000, 0.000000000000000000 ) ) ;
#35118=FACE_OUTER_BOUND ( 'NONE', #13090, .T. ) ;
#35120=CARTESIAN_POINT ( 'NONE',  ( 36.43069203082960428, -15.61618894467929941, 7.530187386896120216 ) ) ;
#35122=EDGE_LOOP ( 'NONE', ( #8508, #13791, #31256, #18228 ) ) ;
#35125=VECTOR ( 'NONE', #16973, 1000.000000000000000 ) ;
#35126=CARTESIAN_POINT ( 'NONE',  ( 43.91474985106849971, -43.54612994170620510, -5.093415854460159764 ) ) ;
#35129=CARTESIAN_POINT ( 'NONE',  ( 55.40394000045360201, 13.88381105524500114, -14.52023566624100148 ) ) ;
#35130=AXIS2_PLACEMENT_3D ( 'NONE', #10557, #42008, #50641 ) ;
#35134=AXIS2_PLACEMENT_3D ( 'NONE', #8432, #24378, #12623 ) ;
#35135=CARTESIAN_POINT ( 'NONE',  ( 45.64758691443690708, -45.19790785473080064, -8.164367006753829870 ) ) ;
#35136=CYLINDRICAL_SURFACE ( 'NONE', #1293, 1.500000000000001332 ) ;
#35137=CARTESIAN_POINT ( 'NONE',  ( 12.16812838080560155, 33.44776901404870273, -15.91929859868259811 ) ) ;
#35140=CARTESIAN_POINT ( 'NONE',  ( 56.46720558104399856, -50.68772439539020525, -74.89154223783529574 ) ) ;
#35141=CARTESIAN_POINT ( 'NONE',  ( 0.6014665695674989987, 22.53381255785799908, -8.430871960909678720 ) ) ;
#35142=CARTESIAN_POINT ( 'NONE',  ( 10.71234811426425715, -55.24696076757936680, -45.27932796213227107 ) ) ;
#35143=CARTESIAN_POINT ( 'NONE',  ( 47.65526630185220114, -54.48436720726729732, -54.69071458794790175 ) ) ;
#35145=EDGE_CURVE ( 'NONE', #25228, #22140, #8741, .T. ) ;
#35148=CARTESIAN_POINT ( 'NONE',  ( -7.471208905905950104, -45.39622512213500016, -4.913224497761048859 ) ) ;
#35149=CARTESIAN_POINT ( 'NONE',  ( 47.51738683343549496, 23.35989739960990264, -54.96699491834060325 ) ) ;
#35154=CARTESIAN_POINT ( 'NONE',  ( 51.70526340020489897, 18.12584497879259615, -76.83585703765098174 ) ) ;
#35155=CARTESIAN_POINT ( 'NONE',  ( 52.85165463198989499, 18.41706942343310160, -48.64955370223109554 ) ) ;
#35156=DIRECTION ( 'NONE',  ( 0.000000000000000000, 0.000000000000000000, -1.000000000000000000 ) ) ;
#35157=CARTESIAN_POINT ( 'NONE',  ( 52.84340795157500281, -49.65376797971740075, -48.59551871909959431 ) ) ;
#35158=CARTESIAN_POINT ( 'NONE',  ( 53.62726140758459792, 17.64839027132520144, -27.04628291361679970 ) ) ;
#35159=CARTESIAN_POINT ( 'NONE',  ( 49.85715601738330349, 22.13586533569470305, -54.14711712984389891 ) ) ;
#35161=CARTESIAN_POINT ( 'NONE',  ( 52.82975622904280755, -49.66092049964720445, -28.15000000000000213 ) ) ;
#35162=CIRCLE ( 'NONE', #23434, 1.400000000000000133 ) ;
#35164=CARTESIAN_POINT ( 'NONE',  ( 62.10661619914199605, -31.21746242632069723, -16.71838601031609883 ) ) ;
#35166=CARTESIAN_POINT ( 'NONE',  ( 11.13393739769619906, 32.13057954558899354, -43.91801182705599871 ) ) ;
#35175=EDGE_LOOP ( 'NONE', ( #50854, #25293, #1475, #41212 ) ) ;
#35176=CARTESIAN_POINT ( 'NONE',  ( 52.26504646883520167, 18.55116755685089913, -77.19463087837650050 ) ) ;
#35177=CARTESIAN_POINT ( 'NONE',  ( 50.12347980195983155, -30.03964280096379014, -16.03354426139003053 ) ) ;
#35179=CARTESIAN_POINT ( 'NONE',  ( 57.59044435501339620, -45.13211036767589945, -25.55064646906290449 ) ) ;
#35181=EDGE_CURVE ( 'NONE', #28327, #42929, #7921, .T. ) ;
#35186=CARTESIAN_POINT ( 'NONE',  ( 42.44161405036800261, -44.94940367324450392, -5.942266020708489194 ) ) ;
#35187=ORIENTED_EDGE ( 'NONE', *, *, #6662, .T. ) ;
#35188=CARTESIAN_POINT ( 'NONE',  ( 50.64365103613339869, -45.11618894467940066, -10.74058096682459862 ) ) ;
#35189=CARTESIAN_POINT ( 'NONE',  ( 51.30165130492172665, 0.6175616045832953427, -17.32271293053486616 ) ) ;
#35190=DIRECTION ( 'NONE',  ( 0.000000000000000000, 0.9319748226751467524, 0.3625230060280709155 ) ) ;
#35192=CARTESIAN_POINT ( 'NONE',  ( 65.46635429658410033, -29.90696431587659987, -16.55440410732879997 ) ) ;
#35193=ADVANCED_FACE ( 'NONE', ( #23371 ), #23125, .F. ) ;
#35195=CARTESIAN_POINT ( 'NONE',  ( 47.13234217445310748, -54.53038550896650349, -75.11917674890220553 ) ) ;
#35197=CARTESIAN_POINT ( 'NONE',  ( 40.92025707381650079, 14.03914583310360165, -5.766237210609819641 ) ) ;
#35200=TOROIDAL_SURFACE ( 'NONE', #41858, 17.39999999955150045, 3.400000000022779911 ) ;
#35202=CARTESIAN_POINT ( 'NONE',  ( 83.86651039750330483, -44.39461367728179653, -46.90523421348220268 ) ) ;
#35203=CARTESIAN_POINT ( 'NONE',  ( 61.72362489370979688, 13.88380460837380070, -28.08315270507459971 ) ) ;
#35206=B_SPLINE_SURFACE_WITH_KNOTS ( 'NONE', 3, 3, ( 
 ( #13499, #37330, #8253, #40480, #4319, #24202, #20286, #41258, #40741, #9037, #28933, #13241, #32582, #21324, #17165, #25255 ),
 ( #4842, #8520, #33115, #12981, #36539, #9311, #21069, #32846, #5117, #29454, #29191, #45196, #5370, #44938, #37071, #20809 ),
 ( #1430, #645, #24985, #17414, #36279, #40230, #24727, #33383, #49398, #387, #16373, #32330, #48350, #12444, #28411, #48878 ),
 ( #44418, #24466, #4571, #20543, #12716, #48616, #28670, #44673, #36799, #909, #16904, #39339, #47215, #14002, #46962, #41517 ),
 ( #21581, #33643, #2207, #11303, #9559, #11044, #25511, #19151, #5634, #45979, #49660, #14965, #7116, #43020, #17674, #35129 ),
 ( #15488, #30932, #35393, #37580, #29704, #3180, #27014, #1686, #10070, #23068, #25770, #50163, #18184, #45717, #13750, #51136 ) ),
 .UNSPECIFIED., .F., .F., .F.,
 ( 4, 1, 1, 4 ),
 ( 4, 2, 2, 2, 2, 2, 2, 4 ),
 ( -7.682816665999999629E-06, 0.3333333333333329818, 0.6666666666666670737, 1.000000000266519917 ),
 ( -7.682816665999999629E-06, 2.041349754395100025, 4.374320902275210088, 5.832427869700279821, 6.561481353412809803, 7.727966927352870385, 9.594343845656959857, 11.66486342221729977 ),
 .UNSPECIFIED. ) ;
#35208=CARTESIAN_POINT ( 'NONE',  ( 52.82976017067200303, -49.66091843452839782, -28.09469381563379997 ) ) ;
#35209=CARTESIAN_POINT ( 'NONE',  ( -5.594544317113800069, -47.37070709791210277, -5.716103250782650136 ) ) ;
#35210=CARTESIAN_POINT ( 'NONE',  ( 76.64846024278141101, 4.391811825665690172, -13.86716462664029947 ) ) ;
#35211=CARTESIAN_POINT ( 'NONE',  ( 74.97543536360356597, 13.88380951271968478, -15.15463076919403385 ) ) ;
#35213=DIRECTION ( 'NONE',  ( 0.000000000000000000, 0.000000000000000000, 1.000000000000000000 ) ) ;
#35214=CARTESIAN_POINT ( 'NONE',  ( 47.21820949846080140, 23.54718703541459845, -54.61573492153319620 ) ) ;
#35215=CARTESIAN_POINT ( 'NONE',  ( 82.28938588685190325, -45.22603122459570102, -47.03253084601389844 ) ) ;
#35216=CARTESIAN_POINT ( 'NONE',  ( 57.41310621417500215, -50.45968287620319614, -53.14417655181500066 ) ) ;
#35217=CARTESIAN_POINT ( 'NONE',  ( 40.90236900589889757, 13.45839943238190095, -4.970360716545739521 ) ) ;
#35220=CARTESIAN_POINT ( 'NONE',  ( 55.10584483452489479, -48.49282765683750540, -48.53157258127289708 ) ) ;
#35221=CARTESIAN_POINT ( 'NONE',  ( 68.13393739769649926, -48.11618894467230234, -75.95000000000109708 ) ) ;
#35222=CARTESIAN_POINT ( 'NONE',  ( 68.39016279111210395, -1.116426826981149922, -18.15415026710280344 ) ) ;
#35223=CARTESIAN_POINT ( 'NONE',  ( 17.96588596253970138, -52.24360429457480137, -75.86497326479759806 ) ) ;
#35224=CARTESIAN_POINT ( 'NONE',  ( 49.80812477255949489, -53.32727295909180043, -54.05131971329959839 ) ) ;
#35229=DIRECTION ( 'NONE',  ( 0.000000000000000000, 0.9319748226751467524, 0.3625230060280709155 ) ) ;
#35230=PLANE ( 'NONE',  #40185 ) ;
#35234=CARTESIAN_POINT ( 'NONE',  ( 42.70758233787309877, -45.85587203478289808, -7.311889205965530714 ) ) ;
#35236=CARTESIAN_POINT ( 'NONE',  ( 17.21347160910339724, 21.88381105532300097, -76.14999999999999147 ) ) ;
#35241=DIRECTION ( 'NONE',  ( -6.128874000000000406E-13, 6.301142999999999861E-13, 1.000000000000000000 ) ) ;
#35246=CARTESIAN_POINT ( 'NONE',  ( 16.13393739769620083, -15.61618894467929941, 6.850000000000000533 ) ) ;
#35247=AXIS2_PLACEMENT_3D ( 'NONE', #43575, #35706, #20215 ) ;
#35249=AXIS2_PLACEMENT_3D ( 'NONE', #22015, #33814, #49828 ) ;
#35252=CARTESIAN_POINT ( 'NONE',  ( 56.81354083976449942, -51.38126045871209868, -54.61518503260169410 ) ) ;
#35253=DIRECTION ( 'NONE',  ( 0.000000000000000000, 0.000000000000000000, -1.000000000000000000 ) ) ;
#35255=ORIENTED_EDGE ( 'NONE', *, *, #4200, .F. ) ;
#35257=CARTESIAN_POINT ( 'NONE',  ( 53.38272228983590395, -51.31658076067470375, -75.68264719383489592 ) ) ;
#35258=CARTESIAN_POINT ( 'NONE',  ( 60.87207086065609474, 14.42513991272290141, -47.67718664521559901 ) ) ;
#35262=CARTESIAN_POINT ( 'NONE',  ( 40.64814218619559938, -44.65225711300990241, -4.018323718197319927 ) ) ;
#35263=CARTESIAN_POINT ( 'NONE',  ( -6.149347183000639205, 15.38699437488089927, -5.438307061430879052 ) ) ;
#35264=CARTESIAN_POINT ( 'NONE',  ( 46.64446957347233536, 22.34959160277791668, -76.02856692476716205 ) ) ;
#35269=CARTESIAN_POINT ( 'NONE',  ( 44.59670004653540332, 14.86796560598379990, -8.701614582662479336 ) ) ;
#35272=CARTESIAN_POINT ( 'NONE',  ( 14.40169973178839946, 19.62547192528419870, -21.38758215360849846 ) ) ;
#35274=AXIS2_PLACEMENT_3D ( 'NONE', #4458, #20428, #32726 ) ;
#35278=CARTESIAN_POINT ( 'NONE',  ( 48.73759501478280498, -54.04467100006880287, -55.00375600211459926 ) ) ;
#35279=CARTESIAN_POINT ( 'NONE',  ( -33.86606260230205123, -20.49712430492939319, -57.75434594776565689 ) ) ;
#35285=ORIENTED_EDGE ( 'NONE', *, *, #18392, .F. ) ;
#35288=CARTESIAN_POINT ( 'NONE',  ( 61.12977893007705177, 14.02110085376754256, -27.62651976406664645 ) ) ;
#35289=CARTESIAN_POINT ( 'NONE',  ( 7.433595052712601792, 30.13535813643414585, -19.83583517853763922 ) ) ;
#35291=CARTESIAN_POINT ( 'NONE',  ( 11.13393739769619906, -15.61618894467929941, -21.14999999999999858 ) ) ;
#35296=CARTESIAN_POINT ( 'NONE',  ( 84.32823919854369876, -43.96175172734450598, -47.43652016892809797 ) ) ;
#35299=EDGE_LOOP ( 'NONE', ( #30547, #4826, #48052 ) ) ;
#35302=CARTESIAN_POINT ( 'NONE',  ( 76.42858925763616185, -23.05672696190767823, -12.91970068794330473 ) ) ;
#35303=CARTESIAN_POINT ( 'NONE',  ( 11.41669899830660029, -65.09235379784719555, -46.91455955995500204 ) ) ;
#35310=CARTESIAN_POINT ( 'NONE',  ( 59.16375433153790198, -3.121456158035090134, -15.65965500696370150 ) ) ;
#35311=CARTESIAN_POINT ( 'NONE',  ( 51.84245873739460819, -49.36807171846500353, -76.99756697886049039 ) ) ;
#35318=DIRECTION ( 'NONE',  ( 0.000000000000000000, 0.000000000000000000, -1.000000000000000000 ) ) ;
#35319=CARTESIAN_POINT ( 'NONE',  ( 55.00894225620579903, -45.11618894467940066, -13.91244749253660018 ) ) ;
#35321=EDGE_CURVE ( 'NONE', #42937, #32383, #29744, .T. ) ;
#35322=CARTESIAN_POINT ( 'NONE',  ( 13.86909323948740180, -50.63828459097629775, -21.27400668797699979 ) ) ;
#35325=CARTESIAN_POINT ( 'NONE',  ( 56.65303980391289684, 13.95236716656019915, -16.48307942864150277 ) ) ;
#35327=CARTESIAN_POINT ( 'NONE',  ( 56.76343337132740174, -50.53654875555030657, -53.08899915645069711 ) ) ;
#35330=ORIENTED_EDGE ( 'NONE', *, *, #17441, .T. ) ;
#35331=CARTESIAN_POINT ( 'NONE',  ( 11.67619942398487609, -64.89165360645621661, -46.39999999999999858 ) ) ;
#35336=DIRECTION ( 'NONE',  ( 0.4145156864928219442, 0.9100421669633690369, 0.000000000000000000 ) ) ;
#35337=CARTESIAN_POINT ( 'NONE',  ( 11.73319001778020088, 34.19002770849310480, -18.17421237891140251 ) ) ;
#35339=CARTESIAN_POINT ( 'NONE',  ( 52.28356737878640814, 18.56723623979891258, -77.20029292997260484 ) ) ;
#35341=CARTESIAN_POINT ( 'NONE',  ( -11.09431950376199971, -42.12535119660120131, -6.431359894498750229 ) ) ;
#35342=CARTESIAN_POINT ( 'NONE',  ( 49.72648160330969347, 22.41435850158130094, -55.11972614036070439 ) ) ;
#35344=CIRCLE ( 'NONE', #33690, 39.99999999999999289 ) ;
#35345=CARTESIAN_POINT ( 'NONE',  ( 53.21884732239679749, -49.50316525696469228, -49.08533780779099942 ) ) ;
#35347=ORIENTED_EDGE ( 'NONE', *, *, #41328, .F. ) ;
#35349=DIRECTION ( 'NONE',  ( 0.000000000000000000, 0.000000000000000000, 1.000000000000000000 ) ) ;
#35350=CARTESIAN_POINT ( 'NONE',  ( 14.18765051980080116, 19.87404487058600111, -22.27225542063749941 ) ) ;
#35353=CARTESIAN_POINT ( 'NONE',  ( 52.67198247596510186, 18.54881933231609992, -48.75776900890529930 ) ) ;
#35354=CARTESIAN_POINT ( 'NONE',  ( 55.76692108999159814, -45.94014556479540090, -17.15567225542880081 ) ) ;
#35355=DIRECTION ( 'NONE',  ( 0.000000000000000000, -3.043741000000000191E-10, -1.000000000000000000 ) ) ;
#35359=ORIENTED_EDGE ( 'NONE', *, *, #49532, .F. ) ;
#35361=CARTESIAN_POINT ( 'NONE',  ( 11.08386367325309863, -65.09065137991299821, -17.36951596971170275 ) ) ;
#35362=CARTESIAN_POINT ( 'NONE',  ( 9.063308985014520758, 32.62929763590770449, -46.73460937141010163 ) ) ;
#35367=CARTESIAN_POINT ( 'NONE',  ( 68.13393739769620083, 1.883811055320649963, -65.65000000000000568 ) ) ;
#35369=EDGE_LOOP ( 'NONE', ( #36186, #33419, #31556, #23726 ) ) ;
#35370=CARTESIAN_POINT ( 'NONE',  ( 61.32241497109522044, 14.33206721631021274, -47.63528208083148030 ) ) ;
#35371=CARTESIAN_POINT ( 'NONE',  ( 11.13393739769619906, -63.33602264272540339, -43.74835161547929374 ) ) ;
#35372=CARTESIAN_POINT ( 'NONE',  ( -1.021187420881286778, 10.64619438059237311, -20.85710678118654471 ) ) ;
#35373=ORIENTED_EDGE ( 'NONE', *, *, #23701, .T. ) ;
#35374=DIRECTION ( 'NONE',  ( -0.3918900565005491998, -0.9200120562340454722, 0.000000000000000000 ) ) ;
#35377=VERTEX_POINT ( 'NONE', #48283 ) ;
#35379=CARTESIAN_POINT ( 'NONE',  ( 50.96213159729676789, 19.72522742365540083, -76.14999999999994884 ) ) ;
#35385=ORIENTED_EDGE ( 'NONE', *, *, #47379, .F. ) ;
#35386=EDGE_CURVE ( 'NONE', #7646, #17962, #22109, .T. ) ;
#35388=LINE ( 'NONE', #2919, #17520 ) ;
#35389=B_SPLINE_CURVE_WITH_KNOTS ( 'NONE', 3,
 ( #7761, #11441, #15875, #39472, #43148, #23191, #27655, #27399 ),
 .UNSPECIFIED., .F., .F.,
 ( 4, 2, 2, 4 ),
 ( -0.6744302025021630120, -0.3586151102909330146, -0.07393671731179696227, 0.000000000000000000 ),
 .UNSPECIFIED. ) ;
#35391=VECTOR ( 'NONE', #49379, 1000.000000000000000 ) ;
#35392=CARTESIAN_POINT ( 'NONE',  ( 52.66091685537959677, -49.78821585947670059, -48.73922092854849808 ) ) ;
#35393=CARTESIAN_POINT ( 'NONE',  ( 47.16461778607949640, 13.88381105532070059, -8.336225867471998896 ) ) ;
#35395=CARTESIAN_POINT ( 'NONE',  ( 47.35709157879159648, 23.41982112160560092, -74.50100479479878857 ) ) ;
#35396=FACE_OUTER_BOUND ( 'NONE', #26472, .T. ) ;
#35398=CARTESIAN_POINT ( 'NONE',  ( 12.15898433499079978, 33.83644259906850493, -16.45263499445269773 ) ) ;
#35403=CARTESIAN_POINT ( 'NONE',  ( 55.64373403256560380, -50.62227426193150137, -76.08015027475811110 ) ) ;
#35404=CARTESIAN_POINT ( 'NONE',  ( -10.40730447694229888, 11.61126731243840027, -6.269948428629449566 ) ) ;
#35407=DIRECTION ( 'NONE',  ( -1.000000000000000000, 2.473715676742926917E-14, 0.000000000000000000 ) ) ;
#35409=CARTESIAN_POINT ( 'NONE',  ( 53.06963669637619319, -49.53524040181889632, -48.79723990372909981 ) ) ;
#35410=CARTESIAN_POINT ( 'NONE',  ( 47.67130882769900069, 23.27448986115780016, -54.89754209372490124 ) ) ;
#35411=CARTESIAN_POINT ( 'NONE',  ( 57.84505944371250052, -45.56276322640520249, -26.25163502090950018 ) ) ;
#35413=CARTESIAN_POINT ( 'NONE',  ( 13.29233961917630147, 19.36776406713639886, -21.35982916590099734 ) ) ;
#35416=CARTESIAN_POINT ( 'NONE',  ( 51.47835655202189997, 18.57467637314109865, -76.47682125365790284 ) ) ;
#35417=CARTESIAN_POINT ( 'NONE',  ( 52.86806023909759489, 18.40847406621560012, -48.68114467674470092 ) ) ;
#35419=LINE ( 'NONE', #3976, #4986 ) ;
#35420=CARTESIAN_POINT ( 'NONE',  ( 51.29354596943910138, 21.74684883274469982, -54.72842898864520578 ) ) ;
#35421=B_SPLINE_CURVE_WITH_KNOTS ( 'NONE', 3,
 ( #8385, #257, #28541, #4445, #16243, #16497 ),
 .UNSPECIFIED., .F., .F.,
 ( 4, 2, 4 ),
 ( 0.000000000000000000, 0.2512731404157662607, 0.5025462808315325214 ),
 .UNSPECIFIED. ) ;
#35423=AXIS2_PLACEMENT_3D ( 'NONE', #44627, #49615, #37025 ) ;
#35427=CARTESIAN_POINT ( 'NONE',  ( 60.61936386226810214, -29.82345567790940066, -15.97700830362510160 ) ) ;
#35431=AXIS2_PLACEMENT_3D ( 'NONE', #27056, #50913, #15007 ) ;
#35437=ORIENTED_EDGE ( 'NONE', *, *, #41564, .F. ) ;
#35438=DIRECTION ( 'NONE',  ( 0.8320502943378731420, 1.839589000000000426E-27, -0.5547001962251850715 ) ) ;
#35441=CARTESIAN_POINT ( 'NONE',  ( 55.83268520914499788, -46.02255925261680147, -25.40756166689039830 ) ) ;
#35447=CARTESIAN_POINT ( 'NONE',  ( 11.09688807260409860, 33.08637917209059509, -23.87186459811089989 ) ) ;
#35451=CARTESIAN_POINT ( 'NONE',  ( 51.35264461321370533, 0.6974074393915098424, -17.41533276683830422 ) ) ;
#35452=CARTESIAN_POINT ( 'NONE',  ( 10.81643727141089961, 33.72113552640900025, -17.63284883033089656 ) ) ;
#35455=CARTESIAN_POINT ( 'NONE',  ( 61.58903658307470153, -29.46446663135400001, -16.00793433331780236 ) ) ;
#35456=( BOUNDED_CURVE ( )  B_SPLINE_CURVE ( 3, ( #46643, #38506, #34031, #26171 ),
 .UNSPECIFIED., .F., .T. ) 
 B_SPLINE_CURVE_WITH_KNOTS ( ( 4, 4 ),
 ( 0.000000000000000000, 1.220017676946477003 ),
 .UNSPECIFIED. ) 
 CURVE ( )  GEOMETRIC_REPRESENTATION_ITEM ( )  RATIONAL_B_SPLINE_CURVE ( ( 1.000000000000000000, 0.8797619696931662236, 0.8797619696931662236, 1.000000000000000000 ) ) 
 REPRESENTATION_ITEM ( '' )  );
#35458=CARTESIAN_POINT ( 'NONE',  ( 47.02648735467300156, -54.07884064525359946, -75.65465545553870186 ) ) ;
#35461=CARTESIAN_POINT ( 'NONE',  ( 42.04041500005769194, 14.50277640103930032, -6.805323752375540103 ) ) ;
#35463=AXIS2_PLACEMENT_3D ( 'NONE', #6695, #10365, #1718 ) ;
#35465=CARTESIAN_POINT ( 'NONE',  ( 82.76927220787739259, -45.23714010519090323, -47.14638044783710313 ) ) ;
#35467=CARTESIAN_POINT ( 'NONE',  ( 60.91810547036719470, 13.88381111439859872, -26.64295475793029766 ) ) ;
#35471=CARTESIAN_POINT ( 'NONE',  ( 52.82976017067200303, -49.66091843452839782, -28.15000000000000213 ) ) ;
#35473=CARTESIAN_POINT ( 'NONE',  ( 15.94238461914479821, -50.98711296417160099, -20.23090583108240281 ) ) ;
#35474=CARTESIAN_POINT ( 'NONE',  ( 76.15791883449350053, -18.73183087738710029, -12.10556864792070009 ) ) ;
#35475=CARTESIAN_POINT ( 'NONE',  ( 75.44523968101177047, 12.62269330545501056, -13.52496103299877817 ) ) ;
#35478=DIRECTION ( 'NONE',  ( 0.000000000000000000, -1.000000000000000000, 0.000000000000000000 ) ) ;
#35479=CARTESIAN_POINT ( 'NONE',  ( 10.12791152504585490, -55.17571126438489415, -23.14397412734965442 ) ) ;
#35480=CARTESIAN_POINT ( 'NONE',  ( 82.81464131963001307, 11.88381105532070059, -49.28546657628889704 ) ) ;
#35481=CARTESIAN_POINT ( 'NONE',  ( 82.54539245911229273, -45.15147844613900219, -46.85686783343579975 ) ) ;
#35482=CARTESIAN_POINT ( 'NONE',  ( 57.32397924865310301, -50.46483022149049447, -53.14987063508399956 ) ) ;
#35483=CARTESIAN_POINT ( 'NONE',  ( 41.87524974339859796, 13.12449424351239990, -5.012953160694429755 ) ) ;
#35484=CARTESIAN_POINT ( 'NONE',  ( 47.64115382883381500, -54.53453007756522197, -74.19838441416023045 ) ) ;
#35486=CARTESIAN_POINT ( 'NONE',  ( 57.45452828658709876, -47.23787284142349563, -47.71980555553449932 ) ) ;
#35487=CARTESIAN_POINT ( 'NONE',  ( 69.22748654599975282, -50.70395984887971252, -73.25000000000218847 ) ) ;
#35489=CARTESIAN_POINT ( 'NONE',  ( 66.71250208829920325, -1.458054078887639937, -17.03570979604049995 ) ) ;
#35490=CARTESIAN_POINT ( 'NONE',  ( 18.21961131258260380, -52.14694418483640703, -75.69083100613939052 ) ) ;
#35491=CARTESIAN_POINT ( 'NONE',  ( 50.09219850407249908, -44.97296149410799870, -7.597817017042959975 ) ) ;
#35494=CARTESIAN_POINT ( 'NONE',  ( 14.16187783161720048, 19.11875810978959933, -20.85710678118659800 ) ) ;
#35495=FACE_BOUND ( 'NONE', #3029, .T. ) ;
#35497=DIRECTION ( 'NONE',  ( -1.000000000000000000, 0.000000000000000000, 0.000000000000000000 ) ) ;
#35500=DIRECTION ( 'NONE',  ( -0.3294064756441338893, -0.9441882088883076785, 0.000000000000000000 ) ) ;
#35502=ADVANCED_FACE ( 'NONE', ( #45126 ), #2868, .T. ) ;
#35503=VERTEX_POINT ( 'NONE', #17096 ) ;
#35504=CARTESIAN_POINT ( 'NONE',  ( 17.53794073517549990, 21.17773733622360410, -76.03043890231919022 ) ) ;
#35505=ORIENTED_EDGE ( 'NONE', *, *, #48493, .F. ) ;
#35511=CARTESIAN_POINT ( 'NONE',  ( 61.63216019317309957, 14.00749853620810015, -47.06783276606689981 ) ) ;
#35518=LINE ( 'NONE', #38946, #23290 ) ;
#35519=CARTESIAN_POINT ( 'NONE',  ( 51.84413677266599763, -51.33743803777170456, -76.02231597519390505 ) ) ;
#35520=CARTESIAN_POINT ( 'NONE',  ( 60.69877040361549092, 14.44127893251400074, -47.62175228562969664 ) ) ;
#35524=CARTESIAN_POINT ( 'NONE',  ( -7.971602555222980335, 13.89700050900779971, -5.685733215756870074 ) ) ;
#35527=ADVANCED_FACE ( 'NONE', ( #9994 ), #29387, .F. ) ;
#35532=EDGE_CURVE ( 'NONE', #20094, #39800, #21254, .T. ) ;
#35533=CIRCLE ( 'NONE', #30506, 1.999999999999997558 ) ;
#35534=CARTESIAN_POINT ( 'NONE',  ( 57.28143945796900027, 19.37965786551299985, -53.75925914748309964 ) ) ;
#35538=CARTESIAN_POINT ( 'NONE',  ( 15.70006563680709988, 19.64728943285669871, -20.26432904851870020 ) ) ;
#35542=CARTESIAN_POINT ( 'NONE',  ( 48.58275802200249416, -54.12519460547050443, -55.12629154858839797 ) ) ;
#35546=CARTESIAN_POINT ( 'NONE',  ( 47.84066234768640413, 23.15588260058000003, -54.73860067540169894 ) ) ;
#35549=CARTESIAN_POINT ( 'NONE',  ( 87.61621807841599718, 1.883811055320649963, -61.12885639714370001 ) ) ;
#35552=CARTESIAN_POINT ( 'NONE',  ( 60.50030625420910013, -45.69302653460029973, -47.49279232948880036 ) ) ;
#35553=CARTESIAN_POINT ( 'NONE',  ( 16.13393739769620083, -15.61618894467929941, 7.944363289481099599 ) ) ;
#35558=CARTESIAN_POINT ( 'NONE',  ( 56.57438608727660068, 19.50039335391339890, -53.83822343184270665 ) ) ;
#35559=EDGE_CURVE ( 'NONE', #29501, #9653, #39715, .T. ) ;
#35563=ORIENTED_EDGE ( 'NONE', *, *, #27033, .T. ) ;
#35565=CARTESIAN_POINT ( 'NONE',  ( 7.853097003783780394, -60.52042854835909935, -20.86915960608759946 ) ) ;
#35567=CARTESIAN_POINT ( 'NONE',  ( 8.875293479575059763, -63.51482374901029715, -46.68678635115289666 ) ) ;
#35569=ORIENTED_EDGE ( 'NONE', *, *, #13218, .T. ) ;
#35570=CARTESIAN_POINT ( 'NONE',  ( 56.10252018248599626, 19.69840918101340321, -53.89291062689480327 ) ) ;
#35571=CIRCLE ( 'NONE', #18023, 4.000000000000050626 ) ;
#35573=CARTESIAN_POINT ( 'NONE',  ( 56.50147281689459788, -50.73097677643320225, -53.50280580149859588 ) ) ;
#35575=CARTESIAN_POINT ( 'NONE',  ( 71.63393739769620083, -15.61618894467929941, -10.21818181818179916 ) ) ;
#35576=CARTESIAN_POINT ( 'NONE',  ( 62.92431185641218860, -0.4811861693229420034, -16.47144764524460214 ) ) ;
#35577=CARTESIAN_POINT ( 'NONE',  ( 51.34762213876319947, -48.99373472892960280, -76.60870781533139962 ) ) ;
#35578=CARTESIAN_POINT ( 'NONE',  ( 47.40322300430479885, -54.65574458090379295, -64.38029159777090626 ) ) ;
#35583=B_SPLINE_CURVE_WITH_KNOTS ( 'NONE', 3,
 ( #2305, #42406, #17518, #22459, #50525, #18543, #33489, #49503, #41884, #13592, #29556, #39757, #27692, #31095, #15396, #47125 ),
 .UNSPECIFIED., .F., .F.,
 ( 4, 2, 2, 2, 2, 2, 2, 4 ),
 ( -4.585261641054179549, -4.291753173737439475, -3.753927176172620062, -2.893405580068910243, -2.204988303185950294, -1.516571026302980130, -0.4151033832902326637, 0.01085480678109984609 ),
 .UNSPECIFIED. ) ;
#35586=CARTESIAN_POINT ( 'NONE',  ( 12.86227365120030086, -49.99703835600479351, -21.07384430431449829 ) ) ;
#35587=CARTESIAN_POINT ( 'NONE',  ( 56.77603274427010405, 19.38693246832160000, -75.16653984338270789 ) ) ;
#35589=CARTESIAN_POINT ( 'NONE',  ( 68.13393739769790614, -49.95860450174320277, -71.35146707679190570 ) ) ;
#35590=CARTESIAN_POINT ( 'NONE',  ( 61.22240636566869654, -45.33348669533059905, -47.17363803446809811 ) ) ;
#35591=DIRECTION ( 'NONE',  ( 0.000000000000000000, 1.000000000000000000, 0.000000000000000000 ) ) ;
#35596=CARTESIAN_POINT ( 'NONE',  ( 13.96137116643440024, -51.22777015964090452, -74.58518005236030035 ) ) ;
#35597=EDGE_CURVE ( 'NONE', #362, #8932, #45390, .T. ) ;
#35599=CARTESIAN_POINT ( 'NONE',  ( 44.73511642677699740, -46.10436220937679508, -8.795271389338660484 ) ) ;
#35600=CIRCLE ( 'NONE', #36407, 1.000000000000000888 ) ;
#35603=CARTESIAN_POINT ( 'NONE',  ( 10.72320681400480069, -64.90816318788569106, -17.84617904804760258 ) ) ;
#35604=CIRCLE ( 'NONE', #1307, 20.79999999999999716 ) ;
#35609=DIRECTION ( 'NONE',  ( 0.000000000000000000, 0.000000000000000000, 1.000000000000000000 ) ) ;
#35610=CARTESIAN_POINT ( 'NONE',  ( 49.45469051709869746, 22.31164040509669988, -54.26811687044270371 ) ) ;
#35612=CARTESIAN_POINT ( 'NONE',  ( 52.65605657214259594, -49.77872703647310715, -48.59647644059229776 ) ) ;
#35613=VERTEX_POINT ( 'NONE', #5562 ) ;
#35620=CARTESIAN_POINT ( 'NONE',  ( 52.56949858562949629, 18.62486711300499920, -48.49330934070029997 ) ) ;
#35621=CARTESIAN_POINT ( 'NONE',  ( 57.24436374624130508, -45.12772278168660023, -17.69927926731909906 ) ) ;
#35622=EDGE_CURVE ( 'NONE', #5583, #34588, #12116, .T. ) ;
#35623=LINE ( 'NONE', #51610, #18114 ) ;
#35625=VERTEX_POINT ( 'NONE', #18361 ) ;
#35629=CARTESIAN_POINT ( 'NONE',  ( 11.62127297442820151, -65.32903965486170250, -17.36671640434929742 ) ) ;
#35630=CARTESIAN_POINT ( 'NONE',  ( 13.00893739769619906, 34.28605925116850273, -47.75434321273180416 ) ) ;
#35633=CARTESIAN_POINT ( 'NONE',  ( 11.62625575059174388, -65.37594719773773022, -22.52256012421784348 ) ) ;
#35638=AXIS2_PLACEMENT_3D ( 'NONE', #22635, #35213, #30756 ) ;
#35639=CARTESIAN_POINT ( 'NONE',  ( 11.10572538624809980, -63.45979201291619631, -44.26003604607290498 ) ) ;
#35640=CARTESIAN_POINT ( 'NONE',  ( 66.23540447448930024, 18.72622661238738573, -69.60146707679315625 ) ) ;
#35641=EDGE_LOOP ( 'NONE', ( #43293, #31155, #40737, #51020, #26060 ) ) ;
#35643=CARTESIAN_POINT ( 'NONE',  ( 56.85837506870640112, 19.39490789456009878, -53.45324575393789956 ) ) ;
#35645=EDGE_LOOP ( 'NONE', ( #45183, #49302, #21304, #50285 ) ) ;
#35647=DIRECTION ( 'NONE',  ( 0.3805321250008311118, 0.000000000000000000, -0.9247677015566405645 ) ) ;
#35649=CARTESIAN_POINT ( 'NONE',  ( 60.36615763377369603, 14.63541242539259990, -47.74315751841469790 ) ) ;
#35655=ORIENTED_EDGE ( 'NONE', *, *, #21166, .F. ) ;
#35657=CARTESIAN_POINT ( 'NONE',  ( 52.90415637000559457, -49.66383135056049980, -49.01931408368830034 ) ) ;
#35660=DIRECTION ( 'NONE',  ( 0.6668512999106330774, -0.3436531272335560661, -0.6612199875609450217 ) ) ;
#35661=CARTESIAN_POINT ( 'NONE',  ( 47.25421481023769843, 23.38596379756510046, -74.80705470093730014 ) ) ;
#35662=ADVANCED_FACE ( 'NONE', ( #46694 ), #30492, .T. ) ;
#35663=LINE ( 'NONE', #30681, #40970 ) ;
#35666=CARTESIAN_POINT ( 'NONE',  ( 11.93287529299120031, 33.86695641789320632, -16.56789608241509626 ) ) ;
#35669=CARTESIAN_POINT ( 'NONE',  ( 55.48119774689679673, -46.46934856230480193, -25.44854998053999751 ) ) ;
#35671=CARTESIAN_POINT ( 'NONE',  ( 55.66467133867650574, -50.64778639553559714, -75.85212640423078767 ) ) ;
#35672=CARTESIAN_POINT ( 'NONE',  ( -0.9227428731364130110, 21.52761613755500036, -9.384612575603730633 ) ) ;
#35675=CARTESIAN_POINT ( 'NONE',  ( 61.25410332236540256, 14.01664428061980061, -46.70604314720559813 ) ) ;
#35677=CARTESIAN_POINT ( 'NONE',  ( 72.13393739769620083, -1.116188944679340045, -20.65000000000000213 ) ) ;
#35679=CARTESIAN_POINT ( 'NONE',  ( 52.79916199400859966, -49.67749117070789566, -48.53936745044679668 ) ) ;
#35680=CARTESIAN_POINT ( 'NONE',  ( 59.90835834505130464, -45.34291689336190245, -26.75034159233819864 ) ) ;
#35682=CARTESIAN_POINT ( 'NONE',  ( 61.50409964634459925, -45.37406455498979341, -47.35437808299670337 ) ) ;
#35684=CARTESIAN_POINT ( 'NONE',  ( 52.11372286138289667, 18.47999854749260251, -77.07264542598700530 ) ) ;
#35685=CARTESIAN_POINT ( 'NONE',  ( 53.13753015649290035, 18.27140341915590227, -48.89206902239920538 ) ) ;
#35686=CARTESIAN_POINT ( 'NONE',  ( -14.86606260230379917, -15.61618894467929941, -20.15000000000000213 ) ) ;
#35688=VERTEX_POINT ( 'NONE', #39081 ) ;
#35691=CARTESIAN_POINT ( 'NONE',  ( 47.69847251993340365, -54.50500465509079362, -55.01789699801200584 ) ) ;
#35694=CARTESIAN_POINT ( 'NONE',  ( 60.83822960227499976, -30.17641036977770241, -16.10447917479509883 ) ) ;
#35698=CARTESIAN_POINT ( 'NONE',  ( 68.13393739769630031, -48.11618894467697061, -70.54999999999976978 ) ) ;
#35699=AXIS2_PLACEMENT_3D ( 'NONE', #29982, #46006, #34441 ) ;
#35700=CARTESIAN_POINT ( 'NONE',  ( 60.90240720208950620, -45.28704519797054928, -27.40842581354857188 ) ) ;
#35701=ORIENTED_EDGE ( 'NONE', *, *, #30369, .T. ) ;
#35704=CARTESIAN_POINT ( 'NONE',  ( 49.87066309494894512, -29.65878804270703029, -15.89390192910206068 ) ) ;
#35705=VERTEX_POINT ( 'NONE', #31177 ) ;
#35706=DIRECTION ( 'NONE',  ( 0.000000000000000000, 0.000000000000000000, 1.000000000000000000 ) ) ;
#35711=CARTESIAN_POINT ( 'NONE',  ( 63.88393739769619373, 20.38443354211860026, -61.34712802272770915 ) ) ;
#35713=AXIS2_PLACEMENT_3D ( 'NONE', #49342, #1626, #38306 ) ;
#35716=CARTESIAN_POINT ( 'NONE',  ( 64.76670119014970339, -29.83072655109479854, -16.45448121326970181 ) ) ;
#35717=CARTESIAN_POINT ( 'NONE',  ( 14.34417029195965476, 19.88381105532280557, -74.33587756533812296 ) ) ;
#35719=CARTESIAN_POINT ( 'NONE',  ( 55.65311171412380276, 14.73495305830999946, -16.92919767242679896 ) ) ;
#35720=CARTESIAN_POINT ( 'NONE',  ( 41.13178742825800072, 13.81684675789199979, -5.658924883871920386 ) ) ;
#35722=CARTESIAN_POINT ( 'NONE',  ( 9.446663254046249847, 23.82152373690511382, -46.46212477756636616 ) ) ;
#35724=CARTESIAN_POINT ( 'NONE',  ( 83.99291904213089310, -44.37437668906760280, -47.15152633430140838 ) ) ;
#35731=CARTESIAN_POINT ( 'NONE',  ( 12.13729495418210114, -65.03660448042120379, -16.30611525569679898 ) ) ;
#35732=CARTESIAN_POINT ( 'NONE',  ( 50.93875529876952868, -35.32972334367127587, -76.36830481639776735 ) ) ;
#35733=CARTESIAN_POINT ( 'NONE',  ( 61.75019934789347076, -45.11618894468048779, -46.51053312274786578 ) ) ;
#35735=VERTEX_POINT ( 'NONE', #35120 ) ;
#35736=CARTESIAN_POINT ( 'NONE',  ( -5.675882129932829478, -46.90160876882899998, -5.248560459082940000 ) ) ;
#35737=CARTESIAN_POINT ( 'NONE',  ( 47.18324198357279897, 23.57489020266570279, -54.61058319554400242 ) ) ;
#35738=AXIS2_PLACEMENT_3D ( 'NONE', #15642, #31595, #38983 ) ;
#35741=CARTESIAN_POINT ( 'NONE',  ( 57.55751162054249903, -50.55753267974190379, -53.43780795143099738 ) ) ;
#35742=CARTESIAN_POINT ( 'NONE',  ( 42.88515050839449572, 12.54233113675140032, -4.897272209574110136 ) ) ;
#35745=CARTESIAN_POINT ( 'NONE',  ( 53.87565362894249432, -49.13748779640440034, -48.87968056552790586 ) ) ;
#35747=CARTESIAN_POINT ( 'NONE',  ( 66.54986620728139712, -1.029621168181320101, -16.95609984218899768 ) ) ;
#35748=CARTESIAN_POINT ( 'NONE',  ( 17.58070283336819983, -52.47980496485550361, -76.04476946176040997 ) ) ;
#35752=CARTESIAN_POINT ( 'NONE',  ( 55.02371555901009970, -47.79053722659219972, -47.27949281187280661 ) ) ;
#35757=CARTESIAN_POINT ( 'NONE',  ( -10.90401617485185604, -41.47682395427644764, -20.56421356237309439 ) ) ;
#35760=CARTESIAN_POINT ( 'NONE',  ( 17.34361748118760005, 21.51730579194029858, -76.12465403027070465 ) ) ;
#35761=ORIENTED_EDGE ( 'NONE', *, *, #41504, .F. ) ;
#35762=VERTEX_POINT ( 'NONE', #43270 ) ;
#35763=CARTESIAN_POINT ( 'NONE',  ( 57.07404348378830861, -45.88224062731829633, -26.24937804946210207 ) ) ;
#35765=( BOUNDED_SURFACE ( )  B_SPLINE_SURFACE ( 2, 2, ( 
 ( #14797, #47303, #27101, #27355, #35221, #38660, #15318, #43361, #23406 ),
 ( #22897, #39427, #2748, #19497, #46785, #42849, #42325, #10874, #50448 ),
 ( #6425, #22382, #38387, #2484, #14535, #30505, #46529, #26572, #42586 ),
 ( #22643, #26839, #3005, #32294, #40706, #605, #35487, #44124, #4036 ),
 ( #48062, #4804, #15823, #15578, #4283, #51479, #27612, #16338, #44635 ) ),
 .UNSPECIFIED., .F., .T., .T. ) 
 B_SPLINE_SURFACE_WITH_KNOTS ( ( 3, 2, 3 ),
 ( 3, 2, 2, 2, 3 ),
 ( -0.003205554299145560102, 0.8238407534178779912, 1.650887061134900025 ),
 ( -3.141592653589790007, -1.570796326794899889, 0.000000000000000000, 1.570796326794899889, 3.141592653589790007 ),
 .UNSPECIFIED. ) 
 GEOMETRIC_REPRESENTATION_ITEM ( )  RATIONAL_B_SPLINE_SURFACE ( (
 ( 1.000000000000000000, 0.7071067811865480168, 1.000000000000000000, 0.7071067811865480168, 1.000000000000000000, 0.7071067811865480168, 1.000000000000000000, 0.7071067811865480168, 1.000000000000000000),
 ( 0.9157107718028779653, 0.6475052963473819645, 0.9157107718028779653, 0.6475052963473819645, 0.9157107718028779653, 0.6475052963473819645, 0.9157107718028779653, 0.6475052963473819645, 0.9157107718028779653),
 ( 1.000000000000000000, 0.7071067811865480168, 1.000000000000000000, 0.7071067811865480168, 1.000000000000000000, 0.7071067811865480168, 1.000000000000000000, 0.7071067811865480168, 1.000000000000000000),
 ( 0.9157107718028449916, 0.6475052963473589829, 0.9157107718028449916, 0.6475052963473589829, 0.9157107718028449916, 0.6475052963473589829, 0.9157107718028449916, 0.6475052963473589829, 0.9157107718028449916),
 ( 1.000000000000000000, 0.7071067811865480168, 1.000000000000000000, 0.7071067811865480168, 1.000000000000000000, 0.7071067811865480168, 1.000000000000000000, 0.7071067811865480168, 1.000000000000000000) ) ) 
 REPRESENTATION_ITEM ( '' )  SURFACE ( )  );
#35768=EDGE_CURVE ( 'NONE', #51745, #51329, #22290, .T. ) ;
#35769=ORIENTED_EDGE ( 'NONE', *, *, #23403, .F. ) ;
#35770=FACE_OUTER_BOUND ( 'NONE', #1085, .T. ) ;
#35773=CARTESIAN_POINT ( 'NONE',  ( 83.95017420394412966, 13.51629706050414370, -47.46180916972096497 ) ) ;
#35774=ORIENTED_EDGE ( 'NONE', *, *, #50275, .F. ) ;
#35777=CARTESIAN_POINT ( 'NONE',  ( 16.13393739769620083, -15.61618894467929941, 6.789625226207629538 ) ) ;
#35778=CARTESIAN_POINT ( 'NONE',  ( 61.28822732917949878, 14.34385274781909914, -47.65091293713199860 ) ) ;
#35780=CARTESIAN_POINT ( 'NONE',  ( 65.03603135424580728, -1.463538230407920082, -19.52361391316370032 ) ) ;
#35782=CARTESIAN_POINT ( 'NONE',  ( -7.622325105801039946, 14.20602405906790011, -5.644196242347629955 ) ) ;
#35785=EDGE_CURVE ( 'NONE', #11209, #34917, #42266, .T. ) ;
#35789=CARTESIAN_POINT ( 'NONE',  ( 42.14447631745849776, 14.59219016048480100, -6.935681727894889015 ) ) ;
#35790=CARTESIAN_POINT ( 'NONE',  ( 12.96406378549919935, 34.28324915656980210, -47.66759396750580180 ) ) ;
#35797=CARTESIAN_POINT ( 'NONE',  ( 48.29537619369070001, -54.13523159704990206, -54.65524445810709864 ) ) ;
#35798=CARTESIAN_POINT ( 'NONE',  ( 51.92090233143009215, -32.82639329994397315, -18.96879582027110800 ) ) ;
#35799=CARTESIAN_POINT ( 'NONE',  ( 58.92073396209919878, -3.116188944679349593, -15.65000000000000036 ) ) ;
#35800=B_SPLINE_CURVE_WITH_KNOTS ( 'NONE', 3,
 ( #39076, #35379, #22798, #47707, #3167, #3427, #51632, #34861, #50861, #11290, #27251, #43265, #7354, #39579, #15988, #14954, #19399, #15727 ),
 .UNSPECIFIED., .F., .F.,
 ( 4, 2, 2, 2, 2, 2, 2, 2, 4 ),
 ( 0.000000000000000000, 0.01645396295165469855, 0.1775000000000971079, 0.3375000000000846212, 0.4375000000000769385, 0.5000000000000713873, 0.6250000000000630607, 0.7632212076873368112, 1.000000000000000000 ),
 .UNSPECIFIED. ) ;
#35801=CARTESIAN_POINT ( 'NONE',  ( 47.75420808716030052, 23.23832663738040338, -54.93836825444449801 ) ) ;
#35807=CARTESIAN_POINT ( 'NONE',  ( 60.72309646253260240, -45.59317018174599667, -47.46061744060280319 ) ) ;
#35808=CARTESIAN_POINT ( 'NONE',  ( 47.83393063578103011, -54.38673743207323241, -54.71871010756845521 ) ) ;
#35812=CARTESIAN_POINT ( 'NONE',  ( 16.13393739769620083, -15.61618894467929941, 7.530187386896120216 ) ) ;
#35819=CARTESIAN_POINT ( 'NONE',  ( 52.27429601900837497, -49.79159170706056159, -77.19751337257605428 ) ) ;
#35820=CARTESIAN_POINT ( 'NONE',  ( 76.60309355059160907, -33.99212704518571826, -13.67166368881104965 ) ) ;
#35829=CARTESIAN_POINT ( 'NONE',  ( 62.05917851177209599, -0.7776122089247741176, -16.28509574527020121 ) ) ;
#35830=CARTESIAN_POINT ( 'NONE',  ( 51.50420586855599936, -49.40990438562260323, -76.63112831509690182 ) ) ;
#35835=CARTESIAN_POINT ( 'NONE',  ( 60.30540951500742608, 14.59285682385894845, -47.61343627861142380 ) ) ;
#35836=DIRECTION ( 'NONE',  ( 0.000000000000000000, 0.000000000000000000, 1.000000000000000000 ) ) ;
#35839=DIRECTION ( 'NONE',  ( -0.2260571801428170324, 0.000000000000000000, 0.9741140340359940586 ) ) ;
#35840=CARTESIAN_POINT ( 'NONE',  ( 70.83393739769719843, -48.11618894467220287, -73.25000000000000000 ) ) ;
#35841=CARTESIAN_POINT ( 'NONE',  ( 16.15069456443690044, 19.81939336389048734, -17.90311212357439885 ) ) ;
#35846=EDGE_CURVE ( 'NONE', #12246, #13362, #35421, .T. ) ;
#35848=LINE ( 'NONE', #35331, #23797 ) ;
#35849=CARTESIAN_POINT ( 'NONE',  ( 47.24353709908209709, -54.76064543437800580, -54.64904795778859636 ) ) ;
#35852=CARTESIAN_POINT ( 'NONE',  ( 17.78608069253172275, 20.27135663923038678, -75.33783710294622438 ) ) ;
#35853=CARTESIAN_POINT ( 'NONE',  ( 15.54400293349995543, -50.81696016472969291, -20.39351698354824549 ) ) ;
#35856=CARTESIAN_POINT ( 'NONE',  ( 10.66246720353709954, 33.63422984119760173, -18.01843150758180201 ) ) ;
#35859=CARTESIAN_POINT ( 'NONE',  ( 13.43643019722925303, -51.25329737159583487, -22.14276204152384508 ) ) ;
#35860=DIRECTION ( 'NONE',  ( 2.812429781167509836E-09, -3.628863640055339935E-09, 1.000000000000000000 ) ) ;
#35861=CARTESIAN_POINT ( 'NONE',  ( 49.07389894158890087, 22.56707546824529942, -54.57361176007880488 ) ) ;
#35862=ORIENTED_EDGE ( 'NONE', *, *, #40516, .F. ) ;
#35863=CARTESIAN_POINT ( 'NONE',  ( 52.62463376634079992, -49.80324691087879785, -48.47378032971909789 ) ) ;
#35866=CYLINDRICAL_SURFACE ( 'NONE', #8501, 2.000000000000001776 ) ;
#35867=CARTESIAN_POINT ( 'NONE',  ( 11.89321892211240161, 34.20364954171930094, -18.17421237891140251 ) ) ;
#35868=CARTESIAN_POINT ( 'NONE',  ( 83.11128256222379207, 13.68219656570800069, -46.57919617705099569 ) ) ;
#35871=CARTESIAN_POINT ( 'NONE',  ( 56.39638450836229566, -45.38884808781619995, -17.16969890501229656 ) ) ;
#35872=CARTESIAN_POINT ( 'NONE',  ( 54.11082558918479890, 16.90719386950179626, -26.08329795554919883 ) ) ;
#35873=ORIENTED_EDGE ( 'NONE', *, *, #39466, .T. ) ;
#35876=CARTESIAN_POINT ( 'NONE',  ( 12.01336146540229954, -65.33303523161541193, -17.10865960907919714 ) ) ;
#35877=CARTESIAN_POINT ( 'NONE',  ( 11.81672205559790179, 34.07977438613860244, -47.29989710098740119 ) ) ;
#35880=CARTESIAN_POINT ( 'NONE',  ( 8.801404170410069838, 31.97031994814190270, -46.67014817202279886 ) ) ;
#35881=CARTESIAN_POINT ( 'NONE',  ( 10.80839229981719818, 21.91123435898759908, -23.15000000000000213 ) ) ;
#35884=VERTEX_POINT ( 'NONE', #32198 ) ;
#35885=CARTESIAN_POINT ( 'NONE',  ( 13.61938558349279305, 20.19483563131725035, -22.88820058412975555 ) ) ;
#35886=CARTESIAN_POINT ( 'NONE',  ( 11.10535958650110011, -63.15872092784729830, -44.25018693357320387 ) ) ;
#35887=EDGE_CURVE ( 'NONE', #8473, #33996, #32155, .T. ) ;
#35888=CARTESIAN_POINT ( 'NONE',  ( 68.13393739769706769, 17.98087126524489321, -74.20351669811762463 ) ) ;
#35890=CARTESIAN_POINT ( 'NONE',  ( 11.18784974601570781, -64.00854372606637810, -43.96560395573440871 ) ) ;
#35891=CARTESIAN_POINT ( 'NONE',  ( 56.56050783432609563, 19.48343119352850294, -53.48830978460669883 ) ) ;
#35893=ADVANCED_FACE ( 'NONE', ( #7624 ), #24336, .T. ) ;
#35897=CARTESIAN_POINT ( 'NONE',  ( 52.82975622904289992, 18.42854261028849905, -48.47378032971769812 ) ) ;
#35898=DIRECTION ( 'NONE',  ( 0.000000000000000000, 0.000000000000000000, -1.000000000000000000 ) ) ;
#35903=ORIENTED_EDGE ( 'NONE', *, *, #33100, .T. ) ;
#35908=CARTESIAN_POINT ( 'NONE',  ( 47.37032927764419554, 23.44277963338160120, -74.14999585054489728 ) ) ;
#35912=CIRCLE ( 'NONE', #13340, 1.500000000000001332 ) ;
#35913=CARTESIAN_POINT ( 'NONE',  ( 11.97330428935280011, 33.54929834488839901, -16.08313759590789971 ) ) ;
#35916=CARTESIAN_POINT ( 'NONE',  ( 56.14177628828820588, -50.61618684426799319, -75.89576364164580013 ) ) ;
#35917=CARTESIAN_POINT ( 'NONE',  ( 57.45269164250755267, 19.38381105532069881, -53.92796674552833736 ) ) ;
#35918=DIRECTION ( 'NONE',  ( -0.2260571801428090388, -1.168509733417976470E-14, 0.9741140340359961680 ) ) ;
#35920=CARTESIAN_POINT ( 'NONE',  ( 61.36488470523620009, 14.00771087096500089, -46.95107575060279714 ) ) ;
#35923=CARTESIAN_POINT ( 'NONE',  ( 52.81415492500530462, -49.66954405245009951, -48.60515561007039764 ) ) ;
#35924=CARTESIAN_POINT ( 'NONE',  ( 57.60436885384490324, -45.58916000359799625, -26.22003782303439934 ) ) ;
#35926=CARTESIAN_POINT ( 'NONE',  ( 61.34434154007890072, 14.12414198815389810, -47.30220718113330491 ) ) ;
#35928=CARTESIAN_POINT ( 'NONE',  ( 51.81521015446629974, 18.95104292838230009, -76.50775191966720001 ) ) ;
#35929=CARTESIAN_POINT ( 'NONE',  ( 53.45012425301570147, 18.11191960133640322, -48.87690323765099976 ) ) ;
#35931=CARTESIAN_POINT ( 'NONE',  ( 53.00700885799259510, -49.56805288106040308, -48.78176285252619948 ) ) ;
#35934=CARTESIAN_POINT ( 'NONE',  ( 47.64800064284560221, -54.53209002898449853, -55.13447052885069866 ) ) ;
#35937=CARTESIAN_POINT ( 'NONE',  ( 61.21881494710749649, -30.86421509516850037, -16.47078615167890092 ) ) ;
#35940=CARTESIAN_POINT ( 'NONE',  ( 51.34657278755454968, -34.59080035391762209, -76.64439721256748328 ) ) ;
#35941=ORIENTED_EDGE ( 'NONE', *, *, #15977, .T. ) ;
#35945=CARTESIAN_POINT ( 'NONE',  ( 57.27851913721940491, 18.92138913705230152, -52.63313635947250191 ) ) ;
#35947=CARTESIAN_POINT ( 'NONE',  ( 51.17464648325179155, -31.65168256193422280, -17.11447666815010749 ) ) ;
#35954=CARTESIAN_POINT ( 'NONE',  ( 10.63867022051679179, 32.44496671321559234, -23.65473282282058420 ) ) ;
#35957=CARTESIAN_POINT ( 'NONE',  ( 60.59736966202989805, 14.55571675506389973, -47.75487759591599968 ) ) ;
#35958=AXIS2_PLACEMENT_3D ( 'NONE', #43360, #27866, #28116 ) ;
#35964=CARTESIAN_POINT ( 'NONE',  ( 61.85129338415519840, -29.25620428968700182, -16.03819528988000087 ) ) ;
#35965=CARTESIAN_POINT ( 'NONE',  ( 11.01561765541599947, -63.47447192843999630, -24.03168025771979899 ) ) ;
#35967=CARTESIAN_POINT ( 'NONE',  ( 43.08932009041299693, 14.67167452393280058, -7.588662368344499143 ) ) ;
#35969=CARTESIAN_POINT ( 'NONE',  ( 9.875683499728980408, 23.89112191037431998, -46.19193022289812234 ) ) ;
#35970=CARTESIAN_POINT ( 'NONE',  ( 82.92203328426339226, -45.19260144532690049, -47.12557951548500057 ) ) ;
#35971=DIRECTION ( 'NONE',  ( 0.000000000000000000, 1.474514954580241538E-14, -1.000000000000000000 ) ) ;
#35973=ORIENTED_EDGE ( 'NONE', *, *, #47727, .F. ) ;
#35974=CARTESIAN_POINT ( 'NONE',  ( 55.38239457922570352, -47.12167877862870569, -26.35045493482720147 ) ) ;
#35975=CARTESIAN_POINT ( 'NONE',  ( 14.73074138132800037, -50.58571459616789667, -20.78918949795549764 ) ) ;
#35980=EDGE_LOOP ( 'NONE', ( #8881, #39721, #49989, #1119, #26801 ) ) ;
#35982=CARTESIAN_POINT ( 'NONE',  ( -2.927826903739159992, -49.19980423205150544, -5.740514721019640554 ) ) ;
#35986=AXIS2_PLACEMENT_3D ( 'NONE', #4367, #2194, #38098 ) ;
#35988=CARTESIAN_POINT ( 'NONE',  ( 57.48162049234600346, -50.51349954334200021, -53.28834583854860085 ) ) ;
#35989=CARTESIAN_POINT ( 'NONE',  ( 41.60772419834029989, 13.38923699642720067, -5.233302257662570511 ) ) ;
#35991=DIRECTION ( 'NONE',  ( 0.000000000000000000, 0.000000000000000000, -1.000000000000000000 ) ) ;
#35999=CARTESIAN_POINT ( 'NONE',  ( 8.815605939025839888, 32.05029769251469673, -46.67186391138339729 ) ) ;
#36003=CARTESIAN_POINT ( 'NONE',  ( 17.32180797866010025, 21.73127465433789851, -76.14999999999999147 ) ) ;
#36004=ORIENTED_EDGE ( 'NONE', *, *, #28769, .T. ) ;
#36011=CARTESIAN_POINT ( 'NONE',  ( 61.53217244954870324, 14.11227144105590092, -47.30221341948519864 ) ) ;
#36012=EDGE_CURVE ( 'NONE', #51752, #29183, #27169, .T. ) ;
#36014=ADVANCED_FACE ( 'NONE', ( #44028 ), #3432, .T. ) ;
#36018=CARTESIAN_POINT ( 'NONE',  ( 52.10267382257649871, 1.883811055284760005, -77.60820171200670359 ) ) ;
#36019=AXIS2_PLACEMENT_3D ( 'NONE', #6138, #38106, #45453 ) ;
#36023=DIRECTION ( 'NONE',  ( -1.224650050763873077E-16, 1.000000000000000000, -1.784227544494129617E-11 ) ) ;
#36025=CARTESIAN_POINT ( 'NONE',  ( 60.37925162440420479, 14.51570526242369930, -47.49800878376869662 ) ) ;
#36030=CARTESIAN_POINT ( 'NONE',  ( 41.72053737372350213, -43.71151935359279861, -3.400228435618770195 ) ) ;
#36031=CARTESIAN_POINT ( 'NONE',  ( -5.340849039197499870, 15.73968974017349964, -4.544762132180990122 ) ) ;
#36032=CARTESIAN_POINT ( 'NONE',  ( 46.95605112311885421, 23.06042441339815596, -75.52284329971668342 ) ) ;
#36033=CARTESIAN_POINT ( 'NONE',  ( 60.51336243011509453, 14.11231868582309978, -27.14572052912820155 ) ) ;
#36035=VERTEX_POINT ( 'NONE', #1297 ) ;
#36037=DIRECTION ( 'NONE',  ( -2.217154000000000151E-17, -9.040936000000000316E-17, 1.000000000000000000 ) ) ;
#36038=CARTESIAN_POINT ( 'NONE',  ( 11.20590614228649962, 32.84406522022800345, -44.01467685434810306 ) ) ;
#36043=CARTESIAN_POINT ( 'NONE',  ( 12.91619884388280148, 18.87515571072599840, -21.10294288757389936 ) ) ;
#36044=CARTESIAN_POINT ( 'NONE',  ( 46.97135722600339847, 23.04975284684289960, -75.52157732621060404 ) ) ;
#36045=CARTESIAN_POINT ( 'NONE',  ( 48.61347624589569705, -53.95572845601289913, -54.54157758230459763 ) ) ;
#36046=CARTESIAN_POINT ( 'NONE',  ( 51.85725430794233404, -32.72518063342734962, -18.71155503439485912 ) ) ;
#36047=CARTESIAN_POINT ( 'NONE',  ( 16.13393739769609780, -15.61618894467929941, 8.449999999999999289 ) ) ;
#36049=CARTESIAN_POINT ( 'NONE',  ( 56.43809645418499343, 13.88381105532070059, -15.14067943257860094 ) ) ;
#36053=( BOUNDED_CURVE ( )  B_SPLINE_CURVE ( 3, ( #50125, #26514, #18400, #42530 ),
 .UNSPECIFIED., .F., .T. ) 
 B_SPLINE_CURVE_WITH_KNOTS ( ( 4, 4 ),
 ( 0.3742143439991775233, 0.4392488787996949862 ),
 .UNSPECIFIED. ) 
 CURVE ( )  GEOMETRIC_REPRESENTATION_ITEM ( )  RATIONAL_B_SPLINE_CURVE ( ( 1.000000000000000000, 0.9996475734957616099, 0.9996475734957616099, 1.000000000000000000 ) ) 
 REPRESENTATION_ITEM ( '' )  );
#36058=CARTESIAN_POINT ( 'NONE',  ( 60.49551174326319369, -45.65747614152789424, -47.34056711453400368 ) ) ;
#36059=CARTESIAN_POINT ( 'NONE',  ( 8.133937397696209715, 28.10308010054979988, -21.14999999999999858 ) ) ;
#36064=CARTESIAN_POINT ( 'NONE',  ( 47.40322300430410252, -54.65574458090419796, -54.88279555090289819 ) ) ;
#36070=CARTESIAN_POINT ( 'NONE',  ( 1.027904703268269992, 11.45423359053189927, -20.15000000000000213 ) ) ;
#36071=CARTESIAN_POINT ( 'NONE',  ( 52.56724181638659843, -49.85961536077480361, -48.49338281493830038 ) ) ;
#36072=DIRECTION ( 'NONE',  ( 0.000000000000000000, 0.000000000000000000, 1.000000000000000000 ) ) ;
#36073=CARTESIAN_POINT ( 'NONE',  ( 76.39106947318838081, -16.04540269916347839, -12.75801850546862504 ) ) ;
#36074=CARTESIAN_POINT ( 'NONE',  ( 52.56495426071009547, -52.43765526798470233, -54.45623365677440120 ) ) ;
#36076=EDGE_LOOP ( 'NONE', ( #26763, #1193, #48543, #39621, #4959, #42853, #37299 ) ) ;
#36078=CARTESIAN_POINT ( 'NONE',  ( 48.08607070564750074, 23.01868680830909852, -54.70522948828759979 ) ) ;
#36080=CARTESIAN_POINT ( 'NONE',  ( 56.33973444090680260, -50.60696655799740284, -52.96824549530209936 ) ) ;
#36082=CARTESIAN_POINT ( 'NONE',  ( 64.07109745055549865, 0.6782384520987629895, -17.38429331904790232 ) ) ;
#36083=CARTESIAN_POINT ( 'NONE',  ( 52.26505149639999814, -49.78354415430390389, -77.19463936772501711 ) ) ;
#36084=ORIENTED_EDGE ( 'NONE', *, *, #4549, .F. ) ;
#36086=DIRECTION ( 'NONE',  ( -0.2260571801428149508, -1.665334536937734318E-16, 0.9741140340359947247 ) ) ;
#36090=CARTESIAN_POINT ( 'NONE',  ( 12.94463750493000020, -50.31721522897190368, -21.18967265423650304 ) ) ;
#36092=EDGE_CURVE ( 'NONE', #7993, #51855, #8664, .T. ) ;
#36093=CARTESIAN_POINT ( 'NONE',  ( 18.43801701820914118, -51.25800930999477600, -15.70152999933596760 ) ) ;
#36094=CARTESIAN_POINT ( 'NONE',  ( 65.43393739769578588, -48.11618894467640217, -73.25000000000000000 ) ) ;
#36095=CARTESIAN_POINT ( 'NONE',  ( 61.48324819819570308, -45.36430604964360214, -47.33702497767190209 ) ) ;
#36096=CIRCLE ( 'NONE', #16838, 48.00000000000000000 ) ;
#36097=CARTESIAN_POINT ( 'NONE',  ( 41.64265090548720138, 15.19461330351670014, -4.296538310234230273 ) ) ;
#36098=VECTOR ( 'NONE', #1087, 1000.000000000000000 ) ;
#36103=CARTESIAN_POINT ( 'NONE',  ( 14.34420985974599816, -51.11618894649849665, -74.14993593045390696 ) ) ;
#36104=CARTESIAN_POINT ( 'NONE',  ( 47.36653643891619936, -54.67788820370529379, -54.81260825270820192 ) ) ;
#36107=CARTESIAN_POINT ( 'NONE',  ( 17.80740971062453326, 20.21129459968210895, -75.25166008038893040 ) ) ;
#36108=CARTESIAN_POINT ( 'NONE',  ( 60.90761281762335244, -45.44548680042808542, -47.17297249547537774 ) ) ;
#36109=ADVANCED_FACE ( 'NONE', ( #37198 ), #2988, .T. ) ;
#36116=CARTESIAN_POINT ( 'NONE',  ( 48.54174064777019737, 22.83460439869960013, -54.75827641492099929 ) ) ;
#36118=CARTESIAN_POINT ( 'NONE',  ( 52.92824266770190178, -49.62542305747680160, -48.92669095312290040 ) ) ;
#36122=CARTESIAN_POINT ( 'NONE',  ( 84.44784216359251161, 11.88381105532070059, -47.47585302082339354 ) ) ;
#36123=CARTESIAN_POINT ( 'NONE',  ( 52.67058128702819175, 18.52949274918249856, -27.99782339546649723 ) ) ;
#36125=CARTESIAN_POINT ( 'NONE',  ( 52.58363278054860501, 18.61045885154019786, -48.51250198868969932 ) ) ;
#36126=CARTESIAN_POINT ( 'NONE',  ( 55.85583526904490270, -45.19818891271899730, -15.37717892060849856 ) ) ;
#36127=CARTESIAN_POINT ( 'NONE',  ( 16.65420337941066720, -51.11618894467930119, -21.07727733026462857 ) ) ;
#36131=CARTESIAN_POINT ( 'NONE',  ( 11.74133921615520038, -65.36765915750379463, -17.40968291634680298 ) ) ;
#36132=CARTESIAN_POINT ( 'NONE',  ( 10.22956136350960143, 32.89403351977829715, -46.33680948560530055 ) ) ;
#36135=AXIS2_PLACEMENT_3D ( 'NONE', #36811, #36037, #15623 ) ;
#36136=CARTESIAN_POINT ( 'NONE',  ( 48.34931318170839631, -53.91658640633450261, -54.01551401094359761 ) ) ;
#36137=CARTESIAN_POINT ( 'NONE',  ( 10.65676624057133637, -63.90657753633119142, -23.61757751456070764 ) ) ;
#36141=EDGE_CURVE ( 'NONE', #27219, #47951, #3771, .T. ) ;
#36143=CARTESIAN_POINT ( 'NONE',  ( 11.13393739769619906, -63.27446496484219551, -43.91455789178539248 ) ) ;
#36147=CARTESIAN_POINT ( 'NONE',  ( 50.12211818213420145, -48.61618485716249438, -76.14999999999999147 ) ) ;
#36153=CARTESIAN_POINT ( 'NONE',  ( 55.40055888017540298, 20.31707842463499958, -53.98551680322430713 ) ) ;
#36157=EDGE_LOOP ( 'NONE', ( #46492, #12293, #35081 ) ) ;
#36161=CARTESIAN_POINT ( 'NONE',  ( 46.84179439965980407, 22.69619787130520194, -75.82399969562499109 ) ) ;
#36163=CARTESIAN_POINT ( 'NONE',  ( 53.41693480164780539, 18.12090330447910347, -48.75416851879779756 ) ) ;
#36167=EDGE_CURVE ( 'NONE', #10465, #29313, #18825, .T. ) ;
#36168=CARTESIAN_POINT ( 'NONE',  ( 56.69209721199219842, -50.61618744975589834, -75.40240639624190067 ) ) ;
#36172=CARTESIAN_POINT ( 'NONE',  ( 61.11825904928579689, 14.08859410275880109, -46.89980876084979400 ) ) ;
#36177=CARTESIAN_POINT ( 'NONE',  ( 52.94585587482559674, -49.60009264233129755, -48.75076953771959865 ) ) ;
#36178=CARTESIAN_POINT ( 'NONE',  ( 59.00011887688039991, -45.52336115602069810, -26.53752582118919889 ) ) ;
#36180=CARTESIAN_POINT ( 'NONE',  ( 57.42933415471480174, 14.50457775711600128, -26.26072587755309939 ) ) ;
#36182=CARTESIAN_POINT ( 'NONE',  ( 50.97631217574399898, 18.77236619143900143, -76.22722516077449484 ) ) ;
#36183=CARTESIAN_POINT ( 'NONE',  ( 53.21743490025700396, 18.23051946133029944, -48.89816786641330282 ) ) ;
#36185=FACE_BOUND ( 'NONE', #7862, .T. ) ;
#36186=ORIENTED_EDGE ( 'NONE', *, *, #2171, .F. ) ;
#36188=CARTESIAN_POINT ( 'NONE',  ( 47.52380275344859939, -54.58920838926499641, -55.02111885050249640 ) ) ;
#36189=CARTESIAN_POINT ( 'NONE',  ( 11.90611060579353087, -65.43712337795734868, -18.00436963408782987 ) ) ;
#36191=CARTESIAN_POINT ( 'NONE',  ( 59.48605679216419873, -29.56288290624030068, -15.85191620889269970 ) ) ;
#36193=DIRECTION ( 'NONE',  ( 0.000000000000000000, 0.000000000000000000, 1.000000000000000000 ) ) ;
#36195=CARTESIAN_POINT ( 'NONE',  ( 51.63119803174421918, -34.05402968804899189, -76.94892812354784439 ) ) ;
#36199=ORIENTED_EDGE ( 'NONE', *, *, #32788, .T. ) ;
#36201=CARTESIAN_POINT ( 'NONE',  ( 50.18734600372286536, -30.13642185530741457, -16.07512387930005815 ) ) ;
#36205=AXIS2_PLACEMENT_3D ( 'NONE', #17212, #20858, #45251 ) ;
#36208=CARTESIAN_POINT ( 'NONE',  ( 16.13393739769620083, -15.61618894467929941, -14.65000000000000036 ) ) ;
#36215=ORIENTED_EDGE ( 'NONE', *, *, #48033, .T. ) ;
#36216=CARTESIAN_POINT ( 'NONE',  ( 11.31451853429699916, -65.21686366208800223, -22.84783898345410336 ) ) ;
#36218=CARTESIAN_POINT ( 'NONE',  ( 45.18452561082949615, 14.58898524498980009, -8.866308698657380916 ) ) ;
#36219=CARTESIAN_POINT ( 'NONE',  ( 14.03951828119850020, 20.70615929725470039, -75.58342519351550948 ) ) ;
#36221=CARTESIAN_POINT ( 'NONE',  ( 82.72635976414500192, -45.16472152492289638, -46.96146434100139544 ) ) ;
#36223=B_SPLINE_CURVE_WITH_KNOTS ( 'NONE', 3,
 ( #38906, #26044, #2996, #10609, #34429, #50438, #7187, #14527, #46777, #2219, #29974, #18198, #18966, #30240 ),
 .UNSPECIFIED., .F., .F.,
 ( 4, 2, 2, 2, 1, 1, 2, 4 ),
 ( 0.000000000000000000, 0.2471173528950156018, 0.3706760293425299113, 0.4324553675662862195, 0.4633450366781692309, 0.4787898712341108753, 0.4865122885120863327, 0.4942347057900616236 ),
 .UNSPECIFIED. ) ;
#36226=CARTESIAN_POINT ( 'NONE',  ( 54.16580280984440776, -48.35420548540910346, -26.76702793006570147 ) ) ;
#36228=CARTESIAN_POINT ( 'NONE',  ( 15.53208191793540038, -50.86428735276679447, -20.56249370038110058 ) ) ;
#36231=CARTESIAN_POINT ( 'NONE',  ( 61.68773928233808590, -45.18163828788996739, -46.89102616239745913 ) ) ;
#36232=CARTESIAN_POINT ( 'NONE',  ( 12.76120697008239802, -49.98606222100620045, -21.08963178055790166 ) ) ;
#36234=CARTESIAN_POINT ( 'NONE',  ( -9.500613363851449833, -43.72129052405930594, -5.962761149281509354 ) ) ;
#36235=AXIS2_PLACEMENT_3D ( 'NONE', #47526, #43083, #11623 ) ;
#36236=AXIS2_PLACEMENT_3D ( 'NONE', #32523, #8203, #40169 ) ;
#36237=CARTESIAN_POINT ( 'NONE',  ( 47.31587322217479397, 23.47801198921460397, -54.77833839503799851 ) ) ;
#36238=CYLINDRICAL_SURFACE ( 'NONE', #31216, 1.999999999999997113 ) ;
#36241=CARTESIAN_POINT ( 'NONE',  ( 41.82061708364619790, 12.78867990672720012, -4.552229662895129536 ) ) ;
#36242=DIRECTION ( 'NONE',  ( 0.000000000000000000, 0.000000000000000000, -1.000000000000000000 ) ) ;
#36243=DIRECTION ( 'NONE',  ( 0.000000000000000000, 0.000000000000000000, 1.000000000000000000 ) ) ;
#36244=DIRECTION ( 'NONE',  ( 0.000000000000000000, 0.000000000000000000, 1.000000000000000000 ) ) ;
#36245=CARTESIAN_POINT ( 'NONE',  ( 57.13638867421310152, -47.42892726663239955, -48.04708942102450209 ) ) ;
#36253=CARTESIAN_POINT ( 'NONE',  ( 8.813920544456330219, 32.04044820803110127, -46.67144773886860065 ) ) ;
#36258=CARTESIAN_POINT ( 'NONE',  ( 18.08040100137599993, 20.38364582413090176, -75.40982873507010709 ) ) ;
#36267=CARTESIAN_POINT ( 'NONE',  ( 75.43171768290677903, 10.53008244115809866, -13.17417775896968735 ) ) ;
#36268=CARTESIAN_POINT ( 'NONE',  ( 12.12757535754312421, 33.95539782499548664, -16.69244757705873283 ) ) ;
#36270=CARTESIAN_POINT ( 'NONE',  ( 11.65410534970359713, -64.86784288575155699, -23.89686975621782139 ) ) ;
#36271=CARTESIAN_POINT ( 'NONE',  ( 57.34776334542480214, -45.81180625069929846, -26.27178910182970029 ) ) ;
#36272=EDGE_LOOP ( 'NONE', ( #51030, #48807, #16815, #38496 ) ) ;
#36273=VECTOR ( 'NONE', #32102, 1000.000000000000000 ) ;
#36278=CARTESIAN_POINT ( 'NONE',  ( 61.11504165468770111, 14.39036167884340145, -47.68917451007700237 ) ) ;
#36279=CARTESIAN_POINT ( 'NONE',  ( 48.24989815756970302, 14.34044383502719988, -10.69710604161790002 ) ) ;
#36280=CARTESIAN_POINT ( 'NONE',  ( -3.202629701451740196, 17.10292418714999840, -4.381046808933160008 ) ) ;
#36281=DIRECTION ( 'NONE',  ( 0.000000000000000000, 0.000000000000000000, -1.000000000000000000 ) ) ;
#36282=CARTESIAN_POINT ( 'NONE',  ( 61.24683137928700205, 13.99389904076519997, -27.77110181634639829 ) ) ;
#36285=CARTESIAN_POINT ( 'NONE',  ( 59.00597303369990243, 15.28899821959569927, -47.85315989107520807 ) ) ;
#36289=CARTESIAN_POINT ( 'NONE',  ( 11.53659969949129938, 33.50198822980290458, -44.98688683885700357 ) ) ;
#36293=CARTESIAN_POINT ( 'NONE',  ( 47.14848365886989967, 23.49639526634990006, -74.72737464375309457 ) ) ;
#36294=CARTESIAN_POINT ( 'NONE',  ( 48.71774127335779525, -54.07467890585870407, -55.20634912303470543 ) ) ;
#36295=CARTESIAN_POINT ( 'NONE',  ( -6.923935172077830380, 14.83398127567929947, -5.625849176739690094 ) ) ;
#36296=CARTESIAN_POINT ( 'NONE',  ( 50.03007040746459921, -48.61618894467930119, -76.14999999999999147 ) ) ;
#36297=CARTESIAN_POINT ( 'NONE',  ( 66.50379331185658316, -33.11590393224402362, -20.28030461099050896 ) ) ;
#36299=VERTEX_POINT ( 'NONE', #29514 ) ;
#36303=ORIENTED_EDGE ( 'NONE', *, *, #8710, .T. ) ;
#36304=DIRECTION ( 'NONE',  ( -0.1999849291395982553, -0.9797989733190325401, 0.000000000000000000 ) ) ;
#36305=CARTESIAN_POINT ( 'NONE',  ( 60.57316152011729571, -45.60666961708100331, -47.23474488792719939 ) ) ;
#36306=CARTESIAN_POINT ( 'NONE',  ( 16.13393739769620083, -15.61618894467929941, -74.14999999999999147 ) ) ;
#36307=CARTESIAN_POINT ( 'NONE',  ( 13.29299421628470057, 18.84434172282420050, -21.00266242605139766 ) ) ;
#36312=ORIENTED_EDGE ( 'NONE', *, *, #51637, .F. ) ;
#36313=CARTESIAN_POINT ( 'NONE',  ( 84.41763914545359171, -43.52694424673759954, -47.43918784650069398 ) ) ;
#36316=ADVANCED_FACE ( 'NONE', ( #446 ), #9098, .F. ) ;
#36317=VERTEX_POINT ( 'NONE', #32390 ) ;
#36320=CARTESIAN_POINT ( 'NONE',  ( 76.40205803391916106, -11.62003586772016739, -12.80537183077186114 ) ) ;
#36321=CARTESIAN_POINT ( 'NONE',  ( 53.77933314157539968, -51.92037616820480395, -54.11586239492699235 ) ) ;
#36327=AXIS2_PLACEMENT_3D ( 'NONE', #21576, #50671, #14768 ) ;
#36328=CARTESIAN_POINT ( 'NONE',  ( -9.882013117715120032, 9.266944274022621997, -19.14999999999999858 ) ) ;
#36331=CARTESIAN_POINT ( 'NONE',  ( 57.42459889539989604, -50.12148349570598782, -52.60814563364522911 ) ) ;
#36332=CARTESIAN_POINT ( 'NONE',  ( 53.10748497486810038, -50.46803858881009575, -76.94545506623299502 ) ) ;
#36336=CARTESIAN_POINT ( 'NONE',  ( 13.63995620566349842, -50.25144441423690012, -20.99590322994719926 ) ) ;
#36338=AXIS2_PLACEMENT_3D ( 'NONE', #8991, #29407, #33846 ) ;
#36339=DIRECTION ( 'NONE',  ( 0.2771081164311157696, -0.6505467637364703570, -0.7071067811865504593 ) ) ;
#36341=CARTESIAN_POINT ( 'NONE',  ( 68.13393739769649926, -48.11618894467230234, -75.95000000000109708 ) ) ;
#36342=CARTESIAN_POINT ( 'NONE',  ( 53.41693480164780539, 18.12090330447910347, -48.75416851879779756 ) ) ;
#36343=AXIS2_PLACEMENT_3D ( 'NONE', #3979, #24372, #44061 ) ;
#36347=ORIENTED_EDGE ( 'NONE', *, *, #23030, .T. ) ;
#36348=CARTESIAN_POINT ( 'NONE',  ( 14.56865064373200092, -51.74824662968959643, -75.61048537065330777 ) ) ;
#36350=CARTESIAN_POINT ( 'NONE',  ( 47.30244424245569945, -54.71834446448549727, -54.68559897975160311 ) ) ;
#36351=SURFACE_STYLE_FILL_AREA ( #32148 ) ;
#36352=CARTESIAN_POINT ( 'NONE',  ( 1.633937397696199056, -15.61618894467930119, -7.139181489322110608 ) ) ;
#36353=CARTESIAN_POINT ( 'NONE',  ( 65.03603135424580728, -29.76883965895079953, -19.52361391316370032 ) ) ;
#36356=CARTESIAN_POINT ( 'NONE',  ( 55.36020812945222502, -46.03748402870435541, -16.50346261846816631 ) ) ;
#36358=CARTESIAN_POINT ( 'NONE',  ( 11.73919149118469996, 34.19054207972979498, -18.11861173564810201 ) ) ;
#36362=CARTESIAN_POINT ( 'NONE',  ( 17.21347160910390173, -53.11618894467930119, -76.14999999999999147 ) ) ;
#36363=CARTESIAN_POINT ( 'NONE',  ( 48.42745381579229758, 22.84070070992420298, -54.64141748400979992 ) ) ;
#36365=CARTESIAN_POINT ( 'NONE',  ( 53.51329535007300109, -49.35893701318239835, -49.05665458397329814 ) ) ;
#36366=ORIENTED_EDGE ( 'NONE', *, *, #40536, .F. ) ;
#36368=LINE ( 'NONE', #27221, #44439 ) ;
#36369=CARTESIAN_POINT ( 'NONE',  ( 56.91872543024629749, -50.64361015893049967, -53.86107397448480327 ) ) ;
#36370=CARTESIAN_POINT ( 'NONE',  ( 82.53147610877040563, 13.90223449766140007, -46.79182873648620244 ) ) ;
#36371=CARTESIAN_POINT ( 'NONE',  ( 54.07036167138819849, 17.11098462788829977, -26.64338358489850123 ) ) ;
#36373=CARTESIAN_POINT ( 'NONE',  ( 53.02879948416539690, 18.37809327181799901, -49.09530617495999394 ) ) ;
#36374=CARTESIAN_POINT ( 'NONE',  ( 57.22186383486660333, -45.12778674492059849, -17.46691603967050099 ) ) ;
#36376=ORIENTED_EDGE ( 'NONE', *, *, #45568, .F. ) ;
#36378=EDGE_CURVE ( 'NONE', #11300, #16107, #28735, .T. ) ;
#36380=CARTESIAN_POINT ( 'NONE',  ( 11.10018451884070068, -65.04197989738689500, -17.19464565520879873 ) ) ;
#36381=CARTESIAN_POINT ( 'NONE',  ( 12.86387693150249945, 34.27459056366519974, -47.65248693957870074 ) ) ;
#36383=DIRECTION ( 'NONE',  ( -0.7089970498513425978, -0.7052114458104695727, -4.077736999999996963E-16 ) ) ;
#36384=CARTESIAN_POINT ( 'NONE',  ( 10.73247463706263893, -64.25243278916070722, -23.51162531654635046 ) ) ;
#36386=ORIENTED_EDGE ( 'NONE', *, *, #24263, .T. ) ;
#36387=CARTESIAN_POINT ( 'NONE',  ( 10.90462426371155757, 24.04048178864984209, -44.90618065568715167 ) ) ;
#36388=CARTESIAN_POINT ( 'NONE',  ( 11.13393739769619906, -63.20626152654000407, -43.91299082816230026 ) ) ;
#36397=CARTESIAN_POINT ( 'NONE',  ( 56.83258908092710016, -50.30522036972260480, -52.72698303625519856 ) ) ;
#36403=CARTESIAN_POINT ( 'NONE',  ( 55.93861191783509668, 19.62789642752380104, -74.87542895885140126 ) ) ;
#36405=CARTESIAN_POINT ( 'NONE',  ( 47.43575969855930197, -54.63575133606219936, -74.19794602913619030 ) ) ;
#36407=AXIS2_PLACEMENT_3D ( 'NONE', #27325, #23126, #31498 ) ;
#36410=CARTESIAN_POINT ( 'NONE',  ( 11.67619456822290047, 33.65927054772580362, -23.88710972541020183 ) ) ;
#36411=CARTESIAN_POINT ( 'NONE',  ( 46.88047926045639713, 22.77644039600379600, -75.76367657470891004 ) ) ;
#36414=EDGE_CURVE ( 'NONE', #32635, #12694, #32916, .T. ) ;
#36415=CARTESIAN_POINT ( 'NONE',  ( 41.54743507844230521, -44.83695157103969819, -5.527281617101080791 ) ) ;
#36416=CARTESIAN_POINT ( 'NONE',  ( 12.31509292275960021, 33.40570322225389788, -15.85496248756799709 ) ) ;
#36418=EDGE_CURVE ( 'NONE', #41267, #5478, #42621, .T. ) ;
#36419=CARTESIAN_POINT ( 'NONE',  ( 56.87436366836959678, -50.61618764704540041, -75.17316017584860788 ) ) ;
#36423=CARTESIAN_POINT ( 'NONE',  ( 61.49092242389700402, 13.92534852783209942, -46.59258487662240356 ) ) ;
#36424=CARTESIAN_POINT ( 'NONE',  ( -0.08095109960796090243, -61.40204063968959503, -48.64221216126409786 ) ) ;
#36425=ORIENTED_EDGE ( 'NONE', *, *, #20197, .T. ) ;
#36426=CARTESIAN_POINT ( 'NONE',  ( 52.90855289046140086, -49.61963672099809486, -48.71990427169439641 ) ) ;
#36427=CARTESIAN_POINT ( 'NONE',  ( 60.64762851420100276, -45.11618901004540305, -26.44263184015450108 ) ) ;
#36430=CARTESIAN_POINT ( 'NONE',  ( 56.87603334809730171, 14.74005630904309960, -26.24549249933449957 ) ) ;
#36432=CARTESIAN_POINT ( 'NONE',  ( 50.45186278194579899, 18.80186278247199994, -76.14999999999999147 ) ) ;
#36433=CARTESIAN_POINT ( 'NONE',  ( 53.10876373110949800, 18.29129782088910261, -48.93018544281289905 ) ) ;
#36436=CARTESIAN_POINT ( 'NONE',  ( 68.83419609097690284, -44.96193019449670203, -12.58053924570920046 ) ) ;
#36441=CARTESIAN_POINT ( 'NONE',  ( 47.68328361370659962, -54.50666145107209815, -54.95376626878769599 ) ) ;
#36442=CARTESIAN_POINT ( 'NONE',  ( -6.441449436378089644, 14.95323763072200052, -4.672284527633559392 ) ) ;
#36444=CARTESIAN_POINT ( 'NONE',  ( 57.72747068869959719, 18.67975836146520052, -52.38194251579410121 ) ) ;
#36446=CARTESIAN_POINT ( 'NONE',  ( 68.13393739769620083, 16.88381105532069881, -75.00000000000000000 ) ) ;
#36451=EDGE_LOOP ( 'NONE', ( #21119, #51757, #45285, #47822, #47735 ) ) ;
#36452=CARTESIAN_POINT ( 'NONE',  ( -6.866062602303800055, -15.61618894467929586, -14.65000000000000036 ) ) ;
#36454=ORIENTED_EDGE ( 'NONE', *, *, #5133, .F. ) ;
#36456=CARTESIAN_POINT ( 'NONE',  ( 22.41796512503769989, 0.7774003680457489684, -74.14999999999999147 ) ) ;
#36459=CARTESIAN_POINT ( 'NONE',  ( 55.80143501159700747, -48.88742250280260038, -53.84278118897339738 ) ) ;
#36472=CIRCLE ( 'NONE', #45704, 21.19999999999999929 ) ;
#36473=CARTESIAN_POINT ( 'NONE',  ( 43.05627104033619901, 14.74862409592560120, -7.622843372308340193 ) ) ;
#36474=VECTOR ( 'NONE', #44143, 1000.000000000000114 ) ;
#36475=CARTESIAN_POINT ( 'NONE',  ( 14.38413149323399942, 20.42705216602020357, -75.51240970683940645 ) ) ;
#36480=ADVANCED_FACE ( 'NONE', ( #2002 ), #37909, .F. ) ;
#36482=CARTESIAN_POINT ( 'NONE',  ( 53.04388686265919972, -49.43765248974969495, -27.51561755457979785 ) ) ;
#36483=CARTESIAN_POINT ( 'NONE',  ( 14.79307399752550012, -50.68537516129959641, -20.88395191203650114 ) ) ;
#36484=CARTESIAN_POINT ( 'NONE',  ( 50.03007040746459921, -36.85417771443089663, -76.14999999999999147 ) ) ;
#36486=CARTESIAN_POINT ( 'NONE',  ( 75.45209363691283500, 12.55602155768010952, -13.50097026880459339 ) ) ;
#36489=CARTESIAN_POINT ( 'NONE',  ( -7.450541063502280181, -45.60837410880110099, -5.667773980459688943 ) ) ;
#36490=CARTESIAN_POINT ( 'NONE',  ( 47.41680556257099965, 23.40808140825799910, -54.70932877154390184 ) ) ;
#36492=FACE_OUTER_BOUND ( 'NONE', #41705, .T. ) ;
#36494=CARTESIAN_POINT ( 'NONE',  ( 13.58674547247159836, 19.15744735761279927, -21.11651667334109916 ) ) ;
#36495=CARTESIAN_POINT ( 'NONE',  ( 54.99093226003984114, 16.49184862051891898, -26.61807943321322156 ) ) ;
#36496=CARTESIAN_POINT ( 'NONE',  ( 11.78395113718259957, 34.19034018254340168, -17.88069380536899899 ) ) ;
#36500=CARTESIAN_POINT ( 'NONE',  ( 53.59080506099410002, -49.40678926384370584, -49.22648751777380483 ) ) ;
#36501=CIRCLE ( 'NONE', #49107, 50.00000000000000000 ) ;
#36504=CARTESIAN_POINT ( 'NONE',  ( 17.90951780689729844, -52.52234239888379363, -75.96669286083250938 ) ) ;
#36505=CARTESIAN_POINT ( 'NONE',  ( 50.03007040746459921, 5.621799825072190337, -76.14999999999999147 ) ) ;
#36508=FACE_OUTER_BOUND ( 'NONE', #38612, .T. ) ;
#36509=ORIENTED_EDGE ( 'NONE', *, *, #26068, .T. ) ;
#36511=CARTESIAN_POINT ( 'NONE',  ( 9.280056505173840620, 31.92632265388400370, -46.53174294612239947 ) ) ;
#36513=VECTOR ( 'NONE', #14791, 1000.000000000000000 ) ;
#36514=CARTESIAN_POINT ( 'NONE',  ( 66.98667323035849108, -30.07752074129929909, -17.21848267116260089 ) ) ;
#36516=CARTESIAN_POINT ( 'NONE',  ( 18.50593879142590126, 20.63771170940629673, -75.29799846200430125 ) ) ;
#36517=VERTEX_POINT ( 'NONE', #9867 ) ;
#36520=CARTESIAN_POINT ( 'NONE',  ( 11.80925469686000007, -65.15757697063340004, -46.63650775655830216 ) ) ;
#36525=ORIENTED_EDGE ( 'NONE', *, *, #19264, .F. ) ;
#36526=CARTESIAN_POINT ( 'NONE',  ( 12.21895745972638814, 33.73857834413064438, -16.28177270833691992 ) ) ;
#36527=ORIENTED_EDGE ( 'NONE', *, *, #13276, .F. ) ;
#36528=CARTESIAN_POINT ( 'NONE',  ( 11.32194239187774443, -64.37711270544450315, -24.04756285534320526 ) ) ;
#36530=CARTESIAN_POINT ( 'NONE',  ( 14.74689884928131356, -52.86909450409968514, -76.12392058103056058 ) ) ;
#36531=DIRECTION ( 'NONE',  ( -1.000000000000000000, 0.000000000000000000, 0.000000000000000000 ) ) ;
#36533=ORIENTED_EDGE ( 'NONE', *, *, #35887, .T. ) ;
#36534=VERTEX_POINT ( 'NONE', #30795 ) ;
#36535=FACE_OUTER_BOUND ( 'NONE', #35175, .T. ) ;
#36537=CARTESIAN_POINT ( 'NONE',  ( 70.56366411589620213, 13.88381105527240145, -14.05866322138230018 ) ) ;
#36538=VECTOR ( 'NONE', #34556, 1000.000000000000000 ) ;
#36539=CARTESIAN_POINT ( 'NONE',  ( 48.07720450831519798, 14.71742899414569905, -10.94662572293029967 ) ) ;
#36541=CARTESIAN_POINT ( 'NONE',  ( -9.444509380504280571, 12.50088983498840101, -5.686455919239249646 ) ) ;
#36542=CARTESIAN_POINT ( 'NONE',  ( -2.328172376426727475, -49.80836506692148191, -5.964500925750916061 ) ) ;
#36544=CARTESIAN_POINT ( 'NONE',  ( 57.59507381935979708, 14.35784622530070109, -26.21889295923039853 ) ) ;
#36547=ORIENTED_EDGE ( 'NONE', *, *, #44547, .T. ) ;
#36548=CARTESIAN_POINT ( 'NONE',  ( 53.59007319642030609, 18.17385789206429791, -49.22505640095140222 ) ) ;
#36550=CARTESIAN_POINT ( 'NONE',  ( 52.10267382254159685, -33.11618894467940066, -20.65000000000000213 ) ) ;
#36551=EDGE_CURVE ( 'NONE', #29481, #13261, #46302, .T. ) ;
#36555=CARTESIAN_POINT ( 'NONE',  ( 13.32695066795020011, 18.94061603315460118, -21.04411651763339819 ) ) ;
#36557=CARTESIAN_POINT ( 'NONE',  ( 49.20993668789899544, -53.61219117315689431, -54.26298610208100115 ) ) ;
#36558=LINE ( 'NONE', #39992, #50739 ) ;
#36559=AXIS2_PLACEMENT_3D ( 'NONE', #41322, #24275, #1237 ) ;
#36566=CARTESIAN_POINT ( 'NONE',  ( 55.40393386216474170, -45.11618894460369944, -14.52023105806692449 ) ) ;
#36567=CARTESIAN_POINT ( 'NONE',  ( 60.90533690232570763, -45.43405919436199980, -47.09747221447039323 ) ) ;
#36568=CARTESIAN_POINT ( 'NONE',  ( 57.18371624257370200, 19.38400875315740279, -53.90359198932329576 ) ) ;
#36569=CARTESIAN_POINT ( 'NONE',  ( 43.91475033527959937, -43.54611815821230891, -5.093413304872340674 ) ) ;
#36573=DIRECTION ( 'NONE',  ( 0.000000000000000000, 1.000000000000000000, 0.000000000000000000 ) ) ;
#36575=CARTESIAN_POINT ( 'NONE',  ( 84.02215818083939780, -44.41825355194460201, -47.25304732090640414 ) ) ;
#36577=ORIENTED_EDGE ( 'NONE', *, *, #33749, .T. ) ;
#36579=CARTESIAN_POINT ( 'NONE',  ( 61.37876400707010305, -45.32826204942830373, -47.24547059479539968 ) ) ;
#36580=CARTESIAN_POINT ( 'NONE',  ( 53.02878878271380358, -49.61118882884069592, -49.09724721214779919 ) ) ;
#36581=DIRECTION ( 'NONE',  ( 0.000000000000000000, 1.000000000000000000, 0.000000000000000000 ) ) ;
#36582=CARTESIAN_POINT ( 'NONE',  ( 76.40558626391258201, -11.02804892670111059, -12.82057542108343640 ) ) ;
#36583=CARTESIAN_POINT ( 'NONE',  ( 54.00935231632030309, -51.82239677024340097, -54.07713036160949827 ) ) ;
#36584=TOROIDAL_SURFACE ( 'NONE', #31565, 36.00000000000000000, 2.000000000000000000 ) ;
#36585=ORIENTED_EDGE ( 'NONE', *, *, #1007, .T. ) ;
#36587=CARTESIAN_POINT ( 'NONE',  ( 49.30929069640199458, 22.32182524534569978, -54.21028152426279689 ) ) ;
#36590=EDGE_CURVE ( 'NONE', #3072, #28015, #42882, .T. ) ;
#36591=CARTESIAN_POINT ( 'NONE',  ( 8.802047646820330584, -63.20618355599279425, -46.67014429624759941 ) ) ;
#36593=CARTESIAN_POINT ( 'NONE',  ( 11.13393739769619906, -63.11543068638779630, -43.74348518090240390 ) ) ;
#36594=EDGE_LOOP ( 'NONE', ( #7438, #39193, #30066, #10315 ) ) ;
#36595=CARTESIAN_POINT ( 'NONE',  ( 14.34417030258640047, -52.11618895234509807, -23.15000000571859928 ) ) ;
#36596=CARTESIAN_POINT ( 'NONE',  ( 53.44459314798190519, -50.52658309343919996, -77.05819699307679116 ) ) ;
#36601=CARTESIAN_POINT ( 'NONE',  ( 41.34908647067909726, -44.75253358332089704, -5.352709625395250193 ) ) ;
#36603=CARTESIAN_POINT ( 'NONE',  ( 61.28189544230230013, -45.60274550571363505, -47.67949669012001834 ) ) ;
#36606=FACE_OUTER_BOUND ( 'NONE', #48984, .T. ) ;
#36608=CARTESIAN_POINT ( 'NONE',  ( 14.66320343668420101, -52.01451994755070274, -75.82251062550810161 ) ) ;
#36609=CARTESIAN_POINT ( 'NONE',  ( 47.31046770529280110, -54.71181978270450230, -54.66537007426079953 ) ) ;
#36611=CARTESIAN_POINT ( 'NONE',  ( 55.52753008314243033, -15.61618894467857110, -5.093415854460129566 ) ) ;
#36613=AXIS2_PLACEMENT_3D ( 'NONE', #27636, #44926, #40990 ) ;
#36616=CARTESIAN_POINT ( 'NONE',  ( 47.66469316585200033, -54.52497965065870034, -55.13865833718669762 ) ) ;
#36617=FACE_OUTER_BOUND ( 'NONE', #41103, .T. ) ;
#36618=CARTESIAN_POINT ( 'NONE',  ( 11.28396737011271433, 33.05014951446679561, -24.06589613998641042 ) ) ;
#36620=CARTESIAN_POINT ( 'NONE',  ( 56.45386930879750054, 19.54637801841160183, -53.73844136669490013 ) ) ;
#36621=CARTESIAN_POINT ( 'NONE',  ( 42.53968774895909633, 12.99877935903693604, -5.088323967986317697 ) ) ;
#36622=CARTESIAN_POINT ( 'NONE',  ( 48.58882027194280084, 22.89737091365429933, -55.21892047541300741 ) ) ;
#36623=ORIENTED_EDGE ( 'NONE', *, *, #43459, .F. ) ;
#36625=ORIENTED_EDGE ( 'NONE', *, *, #19210, .F. ) ;
#36629=CARTESIAN_POINT ( 'NONE',  ( 83.94975121583560451, 13.06368244423120117, -46.94103493214879563 ) ) ;
#36630=CARTESIAN_POINT ( 'NONE',  ( 52.61201187087419839, 18.58180915112900067, -28.06837461485350005 ) ) ;
#36633=CARTESIAN_POINT ( 'NONE',  ( 56.17636210926850282, -45.40492621701339715, -16.65164697100100000 ) ) ;
#36637=CARTESIAN_POINT ( 'NONE',  ( 12.01906023896859921, -65.22423223438029538, -16.79721265542299946 ) ) ;
#36638=CARTESIAN_POINT ( 'NONE',  ( 10.55882748421930017, 32.87867648022200484, -46.00924270197130284 ) ) ;
#36639=CARTESIAN_POINT ( 'NONE',  ( 61.19898206724911915, -45.31222199280929885, -47.06086663119204871 ) ) ;
#36640=CARTESIAN_POINT ( 'NONE',  ( 52.74267556208770458, -49.67209455079629521, -48.33969704999849881 ) ) ;
#36644=CARTESIAN_POINT ( 'NONE',  ( 57.31821422653260356, 14.58415143128349811, -26.26832944716249685 ) ) ;
#36645=EDGE_CURVE ( 'NONE', #37059, #9540, #2263, .T. ) ;
#36646=CARTESIAN_POINT ( 'NONE',  ( 53.61470614374690058, 18.14682731116949554, -49.19246808621250722 ) ) ;
#36647=CARTESIAN_POINT ( 'NONE',  ( 47.47987687170398630, 23.37779866404240536, -54.97289240249585163 ) ) ;
#36648=CARTESIAN_POINT ( 'NONE',  ( 50.48048509850679721, -50.09185786847800159, -76.14999999999999147 ) ) ;
#36649=ADVANCED_FACE ( 'NONE', ( #50482, #14058 ), #30017, .T. ) ;
#36650=CARTESIAN_POINT ( 'NONE',  ( 16.13393739769620083, -15.61618894467929941, -20.15000000000000213 ) ) ;
#36651=ORIENTED_EDGE ( 'NONE', *, *, #15208, .F. ) ;
#36653=DIRECTION ( 'NONE',  ( 0.000000000000000000, 0.000000000000000000, 1.000000000000000000 ) ) ;
#36654=ORIENTED_EDGE ( 'NONE', *, *, #10284, .T. ) ;
#36655=CARTESIAN_POINT ( 'NONE',  ( 56.87160283908409752, -50.28903218254829710, -52.71743054463500044 ) ) ;
#36656=AXIS2_PLACEMENT_3D ( 'NONE', #757, #13606, #49514 ) ;
#36658=EDGE_CURVE ( 'NONE', #28507, #47320, #43133, .T. ) ;
#36660=CARTESIAN_POINT ( 'NONE',  ( 13.89744741416839879, -51.22086835498220125, -22.99801680307020035 ) ) ;
#36661=CARTESIAN_POINT ( 'NONE',  ( 56.23294450515269460, 19.54859116196450231, -74.77228800217299920 ) ) ;
#36663=CARTESIAN_POINT ( 'NONE',  ( 46.87509678320709838, -53.74177327554130557, -75.90467361879859709 ) ) ;
#36667=CARTESIAN_POINT ( 'NONE',  ( 52.88366625939990229, -49.67299857165690469, -49.00384039304309880 ) ) ;
#36668=CARTESIAN_POINT ( 'NONE',  ( 15.67962062511290000, 19.63028992866140143, -15.65622423491010196 ) ) ;
#36669=CARTESIAN_POINT ( 'NONE',  ( 11.83166319397156308, 33.82478071477750348, -23.81848075244050378 ) ) ;
#36670=CARTESIAN_POINT ( 'NONE',  ( 46.48959969234209666, 21.91510670762199808, -76.13710305591399674 ) ) ;
#36673=CARTESIAN_POINT ( 'NONE',  ( 59.94414702407019746, 14.70111394113749981, -47.28272102067069937 ) ) ;
#36674=CARTESIAN_POINT ( 'NONE',  ( 12.36320305067610015, 33.31445045643330616, -15.76422791930239953 ) ) ;
#36681=CARTESIAN_POINT ( 'NONE',  ( 61.42395427194719559, 13.96908307647129988, -46.82082490102270356 ) ) ;
#36683=CARTESIAN_POINT ( 'NONE',  ( -0.4230338164578509863, -63.17480145319609619, -49.86202923830769862 ) ) ;
#36685=CARTESIAN_POINT ( 'NONE',  ( 52.75740204447090065, -49.70242901905119481, -48.47378032971909789 ) ) ;
#36688=CARTESIAN_POINT ( 'NONE',  ( 61.70176194880070142, -45.11618250747869752, -27.87045028019250026 ) ) ;
#36689=CARTESIAN_POINT ( 'NONE',  ( 48.20452265730930463, -54.29503287064159167, -55.30665343754630214 ) ) ;
#36690=CARTESIAN_POINT ( 'NONE',  ( 56.37055690849290102, 14.89250931428609803, -26.19214289511259608 ) ) ;
#36692=CIRCLE ( 'NONE', #23407, 2.000000000000000000 ) ;
#36693=CARTESIAN_POINT ( 'NONE',  ( 51.58108482517790350, 19.09072979187009977, -76.34882618429139711 ) ) ;
#36694=CARTESIAN_POINT ( 'NONE',  ( 53.06129597024689559, 18.31052047746409883, -48.87622692185889406 ) ) ;
#36696=DIRECTION ( 'NONE',  ( 0.6888026391158391659, 0.7071067811865435759, 0.1598465650148942763 ) ) ;
#36697=CARTESIAN_POINT ( 'NONE',  ( 69.03514090041920781, -44.31906284533980767, -11.86759013202009960 ) ) ;
#36702=CARTESIAN_POINT ( 'NONE',  ( 47.54355032392420100, -54.57327899847110331, -54.86427360055650126 ) ) ;
#36703=DIRECTION ( 'NONE',  ( -0.1686178020941830058, -0.6660492713794510244, 0.7265992051412039077 ) ) ;
#36705=CARTESIAN_POINT ( 'NONE',  ( 59.12201268170110069, 16.79103452985640033, -50.30506373816950116 ) ) ;
#36711=ORIENTED_EDGE ( 'NONE', *, *, #554, .T. ) ;
#36714=CARTESIAN_POINT ( 'NONE',  ( 59.34499803081109803, -3.116188944679349593, -15.68015151901639825 ) ) ;
#36718=CARTESIAN_POINT ( 'NONE',  ( 84.32823744777105901, 12.72937168411247555, -47.43651528304791043 ) ) ;
#36720=CARTESIAN_POINT ( 'NONE',  ( 52.02214979817979668, 19.08406620782900021, -76.54113483184499955 ) ) ;
#36721=EDGE_LOOP ( 'NONE', ( #312, #3176, #19871, #433, #13354 ) ) ;
#36725=EDGE_CURVE ( 'NONE', #44314, #3281, #424, .T. ) ;
#36730=CARTESIAN_POINT ( 'NONE',  ( 11.97296053931879989, -65.41364856023331242, -22.92423455041799940 ) ) ;
#36734=CARTESIAN_POINT ( 'NONE',  ( 14.49280304823600041, 21.09308431968760189, -75.96462645239850531 ) ) ;
#36738=CARTESIAN_POINT ( 'NONE',  ( 10.85466640524320070, 33.73459223951330443, -17.55961383757199812 ) ) ;
#36741=CARTESIAN_POINT ( 'NONE',  ( 53.73571933783139798, -48.69420006231280240, -26.82704014588000163 ) ) ;
#36742=CARTESIAN_POINT ( 'NONE',  ( 16.62868081655000196, -51.11618894343789776, -20.46561682067509835 ) ) ;
#36743=CARTESIAN_POINT ( 'NONE',  ( 50.80150374823916337, -35.57053178561582030, -76.30434720868854015 ) ) ;
#36744=CARTESIAN_POINT ( 'NONE',  ( 46.58046218066166233, 12.29309675584422479, -5.686836593841567478 ) ) ;
#36745=CARTESIAN_POINT ( 'NONE',  ( 75.47966807050509885, 12.14072485751589880, -13.40512917118210012 ) ) ;
#36748=CARTESIAN_POINT ( 'NONE',  ( -9.505843262714801511, -43.70152617308460208, -5.901968664759829508 ) ) ;
#36749=CARTESIAN_POINT ( 'NONE',  ( 47.24062726108790145, 23.53053415419130090, -54.65361905327920056 ) ) ;
#36750=EDGE_CURVE ( 'NONE', #46034, #12879, #42304, .T. ) ;
#36751=FACE_OUTER_BOUND ( 'NONE', #15852, .T. ) ;
#36753=CARTESIAN_POINT ( 'NONE',  ( 57.25380931998220291, -50.61618894467930119, -53.86267003311080259 ) ) ;
#36754=CARTESIAN_POINT ( 'NONE',  ( 43.75992007200080280, 12.39321587781959977, -5.076600545294299494 ) ) ;
#36758=CARTESIAN_POINT ( 'NONE',  ( 60.34379256561119576, -45.86802437250690190, -47.72732608210879590 ) ) ;
#36762=CARTESIAN_POINT ( 'NONE',  ( 17.63565729903150014, -52.02998614742870132, -75.83262351151699932 ) ) ;
#36765=CARTESIAN_POINT ( 'NONE',  ( 49.01168265654600020, 13.88381105532070059, -9.596379464580280683 ) ) ;
#36768=CARTESIAN_POINT ( 'NONE',  ( 10.14085492948789913, 31.97598296081329750, -45.99401054949460388 ) ) ;
#36769=CARTESIAN_POINT ( 'NONE',  ( 58.92073396209919878, -3.116188944679349593, -15.65000000000000036 ) ) ;
#36770=AXIS2_PLACEMENT_3D ( 'NONE', #4011, #7943, #2985 ) ;
#36773=CARTESIAN_POINT ( 'NONE',  ( 66.87128124109968041, -31.56637477442769679, -17.65462924257609956 ) ) ;
#36775=CARTESIAN_POINT ( 'NONE',  ( 17.85968403959190098, 20.22256044820920096, -75.26885115310530239 ) ) ;
#36779=ORIENTED_EDGE ( 'NONE', *, *, #3182, .T. ) ;
#36780=CARTESIAN_POINT ( 'NONE',  ( 12.62246544811769944, -65.46760815329750471, -47.29889843674509819 ) ) ;
#36785=CARTESIAN_POINT ( 'NONE',  ( 61.67706982099739577, 13.89683601203829966, -46.59487708233500314 ) ) ;
#36787=DIRECTION ( 'NONE',  ( 0.000000000000000000, 0.000000000000000000, 1.000000000000000000 ) ) ;
#36788=EDGE_CURVE ( 'NONE', #37013, #9540, #24720, .T. ) ;
#36789=CARTESIAN_POINT ( 'NONE',  ( -9.882013117715120032, 9.266944274022621997, -21.14999999999999858 ) ) ;
#36790=EDGE_LOOP ( 'NONE', ( #22406, #37829, #6839, #8799 ) ) ;
#36793=CARTESIAN_POINT ( 'NONE',  ( 10.26917183476574991, -55.18446999559061084, -45.87608767524120168 ) ) ;
#36797=CARTESIAN_POINT ( 'NONE',  ( 33.53393739662440254, -15.61618894541809688, -10.45000000053580180 ) ) ;
#36798=CARTESIAN_POINT ( 'NONE',  ( 66.45612384051480603, 13.88381326200750010, -12.57322850638879963 ) ) ;
#36799=CARTESIAN_POINT ( 'NONE',  ( 50.81599192650290320, 13.97286014258159881, -11.75472651265789992 ) ) ;
#36801=CARTESIAN_POINT ( 'NONE',  ( -3.204518368035979670, 17.10185219687699743, -4.296538305020969339 ) ) ;
#36802=VECTOR ( 'NONE', #42367, 1000.000000000000000 ) ;
#36804=AXIS2_PLACEMENT_3D ( 'NONE', #12479, #44450, #28447 ) ;
#36806=CARTESIAN_POINT ( 'NONE',  ( 55.45321058330383579, 14.78278210347054689, -16.61881412770280875 ) ) ;
#36807=CIRCLE ( 'NONE', #34290, 21.96784688337769964 ) ;
#36810=CARTESIAN_POINT ( 'NONE',  ( 58.55123287010390243, 15.52708936521539940, -47.93263078914269926 ) ) ;
#36811=CARTESIAN_POINT ( 'NONE',  ( 16.13393739769620083, -15.61618894467929941, -7.393828452885189861 ) ) ;
#36813=CARTESIAN_POINT ( 'NONE',  ( 53.62552786343490396, -51.33071804962359153, -75.58099297212140755 ) ) ;
#36819=CARTESIAN_POINT ( 'NONE',  ( 16.65420337941059969, -49.11618894467930829, -17.90311212357429937 ) ) ;
#36821=CARTESIAN_POINT ( 'NONE',  ( 47.20319461169519570, 23.55908263626179888, -74.17383159930358261 ) ) ;
#36822=CARTESIAN_POINT ( 'NONE',  ( 48.90836479786370461, -53.96901701391990258, -54.96636899373179830 ) ) ;
#36825=CARTESIAN_POINT ( 'NONE',  ( 76.70719566378195964, -43.18885252246143125, -14.39567811762877447 ) ) ;
#36829=ORIENTED_EDGE ( 'NONE', *, *, #13315, .F. ) ;
#36833=DIRECTION ( 'NONE',  ( 0.000000000000000000, 0.000000000000000000, -1.000000000000000000 ) ) ;
#36834=CARTESIAN_POINT ( 'NONE',  ( 60.85189549106659967, -45.66403237420649930, -47.67927086682649929 ) ) ;
#36838=CARTESIAN_POINT ( 'NONE',  ( 51.42797784481540191, -51.20406220416529663, -76.10787249881708760 ) ) ;
#36839=LINE ( 'NONE', #28971, #10224 ) ;
#36840=VERTEX_POINT ( 'NONE', #49144 ) ;
#36841=CARTESIAN_POINT ( 'NONE',  ( 84.01174786492798319, -44.61701663110100213, -47.41946551740999638 ) ) ;
#36843=ORIENTED_EDGE ( 'NONE', *, *, #35386, .F. ) ;
#36845=CARTESIAN_POINT ( 'NONE',  ( 61.71627407764110274, -45.13006394953620770, -46.64368077600400397 ) ) ;
#36846=AXIS2_PLACEMENT_3D ( 'NONE', #51506, #11676, #899 ) ;
#36849=CARTESIAN_POINT ( 'NONE',  ( 76.48708243442970911, -3.703201758521061482, -13.17175452297058236 ) ) ;
#36851=VECTOR ( 'NONE', #17078, 1000.000000000000000 ) ;
#36853=ORIENTED_EDGE ( 'NONE', *, *, #5964, .T. ) ;
#36856=ADVANCED_FACE ( 'NONE', ( #8776 ), #35206, .T. ) ;
#36858=CARTESIAN_POINT ( 'NONE',  ( 56.57438608727660068, 19.50039335391339890, -53.83822343184270665 ) ) ;
#36861=DIRECTION ( 'NONE',  ( -7.539420000000001133E-18, 1.452687000000000165E-17, 1.000000000000000000 ) ) ;
#36863=DIRECTION ( 'NONE',  ( -1.000000000000000000, 0.000000000000000000, 0.000000000000000000 ) ) ;
#36869=CARTESIAN_POINT ( 'NONE',  ( 83.69028012337390976, -45.07031254642157592, -47.49659995980665173 ) ) ;
#36871=CARTESIAN_POINT ( 'NONE',  ( 83.89200044194980421, -50.09049722508079583, -52.57651812407429759 ) ) ;
#36872=CARTESIAN_POINT ( 'NONE',  ( 41.75077191591359593, -44.42764855811009994, -5.046633188611889587 ) ) ;
#36873=DIRECTION ( 'NONE',  ( 0.8263629291053539161, 0.3519990991163989835, -0.4395690430656639669 ) ) ;
#36876=CARTESIAN_POINT ( 'NONE',  ( 61.34439110493909908, -45.35647919298600073, -47.30212553788380347 ) ) ;
#36879=CARTESIAN_POINT ( 'NONE',  ( 65.81145605635769869, 1.573399105534700082, -18.80820005952190144 ) ) ;
#36880=VERTEX_POINT ( 'NONE', #27265 ) ;
#36881=CARTESIAN_POINT ( 'NONE',  ( 13.99023357302460013, -52.20804236601910020, -75.66803551354809088 ) ) ;
#36882=CARTESIAN_POINT ( 'NONE',  ( 47.37397992040639849, -54.67284273012320739, -54.79488902382239957 ) ) ;
#36883=CARTESIAN_POINT ( 'NONE',  ( 11.86093866209844983, 34.13069104536225495, -47.45833196164814183 ) ) ;
#36893=EDGE_CURVE ( 'NONE', #24734, #50083, #34099, .T. ) ;
#36895=CARTESIAN_POINT ( 'NONE',  ( 48.40781919080369988, 22.97605840957759682, -55.28683361800550244 ) ) ;
#36900=CARTESIAN_POINT ( 'NONE',  ( 53.59008489733366787, -49.40624463047604564, -49.22507928152084844 ) ) ;
#36901=CARTESIAN_POINT ( 'NONE',  ( 13.73527022026379996, 18.97497658877130178, -20.93080062776429884 ) ) ;
#36902=CARTESIAN_POINT ( 'NONE',  ( 84.42050518244910506, 12.05117995606869918, -47.35805390042769858 ) ) ;
#36903=CARTESIAN_POINT ( 'NONE',  ( 54.15723598241670089, 16.86721667791090340, -26.23832647098850046 ) ) ;
#36905=FACE_OUTER_BOUND ( 'NONE', #20992, .T. ) ;
#36906=CARTESIAN_POINT ( 'NONE',  ( 57.04515152503049791, -45.11618894467940066, -16.25132461468449918 ) ) ;
#36910=CARTESIAN_POINT ( 'NONE',  ( 11.86340152621610144, -64.99742207597500965, -16.42027960340800163 ) ) ;
#36911=CARTESIAN_POINT ( 'NONE',  ( 12.53186402970929869, 34.21131896774730308, -47.19092881324929323 ) ) ;
#36912=LINE ( 'NONE', #28001, #46644 ) ;
#36913=CARTESIAN_POINT ( 'NONE',  ( 51.77723966175119585, -50.84882725107309653, -50.47693161301669562 ) ) ;
#36914=CARTESIAN_POINT ( 'NONE',  ( 19.53299984191638927, 24.23912880602019726, -75.56421462368636810 ) ) ;
#36916=EDGE_CURVE ( 'NONE', #28125, #51191, #6142, .T. ) ;
#36917=DIRECTION ( 'NONE',  ( 0.000000000000000000, 0.000000000000000000, -1.000000000000000000 ) ) ;
#36919=DIRECTION ( 'NONE',  ( -1.000000000000000000, 0.000000000000000000, 0.000000000000000000 ) ) ;
#36922=CARTESIAN_POINT ( 'NONE',  ( 50.55764114179640245, -49.80772761642590041, -76.16355215278129265 ) ) ;
#36924=CIRCLE ( 'NONE', #4301, 1.000000000000001554 ) ;
#36925=ORIENTED_EDGE ( 'NONE', *, *, #9571, .T. ) ;
#36927=AXIS2_PLACEMENT_3D ( 'NONE', #38408, #31040, #47322 ) ;
#36928=CARTESIAN_POINT ( 'NONE',  ( 65.03603135424580728, -1.463538230407920082, -19.52361391316370032 ) ) ;
#36929=ORIENTED_EDGE ( 'NONE', *, *, #37514, .F. ) ;
#36930=CARTESIAN_POINT ( 'NONE',  ( 68.13393739769620083, 4.883811055320659733, -73.60861006572370968 ) ) ;
#36931=CARTESIAN_POINT ( 'NONE',  ( 49.42578290888749848, -46.18034399694119685, -12.04424791257699923 ) ) ;
#36934=CARTESIAN_POINT ( 'NONE',  ( 52.90670265584750354, -49.65877502917909680, -49.00842844558349753 ) ) ;
#36935=CARTESIAN_POINT ( 'NONE',  ( 68.13393739769819035, 19.47158195952109594, -72.59354914830207406 ) ) ;
#36936=CARTESIAN_POINT ( 'NONE',  ( 54.91244656393700296, 19.73665118953919873, -75.41285438732109014 ) ) ;
#36937=CARTESIAN_POINT ( 'NONE',  ( 46.49593472332909982, -53.10326984347969415, -76.13971323818920212 ) ) ;
#36940=CARTESIAN_POINT ( 'NONE',  ( 57.26071802646550424, -50.61617465155239870, -53.75790974367630071 ) ) ;
#36943=CARTESIAN_POINT ( 'NONE',  ( 47.11902681095249790, 23.00695196644999641, -75.46775895608919882 ) ) ;
#36944=CARTESIAN_POINT ( 'NONE',  ( 48.94270149030929673, 20.57433438911350265, -55.11972614036160678 ) ) ;
#36946=CARTESIAN_POINT ( 'NONE',  ( 55.00867404205060041, 17.28694651894000245, -48.28813249775050309 ) ) ;
#36947=CARTESIAN_POINT ( 'NONE',  ( 12.36320305067610015, 33.31445045643330616, -15.76422791930239953 ) ) ;
#36953=CARTESIAN_POINT ( 'NONE',  ( 61.21881552187829811, 14.03327925050890101, -46.68011238816460207 ) ) ;
#36954=CARTESIAN_POINT ( 'NONE',  ( -32.74859963536999885, -25.24211673056830207, -56.32353328738960130 ) ) ;
#36955=EDGE_CURVE ( 'NONE', #40855, #39471, #16504, .T. ) ;
#36956=ORIENTED_EDGE ( 'NONE', *, *, #1192, .T. ) ;
#36958=CARTESIAN_POINT ( 'NONE',  ( 52.77841038127930773, -49.69307296738830360, -48.67385971155560043 ) ) ;
#36961=CARTESIAN_POINT ( 'NONE',  ( 59.25763488836199855, -45.11616244058109970, -25.82585945883460354 ) ) ;
#36963=CARTESIAN_POINT ( 'NONE',  ( 57.05654409593750387, 14.11921858418430098, -25.89448720482640098 ) ) ;
#36964=CONICAL_SURFACE ( 'NONE', #12705, 1.715179901029911802, 0.08257045569470247703 ) ;
#36966=CARTESIAN_POINT ( 'NONE',  ( 50.77884152257319528, 18.99564097152240194, -76.16429374177040756 ) ) ;
#36967=CARTESIAN_POINT ( 'NONE',  ( 53.36583835243820317, 18.19133335057600220, -49.05762109479490363 ) ) ;
#36969=CARTESIAN_POINT ( 'NONE',  ( 41.06001671441600109, -44.29932858193080136, -3.719606166043670115 ) ) ;
#36970=CARTESIAN_POINT ( 'NONE',  ( 47.23343138990082934, 22.78429296043502816, -75.61476957820426037 ) ) ;
#36973=ORIENTED_EDGE ( 'NONE', *, *, #6939, .F. ) ;
#36975=CARTESIAN_POINT ( 'NONE',  ( 47.48078737089889501, -54.60317255200649811, -54.76237954934830299 ) ) ;
#36976=CARTESIAN_POINT ( 'NONE',  ( 11.93174526809839975, -65.43929183185349530, -17.93019253464870033 ) ) ;
#36982=DIRECTION ( 'NONE',  ( 0.000000000000000000, 0.000000000000000000, -1.000000000000000000 ) ) ;
#36986=CARTESIAN_POINT ( 'NONE',  ( 14.03111719126319912, -51.16607778863529887, -22.86119528526040057 ) ) ;
#36987=DIRECTION ( 'NONE',  ( -0.6801873868961743064, -8.329893061828022439E-17, -0.7330382791555664079 ) ) ;
#36988=ORIENTED_EDGE ( 'NONE', *, *, #35768, .T. ) ;
#36990=DIRECTION ( 'NONE',  ( 0.8090169943749490056, 0.5877852522924709167, 0.000000000000000000 ) ) ;
#36993=CARTESIAN_POINT ( 'NONE',  ( 53.51849367552510017, 19.79182752219439934, -75.95517943487810442 ) ) ;
#36994=ORIENTED_EDGE ( 'NONE', *, *, #24854, .F. ) ;
#36995=CYLINDRICAL_SURFACE ( 'NONE', #2471, 1.500000000000001332 ) ;
#37007=CARTESIAN_POINT ( 'NONE',  ( 14.55217714119870109, 21.30155813473500004, -76.03742712147929694 ) ) ;
#37008=B_SPLINE_CURVE_WITH_KNOTS ( 'NONE', 3,
 ( #49572, #25936, #49818, #13405, #29364, #45887, #34060, #9974, #50069, #1076, #41951, #22008, #38017, #42211, #33025, #45369, #17074, #37496, #13156, #1596, #17584, #29106, #45105, #9211, #33554, #29618, #30902, #10758, #34585, #50846 ),
 .UNSPECIFIED., .F., .F.,
 ( 4, 2, 2, 2, 2, 2, 2, 2, 2, 2, 2, 2, 2, 2, 4 ),
 ( -1.979528000000000055E-13, 0.03743706954986000118, 0.1081389423207600037, 0.1523276128025730092, 0.1872210672024020028, 0.2221145216022309965, 0.2911209749156069559, 0.3342500082364670555, 0.3773790415573270440, 0.4312903332084020436, 0.4852016248594769876, 0.5714596915011970202, 0.6485557695154610114, 0.7719094943382839302, 0.8625806664170020399 ),
 .UNSPECIFIED. ) ;
#37011=CARTESIAN_POINT ( 'NONE',  ( 84.42050518244900559, -43.28355784542729623, -47.35805390042769858 ) ) ;
#37013=VERTEX_POINT ( 'NONE', #36668 ) ;
#37014=CARTESIAN_POINT ( 'NONE',  ( 55.96445070656709930, -46.24620190255259899, -26.04161240161580082 ) ) ;
#37015=CARTESIAN_POINT ( 'NONE',  ( 14.24082757525520115, -51.10274004714279528, -22.22799665057710072 ) ) ;
#37017=CARTESIAN_POINT ( 'NONE',  ( 57.26283657379340042, 19.38381106601499937, -53.75815476539330007 ) ) ;
#37020=CARTESIAN_POINT ( 'NONE',  ( 45.07858682377059978, 14.88010818488339915, -9.026855431852879974 ) ) ;
#37021=ORIENTED_EDGE ( 'NONE', *, *, #37853, .T. ) ;
#37022=CARTESIAN_POINT ( 'NONE',  ( -6.896370999502840604, -45.95266115723829614, -5.351785064663849845 ) ) ;
#37024=CARTESIAN_POINT ( 'NONE',  ( 47.20755063152770248, 23.55563156955719961, -54.64231554542519831 ) ) ;
#37025=DIRECTION ( 'NONE',  ( 0.000000000000000000, -1.000000000000000000, 0.000000000000000000 ) ) ;
#37027=CARTESIAN_POINT ( 'NONE',  ( 68.13393739769840352, -50.61618894467879670, -73.25000000000220268 ) ) ;
#37028=CARTESIAN_POINT ( 'NONE',  ( 11.88973808303819979, 34.20270277534309855, -17.85918046449339869 ) ) ;
#37030=DIRECTION ( 'NONE',  ( 1.000000000000000000, 0.000000000000000000, 0.000000000000000000 ) ) ;
#37033=CARTESIAN_POINT ( 'NONE',  ( 58.68718041671409935, -46.61650995022520050, -47.74352678257979221 ) ) ;
#37035=CARTESIAN_POINT ( 'NONE',  ( 52.77452256448989942, 20.89620967665909745, -53.50297542258699934 ) ) ;
#37040=CARTESIAN_POINT ( 'NONE',  ( 8.972584494015238832, 32.01420432709309694, -46.63288471805530122 ) ) ;
#37043=CARTESIAN_POINT ( 'NONE',  ( 66.69979053676949832, -29.76856963367809783, -17.02723542833530246 ) ) ;
#37045=CARTESIAN_POINT ( 'NONE',  ( 18.42983928211069866, 20.84559406376740043, -75.48537863783369062 ) ) ;
#37048=CARTESIAN_POINT ( 'NONE',  ( 48.47823774206090519, 22.94606279175499708, -55.31601837894839946 ) ) ;
#37050=ADVANCED_FACE ( 'NONE', ( #20419 ), #40613, .T. ) ;
#37051=CARTESIAN_POINT ( 'NONE',  ( 13.00893739769619906, -65.51843714052719747, -47.75434321273180416 ) ) ;
#37052=CARTESIAN_POINT ( 'NONE',  ( 56.92231951192260198, -45.87375801872750003, -26.22432845751160002 ) ) ;
#37054=CARTESIAN_POINT ( 'NONE',  ( 61.43383643809819716, 14.05069848591710091, -47.14994843957639858 ) ) ;
#37057=DIRECTION ( 'NONE',  ( 1.000000000000000000, 0.000000000000000000, 0.000000000000000000 ) ) ;
#37058=CARTESIAN_POINT ( 'NONE',  ( 12.08205733926943637, 34.04687828595569243, -16.92411153880798125 ) ) ;
#37059=VERTEX_POINT ( 'NONE', #47974 ) ;
#37060=CARTESIAN_POINT ( 'NONE',  ( 13.61100063765979407, -17.44920979631380220, -28.02168704970069868 ) ) ;
#37062=CARTESIAN_POINT ( 'NONE',  ( 16.13393739769620083, -15.61618894467929941, -7.393828452885189861 ) ) ;
#37064=ORIENTED_EDGE ( 'NONE', *, *, #9214, .T. ) ;
#37066=CARTESIAN_POINT ( 'NONE',  ( 68.13393739769620083, 19.38381105532069881, -71.50000000000000000 ) ) ;
#37067=CARTESIAN_POINT ( 'NONE',  ( 47.15605882434359586, -54.68808827254829907, -74.81076251056920512 ) ) ;
#37068=CARTESIAN_POINT ( 'NONE',  ( 16.13393739769620083, -15.61618894467929941, 6.072546842075589701 ) ) ;
#37071=CARTESIAN_POINT ( 'NONE',  ( 53.99077097435189643, 14.78852379608610157, -15.26363591289520016 ) ) ;
#37073=CARTESIAN_POINT ( 'NONE',  ( -7.623077062098630563, 14.06405699089660111, -5.205469451225369859 ) ) ;
#37075=AXIS2_PLACEMENT_3D ( 'NONE', #42623, #18240, #34992 ) ;
#37077=CARTESIAN_POINT ( 'NONE',  ( 60.70254012041490199, 13.94047785219770041, -26.91002252692619834 ) ) ;
#37080=CARTESIAN_POINT ( 'NONE',  ( 55.02590511137680096, 17.27791867893839850, -48.37054070093110170 ) ) ;
#37081=CARTESIAN_POINT ( 'NONE',  ( -9.957799118347489653, -43.31361225047390207, -6.454149760335369912 ) ) ;
#37086=CARTESIAN_POINT ( 'NONE',  ( 11.19961949155312553, 34.01496270439587732, -18.17421237848505911 ) ) ;
#37087=CARTESIAN_POINT ( 'NONE',  ( 13.03467379948559923, 18.88909056995609603, -21.08705176942839898 ) ) ;
#37089=CARTESIAN_POINT ( 'NONE',  ( 47.12095841086310344, 23.37868049473910048, -75.00831431077000389 ) ) ;
#37090=CARTESIAN_POINT ( 'NONE',  ( 49.50151222300969778, -53.58170550938950072, -54.38302206046300569 ) ) ;
#37091=CARTESIAN_POINT ( 'NONE',  ( 42.80890084010550112, -44.10023144781310123, -5.063862467037759885 ) ) ;
#37094=CARTESIAN_POINT ( 'NONE',  ( 65.03603135455020379, -32.24781572988710110, -17.83403478221860183 ) ) ;
#37096=EDGE_LOOP ( 'NONE', ( #34567, #36956, #51293, #42817 ) ) ;
#37100=CARTESIAN_POINT ( 'NONE',  ( 83.63329919740728258, -44.53040215208500996, -46.55718455497714103 ) ) ;
#37101=CARTESIAN_POINT ( 'NONE',  ( 60.90580219148289842, -45.59792408994620416, -47.59486805843899759 ) ) ;
#37102=CARTESIAN_POINT ( 'NONE',  ( 57.24718408628069710, 19.38381105960650075, -53.91456318494540056 ) ) ;
#37103=CARTESIAN_POINT ( 'NONE',  ( 50.52803440128089818, 19.14656596045000114, -76.14999999999999147 ) ) ;
#37105=LINE ( 'NONE', #13530, #8925 ) ;
#37107=DIRECTION ( 'NONE',  ( 1.000000000000000000, 0.000000000000000000, 0.000000000000000000 ) ) ;
#37108=ORIENTED_EDGE ( 'NONE', *, *, #25115, .T. ) ;
#37109=CARTESIAN_POINT ( 'NONE',  ( 82.70745875113280476, -45.46473719772439637, -47.51979026979380194 ) ) ;
#37115=FACE_OUTER_BOUND ( 'NONE', #30370, .T. ) ;
#37116=AXIS2_PLACEMENT_3D ( 'NONE', #8551, #5145, #21099 ) ;
#37117=CARTESIAN_POINT ( 'NONE',  ( 56.45053593251559931, -50.66578230959599694, -53.16922271350729545 ) ) ;
#37119=ORIENTED_EDGE ( 'NONE', *, *, #10520, .F. ) ;
#37120=ORIENTED_EDGE ( 'NONE', *, *, #20026, .T. ) ;
#37121=CARTESIAN_POINT ( 'NONE',  ( 11.78282090895823053, 34.18901486863271799, -22.36199502296781816 ) ) ;
#37123=CARTESIAN_POINT ( 'NONE',  ( 56.76343336529819794, 19.30417086840829910, -53.08899915780749978 ) ) ;
#37126=FACE_OUTER_BOUND ( 'NONE', #18417, .T. ) ;
#37127=ORIENTED_EDGE ( 'NONE', *, *, #25525, .F. ) ;
#37129=CARTESIAN_POINT ( 'NONE',  ( 51.93051814572950065, -50.26010286414289396, -76.53037494222229498 ) ) ;
#37131=CARTESIAN_POINT ( 'NONE',  ( 83.76204656032335549, -44.99353952466995565, -47.48603732813779033 ) ) ;
#37137=CARTESIAN_POINT ( 'NONE',  ( 41.34377115688720750, 13.52348016558920030, -5.356934324971369676 ) ) ;
#37138=CARTESIAN_POINT ( 'NONE',  ( 42.26864886252769793, -44.36179212852169940, -5.126484877156399556 ) ) ;
#37140=CARTESIAN_POINT ( 'NONE',  ( -11.32734370190460105, 10.64934056395049922, -6.430561461456250072 ) ) ;
#37142=( BOUNDED_CURVE ( )  B_SPLINE_CURVE ( 3, ( #1241, #44225, #16978, #12263 ),
 .UNSPECIFIED., .F., .T. ) 
 B_SPLINE_CURVE_WITH_KNOTS ( ( 4, 4 ),
 ( 3.141592653589798445, 4.527609048992159657 ),
 .UNSPECIFIED. ) 
 CURVE ( )  GEOMETRIC_REPRESENTATION_ITEM ( )  RATIONAL_B_SPLINE_CURVE ( ( 1.000000000000000000, 0.8462184657327389559, 0.8462184657327389559, 1.000000000000000000 ) ) 
 REPRESENTATION_ITEM ( '' )  );
#37145=CARTESIAN_POINT ( 'NONE',  ( 65.32710660623050103, 0.7917214628020530220, -17.54847713914429974 ) ) ;
#37147=CARTESIAN_POINT ( 'NONE',  ( 14.32991954030070048, -51.86173801737519540, -75.67066142420200947 ) ) ;
#37148=CARTESIAN_POINT ( 'NONE',  ( 57.36123080758890325, 18.90300134970469870, -52.61896056700089730 ) ) ;
#37155=CARTESIAN_POINT ( 'NONE',  ( 11.51841290286379937, 34.14186997694120862, -17.84188021311150152 ) ) ;
#37158=CARTESIAN_POINT ( 'NONE',  ( 56.36581425992820726, 19.41514254598320122, -53.07180551597519980 ) ) ;
#37160=CARTESIAN_POINT ( 'NONE',  ( 48.85702442728319284, 22.78471410673780184, -55.29194429108009956 ) ) ;
#37163=VERTEX_POINT ( 'NONE', #13873 ) ;
#37164=DIRECTION ( 'NONE',  ( 0.000000000000000000, -0.7071067811865492381, -0.7071067811865457964 ) ) ;
#37166=CARTESIAN_POINT ( 'NONE',  ( 14.16187783161720048, 19.11875810978959933, -20.85710678118659800 ) ) ;
#37167=CARTESIAN_POINT ( 'NONE',  ( 83.82044569750020457, 13.55688828085889952, -47.35730118573349756 ) ) ;
#37168=CARTESIAN_POINT ( 'NONE',  ( 54.89514228079339375, 15.99142857377610127, -25.88804800509620208 ) ) ;
#37170=DIRECTION ( 'NONE',  ( 0.000000000000000000, -1.000000000000000000, 0.000000000000000000 ) ) ;
#37171=CARTESIAN_POINT ( 'NONE',  ( 61.50409964636570237, 14.14168666559669951, -47.35437808293550432 ) ) ;
#37172=LINE ( 'NONE', #9135, #38163 ) ;
#37175=ORIENTED_EDGE ( 'NONE', *, *, #32926, .F. ) ;
#37176=CARTESIAN_POINT ( 'NONE',  ( 11.93872965651020124, -65.19885638306720921, -16.76612700403689971 ) ) ;
#37177=CARTESIAN_POINT ( 'NONE',  ( 11.91647380877470042, 33.89555377125369517, -46.05219393946750017 ) ) ;
#37179=CARTESIAN_POINT ( 'NONE',  ( 52.10268719324110265, -50.36005704266560201, -49.19170910618320391 ) ) ;
#37180=CARTESIAN_POINT ( 'NONE',  ( 51.49832873845635817, 3.074675621640686973, -76.79134042563141804 ) ) ;
#37183=CARTESIAN_POINT ( 'NONE',  ( 57.34776335324270491, 14.57942837581910034, -26.27178905609630277 ) ) ;
#37186=CARTESIAN_POINT ( 'NONE',  ( 50.45277833511170229, 21.36013689488169831, -53.06622874095319986 ) ) ;
#37190=ORIENTED_EDGE ( 'NONE', *, *, #47809, .T. ) ;
#37194=CARTESIAN_POINT ( 'NONE',  ( 12.51334871620187350, -55.45190834908655830, -75.31104306447832641 ) ) ;
#37198=FACE_OUTER_BOUND ( 'NONE', #2755, .T. ) ;
#37200=CARTESIAN_POINT ( 'NONE',  ( 46.42423052835359698, -53.00637862934869560, -76.14999999999999147 ) ) ;
#37201=EDGE_LOOP ( 'NONE', ( #21828, #25762, #29049, #6929 ) ) ;
#37202=CARTESIAN_POINT ( 'NONE',  ( 54.56504058078360231, 14.73772175096070036, -15.64073168106889788 ) ) ;
#37203=CARTESIAN_POINT ( 'NONE',  ( 57.02020363348529486, -50.59809222457260347, -53.44649995476070359 ) ) ;
#37208=CARTESIAN_POINT ( 'NONE',  ( 47.02522487057739653, 22.84427288168209813, -75.65261601872900599 ) ) ;
#37211=CARTESIAN_POINT ( 'NONE',  ( 41.26357389881030002, -45.58122989547749881, -6.211371138913489354 ) ) ;
#37212=CARTESIAN_POINT ( 'NONE',  ( 12.36320305067610015, 33.31445045643330616, -15.76422791930239953 ) ) ;
#37221=DIRECTION ( 'NONE',  ( 0.3294064756441309472, 0.9441882088883087887, -3.053113317719179500E-16 ) ) ;
#37222=CARTESIAN_POINT ( 'NONE',  ( -25.59424942068570275, -40.82387122898790466, -54.31183179444199993 ) ) ;
#37225=CARTESIAN_POINT ( 'NONE',  ( 52.95585360091419602, -49.59527434762240006, -48.79473317602730020 ) ) ;
#37226=CARTESIAN_POINT ( 'NONE',  ( 58.64502850088660324, -45.25097017255860266, -26.10756731467850145 ) ) ;
#37227=FACE_OUTER_BOUND ( 'NONE', #893, .T. ) ;
#37228=CARTESIAN_POINT ( 'NONE',  ( 13.45432746122430068, 19.59659184310620006, -21.59563733192320001 ) ) ;
#37229=CARTESIAN_POINT ( 'NONE',  ( 56.93624918340190533, 14.63482917628590130, -26.22451992585920166 ) ) ;
#37231=CARTESIAN_POINT ( 'NONE',  ( 50.12211799414349400, 17.52854795053300307, -76.14999999999999147 ) ) ;
#37232=CARTESIAN_POINT ( 'NONE',  ( 52.82044782574460129, 18.44684647757109985, -48.83393253442750392 ) ) ;
#37234=CARTESIAN_POINT ( 'NONE',  ( 41.03393739769609994, -15.61618894467929586, 8.449999999999974420 ) ) ;
#37235=CARTESIAN_POINT ( 'NONE',  ( 75.49020191205489994, -43.37239104213820440, -13.40805175275450090 ) ) ;
#37236=ORIENTED_EDGE ( 'NONE', *, *, #1757, .F. ) ;
#37239=CARTESIAN_POINT ( 'NONE',  ( 47.44496049464380150, -54.63145718528269867, -54.91866264090269567 ) ) ;
#37242=CARTESIAN_POINT ( 'NONE',  ( 58.91899206676210810, -28.48616099405090196, -15.64938374009210165 ) ) ;
#37248=ORIENTED_EDGE ( 'NONE', *, *, #28898, .F. ) ;
#37250=CARTESIAN_POINT ( 'NONE',  ( 8.815605939025839888, -63.28267558187339148, -46.67186391138339729 ) ) ;
#37256=CARTESIAN_POINT ( 'NONE',  ( 51.62415641043660486, 19.44432096110770303, -76.24933075980271724 ) ) ;
#37257=VERTEX_POINT ( 'NONE', #49023 ) ;
#37259=DIRECTION ( 'NONE',  ( -0.7089970498513415986, 0.7052114458104705719, -6.938893903906735340E-16 ) ) ;
#37261=B_SPLINE_SURFACE_WITH_KNOTS ( 'NONE', 3, 3, ( 
 ( #28629, #44895, #32807, #17121, #45153, #32538, #48833, #17375, #36496, #49618, #33604 ),
 ( #1126, #44630, #5590, #16585, #48573, #9000, #25213, #12936, #24944, #13203, #24685 ),
 ( #17637, #37540, #40955, #1646, #49357, #21028, #49102, #12675, #41218, #37028, #40699 ),
 ( #29152, #21284, #4799, #20766, #5332, #29414, #33074, #37289, #1388, #33342, #13459 ),
 ( #45418, #9523, #6359, #14988, #22319, #38595, #25992, #37812, #42004, #26769, #2165 ),
 ( #18913, #22832, #33856, #27037, #50121, #34632, #34896, #46726, #46206, #2686, #10810 ),
 ( #42786, #2414, #50387, #6102, #13963, #50896, #10291, #30954, #22059, #46465, #6882 ),
 ( #11070, #46986, #38853, #38069, #42260, #18145, #29919, #5840, #26254, #21806, #34109 ),
 ( #2942, #1906, #17885, #49870, #45937, #14217, #38325, #10026, #30190, #18396, #34375 ),
 ( #14471, #30444, #10553, #26510, #42526, #22577, #6614, #18658, #50637, #14733, #30704 ),
 ( #27788, #7635, #31189, #3960, #15746, #27527, #35666, #23833, #43785, #11053, #19420 ),
 ( #39092, #11830, #2926, #3187, #23581, #51396, #23320, #51651, #39598, #27019, #11310 ),
 ( #15495, #43536, #14971, #47221, #47724, #44039, #31960, #47980, #19670, #35398, #43026 ),
 ( #18895, #34881, #27274, #7887, #19157, #51142, #47475, #7124, #39854, #30, #19920 ),
 ( #35913, #12082, #43284, #31447, #28036, #8143, #15239, #24088, #50880, #11568, #46969 ),
 ( #23074, #35137, #7373, #39347, #3447, #273, #45072, #16256, #9179, #16777, #24605 ),
 ( #49279, #4718, #20951, #8400, #20176, #24349, #25136, #36416, #28812, #1312, #5252 ),
 ( #9444, #32459, #17041, #17301, #29079, #28553, #36947, #41139, #21205, #37212, #36674 ) ),
 .UNSPECIFIED., .F., .F., .F.,
 ( 4, 2, 2, 2, 2, 2, 2, 2, 4 ),
 ( 4, 1, 1, 1, 1, 1, 1, 1, 4 ),
 ( -0.8717220151850350041, -0.8429723630856670313, -0.6591356692331089562, -0.5442377355752608947, -0.4350764559609309745, -0.3804958161537659866, -0.2931667924623029831, -0.1534403545559610005, 0.001568662496386999828 ),
 ( 0.000000000000000000, 0.1250000000000000000, 0.2500000000000000000, 0.3750000000000000000, 0.5000000000000000000, 0.6250000000000000000, 0.7500000000000000000, 0.8750000000000000000, 1.000000440766789955 ),
 .UNSPECIFIED. ) ;
#37267=CARTESIAN_POINT ( 'NONE',  ( 57.14590266161170007, -45.85825177618220039, -26.25338899624249933 ) ) ;
#37270=CARTESIAN_POINT ( 'NONE',  ( 14.04674101893040117, 20.91311638024189890, -75.69337827730609547 ) ) ;
#37275=ORIENTED_EDGE ( 'NONE', *, *, #19142, .T. ) ;
#37276=CARTESIAN_POINT ( 'NONE',  ( 53.78531600184879835, -48.57334919407480101, -26.63319078974290122 ) ) ;
#37277=AXIS2_PLACEMENT_3D ( 'NONE', #50225, #14314, #30283 ) ;
#37278=CARTESIAN_POINT ( 'NONE',  ( 54.71118390020190247, -51.11900467049459706, -75.31578149455251037 ) ) ;
#37279=CARTESIAN_POINT ( 'NONE',  ( 10.61758738775479927, 33.59332580352769781, -18.17420787144230232 ) ) ;
#37284=CARTESIAN_POINT ( 'NONE',  ( -5.654166889186940992, -46.79365041531399783, -4.894927202041920111 ) ) ;
#37285=CARTESIAN_POINT ( 'NONE',  ( 47.34904504271399617, 23.45336456905550193, -54.69724835834480103 ) ) ;
#37288=CARTESIAN_POINT ( 'NONE',  ( 68.13393739769745139, -49.21324915460503036, -70.54648330188274485 ) ) ;
#37289=CARTESIAN_POINT ( 'NONE',  ( 11.69717481575709961, 34.15430575971510052, -17.57872672726050212 ) ) ;
#37294=CARTESIAN_POINT ( 'NONE',  ( 57.55922429997960421, -47.27898653534939655, -48.12542328384540724 ) ) ;
#37295=CARTESIAN_POINT ( 'NONE',  ( 53.11476273806689363, 18.18247392671170104, -27.56271911843160183 ) ) ;
#37296=CARTESIAN_POINT ( 'NONE',  ( 55.69529708736050111, 19.85053035562459911, -53.59729798802170109 ) ) ;
#37299=ORIENTED_EDGE ( 'NONE', *, *, #40978, .T. ) ;
#37301=CARTESIAN_POINT ( 'NONE',  ( 8.977322698627309805, 32.04338259973479808, -46.63353404011659364 ) ) ;
#37304=CARTESIAN_POINT ( 'NONE',  ( 66.66721609728190856, -29.91978853676059913, -17.00551245635359976 ) ) ;
#37305=CARTESIAN_POINT ( 'NONE',  ( 18.26164351804030161, 20.66741474030959935, -75.53710645103448940 ) ) ;
#37307=ORIENTED_EDGE ( 'NONE', *, *, #16594, .F. ) ;
#37308=DIRECTION ( 'NONE',  ( 0.2260571801428161443, -1.387778780781444751E-17, -0.9741140340359945027 ) ) ;
#37309=ORIENTED_EDGE ( 'NONE', *, *, #48044, .T. ) ;
#37310=CARTESIAN_POINT ( 'NONE',  ( 10.40650514412410033, -63.80199668435589189, -45.90516490080199929 ) ) ;
#37311=CARTESIAN_POINT ( 'NONE',  ( 57.21078602787749645, -45.77107311845719551, -26.23711395555770309 ) ) ;
#37313=CARTESIAN_POINT ( 'NONE',  ( 61.34620581403849826, 14.06250526994010031, -47.14190415927130573 ) ) ;
#37315=ORIENTED_EDGE ( 'NONE', *, *, #33711, .F. ) ;
#37317=AXIS2_PLACEMENT_3D ( 'NONE', #41724, #5831, #37802 ) ;
#37319=CARTESIAN_POINT ( 'NONE',  ( 47.04983409348690060, -45.11618894461270202, -8.541664432791959527 ) ) ;
#37320=TOROIDAL_SURFACE ( 'NONE', #39825, 17.69999999999999929, 3.799999999999830180 ) ;
#37321=ADVANCED_FACE ( 'NONE', ( #778 ), #16778, .T. ) ;
#37323=DIRECTION ( 'NONE',  ( -0.1686178020941670463, 0.6660492713794461395, 0.7265992051412121233 ) ) ;
#37327=CARTESIAN_POINT ( 'NONE',  ( 46.40189200261440305, -53.01982478580160318, -76.14999999999999147 ) ) ;
#37328=CARTESIAN_POINT ( 'NONE',  ( 85.84022851002180232, 17.38381105532069881, -53.47585302082339354 ) ) ;
#37330=CARTESIAN_POINT ( 'NONE',  ( 45.63703752229459809, 14.88915874026919894, -9.401572978158439398 ) ) ;
#37332=DIRECTION ( 'NONE',  ( -0.1414213562373098920, 0.000000000000000000, -0.9899494936611664686 ) ) ;
#37334=AXIS2_PLACEMENT_3D ( 'NONE', #9757, #21787, #34617 ) ;
#37336=CARTESIAN_POINT ( 'NONE',  ( 57.68156670551299925, 13.95962980738159942, -25.76772952340219902 ) ) ;
#37338=EDGE_LOOP ( 'NONE', ( #44272, #33632, #40887, #15602, #48641 ) ) ;
#37339=CARTESIAN_POINT ( 'NONE',  ( 58.49950606315620405, 15.48244237084779940, -47.77607446784710277 ) ) ;
#37340=CARTESIAN_POINT ( 'NONE',  ( -11.08689484260690072, -41.65128607374619918, -5.028175088695070016 ) ) ;
#37341=CARTESIAN_POINT ( 'NONE',  ( 75.67253118882268836, -42.26411609651090373, -13.31112060773330086 ) ) ;
#37345=CARTESIAN_POINT ( 'NONE',  ( 12.26282170032640195, -64.61533680211610431, -15.83707920938230096 ) ) ;
#37346=AXIS2_PLACEMENT_3D ( 'NONE', #6477, #38972, #15113 ) ;
#37347=CARTESIAN_POINT ( 'NONE',  ( 82.35524870416759313, -45.10829932330300096, -46.40105680372339947 ) ) ;
#37349=CARTESIAN_POINT ( 'NONE',  ( 48.99827939567540369, -53.83769105205929861, -54.60353251326420576 ) ) ;
#37351=CARTESIAN_POINT ( 'NONE',  ( -3.429778956281600344, -15.61618894467929763, 7.849999999999999645 ) ) ;
#37356=CARTESIAN_POINT ( 'NONE',  ( 16.13393739769620083, -15.61618894467929941, -6.721843382729280059 ) ) ;
#37357=CARTESIAN_POINT ( 'NONE',  ( 60.87196862875009629, -45.65759271181720180, -47.67694403705610284 ) ) ;
#37359=CARTESIAN_POINT ( 'NONE',  ( 50.77827180918709615, 19.51522592562140090, -76.14999999999999147 ) ) ;
#37363=CARTESIAN_POINT ( 'NONE',  ( 52.71259601604019451, -51.43286903184419856, -75.79898490202970152 ) ) ;
#37367=ORIENTED_EDGE ( 'NONE', *, *, #40516, .T. ) ;
#37369=ORIENTED_EDGE ( 'NONE', *, *, #7474, .F. ) ;
#37370=CARTESIAN_POINT ( 'NONE',  ( 61.61573738770560027, -45.13429482264220383, -46.61624098993680576 ) ) ;
#37373=AXIS2_PLACEMENT_3D ( 'NONE', #33524, #21978, #25650 ) ;
#37374=ORIENTED_EDGE ( 'NONE', *, *, #14014, .T. ) ;
#37381=DIRECTION ( 'NONE',  ( 0.000000000000000000, -1.000000000000000000, 0.000000000000000000 ) ) ;
#37384=CARTESIAN_POINT ( 'NONE',  ( 52.61122377792880656, -50.99960881131569579, -76.13271377727109268 ) ) ;
#37386=CARTESIAN_POINT ( 'NONE',  ( 83.91174613997148413, -44.80490681739117065, -47.46626505639375182 ) ) ;
#37387=CIRCLE ( 'NONE', #30677, 1.999999999999997113 ) ;
#37392=CARTESIAN_POINT ( 'NONE',  ( 45.86660482663089766, 13.88490149991019962, -7.634519155851280381 ) ) ;
#37393=CARTESIAN_POINT ( 'NONE',  ( 42.34652498500450690, -44.08694099878920269, -4.929786139639760201 ) ) ;
#37395=CARTESIAN_POINT ( 'NONE',  ( -11.32734370190460105, 10.64934056395049922, -6.430192534648650593 ) ) ;
#37398=CARTESIAN_POINT ( 'NONE',  ( 66.87130723771809926, 0.3340111767280660171, -17.65465185469040321 ) ) ;
#37400=CARTESIAN_POINT ( 'NONE',  ( 14.35743399087829886, -51.90926368007729508, -75.71157996061791096 ) ) ;
#37401=B_SPLINE_CURVE_WITH_KNOTS ( 'NONE', 3,
 ( #1751, #26880, #6984, #10918, #6468, #42891, #22683, #22938 ),
 .UNSPECIFIED., .F., .F.,
 ( 4, 2, 2, 4 ),
 ( 0.4999999271596042849, 0.6249999999961461938, 0.8117231960810037394, 1.000000000000000000 ),
 .UNSPECIFIED. ) ;
#37402=CARTESIAN_POINT ( 'NONE',  ( 47.21725345290060005, -54.78032235606750078, -54.61943838409560215 ) ) ;
#37405=CIRCLE ( 'NONE', #34892, 32.00000000000000000 ) ;
#37407=CARTESIAN_POINT ( 'NONE',  ( 14.34417029198830029, 20.88381105532299742, -23.15000000000000213 ) ) ;
#37408=CARTESIAN_POINT ( 'NONE',  ( 11.78673863893369855, 34.19465826557939891, -17.91922926160039964 ) ) ;
#37409=CARTESIAN_POINT ( 'NONE',  ( 14.29774505407299934, 19.88381105532299742, -22.54670831509739770 ) ) ;
#37411=CARTESIAN_POINT ( 'NONE',  ( 48.19603879950989977, 23.00596188178739965, -54.83412089522879285 ) ) ;
#37415=DIRECTION ( 'NONE',  ( -0.2260571801428161165, -2.775557561562891043E-17, 0.9741140340359943917 ) ) ;
#37417=CARTESIAN_POINT ( 'NONE',  ( 53.59007904684525414, -49.40624020596621335, -49.22506784124646373 ) ) ;
#37418=CARTESIAN_POINT ( 'NONE',  ( 14.02678725144350302, 19.07322791160352793, -20.88317649143827381 ) ) ;
#37419=CARTESIAN_POINT ( 'NONE',  ( 84.22529662124048855, 12.91617031814629968, -47.36165834067109870 ) ) ;
#37420=CARTESIAN_POINT ( 'NONE',  ( 54.11082558918479890, 16.90719386950179626, -26.08329795554909936 ) ) ;
#37423=CARTESIAN_POINT ( 'NONE',  ( 11.47551314107553289, 33.73997922480182154, -16.61573023121771087 ) ) ;
#37424=CARTESIAN_POINT ( 'NONE',  ( 56.43578946174220334, -45.13008420189939329, -15.60617155886200003 ) ) ;
#37427=ORIENTED_EDGE ( 'NONE', *, *, #9310, .F. ) ;
#37428=ORIENTED_EDGE ( 'NONE', *, *, #14135, .F. ) ;
#37429=ADVANCED_FACE ( 'NONE', ( #34557 ), #37320, .F. ) ;
#37430=CARTESIAN_POINT ( 'NONE',  ( 11.68991505667689879, -64.90566085822540288, -16.36861125146140239 ) ) ;
#37431=CARTESIAN_POINT ( 'NONE',  ( 11.83096648206709922, 33.93729815101410452, -46.65733685557199806 ) ) ;
#37435=ORIENTED_EDGE ( 'NONE', *, *, #14498, .T. ) ;
#37439=CARTESIAN_POINT ( 'NONE',  ( 62.50437461550328777, -1.750381705555160261, -16.13137864070830219 ) ) ;
#37440=CARTESIAN_POINT ( 'NONE',  ( 50.65831133345510295, -49.27121936819580839, -76.22116164247820791 ) ) ;
#37444=CARTESIAN_POINT ( 'NONE',  ( 53.09137791023449893, -49.29352759859440170, -26.91462423334489884 ) ) ;
#37451=CARTESIAN_POINT ( 'NONE',  ( 13.93867182927249893, -51.20113036054549838, -22.80125035677469825 ) ) ;
#37452=CARTESIAN_POINT ( 'NONE',  ( 55.04746246912909413, 19.47632002275969754, -75.94217828162659600 ) ) ;
#37453=CARTESIAN_POINT ( 'NONE',  ( 47.14495913819240513, -54.17197317070149865, -75.51614565244940991 ) ) ;
#37454=ORIENTED_EDGE ( 'NONE', *, *, #22407, .F. ) ;
#37455=CARTESIAN_POINT ( 'NONE',  ( 55.27717382112350464, 14.24043577392810001, -15.58341969604579802 ) ) ;
#37456=CARTESIAN_POINT ( 'NONE',  ( 57.22241558393270111, -50.57952226092219661, -53.44445692378550206 ) ) ;
#37460=EDGE_LOOP ( 'NONE', ( #38056, #51446, #3134, #28326 ) ) ;
#37461=CARTESIAN_POINT ( 'NONE',  ( 47.21824388184999322, 23.05645682666510154, -75.35584192875380438 ) ) ;
#37462=AXIS2_PLACEMENT_3D ( 'NONE', #14743, #38335, #6892 ) ;
#37464=B_SPLINE_CURVE_WITH_KNOTS ( 'NONE', 3,
 ( #48380, #417, #12746, #12476, #44446, #8552, #20838, #17192, #24495, #4601, #20576, #16936, #13011, #36569 ),
 .UNSPECIFIED., .F., .F.,
 ( 4, 2, 2, 2, 2, 2, 4 ),
 ( 0.000000000000000000, 0.1519567928777398325, 0.3055814807050730719, 0.4015969105971532449, 0.5936277703813197526, 0.9008771460359852323, 1.000000000000000000 ),
 .UNSPECIFIED. ) ;
#37466=DIRECTION ( 'NONE',  ( -0.6643794812577336062, 0.7473954140103516997, 0.000000000000000000 ) ) ;
#37469=FACE_OUTER_BOUND ( 'NONE', #8958, .T. ) ;
#37473=CARTESIAN_POINT ( 'NONE',  ( 61.28346094977100478, 13.99940985045950015, -46.43278510584719498 ) ) ;
#37475=CARTESIAN_POINT ( 'NONE',  ( -32.94143001319760344, -20.36928658016449845, -56.02216466475820056 ) ) ;
#37476=EDGE_LOOP ( 'NONE', ( #5617, #46847, #39442, #31029 ) ) ;
#37477=CARTESIAN_POINT ( 'NONE',  ( 52.91697748939440515, -49.61738182755579629, -48.80601310497799261 ) ) ;
#37478=VERTEX_POINT ( 'NONE', #25908 ) ;
#37479=CARTESIAN_POINT ( 'NONE',  ( 58.69147808494039964, -45.17395921270860271, -25.95218655891679660 ) ) ;
#37481=CARTESIAN_POINT ( 'NONE',  ( 57.51163818235249892, 13.96175988552229974, -25.74441108106429965 ) ) ;
#37483=CARTESIAN_POINT ( 'NONE',  ( 50.20000624151339963, 18.43678156217390196, -76.14999999999999147 ) ) ;
#37484=CARTESIAN_POINT ( 'NONE',  ( 52.77791158333219812, 18.46457420104869840, -48.73086690438350388 ) ) ;
#37486=CARTESIAN_POINT ( 'NONE',  ( 67.42785983160000285, -44.32276271297559589, -11.41916062409890031 ) ) ;
#37487=EDGE_CURVE ( 'NONE', #15006, #30985, #28092, .T. ) ;
#37490=ADVANCED_FACE ( 'NONE', ( #30874 ), #26955, .T. ) ;
#37492=CARTESIAN_POINT ( 'NONE',  ( 47.44225467880999503, -54.63206288700619950, -54.85722679016069492 ) ) ;
#37493=CARTESIAN_POINT ( 'NONE',  ( 47.13393739769619373, -15.61618894467929941, -15.65000000000000036 ) ) ;
#37495=CARTESIAN_POINT ( 'NONE',  ( 11.41644049895860036, -65.35642350271008638, -18.17421237901670139 ) ) ;
#37496=CARTESIAN_POINT ( 'NONE',  ( 53.00700879704349688, 18.33567502363469970, -48.78176283131570301 ) ) ;
#37502=VERTEX_POINT ( 'NONE', #45859 ) ;
#37503=CARTESIAN_POINT ( 'NONE',  ( 9.297749548753010629, -63.28389869551808999, -46.53031453602530121 ) ) ;
#37505=VERTEX_POINT ( 'NONE', #41921 ) ;
#37509=CARTESIAN_POINT ( 'NONE',  ( 52.31626064796109432, 19.70647560332339765, -76.18456440489789827 ) ) ;
#37511=DIRECTION ( 'NONE',  ( 0.000000000000000000, 1.000000000000000000, 0.000000000000000000 ) ) ;
#37512=CARTESIAN_POINT ( 'NONE',  ( 52.10267382257649871, 1.883811055284760005, -77.60820171200670359 ) ) ;
#37514=EDGE_CURVE ( 'NONE', #18363, #44083, #26408, .T. ) ;
#37516=DIRECTION ( 'NONE',  ( 0.000000000000000000, 0.000000000000000000, -1.000000000000000000 ) ) ;
#37518=ADVANCED_FACE ( 'NONE', ( #34033 ), #41509, .F. ) ;
#37520=CARTESIAN_POINT ( 'NONE',  ( 18.86789271212754215, 20.55440457922848907, -74.33587756536769575 ) ) ;
#37523=CARTESIAN_POINT ( 'NONE',  ( 14.06610822376199899, 20.17488022308399920, -75.08736963500949457 ) ) ;
#37525=CARTESIAN_POINT ( 'NONE',  ( 41.46798912450119445, -44.88968489520180327, -5.587157704053289820 ) ) ;
#37526=CARTESIAN_POINT ( 'NONE',  ( 82.63159810076149370, -45.06836083909839630, -46.43844420537259765 ) ) ;
#37528=ORIENTED_EDGE ( 'NONE', *, *, #43839, .F. ) ;
#37529=CARTESIAN_POINT ( 'NONE',  ( 53.88942171400410786, -48.39633017241650492, -26.28222357612559890 ) ) ;
#37530=CARTESIAN_POINT ( 'NONE',  ( 55.19366304728959705, -51.02473303371100144, -75.15423526130980747 ) ) ;
#37531=CARTESIAN_POINT ( 'NONE',  ( 9.433581914129849366, 30.61547584016309997, -13.45314291414399932 ) ) ;
#37532=CARTESIAN_POINT ( 'NONE',  ( 16.13393739769620083, -15.61618894467929941, 6.349999999999999645 ) ) ;
#37533=CARTESIAN_POINT ( 'NONE',  ( 14.34417029198879945, -52.11618894467930119, -74.14999999999999147 ) ) ;
#37535=CARTESIAN_POINT ( 'NONE',  ( -3.981438317303439778, -47.92280625716200149, -4.793466068732310070 ) ) ;
#37536=CARTESIAN_POINT ( 'NONE',  ( 47.51972458776440078, 23.33356625217060198, -54.65851536377620334 ) ) ;
#37540=CARTESIAN_POINT ( 'NONE',  ( 10.91696762329730142, 33.77617350747969738, -17.52451613595910374 ) ) ;
#37542=CARTESIAN_POINT ( 'NONE',  ( 68.13393739769810509, 19.38381105532030091, -71.50000000000198952 ) ) ;
#37545=CARTESIAN_POINT ( 'NONE',  ( 52.82976477458089448, 18.42853897965050081, -28.09161879090800085 ) ) ;
#37547=CARTESIAN_POINT ( 'NONE',  ( 52.85039779125390424, 21.08368931838860050, -54.40094741851120119 ) ) ;
#37550=ORIENTED_EDGE ( 'NONE', *, *, #46377, .T. ) ;
#37552=CARTESIAN_POINT ( 'NONE',  ( 9.737523894043130568, 31.98622279338489349, -46.29791410543919739 ) ) ;
#37556=B_SPLINE_CURVE_WITH_KNOTS ( 'NONE', 3,
 ( #18119, #49332, #21522, #37785, #25446, #45911, #5566, #41707, #37520, #6075 ),
 .UNSPECIFIED., .F., .F.,
 ( 4, 2, 2, 2, 4 ),
 ( 0.4999999271656643818, 0.5624999999903476100, 0.6624999999924280347, 0.8224999999957559593, 1.000000000000000000 ),
 .UNSPECIFIED. ) ;
#37561=CARTESIAN_POINT ( 'NONE',  ( 12.46092453159049995, -65.42383766440380555, -47.10609709158759983 ) ) ;
#37562=CARTESIAN_POINT ( 'NONE',  ( 56.74397420296469363, -45.46880684231319947, -25.88716263708979781 ) ) ;
#37563=B_SPLINE_CURVE_WITH_KNOTS ( 'NONE', 3,
 ( #12473, #23210, #7777, #15382, #31335, #31849, #11458, #27415 ),
 .UNSPECIFIED., .F., .F.,
 ( 4, 2, 2, 4 ),
 ( 0.000000000000000000, 0.1749999999961678876, 0.3749999999917854598, 0.4999999271656643818 ),
 .UNSPECIFIED. ) ;
#37565=CARTESIAN_POINT ( 'NONE',  ( 61.72743783710129861, 13.88647446954439957, -46.49120720414349961 ) ) ;
#37568=CIRCLE ( 'NONE', #29180, 20.00000000000001421 ) ;
#37571=CARTESIAN_POINT ( 'NONE',  ( 52.51556228498769485, -45.11618894460669793, -12.38233830838520078 ) ) ;
#37574=EDGE_CURVE ( 'NONE', #18792, #46486, #34669, .T. ) ;
#37578=CARTESIAN_POINT ( 'NONE',  ( 46.55184893656709733, -53.32569582049830359, -76.10173089639540933 ) ) ;
#37579=CARTESIAN_POINT ( 'NONE',  ( 75.40667024492320536, 13.07356525956230087, -13.67454515778790025 ) ) ;
#37580=CARTESIAN_POINT ( 'NONE',  ( 48.37121793235419887, 13.88381105532070059, -9.155085387312430711 ) ) ;
#37581=DIRECTION ( 'NONE',  ( 0.000000000000000000, 0.000000000000000000, -1.000000000000000000 ) ) ;
#37583=CARTESIAN_POINT ( 'NONE',  ( 61.35827264627630484, 13.96263723663859935, -28.15113330384149748 ) ) ;
#37585=ORIENTED_EDGE ( 'NONE', *, *, #21719, .T. ) ;
#37587=CARTESIAN_POINT ( 'NONE',  ( -9.664157262737310461, -43.13799255771849772, -5.051889323743290028 ) ) ;
#37588=CARTESIAN_POINT ( 'NONE',  ( 75.47851028940139884, -43.42898794502159632, -13.41230162649550017 ) ) ;
#37591=CIRCLE ( 'NONE', #48488, 38.00000000000000711 ) ;
#37594=AXIS2_PLACEMENT_3D ( 'NONE', #48936, #20860, #36863 ) ;
#37596=CARTESIAN_POINT ( 'NONE',  ( 49.15407994174589845, -53.83453679569459638, -54.78253050193919904 ) ) ;
#37597=CARTESIAN_POINT ( 'NONE',  ( 51.17843651765708302, -31.65766843421481624, -17.12041166110326174 ) ) ;
#37598=EDGE_CURVE ( 'NONE', #19762, #29825, #15553, .T. ) ;
#37599=VECTOR ( 'NONE', #42529, 1000.000000000000000 ) ;
#37600=DIRECTION ( 'NONE',  ( 0.000000000000000000, 0.000000000000000000, 1.000000000000000000 ) ) ;
#37601=CARTESIAN_POINT ( 'NONE',  ( 18.30650362895240235, -51.22777015963880132, -74.58518005234699899 ) ) ;
#37602=CARTESIAN_POINT ( 'NONE',  ( 56.27102381480889903, -50.57721995146319927, -52.87265154067429762 ) ) ;
#37606=B_SPLINE_CURVE_WITH_KNOTS ( 'NONE', 3,
 ( #36163, #19919, #36946, #32725, #28035, #29, #16509, #272, #36673, #9177 ),
 .UNSPECIFIED., .F., .F.,
 ( 4, 2, 2, 2, 4 ),
 ( -5.773159999999999959E-14, 2.783242270592499956, 5.292080373661850246, 6.860104188080190291, 7.840119072091650487 ),
 .UNSPECIFIED. ) ;
#37607=ADVANCED_FACE ( 'NONE', ( #47415 ), #39791, .T. ) ;
#37609=ORIENTED_EDGE ( 'NONE', *, *, #37598, .F. ) ;
#37611=CARTESIAN_POINT ( 'NONE',  ( 61.24499251173579495, -45.54248517078090686, -47.60670208486399702 ) ) ;
#37616=ADVANCED_FACE ( 'NONE', ( #39279 ), #44839, .F. ) ;
#37617=CARTESIAN_POINT ( 'NONE',  ( 50.96213132486371933, -50.95760513581273443, -76.15000000000004832 ) ) ;
#37618=CARTESIAN_POINT ( 'NONE',  ( 42.00758945880200201, -45.79790383927660002, -6.830514409016920752 ) ) ;
#37620=VERTEX_POINT ( 'NONE', #19094 ) ;
#37623=CARTESIAN_POINT ( 'NONE',  ( 61.11135448844899543, -45.32462824983760186, -46.90702640965010062 ) ) ;
#37624=CARTESIAN_POINT ( 'NONE',  ( 53.05499567186660670, -49.60096502583370182, -49.11111871955459662 ) ) ;
#37625=CARTESIAN_POINT ( 'NONE',  ( 61.28085239525059791, 14.36939662108470017, -47.67834120296360112 ) ) ;
#37632=CARTESIAN_POINT ( 'NONE',  ( 56.09651439476719759, -50.93334530694360041, -53.89358350665009567 ) ) ;
#37634=DIRECTION ( 'NONE',  ( 0.000000000000000000, 0.000000000000000000, 1.000000000000000000 ) ) ;
#37637=ORIENTED_EDGE ( 'NONE', *, *, #11062, .F. ) ;
#37639=CARTESIAN_POINT ( 'NONE',  ( 51.99242832958879745, -50.02583382361060416, -76.70333696065139861 ) ) ;
#37645=CARTESIAN_POINT ( 'NONE',  ( 45.83940546124159710, 13.90408673295529773, -7.873659366785940250 ) ) ;
#37646=CARTESIAN_POINT ( 'NONE',  ( 42.42176421416689891, -44.20760043642759740, -5.045468647411699870 ) ) ;
#37647=CARTESIAN_POINT ( 'NONE',  ( 68.13393739769847457, -50.70395984888145335, -72.15645085170113759 ) ) ;
#37648=CARTESIAN_POINT ( 'NONE',  ( 56.23669252666629603, 14.33142556199779882, -25.29918085107650327 ) ) ;
#37649=EDGE_CURVE ( 'NONE', #19842, #25873, #16472, .T. ) ;
#37652=CARTESIAN_POINT ( 'NONE',  ( 66.95999988526210700, 1.459641452089809999, -18.94776480168570032 ) ) ;
#37654=CARTESIAN_POINT ( 'NONE',  ( 14.92989387051190064, -52.97186080988799972, -76.14999999999999147 ) ) ;
#37655=CARTESIAN_POINT ( 'NONE',  ( 57.36404682476049999, 18.93586243731099827, -52.65764136420510511 ) ) ;
#37660=CARTESIAN_POINT ( 'NONE',  ( 11.77545672747359973, 34.19368150675510520, -17.95294975582580221 ) ) ;
#37661=DIRECTION ( 'NONE',  ( -0.2260571801428140071, 0.000000000000000000, 0.9741140340359949468 ) ) ;
#37663=CARTESIAN_POINT ( 'NONE',  ( 48.37262564244719698, 22.87082288443439992, -54.65898693694939681 ) ) ;
#37664=VECTOR ( 'NONE', #9861, 1000.000000000000114 ) ;
#37671=CARTESIAN_POINT ( 'NONE',  ( 82.46534785695916980, 13.86080115390507750, -46.44243061472944589 ) ) ;
#37674=CARTESIAN_POINT ( 'NONE',  ( 84.17895764879889953, 12.85061017212530032, -47.20739533566359825 ) ) ;
#37675=CARTESIAN_POINT ( 'NONE',  ( 55.85842059416459904, 14.74773178907929960, -25.34033418961709927 ) ) ;
#37679=DIRECTION ( 'NONE',  ( 0.000000000000000000, -1.000000000000000000, 0.000000000000000000 ) ) ;
#37680=EDGE_CURVE ( 'NONE', #21370, #19900, #39055, .T. ) ;
#37681=CARTESIAN_POINT ( 'NONE',  ( 56.67234887970509760, -45.11618894467940066, -15.60614885759789949 ) ) ;
#37683=B_SPLINE_SURFACE_WITH_KNOTS ( 'NONE', 3, 3, ( 
 ( #48925, #5157, #44713, #20585, #40523, #8563, #9078, #1210 ),
 ( #5408, #1469, #36845, #17203, #8820, #49185, #41041, #32371 ),
 ( #13278, #12756, #21366, #29232, #24771, #45239, #951, #49439 ),
 ( #40780, #9349, #37370, #683, #25294, #41299, #24504, #36579 ),
 ( #32891, #13023, #17458, #33423, #13537, #45500, #40271, #4359 ),
 ( #429, #16414, #14558, #14299, #30526, #46550, #6445, #42344 ),
 ( #42608, #41555, #34190, #18485, #26591, #10637, #21619, #45760 ),
 ( #5920, #6704, #46024, #10114, #18739, #26074, #22402, #1987 ),
 ( #25552, #22661, #21886, #50207, #38682, #2768, #37623, #30781 ),
 ( #38409, #34717, #50467, #49952, #2505, #50720, #14819, #9598 ),
 ( #2248, #1729, #14041, #30001, #33935, #42081, #34460, #5672 ) ),
 .UNSPECIFIED., .F., .F., .F.,
 ( 4, 1, 1, 1, 1, 1, 1, 1, 4 ),
 ( 4, 2, 2, 4 ),
 ( -5.055087509999999899E-06, 0.1250000000000000000, 0.2500000000000000000, 0.3750000000000000000, 0.5000000000000000000, 0.6250000000000000000, 0.7500000000000000000, 0.8750000000000000000, 1.000052120045700210 ),
 ( -5.212004572900000261E-05, 0.2077504819954940074, 0.4451796042760580163, 0.5134866592470029856 ),
 .UNSPECIFIED. ) ;
#37685=EDGE_LOOP ( 'NONE', ( #2271, #6183, #15904, #5204, #27062, #12059, #42940, #2301, #21248, #39572 ) ) ;
#37686=ORIENTED_EDGE ( 'NONE', *, *, #19775, .F. ) ;
#37687=CARTESIAN_POINT ( 'NONE',  ( 11.57186432615189986, -64.94495217133389531, -16.50172565924879819 ) ) ;
#37688=CARTESIAN_POINT ( 'NONE',  ( 11.92298585889120055, 33.98754786523329585, -46.74540749962589814 ) ) ;
#37695=CARTESIAN_POINT ( 'NONE',  ( 53.02924607949410074, -49.59742459721449848, -49.05876173540320195 ) ) ;
#37696=CARTESIAN_POINT ( 'NONE',  ( 47.18316543498789883, 23.57499020383020039, -54.61069134556619531 ) ) ;
#37697=CARTESIAN_POINT ( 'NONE',  ( 61.51944663974359884, -1.517445158300650077, -16.03079937703390101 ) ) ;
#37699=CARTESIAN_POINT ( 'NONE',  ( 51.07962911547610219, -49.63241203261180345, -76.32455169559919739 ) ) ;
#37700=AXIS2_PLACEMENT_3D ( 'NONE', #40298, #711, #40809 ) ;
#37701=CARTESIAN_POINT ( 'NONE',  ( 60.69770888843060419, -45.49484844471260203, -47.37007937758740184 ) ) ;
#37704=CARTESIAN_POINT ( 'NONE',  ( 69.22748654599821805, 19.47158195952120963, -71.50000000000200373 ) ) ;
#37705=ORIENTED_EDGE ( 'NONE', *, *, #45992, .T. ) ;
#37709=CARTESIAN_POINT ( 'NONE',  ( 14.26103652196149874, -51.11779225937510063, -22.45545332540699945 ) ) ;
#37710=CARTESIAN_POINT ( 'NONE',  ( 54.43019278679749817, 19.49833644664489896, -76.17363668804328825 ) ) ;
#37711=CARTESIAN_POINT ( 'NONE',  ( 47.52149247108939534, -54.49734860518730528, -74.72520730820750146 ) ) ;
#37713=CIRCLE ( 'NONE', #18441, 1.000000000000000000 ) ;
#37714=CARTESIAN_POINT ( 'NONE',  ( 55.42572184083550013, 14.71981156885540187, -16.50084453451690081 ) ) ;
#37715=CARTESIAN_POINT ( 'NONE',  ( 10.77457706359389888, 32.17075419748780263, -45.20848294960729419 ) ) ;
#37716=CARTESIAN_POINT ( 'NONE',  ( 57.07894516969589915, -50.21246463426640361, -52.67137581470450414 ) ) ;
#37718=CARTESIAN_POINT ( 'NONE',  ( 52.84289957970359808, -49.69201392618609958, -48.97083559310770084 ) ) ;
#37719=EDGE_CURVE ( 'NONE', #1476, #9581, #9116, .T. ) ;
#37724=CARTESIAN_POINT ( 'NONE',  ( 47.55560966394020284, 23.31156186583769951, -74.50254675453470554 ) ) ;
#37725=CARTESIAN_POINT ( 'NONE',  ( 19.90605753960891633, -54.76250717792285627, -18.14605458641800695 ) ) ;
#37726=CARTESIAN_POINT ( 'NONE',  ( 60.89859637212024523, -45.70159618970223647, -47.74371479433301602 ) ) ;
#37730=CARTESIAN_POINT ( 'NONE',  ( 60.23130391297029718, 14.55066440145539985, -47.24246919202519734 ) ) ;
#37732=LINE ( 'NONE', #17808, #24073 ) ;
#37734=CARTESIAN_POINT ( 'NONE',  ( 61.28610485260839624, 13.99802463568589950, -46.40240378558789303 ) ) ;
#37735=DIRECTION ( 'NONE',  ( -0.6653150774959307734, 0.7465626883635316791, 0.000000000000000000 ) ) ;
#37736=CARTESIAN_POINT ( 'NONE',  ( -26.59371227466860077, 10.28970141081249778, -54.97277084359720334 ) ) ;
#37738=EDGE_CURVE ( 'NONE', #16879, #18612, #33362, .T. ) ;
#37739=CARTESIAN_POINT ( 'NONE',  ( 52.95762509366560522, -49.59632487776790555, -48.83320048153250070 ) ) ;
#37743=CARTESIAN_POINT ( 'NONE',  ( 57.47357173634619443, 14.06667768184960110, -25.92429215579529966 ) ) ;
#37746=CARTESIAN_POINT ( 'NONE',  ( 53.53746104739140321, 18.13863166559730189, -49.11443482728900278 ) ) ;
#37747=EDGE_CURVE ( 'NONE', #48296, #121, #28924, .T. ) ;
#37749=CARTESIAN_POINT ( 'NONE',  ( 60.63856430484059956, -45.56966716085530322, -47.11562948342380253 ) ) ;
#37750=CARTESIAN_POINT ( 'NONE',  ( 16.32627796171218293, 19.85723994308319362, -15.67246579343190405 ) ) ;
#37754=CARTESIAN_POINT ( 'NONE',  ( 47.45327857978769970, -54.61763921174910053, -54.72404006642570096 ) ) ;
#37759=CARTESIAN_POINT ( 'NONE',  ( 10.72320681400480069, -64.90816318788569106, -17.84617904804760258 ) ) ;
#37763=AXIS2_PLACEMENT_3D ( 'NONE', #12697, #4821, #28651 ) ;
#37767=ORIENTED_EDGE ( 'NONE', *, *, #4649, .T. ) ;
#37769=CARTESIAN_POINT ( 'NONE',  ( 8.978915886419921222, -63.28580153388660534, -46.63388789120410394 ) ) ;
#37771=ORIENTED_EDGE ( 'NONE', *, *, #42141, .T. ) ;
#37775=CARTESIAN_POINT ( 'NONE',  ( 51.61768760743510143, 19.12657443447390193, -76.35064948391979556 ) ) ;
#37776=B_SPLINE_CURVE_WITH_KNOTS ( 'NONE', 3,
 ( #40294, #12783, #36603, #15675 ),
 .UNSPECIFIED., .F., .F.,
 ( 4, 4 ),
 ( 0.000000000000000000, 1.000000000000000000 ),
 .UNSPECIFIED. ) ;
#37777=ORIENTED_EDGE ( 'NONE', *, *, #37747, .F. ) ;
#37778=CARTESIAN_POINT ( 'NONE',  ( 8.784728771177240603, -63.11543068614769680, -46.67204636144870022 ) ) ;
#37784=ORIENTED_EDGE ( 'NONE', *, *, #8054, .F. ) ;
#37785=CARTESIAN_POINT ( 'NONE',  ( 18.54731091585823677, 20.81200738380825399, -75.33783710306417447 ) ) ;
#37787=CARTESIAN_POINT ( 'NONE',  ( 52.74562315164479998, -49.73950520563579403, -48.86764759941510050 ) ) ;
#37790=CARTESIAN_POINT ( 'NONE',  ( 13.72054943061259991, 20.81202934652590031, -75.33782839756391070 ) ) ;
#37791=ADVANCED_FACE ( 'NONE', ( #16710 ), #45016, .T. ) ;
#37792=FACE_OUTER_BOUND ( 'NONE', #44971, .T. ) ;
#37794=CARTESIAN_POINT ( 'NONE',  ( 43.02887931165090407, -45.36581441162159933, -6.968331744212270529 ) ) ;
#37799=CARTESIAN_POINT ( 'NONE',  ( 52.72629826234909700, -49.69265837912299588, -27.60314321031239970 ) ) ;
#37800=CARTESIAN_POINT ( 'NONE',  ( 16.60577464339360176, -51.11619062818909498, -20.14978695510610152 ) ) ;
#37801=CARTESIAN_POINT ( 'NONE',  ( 10.55533566658999867, 33.19687060618380059, -16.53455939563230004 ) ) ;
#37802=DIRECTION ( 'NONE',  ( -0.08481436951012806535, 0.9963967697281035374, 0.000000000000000000 ) ) ;
#37806=CARTESIAN_POINT ( 'NONE',  ( -3.303846065640429597, -48.27785255937200048, -4.380151423638459995 ) ) ;
#37807=CARTESIAN_POINT ( 'NONE',  ( 47.50639103848880751, 23.34221793459570193, -54.65667269328779554 ) ) ;
#37808=CARTESIAN_POINT ( 'NONE',  ( 56.52536539877740296, -50.75180572374080157, -53.84278118897309895 ) ) ;
#37810=CARTESIAN_POINT ( 'NONE',  ( 12.86000844245529962, 19.41066285990589790, -21.34825237919379859 ) ) ;
#37811=CARTESIAN_POINT ( 'NONE',  ( 61.14309862408159546, 14.08829758490710127, -46.99564608385690434 ) ) ;
#37812=CARTESIAN_POINT ( 'NONE',  ( 11.74133914242139909, 34.13528131095510076, -17.40968318378989821 ) ) ;
#37814=CARTESIAN_POINT ( 'NONE',  ( 83.89200044194980421, 17.38381105532069881, -53.92796738110899923 ) ) ;
#37817=CARTESIAN_POINT ( 'NONE',  ( 55.20364026414679870, -48.56255352766319788, -48.76217699417520635 ) ) ;
#37819=CARTESIAN_POINT ( 'NONE',  ( 52.01880079388769929, 21.21768078984590034, -53.65151492245650644 ) ) ;
#37821=CARTESIAN_POINT ( 'NONE',  ( 11.98643060099639968, -65.41791523794120167, -17.50083490704260214 ) ) ;
#37823=ORIENTED_EDGE ( 'NONE', *, *, #16122, .F. ) ;
#37825=CARTESIAN_POINT ( 'NONE',  ( 11.10544830731869936, 31.99586678468589795, -44.25060200236470109 ) ) ;
#37826=CARTESIAN_POINT ( 'NONE',  ( 58.92073396209919878, -15.61618894467929941, -18.64999999999999858 ) ) ;
#37827=CARTESIAN_POINT ( 'NONE',  ( 66.02283960027239118, -32.66876353588650517, -18.53621209913480072 ) ) ;
#37829=ORIENTED_EDGE ( 'NONE', *, *, #41129, .T. ) ;
#37831=FACE_OUTER_BOUND ( 'NONE', #22956, .T. ) ;
#37832=CARTESIAN_POINT ( 'NONE',  ( 50.01965577494885906, -1.349691835600933087, -15.97243907347640679 ) ) ;
#37833=ORIENTED_EDGE ( 'NONE', *, *, #40095, .F. ) ;
#37834=CARTESIAN_POINT ( 'NONE',  ( 12.06186543847180026, -65.21351140459039186, -46.02873399224909434 ) ) ;
#37835=CARTESIAN_POINT ( 'NONE',  ( 57.48932555802679900, -45.43918670114770464, -26.08426967047639877 ) ) ;
#37839=ORIENTED_EDGE ( 'NONE', *, *, #1473, .F. ) ;
#37840=CIRCLE ( 'NONE', #6031, 6.049999999999999822 ) ;
#37843=CARTESIAN_POINT ( 'NONE',  ( 52.85262840411130014, -45.20798072659410138, -13.23787260301519986 ) ) ;
#37845=CARTESIAN_POINT ( 'NONE',  ( 16.48362619534700002, 19.88018432961980153, -20.43421124880899953 ) ) ;
#37847=DIRECTION ( 'NONE',  ( -0.000000000000000000, -1.000000000000000000, -0.000000000000000000 ) ) ;
#37850=CARTESIAN_POINT ( 'NONE',  ( 47.20301019691079603, -54.79104926684230037, -74.19830160072660874 ) ) ;
#37851=CARTESIAN_POINT ( 'NONE',  ( 56.54598780672240110, 13.11993018277919987, -8.486630820524080576 ) ) ;
#37852=CARTESIAN_POINT ( 'NONE',  ( 50.23538084491709554, -49.77012050973750235, -76.14999999999999147 ) ) ;
#37853=EDGE_CURVE ( 'NONE', #9596, #19643, #13568, .T. ) ;
#37854=CARTESIAN_POINT ( 'NONE',  ( 54.22654478441499748, 20.21700441338549936, -53.14607073534880044 ) ) ;
#37857=CARTESIAN_POINT ( 'NONE',  ( 61.51104789187949962, 13.91173340009640036, -28.09355830686730116 ) ) ;
#37860=DIRECTION ( 'NONE',  ( 0.000000000000000000, 0.000000000000000000, 1.000000000000000000 ) ) ;
#37866=EDGE_CURVE ( 'NONE', #17310, #24832, #14624, .T. ) ;
#37871=CARTESIAN_POINT ( 'NONE',  ( 12.69301297134110129, 19.09118037685809810, -21.19712480391079978 ) ) ;
#37873=ADVANCED_FACE ( 'NONE', ( #3254 ), #2472, .T. ) ;
#37875=CARTESIAN_POINT ( 'NONE',  ( 41.53147706019129970, -44.71252858122500129, -5.331435815133920286 ) ) ;
#37876=CARTESIAN_POINT ( 'NONE',  ( -1.365754458141149819, 11.26366790782569893, -20.15000000000000213 ) ) ;
#37877=CARTESIAN_POINT ( 'NONE',  ( 18.84530080626689852, -51.72201830638929465, -74.14993436883820266 ) ) ;
#37882=ORIENTED_EDGE ( 'NONE', *, *, #29086, .T. ) ;
#37886=FACE_OUTER_BOUND ( 'NONE', #5422, .T. ) ;
#37890=CARTESIAN_POINT ( 'NONE',  ( 44.92052329722529436, -46.01048457530889380, -8.851553140290988608 ) ) ;
#37895=CARTESIAN_POINT ( 'NONE',  ( 53.42104377997379316, -49.46540347068880550, -49.21624230352519902 ) ) ;
#37896=CARTESIAN_POINT ( 'NONE',  ( 52.56522529778620623, -49.86179102641759897, -48.47379134784809906 ) ) ;
#37897=CARTESIAN_POINT ( 'NONE',  ( 54.99091206896520134, -51.40428974184509769, -54.03945093368859887 ) ) ;
#37899=ORIENTED_EDGE ( 'NONE', *, *, #39796, .F. ) ;
#37905=CIRCLE ( 'NONE', #40433, 28.31678667024650409 ) ;
#37906=CARTESIAN_POINT ( 'NONE',  ( 53.23404681179649600, -50.62188124027260017, -76.66833019152879558 ) ) ;
#37907=CARTESIAN_POINT ( 'NONE',  ( 60.74039577305779858, 14.35309089330909949, -47.45735349090180222 ) ) ;
#37909=CYLINDRICAL_SURFACE ( 'NONE', #31345, 1.000000000000029976 ) ;
#37910=CARTESIAN_POINT ( 'NONE',  ( 41.43650635183630015, 13.58022812337069851, -5.462486971552510617 ) ) ;
#37911=ADVANCED_FACE ( 'NONE', ( #7188 ), #18713, .T. ) ;
#37912=CARTESIAN_POINT ( 'NONE',  ( 41.88234443079220171, -43.67296333914980266, -3.969549610420470387 ) ) ;
#37914=CARTESIAN_POINT ( 'NONE',  ( -7.625877374285919608, 14.22289747138790084, -5.682500641286110543 ) ) ;
#37917=CARTESIAN_POINT ( 'NONE',  ( 65.62515792676039439, 0.5188969770332930720, -17.33365040072970231 ) ) ;
#37918=ORIENTED_EDGE ( 'NONE', *, *, #22299, .T. ) ;
#37919=CARTESIAN_POINT ( 'NONE',  ( 15.05440318628160057, -53.11618894467930119, -76.14999999999999147 ) ) ;
#37921=CARTESIAN_POINT ( 'NONE',  ( 47.21101641624719747, -54.78526367574990275, -54.63499203783069902 ) ) ;
#37926=CARTESIAN_POINT ( 'NONE',  ( 48.00591971102450373, -54.35791002652510429, -54.98714547078049719 ) ) ;
#37928=CARTESIAN_POINT ( 'NONE',  ( -8.116933555512177989, -44.87420182799904467, -5.094470741909731260 ) ) ;
#37930=EDGE_CURVE ( 'NONE', #4326, #34714, #24718, .T. ) ;
#37931=CARTESIAN_POINT ( 'NONE',  ( 47.90090429088169799, 23.17274928892609864, -54.97513107683430889 ) ) ;
#37940=CARTESIAN_POINT ( 'NONE',  ( 83.91322170983950457, 13.24675980165680045, -47.13452068490819613 ) ) ;
#37941=CARTESIAN_POINT ( 'NONE',  ( 55.63848436370919615, 15.03490499964270022, -25.39977966304109813 ) ) ;
#37944=CARTESIAN_POINT ( 'NONE',  ( 56.36758570843819882, -45.11618894467940066, -15.20758541532019947 ) ) ;
#37949=ORIENTED_EDGE ( 'NONE', *, *, #1477, .T. ) ;
#37950=CARTESIAN_POINT ( 'NONE',  ( 12.00693377042660082, -64.79851766967649951, -16.09314495739829809 ) ) ;
#37952=CARTESIAN_POINT ( 'NONE',  ( -29.90025726814942431, 4.910446297966914564, -56.90830752171230245 ) ) ;
#37953=CARTESIAN_POINT ( 'NONE',  ( 50.99272666193287051, 4.001659728125646964, -76.39686140629422084 ) ) ;
#37954=ORIENTED_EDGE ( 'NONE', *, *, #42900, .F. ) ;
#37955=VERTEX_POINT ( 'NONE', #30498 ) ;
#37958=CARTESIAN_POINT ( 'NONE',  ( 52.63649943311990143, -49.80150522235119581, -48.66853994086150692 ) ) ;
#37959=CIRCLE ( 'NONE', #7883, 0.9999999999999986677 ) ;
#37960=CARTESIAN_POINT ( 'NONE',  ( 51.92180556447119955, 19.59192512143929932, -50.64576713626780702 ) ) ;
#37961=CARTESIAN_POINT ( 'NONE',  ( 63.15143557569741262, -1.746388215850740000, -16.22393059072330246 ) ) ;
#37962=CARTESIAN_POINT ( 'NONE',  ( 51.40462280232890180, -50.54840350189540032, -76.23573550552210065 ) ) ;
#37963=CARTESIAN_POINT ( 'NONE',  ( 57.50557710143229428, -49.31997340228490145, -51.53210862891840094 ) ) ;
#37969=CARTESIAN_POINT ( 'NONE',  ( 47.78347825172009777, -46.15534745134900163, -10.88057999588169977 ) ) ;
#37971=CARTESIAN_POINT ( 'NONE',  ( 13.64404399975630078, -50.99724096237619619, -21.86438480750510038 ) ) ;
#37972=CARTESIAN_POINT ( 'NONE',  ( 57.06611319472220600, 19.38619040980010055, -74.64592700447491325 ) ) ;
#37974=CARTESIAN_POINT ( 'NONE',  ( 47.57154850773469690, -54.56571258662719970, -74.17405913703889553 ) ) ;
#37976=CARTESIAN_POINT ( 'NONE',  ( 55.96166294374940264, 14.18843861383079918, -16.30655967985860144 ) ) ;
#37977=CARTESIAN_POINT ( 'NONE',  ( 9.299128317299539148, 32.06192745982850312, -46.53057822423220102 ) ) ;
#37978=AXIS2_PLACEMENT_3D ( 'NONE', #36306, #41029, #41288 ) ;
#37980=CARTESIAN_POINT ( 'NONE',  ( 56.96124597811810020, -50.60744642191669840, -53.44837636084510279 ) ) ;
#37983=CARTESIAN_POINT ( 'NONE',  ( 61.28189545210631195, 14.37036762458959238, -47.67949669966547077 ) ) ;
#37984=EDGE_CURVE ( 'NONE', #15596, #45466, #13058, .T. ) ;
#37985=CARTESIAN_POINT ( 'NONE',  ( 47.64143408597180240, 23.30250929682300409, -74.17387245455559253 ) ) ;
#37987=CARTESIAN_POINT ( 'NONE',  ( 75.47966807050509885, -43.37310274687460065, -13.40512917118210012 ) ) ;
#37989=DIRECTION ( 'NONE',  ( 1.000000000000000000, 0.000000000000000000, 0.000000000000000000 ) ) ;
#37997=CARTESIAN_POINT ( 'NONE',  ( 6.300025116805320735, 33.86872402518860525, -48.92608059699399803 ) ) ;
#37998=EDGE_LOOP ( 'NONE', ( #43851, #21065, #14287, #21841, #1869 ) ) ;
#37999=CARTESIAN_POINT ( 'NONE',  ( 53.22411023516859530, -49.46633164296870433, -48.94726693978910248 ) ) ;
#38002=DIRECTION ( 'NONE',  ( -0.2260571801428161165, 7.216449660063443557E-16, 0.9741140340359943917 ) ) ;
#38003=CARTESIAN_POINT ( 'NONE',  ( 55.95312836925540267, 14.62053896309619994, -25.39030107927520064 ) ) ;
#38005=CARTESIAN_POINT ( 'NONE',  ( 50.85760623216560106, 19.45375030590959753, -76.14999999999999147 ) ) ;
#38006=CARTESIAN_POINT ( 'NONE',  ( 52.96692102286459658, 18.37433252106210091, -48.95117868485719725 ) ) ;
#38008=CARTESIAN_POINT ( 'NONE',  ( 60.55542095703709293, -45.61322829028730297, -47.18108258831090041 ) ) ;
#38009=CARTESIAN_POINT ( 'NONE',  ( 16.26108084590278935, 19.84491886401188054, -15.67129894889461994 ) ) ;
#38013=CARTESIAN_POINT ( 'NONE',  ( 16.13393739769620083, -15.61618894467929941, -49.12910085600329779 ) ) ;
#38016=CARTESIAN_POINT ( 'NONE',  ( 56.98397975609619692, 19.46089624346329927, -53.23409293251930308 ) ) ;
#38017=CARTESIAN_POINT ( 'NONE',  ( 52.90855285609569592, 18.38725884964449975, -48.71990423803699599 ) ) ;
#38024=VERTEX_POINT ( 'NONE', #22890 ) ;
#38025=CARTESIAN_POINT ( 'NONE',  ( 8.951579501146909479, -63.12553281437028829, -46.63485218348429839 ) ) ;
#38028=ORIENTED_EDGE ( 'NONE', *, *, #38165, .F. ) ;
#38030=CARTESIAN_POINT ( 'NONE',  ( 57.04000889551539899, 19.39440449634280128, -53.73354994110280103 ) ) ;
#38032=CARTESIAN_POINT ( 'NONE',  ( 53.31396975641249725, 19.22903114769359689, -77.17790062668180440 ) ) ;
#38035=CARTESIAN_POINT ( 'NONE',  ( 16.13393739769620083, -15.61618894467929941, 5.729250452415290518 ) ) ;
#38044=EDGE_CURVE ( 'NONE', #48450, #14522, #2997, .T. ) ;
#38045=CARTESIAN_POINT ( 'NONE',  ( 88.13393739769620083, -15.61618894467929941, -65.65000000000000568 ) ) ;
#38047=CARTESIAN_POINT ( 'NONE',  ( 52.84346301666479917, -49.69122173838940881, -48.96941052353699320 ) ) ;
#38051=CARTESIAN_POINT ( 'NONE',  ( 14.34420549403320067, 19.88381105676229765, -74.14994299942661371 ) ) ;
#38052=DIRECTION ( 'NONE',  ( 1.000000000000000000, 0.000000000000000000, 0.000000000000000000 ) ) ;
#38053=CARTESIAN_POINT ( 'NONE',  ( 41.00663092279180688, -45.00381178176490238, -5.555598286907029504 ) ) ;
#38056=ORIENTED_EDGE ( 'NONE', *, *, #3385, .F. ) ;
#38057=CARTESIAN_POINT ( 'NONE',  ( 53.19504529726539488, -49.21163053193929926, -27.08660439529860042 ) ) ;
#38058=CARTESIAN_POINT ( 'NONE',  ( 53.90939472220419759, -50.74970086946049719, -76.32822664810839797 ) ) ;
#38059=CARTESIAN_POINT ( 'NONE',  ( 2.774641425251900273, 25.39332573679260108, -11.69510809164579968 ) ) ;
#38061=CARTESIAN_POINT ( 'NONE',  ( 8.133937397696209715, 31.88305279702909800, -43.74348518090240390 ) ) ;
#38064=CARTESIAN_POINT ( 'NONE',  ( -3.974232546700849689, -47.86947640837310303, -4.409288521898479196 ) ) ;
#38065=CARTESIAN_POINT ( 'NONE',  ( 47.56368033297190578, 23.31135455392519873, -54.70077872531200569 ) ) ;
#38066=CARTESIAN_POINT ( 'NONE',  ( 17.92370450342619748, 19.88381105532299742, -15.67980087199299888 ) ) ;
#38068=CARTESIAN_POINT ( 'NONE',  ( 61.04011654556379796, 14.12690480185519881, -46.86308378909100014 ) ) ;
#38069=CARTESIAN_POINT ( 'NONE',  ( 11.57222021527569922, 33.85198765799319887, -16.73996640652449841 ) ) ;
#38070=CARTESIAN_POINT ( 'NONE',  ( 51.62358001281780417, 17.38380888595600027, -76.93789421597429623 ) ) ;
#38071=CARTESIAN_POINT ( 'NONE',  ( 53.39111139338680090, 18.13443291158960236, -48.76214190021520523 ) ) ;
#38072=CARTESIAN_POINT ( 'NONE',  ( 19.53299984191638927, 24.23912880602019726, -75.56421462368636810 ) ) ;
#38073=CARTESIAN_POINT ( 'NONE',  ( 57.08416941684100010, -47.57703361919330121, -48.31006120114819424 ) ) ;
#38074=CARTESIAN_POINT ( 'NONE',  ( 54.06609827824310344, 17.30031468964149965, -26.91176089519509773 ) ) ;
#38075=CARTESIAN_POINT ( 'NONE',  ( 56.10252019742019769, 19.69840917465210239, -53.89291062504800323 ) ) ;
#38077=DIRECTION ( 'NONE',  ( 0.6911981449639433839, -0.7226652920947592706, -1.665334536937735550E-16 ) ) ;
#38079=CARTESIAN_POINT ( 'NONE',  ( 19.21228758657862912, 21.54155451009319933, -16.16996892446439205 ) ) ;
#38080=CARTESIAN_POINT ( 'NONE',  ( 11.10535879386450198, 31.92573324508259702, -44.25018954536789551 ) ) ;
#38083=CARTESIAN_POINT ( 'NONE',  ( 66.48974184299869705, -31.33002686145149696, -17.32440450352510197 ) ) ;
#38087=ORIENTED_EDGE ( 'NONE', *, *, #24917, .F. ) ;
#38089=CARTESIAN_POINT ( 'NONE',  ( 76.49475450406279720, -3.230546176492170130, -13.20481461287775460 ) ) ;
#38091=CARTESIAN_POINT ( 'NONE',  ( 12.88931624166749934, -65.50825287758750903, -47.54166358398200032 ) ) ;
#38092=CARTESIAN_POINT ( 'NONE',  ( 57.05606732091469979, -45.81799886118620435, -26.22800298916919814 ) ) ;
#38093=DIRECTION ( 'NONE',  ( 0.000000000000000000, -1.000000000000000000, 0.000000000000000000 ) ) ;
#38094=ADVANCED_FACE ( 'NONE', ( #32282 ), #15132, .T. ) ;
#38098=DIRECTION ( 'NONE',  ( -1.000000000000000000, 0.000000000000000000, 0.000000000000000000 ) ) ;
#38100=AXIS2_PLACEMENT_3D ( 'NONE', #2628, #50327, #18600 ) ;
#38102=ORIENTED_EDGE ( 'NONE', *, *, #874, .F. ) ;
#38103=CARTESIAN_POINT ( 'NONE',  ( 54.53726787685040023, -46.02702818155930231, -15.67786106914689803 ) ) ;
#38105=CARTESIAN_POINT ( 'NONE',  ( 14.72196958650020093, 19.87258839401659927, -22.05098504493599876 ) ) ;
#38106=DIRECTION ( 'NONE',  ( -0.8732394366197193669, -0.4872913772396092469, 0.000000000000000000 ) ) ;
#38107=CARTESIAN_POINT ( 'NONE',  ( 66.70013194292150160, -1.463538230407920082, -17.02746303015019791 ) ) ;
#38108=CARTESIAN_POINT ( 'NONE',  ( 47.18324198357279897, -54.80726809202429450, -74.14999999999999147 ) ) ;
#38109=CARTESIAN_POINT ( 'NONE',  ( 41.51080288407340646, 13.17508010173299837, -4.911631759730330060 ) ) ;
#38111=CARTESIAN_POINT ( 'NONE',  ( 7.853097003783780394, -60.52042854835909935, -20.86915960608759946 ) ) ;
#38114=CARTESIAN_POINT ( 'NONE',  ( 53.43416147895619872, 19.95816927601739721, -75.78314185115898738 ) ) ;
#38115=CARTESIAN_POINT ( 'NONE',  ( 59.18929318893719937, 14.08236763960739957, -26.39549450433730371 ) ) ;
#38120=AXIS2_PLACEMENT_3D ( 'NONE', #23139, #7439, #11896 ) ;
#38121=CARTESIAN_POINT ( 'NONE',  ( -3.382504787385450129, -49.25282957014520235, -5.960458118589759380 ) ) ;
#38122=DIRECTION ( 'NONE',  ( 0.000000000000000000, 0.000000000000000000, 1.000000000000000000 ) ) ;
#38124=CARTESIAN_POINT ( 'NONE',  ( 61.14249685063511208, -45.50505420239858978, -47.52526588987043255 ) ) ;
#38127=CARTESIAN_POINT ( 'NONE',  ( 40.87221884731469856, 13.29834217954369890, -4.420649500702079848 ) ) ;
#38131=CARTESIAN_POINT ( 'NONE',  ( 8.784728771152170879, -54.93525725209899235, -46.67204636145419983 ) ) ;
#38138=CARTESIAN_POINT ( 'NONE',  ( 60.91959772890210445, -45.69583638042100660, -47.74153617882520706 ) ) ;
#38145=CARTESIAN_POINT ( 'NONE',  ( 52.10267382257649871, -33.11618894464340457, -77.60820171200670359 ) ) ;
#38152=EDGE_CURVE ( 'NONE', #45666, #8993, #12130, .T. ) ;
#38153=DIRECTION ( 'NONE',  ( 1.000000000000000000, 0.000000000000000000, 0.000000000000000000 ) ) ;
#38154=ORIENTED_EDGE ( 'NONE', *, *, #27139, .F. ) ;
#38159=ORIENTED_EDGE ( 'NONE', *, *, #13028, .F. ) ;
#38161=CARTESIAN_POINT ( 'NONE',  ( 52.63691518385540036, -50.41536572445579623, -76.75103203777939598 ) ) ;
#38162=CARTESIAN_POINT ( 'NONE',  ( 60.90589200473370113, 14.20139306651049971, -47.09719146388230371 ) ) ;
#38163=VECTOR ( 'NONE', #29294, 1000.000000000000000 ) ;
#38165=EDGE_CURVE ( 'NONE', #10985, #12115, #26764, .T. ) ;
#38166=AXIS2_PLACEMENT_3D ( 'NONE', #13953, #14981, #10283 ) ;
#38168=CARTESIAN_POINT ( 'NONE',  ( 45.18671004937630187, 13.88808930430720068, -7.327102700430730309 ) ) ;
#38170=CARTESIAN_POINT ( 'NONE',  ( 42.65512910181180217, -42.85913616512119972, -3.541891443463950129 ) ) ;
#38172=CARTESIAN_POINT ( 'NONE',  ( 29.52882095054619782, 20.46959749294990161, -75.56421356237308373 ) ) ;
#38180=CARTESIAN_POINT ( 'NONE',  ( 47.18324198357289845, -54.80726809202429450, -54.61058319554170026 ) ) ;
#38185=CARTESIAN_POINT ( 'NONE',  ( 48.01492169973680291, -54.34163064677210286, -54.91800274540270266 ) ) ;
#38188=CARTESIAN_POINT ( 'NONE',  ( -10.44076364992884187, -42.78597905896825182, -5.977015743028451844 ) ) ;
#38189=CARTESIAN_POINT ( 'NONE',  ( 47.98988913041800686, 23.14896199218459927, -55.12692082525529713 ) ) ;
#38192=ORIENTED_EDGE ( 'NONE', *, *, #50275, .T. ) ;
#38194=CARTESIAN_POINT ( 'NONE',  ( 53.59003930803689997, -49.40628012469949937, -49.22510501142529904 ) ) ;
#38195=DIRECTION ( 'NONE',  ( 1.000000000000000000, 0.000000000000000000, 0.000000000000000000 ) ) ;
#38196=CARTESIAN_POINT ( 'NONE',  ( 14.70129771474999103, 19.30056145025122660, -20.74427287069836723 ) ) ;
#38197=CARTESIAN_POINT ( 'NONE',  ( 84.27240597999899308, 12.65244516160949928, -47.25334685439979410 ) ) ;
#38198=CARTESIAN_POINT ( 'NONE',  ( 55.06229968142930176, 15.76352112526989835, -25.67610890140170454 ) ) ;
#38202=CARTESIAN_POINT ( 'NONE',  ( 55.95579871441826469, -45.88748562638757988, -25.57470094210382427 ) ) ;
#38203=ORIENTED_EDGE ( 'NONE', *, *, #21166, .T. ) ;
#38204=CARTESIAN_POINT ( 'NONE',  ( 51.81838445030630425, -33.69149598205980567, -77.22003196546970116 ) ) ;
#38206=ADVANCED_FACE ( 'NONE', ( #18653 ), #23059, .T. ) ;
#38207=EDGE_LOOP ( 'NONE', ( #47885, #31651, #13534, #36711, #46346 ) ) ;
#38208=CARTESIAN_POINT ( 'NONE',  ( 12.36320305068320025, -64.54682834576858852, -15.76422791927960176 ) ) ;
#38211=CARTESIAN_POINT ( 'NONE',  ( 50.96898030287184156, 4.043820165196742700, -76.38408506549473032 ) ) ;
#38213=ORIENTED_EDGE ( 'NONE', *, *, #11675, .F. ) ;
#38215=B_SPLINE_CURVE_WITH_KNOTS ( 'NONE', 3,
 ( #47281, #47027, #35722, #35969, #38897, #3508, #27845, #27335 ),
 .UNSPECIFIED., .F., .F.,
 ( 4, 2, 2, 4 ),
 ( 0.000000000000000000, 0.2515559781046747823, 0.3773339671570129505, 0.5031119562093512299 ),
 .UNSPECIFIED. ) ;
#38218=CARTESIAN_POINT ( 'NONE',  ( 64.45807172334708923, -1.442643869120930011, -16.41040740274739917 ) ) ;
#38220=CARTESIAN_POINT ( 'NONE',  ( 51.18091049923690150, -50.74726768130989996, -76.16568857009508520 ) ) ;
#38221=CARTESIAN_POINT ( 'NONE',  ( 58.58470796083329191, -48.16305383058679723, -50.30464788415889643 ) ) ;
#38222=B_SPLINE_CURVE_WITH_KNOTS ( 'NONE', 3,
 ( #49626, #4808, #45683, #21553, #37821, #17646, #33612, #1914, #40711, #46475, #10818, #50130, #10036, #14226, #50904, #26263, #18667, #43051 ),
 .UNSPECIFIED., .F., .F.,
 ( 4, 2, 2, 2, 2, 2, 2, 2, 4 ),
 ( 0.000000000000000000, 0.03292124886954176516, 0.2434314436876863774, 0.3750003154490272328, 0.5000002523592219639, 0.5625002208143193849, 0.6625001703424752142, 0.8225000895875238527, 1.000000000000000000 ),
 .UNSPECIFIED. ) ;
#38224=CARTESIAN_POINT ( 'NONE',  ( 72.38393739883420608, 11.88381105532070414, -61.44999999999999574 ) ) ;
#38225=CARTESIAN_POINT ( 'NONE',  ( 65.43042069958036677, 17.98087126525108914, -68.79648330188406646 ) ) ;
#38226=ORIENTED_EDGE ( 'NONE', *, *, #43795, .F. ) ;
#38227=CARTESIAN_POINT ( 'NONE',  ( 53.70552627772385534, -51.31509389902640095, -75.56421117895261830 ) ) ;
#38228=CARTESIAN_POINT ( 'NONE',  ( 48.26658354477700641, -45.11618894467940066, -9.084211283567670492 ) ) ;
#38230=CARTESIAN_POINT ( 'NONE',  ( 13.09773310522899870, -50.91350717092480238, -21.58185367788340159 ) ) ;
#38232=CARTESIAN_POINT ( 'NONE',  ( 54.08446768638849989, 19.51091414381249578, -76.27847822918199938 ) ) ;
#38233=EDGE_CURVE ( 'NONE', #33614, #25343, #47572, .T. ) ;
#38234=CARTESIAN_POINT ( 'NONE',  ( 47.27618702399809791, -54.10032693455720221, -75.52157719890121257 ) ) ;
#38235=CARTESIAN_POINT ( 'NONE',  ( 55.91593866523759715, 14.67229690674569831, -17.93020249829309876 ) ) ;
#38237=CARTESIAN_POINT ( 'NONE',  ( 56.53399784783299964, -50.44739419118339896, -52.81205167950179913 ) ) ;
#38240=ORIENTED_EDGE ( 'NONE', *, *, #21437, .T. ) ;
#38241=CARTESIAN_POINT ( 'NONE',  ( 46.35275103504439898, 21.67755452994670406, -76.14999999999999147 ) ) ;
#38245=DIRECTION ( 'NONE',  ( 0.000000000000000000, -0.7371541403039566509, 0.6757246284047478957 ) ) ;
#38246=CIRCLE ( 'NONE', #9790, 17.70000000000000284 ) ;
#38247=CARTESIAN_POINT ( 'NONE',  ( 16.13393739769309931, -15.61618894467859953, -3.187564294432039702 ) ) ;
#38248=CARTESIAN_POINT ( 'NONE',  ( 82.55668469584230706, 14.40343100263957865, -47.71685812434790108 ) ) ;
#38250=CARTESIAN_POINT ( 'NONE',  ( 8.133937397696215044, 28.62669279778661036, -21.14999999999999858 ) ) ;
#38254=CARTESIAN_POINT ( 'NONE',  ( -32.24202920327260102, -6.110563815214810290, -55.86711240520629929 ) ) ;
#38256=CARTESIAN_POINT ( 'NONE',  ( 53.14225961112249763, -49.51472671965699845, -48.98057208336989987 ) ) ;
#38260=CARTESIAN_POINT ( 'NONE',  ( 14.01770721255530106, 19.93736976191020105, -22.72048054942820272 ) ) ;
#38261=CARTESIAN_POINT ( 'NONE',  ( 55.85837259913330399, 14.77764870892549887, -25.54560217317060022 ) ) ;
#38263=CYLINDRICAL_SURFACE ( 'NONE', #14870, 0.9999999999999976685 ) ;
#38264=CARTESIAN_POINT ( 'NONE',  ( 53.03054970849530037, 18.35345454141090116, -49.02174585020699737 ) ) ;
#38265=CARTESIAN_POINT ( 'NONE',  ( 55.81704914353240099, -45.86755745118960448, -17.13878629476699800 ) ) ;
#38274=CARTESIAN_POINT ( 'NONE',  ( 11.93174526809839975, -65.43929183185349530, -17.93019253464870033 ) ) ;
#38275=B_SPLINE_CURVE_WITH_KNOTS ( 'NONE', 3,
 ( #5595, #21811, #29158, #17126, #29923 ),
 .UNSPECIFIED., .F., .F.,
 ( 4, 1, 4 ),
 ( 0.5000152864445784884, 0.6666870483743799758, 1.000000000000000000 ),
 .UNSPECIFIED. ) ;
#38276=CARTESIAN_POINT ( 'NONE',  ( 52.74562315164475734, -49.73950520563583666, -48.86764759941514313 ) ) ;
#38278=CYLINDRICAL_SURFACE ( 'NONE', #41719, 1.999999999999995115 ) ;
#38284=CARTESIAN_POINT ( 'NONE',  ( 10.76970654631240087, -63.14946393425128690, -45.20602416875770047 ) ) ;
#38288=CARTESIAN_POINT ( 'NONE',  ( 56.94695452114130063, 19.24930104416129950, -53.05466020597059895 ) ) ;
#38289=CARTESIAN_POINT ( 'NONE',  ( 52.84793103446079954, 19.11984488519809844, -76.98160984307151011 ) ) ;
#38301=CARTESIAN_POINT ( 'NONE',  ( 56.68830530524120093, -46.09563615325990327, -26.25268044571639692 ) ) ;
#38305=CARTESIAN_POINT ( 'NONE',  ( 13.44492653017840134, 20.50885532556510071, -74.53071772762450564 ) ) ;
#38306=DIRECTION ( 'NONE',  ( 0.000000000000000000, 0.7371541402007432131, -0.6757246285173443834 ) ) ;
#38307=CARTESIAN_POINT ( 'NONE',  ( 41.11636499574930070, -44.91157709887249894, -5.497152887732390525 ) ) ;
#38308=PLANE ( 'NONE',  #9736 ) ;
#38309=EDGE_CURVE ( 'NONE', #7609, #32627, #44401, .T. ) ;
#38312=CARTESIAN_POINT ( 'NONE',  ( 55.92359621412080628, -45.89461707380959865, -25.40852082268940038 ) ) ;
#38314=CARTESIAN_POINT ( 'NONE',  ( 56.61426160987299738, -50.70378515394530439, -74.49626132433751025 ) ) ;
#38315=CARTESIAN_POINT ( 'NONE',  ( 65.03253056770502383, 12.18167892300241206, -10.43310554112815325 ) ) ;
#38317=CARTESIAN_POINT ( 'NONE',  ( 47.46364465723310389, -54.60385569402070161, -54.65913311076389647 ) ) ;
#38321=CARTESIAN_POINT ( 'NONE',  ( 47.43221812499459844, 23.40624208892269920, -54.88095735414919574 ) ) ;
#38324=CARTESIAN_POINT ( 'NONE',  ( 60.76016881783269952, 14.27357726001389970, -47.06493626314229317 ) ) ;
#38325=CARTESIAN_POINT ( 'NONE',  ( 11.85902006005049891, 33.93748487951390302, -16.73665430628790318 ) ) ;
#38327=CARTESIAN_POINT ( 'NONE',  ( 53.01963653383530328, 18.32905899852440257, -48.79855609391960058 ) ) ;
#38329=CARTESIAN_POINT ( 'NONE',  ( 57.59186919487559919, -47.31111691810159670, -48.20254613966260138 ) ) ;
#38330=CARTESIAN_POINT ( 'NONE',  ( 53.79192597912830109, 17.55350234038469992, -27.04907804900940249 ) ) ;
#38332=CARTESIAN_POINT ( 'NONE',  ( 51.58686502407429941, 21.60049488496320080, -54.30991078205589417 ) ) ;
#38334=CARTESIAN_POINT ( 'NONE',  ( 52.90434486281380799, 18.43107897257790029, -49.01850765170799917 ) ) ;
#38335=DIRECTION ( 'NONE',  ( 0.9146474252872274224, -0.000000000000000000, 0.4042525045258791860 ) ) ;
#38336=CARTESIAN_POINT ( 'NONE',  ( 19.80165575756416985, 23.23087915573190543, -17.67623750364432311 ) ) ;
#38337=CARTESIAN_POINT ( 'NONE',  ( 10.49236770985929823, 32.06433946733989870, -45.62571961304500689 ) ) ;
#38339=DIRECTION ( 'NONE',  ( -0.3294064756442134922, -0.9441882088882800339, 8.551492847173810438E-14 ) ) ;
#38341=EDGE_LOOP ( 'NONE', ( #25951, #23108, #4563, #31290, #49123 ) ) ;
#38346=CARTESIAN_POINT ( 'NONE',  ( 76.49467596410896419, -3.235303301204498272, -13.20447617252744621 ) ) ;
#38347=ORIENTED_EDGE ( 'NONE', *, *, #39474, .T. ) ;
#38348=CARTESIAN_POINT ( 'NONE',  ( 11.04919440717550039, -64.12845758586969680, -45.19200995724910541 ) ) ;
#38349=CARTESIAN_POINT ( 'NONE',  ( 56.76310125540409501, -45.25731884260100202, -25.36477901628050091 ) ) ;
#38352=EDGE_LOOP ( 'NONE', ( #24556, #12451, #47343, #33812 ) ) ;
#38356=ORIENTED_EDGE ( 'NONE', *, *, #35559, .F. ) ;
#38359=CARTESIAN_POINT ( 'NONE',  ( 16.62868081655389929, 19.88381105408159755, -20.46561682067460097 ) ) ;
#38361=EDGE_CURVE ( 'NONE', #30947, #29939, #25237, .T. ) ;
#38363=DIRECTION ( 'NONE',  ( 0.3805321250008310008, 0.000000000000000000, -0.9247677015566404535 ) ) ;
#38364=CARTESIAN_POINT ( 'NONE',  ( 47.22839619843820458, -54.42900472606909545, -75.17099345517469544 ) ) ;
#38365=CARTESIAN_POINT ( 'NONE',  ( 60.78498736401110136, 13.10757611403960077, -9.606534188251758977 ) ) ;
#38369=CARTESIAN_POINT ( 'NONE',  ( 52.25623527804339830, 20.09621345565349770, -75.95837141101100087 ) ) ;
#38370=CARTESIAN_POINT ( 'NONE',  ( 57.24929578595760660, -52.61618894467940066, -63.99406948319280275 ) ) ;
#38376=CARTESIAN_POINT ( 'NONE',  ( 9.595232318844979957, -63.69675525222269385, -16.46787902471350051 ) ) ;
#38377=CARTESIAN_POINT ( 'NONE',  ( 76.21567127096270156, -5.958767942511509652, -12.35740042236670000 ) ) ;
#38378=CARTESIAN_POINT ( 'NONE',  ( 75.12459293833639151, 13.75682883240243370, -14.63710905661170081 ) ) ;
#38380=CARTESIAN_POINT ( 'NONE',  ( 12.81875897587595503, -55.47848908301230608, -75.64152464218183525 ) ) ;
#38382=CARTESIAN_POINT ( 'NONE',  ( 61.75019796695539753, -45.11618894467940066, -28.15000000000000213 ) ) ;
#38384=CARTESIAN_POINT ( 'NONE',  ( 40.75026669549949787, 13.34597472761970138, -4.220911263362750354 ) ) ;
#38386=CARTESIAN_POINT ( 'NONE',  ( 7.492845759203685674, -61.18022026567161475, -20.13893727953967172 ) ) ;
#38387=CARTESIAN_POINT ( 'NONE',  ( 66.23540447448809232, -49.95860450174330225, -73.25000000000169109 ) ) ;
#38388=CARTESIAN_POINT ( 'NONE',  ( 76.39354817796227337, -43.26297082301523034, -13.95540116459575586 ) ) ;
#38395=CARTESIAN_POINT ( 'NONE',  ( 10.61754762155600140, 33.59328422689429772, -18.17417937929459981 ) ) ;
#38396=CARTESIAN_POINT ( 'NONE',  ( 60.97391253512209630, -45.68106840025299675, -47.73524043326649746 ) ) ;
#38402=CARTESIAN_POINT ( 'NONE',  ( 4.403190979259558269, -24.13907510292004233, -6.928362978644219794 ) ) ;
#38403=CARTESIAN_POINT ( 'NONE',  ( 60.60294763170050203, -45.58832773382454207, -47.14361286069857471 ) ) ;
#38408=CARTESIAN_POINT ( 'NONE',  ( 18.86789271228509790, -51.78678246903520233, -76.14999999999999147 ) ) ;
#38409=CARTESIAN_POINT ( 'NONE',  ( 61.30390548032649889, -45.22107570635780860, -46.37197824241119548 ) ) ;
#38411=ORIENTED_EDGE ( 'NONE', *, *, #21980, .T. ) ;
#38416=B_SPLINE_CURVE_WITH_KNOTS ( 'NONE', 3,
 ( #31629, #43711, #200, #19851, #11754 ),
 .UNSPECIFIED., .F., .F.,
 ( 4, 1, 4 ),
 ( 0.000000000000000000, 0.3333267645415212144, 0.4999950733969018013 ),
 .UNSPECIFIED. ) ;
#38418=CARTESIAN_POINT ( 'NONE',  ( 52.19402250454749748, -50.90613807397439672, -76.20338398719890449 ) ) ;
#38419=CARTESIAN_POINT ( 'NONE',  ( 60.31836632494100314, 14.50504996450150053, -47.25075699645550742 ) ) ;
#38422=CARTESIAN_POINT ( 'NONE',  ( 40.91145569068659427, 13.87671759085050027, -5.616194440429819856 ) ) ;
#38423=CARTESIAN_POINT ( 'NONE',  ( 42.80229243920160087, -42.71639462152419497, -3.540423289868949830 ) ) ;
#38425=FACE_OUTER_BOUND ( 'NONE', #37998, .T. ) ;
#38430=SPHERICAL_SURFACE ( 'NONE', #29244, 2.000000000000000000 ) ;
#38435=CARTESIAN_POINT ( 'NONE',  ( 43.50059062573970436, 14.79387737681599901, -7.939643042942710061 ) ) ;
#38437=EDGE_CURVE ( 'NONE', #17140, #41357, #43322, .T. ) ;
#38439=DIRECTION ( 'NONE',  ( 0.6911981449639439390, -0.7226652920947588266, 0.000000000000000000 ) ) ;
#38442=CARTESIAN_POINT ( 'NONE',  ( 47.82694498829380336, -54.45586656085379929, -55.20630169768750051 ) ) ;
#38444=DIRECTION ( 'NONE',  ( -1.000000000000000000, 0.000000000000000000, 0.000000000000000000 ) ) ;
#38445=CARTESIAN_POINT ( 'NONE',  ( 48.05894033739649984, 23.11179829524310136, -55.06192549311779771 ) ) ;
#38450=CARTESIAN_POINT ( 'NONE',  ( 82.54525856212266888, 13.91914240249079171, -46.85691352100786844 ) ) ;
#38451=FACE_OUTER_BOUND ( 'NONE', #45006, .T. ) ;
#38452=DIRECTION ( 'NONE',  ( 1.000000000000000000, 0.000000000000000000, 0.000000000000000000 ) ) ;
#38453=CARTESIAN_POINT ( 'NONE',  ( 60.14258128935630054, 13.88381105532070059, -25.78020575349050958 ) ) ;
#38454=CARTESIAN_POINT ( 'NONE',  ( 55.89496596761120628, 14.69986299189930001, -25.41538446139790253 ) ) ;
#38460=VERTEX_POINT ( 'NONE', #24843 ) ;
#38464=VERTEX_POINT ( 'NONE', #45306 ) ;
#38465=CARTESIAN_POINT ( 'NONE',  ( 12.05049839502609998, -64.90519735259998413, -16.21910226669200128 ) ) ;
#38468=DIRECTION ( 'NONE',  ( 1.000000000000000000, 0.000000000000000000, 0.000000000000000000 ) ) ;
#38469=AXIS2_PLACEMENT_3D ( 'NONE', #12589, #40104, #40877 ) ;
#38471=CIRCLE ( 'NONE', #16692, 4.000000000000058620 ) ;
#38473=ORIENTED_EDGE ( 'NONE', *, *, #50529, .F. ) ;
#38476=AXIS2_PLACEMENT_3D ( 'NONE', #37356, #40510, #24757 ) ;
#38477=CARTESIAN_POINT ( 'NONE',  ( 53.55414459173979935, 18.14307244785399931, -49.14835486563159606 ) ) ;
#38478=CARTESIAN_POINT ( 'NONE',  ( 61.18464984179839661, -1.879430190305400039, -15.94894231725639955 ) ) ;
#38479=CARTESIAN_POINT ( 'NONE',  ( 51.13984108499739989, -50.70264635719080104, -76.16554330276399298 ) ) ;
#38480=CARTESIAN_POINT ( 'NONE',  ( 60.44324472221690314, -46.04849446251390077, -48.06791170149890036 ) ) ;
#38482=CARTESIAN_POINT ( 'NONE',  ( 52.56521993351449851, -49.86179673305679927, -28.06704019101890069 ) ) ;
#38483=CARTESIAN_POINT ( 'NONE',  ( 66.23540447448930024, 18.72622661238738573, -69.60146707679315625 ) ) ;
#38484=VERTEX_POINT ( 'NONE', #1023 ) ;
#38486=CARTESIAN_POINT ( 'NONE',  ( 58.76768575440100051, -46.69271212826609485, -47.97336379875430623 ) ) ;
#38488=CARTESIAN_POINT ( 'NONE',  ( 13.95210466151750062, -50.80799586102129695, -21.48689998016109826 ) ) ;
#38489=CARTESIAN_POINT ( 'NONE',  ( 54.18608382124189404, 19.84132336588830015, -75.62481673555129191 ) ) ;
#38490=CARTESIAN_POINT ( 'NONE',  ( 46.42685859020519956, -53.00479672858950408, -76.14999999999999147 ) ) ;
#38491=CARTESIAN_POINT ( 'NONE',  ( 56.80155790502700341, 13.89662352512740107, -16.18051027641230277 ) ) ;
#38493=CARTESIAN_POINT ( 'NONE',  ( 56.48517904004920354, -50.54035073133489675, -52.93690031806480079 ) ) ;
#38496=ORIENTED_EDGE ( 'NONE', *, *, #9854, .F. ) ;
#38497=CARTESIAN_POINT ( 'NONE',  ( 47.60140394363290284, 23.29083994314989781, -74.50357325149190046 ) ) ;
#38499=AXIS2_PLACEMENT_3D ( 'NONE', #34493, #38439, #5699 ) ;
#38501=VECTOR ( 'NONE', #6387, 1000.000000000000000 ) ;
#38503=CARTESIAN_POINT ( 'NONE',  ( 11.84855223979754335, -65.05575864949535969, -23.81153761973788363 ) ) ;
#38505=CARTESIAN_POINT ( 'NONE',  ( 45.92997521403570715, -45.11618897614619783, -7.538598176229350578 ) ) ;
#38506=CARTESIAN_POINT ( 'NONE',  ( 61.75019796695546859, -45.11618894467940066, -26.84765976650484376 ) ) ;
#38507=AXIS2_PLACEMENT_3D ( 'NONE', #20322, #43683, #47367 ) ;
#38508=CIRCLE ( 'NONE', #35986, 23.00000000000000000 ) ;
#38509=DIRECTION ( 'NONE',  ( 3.556943099846429769E-14, -1.469246684736110336E-14, 1.000000000000000000 ) ) ;
#38510=CARTESIAN_POINT ( 'NONE',  ( 82.64668144475160716, 14.08996193411520004, -47.29313766171369338 ) ) ;
#38511=DIRECTION ( 'NONE',  ( 0.8090169943749490056, 0.5877852522924709167, 0.000000000000000000 ) ) ;
#38512=CARTESIAN_POINT ( 'NONE',  ( 65.03603135454920903, 1.015437840524759938, -17.83403478221330118 ) ) ;
#38515=CARTESIAN_POINT ( 'NONE',  ( 6.211423689675569904, 33.74952992075439795, -48.42816009187949788 ) ) ;
#38517=EDGE_LOOP ( 'NONE', ( #40581, #9414, #11088, #39814, #49592, #19463 ) ) ;
#38518=( BOUNDED_CURVE ( )  B_SPLINE_CURVE ( 3, ( #27639, #18749, #7483, #15606 ),
 .UNSPECIFIED., .F., .T. ) 
 B_SPLINE_CURVE_WITH_KNOTS ( ( 4, 4 ),
 ( 0.000000000000000000, 0.7973345187655109800 ),
 .UNSPECIFIED. ) 
 CURVE ( )  GEOMETRIC_REPRESENTATION_ITEM ( )  RATIONAL_B_SPLINE_CURVE ( ( 1.000000000000000000, 0.9477194463320799400, 0.9477194463320799400, 1.000000000000000000 ) ) 
 REPRESENTATION_ITEM ( '' )  );
#38519=CARTESIAN_POINT ( 'NONE',  ( 52.98105876229369926, -49.58786226930830310, -48.88375727566869955 ) ) ;
#38523=CARTESIAN_POINT ( 'NONE',  ( 14.08288962360609986, 19.91677594646370153, -22.65087057678250204 ) ) ;
#38524=CARTESIAN_POINT ( 'NONE',  ( 57.23260717840510381, 13.90933895519079933, -25.52124253973569878 ) ) ;
#38527=CARTESIAN_POINT ( 'NONE',  ( 52.91963044591119569, 18.40471342935619958, -48.95754072428230330 ) ) ;
#38528=CARTESIAN_POINT ( 'NONE',  ( 55.13867673449530571, -45.86707377957979759, -16.04494662851070075 ) ) ;
#38533=EDGE_CURVE ( 'NONE', #50841, #25812, #25010, .T. ) ;
#38534=CIRCLE ( 'NONE', #40314, 1.999999999999998224 ) ;
#38535=CARTESIAN_POINT ( 'NONE',  ( 11.09248976069099868, -65.15264557193228256, -17.64371789480989960 ) ) ;
#38536=CARTESIAN_POINT ( 'NONE',  ( 12.26578330975819853, 34.20340090639090391, -47.53372884124510023 ) ) ;
#38538=CARTESIAN_POINT ( 'NONE',  ( 11.89539497636140020, -65.43621263634180707, -18.11027658854760247 ) ) ;
#38539=CARTESIAN_POINT ( 'NONE',  ( 53.27382404857081610, -49.51603170232991857, -49.18478183594817921 ) ) ;
#38543=VERTEX_POINT ( 'NONE', #51224 ) ;
#38546=CARTESIAN_POINT ( 'NONE',  ( 10.97995962411470039, -63.42200521575770722, -44.74774816381809472 ) ) ;
#38550=CARTESIAN_POINT ( 'NONE',  ( 57.02020359077309308, 19.36571434131419878, -53.44649995584460100 ) ) ;
#38551=CARTESIAN_POINT ( 'NONE',  ( 52.66506589159119756, 18.87069406197509736, -77.26054838684399328 ) ) ;
#38554=CARTESIAN_POINT ( 'NONE',  ( 13.00893739761190027, -65.51843714052189682, -47.75434321210310173 ) ) ;
#38555=CARTESIAN_POINT ( 'NONE',  ( 57.50723796702470025, 15.88381105532069704, -31.98003398807230369 ) ) ;
#38556=VECTOR ( 'NONE', #42610, 1000.000000000000000 ) ;
#38557=CYLINDRICAL_SURFACE ( 'NONE', #31822, 38.00000000000000711 ) ;
#38560=B_SPLINE_SURFACE_WITH_KNOTS ( 'NONE', 3, 3, ( 
 ( #14503, #2971, #38882, #34925, #47266, #11612, #42555, #50924, #27320, #10585 ),
 ( #6647, #2715, #15021, #18688, #30732, #11354, #35447, #39389, #23366, #15284 ),
 ( #31238, #7420, #3493, #46758, #46495, #15540, #51444, #3229, #50668, #14764 ),
 ( #43580, #19720, #7681, #30474, #26541, #42816, #18946, #6912, #38624, #22861 ) ),
 .UNSPECIFIED., .F., .F., .F.,
 ( 4, 4 ),
 ( 4, 1, 1, 1, 1, 1, 1, 4 ),
 ( 1.485879941667409998, 1.508490955196220007 ),
 ( -1.052722112000000057E-06, 0.1428571428571430157, 0.2857142857142860315, 0.4285714285714289917, 0.5714285714285709528, 0.7142857142857139685, 0.8571428571428569843, 1.000000000000000000 ),
 .UNSPECIFIED. ) ;
#38564=EDGE_LOOP ( 'NONE', ( #42425, #20989 ) ) ;
#38565=DIRECTION ( 'NONE',  ( 0.000000000000000000, 0.000000000000000000, -1.000000000000000000 ) ) ;
#38567=CARTESIAN_POINT ( 'NONE',  ( 53.16274104891699892, -49.55751115293769971, -49.15255090718000019 ) ) ;
#38570=CYLINDRICAL_SURFACE ( 'NONE', #8313, 1.999999999999999556 ) ;
#38572=CARTESIAN_POINT ( 'NONE',  ( 13.60549620763140233, 20.19926697308349972, -74.35527526576591129 ) ) ;
#38575=CARTESIAN_POINT ( 'NONE',  ( 45.83940545869849359, -45.13646462238730095, -7.873659365571991309 ) ) ;
#38580=CARTESIAN_POINT ( 'NONE',  ( 56.08336180637530788, -50.80210678062450569, -74.87709413289790916 ) ) ;
#38581=CARTESIAN_POINT ( 'NONE',  ( -1.485984422640509894, 19.61345480293289967, -6.464765694581079636 ) ) ;
#38584=DIRECTION ( 'NONE',  ( 0.9741140340359943917, 0.000000000000000000, 0.2260571801428161165 ) ) ;
#38586=VERTEX_POINT ( 'NONE', #31021 ) ;
#38590=CARTESIAN_POINT ( 'NONE',  ( 47.50173433525049660, 23.36124847523640113, -54.80342700628099806 ) ) ;
#38593=CARTESIAN_POINT ( 'NONE',  ( 56.61928438282120624, 14.09173444410579989, -25.29356196242219923 ) ) ;
#38595=CARTESIAN_POINT ( 'NONE',  ( 11.50351859489629902, 34.04974385669249415, -17.32566793788090109 ) ) ;
#38597=CARTESIAN_POINT ( 'NONE',  ( 52.82947172221679466, 18.42909589620090216, -48.64743982913490328 ) ) ;
#38600=CARTESIAN_POINT ( 'NONE',  ( 52.77132786495689487, 18.46083226933780352, -28.08595485654360147 ) ) ;
#38601=CARTESIAN_POINT ( 'NONE',  ( 50.51123532868781041, 4.833585210846805147, -76.20873194682746998 ) ) ;
#38603=CARTESIAN_POINT ( 'NONE',  ( 52.82976000643810011, -49.66091852057420652, -28.05436868014771079 ) ) ;
#38604=CARTESIAN_POINT ( 'NONE',  ( 53.12218290940240450, 18.34074958227849805, -49.13784296393349393 ) ) ;
#38605=CARTESIAN_POINT ( 'NONE',  ( 53.10211901724390060, -45.11618894467940066, -9.306651317679861535 ) ) ;
#38607=CARTESIAN_POINT ( 'NONE',  ( 11.10559214712420051, 32.11323242349129714, -44.25388736977730275 ) ) ;
#38609=CARTESIAN_POINT ( 'NONE',  ( 65.32710667846340868, -32.02409943616269317, -17.54847724138329923 ) ) ;
#38610=CARTESIAN_POINT ( 'NONE',  ( 18.78670704276689918, 20.36472114263469990, -74.14993923597710079 ) ) ;
#38612=EDGE_LOOP ( 'NONE', ( #2449, #41943 ) ) ;
#38614=CARTESIAN_POINT ( 'NONE',  ( 76.49478695177366205, -3.228580831157734199, -13.20495443489320131 ) ) ;
#38616=CARTESIAN_POINT ( 'NONE',  ( 11.79375100434000068, -65.01330894899159318, -45.51098474479470468 ) ) ;
#38617=CARTESIAN_POINT ( 'NONE',  ( 56.92167681130780466, -45.21777262807209752, -25.50865813986290220 ) ) ;
#38620=CARTESIAN_POINT ( 'NONE',  ( 13.58893910384336046, -51.93861847144918187, -75.09855816271630147 ) ) ;
#38622=CARTESIAN_POINT ( 'NONE',  ( 61.51122975691189509, 13.91278366405479616, -37.26101630944549470 ) ) ;
#38624=CARTESIAN_POINT ( 'NONE',  ( 11.72646946156880077, 32.43593556876640349, -24.74253206387260207 ) ) ;
#38625=VERTEX_POINT ( 'NONE', #10618 ) ;
#38628=CARTESIAN_POINT ( 'NONE',  ( 14.30960224998139907, 19.88381748068809785, -22.40439468542579604 ) ) ;
#38631=TOROIDAL_SURFACE ( 'NONE', #13520, 30.50439988982899564, 1.000000000000000000 ) ;
#38633=CARTESIAN_POINT ( 'NONE',  ( 46.47231003491339862, -53.11747274052710566, -76.13961530627510399 ) ) ;
#38635=CARTESIAN_POINT ( 'NONE',  ( 58.16220902598259812, 13.11504794394689988, -8.909165776004030590 ) ) ;
#38641=CARTESIAN_POINT ( 'NONE',  ( 52.32303876295770095, 20.18503163261420141, -75.90202713928280787 ) ) ;
#38642=CARTESIAN_POINT ( 'NONE',  ( 61.51122975691189509, -45.14516155341349446, -37.26101630944549470 ) ) ;
#38643=ADVANCED_FACE ( 'NONE', ( #19239 ), #35765, .F. ) ;
#38646=CARTESIAN_POINT ( 'NONE',  ( 54.35976913619879980, -48.30693508310460516, -26.83861054538819957 ) ) ;
#38647=CARTESIAN_POINT ( 'NONE',  ( 1.127313977364120090, -53.29995640468419538, -7.495105548070389645 ) ) ;
#38648=CARTESIAN_POINT ( 'NONE',  ( 75.79457347663668543, -29.99145320232659984, -12.10716626236989946 ) ) ;
#38649=CARTESIAN_POINT ( 'NONE',  ( 74.93037820153030282, 13.88381105528979909, -15.31096251095349992 ) ) ;
#38652=B_SPLINE_CURVE_WITH_KNOTS ( 'NONE', 3,
 ( #28205, #20090, #8572, #4892, #32906, #20859, #25038, #9089, #40534, #36591, #692, #32641, #16682, #17213, #33173, #29242 ),
 .UNSPECIFIED., .F., .F.,
 ( 4, 2, 2, 2, 2, 2, 2, 4 ),
 ( 0.000000000000000000, 0.1774999999999995748, 0.3374999999999991340, 0.4375000000000007772, 0.4999999999999992228, 0.6250000000000014433, 0.8249999999999997335, 1.000000000000000000 ),
 .UNSPECIFIED. ) ;
#38653=CARTESIAN_POINT ( 'NONE',  ( 74.93037048120270072, -45.11618894467940066, -15.31097009269700138 ) ) ;
#38655=CARTESIAN_POINT ( 'NONE',  ( 82.51402289001910617, -45.11865457252260114, -46.70332443011600532 ) ) ;
#38657=CARTESIAN_POINT ( 'NONE',  ( 42.16710579538349890, 12.08965825037509845, -3.592545294286160207 ) ) ;
#38659=CARTESIAN_POINT ( 'NONE',  ( 19.58096105366284334, 24.23501488104968260, -75.51638835764758539 ) ) ;
#38660=CARTESIAN_POINT ( 'NONE',  ( 70.83393739769717001, -48.11618894467018492, -75.95000000000109708 ) ) ;
#38662=CARTESIAN_POINT ( 'NONE',  ( 18.30489236469509962, -52.23921076650779582, -75.65449215554859563 ) ) ;
#38663=CARTESIAN_POINT ( 'NONE',  ( 53.17454399592740089, -51.89736142002809771, -53.32454619227790005 ) ) ;
#38666=CIRCLE ( 'NONE', #42854, 25.10000000000000142 ) ;
#38669=ORIENTED_EDGE ( 'NONE', *, *, #31813, .T. ) ;
#38672=CARTESIAN_POINT ( 'NONE',  ( 61.00705302608989911, -45.67218455906219532, -47.73074504205549573 ) ) ;
#38676=CARTESIAN_POINT ( 'NONE',  ( 8.133937397696209715, 23.57564693985150228, -21.14999999999999858 ) ) ;
#38677=CARTESIAN_POINT ( 'NONE',  ( 41.26311261641770045, -45.40138146105840633, -6.071159984357790584 ) ) ;
#38680=ORIENTED_EDGE ( 'NONE', *, *, #3093, .F. ) ;
#38682=CARTESIAN_POINT ( 'NONE',  ( 61.21704192275100098, -45.26864704484780333, -46.77873930917139944 ) ) ;
#38692=CARTESIAN_POINT ( 'NONE',  ( 52.19959688358610350, -51.15283330212230339, -76.05470842491450867 ) ) ;
#38693=CARTESIAN_POINT ( 'NONE',  ( 60.24866557976239534, 14.54998834221819948, -47.36885438232269507 ) ) ;
#38695=CARTESIAN_POINT ( 'NONE',  ( 41.72814281503579537, -43.80724058770579887, -4.012820145101700042 ) ) ;
#38696=CARTESIAN_POINT ( 'NONE',  ( -10.42699089400579915, 11.57162609797640052, -6.107075065358959165 ) ) ;
#38702=CARTESIAN_POINT ( 'NONE',  ( 56.39270784227079503, -50.52750194671250483, -52.86271187454359932 ) ) ;
#38703=EDGE_CURVE ( 'NONE', #1308, #31549, #38275, .T. ) ;
#38706=CARTESIAN_POINT ( 'NONE',  ( 14.30198883284579914, -52.24360429457480137, -75.86497326479759806 ) ) ;
#38707=CARTESIAN_POINT ( 'NONE',  ( 44.98357806667660697, 14.87857081572859919, -8.963106682104738709 ) ) ;
#38710=CARTESIAN_POINT ( 'NONE',  ( 15.10819245920639986, 19.52950791741820069, -20.77789291003839978 ) ) ;
#38713=CARTESIAN_POINT ( 'NONE',  ( 47.85552020099460435, -54.43926621290979995, -55.10000200886270250 ) ) ;
#38714=CARTESIAN_POINT ( 'NONE',  ( 18.86789271228509790, -51.78678246903520233, -74.14999999999999147 ) ) ;
#38716=CARTESIAN_POINT ( 'NONE',  ( 47.86297059184269642, 23.17976950889599763, -54.90440623528039765 ) ) ;
#38717=ORIENTED_EDGE ( 'NONE', *, *, #6985, .T. ) ;
#38719=ORIENTED_EDGE ( 'NONE', *, *, #27312, .F. ) ;
#38720=B_SPLINE_SURFACE_WITH_KNOTS ( 'NONE', 3, 3, ( 
 ( #37279, #45926, #5830, #25715, #49860, #42515, #17625, #17365 ),
 ( #6604, #29406, #18134, #46455, #6092, #21793, #22046, #10543 ),
 ( #46196, #5579, #21534, #37801, #1896, #2401, #33333, #1378 ),
 ( #13949, #45661, #34096, #17873, #18385, #30430, #37531, #26499 ),
 ( #10016, #49348, #33595, #13447, #45406, #9511, #34360, #33844 ),
 ( #38059, #42250, #9764, #50377, #10280, #25458, #41463, #29908 ),
 ( #26242, #41992, #13696, #1636, #50111, #2154, #14206, #6349 ),
 ( #22307, #49609, #29656, #41723, #35141, #34885, #47729, #51656 ),
 ( #35672, #46715, #15501, #23585, #11315, #31454, #43790, #23327 ),
 ( #51400, #50626, #10800, #30943, #30693, #3191, #38581, #43031 ),
 ( #11834, #7128, #23080, #39098, #27534, #18648, #38842, #2675 ),
 ( #27280, #11057, #14977, #2930, #19164, #51146, #31704, #15244 ),
 ( #31194, #27024, #47225, #27794, #18901, #34622, #43289, #22565 ),
 ( #3451, #14723, #7378, #39352, #19424, #26759, #6872, #47480 ),
 ( #42772, #35404, #11572, #39603, #22821, #50885, #46974, #43540 ),
 ( #7640, #3706, #19674, #15750, #28039, #33001, #24611, #32462 ) ),
 .UNSPECIFIED., .F., .F., .F.,
 ( 4, 2, 2, 2, 2, 2, 2, 4 ),
 ( 4, 1, 1, 1, 1, 4 ),
 ( 12.41737348417879971, 14.15001006772950021, 23.85327782795560125, 28.70491170806869974, 32.58621881215919558, 36.46752591624959905, 42.67761728279440092, 46.65092557583719923 ),
 ( -1.202762707400000043E-05, 0.2000000000000000111, 0.4000000000000000222, 0.5999999999999999778, 0.8000000000000000444, 1.000241744799150068 ),
 .UNSPECIFIED. ) ;
#38722=CARTESIAN_POINT ( 'NONE',  ( 82.48407818766771982, 13.86596467738130833, -46.54738304680805783 ) ) ;
#38724=CARTESIAN_POINT ( 'NONE',  ( 17.21347160910390173, -53.11618894467930119, -76.14999999999999147 ) ) ;
#38733=ORIENTED_EDGE ( 'NONE', *, *, #48676, .T. ) ;
#38734=CARTESIAN_POINT ( 'NONE',  ( 12.36320305068320025, -64.54682834576858852, -15.76422791927960176 ) ) ;
#38738=CARTESIAN_POINT ( 'NONE',  ( 13.00893739769619906, -65.51843714052719747, -47.75434321273180416 ) ) ;
#38739=AXIS2_PLACEMENT_3D ( 'NONE', #30855, #46884, #50801 ) ;
#38743=CARTESIAN_POINT ( 'NONE',  ( 54.45614327494340046, 20.39970296835689823, -54.11881936521780290 ) ) ;
#38744=CARTESIAN_POINT ( 'NONE',  ( 50.95939809116894992, -35.29322421015848477, -76.37898009206955408 ) ) ;
#38746=CARTESIAN_POINT ( 'NONE',  ( 52.58363548700440049, -49.84283414857759453, -48.51251314324170494 ) ) ;
#38748=CARTESIAN_POINT ( 'NONE',  ( 61.93068749498159775, -0.2735828025601050317, -16.53651274250989545 ) ) ;
#38749=EDGE_CURVE ( 'NONE', #39228, #49183, #39052, .T. ) ;
#38750=CARTESIAN_POINT ( 'NONE',  ( 57.57487205268949992, -49.96950191258749641, -52.44452323771800195 ) ) ;
#38753=CARTESIAN_POINT ( 'NONE',  ( 76.13592501344869845, 12.07790803439914029, -13.68765646776531320 ) ) ;
#38756=CARTESIAN_POINT ( 'NONE',  ( 54.36584921719999386, -48.99915756198799954, -48.99053282728779379 ) ) ;
#38758=CARTESIAN_POINT ( 'NONE',  ( 13.93396757539989927, -51.17250542873200203, -22.49579876130530209 ) ) ;
#38760=CARTESIAN_POINT ( 'NONE',  ( 56.52130130765199567, 13.95454412478370010, -16.23639984573850015 ) ) ;
#38765=B_SPLINE_CURVE_WITH_KNOTS ( 'NONE', 3,
 ( #42318, #45993, #6670, #23143, #11122, #6415 ),
 .UNSPECIFIED., .F., .F.,
 ( 4, 1, 1, 4 ),
 ( 0.000000000000000000, 0.3333336742575975231, 0.6666673485151961565, 1.000000000000000000 ),
 .UNSPECIFIED. ) ;
#38768=CARTESIAN_POINT ( 'NONE',  ( 46.37807361908240011, 21.71172191342840208, -76.14999999999999147 ) ) ;
#38770=CARTESIAN_POINT ( 'NONE',  ( 43.83352794118219720, -46.05657771629909547, -8.175079556547590443 ) ) ;
#38774=DIRECTION ( 'NONE',  ( 0.000000000000000000, 4.336808689941963009E-16, -1.000000000000000000 ) ) ;
#38775=DIRECTION ( 'NONE',  ( -8.592609827796581962E-15, 1.919972818367709724E-16, -1.000000000000000000 ) ) ;
#38777=CARTESIAN_POINT ( 'NONE',  ( 82.48253024579470605, 14.11464642499709932, -47.31939374336590021 ) ) ;
#38779=CARTESIAN_POINT ( 'NONE',  ( 52.27429626352468262, 18.55921403040872875, -77.19751344877612098 ) ) ;
#38782=CARTESIAN_POINT ( 'NONE',  ( -25.78889119571919863, 9.715729424517359547, -54.35424806255070251 ) ) ;
#38784=CARTESIAN_POINT ( 'NONE',  ( 52.73034409711829795, -49.72355465471469671, -48.63395058221750133 ) ) ;
#38788=CARTESIAN_POINT ( 'NONE',  ( 13.89738755828549976, 19.98851976734169966, -22.99807275174740084 ) ) ;
#38791=CARTESIAN_POINT ( 'NONE',  ( 53.16045451627860530, 18.32047277855539846, -49.13860146820209707 ) ) ;
#38792=CARTESIAN_POINT ( 'NONE',  ( 55.62727650224960740, -45.90849497969049509, -16.78013324446749976 ) ) ;
#38795=ORIENTED_EDGE ( 'NONE', *, *, #39936, .F. ) ;
#38799=CARTESIAN_POINT ( 'NONE',  ( 12.91569276135830080, 34.28022004553969992, -47.73039263113269470 ) ) ;
#38801=LINE ( 'NONE', #2895, #46119 ) ;
#38802=CARTESIAN_POINT ( 'NONE',  ( 52.69474619017665873, -49.76773528829182425, -48.79529908194032117 ) ) ;
#38803=CARTESIAN_POINT ( 'NONE',  ( -33.86606260230286125, -15.61618894467806484, -57.75434458024869855 ) ) ;
#38804=CARTESIAN_POINT ( 'NONE',  ( 50.09664746341090336, -53.48905984871790054, -54.90216016554420264 ) ) ;
#38808=CARTESIAN_POINT ( 'NONE',  ( 9.736265806055229177, -63.20621787679230152, -46.29822409738210354 ) ) ;
#38809=ADVANCED_FACE ( 'NONE', ( #5077 ), #51126, .T. ) ;
#38811=VERTEX_POINT ( 'NONE', #45810 ) ;
#38813=CARTESIAN_POINT ( 'NONE',  ( 57.35590716991889337, 18.90417298847060223, -52.61987026654610133 ) ) ;
#38814=EDGE_CURVE ( 'NONE', #12694, #43570, #20563, .T. ) ;
#38815=CARTESIAN_POINT ( 'NONE',  ( 53.27342892381020079, 19.23708225937859595, -77.09451959761469197 ) ) ;
#38819=CARTESIAN_POINT ( 'NONE',  ( 9.897519174578837564, -64.60056534141453710, -46.94956808238860191 ) ) ;
#38822=CARTESIAN_POINT ( 'NONE',  ( 57.28991729228579288, -50.57887465766769708, -53.44461810997250240 ) ) ;
#38827=ORIENTED_EDGE ( 'NONE', *, *, #19397, .F. ) ;
#38830=CARTESIAN_POINT ( 'NONE',  ( 52.57361112802249892, -49.85323755487960540, -48.51313449024529234 ) ) ;
#38834=EDGE_CURVE ( 'NONE', #43823, #26115, #5312, .T. ) ;
#38835=DIRECTION ( 'NONE',  ( 0.000000000000000000, -1.000000000000000000, 0.000000000000000000 ) ) ;
#38836=CYLINDRICAL_SURFACE ( 'NONE', #43968, 50.00000000000000000 ) ;
#38840=CARTESIAN_POINT ( 'NONE',  ( 52.56521993351449851, -49.86179673305689874, -28.15000000000000213 ) ) ;
#38841=CARTESIAN_POINT ( 'NONE',  ( 54.59220245897340362, -50.90304460341570092, -75.70160923548360188 ) ) ;
#38842=CARTESIAN_POINT ( 'NONE',  ( -2.400008891863520066, 18.68547184855179921, -6.077313690069900076 ) ) ;
#38843=CARTESIAN_POINT ( 'NONE',  ( 16.13393739769620083, -15.61618894467929941, -76.14999999999999147 ) ) ;
#38844=CARTESIAN_POINT ( 'NONE',  ( 47.73667124825149699, -54.43832146008400485, -54.70375119057089819 ) ) ;
#38848=CARTESIAN_POINT ( 'NONE',  ( -6.554330340120890774, -46.10323663931790605, -4.693995879374440072 ) ) ;
#38849=CARTESIAN_POINT ( 'NONE',  ( 47.55845087153019790, 23.33810426020020046, -54.95948882862809626 ) ) ;
#38850=CARTESIAN_POINT ( 'NONE',  ( -1.566062602304203022, -15.61618894467939889, -10.44999999999964757 ) ) ;
#38852=CARTESIAN_POINT ( 'NONE',  ( 61.47032571389799926, 14.17707786984260032, -47.41712456996229719 ) ) ;
#38853=CARTESIAN_POINT ( 'NONE',  ( 11.49145838457179991, 33.80527165212970431, -16.71591419048260008 ) ) ;
#38854=CARTESIAN_POINT ( 'NONE',  ( 51.81471494547309931, 18.30023427017130189, -76.85964192801058914 ) ) ;
#38855=CARTESIAN_POINT ( 'NONE',  ( 52.80356173049369772, 18.44276956637660092, -48.56462661435369910 ) ) ;
#38858=CARTESIAN_POINT ( 'NONE',  ( 54.80579272659560530, 16.60235534783570088, -26.62706727043990185 ) ) ;
#38865=CARTESIAN_POINT ( 'NONE',  ( 11.13393739769619906, 32.09617326967790518, -43.91648406538870120 ) ) ;
#38867=CARTESIAN_POINT ( 'NONE',  ( 66.13977606332380788, -31.03571436735869682, -17.02376530829800316 ) ) ;
#38871=CARTESIAN_POINT ( 'NONE',  ( 41.36298005976649961, 12.80050257910570011, -3.553636961524439641 ) ) ;
#38872=ADVANCED_FACE ( 'NONE', ( #42133 ), #15387, .T. ) ;
#38873=CARTESIAN_POINT ( 'NONE',  ( 49.45810426794375303, -2.188232918999916343, -15.73681870539564365 ) ) ;
#38874=ORIENTED_EDGE ( 'NONE', *, *, #35321, .F. ) ;
#38875=CARTESIAN_POINT ( 'NONE',  ( 10.95435945972059955, -63.78130685611410655, -44.98684614314139907 ) ) ;
#38876=CARTESIAN_POINT ( 'NONE',  ( 56.43568955072729665, -45.44241490114089999, -25.50436399627979966 ) ) ;
#38878=DIRECTION ( 'NONE',  ( 0.8090169943749475623, 0.5877852522924730261, 0.000000000000000000 ) ) ;
#38879=ORIENTED_EDGE ( 'NONE', *, *, #35559, .T. ) ;
#38882=CARTESIAN_POINT ( 'NONE',  ( 11.59229195909269983, 34.14674705323289317, -22.55625370316070288 ) ) ;
#38883=ORIENTED_EDGE ( 'NONE', *, *, #46274, .F. ) ;
#38884=CARTESIAN_POINT ( 'NONE',  ( 52.65940447408669911, -45.11618894467940066, -12.18415347133140081 ) ) ;
#38885=B_SPLINE_CURVE_WITH_KNOTS ( 'NONE', 3,
 ( #34198, #5936, #9611, #34469 ),
 .UNSPECIFIED., .F., .F.,
 ( 4, 4 ),
 ( 0.4987209838069229795, 1.000000000000000000 ),
 .UNSPECIFIED. ) ;
#38888=CARTESIAN_POINT ( 'NONE',  ( 16.08016673438230271, 19.80150180430160134, -20.14986617604239783 ) ) ;
#38890=B_SPLINE_CURVE_WITH_KNOTS ( 'NONE', 3,
 ( #43569, #31992, #51176, #35700, #43314, #48013, #15527, #15271 ),
 .UNSPECIFIED., .F., .F.,
 ( 4, 2, 2, 4 ),
 ( 0.3562431257904284942, 0.5954397627775694923, 0.8830025937151522175, 1.000000000000000000 ),
 .UNSPECIFIED. ) ;
#38891=CARTESIAN_POINT ( 'NONE',  ( 60.74065736930379700, -29.42750435924840247, -15.90652919026539891 ) ) ;
#38893=CARTESIAN_POINT ( 'NONE',  ( 46.35275103504449845, -52.90993241930539881, -76.14999999999999147 ) ) ;
#38894=CARTESIAN_POINT ( 'NONE',  ( 43.03640022808939847, 13.88381105527780157, -6.890438909537429879 ) ) ;
#38897=CARTESIAN_POINT ( 'NONE',  ( 10.00991122538783173, 23.91216740073585001, -46.09048026812309473 ) ) ;
#38898=CARTESIAN_POINT ( 'NONE',  ( 58.53216149070850349, 13.88381120887479980, -25.55155896066500176 ) ) ;
#38901=CARTESIAN_POINT ( 'NONE',  ( 29.52882095054619782, 21.88381105532300097, -74.14999999999999147 ) ) ;
#38902=AXIS2_PLACEMENT_3D ( 'NONE', #13295, #49203, #16695 ) ;
#38903=CARTESIAN_POINT ( 'NONE',  ( -5.957774818403610340, -47.45617016592679960, -6.636813055207410272 ) ) ;
#38904=CARTESIAN_POINT ( 'NONE',  ( 76.56166476258249531, 9.631681111976121201, -13.86454137039240031 ) ) ;
#38905=CARTESIAN_POINT ( 'NONE',  ( 75.38195435473652140, 13.04593086575056127, -13.74600147056045607 ) ) ;
#38906=CARTESIAN_POINT ( 'NONE',  ( 20.13393739768959634, -55.41568642894479524, -74.14999999999999147 ) ) ;
#38907=CARTESIAN_POINT ( 'NONE',  ( 12.77676462293392134, -55.47504473345251341, -75.60405384314019273 ) ) ;
#38908=FACE_OUTER_BOUND ( 'NONE', #12425, .T. ) ;
#38909=CARTESIAN_POINT ( 'NONE',  ( 82.46545078568199472, -45.09314778790560041, -46.44237448698110171 ) ) ;
#38910=CARTESIAN_POINT ( 'NONE',  ( 57.36488636042089695, -50.16807177143650165, -52.65750501476470191 ) ) ;
#38911=CARTESIAN_POINT ( 'NONE',  ( 41.02005863531599772, 13.11595598970779974, -4.033360981351730601 ) ) ;
#38916=CARTESIAN_POINT ( 'NONE',  ( 75.99395259271645386, -43.32339650468484393, -13.62990582981167620 ) ) ;
#38917=CARTESIAN_POINT ( 'NONE',  ( 18.04837480293360130, -52.31213937195320085, -75.84958893011570069 ) ) ;
#38918=CARTESIAN_POINT ( 'NONE',  ( 45.25256250357250565, -43.53500084062090281, -5.388698120161880212 ) ) ;
#38922=CARTESIAN_POINT ( 'NONE',  ( 7.712470290556179719, 30.55595177311299793, -15.52620908427480018 ) ) ;
#38927=CARTESIAN_POINT ( 'NONE',  ( 42.89815834353850477, -45.52996223267120257, -7.114957886879119897 ) ) ;
#38928=VERTEX_POINT ( 'NONE', #43682 ) ;
#38938=VERTEX_POINT ( 'NONE', #31085 ) ;
#38942=DIRECTION ( 'NONE',  ( 0.2993038002561358990, -0.8275125542569267134, 0.4750160078349067727 ) ) ;
#38946=CARTESIAN_POINT ( 'NONE',  ( 61.28610861176739633, 13.99802266614350010, -28.15000000000000213 ) ) ;
#38947=CARTESIAN_POINT ( 'NONE',  ( 52.25623532178450148, -51.32859135100709835, -75.95837140036390167 ) ) ;
#38948=CARTESIAN_POINT ( 'NONE',  ( 60.66089622436710016, 14.32868137727570002, -47.20375295697429863 ) ) ;
#38951=EDGE_CURVE ( 'NONE', #35735, #17152, #23931, .T. ) ;
#38952=CARTESIAN_POINT ( 'NONE',  ( 41.36297991754150161, -44.03288059546810018, -3.553637027260359904 ) ) ;
#38954=CARTESIAN_POINT ( 'NONE',  ( -10.88693382329749859, 11.10980032629789882, -6.245353000315719605 ) ) ;
#38956=DIRECTION ( 'NONE',  ( 0.2260571801428170324, 2.970872000000000522E-15, -0.9741140340359940586 ) ) ;
#38960=CARTESIAN_POINT ( 'NONE',  ( 8.815605938792600682, 32.05029769220720226, -46.67186391141279955 ) ) ;
#38961=CARTESIAN_POINT ( 'NONE',  ( 57.55751162087899786, 19.32515479037619954, -53.43780795140229856 ) ) ;
#38964=CARTESIAN_POINT ( 'NONE',  ( 13.73505343097469833, 18.97478628885919960, -20.93075220000899961 ) ) ;
#38966=EDGE_CURVE ( 'NONE', #33975, #12711, #8065, .T. ) ;
#38970=CARTESIAN_POINT ( 'NONE',  ( 47.81064057165269787, -54.45306024599980077, -55.02164417520120310 ) ) ;
#38972=DIRECTION ( 'NONE',  ( 0.000000000000000000, 0.000000000000000000, -1.000000000000000000 ) ) ;
#38973=CARTESIAN_POINT ( 'NONE',  ( -7.471208905559357127, -45.39622512240971730, -4.913224500014766960 ) ) ;
#38975=CARTESIAN_POINT ( 'NONE',  ( 47.68932896513950226, 23.27841431174140041, -55.03972088634769477 ) ) ;
#38980=CARTESIAN_POINT ( 'NONE',  ( 60.89998638923569985, -45.43270080629340413, -46.98170749212690822 ) ) ;
#38981=DIRECTION ( 'NONE',  ( 0.6801873868961743064, 0.000000000000000000, -0.7330382791555664079 ) ) ;
#38983=DIRECTION ( 'NONE',  ( 1.000000000000000000, 5.245810363639075036E-26, 1.180619220495489865E-10 ) ) ;
#38984=DIRECTION ( 'NONE',  ( 0.000000000000000000, -1.000000000000000000, 0.000000000000000000 ) ) ;
#38991=EDGE_LOOP ( 'NONE', ( #28664, #32678, #7748, #22441 ) ) ;
#38994=CARTESIAN_POINT ( 'NONE',  ( -2.927979189508790103, -49.19984425798019601, -5.740620115512199639 ) ) ;
#38996=CARTESIAN_POINT ( 'NONE',  ( 9.514507235804281038, -64.16384161684520393, -46.74925938990359953 ) ) ;
#38998=ORIENTED_EDGE ( 'NONE', *, *, #5097, .F. ) ;
#39001=AXIS2_PLACEMENT_3D ( 'NONE', #22049, #22825, #33847 ) ;
#39002=CARTESIAN_POINT ( 'NONE',  ( 66.70013194292150160, -1.463538230407920082, -17.02746303015019791 ) ) ;
#39004=DIRECTION ( 'NONE',  ( 0.3619651935900872752, 0.9321916104692696825, -3.469446951953614978E-15 ) ) ;
#39005=CARTESIAN_POINT ( 'NONE',  ( 58.93930182096060122, -2.761714617466529909, -15.64944026956619894 ) ) ;
#39006=CARTESIAN_POINT ( 'NONE',  ( 52.13018415749819923, -49.87691714427380418, -76.92945436144250948 ) ) ;
#39008=ORIENTED_EDGE ( 'NONE', *, *, #15915, .F. ) ;
#39012=CARTESIAN_POINT ( 'NONE',  ( 52.65940447374160271, -45.11618894467940066, -12.18415347180710029 ) ) ;
#39015=CARTESIAN_POINT ( 'NONE',  ( 13.57020051470579958, -51.02066577404819725, -21.88590882852059849 ) ) ;
#39018=CARTESIAN_POINT ( 'NONE',  ( 55.48947357315069695, 13.88381105532070059, -14.40594736128640108 ) ) ;
#39019=CARTESIAN_POINT ( 'NONE',  ( 61.16413136812519724, -45.33305036688479817, -47.10581894728210273 ) ) ;
#39020=CARTESIAN_POINT ( 'NONE',  ( 56.52536539877740296, -50.75180572374080157, -53.84278118897309895 ) ) ;
#39030=EDGE_CURVE ( 'NONE', #2811, #19647, #46611, .T. ) ;
#39033=CARTESIAN_POINT ( 'NONE',  ( 82.71799697060619394, 14.26033053130370121, -47.55443180484209620 ) ) ;
#39038=CARTESIAN_POINT ( 'NONE',  ( 49.54883067255690321, 22.47422963147529984, -54.90668699459310176 ) ) ;
#39041=CARTESIAN_POINT ( 'NONE',  ( 52.87494885159379976, -49.64620920156320238, -48.84793719265900336 ) ) ;
#39046=CARTESIAN_POINT ( 'NONE',  ( 13.90167036883489970, 19.71647169284459977, -21.77341558205650074 ) ) ;
#39047=CARTESIAN_POINT ( 'NONE',  ( 51.88872915794820528, -49.34590157055340143, -77.07840658455160110 ) ) ;
#39049=CARTESIAN_POINT ( 'NONE',  ( 52.91162664118279935, 18.41734443179310077, -48.98817407849419681 ) ) ;
#39050=CARTESIAN_POINT ( 'NONE',  ( 55.90886914330630475, -45.57186394744790192, -16.63621152108130019 ) ) ;
#39051=CARTESIAN_POINT ( 'NONE',  ( 54.39509416807689490, 16.57266139559970242, -25.91861715551300094 ) ) ;
#39052=CIRCLE ( 'NONE', #2200, 15.11955878774480233 ) ;
#39053=ORIENTED_EDGE ( 'NONE', *, *, #47117, .T. ) ;
#39055=B_SPLINE_CURVE_WITH_KNOTS ( 'NONE', 3,
 ( #41335, #29272, #33458, #5448, #8859, #41083, #36356, #17239, #16454, #28496, #48962, #21405, #4400, #5195, #20369, #13314 ),
 .UNSPECIFIED., .F., .F.,
 ( 4, 2, 2, 2, 2, 2, 2, 4 ),
 ( 0.000000000000000000, 0.1775017698726158166, 0.3375008917962792343, 0.4375003429985697689, 0.4999999999999995559, 0.6249993140028615723, 0.8249982164074401991, 1.000000000000000000 ),
 .UNSPECIFIED. ) ;
#39057=CARTESIAN_POINT ( 'NONE',  ( 58.58074692517319448, 15.55817703255979900, -48.00570932831679727 ) ) ;
#39058=CARTESIAN_POINT ( 'NONE',  ( 11.33121657942630023, 33.96965385299019857, -47.25760506163170049 ) ) ;
#39061=CARTESIAN_POINT ( 'NONE',  ( 52.95065152567730138, -49.64318942350852382, -49.05053742289103980 ) ) ;
#39063=CARTESIAN_POINT ( 'NONE',  ( 52.85072064880949938, -52.31592968273889710, -54.40017261481339972 ) ) ;
#39066=FACE_OUTER_BOUND ( 'NONE', #2193, .T. ) ;
#39067=ORIENTED_EDGE ( 'NONE', *, *, #26887, .T. ) ;
#39068=CARTESIAN_POINT ( 'NONE',  ( 10.77331230356430147, -63.33365191942790062, -45.20581385033180055 ) ) ;
#39070=VERTEX_POINT ( 'NONE', #942 ) ;
#39072=CARTESIAN_POINT ( 'NONE',  ( 56.96373068998019562, 19.10405578956169848, -52.80952918204310720 ) ) ;
#39073=CARTESIAN_POINT ( 'NONE',  ( 53.48387700974569725, 19.28793721532720085, -77.13966347312370431 ) ) ;
#39074=ORIENTED_EDGE ( 'NONE', *, *, #13162, .T. ) ;
#39076=CARTESIAN_POINT ( 'NONE',  ( 50.95182575631829991, 19.71852405838109945, -76.14999999999999147 ) ) ;
#39077=CIRCLE ( 'NONE', #2251, 2.000000000000001776 ) ;
#39081=CARTESIAN_POINT ( 'NONE',  ( 61.51122975691189509, 13.91278366405479616, -28.15000000000000213 ) ) ;
#39084=B_SPLINE_CURVE_WITH_KNOTS ( 'NONE', 3,
 ( #8705, #16555, #4001, #20473, #12641, #48536, #16048, #43832, #829, #44600, #24395, #19962, #35957, #24914, #24657, #5038 ),
 .UNSPECIFIED., .F., .F.,
 ( 4, 2, 2, 2, 2, 2, 2, 4 ),
 ( 0.07080984669201570436, 0.1402455969909039979, 0.3005262792662219962, 0.4007017056882959949, 0.4507894188993329943, 0.5309297600369918824, 0.6591543058572471026, 0.8014033947008442071 ),
 .UNSPECIFIED. ) ;
#39087=CARTESIAN_POINT ( 'NONE',  ( 52.62788022554430256, -49.80985595739589655, -48.67187667633960046 ) ) ;
#39092=CARTESIAN_POINT ( 'NONE',  ( 11.68991505668609854, 33.67328296886339700, -16.36861125145140150 ) ) ;
#39095=ADVANCED_FACE ( 'NONE', ( #24762, #25018 ), #8810, .T. ) ;
#39096=VECTOR ( 'NONE', #21902, 1000.000000000000000 ) ;
#39097=CARTESIAN_POINT ( 'NONE',  ( 53.68378902630690419, -51.14674281437299896, -75.73832380907369100 ) ) ;
#39098=CARTESIAN_POINT ( 'NONE',  ( -3.157173927189479645, 18.96160609307260003, -7.169295440220589732 ) ) ;
#39099=DIRECTION ( 'NONE',  ( -0.05023550054955997629, 0.000000000000000000, 0.9987374001630935361 ) ) ;
#39104=CARTESIAN_POINT ( 'NONE',  ( -10.43833443274229822, -42.78838519611409907, -5.987488507031909712 ) ) ;
#39105=CARTESIAN_POINT ( 'NONE',  ( 47.62304984032139998, 23.30770537504639961, -55.01447731861150459 ) ) ;
#39108=CARTESIAN_POINT ( 'NONE',  ( 61.18512861914399537, 14.25518643980569955, -47.51727820143830172 ) ) ;
#39110=CARTESIAN_POINT ( 'NONE',  ( 51.86152320295530416, 18.16617469022599707, -77.00280388411249533 ) ) ;
#39111=CARTESIAN_POINT ( 'NONE',  ( 52.85276752197869854, 18.41685827962099609, -48.69281274069099652 ) ) ;
#39112=CARTESIAN_POINT ( 'NONE',  ( 16.13393739769620083, -15.61618894467929941, 6.789625226207629538 ) ) ;
#39113=DIRECTION ( 'NONE',  ( 0.000000000000000000, 1.000000000000000000, 0.000000000000000000 ) ) ;
#39114=CARTESIAN_POINT ( 'NONE',  ( 52.86922557812509638, 18.38647850950570017, -27.84988300371350078 ) ) ;
#39116=CARTESIAN_POINT ( 'NONE',  ( 10.77457706359389888, -63.40313208684650448, -45.20848294960729419 ) ) ;
#39117=CARTESIAN_POINT ( 'NONE',  ( 52.59025554715780260, 18.60560742025969816, -48.57067451951849790 ) ) ;
#39118=CARTESIAN_POINT ( 'NONE',  ( 65.19670345645570819, -31.70240288822050090, -17.22254538528369849 ) ) ;
#39120=CARTESIAN_POINT ( 'NONE',  ( 39.04269904001555602, 1.028000652403628701, 6.072546842075589701 ) ) ;
#39123=LINE ( 'NONE', #19187, #28460 ) ;
#39127=ORIENTED_EDGE ( 'NONE', *, *, #9563, .T. ) ;
#39128=CARTESIAN_POINT ( 'NONE',  ( 42.11778985390380114, 12.11280974652049913, -3.278435070539889917 ) ) ;
#39132=CARTESIAN_POINT ( 'NONE',  ( 56.26582864981669729, -45.64151070618309802, -25.71051917747889703 ) ) ;
#39133=LINE ( 'NONE', #28076, #1048 ) ;
#39134=ORIENTED_EDGE ( 'NONE', *, *, #27044, .T. ) ;
#39137=DIRECTION ( 'NONE',  ( 1.000000000000000000, 0.000000000000000000, -0.000000000000000000 ) ) ;
#39139=CARTESIAN_POINT ( 'NONE',  ( 48.77938445352399555, -45.11618894467940066, -9.436603585181519094 ) ) ;
#39140=CARTESIAN_POINT ( 'NONE',  ( 51.17461318815491467, 0.4193470954621815738, -17.11446460828111427 ) ) ;
#39142=CARTESIAN_POINT ( 'NONE',  ( 59.89126922325319669, -28.73587617226999669, -15.75816652841679755 ) ) ;
#39143=( BOUNDED_CURVE ( )  B_SPLINE_CURVE ( 3, ( #37166, #37418, #5970, #36901 ),
 .UNSPECIFIED., .F., .T. ) 
 B_SPLINE_CURVE_WITH_KNOTS ( ( 4, 4 ),
 ( 0.7853981633974950194, 0.8959462480754279978 ),
 .UNSPECIFIED. ) 
 CURVE ( )  GEOMETRIC_REPRESENTATION_ITEM ( )  RATIONAL_B_SPLINE_CURVE ( ( 1.000000000000000000, 0.9989818526760920747, 0.9989818526760920747, 1.000000000000000000 ) ) 
 REPRESENTATION_ITEM ( '' )  );
#39145=CARTESIAN_POINT ( 'NONE',  ( 47.24351674907580190, -54.76020115456520188, -74.19815949659729881 ) ) ;
#39147=CARTESIAN_POINT ( 'NONE',  ( 14.93164752284620178, 21.74151571116259873, -76.14999999999999147 ) ) ;
#39148=CARTESIAN_POINT ( 'NONE',  ( 83.56294434887010425, -44.67980675742190044, -46.81484486652620092 ) ) ;
#39150=CARTESIAN_POINT ( 'NONE',  ( 65.05986636033101433, -32.17013944165564965, -17.72012440155577195 ) ) ;
#39153=DIRECTION ( 'NONE',  ( 1.000000000000000000, 0.000000000000000000, 0.000000000000000000 ) ) ;
#39155=CARTESIAN_POINT ( 'NONE',  ( 3.311002740984799964, -55.48809801447850276, -8.795318458723610178 ) ) ;
#39156=CARTESIAN_POINT ( 'NONE',  ( 76.45066347563938791, -5.998607385428130101, -13.01482868083799893 ) ) ;
#39158=CARTESIAN_POINT ( 'NONE',  ( 75.12321108456825414, 13.75868864148215209, -14.64191154256811522 ) ) ;
#39159=CARTESIAN_POINT ( 'NONE',  ( 16.13393739769620083, -15.61618894467929941, -28.02168704970069868 ) ) ;
#39161=CARTESIAN_POINT ( 'NONE',  ( 47.18324198357279897, 23.57489020266570279, -54.61058319554400242 ) ) ;
#39162=CARTESIAN_POINT ( 'NONE',  ( 82.74206167245459653, -45.55975176208480093, -47.63388670989679952 ) ) ;
#39163=CARTESIAN_POINT ( 'NONE',  ( 13.13413232964760091, 19.09465183653970044, -21.17378716131170080 ) ) ;
#39164=CARTESIAN_POINT ( 'NONE',  ( 57.42034897354250234, -50.39122232172000082, -52.99919040445719531 ) ) ;
#39165=CARTESIAN_POINT ( 'NONE',  ( 41.98583911138710079, 12.34957473716399967, -3.946145644750030268 ) ) ;
#39168=FACE_OUTER_BOUND ( 'NONE', #43928, .T. ) ;
#39170=CARTESIAN_POINT ( 'NONE',  ( 67.36987268233460213, -1.219418600938930064, -17.47395685963029877 ) ) ;
#39171=CARTESIAN_POINT ( 'NONE',  ( 18.27764122236090216, -52.20804236601910020, -75.66803551354809088 ) ) ;
#39172=DIRECTION ( 'NONE',  ( 1.000000000000000000, 0.000000000000000000, 0.000000000000000000 ) ) ;
#39175=ORIENTED_EDGE ( 'NONE', *, *, #230, .F. ) ;
#39176=CARTESIAN_POINT ( 'NONE',  ( 8.801404170410069838, 31.97031994814190270, -46.67014817202279886 ) ) ;
#39177=CARTESIAN_POINT ( 'NONE',  ( 85.26960572018150231, 18.79802461769378397, -53.60827425107920874 ) ) ;
#39181=CARTESIAN_POINT ( 'NONE',  ( 42.10988702888519697, -45.61410618971950726, -6.748864943960410478 ) ) ;
#39182=VERTEX_POINT ( 'NONE', #1721 ) ;
#39183=CARTESIAN_POINT ( 'NONE',  ( 17.65712708557559907, 21.25914908875220277, -76.03975947796440948 ) ) ;
#39186=ORIENTED_EDGE ( 'NONE', *, *, #43095, .T. ) ;
#39189=FACE_OUTER_BOUND ( 'NONE', #18630, .T. ) ;
#39191=ORIENTED_EDGE ( 'NONE', *, *, #16786, .F. ) ;
#39193=ORIENTED_EDGE ( 'NONE', *, *, #30644, .F. ) ;
#39194=FACE_BOUND ( 'NONE', #44587, .T. ) ;
#39198=CARTESIAN_POINT ( 'NONE',  ( 51.19516171219699885, -51.09621740586149485, -76.13919816896859061 ) ) ;
#39199=CARTESIAN_POINT ( 'NONE',  ( 60.34509757308260447, 14.55242050680869959, -47.56040643802499801 ) ) ;
#39201=CARTESIAN_POINT ( 'NONE',  ( 41.52331217152200082, -43.88959755902970272, -3.580227202335870551 ) ) ;
#39202=CARTESIAN_POINT ( 'NONE',  ( -2.760456474399689775, 17.67254785648750115, -5.324092234737729967 ) ) ;
#39203=CARTESIAN_POINT ( 'NONE',  ( 46.97440434159817357, 23.10210195763378138, -75.47461153636835718 ) ) ;
#39204=LINE ( 'NONE', #2790, #34772 ) ;
#39206=EDGE_LOOP ( 'NONE', ( #14248, #9795, #46654, #19051, #34985, #22217 ) ) ;
#39207=CYLINDRICAL_SURFACE ( 'NONE', #49793, 1.000000000000001110 ) ;
#39209=CARTESIAN_POINT ( 'NONE',  ( 57.49142314647060203, 19.07070453755489936, -52.84932360955439634 ) ) ;
#39212=EDGE_CURVE ( 'NONE', #37478, #17894, #37105, .T. ) ;
#39213=CARTESIAN_POINT ( 'NONE',  ( 14.09495638489210201, 19.44551819299880080, -21.23638623580700013 ) ) ;
#39221=CARTESIAN_POINT ( 'NONE',  ( 48.50283979947599988, -54.16647448328220094, -55.22557313126660006 ) ) ;
#39222=CARTESIAN_POINT ( 'NONE',  ( -33.86606260230286125, -15.61618894467806484, -57.75434458024869855 ) ) ;
#39223=AXIS2_PLACEMENT_3D ( 'NONE', #40703, #32291, #8482 ) ;
#39228=VERTEX_POINT ( 'NONE', #45492 ) ;
#39230=DIRECTION ( 'NONE',  ( 0.000000000000000000, 0.000000000000000000, 1.000000000000000000 ) ) ;
#39231=CARTESIAN_POINT ( 'NONE',  ( 59.82327988359549664, -45.99681751185720202, -47.29966340866579344 ) ) ;
#39233=CARTESIAN_POINT ( 'NONE',  ( 83.91175033285890095, 13.57253447764839827, -47.46627397093730139 ) ) ;
#39237=CARTESIAN_POINT ( 'NONE',  ( 68.13393739769620083, 17.38381105532069881, -65.65000000000000568 ) ) ;
#39240=ORIENTED_EDGE ( 'NONE', *, *, #50000, .F. ) ;
#39241=ADVANCED_FACE ( 'NONE', ( #1202 ), #41574, .T. ) ;
#39242=ORIENTED_EDGE ( 'NONE', *, *, #30931, .F. ) ;
#39245=DIRECTION ( 'NONE',  ( 0.000000000000000000, 0.000000000000000000, 1.000000000000000000 ) ) ;
#39246=CARTESIAN_POINT ( 'NONE',  ( 11.53802652246220006, -65.15112864915029434, -46.97774799415349634 ) ) ;
#39248=ORIENTED_EDGE ( 'NONE', *, *, #33265, .F. ) ;
#39251=CARTESIAN_POINT ( 'NONE',  ( 56.52536539877759481, -50.75180572374069499, -53.84278118897309895 ) ) ;
#39253=CARTESIAN_POINT ( 'NONE',  ( 60.83673909420080150, -0.6553940542465449548, -16.28925331010010069 ) ) ;
#39254=CARTESIAN_POINT ( 'NONE',  ( 51.75737835881179905, -49.21100704886299582, -76.97426712213069777 ) ) ;
#39258=CARTESIAN_POINT ( 'NONE',  ( 76.79908580335488466, 11.93597894565887430, -14.51620736842078863 ) ) ;
#39261=EDGE_CURVE ( 'NONE', #50083, #36534, #4722, .T. ) ;
#39264=CARTESIAN_POINT ( 'NONE',  ( 13.29196628380899980, -50.07647854234220119, -21.00283603054380066 ) ) ;
#39266=CARTESIAN_POINT ( 'NONE',  ( 56.33352089224590031, 13.89801324381519976, -15.47337191694060010 ) ) ;
#39267=CARTESIAN_POINT ( 'NONE',  ( 61.19909444736899928, -45.31215391586800223, -47.06069671806489652 ) ) ;
#39271=ORIENTED_EDGE ( 'NONE', *, *, #23754, .T. ) ;
#39272=CARTESIAN_POINT ( 'NONE',  ( 13.42257398911860022, -51.72201830638929465, -74.14993436883828792 ) ) ;
#39274=CARTESIAN_POINT ( 'NONE',  ( 43.44329010622809761, -46.02041590603030130, -7.898785361262961047 ) ) ;
#39276=CARTESIAN_POINT ( 'NONE',  ( 55.53661300022847769, -47.20923717753896653, -26.46481881287708759 ) ) ;
#39279=FACE_OUTER_BOUND ( 'NONE', #8178, .T. ) ;
#39281=CARTESIAN_POINT ( 'NONE',  ( 82.34888464648300044, 14.41279304669810024, -47.72707126332089445 ) ) ;
#39286=CARTESIAN_POINT ( 'NONE',  ( 49.20613926322570109, 22.63364074929049607, -55.12403394422909741 ) ) ;
#39289=CARTESIAN_POINT ( 'NONE',  ( 53.14599526630189530, -49.52280220221379636, -49.02433929921330247 ) ) ;
#39290=ORIENTED_EDGE ( 'NONE', *, *, #25931, .F. ) ;
#39294=CARTESIAN_POINT ( 'NONE',  ( 13.67284627086910120, 19.93818776675360027, -22.23398155374439966 ) ) ;
#39299=CARTESIAN_POINT ( 'NONE',  ( 52.60258329861409976, 18.59156606793389699, -48.51134384244380016 ) ) ;
#39300=CARTESIAN_POINT ( 'NONE',  ( 55.66436213888189855, -45.60096027170479971, -16.29539555431340148 ) ) ;
#39301=CARTESIAN_POINT ( 'NONE',  ( 54.18967173931659431, 16.81490735217030164, -26.03594187494229928 ) ) ;
#39303=CIRCLE ( 'NONE', #38476, 15.11955878774480233 ) ;
#39307=CARTESIAN_POINT ( 'NONE',  ( 10.87995450790350205, -64.97548900853969656, -17.51161086048150040 ) ) ;
#39308=CARTESIAN_POINT ( 'NONE',  ( 9.188454688195358600, 32.78433166906430074, -46.76666145987389456 ) ) ;
#39312=FACE_OUTER_BOUND ( 'NONE', #18706, .T. ) ;
#39314=DIRECTION ( 'NONE',  ( 0.9990957361526741076, 0.000000000000000000, -0.04251717301921900671 ) ) ;
#39315=CARTESIAN_POINT ( 'NONE',  ( 10.77136036876739844, -63.23172379110331320, -45.20469033881160215 ) ) ;
#39318=CARTESIAN_POINT ( 'NONE',  ( 68.36163517248512278, -30.78936114711470751, -18.19591817807315692 ) ) ;
#39319=CARTESIAN_POINT ( 'NONE',  ( 56.70659705232079517, 19.32440130277539936, -53.10139024778879957 ) ) ;
#39320=CARTESIAN_POINT ( 'NONE',  ( 47.26610112325450075, 22.82567072896360116, -75.56421356201970241 ) ) ;
#39324=CARTESIAN_POINT ( 'NONE',  ( 83.09574697842404589, -44.89486775114661299, -46.39646040884239397 ) ) ;
#39326=EDGE_CURVE ( 'NONE', #24020, #29481, #27031, .T. ) ;
#39329=DIRECTION ( 'NONE',  ( 0.000000000000000000, 0.000000000000000000, -1.000000000000000000 ) ) ;
#39330=CARTESIAN_POINT ( 'NONE',  ( 61.20224358684065891, -45.27433979179907197, -46.71246603851685819 ) ) ;
#39335=VECTOR ( 'NONE', #51575, 1000.000000000000000 ) ;
#39336=CARTESIAN_POINT ( 'NONE',  ( 12.06284766121009966, -63.44323389162830296, -46.39999999999999858 ) ) ;
#39339=CARTESIAN_POINT ( 'NONE',  ( 52.45428892279399946, 13.97507276140040133, -12.94524249092279966 ) ) ;
#39342=CARTESIAN_POINT ( 'NONE',  ( 47.30600330445400203, 23.48391298978570063, -74.19742682671839873 ) ) ;
#39344=CARTESIAN_POINT ( 'NONE',  ( 49.75282653525520260, -57.95720799465139805, -54.55458065461419892 ) ) ;
#39345=CARTESIAN_POINT ( 'NONE',  ( 68.13393739769620083, 11.88381105532070059, -71.50000000000000000 ) ) ;
#39347=CARTESIAN_POINT ( 'NONE',  ( 12.19720189296489998, 33.46095046226900394, -15.92873818749999870 ) ) ;
#39351=CARTESIAN_POINT ( 'NONE',  ( 54.46179591467679870, -50.62549687492020212, -76.64268959045750762 ) ) ;
#39352=CARTESIAN_POINT ( 'NONE',  ( -9.343064548044289097, 12.51679987183899811, -5.546829476069820686 ) ) ;
#39357=CARTESIAN_POINT ( 'NONE',  ( 14.27930865506306013, 21.26098553221025611, -75.92929758211228375 ) ) ;
#39358=CARTESIAN_POINT ( 'NONE',  ( 47.54404738341980163, 23.34326443908900117, -54.90429578540580025 ) ) ;
#39359=CARTESIAN_POINT ( 'NONE',  ( 61.12509698999170382, -45.25425853416980004, -27.63408038702889868 ) ) ;
#39363=CARTESIAN_POINT ( 'NONE',  ( 51.43588672793779892, 18.51358431124270254, -76.47300566802010735 ) ) ;
#39364=CARTESIAN_POINT ( 'NONE',  ( 52.82975622904280755, 18.42854261028849905, -48.47378032971769812 ) ) ;
#39365=DIRECTION ( 'NONE',  ( 0.2260571801428149230, 0.000000000000000000, -0.9741140340359946137 ) ) ;
#39366=CARTESIAN_POINT ( 'NONE',  ( 52.83236148840860125, -49.65955553127109567, -48.53481065559509489 ) ) ;
#39367=CARTESIAN_POINT ( 'NONE',  ( 49.81362442766570098, 22.09256562639079746, -54.04987025831400160 ) ) ;
#39368=CONICAL_SURFACE ( 'NONE', #19267, 1.942499999999999227, 0.8266833912447979493 ) ;
#39370=CARTESIAN_POINT ( 'NONE',  ( 85.38000601716228743, -48.61618894467930119, -60.34000486924599471 ) ) ;
#39371=CIRCLE ( 'NONE', #34333, 21.19999999999999929 ) ;
#39372=CARTESIAN_POINT ( 'NONE',  ( 60.45235380029059513, -30.32562723922359993, -16.15944822728640062 ) ) ;
#39374=CARTESIAN_POINT ( 'NONE',  ( 11.13393739769619906, 31.98148447116350113, -43.74438458204450342 ) ) ;
#39376=CIRCLE ( 'NONE', #5886, 1.999999999999998224 ) ;
#39378=DIRECTION ( 'NONE',  ( 1.000000000000000000, 0.000000000000000000, 0.000000000000000000 ) ) ;
#39380=ORIENTED_EDGE ( 'NONE', *, *, #44946, .T. ) ;
#39384=CARTESIAN_POINT ( 'NONE',  ( 57.14705973144530304, -45.14741832947689915, -25.37809429576289943 ) ) ;
#39385=DIRECTION ( 'NONE',  ( 0.000000000000000000, 0.000000000000000000, -1.000000000000000000 ) ) ;
#39387=CARTESIAN_POINT ( 'NONE',  ( 10.99717798698634752, 33.61421173664781037, -23.19667442668940893 ) ) ;
#39389=CARTESIAN_POINT ( 'NONE',  ( 11.01453361030839950, 32.67406340009490151, -23.98619660447929647 ) ) ;
#39396=EDGE_CURVE ( 'NONE', #42606, #5918, #15162, .T. ) ;
#39398=CARTESIAN_POINT ( 'NONE',  ( 62.97929662215530300, -29.57076698415579941, -16.19920473766450186 ) ) ;
#39400=CARTESIAN_POINT ( 'NONE',  ( 46.97454301875460203, -53.98875319215230206, -75.73879140141839628 ) ) ;
#39402=DIRECTION ( 'NONE',  ( 0.000000000000000000, 0.7371541402007423249, 0.6757246285173452716 ) ) ;
#39403=CARTESIAN_POINT ( 'NONE',  ( 41.23776877753270753, 13.84931952467590044, -5.742138678026360132 ) ) ;
#39404=FACE_OUTER_BOUND ( 'NONE', #38207, .T. ) ;
#39405=CIRCLE ( 'NONE', #26818, 20.00000000000000355 ) ;
#39406=CARTESIAN_POINT ( 'NONE',  ( 82.53147610877059037, -45.13461238702009837, -46.79182873648620244 ) ) ;
#39407=CARTESIAN_POINT ( 'NONE',  ( 65.10753665118122058, -31.99864820310045133, -17.50331349256994073 ) ) ;
#39409=B_SPLINE_CURVE_WITH_KNOTS ( 'NONE', 3,
 ( #27855, #19985, #16327, #15308, #7953, #28104, #36232, #24157, #31261, #40178, #47293, #4272, #47794, #3775, #19741, #28361 ),
 .UNSPECIFIED., .F., .F.,
 ( 4, 2, 2, 2, 2, 2, 2, 4 ),
 ( -1.047176999999999937E-15, 0.4421363464883489858, 0.9474350281893189063, 1.263246704252430019, 1.421152542283979914, 1.673801883134459878, 2.076007908835539872, 2.526493408504850269 ),
 .UNSPECIFIED. ) ;
#39411=EDGE_CURVE ( 'NONE', #47621, #43823, #49602, .T. ) ;
#39413=CARTESIAN_POINT ( 'NONE',  ( 55.53662353292170195, -47.20924349302610068, -26.46482561396789990 ) ) ;
#39414=CARTESIAN_POINT ( 'NONE',  ( 16.05644225716720186, -51.03148892433259931, -20.34167354763580349 ) ) ;
#39415=CARTESIAN_POINT ( 'NONE',  ( 76.37043116117959585, -8.469752128233089650, -12.66764180611509971 ) ) ;
#39417=CYLINDRICAL_SURFACE ( 'NONE', #34022, 0.9999999999999407141 ) ;
#39419=CARTESIAN_POINT ( 'NONE',  ( 47.18324198357279897, 23.57489020266570279, -54.61058319554400242 ) ) ;
#39421=CARTESIAN_POINT ( 'NONE',  ( 82.39374053741410364, -45.13655374397700371, -46.71923274431809858 ) ) ;
#39422=CARTESIAN_POINT ( 'NONE',  ( 57.48533814307809564, -50.45530859044179550, -53.13639308838089903 ) ) ;
#39423=CARTESIAN_POINT ( 'NONE',  ( 43.68128689219040695, 12.31476791676119831, -5.037759820107959641 ) ) ;
#39424=CARTESIAN_POINT ( 'NONE',  ( 47.62441104666342540, -54.51319350588585877, -74.50474471046057090 ) ) ;
#39426=CARTESIAN_POINT ( 'NONE',  ( 56.94228693352650339, -47.50625043831589522, -47.82842110489030318 ) ) ;
#39427=CARTESIAN_POINT ( 'NONE',  ( 65.43042069957887463, -49.21324915460706961, -70.54648330188271643 ) ) ;
#39429=CARTESIAN_POINT ( 'NONE',  ( 17.81969638158939873, -51.79813798162680172, -75.64877291256318870 ) ) ;
#39431=CARTESIAN_POINT ( 'NONE',  ( 45.23836003753899604, -43.83063101194750288, -5.450403507060779695 ) ) ;
#39442=ORIENTED_EDGE ( 'NONE', *, *, #9715, .T. ) ;
#39443=CARTESIAN_POINT ( 'NONE',  ( 17.50704397559620062, 21.63336578114690312, -76.12563501418109979 ) ) ;
#39444=EDGE_LOOP ( 'NONE', ( #14431, #23943, #24383, #38192 ) ) ;
#39445=ORIENTED_EDGE ( 'NONE', *, *, #42677, .T. ) ;
#39450=CARTESIAN_POINT ( 'NONE',  ( 61.51131554793239786, 14.10369252969250020, -47.28580145422539971 ) ) ;
#39456=CARTESIAN_POINT ( 'NONE',  ( 82.75389963950189554, 14.36256073625980001, -47.67227237920639737 ) ) ;
#39458=FACE_OUTER_BOUND ( 'NONE', #49076, .T. ) ;
#39459=ORIENTED_EDGE ( 'NONE', *, *, #2722, .T. ) ;
#39460=CARTESIAN_POINT ( 'NONE',  ( 59.34499803081116198, -28.79149204250002825, -15.68015151901640181 ) ) ;
#39461=CARTESIAN_POINT ( 'NONE',  ( 51.62415613633279321, -50.67669871992969632, -76.24933076846630797 ) ) ;
#39462=CARTESIAN_POINT ( 'NONE',  ( 60.27360767123079910, 14.56433066022209921, -47.49318409392830631 ) ) ;
#39463=DIRECTION ( 'NONE',  ( -0.7782863420137342558, -0.3536342755907660451, 0.5188575613424891708 ) ) ;
#39465=CARTESIAN_POINT ( 'NONE',  ( -2.700142691300089659, 17.56628513837100058, -5.083883929925409717 ) ) ;
#39466=EDGE_CURVE ( 'NONE', #33614, #49749, #18123, .T. ) ;
#39467=DIRECTION ( 'NONE',  ( 0.9441882088883092328, -0.3294064756441295039, 0.000000000000000000 ) ) ;
#39471=VERTEX_POINT ( 'NONE', #46184 ) ;
#39472=CARTESIAN_POINT ( 'NONE',  ( 56.72051766773449799, -50.68676931991499401, -53.84018978630579966 ) ) ;
#39473=CARTESIAN_POINT ( 'NONE',  ( 57.49678186962110260, 18.90849154042449953, -52.63232334799329237 ) ) ;
#39474=EDGE_CURVE ( 'NONE', #28709, #34084, #18976, .T. ) ;
#39477=CARTESIAN_POINT ( 'NONE',  ( 15.78591284857189869, 19.69271321420649912, -20.28298178678300090 ) ) ;
#39483=CARTESIAN_POINT ( 'NONE',  ( 48.50426931947900044, -54.16735222170059671, -55.28601062726929882 ) ) ;
#39484=FACE_OUTER_BOUND ( 'NONE', #18590, .T. ) ;
#39486=CARTESIAN_POINT ( 'NONE',  ( 47.69758263342730942, 23.27859210216669794, -55.15459985148470423 ) ) ;
#39487=VERTEX_POINT ( 'NONE', #29648 ) ;
#39489=DIRECTION ( 'NONE',  ( 1.000000000000000000, 0.000000000000000000, 0.000000000000000000 ) ) ;
#39492=CARTESIAN_POINT ( 'NONE',  ( 60.61713456004790146, -45.58380821826049356, -47.21957072048249415 ) ) ;
#39494=CARTESIAN_POINT ( 'NONE',  ( 83.63329895952738013, 13.29802447021414658, -46.55718444776781695 ) ) ;
#39495=CARTESIAN_POINT ( 'NONE',  ( 84.02703262422839714, 13.40384015226580061, -47.45290575524859378 ) ) ;
#39496=CARTESIAN_POINT ( 'NONE',  ( 8.133937397696209715, 23.57564693985150228, -21.14999999999999858 ) ) ;
#39498=CARTESIAN_POINT ( 'NONE',  ( 56.84932596551129791, 19.42421318737730118, -53.85230338955989993 ) ) ;
#39503=LINE ( 'NONE', #3602, #1880 ) ;
#39504=DIRECTION ( 'NONE',  ( 0.000000000000000000, 0.000000000000000000, -1.000000000000000000 ) ) ;
#39506=CARTESIAN_POINT ( 'NONE',  ( 9.182372922795538628, -63.76165471016090436, -46.66759804741280249 ) ) ;
#39509=CARTESIAN_POINT ( 'NONE',  ( 55.73977427078670388, 19.85292510813409805, -53.93776639284670438 ) ) ;
#39510=CARTESIAN_POINT ( 'NONE',  ( 57.34990408955430041, -45.12238703601330059, -25.32055789762510045 ) ) ;
#39512=ADVANCED_FACE ( 'NONE', ( #37792 ), #10532, .F. ) ;
#39514=CARTESIAN_POINT ( 'NONE',  ( 59.04235309263319920, -3.122828794254560059, -15.65226437496019685 ) ) ;
#39515=CARTESIAN_POINT ( 'NONE',  ( 58.41900308037850209, -49.15319073655110316, -51.55400195476909886 ) ) ;
#39519=CIRCLE ( 'NONE', #16919, 3.500000000000003109 ) ;
#39525=CARTESIAN_POINT ( 'NONE',  ( 56.88828947208789799, 19.38381105532069881, -75.24793329859650726 ) ) ;
#39527=CARTESIAN_POINT ( 'NONE',  ( 70.83745409581578656, -49.21324915460098026, -73.25000000000119371 ) ) ;
#39528=CARTESIAN_POINT ( 'NONE',  ( 61.14309852062039852, -45.32067553311819808, -46.99564627970399755 ) ) ;
#39531=CARTESIAN_POINT ( 'NONE',  ( 71.71126032029680175, 14.01986140997038888, -47.09707863094710945 ) ) ;
#39533=CARTESIAN_POINT ( 'NONE',  ( 11.19961949155312908, -65.24734059375452944, -18.17421237899869979 ) ) ;
#39536=CARTESIAN_POINT ( 'NONE',  ( 44.22606915973489805, -46.08296596967250025, -8.447826951465771117 ) ) ;
#39539=DIRECTION ( 'NONE',  ( -1.529205156547310004E-10, -1.048235172004079997E-08, -1.000000000000000000 ) ) ;
#39540=CARTESIAN_POINT ( 'NONE',  ( 11.04564840988309982, 33.94644972953989992, -17.95839446270849749 ) ) ;
#39541=DIRECTION ( 'NONE',  ( 1.687892000000000095E-11, 1.766113999999999920E-11, 1.000000000000000000 ) ) ;
#39542=CARTESIAN_POINT ( 'NONE',  ( 63.63879714068243487, 0.6399062447643286689, -17.33502972194290237 ) ) ;
#39544=CARTESIAN_POINT ( 'NONE',  ( 11.67619456822290047, 33.65927054772580362, -23.88710972541020183 ) ) ;
#39545=CARTESIAN_POINT ( 'NONE',  ( 49.40539548389219959, 22.26547577746109852, -54.15746054660889541 ) ) ;
#39547=CARTESIAN_POINT ( 'NONE',  ( 52.61723843343860096, -49.81156647556650086, -48.56633104006370161 ) ) ;
#39548=CIRCLE ( 'NONE', #27830, 2.999999999999999112 ) ;
#39549=EDGE_LOOP ( 'NONE', ( #6747, #49628, #42068 ) ) ;
#39551=CARTESIAN_POINT ( 'NONE',  ( 66.72561048563109409, -33.11618894467930829, -20.64999999980150136 ) ) ;
#39552=CARTESIAN_POINT ( 'NONE',  ( 57.77564497937559906, -3.116188944679349593, -20.65000000000000213 ) ) ;
#39555=CARTESIAN_POINT ( 'NONE',  ( 16.13393739769620083, -15.61618894467929941, -14.65000000000000036 ) ) ;
#39556=CARTESIAN_POINT ( 'NONE',  ( 55.17361021118440334, -45.21029328161770167, -14.82786001016749999 ) ) ;
#39560=ORIENTED_EDGE ( 'NONE', *, *, #36725, .F. ) ;
#39561=CARTESIAN_POINT ( 'NONE',  ( 11.28671405514150017, -65.00701117576899435, -16.86100849032779792 ) ) ;
#39562=CARTESIAN_POINT ( 'NONE',  ( 11.68049157650639991, 33.98099422647310774, -47.05230233363739956 ) ) ;
#39564=CARTESIAN_POINT ( 'NONE',  ( 48.89387259858359869, -53.88404306600559579, -54.59098453863079925 ) ) ;
#39565=CARTESIAN_POINT ( 'NONE',  ( 10.94680987515031489, -64.76538349226117930, -23.25394996400440917 ) ) ;
#39569=CARTESIAN_POINT ( 'NONE',  ( 11.13393739769619906, -63.48571094816200855, -43.92550228023370096 ) ) ;
#39572=ORIENTED_EDGE ( 'NONE', *, *, #1106, .F. ) ;
#39575=EDGE_CURVE ( 'NONE', #13982, #37163, #24087, .T. ) ;
#39579=CARTESIAN_POINT ( 'NONE',  ( 52.57481508192923059, 20.19967092288929678, -75.83555757118507756 ) ) ;
#39581=CARTESIAN_POINT ( 'NONE',  ( 50.00746865674540231, 21.72397341460670006, -53.49641930188690253 ) ) ;
#39584=DIRECTION ( 'NONE',  ( 1.000000000000000000, 0.000000000000000000, 0.000000000000000000 ) ) ;
#39589=AXIS2_PLACEMENT_3D ( 'NONE', #999, #21158, #5461 ) ;
#39591=AXIS2_PLACEMENT_3D ( 'NONE', #1926, #17907, #13222 ) ;
#39594=CARTESIAN_POINT ( 'NONE',  ( 47.30620416954659646, 23.48429288067650234, -74.14999584438369595 ) ) ;
#39596=ADVANCED_FACE ( 'NONE', ( #3186 ), #51395, .T. ) ;
#39598=CARTESIAN_POINT ( 'NONE',  ( 12.10148745386679892, 33.86065729770509591, -16.50605066005979893 ) ) ;
#39600=CARTESIAN_POINT ( 'NONE',  ( 52.82216258569669520, -49.58646061845040265, -27.28071896258420281 ) ) ;
#39602=CARTESIAN_POINT ( 'NONE',  ( 56.91185928905259317, -50.61618894550459657, -75.19908646239869654 ) ) ;
#39603=CARTESIAN_POINT ( 'NONE',  ( -10.28442671929420094, 11.53361155615709954, -5.475821530260660097 ) ) ;
#39606=CARTESIAN_POINT ( 'NONE',  ( 61.34198049900449945, 13.97791997643200190, -46.66621099661489325 ) ) ;
#39609=CARTESIAN_POINT ( 'NONE',  ( 53.05372066228549954, -49.54357925801589602, -48.79446872794070345 ) ) ;
#39610=CARTESIAN_POINT ( 'NONE',  ( 47.50357687577830035, 23.36731487144420072, -54.99836346755289895 ) ) ;
#39611=ADVANCED_FACE ( 'NONE', ( #14970 ), #35136, .T. ) ;
#39612=CARTESIAN_POINT ( 'NONE',  ( 60.26237441151779706, -45.38172583291230211, -27.01215158688860285 ) ) ;
#39614=CARTESIAN_POINT ( 'NONE',  ( 61.62035637548115119, -45.25224449890009737, -47.09707516299204144 ) ) ;
#39616=CARTESIAN_POINT ( 'NONE',  ( 51.09074887001380461, 17.58698902652399809, -76.44262319005990491 ) ) ;
#39617=CARTESIAN_POINT ( 'NONE',  ( 53.19709010659749993, 18.24734634467580463, -48.94481910643570188 ) ) ;
#39621=ORIENTED_EDGE ( 'NONE', *, *, #8384, .F. ) ;
#39624=CARTESIAN_POINT ( 'NONE',  ( 47.54281612864539852, -54.55267448867429891, -54.67232832126270381 ) ) ;
#39625=CARTESIAN_POINT ( 'NONE',  ( 63.02122824129657630, -31.65172625870799195, -17.11446970408973201 ) ) ;
#39627=CARTESIAN_POINT ( 'NONE',  ( 63.90257177041379322, -31.03871148548129710, -16.68334962132160015 ) ) ;
#39634=VERTEX_POINT ( 'NONE', #50618 ) ;
#39638=ORIENTED_EDGE ( 'NONE', *, *, #17095, .F. ) ;
#39639=CARTESIAN_POINT ( 'NONE',  ( 16.65420337941059969, -51.11618894467930119, -15.67544740040250062 ) ) ;
#39641=ORIENTED_EDGE ( 'NONE', *, *, #36893, .F. ) ;
#39645=EDGE_CURVE ( 'NONE', #5608, #40081, #7243, .T. ) ;
#39650=CARTESIAN_POINT ( 'NONE',  ( 60.19729760361229864, -28.87421560293969947, -15.80187452458650021 ) ) ;
#39652=CARTESIAN_POINT ( 'NONE',  ( 46.77112351560430170, -53.52311952442669707, -76.01558715013979395 ) ) ;
#39655=CARTESIAN_POINT ( 'NONE',  ( 44.37484003570580171, 14.76830914866819988, -8.485749550088890203 ) ) ;
#39656=CYLINDRICAL_SURFACE ( 'NONE', #36770, 1.999999999999999556 ) ;
#39657=CIRCLE ( 'NONE', #40505, 1.000000000000000666 ) ;
#39659=CARTESIAN_POINT ( 'NONE',  ( 84.25787305080559975, -43.86029743537079639, -47.19072229952409714 ) ) ;
#39662=VERTEX_POINT ( 'NONE', #11049 ) ;
#39663=CARTESIAN_POINT ( 'NONE',  ( 83.63329895952738013, 13.29802447021414658, -46.55718444776781695 ) ) ;
#39664=CARTESIAN_POINT ( 'NONE',  ( 15.91925957856740048, -50.98337423471310359, -20.31192411766179973 ) ) ;
#39665=CARTESIAN_POINT ( 'NONE',  ( 75.47850982819889509, 12.19658742805970064, -13.41229538484630091 ) ) ;
#39666=CARTESIAN_POINT ( 'NONE',  ( 61.62035637548115119, -45.25224449890009737, -47.09707516299204144 ) ) ;
#39669=CARTESIAN_POINT ( 'NONE',  ( -2.760456472307890152, -48.90492574716959950, -5.324092234941129931 ) ) ;
#39670=CARTESIAN_POINT ( 'NONE',  ( 47.18324198357279897, 23.57489020266570279, -54.61058319554400242 ) ) ;
#39674=CARTESIAN_POINT ( 'NONE',  ( 57.34403477439209240, -50.39786884706040127, -53.00646970444169881 ) ) ;
#39675=CARTESIAN_POINT ( 'NONE',  ( 42.63373765601389920, 12.86607404123980025, -5.023048285142680314 ) ) ;
#39676=CARTESIAN_POINT ( 'NONE',  ( 47.64143405400680109, -54.53488714545009941, -74.14999999999999147 ) ) ;
#39678=CARTESIAN_POINT ( 'NONE',  ( 57.08448514777830241, -47.43174880974720509, -47.79773139290949757 ) ) ;
#39680=ADVANCED_FACE ( 'NONE', ( #46967 ), #30939, .T. ) ;
#39682=CARTESIAN_POINT ( 'NONE',  ( 67.93183287108219304, -0.9264572295258779455, -17.84858513530449997 ) ) ;
#39683=CARTESIAN_POINT ( 'NONE',  ( 18.11569087717129634, -52.24722748763079494, -75.79330468503940210 ) ) ;
#39684=EDGE_CURVE ( 'NONE', #9603, #47075, #19799, .T. ) ;
#39687=CARTESIAN_POINT ( 'NONE',  ( 52.52075712594130152, -50.56176064652730417, -50.61493809237359898 ) ) ;
#39689=CARTESIAN_POINT ( 'NONE',  ( 45.14276784632605910, 14.67923546272599289, -8.929571664405379749 ) ) ;
#39690=CARTESIAN_POINT ( 'NONE',  ( 10.64863409883700029, 32.21085600226960111, -23.66469670114080159 ) ) ;
#39694=ORIENTED_EDGE ( 'NONE', *, *, #49196, .T. ) ;
#39695=CARTESIAN_POINT ( 'NONE',  ( 17.21347160910339724, 21.88381105532300097, -76.14999999999999147 ) ) ;
#39696=ORIENTED_EDGE ( 'NONE', *, *, #3394, .T. ) ;
#39700=CARTESIAN_POINT ( 'NONE',  ( 57.24929578595760660, -52.61618894467940066, -63.99406948319280275 ) ) ;
#39705=DIRECTION ( 'NONE',  ( -1.000000000000000000, -7.683667316014053881E-33, 8.592609827796581962E-15 ) ) ;
#39707=CARTESIAN_POINT ( 'NONE',  ( 68.13393739769620083, 11.88381105532070059, -71.50000000000000000 ) ) ;
#39713=CARTESIAN_POINT ( 'NONE',  ( 60.70528289702870239, 14.47951718819379963, -47.69124897247409933 ) ) ;
#39715=CIRCLE ( 'NONE', #10431, 35.00000000000000000 ) ;
#39717=CARTESIAN_POINT ( 'NONE',  ( -3.373810796937729783, 17.44610948361469838, -5.485032747920929985 ) ) ;
#39721=ORIENTED_EDGE ( 'NONE', *, *, #37680, .T. ) ;
#39724=CARTESIAN_POINT ( 'NONE',  ( 42.48913757721220463, 14.65938426827190000, -7.200519650645810010 ) ) ;
#39727=CARTESIAN_POINT ( 'NONE',  ( 15.58442563903700062, 19.61232422376169993, -20.41433498000760238 ) ) ;
#39728=CARTESIAN_POINT ( 'NONE',  ( 50.03007040746459921, 10.05946586878370042, -78.14999999999999147 ) ) ;
#39731=CARTESIAN_POINT ( 'NONE',  ( 48.56553214184410194, -54.10406106784840574, -54.94095612633750392 ) ) ;
#39732=CARTESIAN_POINT ( 'NONE',  ( 52.10267377731729965, -33.11618894492853116, -20.31847448329631689 ) ) ;
#39737=ADVANCED_FACE ( 'NONE', ( #18894 ), #38836, .T. ) ;
#39741=CARTESIAN_POINT ( 'NONE',  ( 61.75019796695539753, 13.88381105532070059, -46.37203261889099792 ) ) ;
#39744=CARTESIAN_POINT ( 'NONE',  ( 60.91168278986669549, -45.44839912269959825, -47.20849308954799994 ) ) ;
#39748=CARTESIAN_POINT ( 'NONE',  ( 9.127429636406484192, 23.77844269387289700, -22.14349223871028016 ) ) ;
#39753=AXIS2_PLACEMENT_3D ( 'NONE', #15994, #43770, #47710 ) ;
#39754=ORIENTED_EDGE ( 'NONE', *, *, #29048, .F. ) ;
#39755=CARTESIAN_POINT ( 'NONE',  ( 76.87859648677320479, 11.88381402801379849, -14.85884684523960075 ) ) ;
#39757=CARTESIAN_POINT ( 'NONE',  ( 12.64313521567289911, 34.23242425601760175, -47.04313497446949555 ) ) ;
#39758=CARTESIAN_POINT ( 'NONE',  ( 10.85544419465600008, -64.15949727455540597, -45.65651250914780235 ) ) ;
#39766=EDGE_CURVE ( 'NONE', #5505, #2815, #8194, .T. ) ;
#39767=CARTESIAN_POINT ( 'NONE',  ( 65.19625039218108498, 0.4699309295582059787, -17.22242890042259944 ) ) ;
#39768=CARTESIAN_POINT ( 'NONE',  ( 51.95459423065859994, -49.70792072429919983, -76.89034159680979030 ) ) ;
#39769=DIRECTION ( 'NONE',  ( 0.000000000000000000, -1.000000000000000000, 0.000000000000000000 ) ) ;
#39772=CARTESIAN_POINT ( 'NONE',  ( 76.62512003803935556, 11.98806601119159509, -14.19602650844148251 ) ) ;
#39776=CARTESIAN_POINT ( 'NONE',  ( 12.69633964006179916, -49.98156586428169845, -21.09933892718569837 ) ) ;
#39777=CARTESIAN_POINT ( 'NONE',  ( 54.08392444393659559, 19.39418736748219629, -76.77911274294029909 ) ) ;
#39779=CARTESIAN_POINT ( 'NONE',  ( 57.50723796698959944, 13.88381105532070059, -17.93020914085149897 ) ) ;
#39780=CARTESIAN_POINT ( 'NONE',  ( 61.28265261588620660, -45.34131656260610299, -47.23924683292639770 ) ) ;
#39784=VERTEX_POINT ( 'NONE', #12328 ) ;
#39786=CARTESIAN_POINT ( 'NONE',  ( 14.13833173590930059, -51.13036009974659635, -74.14993170018701107 ) ) ;
#39787=CARTESIAN_POINT ( 'NONE',  ( 47.25314650905760772, -54.75284751476729639, -54.62484584475070193 ) ) ;
#39788=CARTESIAN_POINT ( 'NONE',  ( 41.40756764072759921, -44.77159127043780273, -5.393983506378570603 ) ) ;
#39791=CYLINDRICAL_SURFACE ( 'NONE', #46546, 1.999999999999996891 ) ;
#39792=CARTESIAN_POINT ( 'NONE',  ( 10.73482432378980000, 33.71481228277630038, -18.15071127990200139 ) ) ;
#39796=EDGE_CURVE ( 'NONE', #42552, #37955, #8848, .T. ) ;
#39800=VERTEX_POINT ( 'NONE', #8921 ) ;
#39801=CARTESIAN_POINT ( 'NONE',  ( 52.83551392347279574, -49.68567921497080420, -48.92570524573309854 ) ) ;
#39806=CARTESIAN_POINT ( 'NONE',  ( 84.13361756236649569, 12.76145366115379964, -46.96659941728370313 ) ) ;
#39808=CARTESIAN_POINT ( 'NONE',  ( 52.82359344163219816, 18.46824642947949968, -48.95125676800460468 ) ) ;
#39809=CARTESIAN_POINT ( 'NONE',  ( 56.39862374920090105, -45.18896474930410534, -16.03846417670529689 ) ) ;
#39811=B_SPLINE_CURVE_WITH_KNOTS ( 'NONE', 3,
 ( #11251, #27213, #43226, #7318, #51341, #47420, #48966, #40055, #45020, #36618, #44499, #19868, #215 ),
 .UNSPECIFIED., .F., .F.,
 ( 4, 2, 2, 1, 2, 2, 4 ),
 ( 0.000000000000000000, 0.2500000000000435207, 0.3750000000000643929, 0.4375000000000756062, 0.4687500000000812128, 0.5000000000000868194, 1.000000000000000000 ),
 .UNSPECIFIED. ) ;
#39814=ORIENTED_EDGE ( 'NONE', *, *, #19984, .F. ) ;
#39815=CARTESIAN_POINT ( 'NONE',  ( 11.50351869910530134, -65.28212171173150580, -17.32566767997679946 ) ) ;
#39816=CARTESIAN_POINT ( 'NONE',  ( 10.32439802925660111, 33.01400591537749563, -46.37725779926459779 ) ) ;
#39820=CARTESIAN_POINT ( 'NONE',  ( 8.798174420955659158, 31.95288804203559607, -46.67020513285999783 ) ) ;
#39825=AXIS2_PLACEMENT_3D ( 'NONE', #46904, #38775, #22239 ) ;
#39826=CARTESIAN_POINT ( 'NONE',  ( 11.13393739769619906, -63.23117314113459031, -43.74478398217730302 ) ) ;
#39827=CARTESIAN_POINT ( 'NONE',  ( 70.03247032090600044, 18.72622661238320063, -71.50000000000139266 ) ) ;
#39829=EDGE_CURVE ( 'NONE', #36880, #22605, #37606, .T. ) ;
#39832=CARTESIAN_POINT ( 'NONE',  ( 13.73896035130837490, -52.05916771826542089, -75.36997958382971774 ) ) ;
#39834=VERTEX_POINT ( 'NONE', #24348 ) ;
#39837=DIRECTION ( 'NONE',  ( 0.000000000000000000, -1.000000000000000000, 0.000000000000000000 ) ) ;
#39842=DIRECTION ( 'NONE',  ( 0.000000000000000000, 0.000000000000000000, -1.000000000000000000 ) ) ;
#39844=VERTEX_POINT ( 'NONE', #44289 ) ;
#39846=AXIS2_PLACEMENT_3D ( 'NONE', #47878, #51800, #15392 ) ;
#39849=AXIS2_PLACEMENT_3D ( 'NONE', #39864, #3194, #3966 ) ;
#39850=CARTESIAN_POINT ( 'NONE',  ( 46.35275103504439898, 21.67755452994670406, -76.14999999999999147 ) ) ;
#39854=CARTESIAN_POINT ( 'NONE',  ( 12.17667205660850094, 33.72359997743659932, -16.26506704563800199 ) ) ;
#39858=CARTESIAN_POINT ( 'NONE',  ( 57.06416426806980269, -50.61857174473429666, -74.65301306984240171 ) ) ;
#39860=CARTESIAN_POINT ( 'NONE',  ( 10.52466370152206565, -55.22087153724935860, -45.55758753228428048 ) ) ;
#39863=CARTESIAN_POINT ( 'NONE',  ( 61.28624124790810157, 14.05922653848760007, -47.08353149416500827 ) ) ;
#39864=CARTESIAN_POINT ( 'NONE',  ( 57.77564497937559906, -28.11618894467929763, -20.65000000000000213 ) ) ;
#39867=CARTESIAN_POINT ( 'NONE',  ( 52.96846357502160174, -49.58824783477410136, -48.76456334744820253 ) ) ;
#39869=CARTESIAN_POINT ( 'NONE',  ( 58.60333746479689410, -45.35543772810689944, -26.24757126836300003 ) ) ;
#39871=CARTESIAN_POINT ( 'NONE',  ( 61.40708214766610240, 14.14652340182849954, -47.36186230186000046 ) ) ;
#39874=CARTESIAN_POINT ( 'NONE',  ( 51.15450546912109786, 17.91792957071369941, -76.44814621710780500 ) ) ;
#39875=CARTESIAN_POINT ( 'NONE',  ( 53.45906946093850109, 18.13273169594320322, -49.00044373679480003 ) ) ;
#39876=CARTESIAN_POINT ( 'NONE',  ( 48.93887227096879400, 13.88381105532070059, -44.18916148508130703 ) ) ;
#39878=B_SPLINE_CURVE_WITH_KNOTS ( 'NONE', 3,
 ( #24551, #7581, #35341, #51343, #31906, #47421, #28239, #27473, #8340, #43983, #15441, #23525, #11775, #32158 ),
 .UNSPECIFIED., .F., .F.,
 ( 4, 2, 2, 2, 2, 2, 4 ),
 ( 3.901664560647569946, 4.407177605192729608, 8.834505823316810336, 16.99747883129379744, 26.70074659151990204, 31.55238047163300052, 38.13645368273460434 ),
 .UNSPECIFIED. ) ;
#39879=CIRCLE ( 'NONE', #14776, 2.000000000000000000 ) ;
#39882=CARTESIAN_POINT ( 'NONE',  ( 47.49651569575760135, -54.60323047930179996, -54.97533461431780211 ) ) ;
#39885=CARTESIAN_POINT ( 'NONE',  ( 62.08467266925860173, -31.29317986265380114, -16.78003447424929817 ) ) ;
#39887=CARTESIAN_POINT ( 'NONE',  ( 11.13393739769619906, 32.24192143019860168, -43.75640488079960733 ) ) ;
#39897=CARTESIAN_POINT ( 'NONE',  ( 50.37360157917204617, -30.41936351533771088, -16.20717240613429766 ) ) ;
#39898=VERTEX_POINT ( 'NONE', #48486 ) ;
#39899=EDGE_CURVE ( 'NONE', #16152, #30077, #6995, .T. ) ;
#39900=CARTESIAN_POINT ( 'NONE',  ( 11.67619942398489918, -64.89165360645620240, -45.08494251881790404 ) ) ;
#39902=ORIENTED_EDGE ( 'NONE', *, *, #8895, .F. ) ;
#39909=CARTESIAN_POINT ( 'NONE',  ( 10.63085952368594889, 33.60671464058745528, -18.12437699077790398 ) ) ;
#39910=CARTESIAN_POINT ( 'NONE',  ( 59.34191102089160097, -28.54411838181400185, -15.68387058390849731 ) ) ;
#39911=CARTESIAN_POINT ( 'NONE',  ( 12.07188845762700069, -65.28371144306440499, -23.58588067924090126 ) ) ;
#39914=CARTESIAN_POINT ( 'NONE',  ( 41.10495153987889694, 13.67547663053780127, -5.488531527733360171 ) ) ;
#39915=AXIS2_PLACEMENT_3D ( 'NONE', #30935, #22813, #18372 ) ;
#39918=CARTESIAN_POINT ( 'NONE',  ( 83.85202357338310719, -44.35879849486410365, -46.78691132286899546 ) ) ;
#39919=AXIS2_PLACEMENT_3D ( 'NONE', #48824, #12929, #4791 ) ;
#39923=CARTESIAN_POINT ( 'NONE',  ( 52.77132806972499424, -49.69320935574780407, -28.08932869332100069 ) ) ;
#39924=CARTESIAN_POINT ( 'NONE',  ( 13.94847430741750038, -50.27910463884859382, -20.89779807319060012 ) ) ;
#39925=CARTESIAN_POINT ( 'NONE',  ( 75.44242163376010524, 10.98619150729950000, -13.23847946865800118 ) ) ;
#39929=CARTESIAN_POINT ( 'NONE',  ( -8.077363885194191795, -45.04970852165219952, -5.734713034113010366 ) ) ;
#39932=LINE ( 'NONE', #23657, #23652 ) ;
#39934=CARTESIAN_POINT ( 'NONE',  ( 57.55751162063140214, -50.09049722514059511, -52.57651812413949699 ) ) ;
#39935=CARTESIAN_POINT ( 'NONE',  ( 43.46307289448610334, 11.85965047528820016, -4.765184494693460060 ) ) ;
#39936=EDGE_CURVE ( 'NONE', #19952, #40162, #43196, .T. ) ;
#39937=CARTESIAN_POINT ( 'NONE',  ( 16.13393739769620083, -15.61618894467929941, -74.14999999999999147 ) ) ;
#39942=CARTESIAN_POINT ( 'NONE',  ( 17.21347160910390173, -53.11618894467930119, -76.14999999999999147 ) ) ;
#39945=CARTESIAN_POINT ( 'NONE',  ( 55.78679745002460066, -46.85824937871690565, -46.15739089836610276 ) ) ;
#39947=CARTESIAN_POINT ( 'NONE',  ( 8.808908491334550561, 32.01182072428549930, -46.67060441505820023 ) ) ;
#39952=CARTESIAN_POINT ( 'NONE',  ( 17.85447849914849883, 20.77357945327109690, -75.79069550273320033 ) ) ;
#39953=VERTEX_POINT ( 'NONE', #1821 ) ;
#39956=CARTESIAN_POINT ( 'NONE',  ( 56.54338727600670467, -46.22346027527899537, -26.26862031791669949 ) ) ;
#39958=CARTESIAN_POINT ( 'NONE',  ( 61.55801500889180033, 14.08519212220829964, -47.24870750647819762 ) ) ;
#39962=DIRECTION ( 'NONE',  ( 1.000000000000000000, 0.000000000000000000, 0.000000000000000000 ) ) ;
#39963=CARTESIAN_POINT ( 'NONE',  ( 16.13393739707289853, -15.61618894541809865, -10.45000000021869901 ) ) ;
#39968=CARTESIAN_POINT ( 'NONE',  ( 60.76852316973799617, 14.41550492289180063, -47.61461981903249807 ) ) ;
#39970=EDGE_CURVE ( 'NONE', #27228, #38928, #33240, .T. ) ;
#39971=EDGE_CURVE ( 'NONE', #2811, #5359, #27462, .T. ) ;
#39972=DIRECTION ( 'NONE',  ( 0.000000000000000000, 0.000000000000000000, -1.000000000000000000 ) ) ;
#39974=CARTESIAN_POINT ( 'NONE',  ( 41.06001671441610057, -44.29932858193069478, -3.719606166043679885 ) ) ;
#39975=CARTESIAN_POINT ( 'NONE',  ( -7.100262879277110528, 14.45415374298890043, -4.868184076090540380 ) ) ;
#39977=CARTESIAN_POINT ( 'NONE',  ( 57.57964031801950000, 14.54583681789700123, -26.30006412837039775 ) ) ;
#39979=ORIENTED_EDGE ( 'NONE', *, *, #5333, .F. ) ;
#39980=FACE_OUTER_BOUND ( 'NONE', #31089, .T. ) ;
#39982=CARTESIAN_POINT ( 'NONE',  ( 11.74952994020519981, 33.73588971661489921, -45.42180763390059894 ) ) ;
#39987=CARTESIAN_POINT ( 'NONE',  ( 50.03007040746459921, 10.05946586878370042, -78.14999999999999147 ) ) ;
#39988=CARTESIAN_POINT ( 'NONE',  ( 13.29299421255960034, 18.84434171226279986, -21.00266242150379981 ) ) ;
#39990=CARTESIAN_POINT ( 'NONE',  ( 47.04950481043260169, 23.22170069367189882, -75.29714959418029707 ) ) ;
#39991=CARTESIAN_POINT ( 'NONE',  ( 48.57498399731990446, -54.11662796927669916, -55.03331795735149967 ) ) ;
#39992=CARTESIAN_POINT ( 'NONE',  ( -5.866062602303799167, -15.61618894467929586, -13.15000000000000036 ) ) ;
#39994=DIRECTION ( 'NONE',  ( 0.5685928097855371677, 0.5944782866685501821, -0.5685928097855381669 ) ) ;
#39996=VERTEX_POINT ( 'NONE', #6531 ) ;
#40001=CARTESIAN_POINT ( 'NONE',  ( 60.87670858091210135, -45.49189414910050289, -47.32752941579799710 ) ) ;
#40002=CARTESIAN_POINT ( 'NONE',  ( 48.03526516117433687, -54.27886751425135259, -54.71370355240628669 ) ) ;
#40011=ORIENTED_EDGE ( 'NONE', *, *, #8398, .F. ) ;
#40012=CIRCLE ( 'NONE', #37462, 1.999999999999999556 ) ;
#40013=ORIENTED_EDGE ( 'NONE', *, *, #9772, .T. ) ;
#40014=DIRECTION ( 'NONE',  ( 0.000000000000000000, -1.000000000000000000, 0.000000000000000000 ) ) ;
#40016=CARTESIAN_POINT ( 'NONE',  ( 76.39175890687408810, -17.20318815803477008, -12.76101989214891042 ) ) ;
#40017=CARTESIAN_POINT ( 'NONE',  ( 52.33875389174439619, -52.31399363568380068, -53.58658487175770091 ) ) ;
#40022=CARTESIAN_POINT ( 'NONE',  ( 56.37791752366599951, -50.59128047935769956, -52.96495778846580293 ) ) ;
#40024=CARTESIAN_POINT ( 'NONE',  ( 61.86520133577609926, -0.04549255600530619642, -16.70179762356000097 ) ) ;
#40025=CARTESIAN_POINT ( 'NONE',  ( 51.85719455852780158, -49.29163194590670116, -77.06877200303979691 ) ) ;
#40028=CARTESIAN_POINT ( 'NONE',  ( 52.27433127813800695, -49.79152405959709426, -77.19764541630020460 ) ) ;
#40033=CARTESIAN_POINT ( 'NONE',  ( 13.03464451127720025, -50.12146493690359961, -21.08705571738870077 ) ) ;
#40034=CARTESIAN_POINT ( 'NONE',  ( 54.70720528295199614, 19.38381105532069881, -76.79588817750999397 ) ) ;
#40037=CARTESIAN_POINT ( 'NONE',  ( 66.23540447448809232, -49.95860450174330225, -73.25000000000169109 ) ) ;
#40039=DIRECTION ( 'NONE',  ( 0.7702700562049007438, -0.6377178376947748584, -1.307070999999999778E-15 ) ) ;
#40042=CARTESIAN_POINT ( 'NONE',  ( 17.80204587918421311, -52.64324137133318970, -76.02665054607163597 ) ) ;
#40044=CARTESIAN_POINT ( 'NONE',  ( 47.20214429186539462, 22.74469373903359681, -75.65864031442400517 ) ) ;
#40045=CARTESIAN_POINT ( 'NONE',  ( 47.40268433751139554, -54.65101820823279866, -54.72406345013450135 ) ) ;
#40048=( BOUNDED_CURVE ( )  B_SPLINE_CURVE ( 3, ( #29032, #21665, #9640, #13079 ),
 .UNSPECIFIED., .F., .T. ) 
 B_SPLINE_CURVE_WITH_KNOTS ( ( 4, 4 ),
 ( 0.7390344460998500287, 0.8357509604174070406 ),
 .UNSPECIFIED. ) 
 CURVE ( )  GEOMETRIC_REPRESENTATION_ITEM ( )  RATIONAL_B_SPLINE_CURVE ( ( 1.000000000000000000, 0.9992206448841429722, 0.9992206448841429722, 1.000000000000000000 ) ) 
 REPRESENTATION_ITEM ( '' )  );
#40052=CARTESIAN_POINT ( 'NONE',  ( 10.98409431999460040, 33.91773787654379646, -18.15364188623160047 ) ) ;
#40054=CARTESIAN_POINT ( 'NONE',  ( 60.91034051252194104, 14.19489810164233567, -46.97125969379186472 ) ) ;
#40055=CARTESIAN_POINT ( 'NONE',  ( 11.30082206529223043, 33.08990382518435780, -24.05782791655008879 ) ) ;
#40056=DIRECTION ( 'NONE',  ( 0.000000000000000000, 1.000000000000000000, 0.000000000000000000 ) ) ;
#40057=VERTEX_POINT ( 'NONE', #36611 ) ;
#40058=CARTESIAN_POINT ( 'NONE',  ( 52.97994255623930115, -49.61893679407219793, -49.03242412254559923 ) ) ;
#40059=ORIENTED_EDGE ( 'NONE', *, *, #43889, .F. ) ;
#40061=DIRECTION ( 'NONE',  ( 0.000000000000000000, 0.000000000000000000, 1.000000000000000000 ) ) ;
#40062=CARTESIAN_POINT ( 'NONE',  ( 11.89321781987602833, 34.20365306160432795, -18.08603052195102379 ) ) ;
#40063=CARTESIAN_POINT ( 'NONE',  ( 84.44784216359251161, 11.88381105532070059, -47.47585302082339354 ) ) ;
#40064=CARTESIAN_POINT ( 'NONE',  ( 54.64278745374110002, 16.37561111237029721, -26.20171088721290076 ) ) ;
#40066=CARTESIAN_POINT ( 'NONE',  ( 52.74562310603300119, 18.50712734077499988, -48.86764753959050012 ) ) ;
#40067=CARTESIAN_POINT ( 'NONE',  ( 56.79701897584680381, -45.18238399616610224, -16.80948030656859871 ) ) ;
#40072=CARTESIAN_POINT ( 'NONE',  ( 11.56756868770579949, -65.34628264660689467, -17.53311441804959969 ) ) ;
#40073=CARTESIAN_POINT ( 'NONE',  ( 10.43078750819270084, 32.63024664643640449, -45.92124766861530105 ) ) ;
#40074=CARTESIAN_POINT ( 'NONE',  ( -9.882013117715120032, -40.49932216338130075, -19.14999999999999858 ) ) ;
#40076=CARTESIAN_POINT ( 'NONE',  ( 48.48453225901420183, -53.88010102980479843, -54.18220335411630373 ) ) ;
#40077=CARTESIAN_POINT ( 'NONE',  ( 11.36441734053757280, -65.23609907320785339, -22.79629275943423750 ) ) ;
#40080=VECTOR ( 'NONE', #9909, 1000.000000000000000 ) ;
#40081=VERTEX_POINT ( 'NONE', #39788 ) ;
#40083=DIRECTION ( 'NONE',  ( 0.000000000000000000, -1.000000000000000000, 0.000000000000000000 ) ) ;
#40085=ORIENTED_EDGE ( 'NONE', *, *, #34427, .F. ) ;
#40086=CARTESIAN_POINT ( 'NONE',  ( 82.75389963950320293, -45.59493862562369770, -47.67227237921210303 ) ) ;
#40088=CARTESIAN_POINT ( 'NONE',  ( 13.39998208317153328, -51.78678246883065839, -74.34716300802820399 ) ) ;
#40092=CARTESIAN_POINT ( 'NONE',  ( 57.20288283122350492, -50.17392941253179828, -52.64687565050539320 ) ) ;
#40093=CARTESIAN_POINT ( 'NONE',  ( 49.45585557151159861, 22.20491319630109928, -54.07529678225080261 ) ) ;
#40095=EDGE_CURVE ( 'NONE', #18259, #35705, #985, .T. ) ;
#40097=CARTESIAN_POINT ( 'NONE',  ( 55.22814166963710392, 19.75351993034290032, -75.19629012753209452 ) ) ;
#40103=CARTESIAN_POINT ( 'NONE',  ( 47.16988561617409914, 23.37564389197909875, -74.94862676396610368 ) ) ;
#40104=DIRECTION ( 'NONE',  ( -0.000000000000000000, 0.7371541402007413257, 0.6757246285173463818 ) ) ;
#40106=VECTOR ( 'NONE', #19654, 1000.000000000000000 ) ;
#40112=CARTESIAN_POINT ( 'NONE',  ( 54.14149310402689963, -50.61618454481969565, -76.93510071694009866 ) ) ;
#40117=CARTESIAN_POINT ( 'NONE',  ( 61.39316702964359962, 13.94954103750900032, -46.44855131092970169 ) ) ;
#40119=ORIENTED_EDGE ( 'NONE', *, *, #15560, .T. ) ;
#40120=CARTESIAN_POINT ( 'NONE',  ( 52.82466438858409674, -49.66358825752709549, -48.56035088502149222 ) ) ;
#40121=CARTESIAN_POINT ( 'NONE',  ( 57.37879763608390249, -45.44474840326299869, -26.07263843129119962 ) ) ;
#40123=CARTESIAN_POINT ( 'NONE',  ( 56.84321736728299612, 14.68190763298639823, -26.22409755557089994 ) ) ;
#40125=CARTESIAN_POINT ( 'NONE',  ( 50.12211818213420145, 17.38380696780440005, -76.14999999999999147 ) ) ;
#40126=CARTESIAN_POINT ( 'NONE',  ( 52.94725091888329871, 18.37265018205049572, -48.86448475008189973 ) ) ;
#40128=DIRECTION ( 'NONE',  ( 0.000000000000000000, 0.000000000000000000, 1.000000000000000000 ) ) ;
#40131=CARTESIAN_POINT ( 'NONE',  ( 47.64370562464430492, -54.49759886933879471, -54.72342076385189813 ) ) ;
#40132=CARTESIAN_POINT ( 'NONE',  ( -7.106986606757430103, 14.44895595925419940, -4.821389474212189441 ) ) ;
#40134=CARTESIAN_POINT ( 'NONE',  ( 59.10309207328680259, -28.11008969156920045, -15.65534454924780228 ) ) ;
#40143=CIRCLE ( 'NONE', #25070, 1.999999999999998668 ) ;
#40144=CARTESIAN_POINT ( 'NONE',  ( 51.17461318815491467, 0.4193470954621815738, -17.11446460828111427 ) ) ;
#40145=EDGE_LOOP ( 'NONE', ( #8327, #43195, #15168, #20461 ) ) ;
#40146=CARTESIAN_POINT ( 'NONE',  ( 12.89514948620979951, -65.50886967600349919, -47.53407058462189383 ) ) ;
#40157=EDGE_CURVE ( 'NONE', #21630, #9438, #33788, .T. ) ;
#40159=AXIS2_PLACEMENT_3D ( 'NONE', #25013, #36833, #20573 ) ;
#40161=( NAMED_UNIT ( * ) PLANE_ANGLE_UNIT ( ) SI_UNIT ( $, .RADIAN. ) );
#40162=VERTEX_POINT ( 'NONE', #22170 ) ;
#40163=CARTESIAN_POINT ( 'NONE',  ( 11.75958203967580040, -63.96014122186749518, -24.73059913046229852 ) ) ;
#40165=CARTESIAN_POINT ( 'NONE',  ( 40.99540355667089386, 13.76721783747789907, -5.546227284263019364 ) ) ;
#40166=CARTESIAN_POINT ( 'NONE',  ( 14.40490240792330034, 20.47201121247589839, -75.55956264724760274 ) ) ;
#40168=CARTESIAN_POINT ( 'NONE',  ( 83.88693549187640031, -44.43477735121779659, -47.02124945944449763 ) ) ;
#40169=DIRECTION ( 'NONE',  ( -0.3918900565005491998, -0.9200120562340454722, 0.000000000000000000 ) ) ;
#40172=CARTESIAN_POINT ( 'NONE',  ( 52.71556874866190157, -49.72995812607539534, -28.08384389970240136 ) ) ;
#40173=CARTESIAN_POINT ( 'NONE',  ( 13.73505343097379949, -50.20716417821699906, -20.93075220000860170 ) ) ;
#40174=CARTESIAN_POINT ( 'NONE',  ( 75.40827277404349616, 9.774041233901940018, -13.07349299794950070 ) ) ;
#40176=CARTESIAN_POINT ( 'NONE',  ( 75.45689852989164592, 12.50467538828190328, -13.48414116180180145 ) ) ;
#40177=EDGE_CURVE ( 'NONE', #51255, #25744, #2018, .T. ) ;
#40178=CARTESIAN_POINT ( 'NONE',  ( 12.98723924884970060, -50.01451382913280241, -21.05373176175340078 ) ) ;
#40179=VERTEX_POINT ( 'NONE', #17997 ) ;
#40181=CARTESIAN_POINT ( 'NONE',  ( -5.240462745371109676, -47.41486970062130268, -5.522706056646890183 ) ) ;
#40183=CARTESIAN_POINT ( 'NONE',  ( 47.32156641489019933, 23.47414238136689946, -54.76481957694370095 ) ) ;
#40185=AXIS2_PLACEMENT_3D ( 'NONE', #48325, #11402, #40203 ) ;
#40187=CARTESIAN_POINT ( 'NONE',  ( 68.13393739769847457, -50.70395984888145335, -72.15645085170113759 ) ) ;
#40189=CARTESIAN_POINT ( 'NONE',  ( 42.68710801736580152, 12.13362923386000070, -4.456284347609099861 ) ) ;
#40192=CARTESIAN_POINT ( 'NONE',  ( 57.69561854573869653, -47.11155889976559763, -47.75703836848589390 ) ) ;
#40202=CARTESIAN_POINT ( 'NONE',  ( 10.97210468079041235, -63.46994206267282834, -23.98816728309422075 ) ) ;
#40203=DIRECTION ( 'NONE',  ( 0.000000000000000000, 0.000000000000000000, -1.000000000000000000 ) ) ;
#40206=CARTESIAN_POINT ( 'NONE',  ( 17.91138945588609843, 20.67521890232639947, -75.71427953954510315 ) ) ;
#40214=DIRECTION ( 'NONE',  ( 0.000000000000000000, 0.000000000000000000, 1.000000000000000000 ) ) ;
#40218=CARTESIAN_POINT ( 'NONE',  ( 57.59061018188805292, -45.77595549251508800, -26.30140927225744818 ) ) ;
#40222=ORIENTED_EDGE ( 'NONE', *, *, #1600, .F. ) ;
#40226=CIRCLE ( 'NONE', #25985, 1.000000000000000888 ) ;
#40227=CARTESIAN_POINT ( 'NONE',  ( 60.70907960343409826, 14.40011400920250040, -47.54491343677150184 ) ) ;
#40230=CARTESIAN_POINT ( 'NONE',  ( 49.27319349346669952, 14.34782011532229973, -11.42332069360450042 ) ) ;
#40231=DIRECTION ( 'NONE',  ( -0.4872913772396108012, -0.8732394366197184787, 0.000000000000000000 ) ) ;
#40232=CARTESIAN_POINT ( 'NONE',  ( -9.455812343875759751, 12.48625188284650100, -5.621938366128030218 ) ) ;
#40233=CARTESIAN_POINT ( 'NONE',  ( 47.18324200477937325, 23.57489024965510183, -74.17387245455509515 ) ) ;
#40234=CARTESIAN_POINT ( 'NONE',  ( 55.69413454653252415, 14.72513308957886480, -17.00762811886805181 ) ) ;
#40237=CARTESIAN_POINT ( 'NONE',  ( 54.22814610077939790, 17.69588697627349916, -48.59159517877870371 ) ) ;
#40239=CARTESIAN_POINT ( 'NONE',  ( 53.91125626133197102, -50.74963256429811764, -76.32770878461298025 ) ) ;
#40243=CYLINDRICAL_SURFACE ( 'NONE', #21452, 1.999999999999998890 ) ;
#40244=CARTESIAN_POINT ( 'NONE',  ( 46.71778720834619492, 22.48989871831510001, -75.96273541337029656 ) ) ;
#40245=CARTESIAN_POINT ( 'NONE',  ( 48.31363620257710068, -54.24728121639749645, -55.22991850671440517 ) ) ;
#40256=CARTESIAN_POINT ( 'NONE',  ( 61.10834071495050068, -45.42417164445600264, -47.35406349611150034 ) ) ;
#40260=CARTESIAN_POINT ( 'NONE',  ( 46.85765394103209758, 21.46248514361199966, -55.14905519569659731 ) ) ;
#40262=VECTOR ( 'NONE', #5290, 1000.000000000000000 ) ;
#40266=CARTESIAN_POINT ( 'NONE',  ( 83.85375176557759858, -44.83517184343819650, -47.43402238021350570 ) ) ;
#40268=EDGE_LOOP ( 'NONE', ( #20707, #14187, #23616, #35330 ) ) ;
#40271=CARTESIAN_POINT ( 'NONE',  ( 61.33923903537449718, -45.29997321760770035, -47.15257578971730368 ) ) ;
#40273=CARTESIAN_POINT ( 'NONE',  ( 76.41382631677322479, -21.54755901427089526, -12.85609321466854027 ) ) ;
#40274=CARTESIAN_POINT ( 'NONE',  ( 49.53395860104419768, -53.61039739033260076, -54.45855173817700745 ) ) ;
#40275=ORIENTED_EDGE ( 'NONE', *, *, #27500, .F. ) ;
#40276=VERTEX_POINT ( 'NONE', #41078 ) ;
#40278=CARTESIAN_POINT ( 'NONE',  ( 57.07913431483230227, -45.16254433447520000, -25.30508418749239752 ) ) ;
#40280=DIRECTION ( 'NONE',  ( 1.000000000000000000, 0.000000000000000000, 0.000000000000000000 ) ) ;
#40281=CARTESIAN_POINT ( 'NONE',  ( 60.81548642094829660, -0.5902880540152319888, -16.32683701710460156 ) ) ;
#40284=ORIENTED_EDGE ( 'NONE', *, *, #40807, .F. ) ;
#40285=CARTESIAN_POINT ( 'NONE',  ( -2.927827710953269769, 17.96742650791509988, -5.740515240579870060 ) ) ;
#40286=CARTESIAN_POINT ( 'NONE',  ( 52.71937672608480341, -50.18624820298519751, -77.16972201296600531 ) ) ;
#40291=CARTESIAN_POINT ( 'NONE',  ( 12.76011332328899961, -50.09570302368800299, -21.12207829526439795 ) ) ;
#40294=CARTESIAN_POINT ( 'NONE',  ( 61.28398356449380202, -45.60471458446119897, -47.68178229846480320 ) ) ;
#40295=CARTESIAN_POINT ( 'NONE',  ( 61.40713123412509589, -45.37885581412189850, -47.36177601773500356 ) ) ;
#40298=CARTESIAN_POINT ( 'NONE',  ( 16.13393739846020125, -15.61618894405949831, -8.049999999938441064 ) ) ;
#40301=CARTESIAN_POINT ( 'NONE',  ( 13.96298243069049860, -52.23921076650779582, -75.65449215554859563 ) ) ;
#40302=CARTESIAN_POINT ( 'NONE',  ( 47.35344256344840375, -54.67958107652259514, -54.64484088995269673 ) ) ;
#40304=CARTESIAN_POINT ( 'NONE',  ( 12.48759467940610435, 34.23991394352164264, -47.62022110713834877 ) ) ;
#40308=CARTESIAN_POINT ( 'NONE',  ( 60.83133136721959744, 14.23629320661039976, -47.01992809069390233 ) ) ;
#40309=CARTESIAN_POINT ( 'NONE',  ( 13.06064430388411957, -50.89607785224676917, -21.55066631622714723 ) ) ;
#40311=CARTESIAN_POINT ( 'NONE',  ( 48.57499813573529934, 22.88423463883380293, -55.03262398412059753 ) ) ;
#40312=ORIENTED_EDGE ( 'NONE', *, *, #24530, .T. ) ;
#40313=CARTESIAN_POINT ( 'NONE',  ( 52.71454542960869816, -49.74875623591339746, -48.77936393691420136 ) ) ;
#40314=AXIS2_PLACEMENT_3D ( 'NONE', #14065, #17991, #29521 ) ;
#40315=ORIENTED_EDGE ( 'NONE', *, *, #35532, .F. ) ;
#40316=CARTESIAN_POINT ( 'NONE',  ( 18.38332337263111427, -52.17615710686938968, -75.56421430878999956 ) ) ;
#40317=CARTESIAN_POINT ( 'NONE',  ( 16.13393739769620083, -15.61618894467929941, -4.296538310234230273 ) ) ;
#40318=CARTESIAN_POINT ( 'NONE',  ( 56.88339342946630239, -50.64986849223689802, -53.85640383950750021 ) ) ;
#40319=CARTESIAN_POINT ( 'NONE',  ( 84.42643369580130752, 12.06118485168240007, -47.38360074682189804 ) ) ;
#40320=CARTESIAN_POINT ( 'NONE',  ( 56.18972689709309520, 14.75003178236420176, -26.01119383299409904 ) ) ;
#40323=CARTESIAN_POINT ( 'NONE',  ( 52.59025554715780260, 18.60560742025969816, -48.57067451951849790 ) ) ;
#40324=CARTESIAN_POINT ( 'NONE',  ( 55.28820859282659939, -45.64641271493429997, -15.90562343326089945 ) ) ;
#40330=CARTESIAN_POINT ( 'NONE',  ( 11.84787509014739904, -65.28991114173599897, -17.04454481949920108 ) ) ;
#40331=CARTESIAN_POINT ( 'NONE',  ( 10.67388688448640188, 32.32518983410499658, -45.41653795764540291 ) ) ;
#40334=CARTESIAN_POINT ( 'NONE',  ( 47.76312238234860530, -54.35589300656749856, -54.31785946381069863 ) ) ;
#40335=CARTESIAN_POINT ( 'NONE',  ( 10.91980184567070644, -64.71824133905012388, -23.28490012654648922 ) ) ;
#40337=VERTEX_POINT ( 'NONE', #29657 ) ;
#40338=CARTESIAN_POINT ( 'NONE',  ( 13.43643018811596157, 20.02091947432642627, -22.14276202162402285 ) ) ;
#40339=CARTESIAN_POINT ( 'NONE',  ( 10.97861341538039781, -63.23619217347560806, -44.74199978104029896 ) ) ;
#40340=CARTESIAN_POINT ( 'NONE',  ( 13.84626747563856242, 20.91301623525153985, -75.51793353176734058 ) ) ;
#40345=CARTESIAN_POINT ( 'NONE',  ( 16.13393739769620083, -15.61618894467929941, -10.44999999999999929 ) ) ;
#40348=CARTESIAN_POINT ( 'NONE',  ( 59.71523078726419698, 15.48044394707019933, -48.67158068971760088 ) ) ;
#40357=CARTESIAN_POINT ( 'NONE',  ( 12.03469375213867032, 33.98406662134181744, -23.73059634278166996 ) ) ;
#40358=CARTESIAN_POINT ( 'NONE',  ( 47.23197633308699750, 23.50398264039059981, -74.50254677461771280 ) ) ;
#40365=CARTESIAN_POINT ( 'NONE',  ( 56.34559392600819905, -50.61618894589719986, -75.80272952737600178 ) ) ;
#40366=FACE_OUTER_BOUND ( 'NONE', #40900, .T. ) ;
#40369=CARTESIAN_POINT ( 'NONE',  ( 61.17186926503560329, 14.07231709399069963, -46.96206214597430062 ) ) ;
#40370=CARTESIAN_POINT ( 'NONE',  ( -17.64362745039570157, -51.14126898808360266, -52.54414402675330109 ) ) ;
#40372=CARTESIAN_POINT ( 'NONE',  ( 52.83359533572390632, -49.65890908409249960, -48.59873101611960067 ) ) ;
#40373=CARTESIAN_POINT ( 'NONE',  ( 61.35829355718019684, -45.19500725088990123, -28.15102488364330213 ) ) ;
#40375=CARTESIAN_POINT ( 'NONE',  ( 13.09773361826850113, 19.68112921523509939, -21.58185394810089974 ) ) ;
#40376=CARTESIAN_POINT ( 'NONE',  ( 56.39899885288320291, 14.62458411682690063, -26.05220366909510332 ) ) ;
#40378=CARTESIAN_POINT ( 'NONE',  ( 51.61772101699799720, 19.12659659585209937, -76.35065455175050886 ) ) ;
#40379=B_SPLINE_SURFACE_WITH_KNOTS ( 'NONE', 3, 3, ( 
 ( #30593, #41368, #18552, #42417, #14105, #34528, #13600, #22469, #46614, #37961, #50281, #9915, #22209, #26142 ),
 ( #5483, #21440, #42153, #6252, #2314, #49762, #46097, #21949, #37439, #2578, #5989, #38218, #2058, #6509 ),
 ( #14367, #29811, #45828, #25878, #30335, #38478, #33496, #41892, #46357, #1540, #10444, #49509, #45569, #18036 ),
 ( #5731, #26397, #9662, #25621, #41624, #21691, #37697, #10182, #1794, #17777, #33747, #50015, #30072, #10964 ),
 ( #35310, #19330, #19839, #23490, #31873, #43697, #26656, #11740, #15147, #27440, #51311, #31106, #3101, #15406 ),
 ( #31359, #42678, #11483, #7801, #47387, #11221, #43443, #35829, #26928, #35576, #46877, #42934, #27184, #7546 ),
 ( #39514, #27699, #3614, #7033, #22983, #47134, #19586, #51561, #51813, #15662, #47891, #23751, #6774, #39767 ),
 ( #31615, #47633, #43191, #19067, #3869, #15919, #22725, #38748, #2841, #18807, #34786, #7286, #50793, #14881 ),
 ( #30846, #39005, #35041, #23236, #51050, #39253, #3356, #4627, #962, #4893, #24004, #36082, #48402, #12243 ),
 ( #11994, #187, #8055, #27949, #43953, #40281, #20091, #40024, #16167, #32907, #8573, #48667, #4114, #32382 ) ),
 .UNSPECIFIED., .F., .F., .F.,
 ( 4, 1, 1, 1, 1, 1, 1, 4 ),
 ( 4, 2, 2, 2, 2, 2, 4 ),
 ( -0.001601301838199999930, 0.1428571428571430157, 0.2857142857142860315, 0.4285714285714289917, 0.5714285714285709528, 0.7142857142857139685, 0.8571428571428569843, 1.000147433196030056 ),
 ( -0.001601301838199999930, 0.2220862982459869961, 0.4758992105271160344, 0.6345322807028209722, 0.7138488157906729414, 0.8407552719312380018, 0.9741502278125520053 ),
 .UNSPECIFIED. ) ;
#40380=CARTESIAN_POINT ( 'NONE',  ( 53.46953806481329963, 18.11317590511340114, -48.93764703831700302 ) ) ;
#40382=CARTESIAN_POINT ( 'NONE',  ( 16.13393739846020125, -15.61618894405949831, -8.049999999938441064 ) ) ;
#40387=EDGE_CURVE ( 'NONE', #3494, #33030, #8012, .T. ) ;
#40388=CARTESIAN_POINT ( 'NONE',  ( 47.69553636805479613, -54.48351236463479808, -54.81782713205149804 ) ) ;
#40389=CARTESIAN_POINT ( 'NONE',  ( 83.89200044194980421, 18.85811933572209753, -52.57651812407429759 ) ) ;
#40391=CARTESIAN_POINT ( 'NONE',  ( 61.09078957334159554, 14.31200446843280005, -47.59852323931760054 ) ) ;
#40393=CARTESIAN_POINT ( 'NONE',  ( 62.09157612670949788, 1.883811055320649963, -65.34607522167520699 ) ) ;
#40397=ORIENTED_EDGE ( 'NONE', *, *, #42419, .T. ) ;
#40401=EDGE_LOOP ( 'NONE', ( #43737, #29041, #20619, #34774 ) ) ;
#40409=DIRECTION ( 'NONE',  ( 1.000000000000000000, 0.000000000000000000, 0.000000000000000000 ) ) ;
#40416=CARTESIAN_POINT ( 'NONE',  ( 12.27549348550230057, -65.46856705471530802, -22.61746666998769939 ) ) ;
#40418=DIRECTION ( 'NONE',  ( -0.05023550054956202326, 0.000000000000000000, 0.9987374001630934250 ) ) ;
#40419=CARTESIAN_POINT ( 'NONE',  ( 14.52015376228360033, 20.37930389448659696, -75.46937177410659103 ) ) ;
#40421=CARTESIAN_POINT ( 'NONE',  ( 83.84636189228659475, -44.33791279555990172, -46.70679156566489354 ) ) ;
#40425=CARTESIAN_POINT ( 'NONE',  ( 52.71556874866190157, -49.72995812607539534, -28.15000000000000213 ) ) ;
#40426=CARTESIAN_POINT ( 'NONE',  ( 15.22027405774909958, -50.86891089868439764, -20.91173439138849943 ) ) ;
#40427=CARTESIAN_POINT ( 'NONE',  ( 50.07689680525066223, -36.77944211564444288, -76.14999999999999147 ) ) ;
#40431=ORIENTED_EDGE ( 'NONE', *, *, #4594, .T. ) ;
#40432=CARTESIAN_POINT ( 'NONE',  ( -4.138844267738590155, -48.25635689139589601, -5.557732677314410452 ) ) ;
#40433=AXIS2_PLACEMENT_3D ( 'NONE', #49143, #28668, #29703 ) ;
#40434=CARTESIAN_POINT ( 'NONE',  ( 47.20960036188380116, 23.55400766168000004, -54.63720401602729737 ) ) ;
#40437=CARTESIAN_POINT ( 'NONE',  ( 13.18314425874230089, 19.09886800652760286, -21.16865821970199946 ) ) ;
#40438=CARTESIAN_POINT ( 'NONE',  ( 56.49020273170298623, 15.04445699649443569, -26.27688945974474422 ) ) ;
#40439=CARTESIAN_POINT ( 'NONE',  ( 41.53965881163059493, 12.99627826066740077, -4.633657234686240578 ) ) ;
#40442=CARTESIAN_POINT ( 'NONE',  ( 20.13393739768959634, -55.41568642894479524, -74.14999999999999147 ) ) ;
#40443=CARTESIAN_POINT ( 'NONE',  ( 57.22384866945419901, -47.50201179472099966, -48.27676837875709737 ) ) ;
#40447=CARTESIAN_POINT ( 'NONE',  ( 17.69762321645020009, -52.06302405750739837, -75.84958893011570069 ) ) ;
#40449=CARTESIAN_POINT ( 'NONE',  ( 51.04010994513039634, 13.88381105532070059, -11.02192607461959994 ) ) ;
#40452=CARTESIAN_POINT ( 'NONE',  ( 10.14595732507179981, 32.05463481625440636, -45.99315448786889959 ) ) ;
#40453=CARTESIAN_POINT ( 'NONE',  ( 42.75215489670460300, 13.74995302045830137, -6.093637046069630081 ) ) ;
#40454=CARTESIAN_POINT ( 'NONE',  ( 67.33934068966290454, -30.19343665506969998, -17.45359291235359933 ) ) ;
#40456=CARTESIAN_POINT ( 'NONE',  ( 18.24473874235309978, 20.10118929730710136, -74.92517623884199907 ) ) ;
#40461=CARTESIAN_POINT ( 'NONE',  ( 57.40532849796809245, -45.80460617788560285, -26.27934586546770035 ) ) ;
#40466=CARTESIAN_POINT ( 'NONE',  ( 75.27759724181119338, 4.400931120799945973, -12.42500406430217907 ) ) ;
#40467=CARTESIAN_POINT ( 'NONE',  ( 11.13393739769619906, -15.61618894467929941, -46.14999999999999858 ) ) ;
#40468=ORIENTED_EDGE ( 'NONE', *, *, #25652, .F. ) ;
#40469=CARTESIAN_POINT ( 'NONE',  ( 54.47259998646330104, -46.25234364376770202, -15.76423879730199928 ) ) ;
#40471=EDGE_CURVE ( 'NONE', #18008, #35377, #12181, .T. ) ;
#40475=ORIENTED_EDGE ( 'NONE', *, *, #39796, .T. ) ;
#40476=CARTESIAN_POINT ( 'NONE',  ( 69.89373504110858448, 1.883811054953212993, -20.65000000000000924 ) ) ;
#40478=CARTESIAN_POINT ( 'NONE',  ( 12.06284766121009966, 32.21085600226960111, -46.39999999999999858 ) ) ;
#40479=CARTESIAN_POINT ( 'NONE',  ( 74.93466528652979264, 13.88381105527180104, -15.31219498128760037 ) ) ;
#40480=CARTESIAN_POINT ( 'NONE',  ( 47.38130800000779885, 14.91675872927610058, -10.59906833146859917 ) ) ;
#40481=LINE ( 'NONE', #44675, #8311 ) ;
#40482=CARTESIAN_POINT ( 'NONE',  ( -10.43962737580419819, 11.55570939729970092, -6.045128938053459855 ) ) ;
#40484=CARTESIAN_POINT ( 'NONE',  ( 61.07580650143209766, 14.01630602148660110, -27.53710762590180039 ) ) ;
#40487=CARTESIAN_POINT ( 'NONE',  ( 60.03117800382469227, 14.75234466156519986, -47.69329595932870092 ) ) ;
#40490=CARTESIAN_POINT ( 'NONE',  ( 54.14338603149285234, -50.61618765074635462, -76.93434640323403073 ) ) ;
#40494=CARTESIAN_POINT ( 'NONE',  ( 12.38542484659079967, 18.88631011504679691, -21.15108199309460346 ) ) ;
#40496=CARTESIAN_POINT ( 'NONE',  ( 47.11356394356230481, 23.41745045323149910, -74.95177818529600700 ) ) ;
#40497=CARTESIAN_POINT ( 'NONE',  ( 48.93508874961730015, -53.77152385436419735, -54.40024034726540236 ) ) ;
#40499=EDGE_CURVE ( 'NONE', #18289, #39898, #48859, .T. ) ;
#40504=EDGE_CURVE ( 'NONE', #14841, #19647, #28221, .T. ) ;
#40505=AXIS2_PLACEMENT_3D ( 'NONE', #5764, #6808, #37735 ) ;
#40509=ORIENTED_EDGE ( 'NONE', *, *, #43889, .T. ) ;
#40510=DIRECTION ( 'NONE',  ( 0.000000000000000000, 0.000000000000000000, -1.000000000000000000 ) ) ;
#40511=CARTESIAN_POINT ( 'NONE',  ( 60.60295391979060042, -45.60334326694930240, -47.31465422358670025 ) ) ;
#40513=CARTESIAN_POINT ( 'NONE',  ( 12.76110940284849882, 18.75367529502860009, -21.08964676157749807 ) ) ;
#40516=EDGE_CURVE ( 'NONE', #32428, #13650, #2148, .T. ) ;
#40518=ORIENTED_EDGE ( 'NONE', *, *, #11891, .F. ) ;
#40519=CARTESIAN_POINT ( 'NONE',  ( 82.89855244518309974, -45.51886959512750508, -47.58879117305969686 ) ) ;
#40523=CARTESIAN_POINT ( 'NONE',  ( 61.62921802303379337, -45.24296170225480296, -47.09041573235759870 ) ) ;
#40524=CARTESIAN_POINT ( 'NONE',  ( 53.16310686614889391, -49.55825684149800026, -49.15478280794970090 ) ) ;
#40526=CARTESIAN_POINT ( 'NONE',  ( 76.44629721152865898, -6.610254442245663498, -12.99600492729799939 ) ) ;
#40527=CARTESIAN_POINT ( 'NONE',  ( 52.78795861510499776, -52.32134061137240622, -54.06277347879859718 ) ) ;
#40530=CARTESIAN_POINT ( 'NONE',  ( 48.25395546892340093, 22.92590509088350004, -54.66662523256869832 ) ) ;
#40534=CARTESIAN_POINT ( 'NONE',  ( 8.800117217589539464, -63.19572640051600132, -46.67015592357310538 ) ) ;
#40536=EDGE_CURVE ( 'NONE', #362, #26902, #6343, .T. ) ;
#40538=ORIENTED_EDGE ( 'NONE', *, *, #42112, .F. ) ;
#40540=CARTESIAN_POINT ( 'NONE',  ( 53.18839701416040100, -50.49756234138030209, -76.93089027597029883 ) ) ;
#40542=CARTESIAN_POINT ( 'NONE',  ( 82.91593256429321457, -45.56280716946599085, -47.63721988159374376 ) ) ;
#40545=CARTESIAN_POINT ( 'NONE',  ( 54.35139833030309831, 19.38381105532069881, -76.94248449261100120 ) ) ;
#40547=CARTESIAN_POINT ( 'NONE',  ( 43.19833518102579717, -43.80395068146980719, -5.006617643003630214 ) ) ;
#40548=CARTESIAN_POINT ( 'NONE',  ( 18.86789271272390067, -51.78678247029300508, -15.81497036395479761 ) ) ;
#40549=FACE_OUTER_BOUND ( 'NONE', #49125, .T. ) ;
#40551=ADVANCED_FACE ( 'NONE', ( #19165 ), #50886, .T. ) ;
#40555=CARTESIAN_POINT ( 'NONE',  ( 14.04826348280290027, -52.14694418483630045, -75.69083100613939052 ) ) ;
#40556=CARTESIAN_POINT ( 'NONE',  ( 47.41638517356940241, -54.63912780781220135, -54.68870541073049907 ) ) ;
#40566=CARTESIAN_POINT ( 'NONE',  ( 48.83374951863850555, 22.78418287378880080, -55.08837257690210265 ) ) ;
#40570=FACE_OUTER_BOUND ( 'NONE', #21733, .T. ) ;
#40572=CARTESIAN_POINT ( 'NONE',  ( 56.99190259421959581, -50.63247588149960166, -53.87165542791530726 ) ) ;
#40573=CARTESIAN_POINT ( 'NONE',  ( 83.75509190357360012, 13.34125973800720111, -46.98971415009500419 ) ) ;
#40574=CARTESIAN_POINT ( 'NONE',  ( 54.30663165020069982, 16.75924678417570135, -26.35036544773539902 ) ) ;
#40576=CARTESIAN_POINT ( 'NONE',  ( 52.56521993351460509, 18.62941884369810097, -48.47378032971769812 ) ) ;
#40578=CARTESIAN_POINT ( 'NONE',  ( 56.62787340350230636, -45.26860272202350188, -17.10917261918480037 ) ) ;
#40581=ORIENTED_EDGE ( 'NONE', *, *, #25494, .F. ) ;
#40582=CARTESIAN_POINT ( 'NONE',  ( 11.57222021527059930, -65.08436554735389734, -16.73996640653249912 ) ) ;
#40583=CARTESIAN_POINT ( 'NONE',  ( 13.00893739769619906, 34.28605925116850273, -47.75434321273180416 ) ) ;
#40584=CARTESIAN_POINT ( 'NONE',  ( 61.44122352006623800, -45.34727173273595469, -47.30181503080611094 ) ) ;
#40589=CARTESIAN_POINT ( 'NONE',  ( 11.10574934303680017, -63.48107579820671020, -44.26157399421149563 ) ) ;
#40590=CARTESIAN_POINT ( 'NONE',  ( 13.88455142272560039, 20.94377921756336036, -75.56421430877985301 ) ) ;
#40595=ORIENTED_EDGE ( 'NONE', *, *, #36378, .T. ) ;
#40600=CARTESIAN_POINT ( 'NONE',  ( 60.22029979666620392, 14.82624742056550105, -47.95282500047770213 ) ) ;
#40601=B_SPLINE_CURVE_WITH_KNOTS ( 'NONE', 3,
 ( #6875, #50380, #10802, #5833, #21796, #46458 ),
 .UNSPECIFIED., .F., .F.,
 ( 4, 2, 4 ),
 ( 0.000000000000000000, 0.6321606378469137866, 1.000000000000000000 ),
 .UNSPECIFIED. ) ;
#40604=CARTESIAN_POINT ( 'NONE',  ( 68.13393739769810509, 19.38381105532030091, -71.50000000000198952 ) ) ;
#40605=CARTESIAN_POINT ( 'NONE',  ( 56.57234443381329925, 19.50072803673270272, -74.30166440113460169 ) ) ;
#40607=CARTESIAN_POINT ( 'NONE',  ( 46.90719325741979873, -53.72294727813159909, -75.90528168595349712 ) ) ;
#40611=CARTESIAN_POINT ( 'NONE',  ( 53.36506516905719621, -49.48367947020049940, -49.20548766773279681 ) ) ;
#40613=CYLINDRICAL_SURFACE ( 'NONE', #24672, 0.9999999999999991118 ) ;
#40614=DIRECTION ( 'NONE',  ( 0.000000000000000000, -1.000000000000000000, 0.000000000000000000 ) ) ;
#40616=CARTESIAN_POINT ( 'NONE',  ( 46.82266861842990124, 22.42583874316209958, -75.96020792128800281 ) ) ;
#40620=CARTESIAN_POINT ( 'NONE',  ( 75.10755973209502656, -25.67677511771720944, -11.59100465374893574 ) ) ;
#40626=CARTESIAN_POINT ( 'NONE',  ( 61.14297824559450589, 14.08836494215110058, -46.99581295334250086 ) ) ;
#40627=CARTESIAN_POINT ( 'NONE',  ( 6.264007226339749934, -63.37915212591551040, -47.23119725298560212 ) ) ;
#40630=CARTESIAN_POINT ( 'NONE',  ( 53.06802000122009844, -49.53608743370789824, -48.81041485548290382 ) ) ;
#40631=CARTESIAN_POINT ( 'NONE',  ( 61.58999301232780255, -45.12803339529550328, -28.02454186838919981 ) ) ;
#40633=CARTESIAN_POINT ( 'NONE',  ( 47.95926718124380272, -54.39950235201530404, -55.26638612347969826 ) ) ;
#40634=CARTESIAN_POINT ( 'NONE',  ( 56.77968109326819501, 14.56960969026870067, -26.16725212139149903 ) ) ;
#40636=CARTESIAN_POINT ( 'NONE',  ( 50.55910572479910314, 19.00727530243110053, -76.14999999999999147 ) ) ;
#40637=CARTESIAN_POINT ( 'NONE',  ( 53.32371982237880559, 18.17626688474259922, -48.89504544885870274 ) ) ;
#40640=CARTESIAN_POINT ( 'NONE',  ( 41.55663456559430102, -43.85962873145379604, -3.466044033466880059 ) ) ;
#40641=CARTESIAN_POINT ( 'NONE',  ( 63.88486207242520720, -43.42060977382210041, -10.13980136567960066 ) ) ;
#40643=ORIENTED_EDGE ( 'NONE', *, *, #44814, .T. ) ;
#40646=CARTESIAN_POINT ( 'NONE',  ( 47.59050665785859735, -54.53298138600730027, -54.74365073385350655 ) ) ;
#40649=CARTESIAN_POINT ( 'NONE',  ( 42.11778985390380114, 12.11280974652049913, -3.278435070539889917 ) ) ;
#40650=CARTESIAN_POINT ( 'NONE',  ( 59.73488990452629821, 15.43279671172489920, -48.60609801886729997 ) ) ;
#40652=LINE ( 'NONE', #40393, #20796 ) ;
#40656=ORIENTED_EDGE ( 'NONE', *, *, #9310, .T. ) ;
#40659=LINE ( 'NONE', #36714, #4306 ) ;
#40661=CARTESIAN_POINT ( 'NONE',  ( 11.38042686594670094, -64.49026764409909163, -44.43661832440050574 ) ) ;
#40664=CARTESIAN_POINT ( 'NONE',  ( 52.48374443017399926, 19.52726341579099767, -76.33825989979830240 ) ) ;
#40665=VERTEX_POINT ( 'NONE', #20180 ) ;
#40666=CARTESIAN_POINT ( 'NONE',  ( 11.53605495837543948, -55.35105376503654639, -21.73576846289474318 ) ) ;
#40669=VECTOR ( 'NONE', #23205, 1000.000000000000114 ) ;
#40672=( NAMED_UNIT ( * ) SI_UNIT ( $, .STERADIAN. ) SOLID_ANGLE_UNIT ( ) );
#40678=EDGE_CURVE ( 'NONE', #17738, #51359, #24612, .T. ) ;
#40679=CARTESIAN_POINT ( 'NONE',  ( 13.80985048470530074, 20.88378464714680049, -75.46937177410670472 ) ) ;
#40681=CARTESIAN_POINT ( 'NONE',  ( 51.85719037988729951, 18.05925585374960107, -77.06876492569810466 ) ) ;
#40682=CARTESIAN_POINT ( 'NONE',  ( 83.54531734280109845, -44.64140434283670089, -46.66630366969080512 ) ) ;
#40686=CARTESIAN_POINT ( 'NONE',  ( 53.03694355186379994, -49.40910104661059421, -27.39159970799200039 ) ) ;
#40687=CARTESIAN_POINT ( 'NONE',  ( 14.61081989480809895, -51.05470123690699324, -21.82083395458209907 ) ) ;
#40688=CARTESIAN_POINT ( 'NONE',  ( 50.40119816437731259, -36.24976658303432941, -76.18455893466475004 ) ) ;
#40693=CARTESIAN_POINT ( 'NONE',  ( -7.621576387460760493, -45.43712284492340103, -5.646501867015009779 ) ) ;
#40694=CARTESIAN_POINT ( 'NONE',  ( 47.24472437627869681, 23.52728567798950010, -54.64339285785950295 ) ) ;
#40696=DIRECTION ( 'NONE',  ( -1.000000000000000000, 0.000000000000000000, 0.000000000000000000 ) ) ;
#40699=CARTESIAN_POINT ( 'NONE',  ( 11.93810463912310027, 34.20707664335219533, -17.87564887320120022 ) ) ;
#40701=CARTESIAN_POINT ( 'NONE',  ( 68.13393739769769297, 18.72622661238600017, -69.60146707679309941 ) ) ;
#40702=EDGE_CURVE ( 'NONE', #47510, #44163, #33132, .T. ) ;
#40703=CARTESIAN_POINT ( 'NONE',  ( 68.13393739769620083, -48.61618894467930119, -65.65000000000000568 ) ) ;
#40704=CARTESIAN_POINT ( 'NONE',  ( 57.81609062655950027, -47.19091213400450613, -48.15256270216469403 ) ) ;
#40705=VECTOR ( 'NONE', #19373, 1000.000000000000000 ) ;
#40706=CARTESIAN_POINT ( 'NONE',  ( 68.13393739769847457, -50.70395984887981200, -74.34354914830335304 ) ) ;
#40708=CARTESIAN_POINT ( 'NONE',  ( 17.73212549933870008, -52.38593004734789815, -75.99067819366339904 ) ) ;
#40710=CARTESIAN_POINT ( 'NONE',  ( 16.65420337941489848, 17.88381105532299742, -17.90311212357439885 ) ) ;
#40711=CARTESIAN_POINT ( 'NONE',  ( 12.09990282912350068, -65.24532120969969640, -16.83009741455080288 ) ) ;
#40715=CARTESIAN_POINT ( 'NONE',  ( 9.299128317299539148, 32.06192745982850312, -46.53057822423220102 ) ) ;
#40716=DIRECTION ( 'NONE',  ( 1.000000000000000000, 0.000000000000000000, 0.000000000000000000 ) ) ;
#40718=CARTESIAN_POINT ( 'NONE',  ( 67.73239348926679781, -31.31112839167719741, -17.99563373446390102 ) ) ;
#40720=CARTESIAN_POINT ( 'NONE',  ( 18.76586980408200134, 20.63642445556759952, -74.86150924066380696 ) ) ;
#40723=ORIENTED_EDGE ( 'NONE', *, *, #24509, .T. ) ;
#40725=CARTESIAN_POINT ( 'NONE',  ( 10.67183281957709973, -63.52764994537149335, -45.41177609095300483 ) ) ;
#40726=DIRECTION ( 'NONE',  ( 0.000000000000000000, 0.000000000000000000, -1.000000000000000000 ) ) ;
#40728=CARTESIAN_POINT ( 'NONE',  ( 61.52836517851630305, 13.92984914567709964, -46.71062307070980069 ) ) ;
#40729=EDGE_LOOP ( 'NONE', ( #815, #37637 ) ) ;
#40730=CARTESIAN_POINT ( 'NONE',  ( 75.24618922237742424, 2.926750969086042709, -12.27132002303570069 ) ) ;
#40731=CARTESIAN_POINT ( 'NONE',  ( 12.16177389586671964, 33.87933702454814977, -16.53048054918994936 ) ) ;
#40733=CARTESIAN_POINT ( 'NONE',  ( 49.42577828663870321, -46.18035913434329842, -12.04425446003870093 ) ) ;
#40737=ORIENTED_EDGE ( 'NONE', *, *, #44062, .T. ) ;
#40739=CARTESIAN_POINT ( 'NONE',  ( 10.89208569015771388, -65.00086843820284344, -17.57297834641052603 ) ) ;
#40741=CARTESIAN_POINT ( 'NONE',  ( 50.20812286835639782, 14.95963111490540065, -12.60694443316879898 ) ) ;
#40744=CARTESIAN_POINT ( 'NONE',  ( -11.32734370190460105, 10.64934056395049922, -6.430192534648650593 ) ) ;
#40746=AXIS2_PLACEMENT_3D ( 'NONE', #40074, #24314, #48989 ) ;
#40747=CARTESIAN_POINT ( 'NONE',  ( 55.78775146822957254, 14.70279260508580776, -17.21510844903624005 ) ) ;
#40751=CARTESIAN_POINT ( 'NONE',  ( 12.00070700938809942, 33.94152585701019831, -45.91242252782910072 ) ) ;
#40754=CARTESIAN_POINT ( 'NONE',  ( 13.19614974924530060, 18.82172380121849997, -21.01902014306970301 ) ) ;
#40755=CARTESIAN_POINT ( 'NONE',  ( 47.17214619674849985, 23.54985310318610203, -74.50417157308129390 ) ) ;
#40756=EDGE_CURVE ( 'NONE', #51329, #28860, #6391, .T. ) ;
#40757=CARTESIAN_POINT ( 'NONE',  ( 49.12468868441940373, -53.81509191060310116, -54.67300365794890382 ) ) ;
#40758=CARTESIAN_POINT ( 'NONE',  ( 58.92073396209919878, -3.116188944679349593, -15.65000000000000036 ) ) ;
#40760=FACE_OUTER_BOUND ( 'NONE', #9285, .T. ) ;
#40761=EDGE_CURVE ( 'NONE', #49655, #20898, #39811, .T. ) ;
#40762=CARTESIAN_POINT ( 'NONE',  ( 57.00722761779879733, 13.88381105532070059, -15.97596069844019873 ) ) ;
#40763=ORIENTED_EDGE ( 'NONE', *, *, #20026, .F. ) ;
#40767=CARTESIAN_POINT ( 'NONE',  ( 84.41931977238152740, -43.28155736009810539, -47.35294579201847398 ) ) ;
#40768=CARTESIAN_POINT ( 'NONE',  ( 60.35161375623229674, -45.78197740793289938, -47.56115285142140436 ) ) ;
#40769=CARTESIAN_POINT ( 'NONE',  ( 56.99190255428169394, 19.40009799746960084, -53.87165542181880085 ) ) ;
#40770=CARTESIAN_POINT ( 'NONE',  ( 12.28937882765760037, 18.77527565194250059, -21.14656491342549671 ) ) ;
#40772=DIRECTION ( 'NONE',  ( 0.000000000000000000, 0.000000000000000000, -1.000000000000000000 ) ) ;
#40776=CARTESIAN_POINT ( 'NONE',  ( 83.77685426296399385, -44.72604696044789563, -47.23654203728539613 ) ) ;
#40777=VERTEX_POINT ( 'NONE', #27979 ) ;
#40779=EDGE_LOOP ( 'NONE', ( #27540, #1974, #16619, #46284, #6120, #7947 ) ) ;
#40780=CARTESIAN_POINT ( 'NONE',  ( 61.62976587585850297, -45.12285621563059834, -46.37194070680949665 ) ) ;
#40782=CARTESIAN_POINT ( 'NONE',  ( 76.42335732216182009, -22.53194434191319218, -12.89715778059380824 ) ) ;
#40783=CARTESIAN_POINT ( 'NONE',  ( 56.15635836398279679, -50.90785405786900242, -53.88620114773970471 ) ) ;
#40784=CIRCLE ( 'NONE', #46691, 2.000000000000001776 ) ;
#40785=ORIENTED_EDGE ( 'NONE', *, *, #26605, .F. ) ;
#40786=ORIENTED_EDGE ( 'NONE', *, *, #8269, .T. ) ;
#40787=CARTESIAN_POINT ( 'NONE',  ( 48.64758560217519801, 22.70397928459539827, -54.52813621919599996 ) ) ;
#40790=CARTESIAN_POINT ( 'NONE',  ( 16.13393739769620083, -15.61618894467929941, -170.7999095292539948 ) ) ;
#40793=ORIENTED_EDGE ( 'NONE', *, *, #50363, .F. ) ;
#40795=CARTESIAN_POINT ( 'NONE',  ( 53.48387799555199251, -50.52031544494510484, -77.13966324944060204 ) ) ;
#40797=CARTESIAN_POINT ( 'NONE',  ( 60.49536215360559765, 14.41231689077920031, -47.20225698283260840 ) ) ;
#40799=DIRECTION ( 'NONE',  ( 0.000000000000000000, 1.000000000000000000, 0.000000000000000000 ) ) ;
#40800=EDGE_CURVE ( 'NONE', #12954, #19589, #1666, .T. ) ;
#40801=CARTESIAN_POINT ( 'NONE',  ( 41.57868392304440164, -44.36040080565599908, -4.871763622046390019 ) ) ;
#40804=CARTESIAN_POINT ( 'NONE',  ( 61.20230452259990273, -45.64718664723880437, -47.73655850518729693 ) ) ;
#40807=EDGE_CURVE ( 'NONE', #30733, #43378, #16696, .T. ) ;
#40809=DIRECTION ( 'NONE',  ( -1.000000000000000000, -1.791661345120054866E-29, -4.486507500526829843E-12 ) ) ;
#40811=CARTESIAN_POINT ( 'NONE',  ( 66.39756463022349919, 1.816743601633340033, -19.74079115529689687 ) ) ;
#40812=B_SPLINE_SURFACE_WITH_KNOTS ( 'NONE', 3, 3, ( 
 ( #23159, #19247, #11655, #31280, #23672, #27874, #11140, #39176, #47814, #364, #11921, #43877, #39947, #4043, #36253, #35999 ),
 ( #27110, #43113, #24956, #9013, #9534, #13214, #45163, #44643, #44907, #21297, #21038, #29165, #37040, #8749, #37301, #17133 ),
 ( #48324, #40968, #12688, #36511, #28383, #24697, #613, #9277, #28641, #33354, #879, #16872, #25484, #32820, #49115, #40715 ),
 ( #32301, #44390, #28905, #1399, #29425, #49372, #8491, #37552, #4812, #25225, #45431, #5344, #20778, #41230, #17388, #13470 ),
 ( #12950, #5085, #16599, #24437, #41488, #36768, #5601, #32552, #1138, #21557, #12419, #16345, #40452, #4545, #48846, #33085 ),
 ( #20517, #48587, #10821, #22844, #41747, #18156, #29932, #13723, #34644, #18410, #22331, #38337, #26783, #5853, #10304, #46478 ),
 ( #2426, #30455, #6115, #14745, #1918, #33616, #26004, #42798, #1658, #30715, #2697, #26266, #46737, #25740, #50649, #6894 ),
 ( #10564, #22071, #34386, #50398, #9788, #17650, #49630, #14484, #26521, #42538, #10040, #6369, #34122, #29677, #45687, #50133 ),
 ( #14229, #18670, #38080, #13975, #37825, #21817, #42272, #2177, #46218, #17896, #38607, #33869, #49880, #30201, #45949, #6626 ),
 ( #22590, #43054, #51428, #19185, #11082, #2954, #27050, #34908, #38865, #18924, #35166, #50907, #14999, #30967, #19949, #19446 ),
 ( #16033, #51173, #15774, #39374, #23865, #47500, #15267, #31222, #27557, #3214, #47754, #46998, #15524, #39887, #47249, #7150 ) ),
 .UNSPECIFIED., .F., .F., .F.,
 ( 4, 1, 1, 1, 1, 1, 1, 1, 4 ),
 ( 4, 2, 2, 2, 2, 2, 2, 4 ),
 ( 0.000000000000000000, 0.1250000000000000000, 0.2500000000000000000, 0.3750000000000000000, 0.5000000000000000000, 0.6250000000000000000, 0.7500000000000000000, 0.8750000000000000000, 1.000000000000000000 ),
 ( -0.4072589812491140271, -0.3359886595305190404, -0.2545368632806960241, -0.2036294906245569858, -0.1781758042964870226, -0.1374499061715759862, -0.07228846917171800890, 0.000000000000000000 ),
 .UNSPECIFIED. ) ;
#40814=CARTESIAN_POINT ( 'NONE',  ( 14.44817841379610002, -51.79813798162680172, -75.64877291256318870 ) ) ;
#40815=CARTESIAN_POINT ( 'NONE',  ( 47.31442551589749712, -54.70848342480089599, -54.65525844330269933 ) ) ;
#40817=CARTESIAN_POINT ( 'NONE',  ( 84.37071824923931729, 12.21453748216318225, -47.23470636407145662 ) ) ;
#40818=CARTESIAN_POINT ( 'NONE',  ( 60.87196308501805930, -45.45251507131489177, -47.10470314364983579 ) ) ;
#40821=CARTESIAN_POINT ( 'NONE',  ( 47.80576864997149755, -54.41529265479059774, -54.77142112296580478 ) ) ;
#40823=CARTESIAN_POINT ( 'NONE',  ( -6.571053818291229476, -46.36898988238050379, -5.603118524855751126 ) ) ;
#40826=EDGE_CURVE ( 'NONE', #17149, #2490, #18004, .T. ) ;
#40827=CARTESIAN_POINT ( 'NONE',  ( 48.51680376425250074, 22.79139865270589738, -54.61040359998320071 ) ) ;
#40831=FACE_BOUND ( 'NONE', #48562, .T. ) ;
#40832=CARTESIAN_POINT ( 'NONE',  ( 53.48663704675684016, -49.34136594389416075, -49.00013169077879382 ) ) ;
#40833=CARTESIAN_POINT ( 'NONE',  ( 57.18371625260090241, -50.61638664230350315, -53.90359199106109855 ) ) ;
#40834=CARTESIAN_POINT ( 'NONE',  ( 83.23750369908759694, 13.58709911348850063, -46.42259446247510368 ) ) ;
#40835=CARTESIAN_POINT ( 'NONE',  ( 52.71768855521909813, 18.48070669118740028, -27.77299963332060173 ) ) ;
#40837=CARTESIAN_POINT ( 'NONE',  ( 82.75389963950320293, -45.59493862562369770, -47.67227237921210303 ) ) ;
#40838=CARTESIAN_POINT ( 'NONE',  ( 57.12835595156409596, -45.11618894467940066, -16.21298877816359862 ) ) ;
#40840=ORIENTED_EDGE ( 'NONE', *, *, #8920, .F. ) ;
#40842=CARTESIAN_POINT ( 'NONE',  ( 11.43875273178739960, -65.00398667583539236, -16.70124317897120036 ) ) ;
#40843=CARTESIAN_POINT ( 'NONE',  ( 12.94333334658009882, 34.28195096612819981, -47.69450768049080125 ) ) ;
#40845=CARTESIAN_POINT ( 'NONE',  ( 50.25595676683099811, -52.23737648766640262, -51.95249114396919765 ) ) ;
#40847=EDGE_CURVE ( 'NONE', #15849, #5766, #42364, .T. ) ;
#40850=CARTESIAN_POINT ( 'NONE',  ( 54.57308664466630432, 16.87911987759756727, -26.75817216227180495 ) ) ;
#40852=DIRECTION ( 'NONE',  ( 0.000000000000000000, 0.000000000000000000, -1.000000000000000000 ) ) ;
#40853=CARTESIAN_POINT ( 'NONE',  ( 50.28917927772980079, -49.63951472337090109, -76.14999999999999147 ) ) ;
#40855=VERTEX_POINT ( 'NONE', #45279 ) ;
#40856=CARTESIAN_POINT ( 'NONE',  ( 53.87584899166620289, -48.41195041224399631, -26.23515327084989934 ) ) ;
#40861=CARTESIAN_POINT ( 'NONE',  ( 53.93371072663619969, -46.24504243184900076, -15.35642390276739988 ) ) ;
#40863=CARTESIAN_POINT ( 'NONE',  ( 13.64848148378749926, -51.39660537786010508, -23.00152637257979649 ) ) ;
#40865=EDGE_CURVE ( 'NONE', #39487, #13362, #6219, .T. ) ;
#40866=CARTESIAN_POINT ( 'NONE',  ( 47.50285049045650254, -54.59925851099900029, -74.19801721955809626 ) ) ;
#40871=CARTESIAN_POINT ( 'NONE',  ( 57.27851914992729832, -50.15376702335620251, -52.63313635724109929 ) ) ;
#40872=CARTESIAN_POINT ( 'NONE',  ( 52.77360392991350579, -49.72529414377589774, -48.90177011830709830 ) ) ;
#40875=EDGE_CURVE ( 'NONE', #47320, #4677, #1366, .T. ) ;
#40876=CARTESIAN_POINT ( 'NONE',  ( 47.48811402935950099, 23.34517892920809956, -74.50151902752439526 ) ) ;
#40877=DIRECTION ( 'NONE',  ( 1.000000000000000000, 0.000000000000000000, 0.000000000000000000 ) ) ;
#40878=CARTESIAN_POINT ( 'NONE',  ( 59.28524734660857831, -29.42491135532547020, -15.78018370959630445 ) ) ;
#40881=DIRECTION ( 'NONE',  ( 0.000000000000000000, 1.000000000000000000, 0.000000000000000000 ) ) ;
#40884=DIRECTION ( 'NONE',  ( 0.000000000000000000, -1.000000000000000000, 0.000000000000000000 ) ) ;
#40886=CARTESIAN_POINT ( 'NONE',  ( -33.45614285200539939, -20.42943855637770056, -56.47882598457800185 ) ) ;
#40887=ORIENTED_EDGE ( 'NONE', *, *, #27688, .F. ) ;
#40888=CARTESIAN_POINT ( 'NONE',  ( 52.75872680408620141, -49.70160015685030430, -48.48805751657780405 ) ) ;
#40890=DIRECTION ( 'NONE',  ( 0.4808500020228050897, 0.3493579760610313056, 0.8041966675616158966 ) ) ;
#40892=CARTESIAN_POINT ( 'NONE',  ( 57.22461981268290288, 14.53251969692440149, -26.23717558781860149 ) ) ;
#40895=CARTESIAN_POINT ( 'NONE',  ( 51.36576727628780503, 19.27592626937499887, -76.23494648113261007 ) ) ;
#40896=CARTESIAN_POINT ( 'NONE',  ( 52.92152585432570078, 18.39031306738499794, -48.88490681319890285 ) ) ;
#40898=CARTESIAN_POINT ( 'NONE',  ( 42.29536634146680285, -43.17774985521609921, -3.241362036132339863 ) ) ;
#40899=CARTESIAN_POINT ( 'NONE',  ( 75.47882570655470147, -43.69042101453369753, -13.44752134567739965 ) ) ;
#40900=EDGE_LOOP ( 'NONE', ( #36525, #41058, #6512, #44776 ) ) ;
#40904=CARTESIAN_POINT ( 'NONE',  ( 47.46127172027109964, -54.61040224951049993, -54.70311265894389408 ) ) ;
#40907=CARTESIAN_POINT ( 'NONE',  ( 60.43132024577979422, -30.38530924120979648, -16.18952559267319913 ) ) ;
#40911=EDGE_CURVE ( 'NONE', #19573, #30947, #26094, .T. ) ;
#40914=ORIENTED_EDGE ( 'NONE', *, *, #5430, .F. ) ;
#40916=EDGE_LOOP ( 'NONE', ( #13165, #20551, #41967, #25381 ) ) ;
#40917=CARTESIAN_POINT ( 'NONE',  ( 8.806603807574589382, -63.23125877106109982, -46.67034945549170288 ) ) ;
#40919=ORIENTED_EDGE ( 'NONE', *, *, #41710, .F. ) ;
#40923=CARTESIAN_POINT ( 'NONE',  ( 52.12109120452969790, 19.65124629421640279, -76.21339085878619812 ) ) ;
#40932=CARTESIAN_POINT ( 'NONE',  ( 12.93852378631490119, -65.51408294560670242, -23.45535008101469998 ) ) ;
#40934=CIRCLE ( 'NONE', #11658, 1.999999999999997335 ) ;
#40935=CARTESIAN_POINT ( 'NONE',  ( 53.16045469121779377, -49.55285059943579995, -49.13860152736959463 ) ) ;
#40938=AXIS2_PLACEMENT_3D ( 'NONE', #42484, #29877, #9984 ) ;
#40939=ADVANCED_FACE ( 'NONE', ( #22698 ), #15374, .T. ) ;
#40940=CARTESIAN_POINT ( 'NONE',  ( 14.43857095918710165, 21.38897561371040013, -76.01805773991210913 ) ) ;
#40942=CARTESIAN_POINT ( 'NONE',  ( 84.22671941158239406, -43.79042781477089363, -46.99905560746359612 ) ) ;
#40944=ORIENTED_EDGE ( 'NONE', *, *, #24545, .T. ) ;
#40945=CARTESIAN_POINT ( 'NONE',  ( 52.80815860113929716, -49.65884401321449815, -27.90951286951370136 ) ) ;
#40949=DIRECTION ( 'NONE',  ( -0.9441882088883105650, 0.3294064756441258957, 0.000000000000000000 ) ) ;
#40951=CARTESIAN_POINT ( 'NONE',  ( -5.156079666866680178, -47.20144821879819830, -5.042520396575470798 ) ) ;
#40952=CARTESIAN_POINT ( 'NONE',  ( 47.21369982259609799, 23.55075984592539839, -54.62698095723159497 ) ) ;
#40955=CARTESIAN_POINT ( 'NONE',  ( 10.99341259034149942, 33.83928202847379652, -17.55111665511150321 ) ) ;
#40959=CARTESIAN_POINT ( 'NONE',  ( 59.93954269256689571, -46.08041885259859782, -47.78497886280250384 ) ) ;
#40961=CARTESIAN_POINT ( 'NONE',  ( 53.21122265239769433, 20.71035719222260241, -53.42198562142930029 ) ) ;
#40962=AXIS2_PLACEMENT_3D ( 'NONE', #36047, #158, #16394 ) ;
#40966=EDGE_LOOP ( 'NONE', ( #3094, #5012, #47765, #27055 ) ) ;
#40968=CARTESIAN_POINT ( 'NONE',  ( 9.275098868232870331, 31.89349584429000117, -46.53342726108229499 ) ) ;
#40970=VECTOR ( 'NONE', #51649, 1000.000000000000000 ) ;
#40972=CIRCLE ( 'NONE', #14193, 1.999999999999998446 ) ;
#40974=CARTESIAN_POINT ( 'NONE',  ( 66.71248721992220965, -29.77431715107189802, -17.03569988378740163 ) ) ;
#40976=CARTESIAN_POINT ( 'NONE',  ( 18.62136613317600009, 20.52576179366229780, -75.06145659859170394 ) ) ;
#40978=EDGE_CURVE ( 'NONE', #5671, #19643, #8528, .T. ) ;
#40981=ORIENTED_EDGE ( 'NONE', *, *, #44423, .F. ) ;
#40982=CARTESIAN_POINT ( 'NONE',  ( 12.92578146920380000, -65.51322971429019049, -47.67849912756199871 ) ) ;
#40983=CARTESIAN_POINT ( 'NONE',  ( 57.18780975371719677, -45.32813116653040453, -25.90209649327980301 ) ) ;
#40985=ADVANCED_FACE ( 'NONE', ( #46843 ), #44040, .T. ) ;
#40986=CARTESIAN_POINT ( 'NONE',  ( 61.60447260105160439, 13.96386167667579947, -46.92884096198559263 ) ) ;
#40990=DIRECTION ( 'NONE',  ( 0.3805321250008310008, 0.000000000000000000, -0.9247677015566404535 ) ) ;
#40995=ORIENTED_EDGE ( 'NONE', *, *, #47384, .F. ) ;
#40998=CARTESIAN_POINT ( 'NONE',  ( 47.04949829066929823, -54.45405841347059805, -75.29717685666371096 ) ) ;
#40999=LINE ( 'NONE', #37328, #3607 ) ;
#41000=ADVANCED_FACE ( 'NONE', ( #39484 ), #3582, .T. ) ;
#41002=CARTESIAN_POINT ( 'NONE',  ( 13.00893796619580023, 34.28605843179359880, -23.32157451048000141 ) ) ;
#41003=CARTESIAN_POINT ( 'NONE',  ( -11.32734370190460105, 10.64934056395049922, -6.430192534648650593 ) ) ;
#41004=AXIS2_PLACEMENT_3D ( 'NONE', #45512, #21629, #37634 ) ;
#41007=CARTESIAN_POINT ( 'NONE',  ( 11.34401365722481536, 24.09645396166900611, -21.54733585199151236 ) ) ;
#41008=CARTESIAN_POINT ( 'NONE',  ( 37.63393739769620083, -15.61618894467929941, -11.65000000000000036 ) ) ;
#41009=CIRCLE ( 'NONE', #25085, 30.99999999999999645 ) ;
#41011=B_SPLINE_SURFACE_WITH_KNOTS ( 'NONE', 3, 3, ( 
 ( #34999, #51267, #51004, #11178, #27145, #15362, #19540, #51521, #47594, #24213 ),
 ( #20552, #25262, #32339, #4850, #21077, #48101, #21334, #37080, #40237, #1177 ),
 ( #17173, #24475, #12452, #41268, #37339, #4328, #32595, #20297, #48358, #12990 ),
 ( #48886, #40487, #5124, #36285, #36810, #28941, #44945, #28422, #12200, #33125 ),
 ( #4579, #24736, #8785, #9318, #9046, #16121, #49153, #32082, #13249, #36548 ) ),
 .UNSPECIFIED., .F., .F., .F.,
 ( 4, 1, 4 ),
 ( 4, 2, 2, 2, 4 ),
 ( 0.000000000000000000, 0.5000000000000000000, 1.000000000000000000 ),
 ( -5.804775000000000375E-14, 0.9800148840114050186, 2.548038698429749616, 5.056876801499090135, 7.840119072091650487 ),
 .UNSPECIFIED. ) ;
#41013=CARTESIAN_POINT ( 'NONE',  ( -11.32756203325930144, -41.88149018212450159, -6.430250179200330152 ) ) ;
#41014=CARTESIAN_POINT ( 'NONE',  ( 12.45971295116610023, 34.17435175702340189, -46.68166270206700119 ) ) ;
#41017=CARTESIAN_POINT ( 'NONE',  ( 47.10255859972780712, 23.39255633749860053, -75.00952388492770240 ) ) ;
#41018=CARTESIAN_POINT ( 'NONE',  ( 49.45469051709810060, -53.54401829445560423, -54.26811687044310162 ) ) ;
#41019=CARTESIAN_POINT ( 'NONE',  ( 41.66707677620669870, -44.64833008590599661, -5.278831885195840457 ) ) ;
#41026=ORIENTED_EDGE ( 'NONE', *, *, #39971, .T. ) ;
#41027=CARTESIAN_POINT ( 'NONE',  ( 54.71776772591253035, -45.61739577595168527, -15.43675199817832500 ) ) ;
#41028=CARTESIAN_POINT ( 'NONE',  ( 60.61561495333980076, -45.70472510158130319, -47.62765810040219350 ) ) ;
#41029=DIRECTION ( 'NONE',  ( 0.000000000000000000, 0.000000000000000000, -1.000000000000000000 ) ) ;
#41032=CARTESIAN_POINT ( 'NONE',  ( 32.63393739769630031, -15.61618894467929941, -6.649999999999999467 ) ) ;
#41035=ORIENTED_EDGE ( 'NONE', *, *, #10791, .T. ) ;
#41036=CARTESIAN_POINT ( 'NONE',  ( 83.86237639949339950, -44.73853788847340240, -47.35515635286719771 ) ) ;
#41037=VERTEX_POINT ( 'NONE', #38714 ) ;
#41039=ORIENTED_EDGE ( 'NONE', *, *, #13740, .F. ) ;
#41040=EDGE_LOOP ( 'NONE', ( #17245, #45495, #34532, #24568 ) ) ;
#41041=CARTESIAN_POINT ( 'NONE',  ( 61.50451778728459828, -45.34291071716570087, -47.29822066312470241 ) ) ;
#41045=CARTESIAN_POINT ( 'NONE',  ( 76.39434454947775066, -13.53395835587781626, -12.77213375745345481 ) ) ;
#41052=FACE_OUTER_BOUND ( 'NONE', #49248, .T. ) ;
#41053=CARTESIAN_POINT ( 'NONE',  ( 56.52293937402539825, 19.39991365250580202, -53.14906066056489919 ) ) ;
#41054=LINE ( 'NONE', #5166, #6188 ) ;
#41058=ORIENTED_EDGE ( 'NONE', *, *, #14370, .T. ) ;
#41059=B_SPLINE_CURVE_WITH_KNOTS ( 'NONE', 3,
 ( #45085, #46398, #50573, #22250, #6813, #30373, #34043, #14147 ),
 .UNSPECIFIED., .F., .F.,
 ( 4, 2, 2, 4 ),
 ( 0.5000003605123823913, 0.6250000000001332268, 0.8250000000000607958, 1.000000000000000000 ),
 .UNSPECIFIED. ) ;
#41061=CARTESIAN_POINT ( 'NONE',  ( 52.91674793875649385, -50.26601136226660316, -77.24667101312410011 ) ) ;
#41063=CARTESIAN_POINT ( 'NONE',  ( 60.31436991762949873, 14.50714379426369938, -47.22798074803809953 ) ) ;
#41069=CARTESIAN_POINT ( 'NONE',  ( 42.70036219403750266, -44.15320494937070350, -5.071714815372149410 ) ) ;
#41070=CARTESIAN_POINT ( 'NONE',  ( 69.22748654599971019, -50.70395984888047991, -72.15645085170115181 ) ) ;
#41071=CARTESIAN_POINT ( 'NONE',  ( 67.77185291767722219, 1.249071374518028188, -19.08055332124363446 ) ) ;
#41073=CARTESIAN_POINT ( 'NONE',  ( 17.36723149245495179, -52.99263552516109854, -76.14999999999999147 ) ) ;
#41074=CARTESIAN_POINT ( 'NONE',  ( 67.77844493121459379, 0.7065659173237569535, -18.45139661994250346 ) ) ;
#41076=CARTESIAN_POINT ( 'NONE',  ( 14.12318226124150122, -51.80504026018019914, -75.54815173289030383 ) ) ;
#41077=CARTESIAN_POINT ( 'NONE',  ( 57.25380934771570196, 19.38381105532069881, -53.86267014602349690 ) ) ;
#41078=CARTESIAN_POINT ( 'NONE',  ( 18.38332385620206111, 20.94377882893676102, -75.56421372420827254 ) ) ;
#41079=DIRECTION ( 'NONE',  ( 0.000000000000000000, 0.000000000000000000, -1.000000000000000000 ) ) ;
#41081=AXIS2_PLACEMENT_3D ( 'NONE', #41536, #32608, #37600 ) ;
#41083=CARTESIAN_POINT ( 'NONE',  ( 55.29972780508609986, -46.05201784173636526, -16.43382449896097697 ) ) ;
#41084=AXIS2_PLACEMENT_3D ( 'NONE', #26937, #46883, #27447 ) ;
#41085=CARTESIAN_POINT ( 'NONE',  ( 47.75981413591419766, -54.46820368462779527, -54.94005077776210300 ) ) ;
#41086=CARTESIAN_POINT ( 'NONE',  ( 13.89738755482740018, 19.98851976907650041, -22.99807273771689964 ) ) ;
#41087=CARTESIAN_POINT ( 'NONE',  ( -9.066986571212598989, -44.13582524313829936, -5.880785460427049749 ) ) ;
#41088=CARTESIAN_POINT ( 'NONE',  ( 56.46191916141020073, 19.54532074681500120, -53.81431225014880226 ) ) ;
#41089=CARTESIAN_POINT ( 'NONE',  ( 42.70036219816795153, 12.92082705528767583, -5.071714813363838559 ) ) ;
#41090=CARTESIAN_POINT ( 'NONE',  ( 48.78347455189079795, 22.74609578351320138, -54.78766944749870049 ) ) ;
#41093=ORIENTED_EDGE ( 'NONE', *, *, #10880, .F. ) ;
#41094=FACE_OUTER_BOUND ( 'NONE', #20211, .T. ) ;
#41097=CARTESIAN_POINT ( 'NONE',  ( 84.44784216359251161, 11.88381105532070059, -47.47585302082339354 ) ) ;
#41098=CARTESIAN_POINT ( 'NONE',  ( 52.66668290531129770, 18.52378580962789911, -27.74344827129370117 ) ) ;
#41103=EDGE_LOOP ( 'NONE', ( #4849, #17900, #43876, #18482, #19255, #22786, #13197, #42909, #27128 ) ) ;
#41104=EDGE_CURVE ( 'NONE', #5682, #43692, #7980, .T. ) ;
#41106=CARTESIAN_POINT ( 'NONE',  ( 11.59391792476989913, -64.95860477368741215, -16.50763286606999714 ) ) ;
#41107=CARTESIAN_POINT ( 'NONE',  ( 11.65647435635129980, 33.66779149316020181, -45.60641158798500072 ) ) ;
#41109=CARTESIAN_POINT ( 'NONE',  ( 47.69072379162619768, -54.40457714162659641, -54.20239749881680069 ) ) ;
#41112=CARTESIAN_POINT ( 'NONE',  ( 10.67151123448148375, 24.00903292272008827, -45.35245340590078200 ) ) ;
#41118=( BOUNDED_CURVE ( )  B_SPLINE_CURVE ( 3, ( #15454, #36127, #232, #48187 ),
 .UNSPECIFIED., .F., .T. ) 
 B_SPLINE_CURVE_WITH_KNOTS ( ( 4, 4 ),
 ( 0.000000000000000000, 0.8959462480744248003 ),
 .UNSPECIFIED. ) 
 CURVE ( )  GEOMETRIC_REPRESENTATION_ITEM ( )  RATIONAL_B_SPLINE_CURVE ( ( 1.000000000000000000, 0.9342179155434778837, 0.9342179155434778837, 1.000000000000000000 ) ) 
 REPRESENTATION_ITEM ( '' )  );
#41119=ORIENTED_EDGE ( 'NONE', *, *, #24530, .F. ) ;
#41120=CARTESIAN_POINT ( 'NONE',  ( 55.91595722987329964, -45.90465052577939531, -25.32543029193989881 ) ) ;
#41121=VECTOR ( 'NONE', #13923, 1000.000000000000227 ) ;
#41123=ORIENTED_EDGE ( 'NONE', *, *, #38966, .T. ) ;
#41124=CARTESIAN_POINT ( 'NONE',  ( 12.64094934536730364, -55.46337509643738173, -75.46694760811912772 ) ) ;
#41128=CARTESIAN_POINT ( 'NONE',  ( 55.90673615822279885, 19.65302146644049941, -74.84519705601209694 ) ) ;
#41129=EDGE_CURVE ( 'NONE', #21618, #42976, #36558, .T. ) ;
#41130=CARTESIAN_POINT ( 'NONE',  ( 47.32558733251070038, -54.23003007210349580, -75.35929005681119008 ) ) ;
#41132=CARTESIAN_POINT ( 'NONE',  ( 55.99603443303359285, 14.48522708022579941, -17.30520569459709890 ) ) ;
#41133=CARTESIAN_POINT ( 'NONE',  ( 57.27159525777589977, -50.25201018848400025, -52.75109249795529109 ) ) ;
#41136=CARTESIAN_POINT ( 'NONE',  ( 47.09676272639270422, 22.96834012079289877, -75.51614565245159838 ) ) ;
#41139=CARTESIAN_POINT ( 'NONE',  ( 12.36320305067610015, 33.31445045643330616, -15.76422791930239953 ) ) ;
#41145=CARTESIAN_POINT ( 'NONE',  ( -17.48391069661419905, -50.96347608314179922, -52.50953498851679768 ) ) ;
#41146=ORIENTED_EDGE ( 'NONE', *, *, #33117, .T. ) ;
#41147=VECTOR ( 'NONE', #32103, 1000.000000000000000 ) ;
#41148=CARTESIAN_POINT ( 'NONE',  ( 53.13753028352629570, -49.50378124343389885, -48.89206903948300464 ) ) ;
#41150=CARTESIAN_POINT ( 'NONE',  ( 61.64818500071270080, -45.11839462663610334, -27.88144317553240015 ) ) ;
#41151=CARTESIAN_POINT ( 'NONE',  ( 63.88393739769619373, 11.88381105532070059, -61.44999999999999574 ) ) ;
#41152=CARTESIAN_POINT ( 'NONE',  ( 57.39314836427140420, 14.50720453784729891, -26.25563593084900305 ) ) ;
#41153=VECTOR ( 'NONE', #8830, 1000.000000000000000 ) ;
#41155=CARTESIAN_POINT ( 'NONE',  ( 51.18091049923660307, 19.51488979195089968, -76.16568857009508520 ) ) ;
#41156=CARTESIAN_POINT ( 'NONE',  ( 53.20332254885359902, 18.25314851316870346, -48.99213401679070046 ) ) ;
#41158=CARTESIAN_POINT ( 'NONE',  ( 16.13393739769620083, -15.61618894467929941, -21.14999999999999858 ) ) ;
#41159=CARTESIAN_POINT ( 'NONE',  ( 69.10082108401860523, -43.71177200353350401, -11.63456562794259952 ) ) ;
#41161=ADVANCED_FACE ( 'NONE', ( #28688 ), #32866, .F. ) ;
#41166=CARTESIAN_POINT ( 'NONE',  ( 47.46364465723310389, -54.60385569402070161, -54.65913311076389647 ) ) ;
#41167=CARTESIAN_POINT ( 'NONE',  ( -2.623662905535780077, 17.43154064245049994, -4.296538310234220504 ) ) ;
#41169=CARTESIAN_POINT ( 'NONE',  ( 56.75852129267509838, 18.90901482631310060, -52.43727812511399833 ) ) ;
#41171=EDGE_CURVE ( 'NONE', #12686, #40179, #16393, .T. ) ;
#41178=EDGE_LOOP ( 'NONE', ( #33422, #33677, #50851, #1161 ) ) ;
#41180=CARTESIAN_POINT ( 'NONE',  ( 13.68997055320560108, -51.35827251201860122, -23.13969638325859890 ) ) ;
#41181=CARTESIAN_POINT ( 'NONE',  ( 15.05440318628110141, 21.88381105532300097, -76.14999999999999147 ) ) ;
#41182=ORIENTED_EDGE ( 'NONE', *, *, #15945, .T. ) ;
#41184=LINE ( 'NONE', #41435, #41954 ) ;
#41185=DIRECTION ( 'NONE',  ( 0.4640893551880597712, 0.8857883891771956009, 0.000000000000000000 ) ) ;
#41186=CARTESIAN_POINT ( 'NONE',  ( 53.33359353556529925, 19.40928134151669937, -76.65020911032560491 ) ) ;
#41190=CARTESIAN_POINT ( 'NONE',  ( 50.03007040746459921, 17.38381105532069881, -76.14999999999999147 ) ) ;
#41194=EDGE_CURVE ( 'NONE', #19736, #14545, #23968, .T. ) ;
#41196=FACE_OUTER_BOUND ( 'NONE', #2701, .T. ) ;
#41198=VECTOR ( 'NONE', #20580, 1000.000000000000000 ) ;
#41201=CARTESIAN_POINT ( 'NONE',  ( 14.24699128871759868, 20.74698410172580054, -75.72128529899769944 ) ) ;
#41202=CARTESIAN_POINT ( 'NONE',  ( 51.95831930592699877, 18.21933529978510080, -77.09973198023169516 ) ) ;
#41203=CARTESIAN_POINT ( 'NONE',  ( 82.49223220840650583, -45.10152342427350192, -46.59234684980519603 ) ) ;
#41204=ADVANCED_FACE ( 'NONE', ( #51783 ), #20564, .F. ) ;
#41206=EDGE_LOOP ( 'NONE', ( #4792, #49737, #44403, #32452 ) ) ;
#41207=CARTESIAN_POINT ( 'NONE',  ( 55.95580649448950084, -45.88747549310949836, -25.57469933290609987 ) ) ;
#41208=CARTESIAN_POINT ( 'NONE',  ( 54.43935813201120055, -51.17211618503599624, -75.39236096530039788 ) ) ;
#41210=DIRECTION ( 'NONE',  ( -0.6911981449639438280, -0.7226652920947587155, -3.885780586188048385E-16 ) ) ;
#41212=ORIENTED_EDGE ( 'NONE', *, *, #14001, .T. ) ;
#41213=CARTESIAN_POINT ( 'NONE',  ( -5.658245767086419242, -46.75968762783350030, -4.712742916676430305 ) ) ;
#41214=CARTESIAN_POINT ( 'NONE',  ( 47.29521656555830589, 23.49172283449389909, -54.72089720754819808 ) ) ;
#41217=CARTESIAN_POINT ( 'NONE',  ( 57.31533492135169894, -50.46532389091750304, -53.15033574623170409 ) ) ;
#41218=CARTESIAN_POINT ( 'NONE',  ( 11.79333626495519916, 34.19002346076609911, -17.82631612918970276 ) ) ;
#41222=CARTESIAN_POINT ( 'NONE',  ( 57.05080397350140231, -47.54530775247659591, -48.23310989717779762 ) ) ;
#41223=CARTESIAN_POINT ( 'NONE',  ( 16.13393739769620083, -15.61618894467929941, -6.721843382729280059 ) ) ;
#41224=CARTESIAN_POINT ( 'NONE',  ( 52.32346883964469697, 21.19168061802760050, -53.80955079009429909 ) ) ;
#41230=CARTESIAN_POINT ( 'NONE',  ( 9.744550898871700895, 32.05767636941019560, -46.29747639044499863 ) ) ;
#41232=CARTESIAN_POINT ( 'NONE',  ( 31.37998729184774405, -15.61618894467929941, -7.101316701949489385 ) ) ;
#41234=EDGE_CURVE ( 'NONE', #37257, #6515, #46704, .T. ) ;
#41236=CARTESIAN_POINT ( 'NONE',  ( 18.14361831065170350, 20.57417486552859742, -75.54540032568610286 ) ) ;
#41237=VERTEX_POINT ( 'NONE', #21864 ) ;
#41241=CARTESIAN_POINT ( 'NONE',  ( 11.56804367855430016, -65.08699574139150457, -46.73148076027570141 ) ) ;
#41242=CARTESIAN_POINT ( 'NONE',  ( 56.34549632421120435, -45.90303496147449636, -26.05542634681239988 ) ) ;
#41245=CARTESIAN_POINT ( 'NONE',  ( 61.64879318626500293, 13.92293292261859960, -46.76047835613849202 ) ) ;
#41250=CARTESIAN_POINT ( 'NONE',  ( 50.81623145755629878, -45.20523958689630462, -11.75436512841420011 ) ) ;
#41251=AXIS2_PLACEMENT_3D ( 'NONE', #37493, #13654, #49307 ) ;
#41253=FACE_OUTER_BOUND ( 'NONE', #42409, .T. ) ;
#41254=ORIENTED_EDGE ( 'NONE', *, *, #46241, .T. ) ;
#41256=CARTESIAN_POINT ( 'NONE',  ( 46.71028574728679672, -53.65544939505299737, -75.98322477344710535 ) ) ;
#41257=CARTESIAN_POINT ( 'NONE',  ( 60.41031538789670208, 14.61374794153990031, -47.73939764575179368 ) ) ;
#41258=CARTESIAN_POINT ( 'NONE',  ( 50.01275137939290261, 14.95673839075170086, -12.46590880385850042 ) ) ;
#41259=DIRECTION ( 'NONE',  ( -0.6653150774946533508, -0.7465626883646701017, 0.000000000000000000 ) ) ;
#41262=AXIS2_PLACEMENT_3D ( 'NONE', #22159, #11172, #6464 ) ;
#41264=CARTESIAN_POINT ( 'NONE',  ( 61.58984847289840303, 13.89565763300190149, -28.15139565950990175 ) ) ;
#41267=VERTEX_POINT ( 'NONE', #45475 ) ;
#41268=CARTESIAN_POINT ( 'NONE',  ( 58.95547274812099658, 15.24358996499610086, -47.69626354652410072 ) ) ;
#41273=CARTESIAN_POINT ( 'NONE',  ( 11.28671405514150017, -65.00701117576899435, -16.86100849032779792 ) ) ;
#41276=CARTESIAN_POINT ( 'NONE',  ( 49.24754892657740157, -53.85074344983969752, -55.23177050136099808 ) ) ;
#41279=CARTESIAN_POINT ( 'NONE',  ( 60.68764924188080556, -0.5980872046737689685, -16.28104295442377847 ) ) ;
#41280=CARTESIAN_POINT ( 'NONE',  ( 18.48305433236689765, -51.32863061914290626, -74.59027663912431194 ) ) ;
#41282=ORIENTED_EDGE ( 'NONE', *, *, #34835, .F. ) ;
#41287=CARTESIAN_POINT ( 'NONE',  ( 60.95712442611549875, -45.66700790346930461, -47.71416869798230209 ) ) ;
#41288=DIRECTION ( 'NONE',  ( -1.000000000000000000, 0.000000000000000000, 0.000000000000000000 ) ) ;
#41289=CARTESIAN_POINT ( 'NONE',  ( 50.90851972497010536, 19.66920513271909954, -76.14999999999999147 ) ) ;
#41292=CARTESIAN_POINT ( 'NONE',  ( 51.08534762786979400, -51.03566300605200468, -76.14824064460249531 ) ) ;
#41294=EDGE_CURVE ( 'NONE', #40081, #24770, #14843, .T. ) ;
#41295=EDGE_LOOP ( 'NONE', ( #15229, #44729 ) ) ;
#41296=ORIENTED_EDGE ( 'NONE', *, *, #5872, .F. ) ;
#41299=CARTESIAN_POINT ( 'NONE',  ( 61.42101946455129990, -45.29358752071379968, -47.17308591776039606 ) ) ;
#41300=CARTESIAN_POINT ( 'NONE',  ( 47.18324681005260146, -54.80726426785999905, -54.61059023070370699 ) ) ;
#41302=CARTESIAN_POINT ( 'NONE',  ( 55.58382303305679528, -50.93169950793019751, -53.05694829722840211 ) ) ;
#41304=ORIENTED_EDGE ( 'NONE', *, *, #28926, .T. ) ;
#41306=ORIENTED_EDGE ( 'NONE', *, *, #14014, .F. ) ;
#41312=CARTESIAN_POINT ( 'NONE',  ( 2.457383035027194129, 23.39947848051994939, -8.319647256471711216 ) ) ;
#41313=CARTESIAN_POINT ( 'NONE',  ( 52.81902783802529910, -50.66264935548120718, -76.50043241030529373 ) ) ;
#41315=CARTESIAN_POINT ( 'NONE',  ( 83.95017614158776098, -44.74867211454660776, -47.46180894508327697 ) ) ;
#41319=CARTESIAN_POINT ( 'NONE',  ( 45.45709021471650146, 14.00253322601350092, -8.052805789834080130 ) ) ;
#41320=CARTESIAN_POINT ( 'NONE',  ( 42.20562640647980146, -44.31827357521319755, -5.077271965990960645 ) ) ;
#41322=CARTESIAN_POINT ( 'NONE',  ( 16.13393739769620083, -15.61618894467929941, -21.14999999999999858 ) ) ;
#41325=CARTESIAN_POINT ( 'NONE',  ( 66.55657083749090930, -1.025637880372419986, -16.96067586332220145 ) ) ;
#41327=CARTESIAN_POINT ( 'NONE',  ( 14.06555357016280006, -51.72389970538209525, -75.45052476223459337 ) ) ;
#41328=EDGE_CURVE ( 'NONE', #33083, #39662, #36472, .T. ) ;
#41329=CARTESIAN_POINT ( 'NONE',  ( 57.27213619417380386, 19.37967000028660181, -53.75872744438189699 ) ) ;
#41330=EDGE_CURVE ( 'NONE', #2432, #12711, #46003, .T. ) ;
#41332=CIRCLE ( 'NONE', #27123, 3.500000000000003109 ) ;
#41335=CARTESIAN_POINT ( 'NONE',  ( 54.47259832750690123, -46.25232753665150653, -15.76422791930239953 ) ) ;
#41339=CARTESIAN_POINT ( 'NONE',  ( 56.44840490959330026, 19.52003022522620412, -53.50788452149080143 ) ) ;
#41340=CARTESIAN_POINT ( 'NONE',  ( 48.66928706773219915, 22.73500733612779712, -54.62024785781569847 ) ) ;
#41346=CARTESIAN_POINT ( 'NONE',  ( 50.95182575631829991, 19.71852405838109945, -78.14999999999999147 ) ) ;
#41347=CARTESIAN_POINT ( 'NONE',  ( 84.41763914545359171, 12.29456635737889947, -47.43918784650060161 ) ) ;
#41348=CARTESIAN_POINT ( 'NONE',  ( 54.20264060170759990, 16.79968848045730212, -26.08911483772730122 ) ) ;
#41351=CARTESIAN_POINT ( 'NONE',  ( 55.48947750614289731, -45.11618894467940066, -14.40595025803260043 ) ) ;
#41352=EDGE_CURVE ( 'NONE', #26727, #24020, #33583, .T. ) ;
#41357=VERTEX_POINT ( 'NONE', #3391 ) ;
#41358=CARTESIAN_POINT ( 'NONE',  ( 11.66836325772209904, -64.97277996009040635, -16.48189043738600290 ) ) ;
#41359=CARTESIAN_POINT ( 'NONE',  ( 13.00893739769619906, 34.28605925116850273, -47.75434321273180416 ) ) ;
#41360=CARTESIAN_POINT ( 'NONE',  ( 55.10456381066440201, 13.97851885024129892, -14.92011627202030155 ) ) ;
#41363=ORIENTED_EDGE ( 'NONE', *, *, #828, .T. ) ;
#41367=CARTESIAN_POINT ( 'NONE',  ( 13.80986494171299483, 20.88376505836721364, -75.46937998419059568 ) ) ;
#41368=CARTESIAN_POINT ( 'NONE',  ( 59.34401236131339630, -2.970618261826989848, -15.68001078640890178 ) ) ;
#41374=CARTESIAN_POINT ( 'NONE',  ( 70.83745409581385388, 17.98087126524510637, -71.50000000000081002 ) ) ;
#41376=CARTESIAN_POINT ( 'NONE',  ( 55.27618969335288313, -51.00839723918451085, -75.15723747982120528 ) ) ;
#41377=CARTESIAN_POINT ( 'NONE',  ( 48.91612765617589531, -46.17266810153950019, -11.68042562226399994 ) ) ;
#41380=CARTESIAN_POINT ( 'NONE',  ( 53.83029454980940187, 19.62285200761009918, -76.11627055017599730 ) ) ;
#41381=CARTESIAN_POINT ( 'NONE',  ( 46.35275103504449845, -52.90993241930539881, -76.14999999999999147 ) ) ;
#41383=CARTESIAN_POINT ( 'NONE',  ( 54.50029541982960524, 14.92341241185250134, -15.72721313530920106 ) ) ;
#41384=CARTESIAN_POINT ( 'NONE',  ( 56.93466175439829868, -50.26424374751940150, -52.70269902980160026 ) ) ;
#41385=CARTESIAN_POINT ( 'NONE',  ( 52.63829942681260121, -49.80293474851259816, -48.69642957805589845 ) ) ;
#41389=CARTESIAN_POINT ( 'NONE',  ( 46.50762589553990267, 21.90427357326890245, -76.13714234130850400 ) ) ;
#41392=CARTESIAN_POINT ( 'NONE',  ( 61.00705302608983516, -45.67218455906213137, -47.73074504205541047 ) ) ;
#41396=CARTESIAN_POINT ( 'NONE',  ( 68.13393739769620083, 4.883811055320659733, -65.65000000000000568 ) ) ;
#41402=CARTESIAN_POINT ( 'NONE',  ( 6.211423689671518922, -64.98190781011250294, -48.42816009188030080 ) ) ;
#41403=ORIENTED_EDGE ( 'NONE', *, *, #12008, .T. ) ;
#41404=CARTESIAN_POINT ( 'NONE',  ( 52.72266114154869854, -49.72553381474750012, -48.47378032971909789 ) ) ;
#41406=CARTESIAN_POINT ( 'NONE',  ( 61.66998612247429890, -45.11833688862720493, -28.01639554107829966 ) ) ;
#41407=CARTESIAN_POINT ( 'NONE',  ( 48.76904876940009359, -54.05456627190059749, -55.30034376619679648 ) ) ;
#41408=CARTESIAN_POINT ( 'NONE',  ( 13.32539556584979934, 19.89887940024619795, -21.90066023095720027 ) ) ;
#41409=CARTESIAN_POINT ( 'NONE',  ( 55.91421057036799880, 14.69455263003700018, -25.53646976440970207 ) ) ;
#41411=CARTESIAN_POINT ( 'NONE',  ( 50.52803440128089818, 19.14656596045000114, -76.14999999999999147 ) ) ;
#41412=CARTESIAN_POINT ( 'NONE',  ( 52.72966687298379895, 18.49590603975559588, -48.70009282041390009 ) ) ;
#41413=CARTESIAN_POINT ( 'NONE',  ( 60.61194832405840316, -45.58361201891599990, -47.15894465080069864 ) ) ;
#41414=CARTESIAN_POINT ( 'NONE',  ( 64.87855344762060383, -43.72806524318039578, -10.46215703267770003 ) ) ;
#41417=EDGE_CURVE ( 'NONE', #4867, #49956, #26442, .T. ) ;
#41419=CARTESIAN_POINT ( 'NONE',  ( 47.52424585455850092, -54.57167504433569860, -54.72304599233210354 ) ) ;
#41422=( BOUNDED_CURVE ( )  B_SPLINE_CURVE ( 3, ( #17938, #50441, #26045, #26307 ),
 .UNSPECIFIED., .F., .T. ) 
 B_SPLINE_CURVE_WITH_KNOTS ( ( 4, 4 ),
 ( 0.7853981633974366217, 1.053572925743754274 ),
 .UNSPECIFIED. ) 
 CURVE ( )  GEOMETRIC_REPRESENTATION_ITEM ( )  RATIONAL_B_SPLINE_CURVE ( ( 1.000000000000000000, 0.9940158321278126374, 0.9940158321278126374, 1.000000000000000000 ) ) 
 REPRESENTATION_ITEM ( '' )  );
#41423=CARTESIAN_POINT ( 'NONE',  ( 60.34156420439850876, 15.53871978590400005, -48.95535497881819964 ) ) ;
#41431=CARTESIAN_POINT ( 'NONE',  ( 13.65323237295500114, -51.39160756102839400, -23.15000000000000213 ) ) ;
#41432=CARTESIAN_POINT ( 'NONE',  ( 15.94849651692706338, -50.98802678465642657, -15.66350744312629217 ) ) ;
#41435=CARTESIAN_POINT ( 'NONE',  ( -4.666062602303798990, -15.61618894467930119, -11.54999999999999893 ) ) ;
#41437=CARTESIAN_POINT ( 'NONE',  ( 53.60866038548149959, 19.65083965924290155, -76.14577118446059956 ) ) ;
#41438=ORIENTED_EDGE ( 'NONE', *, *, #40756, .T. ) ;
#41442=B_SPLINE_SURFACE_WITH_KNOTS ( 'NONE', 3, 3, ( 
 ( #51229, #43109, #23155, #2751, #15581, #23411 ),
 ( #18981, #6949, #3530, #3267, #44313, #4478 ),
 ( #31275, #22646, #27358, #24370, #39431, #38918 ),
 ( #19501, #47554, #35491, #47049, #11396, #18723 ),
 ( #50451, #3009, #14540, #14801, #43365, #51482 ),
 ( #46533, #26575, #42590, #46788, #31025, #6686 ),
 ( #10879, #34701, #50702, #42852, #11136, #22901 ),
 ( #27105, #7457, #5272, #21223, #45613, #40641 ),
 ( #16799, #16530, #20969, #25672, #41414, #28834 ),
 ( #8674, #1587, #44838, #37486, #49301, #41674 ),
 ( #20706, #45361, #36436, #36697, #41159, #33016 ),
 ( #17576, #9463, #12878, #5009, #8945, #5532 ),
 ( #24887, #33284, #5780, #13649, #49562, #25154 ),
 ( #44573, #21487, #544, #32480, #40899, #37235 ) ),
 .UNSPECIFIED., .F., .F., .F.,
 ( 4, 2, 2, 2, 2, 2, 4 ),
 ( 4, 1, 1, 4 ),
 ( 3.150553799287940215, 8.744225258584139127, 18.73762555410890229, 24.98350073881190170, 28.10643833116330015, 33.10313847892570038, 38.05651419634610022 ),
 ( 0.000000000000000000, 0.3333333333333329818, 0.6666666666666670737, 1.000235426512150028 ),
 .UNSPECIFIED. ) ;
#41444=DIRECTION ( 'NONE',  ( 0.000000000000000000, 0.000000000000000000, 1.000000000000000000 ) ) ;
#41447=CARTESIAN_POINT ( 'NONE',  ( 56.56423663003400293, -46.20304009252470223, -26.26562856521130129 ) ) ;
#41449=CARTESIAN_POINT ( 'NONE',  ( 44.88838914241820532, 14.87646786394859966, -8.899003544310730263 ) ) ;
#41451=CARTESIAN_POINT ( 'NONE',  ( 14.34420360062739874, 19.88380572466640217, -74.33583724502659607 ) ) ;
#41452=EDGE_CURVE ( 'NONE', #35762, #12879, #19206, .T. ) ;
#41456=AXIS2_PLACEMENT_3D ( 'NONE', #38843, #2931, #34886 ) ;
#41460=CARTESIAN_POINT ( 'NONE',  ( 52.86912716173040394, -49.53963500218709726, -27.34061465770520272 ) ) ;
#41461=VECTOR ( 'NONE', #41835, 1000.000000000000000 ) ;
#41462=CARTESIAN_POINT ( 'NONE',  ( 15.92174032689569785, -51.05401459586040147, -20.83925419535820112 ) ) ;
#41463=CARTESIAN_POINT ( 'NONE',  ( 4.229204521551100271, 25.38381512987610122, -9.628996958294839814 ) ) ;
#41465=CARTESIAN_POINT ( 'NONE',  ( 50.01275587524209953, 14.95672356651379964, -12.46590248485050090 ) ) ;
#41467=ORIENTED_EDGE ( 'NONE', *, *, #17913, .F. ) ;
#41468=B_SPLINE_CURVE_WITH_KNOTS ( 'NONE', 3,
 ( #44475, #40542, #4632, #27448, #20869, #36869, #37131, #1489, #37386, #41315 ),
 .UNSPECIFIED., .F., .F.,
 ( 4, 2, 2, 2, 4 ),
 ( 0.000000000000000000, 0.1774999999751137592, 0.3374999999737621770, 0.4374999999729171085, 0.5000013127411032654 ),
 .UNSPECIFIED. ) ;
#41469=CARTESIAN_POINT ( 'NONE',  ( -6.906756203940550343, -45.84230676707479546, -4.921515829384339291 ) ) ;
#41470=CARTESIAN_POINT ( 'NONE',  ( 47.47474619565739573, 23.38248241296770047, -54.92426841363709400 ) ) ;
#41473=CARTESIAN_POINT ( 'NONE',  ( 60.66036711866519937, 14.32586616646070077, -47.11242423095009713 ) ) ;
#41474=CARTESIAN_POINT ( 'NONE',  ( 42.53968775098609711, 12.99877936061140105, -5.088323969512570599 ) ) ;
#41476=CARTESIAN_POINT ( 'NONE',  ( 52.93498290923280081, 18.37341140428640074, -48.74287987618620122 ) ) ;
#41479=CARTESIAN_POINT ( 'NONE',  ( 56.65979965533069418, -47.79656003688090493, -48.39907199131990012 ) ) ;
#41481=CARTESIAN_POINT ( 'NONE',  ( 54.22654478441499748, 20.21700441338549936, -53.14607073534880044 ) ) ;
#41487=LINE ( 'NONE', #2176, #25413 ) ;
#41488=CARTESIAN_POINT ( 'NONE',  ( 10.13923265016959974, 31.95181006972909543, -45.99474826666039462 ) ) ;
#41490=FACE_OUTER_BOUND ( 'NONE', #48608, .T. ) ;
#41495=CARTESIAN_POINT ( 'NONE',  ( 47.64143405402000297, 23.30250925608569901, -55.14905519569659731 ) ) ;
#41496=ORIENTED_EDGE ( 'NONE', *, *, #25587, .T. ) ;
#41497=CARTESIAN_POINT ( 'NONE',  ( 10.32185532229130054, -63.49178473827629432, -45.85329026226229843 ) ) ;
#41498=CARTESIAN_POINT ( 'NONE',  ( 56.94849961771190294, -45.38884577364979833, -25.89141764539759905 ) ) ;
#41501=CARTESIAN_POINT ( 'NONE',  ( 61.54360026869530031, 13.96084431199959930, -46.89388919338750128 ) ) ;
#41503=ORIENTED_EDGE ( 'NONE', *, *, #7411, .F. ) ;
#41504=EDGE_CURVE ( 'NONE', #5359, #34565, #28556, .T. ) ;
#41505=CARTESIAN_POINT ( 'NONE',  ( 75.24376310073057539, 2.809539095331776259, -12.25943769873225442 ) ) ;
#41507=EDGE_LOOP ( 'NONE', ( #1258, #41568, #49948, #49240, #45244 ) ) ;
#41508=CARTESIAN_POINT ( 'NONE',  ( 49.51534909287300223, -45.20344304405800528, -10.82567614850110083 ) ) ;
#41509=TOROIDAL_SURFACE ( 'NONE', #6347, 40.00000000000310507, 2.000000000000059952 ) ;
#41514=CARTESIAN_POINT ( 'NONE',  ( 47.20045633199760005, -54.78545101841919518, -74.36298856109941369 ) ) ;
#41516=VECTOR ( 'NONE', #6926, 1000.000000000000000 ) ;
#41517=CARTESIAN_POINT ( 'NONE',  ( 55.10456381066440201, 13.97851885024129892, -14.92011627202030155 ) ) ;
#41520=CARTESIAN_POINT ( 'NONE',  ( 60.77271789202009700, 13.90791468296399991, -26.82299636899789874 ) ) ;
#41525=CARTESIAN_POINT ( 'NONE',  ( 52.26132335211670465, 19.59060111016600203, -50.93306148729159588 ) ) ;
#41529=CARTESIAN_POINT ( 'NONE',  ( 12.56262532525460074, -39.78532101326960202, -74.14999999999999147 ) ) ;
#41533=CARTESIAN_POINT ( 'NONE',  ( 48.96779238971210191, -53.80776418538130201, -54.50050231667190559 ) ) ;
#41534=AXIS2_PLACEMENT_3D ( 'NONE', #14604, #6753, #14862 ) ;
#41536=CARTESIAN_POINT ( 'NONE',  ( 63.88393739769619373, 20.38443354211860026, -61.44999999999999574 ) ) ;
#41537=CYLINDRICAL_SURFACE ( 'NONE', #35699, 2.000000000000001776 ) ;
#41539=ORIENTED_EDGE ( 'NONE', *, *, #1174, .T. ) ;
#41543=CARTESIAN_POINT ( 'NONE',  ( 55.55365133010059964, -45.11618894467940066, -14.32025150907159983 ) ) ;
#41544=CARTESIAN_POINT ( 'NONE',  ( 61.12101616177810826, -45.46746661123680155, -47.45428572051350358 ) ) ;
#41545=CARTESIAN_POINT ( 'NONE',  ( 1.167123001759671430, -26.49021611209005655, 7.849999999999997868 ) ) ;
#41554=ORIENTED_EDGE ( 'NONE', *, *, #41754, .T. ) ;
#41555=CARTESIAN_POINT ( 'NONE',  ( 61.45294886705139703, -45.16075153748559501, -46.46810862312010215 ) ) ;
#41556=CARTESIAN_POINT ( 'NONE',  ( 53.02878341227049930, -49.61154767067039728, -49.09821772105390636 ) ) ;
#41557=CARTESIAN_POINT ( 'NONE',  ( 48.12002887478553959, -54.05111908400336063, -53.67198234080560582 ) ) ;
#41558=CARTESIAN_POINT ( 'NONE',  ( 54.43067208826479941, -51.42334665385340031, -53.21919371617259742 ) ) ;
#41559=VECTOR ( 'NONE', #46258, 1000.000000000000114 ) ;
#41562=ORIENTED_EDGE ( 'NONE', *, *, #8824, .F. ) ;
#41564=EDGE_CURVE ( 'NONE', #44442, #39070, #20371, .T. ) ;
#41565=B_SPLINE_CURVE_WITH_KNOTS ( 'NONE', 3,
 ( #18028, #18542, #41360, #30058, #6501, #33992 ),
 .UNSPECIFIED., .F., .F.,
 ( 4, 1, 1, 4 ),
 ( 0.000000000000000000, 0.3333333470322403236, 0.6666666937979618401, 1.000000000000000000 ),
 .UNSPECIFIED. ) ;
#41566=CARTESIAN_POINT ( 'NONE',  ( 54.02518786316219490, -51.81565143108780092, -54.18996768095620098 ) ) ;
#41568=ORIENTED_EDGE ( 'NONE', *, *, #16556, .T. ) ;
#41570=CARTESIAN_POINT ( 'NONE',  ( 51.61768760778490162, -50.35895232405650290, -76.35064948397560158 ) ) ;
#41571=CARTESIAN_POINT ( 'NONE',  ( 60.51833370568750325, 14.40028145102449919, -47.19438552604259485 ) ) ;
#41574=TOROIDAL_SURFACE ( 'NONE', #23958, 48.00000000000000000, 2.000000000000000000 ) ;
#41576=CARTESIAN_POINT ( 'NONE',  ( 45.76571748013050467, 13.88566788246860106, -7.589016501219620459 ) ) ;
#41577=CARTESIAN_POINT ( 'NONE',  ( 42.29463402943059691, -44.11680428309589530, -4.936190359317110143 ) ) ;
#41583=CARTESIAN_POINT ( 'NONE',  ( 65.61159314286859967, 0.5046460432913409955, -17.31747064995380114 ) ) ;
#41586=CARTESIAN_POINT ( 'NONE',  ( 14.97377065893240022, -52.94069807145589834, -76.14999999999999147 ) ) ;
#41587=AXIS2_PLACEMENT_3D ( 'NONE', #18505, #49466, #42624 ) ;
#41589=CARTESIAN_POINT ( 'NONE',  ( 9.469557472586508595, 33.05699343160934944, -46.83899467898784508 ) ) ;
#41593=CARTESIAN_POINT ( 'NONE',  ( 7.853097003783780394, -60.52042854835909935, -20.86915960608759946 ) ) ;
#41595=CARTESIAN_POINT ( 'NONE',  ( 56.48532678114089833, 19.53534987139169843, -53.84780880325180163 ) ) ;
#41597=CARTESIAN_POINT ( 'NONE',  ( 48.08307792209969733, 23.04244796336689660, -54.77528017867940235 ) ) ;
#41599=B_SPLINE_CURVE_WITH_KNOTS ( 'NONE', 3,
 ( #14850, #51781, #46841, #7768, #11701, #19294, #42901, #23717, #51274, #15884, #15372 ),
 .UNSPECIFIED., .F., .F.,
 ( 4, 1, 1, 1, 1, 1, 1, 1, 4 ),
 ( 0.000000000000000000, 0.1249775000236086064, 0.2499805368352087664, 0.3749835736468090097, 0.4999866104584091420, 0.6249896472700092742, 0.7499926840816094620, 0.8749957208932096497, 1.000000000000000000 ),
 .UNSPECIFIED. ) ;
#41600=ORIENTED_EDGE ( 'NONE', *, *, #50405, .F. ) ;
#41605=CARTESIAN_POINT ( 'NONE',  ( 82.92203328426339226, 13.96022355596819864, -47.12557951548500057 ) ) ;
#41606=CARTESIAN_POINT ( 'NONE',  ( 53.38525277802689573, 17.73587511727710009, -26.66601672333850104 ) ) ;
#41608=CARTESIAN_POINT ( 'NONE',  ( 11.68991505668612518, 33.67328296886341832, -16.36861125145141216 ) ) ;
#41609=CARTESIAN_POINT ( 'NONE',  ( 56.92059784994150107, -45.11618894467940066, -15.82169481042769732 ) ) ;
#41613=CARTESIAN_POINT ( 'NONE',  ( 11.62560706825669854, -64.94769956958019463, -16.46999247997619875 ) ) ;
#41614=CARTESIAN_POINT ( 'NONE',  ( 11.25984818798209908, 33.08560177680430314, -44.83508380383680247 ) ) ;
#41617=CARTESIAN_POINT ( 'NONE',  ( 16.13393739769620083, -15.61618894467929941, -76.14999999999999147 ) ) ;
#41622=CARTESIAN_POINT ( 'NONE',  ( 53.40028332572070013, -49.44759849848939837, -49.16199268861880256 ) ) ;
#41623=CARTESIAN_POINT ( 'NONE',  ( 52.08434102009589850, 19.14628782832189913, -49.21477419871119707 ) ) ;
#41624=CARTESIAN_POINT ( 'NONE',  ( 60.24110131066720442, -2.014342208693430170, -15.82687703305419724 ) ) ;
#41625=CARTESIAN_POINT ( 'NONE',  ( 50.62541591398729679, -49.13085010712609346, -76.22054775283200456 ) ) ;
#41626=ADVANCED_FACE ( 'NONE', ( #20630 ), #19867, .T. ) ;
#41631=ORIENTED_EDGE ( 'NONE', *, *, #22824, .F. ) ;
#41635=CARTESIAN_POINT ( 'NONE',  ( 52.95214323273720680, -49.63863283588430164, -49.03964316977230453 ) ) ;
#41636=CARTESIAN_POINT ( 'NONE',  ( 13.69516921742209981, -51.31182003115529966, -22.67922162956820031 ) ) ;
#41637=CARTESIAN_POINT ( 'NONE',  ( 53.76985203492770182, 19.90181730786409986, -75.72009270347381005 ) ) ;
#41638=CARTESIAN_POINT ( 'NONE',  ( 47.41051750594289871, -54.24117355536539975, -75.29851419728690587 ) ) ;
#41640=CARTESIAN_POINT ( 'NONE',  ( 55.88004532031900595, 14.19452913225929969, -16.19747281084099910 ) ) ;
#41642=CARTESIAN_POINT ( 'NONE',  ( 56.99190259417219551, -50.63247588150580469, -53.87165542819400343 ) ) ;
#41643=CARTESIAN_POINT ( 'NONE',  ( 52.74474875099170390, -49.74042103855280317, -48.86872004196769836 ) ) ;
#41646=CARTESIAN_POINT ( 'NONE',  ( 41.64265090548820325, -46.42699119287450316, -4.296538310234230273 ) ) ;
#41649=CARTESIAN_POINT ( 'NONE',  ( 46.99746007022550032, 22.70443078719620189, -75.76112237679920725 ) ) ;
#41652=CARTESIAN_POINT ( 'NONE',  ( 75.33555834693952136, -38.13639482886969745, -12.70678390277496739 ) ) ;
#41654=CARTESIAN_POINT ( 'NONE',  ( 43.87440825508269882, -45.06628648458400477, -6.621182746357190396 ) ) ;
#41658=DIRECTION ( 'NONE',  ( 0.000000000000000000, 0.000000000000000000, 1.000000000000000000 ) ) ;
#41660=CARTESIAN_POINT ( 'NONE',  ( 61.26653127891100326, 14.00827977936110003, -46.51747653042859554 ) ) ;
#41662=CARTESIAN_POINT ( 'NONE',  ( -12.80120649412369893, 25.67501472466429746, -52.53814278327410392 ) ) ;
#41663=ORIENTED_EDGE ( 'NONE', *, *, #37719, .F. ) ;
#41664=CARTESIAN_POINT ( 'NONE',  ( 52.98906690378920104, -49.58008332147559827, -48.84983108313470268 ) ) ;
#41666=CARTESIAN_POINT ( 'NONE',  ( 61.75057827614799777, -45.11618897208180101, -28.00818819871750165 ) ) ;
#41667=CARTESIAN_POINT ( 'NONE',  ( 49.48213591681099643, -53.75081833664790310, -55.18208724449630154 ) ) ;
#41668=CARTESIAN_POINT ( 'NONE',  ( 55.94694845493520319, 14.62810299609100007, -25.32096506064640096 ) ) ;
#41671=CARTESIAN_POINT ( 'NONE',  ( 53.14599511491060468, 18.29042438231470058, -49.02433925890680655 ) ) ;
#41673=CARTESIAN_POINT ( 'NONE',  ( 60.87621821856699711, -45.44515361684550214, -47.03457408321020239 ) ) ;
#41674=CARTESIAN_POINT ( 'NONE',  ( 67.50573363472270216, -43.40389107515569833, -11.14099675621210039 ) ) ;
#41678=CARTESIAN_POINT ( 'NONE',  ( 47.43330265715069771, -54.63190133673469973, -54.73918112570320460 ) ) ;
#41681=CARTESIAN_POINT ( 'NONE',  ( 11.90332973437990027, -65.43688732449989232, -18.04110290864220190 ) ) ;
#41685=CIRCLE ( 'NONE', #36613, 20.00000000000001421 ) ;
#41686=CARTESIAN_POINT ( 'NONE',  ( 50.03007040746459921, -32.48240620400619605, -78.14999999999999147 ) ) ;
#41689=CARTESIAN_POINT ( 'NONE',  ( 13.77296168464159898, -51.29346510734379905, -23.09857315614619822 ) ) ;
#41690=EDGE_CURVE ( 'NONE', #39, #12214, #37387, .T. ) ;
#41694=DIRECTION ( 'NONE',  ( 0.000000000000000000, 0.000000000000000000, -1.000000000000000000 ) ) ;
#41695=CARTESIAN_POINT ( 'NONE',  ( 16.13393739769620083, -15.61618894467929941, -20.65000000000000213 ) ) ;
#41696=CARTESIAN_POINT ( 'NONE',  ( 52.96553908380789721, 19.62936139908589794, -76.26079946550269995 ) ) ;
#41700=CARTESIAN_POINT ( 'NONE',  ( 0.5406133260286669628, -43.55985091651039909, -21.14999999999999858 ) ) ;
#41704=B_SPLINE_CURVE_WITH_KNOTS ( 'NONE', 3,
 ( #33718, #29276, #24816, #45022, #13822, #21409 ),
 .UNSPECIFIED., .F., .F.,
 ( 4, 2, 4 ),
 ( 0.4942347057900616236, 0.7471173528950307841, 1.000000000000000000 ),
 .UNSPECIFIED. ) ;
#41705=EDGE_LOOP ( 'NONE', ( #21462, #39638, #38087, #25354, #5262 ) ) ;
#41706=ADVANCED_FACE ( 'NONE', ( #36617 ), #28500, .T. ) ;
#41707=CARTESIAN_POINT ( 'NONE',  ( 18.84631954156857958, 20.57173965347324085, -74.52173647808412227 ) ) ;
#41710=EDGE_CURVE ( 'NONE', #45901, #34463, #2710, .T. ) ;
#41712=CARTESIAN_POINT ( 'NONE',  ( 14.38800548507090049, 20.00715776053360173, -74.86150924066380696 ) ) ;
#41713=CARTESIAN_POINT ( 'NONE',  ( 17.46614295537689188, -52.40467206555150170, -76.02665054608505102 ) ) ;
#41714=CARTESIAN_POINT ( 'NONE',  ( 43.16863801754030305, -45.22759163273670424, -6.804293086635070154 ) ) ;
#41717=AXIS2_PLACEMENT_3D ( 'NONE', #29456, #33386, #34352 ) ;
#41719=AXIS2_PLACEMENT_3D ( 'NONE', #41952, #22528, #29868 ) ;
#41721=CARTESIAN_POINT ( 'NONE',  ( 53.59918250157210196, -48.73737415287079955, -26.59416019702899803 ) ) ;
#41722=CARTESIAN_POINT ( 'NONE',  ( 15.12151582310530173, -51.00866790501009973, -21.37863257647040172 ) ) ;
#41723=CARTESIAN_POINT ( 'NONE',  ( 0.3082428996584600234, 22.56277195501860078, -8.880561424264220349 ) ) ;
#41724=CARTESIAN_POINT ( 'NONE',  ( 12.06284766121009966, 32.21085600226960111, -22.25048313876769868 ) ) ;
#41725=AXIS2_PLACEMENT_3D ( 'NONE', #13714, #13967, #30193 ) ;
#41730=CARTESIAN_POINT ( 'NONE',  ( -6.526761852427129362, -46.19170520793110057, -5.162139400474170081 ) ) ;
#41731=CARTESIAN_POINT ( 'NONE',  ( 47.61834138556270091, 23.27905552449800197, -54.71304456415500539 ) ) ;
#41734=CARTESIAN_POINT ( 'NONE',  ( 60.89647461220410207, 14.20609866861669879, -47.10144183209600044 ) ) ;
#41735=CARTESIAN_POINT ( 'NONE',  ( 41.53147733802239827, 13.48015055944119922, -5.331435674896719767 ) ) ;
#41737=CARTESIAN_POINT ( 'NONE',  ( 52.87018954733409970, 18.40735846197139836, -48.66536493865070412 ) ) ;
#41739=CARTESIAN_POINT ( 'NONE',  ( 56.38058255011799957, -47.94564697141260012, -48.46858237008240167 ) ) ;
#41741=CARTESIAN_POINT ( 'NONE',  ( 52.18370254490579896, 21.34631496022210229, -54.18358737671120196 ) ) ;
#41747=CARTESIAN_POINT ( 'NONE',  ( 10.48840365866050028, 31.96111183504329745, -45.62648676466370290 ) ) ;
#41749=CARTESIAN_POINT ( 'NONE',  ( 65.34026062434320181, -32.03876047116569481, -17.56708739201410197 ) ) ;
#41753=CARTESIAN_POINT ( 'NONE',  ( 68.13393739769620083, -49.36618894467930829, -69.74999999999998579 ) ) ;
#41754=EDGE_CURVE ( 'NONE', #121, #19573, #27822, .T. ) ;
#41755=VERTEX_POINT ( 'NONE', #14278 ) ;
#41756=CARTESIAN_POINT ( 'NONE',  ( 11.18874931098019943, -64.42258565248579316, -45.43117042558289853 ) ) ;
#41757=CARTESIAN_POINT ( 'NONE',  ( 57.02224680057370421, -45.69358534429309771, -26.17123580714500264 ) ) ;
#41766=EDGE_LOOP ( 'NONE', ( #31809, #47183, #22143, #47253, #20449 ) ) ;
#41767=CARTESIAN_POINT ( 'NONE',  ( 51.20902500803299517, -45.20577485588830058, -12.03792161267199923 ) ) ;
#41773=CARTESIAN_POINT ( 'NONE',  ( 47.06284339357189594, -54.38660427466870573, -75.35929005681109061 ) ) ;
#41774=CARTESIAN_POINT ( 'NONE',  ( 56.20234825743239782, 13.88381317902869938, -9.796652857581651830 ) ) ;
#41776=CARTESIAN_POINT ( 'NONE',  ( 50.95182575631829991, -50.95090194773979420, -76.14999999999999147 ) ) ;
#41777=EDGE_CURVE ( 'NONE', #48296, #10465, #11435, .T. ) ;
#41778=CARTESIAN_POINT ( 'NONE',  ( 52.21238886552460201, 21.07428037441609803, -53.50655909053360659 ) ) ;
#41779=CARTESIAN_POINT ( 'NONE',  ( 52.69947992273029769, 19.98405221369169737, -75.94570066465868763 ) ) ;
#41780=CARTESIAN_POINT ( 'NONE',  ( 59.38732174131899910, 13.88378496296120090, -25.87842628801869793 ) ) ;
#41784=CARTESIAN_POINT ( 'NONE',  ( -11.21096888454679963, -42.00339129323769782, -6.430231290899450336 ) ) ;
#41785=CARTESIAN_POINT ( 'NONE',  ( 75.63943938881949691, -41.11453081253210229, -13.15457824778729901 ) ) ;
#41787=AXIS2_PLACEMENT_3D ( 'NONE', #45638, #37511, #13675 ) ;
#41789=DIRECTION ( 'NONE',  ( 0.000000000000000000, 0.000000000000000000, -1.000000000000000000 ) ) ;
#41790=AXIS2_PLACEMENT_3D ( 'NONE', #47550, #43866, #19496 ) ;
#41793=CARTESIAN_POINT ( 'NONE',  ( 47.29473062437306652, -54.09431091756849241, -75.51963295453231240 ) ) ;
#41796=CARTESIAN_POINT ( 'NONE',  ( 76.30778676816969153, -43.27873611837556922, -13.86615964815592683 ) ) ;
#41803=CARTESIAN_POINT ( 'NONE',  ( 60.75061855898859875, -45.69690118108319865, -47.68872599397300149 ) ) ;
#41809=CARTESIAN_POINT ( 'NONE',  ( 41.71811382534419721, -45.72808319846629388, -6.599653652364029455 ) ) ;
#41810=ORIENTED_EDGE ( 'NONE', *, *, #47528, .T. ) ;
#41812=EDGE_CURVE ( 'NONE', #23932, #1009, #2744, .T. ) ;
#41815=CARTESIAN_POINT ( 'NONE',  ( 53.27482191496699926, -49.51724129999239921, -49.18843185985679867 ) ) ;
#41816=CARTESIAN_POINT ( 'NONE',  ( 60.86539860968923676, 14.21958044004319532, -47.09330236170970352 ) ) ;
#41817=EDGE_CURVE ( 'NONE', #37257, #21277, #16435, .T. ) ;
#41818=CARTESIAN_POINT ( 'NONE',  ( 55.64349245618699769, -51.00987811372980474, -53.26417807816250161 ) ) ;
#41821=EDGE_CURVE ( 'NONE', #4059, #21277, #30243, .T. ) ;
#41823=CARTESIAN_POINT ( 'NONE',  ( 11.13393739770110002, -63.48207374982479934, -22.73376795960439978 ) ) ;
#41824=CARTESIAN_POINT ( 'NONE',  ( 47.64143405402000297, 23.30250925608569901, -55.14905519569659731 ) ) ;
#41825=B_SPLINE_CURVE_WITH_KNOTS ( 'NONE', 3,
 ( #14675, #22778, #6558, #22263, #39057, #41946, #22004, #19118, #34055, #3150 ),
 .UNSPECIFIED., .F., .F.,
 ( 4, 2, 2, 2, 4 ),
 ( -5.804775000000000375E-14, 0.9800148840114050186, 2.548038698429749616, 5.056876801499090135, 7.840119072091650487 ),
 .UNSPECIFIED. ) ;
#41830=CARTESIAN_POINT ( 'NONE',  ( 52.47362271920999888, -50.54282858732130279, -76.54035590516859600 ) ) ;
#41831=CARTESIAN_POINT ( 'NONE',  ( 60.87675474826550470, 14.21249462454519907, -47.03427939643230360 ) ) ;
#41832=CIRCLE ( 'NONE', #35958, 16.33504667647529729 ) ;
#41835=DIRECTION ( 'NONE',  ( 0.8732394366197182567, 0.4872913772396111343, 0.000000000000000000 ) ) ;
#41836=CARTESIAN_POINT ( 'NONE',  ( 42.47710464005660214, 13.93869629074949934, -6.396644207099989821 ) ) ;
#41840=CARTESIAN_POINT ( 'NONE',  ( 42.37474662285829652, -43.39983076957700092, -4.189334837963389901 ) ) ;
#41842=CARTESIAN_POINT ( 'NONE',  ( -5.431977005845720186, 16.07634798542799714, -5.576406780277120667 ) ) ;
#41844=DIRECTION ( 'NONE',  ( 1.000000000000000000, 0.000000000000000000, 0.000000000000000000 ) ) ;
#41845=CARTESIAN_POINT ( 'NONE',  ( 66.13978414627780467, -0.1966566410384200103, -17.02377224954269863 ) ) ;
#41847=CARTESIAN_POINT ( 'NONE',  ( 14.35835698848820030, -52.52234239888379363, -75.96669286083250938 ) ) ;
#41851=CARTESIAN_POINT ( 'NONE',  ( 46.68381635779479666, -53.67199518238830080, -75.98463753095340678 ) ) ;
#41854=FACE_OUTER_BOUND ( 'NONE', #43493, .T. ) ;
#41855=CARTESIAN_POINT ( 'NONE',  ( 85.66799001034409855, 17.38381105532069881, -61.58097075742929860 ) ) ;
#41856=CARTESIAN_POINT ( 'NONE',  ( 56.49779820569929711, 19.52786438580549699, -53.73084179205309852 ) ) ;
#41857=CARTESIAN_POINT ( 'NONE',  ( 48.25700189825269604, 23.04030082563999926, -55.28230106632420160 ) ) ;
#41858=AXIS2_PLACEMENT_3D ( 'NONE', #39963, #16366, #28145 ) ;
#41859=ORIENTED_EDGE ( 'NONE', *, *, #30983, .F. ) ;
#41860=AXIS2_PLACEMENT_3D ( 'NONE', #31389, #7832, #15690 ) ;
#41864=CARTESIAN_POINT ( 'NONE',  ( 82.61176995027730641, 14.02130663610568284, -47.15275950339798783 ) ) ;
#41866=CARTESIAN_POINT ( 'NONE',  ( 6.187261889072820154, -46.71083452957879700, -20.15000000000000213 ) ) ;
#41867=CARTESIAN_POINT ( 'NONE',  ( 83.30156758793411598, 13.69860857563659984, -46.93423283396209911 ) ) ;
#41868=CARTESIAN_POINT ( 'NONE',  ( 53.19499043075920497, 17.94716954222059613, -26.84764288680280231 ) ) ;
#41872=CARTESIAN_POINT ( 'NONE',  ( 12.06284766121009966, 32.21085600226960111, -22.25048313876769868 ) ) ;
#41873=CARTESIAN_POINT ( 'NONE',  ( 56.66909264166819327, -45.11618894467940066, -15.43624580850259953 ) ) ;
#41875=B_SPLINE_SURFACE_WITH_KNOTS ( 'NONE', 3, 3, ( 
 ( #51209, #34942, #42835, #39413, #11118, #31257, #15302, #38646, #50942, #50684, #2734, #14781, #31768, #19222, #3513, #27851, #47033, #31517, #3249, #43852, #47288, #7183, #35208, #35471 ),
 ( #27593, #11379, #7948, #19480, #18707, #43601, #30750, #46772, #6930, #24933, #48555, #17109, #48046, #5056, #1113, #20491, #16845, #44361, #4786, #4267, #12144, #28616, #48297, #16572 ),
 ( #20237, #19980, #23898, #35974, #21016, #4518, #24671, #33062, #36226, #848, #24413, #8987, #32527, #337, #16321, #20754, #36482, #13191, #28880, #587, #40945, #32275, #39923, #49088 ),
 ( #29141, #37014, #12663, #45142, #28099, #4019, #93, #44617, #32794, #8466, #36741, #8723, #32021, #16064, #44107, #40686, #48817, #12925, #12394, #44882, #8206, #24152, #40172, #40425 ),
 ( #28356, #25201, #1376, #13694, #49607, #33593, #29654, #41988, #42248, #37276, #45658, #22044, #5316, #38057, #17363, #49346, #9761, #13445, #25456, #6090, #25713, #2151, #17623, #50109 ),
 ( #41207, #33842, #18131, #26240, #14204, #21272, #45404, #34094, #5576, #6346, #41721, #5827, #18383, #21790, #30174, #1632, #41460, #33329, #37799, #49857, #1894, #46194, #22305, #29404 ),
 ( #38312, #29906, #17871, #45924, #34358, #9509, #10277, #21532, #37529, #13947, #10014, #25975, #2399, #50375, #14459, #30427, #9252, #50623, #7126, #11313, #15242, #31191, #3704, #14720 ),
 ( #43286, #27021, #35669, #51398, #23077, #31451, #6870, #46453, #19672, #18645, #18897, #10540, #15498, #23583, #22818, #2928, #39600, #26496, #6602, #51654, #34620, #11570, #19422, #38840 ) ),
 .UNSPECIFIED., .F., .F., .F.,
 ( 4, 1, 1, 1, 1, 4 ),
 ( 4, 2, 2, 2, 2, 2, 2, 2, 2, 2, 2, 4 ),
 ( -1.333460192499999945E-05, 0.2000000000000000111, 0.4000000000000000222, 0.5999999999999999778, 0.8000000000000000444, 1.000000000000000000 ),
 ( -1.333460192499999945E-05, 1.104949632659680159, 2.367749212842169992, 3.156998950456220143, 3.551623819263250326, 4.183023609354489913, 4.647713308159810097, 5.112403006965129393, 5.464321026995399677, 5.816239047025679731, 6.065118473969059565, 6.313997900912440286 ),
 .UNSPECIFIED. ) ;
#41879=CARTESIAN_POINT ( 'NONE',  ( 11.74347662706570006, -64.88511784619510081, -16.31133514117630057 ) ) ;
#41880=CARTESIAN_POINT ( 'NONE',  ( 11.13319320311270033, 33.09033149884700009, -45.34134544340819417 ) ) ;
#41882=EDGE_CURVE ( 'NONE', #28130, #5735, #46524, .T. ) ;
#41884=CARTESIAN_POINT ( 'NONE',  ( 12.25380415227330033, 34.08744772704470449, -46.27199321459300307 ) ) ;
#41885=CARTESIAN_POINT ( 'NONE',  ( 12.77233515483190018, -65.50098146117900910, -47.69352623515830203 ) ) ;
#41890=CARTESIAN_POINT ( 'NONE',  ( 52.64726764441159901, -49.79428164651599786, -48.69236602696069838 ) ) ;
#41891=CARTESIAN_POINT ( 'NONE',  ( 52.15791131231179634, 19.08239589345419773, -49.32805031943310325 ) ) ;
#41892=CARTESIAN_POINT ( 'NONE',  ( 62.23727147033270057, -1.604945995984039975, -16.10252877210989908 ) ) ;
#41893=CARTESIAN_POINT ( 'NONE',  ( 50.58622399129809821, -48.86524564621230127, -76.21981748726450689 ) ) ;
#41894=VECTOR ( 'NONE', #19604, 1000.000000000000000 ) ;
#41895=CARTESIAN_POINT ( 'NONE',  ( 56.57680611020050065, -50.33247776572370213, -52.64782081613199693 ) ) ;
#41896=VERTEX_POINT ( 'NONE', #34692 ) ;
#41897=CARTESIAN_POINT ( 'NONE',  ( 52.82216258569669520, -49.58646061845040265, -27.28071896258420281 ) ) ;
#41899=ORIENTED_EDGE ( 'NONE', *, *, #37649, .F. ) ;
#41900=CARTESIAN_POINT ( 'NONE',  ( 12.18502729926166595, -55.42069105936809592, -74.66536237510875651 ) ) ;
#41901=DIRECTION ( 'NONE',  ( 0.8857883891771956009, -0.4640893551880597157, 2.775557561562888270E-17 ) ) ;
#41903=CARTESIAN_POINT ( 'NONE',  ( 13.31268657292829971, -51.13566752317600361, -21.89251117597479990 ) ) ;
#41904=CARTESIAN_POINT ( 'NONE',  ( 54.76877112936399783, 19.42876175676859773, -76.28131348449389293 ) ) ;
#41905=CARTESIAN_POINT ( 'NONE',  ( 46.50118480118399589, -53.10011392806350727, -76.13977852870850427 ) ) ;
#41907=CARTESIAN_POINT ( 'NONE',  ( 54.83244439671879888, 14.27556882037980124, -15.28355485841840000 ) ) ;
#41909=CARTESIAN_POINT ( 'NONE',  ( 57.34583854987740636, -50.23863174456870695, -52.73888232562049438 ) ) ;
#41913=CIRCLE ( 'NONE', #2599, 20.00000000000000355 ) ;
#41915=CARTESIAN_POINT ( 'NONE',  ( 47.44037494016029655, 23.08122949994629991, -75.17655532006401131 ) ) ;
#41917=CARTESIAN_POINT ( 'NONE',  ( 75.29749630104785751, -36.46059068598260922, -12.51818644522628610 ) ) ;
#41919=CARTESIAN_POINT ( 'NONE',  ( -33.86606260230380627, -15.61618894467806307, -46.39999999999999858 ) ) ;
#41920=ADVANCED_FACE ( 'NONE', ( #42844 ), #50444, .T. ) ;
#41921=CARTESIAN_POINT ( 'NONE',  ( 14.34417029198879945, -51.11618894467930119, -74.14999999999999147 ) ) ;
#41923=EDGE_CURVE ( 'NONE', #10696, #20725, #43233, .T. ) ;
#41927=CARTESIAN_POINT ( 'NONE',  ( 61.27342693744519408, 14.00466695065149914, -46.49030966888999927 ) ) ;
#41928=CARTESIAN_POINT ( 'NONE',  ( -12.67430703014560045, 25.29472265930930064, -51.91878751810720161 ) ) ;
#41929=ADVANCED_FACE ( 'NONE', ( #46781 ), #27254, .T. ) ;
#41930=ORIENTED_EDGE ( 'NONE', *, *, #43117, .F. ) ;
#41931=CARTESIAN_POINT ( 'NONE',  ( 52.83705234978589971, -49.66563195679469800, -48.81125901731440564 ) ) ;
#41932=ORIENTED_EDGE ( 'NONE', *, *, #45860, .F. ) ;
#41935=CARTESIAN_POINT ( 'NONE',  ( 13.78923984081539977, 19.56813522593770216, -21.52746261380119819 ) ) ;
#41936=CARTESIAN_POINT ( 'NONE',  ( 56.45642129034870038, 14.19690291267379934, -25.50404404838770134 ) ) ;
#41939=CARTESIAN_POINT ( 'NONE',  ( 53.44641931178580307, 18.15579562409830316, -49.05897173235240416 ) ) ;
#41941=CARTESIAN_POINT ( 'NONE',  ( 60.75208945151790374, -45.51018815575340426, -47.06168269646809676 ) ) ;
#41942=CARTESIAN_POINT ( 'NONE',  ( 65.03603135424580728, -15.61618894467929941, -19.52361391316370032 ) ) ;
#41943=ORIENTED_EDGE ( 'NONE', *, *, #19264, .T. ) ;
#41946=CARTESIAN_POINT ( 'NONE',  ( 57.40277299468780114, 16.17492991088059995, -48.23107244050790143 ) ) ;
#41949=CIRCLE ( 'NONE', #30224, 38.00000000000000000 ) ;
#41950=CARTESIAN_POINT ( 'NONE',  ( 11.89948726634279907, -65.43656066622459377, -18.06739951304799874 ) ) ;
#41951=CARTESIAN_POINT ( 'NONE',  ( 52.87578304523380268, 18.40442787170260175, -48.67531064471670277 ) ) ;
#41952=CARTESIAN_POINT ( 'NONE',  ( 82.02429831058030629, -41.23866635630079713, -45.87976092105969883 ) ) ;
#41954=VECTOR ( 'NONE', #41694, 1000.000000000000000 ) ;
#41960=CARTESIAN_POINT ( 'NONE',  ( 8.963661153849718843, -63.19364268998111100, -46.63283991472749790 ) ) ;
#41962=ORIENTED_EDGE ( 'NONE', *, *, #39899, .F. ) ;
#41966=CARTESIAN_POINT ( 'NONE',  ( 52.16338521619510260, 18.67182647646719929, -76.93802992565549914 ) ) ;
#41967=ORIENTED_EDGE ( 'NONE', *, *, #15680, .T. ) ;
#41970=CARTESIAN_POINT ( 'NONE',  ( -19.86606260230379917, -15.61618894467933494, -19.14999999999999858 ) ) ;
#41978=CARTESIAN_POINT ( 'NONE',  ( 53.26966627192010151, -49.51099171206949734, -49.16957340299519785 ) ) ;
#41980=CARTESIAN_POINT ( 'NONE',  ( 14.23591865958499980, 20.10714342530040000, -75.06145659859170394 ) ) ;
#41982=VECTOR ( 'NONE', #47111, 1000.000000000000000 ) ;
#41983=CARTESIAN_POINT ( 'NONE',  ( 42.30722599539220141, -45.03182078332450544, -6.083982332172880092 ) ) ;
#41984=CARTESIAN_POINT ( 'NONE',  ( 47.64143405400680109, -54.53488714545009941, -74.14999999999999147 ) ) ;
#41985=AXIS2_PLACEMENT_3D ( 'NONE', #32124, #30010, #17719 ) ;
#41988=CARTESIAN_POINT ( 'NONE',  ( 54.06806631522740503, -48.25978409922480239, -26.47101390624369799 ) ) ;
#41990=CARTESIAN_POINT ( 'NONE',  ( 56.57214737956470429, -50.73313417699420569, -74.14929904960109752 ) ) ;
#41992=CARTESIAN_POINT ( 'NONE',  ( 1.813848851336939738, 24.38879552280330287, -10.83645643805460068 ) ) ;
#41994=LINE ( 'NONE', #6094, #2056 ) ;
#41998=CARTESIAN_POINT ( 'NONE',  ( -2.623662900336269921, -48.66391853426490144, -4.386168476009399519 ) ) ;
#41999=CARTESIAN_POINT ( 'NONE',  ( 47.54275987186800023, 23.32401250507800228, -54.69604644530389947 ) ) ;
#42002=CARTESIAN_POINT ( 'NONE',  ( 13.09359062182869948, 19.38068958424499755, -21.36973451213659914 ) ) ;
#42004=CARTESIAN_POINT ( 'NONE',  ( 11.86319492706100043, 34.16543365841759794, -17.45438025052920139 ) ) ;
#42005=CARTESIAN_POINT ( 'NONE',  ( 7.768034174689467442, 29.40613003788450186, -20.78409677699325897 ) ) ;
#42006=DIRECTION ( 'NONE',  ( -0.2260571801428161165, 7.216449660063443557E-16, 0.9741140340359943917 ) ) ;
#42008=DIRECTION ( 'NONE',  ( 0.000000000000000000, 0.000000000000000000, -1.000000000000000000 ) ) ;
#42010=CARTESIAN_POINT ( 'NONE',  ( 56.09099783350909973, 19.70331726233800040, -53.77926613765360031 ) ) ;
#42014=DIRECTION ( 'NONE',  ( 0.000000000000000000, -3.054848041326977894E-12, 1.000000000000000000 ) ) ;
#42016=CARTESIAN_POINT ( 'NONE',  ( 65.04199857771129700, -32.25459573065409558, -17.84398015535190041 ) ) ;
#42017=EDGE_CURVE ( 'NONE', #48724, #37163, #15410, .T. ) ;
#42018=CARTESIAN_POINT ( 'NONE',  ( 54.13393739769620083, -15.61618894467929941, 6.349999999999999645 ) ) ;
#42019=EDGE_LOOP ( 'NONE', ( #27519, #48734, #37427, #36625, #38733 ) ) ;
#42021=CARTESIAN_POINT ( 'NONE',  ( 48.25528797735789510, 23.04103089059050191, -55.30957496453539335 ) ) ;
#42023=CARTESIAN_POINT ( 'NONE',  ( 49.27279687193958324, -2.461837687523397378, -15.69245132549682431 ) ) ;
#42025=CARTESIAN_POINT ( 'NONE',  ( 12.36185612747330076, -65.36949588230230290, -46.58846889824079796 ) ) ;
#42026=CARTESIAN_POINT ( 'NONE',  ( 56.96971367505879869, -45.85215597628009476, -26.22514245738749850 ) ) ;
#42028=CARTESIAN_POINT ( 'NONE',  ( 10.47406283454438203, -59.02534396924340143, -45.62066736167659542 ) ) ;
#42031=DIRECTION ( 'NONE',  ( 0.000000000000000000, -0.9319748226751538578, -0.3625230060280530409 ) ) ;
#42034=CARTESIAN_POINT ( 'NONE',  ( 47.51452104107959684, -45.56742998877640360, -10.18306270678010073 ) ) ;
#42036=CARTESIAN_POINT ( 'NONE',  ( 16.35031946894069677, 19.87963569218470283, -20.80740584792750170 ) ) ;
#42038=CARTESIAN_POINT ( 'NONE',  ( 68.13393739769620083, 17.38381105532069881, -65.65000000000000568 ) ) ;
#42039=CARTESIAN_POINT ( 'NONE',  ( 47.06489453142850010, -54.53966941020699721, -75.17791912558919876 ) ) ;
#42040=CARTESIAN_POINT ( 'NONE',  ( 60.59298274472079981, 13.73382843762409777, -10.31706438195179842 ) ) ;
#42041=CARTESIAN_POINT ( 'NONE',  ( 50.36549737501839985, -50.07561419642740219, -76.14999999999999147 ) ) ;
#42044=B_SPLINE_SURFACE_WITH_KNOTS ( 'NONE', 3, 3, ( 
 ( #686, #42995, #48660, #40274, #48135, #22785 ),
 ( #18864, #38804, #34848, #4620, #4104, #24248 ),
 ( #2898, #27237, #35105, #26989, #28459, #44459 ),
 ( #12491, #16674, #24508, #43255, #4362, #50848 ),
 ( #14941, #11020, #31162, #30904, #20082, #46934 ),
 ( #36074, #12759, #8042, #23996, #40017, #8566 ),
 ( #39063, #23043, #40527, #32374, #3156, #19125 ),
 ( #51104, #20333, #28716, #20589, #15207, #32117 ),
 ( #11277, #180, #44717, #47190, #16159, #44200 ),
 ( #12235, #36321, #32633, #8298, #28197, #432 ),
 ( #48393, #36583, #44980, #9602, #29234, #9351 ),
 ( #14043, #32896, #21369, #17205, #41558, #25296 ),
 ( #37897, #28981, #33937, #25555, #33425, #8823 ),
 ( #4885, #24774, #20852, #41818, #41302, #5674 ),
 ( #40783, #17971, #5411, #17715, #25810, #48928 ),
 ( #9082, #33683, #13539, #37117, #9853, #21622 ) ),
 .UNSPECIFIED., .F., .F., .F.,
 ( 4, 2, 2, 2, 2, 2, 2, 4 ),
 ( 4, 1, 1, 4 ),
 ( 0.000000000000000000, 1.325233610615540014, 2.839786308461869968, 3.786381744615829881, 4.259679462692810503, 5.016955811615980032, 6.228597969893040265, 7.536345830558680348 ),
 ( 0.000000000000000000, 0.3333333333333329818, 0.6666666666666670737, 1.000000000000000000 ),
 .UNSPECIFIED. ) ;
#42045=CARTESIAN_POINT ( 'NONE',  ( 51.55044211529290266, 20.01891078301889948, -76.08578284841350126 ) ) ;
#42046=CARTESIAN_POINT ( 'NONE',  ( 57.47755809313429864, 13.88376667797570008, -25.39851124859779929 ) ) ;
#42048=ORIENTED_EDGE ( 'NONE', *, *, #15076, .T. ) ;
#42055=VECTOR ( 'NONE', #20348, 1000.000000000000114 ) ;
#42058=CARTESIAN_POINT ( 'NONE',  ( 41.62693577923219834, 12.58261528623730108, -3.742293453206330334 ) ) ;
#42060=CARTESIAN_POINT ( 'NONE',  ( 19.55572504588462124, 24.23719298256126820, -75.54211829725619509 ) ) ;
#42063=CARTESIAN_POINT ( 'NONE',  ( 18.11395681486079923, -51.16362366046149646, -74.57010117178208475 ) ) ;
#42068=ORIENTED_EDGE ( 'NONE', *, *, #25652, .T. ) ;
#42069=CARTESIAN_POINT ( 'NONE',  ( 52.68908936341578908, 18.51792035577400242, -48.47378032971769812 ) ) ;
#42079=EDGE_CURVE ( 'NONE', #12246, #36840, #21027, .T. ) ;
#42081=CARTESIAN_POINT ( 'NONE',  ( 61.08134338338769709, -45.33768279644640131, -46.82317710124809906 ) ) ;
#42082=CARTESIAN_POINT ( 'NONE',  ( 52.77282165433940264, -49.72616459520740051, -48.90295367273579785 ) ) ;
#42085=ORIENTED_EDGE ( 'NONE', *, *, #36916, .T. ) ;
#42086=VERTEX_POINT ( 'NONE', #1387 ) ;
#42087=CARTESIAN_POINT ( 'NONE',  ( 14.34417021472880016, 20.88381098710710049, -23.14999995404869892 ) ) ;
#42091=ORIENTED_EDGE ( 'NONE', *, *, #4399, .F. ) ;
#42094=CARTESIAN_POINT ( 'NONE',  ( 52.14531167019610081, -49.88992925342000007, -76.93287919525420193 ) ) ;
#42095=CARTESIAN_POINT ( 'NONE',  ( 61.01670509829179423, 14.23156206065599960, -47.38493383915780299 ) ) ;
#42097=CARTESIAN_POINT ( 'NONE',  ( 57.50723796701959856, -45.11618894467940066, -25.33268394681470070 ) ) ;
#42098=CARTESIAN_POINT ( 'NONE',  ( 44.76368420724840291, 13.86998310020809910, -7.024004829805569727 ) ) ;
#42099=CARTESIAN_POINT ( 'NONE',  ( 41.59466734061630433, -44.04155483751850397, -4.344851959883419212 ) ) ;
#42100=DIRECTION ( 'NONE',  ( 0.5685928097855449392, 0.5944782866685399680, -0.5685928097855409424 ) ) ;
#42101=CARTESIAN_POINT ( 'NONE',  ( -2.927826905750240183, 17.96742634125930138, -5.740514720776229929 ) ) ;
#42106=DIRECTION ( 'NONE',  ( 0.4936210606096666509, 0.8696770943991728453, 0.000000000000000000 ) ) ;
#42109=CARTESIAN_POINT ( 'NONE',  ( 40.16190654090002710, 1.841152499458795999, 7.944363289481099599 ) ) ;
#42110=CARTESIAN_POINT ( 'NONE',  ( 8.815605938792600682, 32.05029769220720226, -46.67186391141279955 ) ) ;
#42112=EDGE_CURVE ( 'NONE', #38586, #26354, #25961, .T. ) ;
#42116=CARTESIAN_POINT ( 'NONE',  ( 47.88434815289430446, -54.36569397686789529, -54.74340954032749806 ) ) ;
#42119=AXIS2_PLACEMENT_3D ( 'NONE', #17508, #49495, #13582 ) ;
#42120=CARTESIAN_POINT ( 'NONE',  ( -3.306064913430322161, -48.27659316133668455, -4.296538305446551576 ) ) ;
#42121=CARTESIAN_POINT ( 'NONE',  ( 48.18093947880029759, 23.07156810961839710, -55.22362743473310331 ) ) ;
#42126=ORIENTED_EDGE ( 'NONE', *, *, #41171, .F. ) ;
#42129=DIRECTION ( 'NONE',  ( 0.000000000000000000, 1.000000000000000000, 0.000000000000000000 ) ) ;
#42130=CARTESIAN_POINT ( 'NONE',  ( 15.65806028500812630, 19.62302339113210436, -20.25522482650049128 ) ) ;
#42131=EDGE_CURVE ( 'NONE', #9203, #29653, #21543, .T. ) ;
#42132=CARTESIAN_POINT ( 'NONE',  ( 83.58813978703560110, 13.49428892428420035, -46.95981403914270658 ) ) ;
#42133=FACE_OUTER_BOUND ( 'NONE', #22107, .T. ) ;
#42135=CARTESIAN_POINT ( 'NONE',  ( 18.06932202639930196, -55.56934008872529773, -76.14999999999999147 ) ) ;
#42137=CARTESIAN_POINT ( 'NONE',  ( 56.05190491853310419, -45.91616149951833847, -25.80821180466989517 ) ) ;
#42141=EDGE_CURVE ( 'NONE', #28405, #23493, #18945, .T. ) ;
#42142=ORIENTED_EDGE ( 'NONE', *, *, #25931, .T. ) ;
#42143=CARTESIAN_POINT ( 'NONE',  ( 12.36320305068320025, -64.54682834576858852, -15.76422791927960176 ) ) ;
#42146=CARTESIAN_POINT ( 'NONE',  ( 11.55867067482810029, -65.29213368340509760, -47.38009360661429525 ) ) ;
#42151=CARTESIAN_POINT ( 'NONE',  ( 53.05395541577509988, -49.58683839042910080, -49.07041596672719663 ) ) ;
#42152=CARTESIAN_POINT ( 'NONE',  ( 53.43548356396929933, 18.14259979176529924, -49.05614973121760158 ) ) ;
#42153=CARTESIAN_POINT ( 'NONE',  ( 59.43939780494530112, -2.800449505682500284, -15.69362887585340083 ) ) ;
#42154=CARTESIAN_POINT ( 'NONE',  ( 51.08267997340979605, -48.71747343918639928, -76.44192736852110670 ) ) ;
#42156=CARTESIAN_POINT ( 'NONE',  ( 57.38779215104710119, -50.16954271334839888, -52.66274956582070388 ) ) ;
#42157=EDGE_LOOP ( 'NONE', ( #21307, #50049 ) ) ;
#42158=CARTESIAN_POINT ( 'NONE',  ( 52.72378859808809892, -49.69239786187580421, -27.46381703610880010 ) ) ;
#42160=CARTESIAN_POINT ( 'NONE',  ( 54.57779867077987745, -51.14476727363286557, -75.37910404347289273 ) ) ;
#42161=CARTESIAN_POINT ( 'NONE',  ( 57.59002137063620097, -47.30929821719110606, -48.19818069499370239 ) ) ;
#42164=CARTESIAN_POINT ( 'NONE',  ( 13.91136646146859945, -51.07664658664480584, -22.10163017854790013 ) ) ;
#42165=CARTESIAN_POINT ( 'NONE',  ( 55.14382500610250304, 19.42312599486780300, -76.11832371178049073 ) ) ;
#42166=CARTESIAN_POINT ( 'NONE',  ( 47.12413796937290300, -53.90319693934949896, -75.74320899229410031 ) ) ;
#42168=CARTESIAN_POINT ( 'NONE',  ( 55.58645560292939791, 14.21669597304580002, -15.86644146958279755 ) ) ;
#42171=CARTESIAN_POINT ( 'NONE',  ( 82.13853704237929776, 13.88381105532070059, -46.37203261889099792 ) ) ;
#42174=CARTESIAN_POINT ( 'NONE',  ( 61.28398356453099893, 14.37233669519349988, -47.68178229854910199 ) ) ;
#42176=CARTESIAN_POINT ( 'NONE',  ( 46.78634582468389880, 22.26413375686030349, -76.02748008299779769 ) ) ;
#42178=CARTESIAN_POINT ( 'NONE',  ( 75.29643519189366430, -36.41381154147628507, -12.51292969751692574 ) ) ;
#42183=CARTESIAN_POINT ( 'NONE',  ( 82.75736676522110713, 14.37198029891985840, -47.68254826574469973 ) ) ;
#42186=CARTESIAN_POINT ( 'NONE',  ( 8.038038740883376221, 29.03132506359100518, -21.05410134318715976 ) ) ;
#42190=CARTESIAN_POINT ( 'NONE',  ( 12.82281323259459960, 33.73355787245069592, -46.32794539105000098 ) ) ;
#42191=ORIENTED_EDGE ( 'NONE', *, *, #12089, .T. ) ;
#42193=CARTESIAN_POINT ( 'NONE',  ( 53.10972322296039749, -49.53037264418929198, -48.97251034775650425 ) ) ;
#42197=CARTESIAN_POINT ( 'NONE',  ( 13.89444719274460027, 19.98929110357370220, -22.84407598213759982 ) ) ;
#42198=CARTESIAN_POINT ( 'NONE',  ( 56.78931313380690682, 14.03059450484890114, -25.50518706664649926 ) ) ;
#42201=CARTESIAN_POINT ( 'NONE',  ( 53.02924604216119775, 18.36504672385269998, -49.05876171777440220 ) ) ;
#42203=FACE_OUTER_BOUND ( 'NONE', #21871, .T. ) ;
#42204=ORIENTED_EDGE ( 'NONE', *, *, #15659, .F. ) ;
#42210=CARTESIAN_POINT ( 'NONE',  ( 10.73482432373229756, -64.94719017208709033, -18.15071128010919921 ) ) ;
#42211=CARTESIAN_POINT ( 'NONE',  ( 52.93498290923280081, 18.37341140428640074, -48.74287987618630069 ) ) ;
#42212=FACE_OUTER_BOUND ( 'NONE', #4875, .T. ) ;
#42214=DIRECTION ( 'NONE',  ( 0.000000000000000000, -1.000000000000000000, 0.000000000000000000 ) ) ;
#42217=CARTESIAN_POINT ( 'NONE',  ( 10.49070342362870001, -63.25259970453439706, -45.62560734925740036 ) ) ;
#42219=ORIENTED_EDGE ( 'NONE', *, *, #24545, .F. ) ;
#42221=CARTESIAN_POINT ( 'NONE',  ( 16.65420337941489848, 17.88381105532299742, -17.90311212357439885 ) ) ;
#42222=CARTESIAN_POINT ( 'NONE',  ( 53.23471704948639882, 19.19657966078460376, -77.19501645526850098 ) ) ;
#42225=DIRECTION ( 'NONE',  ( 0.000000000000000000, 0.000000000000000000, 1.000000000000000000 ) ) ;
#42227=EDGE_CURVE ( 'NONE', #26440, #22140, #5568, .T. ) ;
#42233=ORIENTED_EDGE ( 'NONE', *, *, #9218, .T. ) ;
#42234=B_SPLINE_CURVE_WITH_KNOTS ( 'NONE', 3,
 ( #3363, #34266, #38756, #26406, #26151, #30601, #19337, #15154, #22478, #42161, #2322, #47140, #38486, #31115, #42942, #18815 ),
 .UNSPECIFIED., .F., .F.,
 ( 4, 2, 2, 2, 2, 2, 2, 4 ),
 ( 0.000000000000000000, 1.372899869568840137, 2.941928291933239681, 3.922571055910980320, 4.412892437899861520, 5.197406649082060071, 6.452629386973570469, 7.845142111821970410 ),
 .UNSPECIFIED. ) ;
#42235=CARTESIAN_POINT ( 'NONE',  ( 56.71514755247739714, -46.07503343450810007, -26.25075064288229854 ) ) ;
#42238=DIRECTION ( 'NONE',  ( 1.000000000000000000, 0.000000000000000000, 0.000000000000000000 ) ) ;
#42240=CARTESIAN_POINT ( 'NONE',  ( 13.62850291019639926, 20.22628383398669882, -74.56034069004439857 ) ) ;
#42243=CARTESIAN_POINT ( 'NONE',  ( 43.82158222066500031, -45.08534330693629499, -6.692173543831889226 ) ) ;
#42244=FACE_OUTER_BOUND ( 'NONE', #46832, .T. ) ;
#42246=EDGE_CURVE ( 'NONE', #34780, #18612, #15404, .T. ) ;
#42247=ORIENTED_EDGE ( 'NONE', *, *, #40826, .F. ) ;
#42248=CARTESIAN_POINT ( 'NONE',  ( 53.98906395436699768, -48.34780241224260067, -26.51423003085930219 ) ) ;
#42249=CARTESIAN_POINT ( 'NONE',  ( 56.57234934511910041, -50.73310576891860535, -74.30382550411290765 ) ) ;
#42250=CARTESIAN_POINT ( 'NONE',  ( 2.830591470287960210, 25.45182595484199695, -11.52757872387000049 ) ) ;
#42254=ORIENTED_EDGE ( 'NONE', *, *, #47218, .T. ) ;
#42256=CARTESIAN_POINT ( 'NONE',  ( 47.49898707597870384, 23.35465752766770109, -54.71508157337640199 ) ) ;
#42257=CARTESIAN_POINT ( 'NONE',  ( 43.87440825508269882, -45.06628648458400477, -6.621182746357190396 ) ) ;
#42260=CARTESIAN_POINT ( 'NONE',  ( 11.65450058717340021, 33.89481885373739800, -16.76600934541039933 ) ) ;
#42262=CARTESIAN_POINT ( 'NONE',  ( 53.26902542446040201, 18.19839717132569845, -48.80947755968719548 ) ) ;
#42263=CARTESIAN_POINT ( 'NONE',  ( 19.04984016102106281, 24.27634599866043175, -75.91709172409272810 ) ) ;
#42264=CARTESIAN_POINT ( 'NONE',  ( 53.97934697425230155, -49.20473928360389948, -49.10921081283519385 ) ) ;
#42265=CARTESIAN_POINT ( 'NONE',  ( 56.42508253464700374, 14.99986749066500025, -26.25079172228680235 ) ) ;
#42266=CIRCLE ( 'NONE', #7110, 1.000000000000000444 ) ;
#42267=CARTESIAN_POINT ( 'NONE',  ( 50.04538724767210311, 22.25689945218810095, -54.67691783917840098 ) ) ;
#42269=CARTESIAN_POINT ( 'NONE',  ( 53.23851273770399928, 18.29663818490410421, -49.17579072038760302 ) ) ;
#42270=DIRECTION ( 'NONE',  ( 0.000000000000000000, -1.000000000000000000, 0.000000000000000000 ) ) ;
#42271=CARTESIAN_POINT ( 'NONE',  ( 20.02514464312236342, 23.87147242321097096, -18.88231557620769863 ) ) ;
#42272=CARTESIAN_POINT ( 'NONE',  ( 11.10551642654870008, 32.05074912355050287, -44.25176302638880088 ) ) ;
#42275=CARTESIAN_POINT ( 'NONE',  ( 65.46218529380999485, -32.54800987811099588, -18.25464570420819754 ) ) ;
#42277=CARTESIAN_POINT ( 'NONE',  ( 18.84529956396119843, 20.48963776793139857, -74.14994161014911356 ) ) ;
#42280=CARTESIAN_POINT ( 'NONE',  ( 42.29536634374500181, 11.94537196368429832, -3.241362035758810212 ) ) ;
#42282=CARTESIAN_POINT ( 'NONE',  ( 49.58508211105249330, -2.000197079579435044, -15.77316264483759767 ) ) ;
#42284=CARTESIAN_POINT ( 'NONE',  ( 12.28449157720250007, -65.33530493076349899, -46.44573566506809925 ) ) ;
#42285=CARTESIAN_POINT ( 'NONE',  ( 57.61832698878280468, -45.11897047559610030, -25.41289556137760286 ) ) ;
#42288=CARTESIAN_POINT ( 'NONE',  ( 13.39998208310050032, -51.78678246903520233, -74.14999999999999147 ) ) ;
#42289=EDGE_LOOP ( 'NONE', ( #16413, #47593, #21697 ) ) ;
#42294=CARTESIAN_POINT ( 'NONE',  ( 46.78799807556309531, -45.19957043902829952, -8.930844661211528646 ) ) ;
#42295=ADVANCED_FACE ( 'NONE', ( #9522 ), #26553, .T. ) ;
#42296=CARTESIAN_POINT ( 'NONE',  ( 52.01928562022798985, 1.750919267526578560, -19.49271441683317718 ) ) ;
#42297=CARTESIAN_POINT ( 'NONE',  ( 14.28039018034760055, 19.72599742411139800, -21.66377081666459858 ) ) ;
#42302=CARTESIAN_POINT ( 'NONE',  ( 47.16564018750800358, -54.32016963230069706, -75.35585495399020317 ) ) ;
#42303=CARTESIAN_POINT ( 'NONE',  ( 64.36501694216710234, 13.88381105527329851, -12.32038502994480034 ) ) ;
#42304=CIRCLE ( 'NONE', #13819, 3.000000000000004885 ) ;
#42306=CARTESIAN_POINT ( 'NONE',  ( 52.19959685038109853, 19.92045540604299703, -76.05470843165690553 ) ) ;
#42307=CARTESIAN_POINT ( 'NONE',  ( 61.43371642943920108, 13.93409536008670102, -28.09734365521990185 ) ) ;
#42311=ORIENTED_EDGE ( 'NONE', *, *, #16748, .F. ) ;
#42314=CARTESIAN_POINT ( 'NONE',  ( -5.143620389462549625, -47.12425989114009894, -5.067427102881679524 ) ) ;
#42315=CARTESIAN_POINT ( 'NONE',  ( 75.68173550483029999, -18.74328204524080022, -11.58966857824820096 ) ) ;
#42316=EDGE_CURVE ( 'NONE', #26368, #25343, #46043, .T. ) ;
#42318=CARTESIAN_POINT ( 'NONE',  ( 74.93037156228848517, -45.11618894467250129, -15.31097063366330069 ) ) ;
#42321=CARTESIAN_POINT ( 'NONE',  ( 82.32429201311688871, -45.44102527263400049, -47.46868292619190299 ) ) ;
#42322=CARTESIAN_POINT ( 'NONE',  ( 41.44023872227730010, 12.74910146949009970, -3.815737712921210001 ) ) ;
#42325=CARTESIAN_POINT ( 'NONE',  ( 70.83745409581578656, -49.21324915460098026, -73.25000000000119371 ) ) ;
#42327=DIRECTION ( 'NONE',  ( -0.2389682100434953882, -0.9710273912658735629, 0.000000000000000000 ) ) ;
#42328=VERTEX_POINT ( 'NONE', #27804 ) ;
#42330=B_SPLINE_CURVE_WITH_KNOTS ( 'NONE', 3,
 ( #34239, #5716, #5977, #25858, #42137, #38202, #22451, #21933 ),
 .UNSPECIFIED., .F., .F.,
 ( 4, 1, 1, 1, 1, 4 ),
 ( 0.000000000000000000, 0.2000000000001341816, 0.4000000000001006084, 0.6000000000000670353, 0.8000000000000334621, 1.000000000000000000 ),
 .UNSPECIFIED. ) ;
#42332=ORIENTED_EDGE ( 'NONE', *, *, #23575, .F. ) ;
#42343=EDGE_LOOP ( 'NONE', ( #15725, #15843, #30490, #14750, #31227 ) ) ;
#42344=CARTESIAN_POINT ( 'NONE',  ( 61.25719188131670023, -45.31066424344650301, -47.12453700741409790 ) ) ;
#42349=ADVANCED_FACE ( 'NONE', ( #3717 ), #10677, .T. ) ;
#42354=CARTESIAN_POINT ( 'NONE',  ( 51.73525746098499667, -50.43300767444429766, -76.36782564804489937 ) ) ;
#42355=CARTESIAN_POINT ( 'NONE',  ( 60.63565020168820041, 14.37421254607160037, -47.39321454885000406 ) ) ;
#42356=CIRCLE ( 'NONE', #39846, 3.000000000000003109 ) ;
#42358=DIRECTION ( 'NONE',  ( -0.2389682100434953882, -0.9710273912658735629, 0.000000000000000000 ) ) ;
#42359=CARTESIAN_POINT ( 'NONE',  ( 45.11068418675889546, 14.77969269803630148, -8.978235662926250527 ) ) ;
#42360=CARTESIAN_POINT ( 'NONE',  ( 42.98728576779360111, -42.87622043099199942, -4.202726304278470160 ) ) ;
#42362=CARTESIAN_POINT ( 'NONE',  ( 56.61928438282120624, 14.09173444410579989, -25.29356196242219923 ) ) ;
#42364=CIRCLE ( 'NONE', #34796, 1.000000000000000888 ) ;
#42367=DIRECTION ( 'NONE',  ( 1.000000000000000000, 0.000000000000000000, 0.000000000000000000 ) ) ;
#42373=CARTESIAN_POINT ( 'NONE',  ( 44.88839470740660431, 14.87643554339019936, -8.898984674148820773 ) ) ;
#42377=CARTESIAN_POINT ( 'NONE',  ( 46.85564613059059980, -54.06445821833459320, -75.74423906255060501 ) ) ;
#42380=CARTESIAN_POINT ( 'NONE',  ( 47.75291977277729671, -54.48739848013099873, -55.20309039576459753 ) ) ;
#42381=CARTESIAN_POINT ( 'NONE',  ( 13.00893739761190027, -65.51843714052189682, -47.75434321210310173 ) ) ;
#42383=CARTESIAN_POINT ( 'NONE',  ( 47.81306074494699487, 23.22517729902449801, -55.08809726227399750 ) ) ;
#42392=CARTESIAN_POINT ( 'NONE',  ( 82.89855244518290078, 14.28649170576880145, -47.58879117305969686 ) ) ;
#42393=CARTESIAN_POINT ( 'NONE',  ( 55.92359121559390189, 14.66224575315600021, -25.40852202100330004 ) ) ;
#42399=CARTESIAN_POINT ( 'NONE',  ( 27.73905384484250192, -53.11618894467930119, -74.14999999999999147 ) ) ;
#42400=B_SPLINE_CURVE_WITH_KNOTS ( 'NONE', 3,
 ( #21681, #30325, #1788, #46349, #6243, #5725, #37952, #34247, #14097, #22201 ),
 .UNSPECIFIED., .F., .F.,
 ( 4, 2, 2, 2, 4 ),
 ( 0.000000000000000000, 0.1338527402502077968, 0.2763488516921074889, 0.4029155702267074868, 0.4999999999999911737 ),
 .UNSPECIFIED. ) ;
#42403=ORIENTED_EDGE ( 'NONE', *, *, #24263, .F. ) ;
#42406=CARTESIAN_POINT ( 'NONE',  ( 11.69945459769019891, 33.68403274003249948, -45.13438395913740209 ) ) ;
#42407=CARTESIAN_POINT ( 'NONE',  ( 16.13393739769620083, -15.61618894467929941, -6.649999999999999467 ) ) ;
#42409=EDGE_LOOP ( 'NONE', ( #40222, #7727, #23167, #17669 ) ) ;
#42411=CARTESIAN_POINT ( 'NONE',  ( 51.29354596943910138, 21.74684883274469982, -54.72842898864520578 ) ) ;
#42413=CARTESIAN_POINT ( 'NONE',  ( 57.07057989771080031, 14.65163658184950002, -26.24936944650179882 ) ) ;
#42414=CARTESIAN_POINT ( 'NONE',  ( 53.34803077867909593, -49.46767309333149854, -49.15544592153489845 ) ) ;
#42416=CARTESIAN_POINT ( 'NONE',  ( 48.43106010952779883, 22.58642710690570254, -53.38354561996749936 ) ) ;
#42417=CARTESIAN_POINT ( 'NONE',  ( 59.95038794592539944, -2.512083940479500122, -15.76663620625850015 ) ) ;
#42418=CARTESIAN_POINT ( 'NONE',  ( 51.37232876478519472, -49.64415483134600038, -76.46732863254598556 ) ) ;
#42419=EDGE_CURVE ( 'NONE', #20901, #26902, #24737, .T. ) ;
#42420=CARTESIAN_POINT ( 'NONE',  ( 56.58402204250390355, -50.55592571534859303, -53.00599847022490252 ) ) ;
#42424=CARTESIAN_POINT ( 'NONE',  ( 67.04038824939809160, 19.47158195952359705, -70.40645085170191919 ) ) ;
#42425=ORIENTED_EDGE ( 'NONE', *, *, #17043, .T. ) ;
#42427=CARTESIAN_POINT ( 'NONE',  ( 54.13393739769620083, -15.61618894467929941, -3.187564294433600232 ) ) ;
#42429=CARTESIAN_POINT ( 'NONE',  ( 13.86432996969659825, -51.09005464285149856, -22.12930180663200019 ) ) ;
#42431=CARTESIAN_POINT ( 'NONE',  ( 56.42418868998549897, 19.40436683310219834, -75.33371615204529803 ) ) ;
#42432=CARTESIAN_POINT ( 'NONE',  ( 47.58822567098650325, -54.46711296191460150, -74.72768729699521373 ) ) ;
#42433=CARTESIAN_POINT ( 'NONE',  ( 55.45985160373810174, 14.08381916207730100, -15.39201607824520046 ) ) ;
#42434=CARTESIAN_POINT ( 'NONE',  ( 47.73557342949970206, 23.25259336863290116, -54.98607376159549887 ) ) ;
#42435=CARTESIAN_POINT ( 'NONE',  ( 82.45630311851421368, 13.86034003618500066, -46.38988467804559690 ) ) ;
#42440=CARTESIAN_POINT ( 'NONE',  ( 46.37900464578690674, 21.71116150353940100, -76.14999999999999147 ) ) ;
#42442=EDGE_CURVE ( 'NONE', #41357, #39182, #26607, .T. ) ;
#42444=CARTESIAN_POINT ( 'NONE',  ( 11.89611903400246540, -65.09453069998440355, -23.79086514498333216 ) ) ;
#42448=CARTESIAN_POINT ( 'NONE',  ( 82.30072452188801435, 14.05343120103280086, -47.18357693586790447 ) ) ;
#42453=CARTESIAN_POINT ( 'NONE',  ( 6.156981251806739053, 33.30392151337740358, -47.78905844756960164 ) ) ;
#42455=CARTESIAN_POINT ( 'NONE',  ( 52.77791368993419496, -49.69695095401060314, -48.73087024381919719 ) ) ;
#42456=ORIENTED_EDGE ( 'NONE', *, *, #4717, .F. ) ;
#42460=CARTESIAN_POINT ( 'NONE',  ( 14.12421044447399865, 19.90653214807120008, -22.60548794454369670 ) ) ;
#42461=CARTESIAN_POINT ( 'NONE',  ( 57.53087442631830584, 14.06726690696280002, -25.93050682469580082 ) ) ;
#42463=CARTESIAN_POINT ( 'NONE',  ( 51.00677359191169558, 19.62691423242569755, -76.14999999999999147 ) ) ;
#42464=CARTESIAN_POINT ( 'NONE',  ( 52.86566475114400276, 18.43067181376370200, -48.91558075316019938 ) ) ;
#42465=CARTESIAN_POINT ( 'NONE',  ( 55.25725834564570249, -45.84610244531269529, -16.15205766596429982 ) ) ;
#42467=ORIENTED_EDGE ( 'NONE', *, *, #44916, .F. ) ;
#42469=CARTESIAN_POINT ( 'NONE',  ( 11.49541394825729768, -65.34930665952259687, -17.78290644886060079 ) ) ;
#42470=CARTESIAN_POINT ( 'NONE',  ( 10.66940904945339952, 33.58243990817589264, -46.87940410059270135 ) ) ;
#42472=CARTESIAN_POINT ( 'NONE',  ( 11.73545769477099832, -65.42259919599071338, -18.15007894733780347 ) ) ;
#42473=CARTESIAN_POINT ( 'NONE',  ( 16.65420337943509566, -51.11618894467930119, -15.67544740040250062 ) ) ;
#42480=CARTESIAN_POINT ( 'NONE',  ( 10.77457706359389888, -63.40313208684650448, -45.20848294960729419 ) ) ;
#42484=CARTESIAN_POINT ( 'NONE',  ( -11.32734370190460105, 10.64934056395049922, 8.349999999999999645 ) ) ;
#42485=CARTESIAN_POINT ( 'NONE',  ( 68.13393739769620083, -33.11618894467940066, -65.65000000000000568 ) ) ;
#42486=EDGE_CURVE ( 'NONE', #3287, #26440, #38246, .T. ) ;
#42487=CARTESIAN_POINT ( 'NONE',  ( 52.24694086453770581, 18.59896962735679793, -77.11046207536941210 ) ) ;
#42490=PLANE ( 'NONE',  #45056 ) ;
#42500=CARTESIAN_POINT ( 'NONE',  ( 65.46029542295769943, -1.463538230407920082, -16.55376543218019947 ) ) ;
#42504=CARTESIAN_POINT ( 'NONE',  ( 14.46049191127040068, 20.21128881784729714, -75.25165125838280744 ) ) ;
#42505=B_SPLINE_CURVE_WITH_KNOTS ( 'NONE', 3,
 ( #50929, #3233, #39909, #15288, #7686, #32007, #12129, #16051, #35452, #48031 ),
 .UNSPECIFIED., .F., .F.,
 ( 4, 2, 2, 2, 4 ),
 ( 0.000000000000000000, 0.1249361396779638672, 0.3249507363229993118, 0.6449740909550615298, 1.000000000000000000 ),
 .UNSPECIFIED. ) ;
#42506=ADVANCED_FACE ( 'NONE', ( #3402 ), #3871, .T. ) ;
#42507=CARTESIAN_POINT ( 'NONE',  ( 17.60468922291027027, -52.01452886433823153, -75.82251645567225751 ) ) ;
#42508=( BOUNDED_CURVE ( )  B_SPLINE_CURVE ( 3, ( #2270, #34736, #33957, #10138 ),
 .UNSPECIFIED., .F., .T. ) 
 B_SPLINE_CURVE_WITH_KNOTS ( ( 4, 4 ),
 ( 5.485850788443479509, 6.283185307179586232 ),
 .UNSPECIFIED. ) 
 CURVE ( )  GEOMETRIC_REPRESENTATION_ITEM ( )  RATIONAL_B_SPLINE_CURVE ( ( 1.000000000000000000, 0.9477194463358846743, 0.9477194463358846743, 1.000000000000000000 ) ) 
 REPRESENTATION_ITEM ( '' )  );
#42509=CARTESIAN_POINT ( 'NONE',  ( 40.88927314113769285, -45.09957127860379700, -5.596099653381020111 ) ) ;
#42512=ORIENTED_EDGE ( 'NONE', *, *, #34752, .T. ) ;
#42514=CARTESIAN_POINT ( 'NONE',  ( 56.68161731648030610, -50.69729438425329704, -74.14921287266520267 ) ) ;
#42515=CARTESIAN_POINT ( 'NONE',  ( 12.13746661513899916, 33.80420561274659974, -16.30595336032680009 ) ) ;
#42517=DIRECTION ( 'NONE',  ( 0.000000000000000000, 0.000000000000000000, 1.000000000000000000 ) ) ;
#42521=CARTESIAN_POINT ( 'NONE',  ( 47.49808756796829812, 23.36748740488750187, -54.86913899898670621 ) ) ;
#42523=CARTESIAN_POINT ( 'NONE',  ( 43.46647314489950276, -45.04259908834720250, -6.433232421327499395 ) ) ;
#42525=CARTESIAN_POINT ( 'NONE',  ( 57.46491512144735481, 13.88414644239919404, -25.32915905940588885 ) ) ;
#42526=CARTESIAN_POINT ( 'NONE',  ( 11.77474680307169841, 33.82436456779279865, -16.56178175560690136 ) ) ;
#42527=CARTESIAN_POINT ( 'NONE',  ( 51.84245824985789852, 18.13569299140640112, -76.99756684514699145 ) ) ;
#42528=CARTESIAN_POINT ( 'NONE',  ( 52.91916940086609600, 18.38207858727010091, -48.76921091615339776 ) ) ;
#42529=DIRECTION ( 'NONE',  ( 0.000000000000000000, 1.000000000000000000, 0.000000000000000000 ) ) ;
#42530=CARTESIAN_POINT ( 'NONE',  ( 57.55751162049570269, -50.61618894467930119, -53.92796738110899923 ) ) ;
#42531=CARTESIAN_POINT ( 'NONE',  ( 53.18313144231220235, 18.10656684143660300, -27.45873945498200186 ) ) ;
#42538=CARTESIAN_POINT ( 'NONE',  ( 10.97915888064600054, 32.07709238800340046, -44.74319236371729858 ) ) ;
#42540=DIRECTION ( 'NONE',  ( 1.000000000000000000, 0.000000000000000000, 0.000000000000000000 ) ) ;
#42541=CARTESIAN_POINT ( 'NONE',  ( 12.73487912048826232, 24.23912916116268690, -75.56421958049274679 ) ) ;
#42542=ORIENTED_EDGE ( 'NONE', *, *, #31306, .F. ) ;
#42543=ORIENTED_EDGE ( 'NONE', *, *, #10791, .F. ) ;
#42544=CARTESIAN_POINT ( 'NONE',  ( 41.06001733956060207, 13.06695014755839956, -3.719605790254209676 ) ) ;
#42545=CARTESIAN_POINT ( 'NONE',  ( 76.55758335127733005, 0.1435741152385172914, -13.47555346654003827 ) ) ;
#42546=ORIENTED_EDGE ( 'NONE', *, *, #51758, .T. ) ;
#42547=CARTESIAN_POINT ( 'NONE',  ( 11.70108564249209948, -64.94919988858430315, -45.68669056181820309 ) ) ;
#42548=CARTESIAN_POINT ( 'NONE',  ( 56.70280968235780250, -45.37092424972929905, -25.70441953237769894 ) ) ;
#42551=CARTESIAN_POINT ( 'NONE',  ( 56.52536539877749533, 19.51942783438209972, -53.84278118897309895 ) ) ;
#42552=VERTEX_POINT ( 'NONE', #15126 ) ;
#42553=LINE ( 'NONE', #38622, #34340 ) ;
#42555=CARTESIAN_POINT ( 'NONE',  ( 10.73251648177490125, 33.05260077103709904, -23.50916409409499863 ) ) ;
#42556=EDGE_CURVE ( 'NONE', #18612, #1476, #3011, .T. ) ;
#42558=CARTESIAN_POINT ( 'NONE',  ( 51.63377760632049984, -45.11618894467940066, -11.44539556602689956 ) ) ;
#42561=CARTESIAN_POINT ( 'NONE',  ( 16.33938386690500266, 19.86387930602199958, -20.40297663956880214 ) ) ;
#42565=CARTESIAN_POINT ( 'NONE',  ( 47.37011039443260074, -54.67477790795700088, -74.19794602913619030 ) ) ;
#42566=CARTESIAN_POINT ( 'NONE',  ( 61.85779513593570300, 12.50882928757600077, -9.638490008265870657 ) ) ;
#42567=CIRCLE ( 'NONE', #36656, 20.79999999999999716 ) ;
#42568=CARTESIAN_POINT ( 'NONE',  ( 56.27102044028909944, 19.34483705538490028, -52.87264067008490542 ) ) ;
#42569=CARTESIAN_POINT ( 'NONE',  ( 52.03834263415010497, 20.05835102498519973, -76.00976797213479585 ) ) ;
#42570=CARTESIAN_POINT ( 'NONE',  ( 11.93174526809839975, 34.20691394249479345, -17.93019253464870033 ) ) ;
#42572=ORIENTED_EDGE ( 'NONE', *, *, #26025, .T. ) ;
#42574=CARTESIAN_POINT ( 'NONE',  ( 9.023247183187249831, -62.42415218838889501, -14.37474631752760068 ) ) ;
#42575=CARTESIAN_POINT ( 'NONE',  ( 76.39865836638340113, -5.985310478428520042, -12.78927121757400087 ) ) ;
#42577=CARTESIAN_POINT ( 'NONE',  ( 61.14784649246698933, -45.50800750378603254, -47.53180933876430458 ) ) ;
#42578=CARTESIAN_POINT ( 'NONE',  ( 13.21803463400281231, -55.50872388801388979, -75.91709172390962124 ) ) ;
#42580=ADVANCED_FACE ( 'NONE', ( #31084 ), #14831, .F. ) ;
#42581=CARTESIAN_POINT ( 'NONE',  ( 82.48418901823390570, -45.09830753207049270, -46.54733415317949863 ) ) ;
#42582=CARTESIAN_POINT ( 'NONE',  ( 52.82975622904280755, -49.66092049964720445, -48.47378032971909789 ) ) ;
#42583=CARTESIAN_POINT ( 'NONE',  ( 42.73119093514949896, 11.67612964396700015, -3.876063987046979964 ) ) ;
#42586=CARTESIAN_POINT ( 'NONE',  ( 68.13393739769790614, -49.95860450174320277, -71.35146707679190570 ) ) ;
#42587=ADVANCED_FACE ( 'NONE', ( #10423 ), #22446, .T. ) ;
#42589=CARTESIAN_POINT ( 'NONE',  ( 18.67895139973730068, -51.93864758878049059, -75.09854824053090283 ) ) ;
#42590=CARTESIAN_POINT ( 'NONE',  ( 58.57901109696710051, -44.96736093356130226, -9.776967083451840068 ) ) ;
#42597=CARTESIAN_POINT ( 'NONE',  ( 74.93037295002240228, 11.88381105532070059, -15.31098073120859837 ) ) ;
#42599=VECTOR ( 'NONE', #10907, 1000.000000000000000 ) ;
#42603=CARTESIAN_POINT ( 'NONE',  ( 42.04042276467250616, -45.73515590541849463, -6.805329779705280302 ) ) ;
#42606=VERTEX_POINT ( 'NONE', #38724 ) ;
#42608=CARTESIAN_POINT ( 'NONE',  ( 61.45294174207020177, -45.16075577691309917, -46.37196027249549957 ) ) ;
#42610=DIRECTION ( 'NONE',  ( 0.7675009104025395379, 0.5576220516902739011, 0.3162277660168420490 ) ) ;
#42611=ORIENTED_EDGE ( 'NONE', *, *, #23895, .F. ) ;
#42616=CARTESIAN_POINT ( 'NONE',  ( 11.89321892217540011, -65.43602743108330344, -18.17421237901570308 ) ) ;
#42617=ORIENTED_EDGE ( 'NONE', *, *, #43077, .F. ) ;
#42618=CARTESIAN_POINT ( 'NONE',  ( 53.62552786343490396, -51.33071804962359153, -75.58099297212140755 ) ) ;
#42619=CARTESIAN_POINT ( 'NONE',  ( 52.09209166129659963, -51.30114848017019824, -75.99731152592609362 ) ) ;
#42620=CARTESIAN_POINT ( 'NONE',  ( 60.78179592255849428, 14.26585277497870052, -47.15482822166340071 ) ) ;
#42621=LINE ( 'NONE', #46562, #17975 ) ;
#42622=CARTESIAN_POINT ( 'NONE',  ( 41.26036424091849852, -44.20758967157720321, -4.192607877207990441 ) ) ;
#42623=CARTESIAN_POINT ( 'NONE',  ( 0.5406133260286669628, -43.55985091651039909, -20.15000000000000213 ) ) ;
#42624=DIRECTION ( 'NONE',  ( 0.2771081164311154366, 0.6505467637364714673, -0.7071067811865496822 ) ) ;
#42633=CARTESIAN_POINT ( 'NONE',  ( 14.21949999245200047, -52.31213937195320085, -75.84958893011570069 ) ) ;
#42634=CARTESIAN_POINT ( 'NONE',  ( 57.55751162087899786, 19.38381105532060289, -53.87300832421969687 ) ) ;
#42640=CARTESIAN_POINT ( 'NONE',  ( 47.18305862770080239, -54.80685414274160649, -74.19838441418400521 ) ) ;
#42642=CARTESIAN_POINT ( 'NONE',  ( 47.79229160385850150, -54.46650021306819411, -55.08202210981530556 ) ) ;
#42646=CARTESIAN_POINT ( 'NONE',  ( 47.82372406217509564, 23.16461151845500410, -54.73644791471539861 ) ) ;
#42663=CARTESIAN_POINT ( 'NONE',  ( 12.28895731154639925, -64.62670895685438666, -15.84602084846439851 ) ) ;
#42666=AXIS2_PLACEMENT_3D ( 'NONE', #36208, #32254, #20998 ) ;
#42667=CARTESIAN_POINT ( 'NONE',  ( 76.46740023287678412, -26.22475495909479903, -13.08694098715510812 ) ) ;
#42668=CARTESIAN_POINT ( 'NONE',  ( 13.00893739769619906, -65.51843714052719747, -47.75434321273180416 ) ) ;
#42669=AXIS2_PLACEMENT_3D ( 'NONE', #47219, #34878, #27524 ) ;
#42671=AXIS2_PLACEMENT_3D ( 'NONE', #17642, #33608, #45679 ) ;
#42672=EDGE_LOOP ( 'NONE', ( #34823, #22462, #23031, #28189 ) ) ;
#42675=CARTESIAN_POINT ( 'NONE',  ( 56.59172680816769940, 14.94416698784849906, -26.26184181833360043 ) ) ;
#42676=CARTESIAN_POINT ( 'NONE',  ( 49.71164272696770325, 21.47435747220460200, -52.28127911264229510 ) ) ;
#42677=EDGE_CURVE ( 'NONE', #11471, #22490, #695, .T. ) ;
#42678=CARTESIAN_POINT ( 'NONE',  ( 59.10140662637690667, -2.844898398060870193, -15.65498877140790057 ) ) ;
#42679=CARTESIAN_POINT ( 'NONE',  ( 51.36577782788289426, -50.50831518850419855, -76.23494669504191279 ) ) ;
#42680=CARTESIAN_POINT ( 'NONE',  ( 57.70617712934760135, -49.34354290365170215, -51.67788969020119794 ) ) ;
#42684=EDGE_LOOP ( 'NONE', ( #7605, #9638, #33873, #48077, #9019 ) ) ;
#42685=PLANE ( 'NONE',  #41084 ) ;
#42686=CARTESIAN_POINT ( 'NONE',  ( 46.03121886948380137, -45.11618894467940066, -7.582877905987319700 ) ) ;
#42688=CARTESIAN_POINT ( 'NONE',  ( 13.51721644893999930, -51.27681913022160387, -22.28354840475149956 ) ) ;
#42689=CARTESIAN_POINT ( 'NONE',  ( 54.61320183681609564, 19.39270185280140169, -76.58475370837619778 ) ) ;
#42691=CARTESIAN_POINT ( 'NONE',  ( 47.13794097070190503, -53.89583813975270488, -75.74423906255060501 ) ) ;
#42693=CARTESIAN_POINT ( 'NONE',  ( 56.31194726212379464, 13.95803596900150012, -15.90921559078330105 ) ) ;
#42694=CARTESIAN_POINT ( 'NONE',  ( 47.77115924678660264, 23.22414640103279737, -54.89636912190230333 ) ) ;
#42695=CARTESIAN_POINT ( 'NONE',  ( 56.72051766772629833, -50.68676931991719670, -53.84018978630530228 ) ) ;
#42699=CARTESIAN_POINT ( 'NONE',  ( 47.57154850773209631, 23.33333469726499843, -74.14999583207048772 ) ) ;
#42705=CARTESIAN_POINT ( 'NONE',  ( 57.73379141935919989, 13.88381105532070059, -10.52253854761309881 ) ) ;
#42706=AXIS2_PLACEMENT_3D ( 'NONE', #50651, #38339, #2429 ) ;
#42708=CARTESIAN_POINT ( 'NONE',  ( 82.34446853826591450, 14.37294419959810021, -47.68359979375730262 ) ) ;
#42709=DIRECTION ( 'NONE',  ( 0.000000000000000000, 0.000000000000000000, 1.000000000000000000 ) ) ;
#42710=CARTESIAN_POINT ( 'NONE',  ( 47.58828883988076086, 23.23481555469353665, -74.72737448183970344 ) ) ;
#42714=CARTESIAN_POINT ( 'NONE',  ( -33.07468191286329784, -5.899192223876280394, -56.92399776842329828 ) ) ;
#42716=CARTESIAN_POINT ( 'NONE',  ( 52.88917640181519886, -49.63475167565859891, -48.82176623077139510 ) ) ;
#42720=CARTESIAN_POINT ( 'NONE',  ( 13.77293538034790110, 20.06110664901489926, -23.09858809179250017 ) ) ;
#42721=CARTESIAN_POINT ( 'NONE',  ( 84.44784216359251161, 11.88381105532070059, -47.47585302082339354 ) ) ;
#42724=CARTESIAN_POINT ( 'NONE',  ( 52.64535713109459891, 18.55400356624080160, -48.56190053269869367 ) ) ;
#42725=CARTESIAN_POINT ( 'NONE',  ( 54.65216101584789499, -46.12197618676970734, -15.81768032851119798 ) ) ;
#42727=ORIENTED_EDGE ( 'NONE', *, *, #32329, .F. ) ;
#42729=ORIENTED_EDGE ( 'NONE', *, *, #49692, .T. ) ;
#42732=CARTESIAN_POINT ( 'NONE',  ( 8.815605938091740867, 32.05029769240140070, -46.67186391159280134 ) ) ;
#42734=CARTESIAN_POINT ( 'NONE',  ( 11.43830175781249991, -65.36132525204969568, -18.07704217317780149 ) ) ;
#42742=CARTESIAN_POINT ( 'NONE',  ( 10.76899899952330131, -63.11543068638779630, -45.20723331625340791 ) ) ;
#42744=VERTEX_POINT ( 'NONE', #35757 ) ;
#42746=CARTESIAN_POINT ( 'NONE',  ( 13.88455093916192951, -52.17615671833033275, -75.56421372420085447 ) ) ;
#42747=CARTESIAN_POINT ( 'NONE',  ( 56.96124594780639683, 19.37506853770539905, -53.44837636194950647 ) ) ;
#42748=CARTESIAN_POINT ( 'NONE',  ( 51.99242832924639401, 18.79345593400340064, -76.70333696056400186 ) ) ;
#42749=ORIENTED_EDGE ( 'NONE', *, *, #44547, .F. ) ;
#42753=CARTESIAN_POINT ( 'NONE',  ( 14.98932469835694015, 21.70055148386502708, -76.14999999999994884 ) ) ;
#42755=B_SPLINE_SURFACE_WITH_KNOTS ( 'NONE', 3, 3, ( 
 ( #15110, #31325, #11447, #11959, #27663, #43406, #7508, #23455, #47601, #15628, #43918, #40754, #39988, #20052, #403, #48897 ),
 ( #16389, #12731, #40494, #32345, #28948, #16643, #20559, #36043, #21086, #37087, #153, #16129, #36555, #50182, #50443, #21595 ),
 ( #17940, #21860, #45733, #37871, #26567, #34691, #18970, #23659, #27095, #39163, #40437, #864, #32805, #36494, #15817, #12156 ),
 ( #347, #16333, #37810, #33854, #25989, #42002, #22057, #30187, #43298, #35413, #30442, #2940, #18911, #537, #19935, #16271 ),
 ( #24362, #40375, #32472, #20699, #8937, #17056, #33277, #49556, #21217, #37228, #33538, #13140, #29852, #41935, #9958, #13390 ),
 ( #13894, #41408, #21481, #6035, #29603, #14149, #44832, #45087, #9705, #25665, #5772, #10228, #2880, #39046, #47172, #35085 ),
 ( #51088, #6295, #15186, #6815, #14665, #30635, #39294, #46659, #11002, #50321, #26186, #14407, #31147, #26444, #18848, #43235 ),
 ( #27222, #10742, #7327, #7074, #23274, #19108, #18594, #26970, #11260, #3401, #19368, #34308, #30375, #22769, #35350, #34570 ),
 ( #46916, #50575, #46400, #46137, #51350, #30118, #42197, #22253, #10488, #26698, #38260, #38523, #42460, #2353, #18327, #6547 ),
 ( #22512, #2622, #42979, #42720, #30888, #38788, #23024, #34831, #50832, #14924, #3140, #51859, #4668, #20380, #7841, #11521 ) ),
 .UNSPECIFIED., .F., .F., .F.,
 ( 4, 1, 1, 1, 1, 1, 1, 4 ),
 ( 4, 2, 2, 2, 2, 2, 2, 4 ),
 ( -5.223883000000000085E-09, 0.1428571428571430157, 0.2857142857142860315, 0.4285714285714289917, 0.5714285714285709528, 0.7142857142857139685, 0.8571428571428569843, 1.000000005223879995 ),
 ( -5.223902000000000352E-09, 0.4421500870759600410, 0.9474644723056518947, 1.263285963074209928, 1.421196708458489999, 1.673853901073329986, 2.078105409257089864, 2.526571926298299964 ),
 .UNSPECIFIED. ) ;
#42758=LINE ( 'NONE', #47969, #26682 ) ;
#42759=ORIENTED_EDGE ( 'NONE', *, *, #27890, .F. ) ;
#42761=CARTESIAN_POINT ( 'NONE',  ( 59.34499803081109803, -3.116188944679349593, -15.68015151901639825 ) ) ;
#42764=DIRECTION ( 'NONE',  ( 0.000000000000000000, 0.000000000000000000, 1.000000000000000000 ) ) ;
#42765=CARTESIAN_POINT ( 'NONE',  ( 61.54865580197261465, 14.09499822944240677, -47.27157924453907611 ) ) ;
#42767=CARTESIAN_POINT ( 'NONE',  ( 43.41850781425760175, -45.38663701516029647, -7.209125745969769739 ) ) ;
#42771=CARTESIAN_POINT ( 'NONE',  ( 56.43501562198250099, -50.77275378297979813, -74.43358758419878995 ) ) ;
#42772=CARTESIAN_POINT ( 'NONE',  ( -10.41134978075270112, 11.60703557408290010, -6.431294820763719500 ) ) ;
#42774=EDGE_CURVE ( 'NONE', #20020, #21835, #805, .T. ) ;
#42775=CARTESIAN_POINT ( 'NONE',  ( 47.81335647231890107, -54.39749252969859583, -54.71582838609030119 ) ) ;
#42778=CARTESIAN_POINT ( 'NONE',  ( 14.90280893508995419, 21.76199782481209510, -76.14999999999999147 ) ) ;
#42780=VECTOR ( 'NONE', #35241, 1000.000000000000000 ) ;
#42781=CARTESIAN_POINT ( 'NONE',  ( 47.77676144020560400, 23.19303230712679920, -54.74761805967199990 ) ) ;
#42782=CARTESIAN_POINT ( 'NONE',  ( 44.76356921293569968, -45.10235736362039916, -7.023953210218369492 ) ) ;
#42784=CARTESIAN_POINT ( 'NONE',  ( 61.09287626159920137, 14.33135539182030094, -47.61635106652619953 ) ) ;
#42785=CIRCLE ( 'NONE', #12626, 35.00000000000000000 ) ;
#42786=CARTESIAN_POINT ( 'NONE',  ( 11.28671401888810166, 33.77463329229920674, -16.86100853830619783 ) ) ;
#42788=CARTESIAN_POINT ( 'NONE',  ( 51.57064462373369906, 17.81647325063629950, -76.80688255937791098 ) ) ;
#42789=CARTESIAN_POINT ( 'NONE',  ( 52.83359294848519738, 18.42653244547510027, -48.59872226080710078 ) ) ;
#42792=CARTESIAN_POINT ( 'NONE',  ( 55.30698993685479792, 16.11823302483700004, -26.47716174366970066 ) ) ;
#42793=CARTESIAN_POINT ( 'NONE',  ( 50.72687041832384836, 4.467326087330391715, -76.27485697391391284 ) ) ;
#42798=CARTESIAN_POINT ( 'NONE',  ( 10.77201485400030023, 32.03292712579329304, -45.20473333481510281 ) ) ;
#42800=CARTESIAN_POINT ( 'NONE',  ( 65.70572775221249628, -32.85841248749620291, -18.95019544618720175 ) ) ;
#42805=CARTESIAN_POINT ( 'NONE',  ( 76.49486337784722423, -3.223960196710998094, -13.20528376621882671 ) ) ;
#42808=CARTESIAN_POINT ( 'NONE',  ( 10.93389818273009872, -63.58325642793808896, -44.91480761438189973 ) ) ;
#42809=CARTESIAN_POINT ( 'NONE',  ( 57.47931744391669895, -45.11451192150079947, -25.32996107807690223 ) ) ;
#42813=ORIENTED_EDGE ( 'NONE', *, *, #32751, .F. ) ;
#42816=CARTESIAN_POINT ( 'NONE',  ( 11.97592558356920023, 33.51641353631480058, -24.42566912137219859 ) ) ;
#42817=ORIENTED_EDGE ( 'NONE', *, *, #43530, .T. ) ;
#42819=CARTESIAN_POINT ( 'NONE',  ( 52.10267377313040527, 1.883811054805347496, -20.31845379076632696 ) ) ;
#42820=CARTESIAN_POINT ( 'NONE',  ( 14.38278649113999919, 19.81652936503730089, -21.89951529875269998 ) ) ;
#42822=CARTESIAN_POINT ( 'NONE',  ( 61.79720211019959208, -29.51961015981989789, -16.03830591840080189 ) ) ;
#42826=CARTESIAN_POINT ( 'NONE',  ( 46.73688746986190523, -53.63908013404079611, -75.98233228156729524 ) ) ;
#42827=AXIS2_PLACEMENT_3D ( 'NONE', #42221, #30143, #15215 ) ;
#42828=CARTESIAN_POINT ( 'NONE',  ( 49.56322960257909926, 13.74100540729780029, -7.475321071136599826 ) ) ;
#42829=EDGE_CURVE ( 'NONE', #42328, #814, #17347, .T. ) ;
#42830=VECTOR ( 'NONE', #21759, 1000.000000000000000 ) ;
#42834=VERTEX_POINT ( 'NONE', #25419 ) ;
#42835=CARTESIAN_POINT ( 'NONE',  ( 56.06469054980239974, -46.69807554794920179, -26.34903941785619708 ) ) ;
#42836=CARTESIAN_POINT ( 'NONE',  ( -4.162434749930929989, -49.37281588411619992, -7.617592385375469455 ) ) ;
#42837=CARTESIAN_POINT ( 'NONE',  ( 75.71017558016721694, -8.423768395189359381, -11.72022506976029987 ) ) ;
#42838=CARTESIAN_POINT ( 'NONE',  ( 75.12127646723587304, 13.76128322658033021, -14.64863796607091473 ) ) ;
#42842=DIRECTION ( 'NONE',  ( 0.000000000000000000, -0.9319748226751538578, -0.3625230060280530409 ) ) ;
#42843=CARTESIAN_POINT ( 'NONE',  ( 82.13853704237929776, -45.60474347597770617, -47.68296857959820301 ) ) ;
#42844=FACE_OUTER_BOUND ( 'NONE', #11502, .T. ) ;
#42845=CARTESIAN_POINT ( 'NONE',  ( 41.00922577670660019, 13.27405061951239951, -4.614727581921130195 ) ) ;
#42848=CARTESIAN_POINT ( 'NONE',  ( 15.05440318628160057, -53.11618894467930119, -76.14999999999999147 ) ) ;
#42849=CARTESIAN_POINT ( 'NONE',  ( 70.83745409581581498, -49.21324915459896943, -75.95351669811965678 ) ) ;
#42850=CARTESIAN_POINT ( 'NONE',  ( 76.38512529972561538, -43.26453402920058977, -13.94652733128153344 ) ) ;
#42851=CARTESIAN_POINT ( 'NONE',  ( 18.58833069766529889, -51.79024427787479823, -75.14498753491568550 ) ) ;
#42852=CARTESIAN_POINT ( 'NONE',  ( 60.78568630568080522, -44.33970749964649372, -9.604110006574771319 ) ) ;
#42853=ORIENTED_EDGE ( 'NONE', *, *, #1535, .T. ) ;
#42854=AXIS2_PLACEMENT_3D ( 'NONE', #27161, #47364, #3848 ) ;
#42859=AXIS2_PLACEMENT_3D ( 'NONE', #45945, #38077, #11079 ) ;
#42860=DIRECTION ( 'NONE',  ( 0.000000000000000000, 0.000000000000000000, -1.000000000000000000 ) ) ;
#42862=CARTESIAN_POINT ( 'NONE',  ( 7.492845759203685674, -61.18022026567161475, -20.13893727953967172 ) ) ;
#42864=CARTESIAN_POINT ( 'NONE',  ( 43.16098550650539778, -45.75650059835369632, -7.511432296416719723 ) ) ;
#42867=VERTEX_POINT ( 'NONE', #23675 ) ;
#42870=CARTESIAN_POINT ( 'NONE',  ( 82.48407194341798743, -45.09832794361063435, -46.54736621596860147 ) ) ;
#42877=CARTESIAN_POINT ( 'NONE',  ( 13.88455142272560039, 20.94377921756336036, -75.56421430877985301 ) ) ;
#42878=CARTESIAN_POINT ( 'NONE',  ( 51.20054084488780433, -50.75953116010929733, -76.16661697631359118 ) ) ;
#42879=CARTESIAN_POINT ( 'NONE',  ( 60.66491735500950000, 14.33979589326570014, -47.29697835118949456 ) ) ;
#42882=LINE ( 'NONE', #42097, #17199 ) ;
#42883=CARTESIAN_POINT ( 'NONE',  ( 40.90236900589889757, -44.69077732174059747, -4.970360716545750179 ) ) ;
#42886=CARTESIAN_POINT ( 'NONE',  ( -3.426429430513819874, 17.54101937228130126, -5.615273139885949227 ) ) ;
#42891=CARTESIAN_POINT ( 'NONE',  ( 17.91327630046971819, -51.14555453227458770, -74.54430098196459653 ) ) ;
#42893=ORIENTED_EDGE ( 'NONE', *, *, #25464, .T. ) ;
#42894=FACE_OUTER_BOUND ( 'NONE', #7615, .T. ) ;
#42895=CARTESIAN_POINT ( 'NONE',  ( 57.55751162087899786, 18.96618911681419917, -52.70112124855629787 ) ) ;
#42898=CARTESIAN_POINT ( 'NONE',  ( 15.65736449273109976, 19.70849029160099875, -20.65166207265459875 ) ) ;
#42900=EDGE_CURVE ( 'NONE', #17894, #19377, #50943, .T. ) ;
#42901=CARTESIAN_POINT ( 'NONE',  ( 61.31732713205895635, 14.08360349558539149, -47.18610833908295632 ) ) ;
#42902=CARTESIAN_POINT ( 'NONE',  ( 48.02939153114380133, -54.36963205275340272, -55.28067537372130147 ) ) ;
#42904=CARTESIAN_POINT ( 'NONE',  ( -5.159222269204799538, -47.09623647380401934, -4.453993764612231843 ) ) ;
#42906=CARTESIAN_POINT ( 'NONE',  ( 47.77546308418779830, 23.20957882008939777, -54.82267176636759842 ) ) ;
#42907=ORIENTED_EDGE ( 'NONE', *, *, #23527, .T. ) ;
#42909=ORIENTED_EDGE ( 'NONE', *, *, #1431, .T. ) ;
#42911=CARTESIAN_POINT ( 'NONE',  ( 60.27779889700099147, -45.75868226597979316, -47.23595182050330266 ) ) ;
#42912=CARTESIAN_POINT ( 'NONE',  ( 56.94228693352650339, -47.50625043831589522, -47.82842110489030318 ) ) ;
#42916=DIRECTION ( 'NONE',  ( 3.556943099846429769E-14, -1.469246684736110336E-14, 1.000000000000000000 ) ) ;
#42919=VERTEX_POINT ( 'NONE', #20395 ) ;
#42922=ORIENTED_EDGE ( 'NONE', *, *, #21884, .T. ) ;
#42923=CARTESIAN_POINT ( 'NONE',  ( 12.33251669429900055, -64.64566256145140244, -15.86092359077770020 ) ) ;
#42924=CARTESIAN_POINT ( 'NONE',  ( 68.13393739769620083, 19.38381105532069881, -75.00000000000000000 ) ) ;
#42925=CARTESIAN_POINT ( 'NONE',  ( 76.44421473112753063, -24.47276274790905504, -12.98703123328389708 ) ) ;
#42926=CARTESIAN_POINT ( 'NONE',  ( 9.020077921220060801, -63.39297508468359865, -46.63174122437119706 ) ) ;
#42929=VERTEX_POINT ( 'NONE', #32431 ) ;
#42931=CARTESIAN_POINT ( 'NONE',  ( 11.19961559249191474, -65.24734874261105233, -22.25048313876769868 ) ) ;
#42934=CARTESIAN_POINT ( 'NONE',  ( 64.25188488369910544, -0.1060032360258039985, -16.75951320883940099 ) ) ;
#42935=CARTESIAN_POINT ( 'NONE',  ( 51.75950599516050232, -49.44977665203700212, -76.84761942479970287 ) ) ;
#42937=VERTEX_POINT ( 'NONE', #8624 ) ;
#42940=ORIENTED_EDGE ( 'NONE', *, *, #48917, .T. ) ;
#42942=CARTESIAN_POINT ( 'NONE',  ( 59.93898548971230156, -46.07977442274060564, -47.78350827547860291 ) ) ;
#42945=CARTESIAN_POINT ( 'NONE',  ( 13.90974566255180100, -51.18269991979300215, -22.51683827224059797 ) ) ;
#42949=CARTESIAN_POINT ( 'NONE',  ( 56.71523363900320192, 14.03280086630570089, -17.52449187449219536 ) ) ;
#42950=CARTESIAN_POINT ( 'NONE',  ( 60.90942164635529821, -45.48565787205490096, -47.35587748028390109 ) ) ;
#42951=CARTESIAN_POINT ( 'NONE',  ( 56.58636862550530111, -50.60438040973590290, -53.13121941639199974 ) ) ;
#42955=CARTESIAN_POINT ( 'NONE',  ( 47.61801188784319550, 23.31248625996650148, -74.17383159519339131 ) ) ;
#42959=AXIS2_PLACEMENT_3D ( 'NONE', #13324, #44766, #37164 ) ;
#42961=CARTESIAN_POINT ( 'NONE',  ( 15.41380670901278194, -50.77307959834621442, -20.47803142984178493 ) ) ;
#42963=DIRECTION ( 'NONE',  ( -0.5109955813515499878, 0.8595833385072046973, 0.000000000000000000 ) ) ;
#42965=EDGE_CURVE ( 'NONE', #42744, #47075, #13977, .T. ) ;
#42966=CARTESIAN_POINT ( 'NONE',  ( 82.13853704237929776, 14.12152868491880042, -47.32252334011910477 ) ) ;
#42969=CARTESIAN_POINT ( 'NONE',  ( 83.89200044194980421, -48.61618894467930119, -53.92796738110899923 ) ) ;
#42970=EDGE_CURVE ( 'NONE', #4421, #26368, #28357, .T. ) ;
#42972=CARTESIAN_POINT ( 'NONE',  ( 68.13393739769620083, 19.38381105532069881, -71.50000000000000000 ) ) ;
#42973=CARTESIAN_POINT ( 'NONE',  ( 49.08014769244979902, 22.68967210332029794, -55.22540290251299666 ) ) ;
#42974=ORIENTED_EDGE ( 'NONE', *, *, #25525, .T. ) ;
#42975=CARTESIAN_POINT ( 'NONE',  ( 52.78692773688430151, -49.69208888116699541, -48.74514769400369829 ) ) ;
#42976=VERTEX_POINT ( 'NONE', #742 ) ;
#42979=CARTESIAN_POINT ( 'NONE',  ( 13.68997053979789946, 20.12589560456379800, -23.13969475654330310 ) ) ;
#42982=CARTESIAN_POINT ( 'NONE',  ( 52.62463376634089940, 18.57086902152009955, -48.47378032971769812 ) ) ;
#42983=CARTESIAN_POINT ( 'NONE',  ( 56.18245545401309471, -45.53975730964529589, -17.22565076933249983 ) ) ;
#42985=AXIS2_PLACEMENT_3D ( 'NONE', #41866, #5207, #25346 ) ;
#42986=EDGE_LOOP ( 'NONE', ( #46397, #33370, #23929, #16719 ) ) ;
#42990=CARTESIAN_POINT ( 'NONE',  ( 9.422115487779029408, 32.29033719602479380, -46.51238083606079954 ) ) ;
#42993=CARTESIAN_POINT ( 'NONE',  ( 52.90434498377167216, -49.66345680823592090, -49.01850774012503820 ) ) ;
#42995=CARTESIAN_POINT ( 'NONE',  ( 49.70112820465350012, -53.65753597205910097, -55.00786376658719945 ) ) ;
#42999=CARTESIAN_POINT ( 'NONE',  ( 10.48761941044149815, -63.17386106513639277, -45.62707961905420717 ) ) ;
#43000=CARTESIAN_POINT ( 'NONE',  ( 69.22748654599821805, 19.47158195952120963, -71.50000000000200373 ) ) ;
#43003=CARTESIAN_POINT ( 'NONE',  ( 57.35856958860869526, 18.90358493063820333, -52.61941485291330167 ) ) ;
#43004=CARTESIAN_POINT ( 'NONE',  ( 53.72303973069330141, 19.38806196010829908, -76.82797360176211043 ) ) ;
#43005=CIRCLE ( 'NONE', #3637, 30.50439988982899564 ) ;
#43008=DIRECTION ( 'NONE',  ( -1.000000000000000000, 0.000000000000000000, 0.000000000000000000 ) ) ;
#43009=CARTESIAN_POINT ( 'NONE',  ( 67.35174094906719233, -47.86618894467930119, -50.14999999999999858 ) ) ;
#43014=DIRECTION ( 'NONE',  ( -0.4640893551880601597, 0.8857883891771953788, 0.000000000000000000 ) ) ;
#43015=DIRECTION ( 'NONE',  ( 0.3569024281753349626, 0.000000000000000000, 0.9341416684649872515 ) ) ;
#43017=ORIENTED_EDGE ( 'NONE', *, *, #39466, .F. ) ;
#43020=CARTESIAN_POINT ( 'NONE',  ( 54.29943625382440331, 13.88381105524610071, -13.69441485379169876 ) ) ;
#43025=CARTESIAN_POINT ( 'NONE',  ( 68.13393739769840352, -50.61618894467879670, -73.25000000000220268 ) ) ;
#43026=CARTESIAN_POINT ( 'NONE',  ( 12.17742765527019877, 33.84218639868790035, -16.46016921338960159 ) ) ;
#43027=B_SPLINE_CURVE_WITH_KNOTS ( 'NONE', 3,
 ( #26642, #38204, #5978, #21934 ),
 .UNSPECIFIED., .F., .F.,
 ( 4, 4 ),
 ( 3.936509634373229982, 4.045282574772550710 ),
 .UNSPECIFIED. ) ;
#43030=CARTESIAN_POINT ( 'NONE',  ( 53.86687988220850087, -51.12005429169590087, -75.69951437311600273 ) ) ;
#43031=CARTESIAN_POINT ( 'NONE',  ( -1.367282239498279983, 19.54806105385790005, -6.357905677808130207 ) ) ;
#43032=CARTESIAN_POINT ( 'NONE',  ( 11.07421692656308210, -55.29505889823902010, -44.42833690484276588 ) ) ;
#43033=CARTESIAN_POINT ( 'NONE',  ( 16.13393739769620083, -15.61618894467929941, -14.65000000000000036 ) ) ;
#43036=ORIENTED_EDGE ( 'NONE', *, *, #18550, .F. ) ;
#43038=CARTESIAN_POINT ( 'NONE',  ( 47.57263996198259548, 23.32900398977909973, -54.92582527468099585 ) ) ;
#43039=CARTESIAN_POINT ( 'NONE',  ( 41.84490955069979634, -44.86154966424449952, -5.635703470643719903 ) ) ;
#43041=CARTESIAN_POINT ( 'NONE',  ( 60.80565946055000381, 14.31573824510140014, -47.42904253344379839 ) ) ;
#43043=CARTESIAN_POINT ( 'NONE',  ( 52.04689645930250208, 18.41021695652339929, -77.05403426700469538 ) ) ;
#43044=CARTESIAN_POINT ( 'NONE',  ( 52.82121948977260217, 18.43301524717529816, -48.53631916346480324 ) ) ;
#43046=CARTESIAN_POINT ( 'NONE',  ( 52.89416330280510437, -49.62717582914000047, -48.70339649242369973 ) ) ;
#43047=CARTESIAN_POINT ( 'NONE',  ( 53.99942095567629252, 17.28615893591289776, -26.84178626193609674 ) ) ;
#43048=CARTESIAN_POINT ( 'NONE',  ( 51.41560511219569918, 21.47411202558799914, -53.77857906372980068 ) ) ;
#43050=CARTESIAN_POINT ( 'NONE',  ( 52.99619512781969632, -49.51755756157847799, -27.70008372195887603 ) ) ;
#43051=CARTESIAN_POINT ( 'NONE',  ( 12.36324357420019915, -64.54680782163349306, -15.76420532458509882 ) ) ;
#43052=CARTESIAN_POINT ( 'NONE',  ( 59.09889384191680506, -28.80061074846929969, -15.68544870528650037 ) ) ;
#43054=CARTESIAN_POINT ( 'NONE',  ( 11.13393739769619906, 31.90600321400949824, -43.91241836587330027 ) ) ;
#43056=CARTESIAN_POINT ( 'NONE',  ( 51.08833026580700221, -35.06325589799279641, -76.45203734832688269 ) ) ;
#43061=CARTESIAN_POINT ( 'NONE',  ( 50.08086529025462141, -1.257411408365102901, -16.00829333108001151 ) ) ;
#43062=ORIENTED_EDGE ( 'NONE', *, *, #39829, .F. ) ;
#43063=CARTESIAN_POINT ( 'NONE',  ( 57.12729451229770206, -45.23260415549869862, -25.71705107423920111 ) ) ;
#43064=CARTESIAN_POINT ( 'NONE',  ( 37.88393739769619373, -15.61618894467929941, -11.65000000000000036 ) ) ;
#43066=CARTESIAN_POINT ( 'NONE',  ( 13.88455093916192951, -52.17615671833033275, -75.56421372420085447 ) ) ;
#43075=CIRCLE ( 'NONE', #24579, 1.999999999999997335 ) ;
#43077=EDGE_CURVE ( 'NONE', #998, #11471, #36912, .T. ) ;
#43078=CARTESIAN_POINT ( 'NONE',  ( 59.34570819444679302, -28.11291636370129865, -15.68025305306860062 ) ) ;
#43082=CARTESIAN_POINT ( 'NONE',  ( 47.30620416954869967, -54.71667077003900204, -74.17398805956220542 ) ) ;
#43083=DIRECTION ( 'NONE',  ( -1.000000000000000000, 0.000000000000000000, 0.000000000000000000 ) ) ;
#43085=CARTESIAN_POINT ( 'NONE',  ( 14.94606681672440018, 21.73127465433789851, -76.14999999999999147 ) ) ;
#43086=CARTESIAN_POINT ( 'NONE',  ( 83.16755290732228900, -45.00330858143559709, -46.93255211562899376 ) ) ;
#43087=CARTESIAN_POINT ( 'NONE',  ( 58.78347454168720532, 13.88381119830360078, -25.62280592735929829 ) ) ;
#43090=CYLINDRICAL_SURFACE ( 'NONE', #7159, 1.999999999999997780 ) ;
#43092=CARTESIAN_POINT ( 'NONE',  ( 3.173549631555339978, -55.55485688747910444, -8.896876761822769097 ) ) ;
#43093=CARTESIAN_POINT ( 'NONE',  ( 75.04668702423900584, -14.04868477427920048, -11.30405884009489981 ) ) ;
#43094=CARTESIAN_POINT ( 'NONE',  ( 75.43567969634317194, 12.70586975596460277, -13.55812906738603019 ) ) ;
#43095=EDGE_CURVE ( 'NONE', #8693, #998, #50818, .T. ) ;
#43096=CARTESIAN_POINT ( 'NONE',  ( 61.13058997637050851, -45.49867003083084427, -47.51052979104920837 ) ) ;
#43099=CARTESIAN_POINT ( 'NONE',  ( 82.53029411324719433, -45.52163144278929963, -47.58593199419160413 ) ) ;
#43100=CARTESIAN_POINT ( 'NONE',  ( 57.38208912676239493, -50.61190356253609934, -53.76446502280590067 ) ) ;
#43101=CARTESIAN_POINT ( 'NONE',  ( 40.47914112739019998, 13.57210277531459930, -4.470311448230490647 ) ) ;
#43103=FACE_OUTER_BOUND ( 'NONE', #46759, .T. ) ;
#43104=CARTESIAN_POINT ( 'NONE',  ( 58.64232589198999790, -46.61555239613360158, -47.49232833693479705 ) ) ;
#43105=B_SPLINE_CURVE_WITH_KNOTS ( 'NONE', 3,
 ( #48991, #45043, #9143, #37180, #1277, #20147, #31929, #47950, #12052, #28004, #44010, #45561, #45822, #22202, #21941, #30061, #37953, #9658, #38211, #18030, #50273, #46091 ),
 .UNSPECIFIED., .F., .F.,
 ( 4, 2, 1, 1, 1, 2, 2, 2, 2, 1, 1, 1, 2, 4 ),
 ( 0.000000000000000000, 0.1189054937112668242, 0.1783582405669016657, 0.2080846139947190865, 0.2229478007086256597, 0.2303793940655803063, 0.2378109874225349807, 0.3567164811337855679, 0.4161692279894141366, 0.4458956014172286708, 0.4607587881311373534, 0.4681903814880929438, 0.4719061781665709332, 0.4756219748450489226 ),
 .UNSPECIFIED. ) ;
#43107=FACE_OUTER_BOUND ( 'NONE', #20024, .T. ) ;
#43108=CARTESIAN_POINT ( 'NONE',  ( 17.79388969624029926, -51.62356816798740056, -75.48775473117470369 ) ) ;
#43109=CARTESIAN_POINT ( 'NONE',  ( 41.23501660619890430, -45.11618894467940066, -6.199054889248789557 ) ) ;
#43113=CARTESIAN_POINT ( 'NONE',  ( 8.951553309972659633, 31.89301264151889725, -46.63485964089979774 ) ) ;
#43117=EDGE_CURVE ( 'NONE', #9275, #29825, #41565, .T. ) ;
#43119=CARTESIAN_POINT ( 'NONE',  ( 44.12335005272829846, -45.59245195477699752, -7.915725708897361379 ) ) ;
#43121=CARTESIAN_POINT ( 'NONE',  ( 17.57188048229909683, 20.96156756881190120, -75.93682688742939035 ) ) ;
#43123=EDGE_LOOP ( 'NONE', ( #44910, #18991, #15349 ) ) ;
#43131=ORIENTED_EDGE ( 'NONE', *, *, #12013, .F. ) ;
#43133=CIRCLE ( 'NONE', #37277, 1.999999999999999778 ) ;
#43136=ORIENTED_EDGE ( 'NONE', *, *, #13611, .F. ) ;
#43139=CARTESIAN_POINT ( 'NONE',  ( 51.41399413552429820, -50.55426312863379934, -76.23672004883859188 ) ) ;
#43140=CARTESIAN_POINT ( 'NONE',  ( 61.04997942697320212, 14.17778449832839982, -47.26479615961609682 ) ) ;
#43143=CARTESIAN_POINT ( 'NONE',  ( -4.878462934014000218, 16.25210934087710157, -5.225023538751180752 ) ) ;
#43144=CARTESIAN_POINT ( 'NONE',  ( 46.38667134030966110, 21.75602058146941076, -76.14873014702969556 ) ) ;
#43148=CARTESIAN_POINT ( 'NONE',  ( 56.76664445297700468, -50.67471734267000016, -53.84360320736509919 ) ) ;
#43149=CARTESIAN_POINT ( 'NONE',  ( 57.47269723223679705, 19.35962728544430078, -53.60395066395300034 ) ) ;
#43154=CARTESIAN_POINT ( 'NONE',  ( 15.45245043279679997, 19.57241326031720163, -20.50565891244509942 ) ) ;
#43158=CARTESIAN_POINT ( 'NONE',  ( 48.50471607674010244, -54.16716192014190057, -55.31622937648399585 ) ) ;
#43160=CARTESIAN_POINT ( 'NONE',  ( -29.90025726814942431, -36.14282418732561553, -56.90830752171230245 ) ) ;
#43162=CARTESIAN_POINT ( 'NONE',  ( 47.90440150906960071, 23.11714053132569902, -54.72371951289599679 ) ) ;
#43167=CARTESIAN_POINT ( 'NONE',  ( 60.59785292327919848, -45.59099699431040165, -47.16459466356160135 ) ) ;
#43168=CARTESIAN_POINT ( 'NONE',  ( 48.61347624589590311, -53.95572845601323309, -54.54157758230553554 ) ) ;
#43169=CARTESIAN_POINT ( 'NONE',  ( 83.09574697852120551, 13.66248986189807901, -46.39646041021766365 ) ) ;
#43170=CARTESIAN_POINT ( 'NONE',  ( 83.49396592876078671, 14.01990206489290003, -47.52773119087509457 ) ) ;
#43171=DIRECTION ( 'NONE',  ( -1.000000000000000000, 0.000000000000000000, 0.000000000000000000 ) ) ;
#43173=CARTESIAN_POINT ( 'NONE',  ( -5.066062602303800233, -15.61618894467930119, -11.54999999999999893 ) ) ;
#43180=LINE ( 'NONE', #20077, #28604 ) ;
#43181=CARTESIAN_POINT ( 'NONE',  ( 56.55522360613520760, 14.97957722649010037, -26.26695323647559732 ) ) ;
#43183=CARTESIAN_POINT ( 'NONE',  ( 9.409749845209210761, -63.48355100517809291, -46.51068098438339860 ) ) ;
#43187=AXIS2_PLACEMENT_3D ( 'NONE', #15247, #31198, #47228 ) ;
#43188=CARTESIAN_POINT ( 'NONE',  ( 56.67708563387860465, -45.29633254537559850, -25.29391797581589785 ) ) ;
#43189=CARTESIAN_POINT ( 'NONE',  ( 56.41160612050880019, -50.71163893462430394, -53.28620048350840221 ) ) ;
#43191=CARTESIAN_POINT ( 'NONE',  ( 59.09559851695989607, -2.441367974390179718, -15.68447099303350178 ) ) ;
#43192=CARTESIAN_POINT ( 'NONE',  ( 51.91394866954649956, -49.47671654292729926, -77.01723411093288973 ) ) ;
#43195=ORIENTED_EDGE ( 'NONE', *, *, #22695, .T. ) ;
#43196=B_SPLINE_CURVE_WITH_KNOTS ( 'NONE', 3,
 ( #2337, #18311, #13877, #5756, #2083, #13371, #1563, #37726, #46384, #49785, #41392, #21714, #25135, #50039, #5508, #29837 ),
 .UNSPECIFIED., .F., .F.,
 ( 4, 2, 2, 2, 2, 2, 2, 4 ),
 ( 0.000000000000000000, 0.2171919328280763339, 0.4113453696724681530, 0.5484604928966247961, 0.6170180545087031732, 0.7267101530880277771, 0.9022175108149470546, 1.000000000000000000 ),
 .UNSPECIFIED. ) ;
#43204=B_SPLINE_CURVE_WITH_KNOTS ( 'NONE', 3,
 ( #38395, #14030, #1975, #38922, #50196, #3014, #10102, #34447, #14806, #25793, #50963, #34966, #46793, #30255, #2494, #26848 ),
 .UNSPECIFIED., .F., .F.,
 ( 4, 2, 2, 2, 2, 2, 2, 4 ),
 ( 12.41746251024190073, 14.15001006772948955, 23.85327782795553730, 28.70491170806860382, 32.58621881215907479, 36.46752591624945694, 42.67761728279422329, 46.65082938388610501 ),
 .UNSPECIFIED. ) ;
#43206=CARTESIAN_POINT ( 'NONE',  ( 13.02865871864519853, -50.32049581721639697, -21.18330777480309735 ) ) ;
#43208=CARTESIAN_POINT ( 'NONE',  ( 56.54446371377569847, 13.89738154011810067, -15.75405245971630031 ) ) ;
#43209=CARTESIAN_POINT ( 'NONE',  ( 61.05628860138500613, -45.35080969805910200, -46.88525996552779418 ) ) ;
#43210=CARTESIAN_POINT ( 'NONE',  ( 56.45963719500250022, -50.66310011266489255, -53.16982888481129521 ) ) ;
#43214=CARTESIAN_POINT ( 'NONE',  ( 14.35463486013270007, -51.14554741935889837, -74.54427505470819426 ) ) ;
#43221=CARTESIAN_POINT ( 'NONE',  ( 10.81643727139639921, -64.95351341576260040, -17.63284883035869655 ) ) ;
#43223=CARTESIAN_POINT ( 'NONE',  ( 82.13853704237929776, 14.30143299382709898, -47.59887875144359981 ) ) ;
#43226=CARTESIAN_POINT ( 'NONE',  ( 11.50961124680121728, 33.46337070016348747, -23.96126768911706861 ) ) ;
#43228=CARTESIAN_POINT ( 'NONE',  ( 49.48559182206740559, 22.51696836342139818, -55.18124709514480486 ) ) ;
#43229=EDGE_LOOP ( 'NONE', ( #11091, #40397, #13273, #12633 ) ) ;
#43230=CARTESIAN_POINT ( 'NONE',  ( 52.80437713202650230, -49.69361475838819331, -48.85649632429790046 ) ) ;
#43233=CIRCLE ( 'NONE', #524, 16.33504667647529729 ) ;
#43234=DIRECTION ( 'NONE',  ( 0.05355673475992397264, -0.9985648081931662867, 0.000000000000000000 ) ) ;
#43235=CARTESIAN_POINT ( 'NONE',  ( 14.13996207071689959, 19.81020116829009936, -21.96868406873839774 ) ) ;
#43236=CARTESIAN_POINT ( 'NONE',  ( 51.85719039531000618, -49.29163377067489904, -77.06876493040969933 ) ) ;
#43239=CARTESIAN_POINT ( 'NONE',  ( 52.72599990135299919, 18.50994649268380243, -48.79685834802910449 ) ) ;
#43240=CARTESIAN_POINT ( 'NONE',  ( 55.76563889033010213, -45.58887186001610559, -16.42694171794889968 ) ) ;
#43241=CARTESIAN_POINT ( 'NONE',  ( 55.63848436370909667, 15.03490499964270022, -25.39977966304109813 ) ) ;
#43243=EDGE_CURVE ( 'NONE', #22490, #28125, #1321, .T. ) ;
#43244=ORIENTED_EDGE ( 'NONE', *, *, #2728, .F. ) ;
#43247=ORIENTED_EDGE ( 'NONE', *, *, #40678, .T. ) ;
#43249=CARTESIAN_POINT ( 'NONE',  ( 11.51020352941140068, -65.19111653312340593, -17.03655004557180064 ) ) ;
#43250=CARTESIAN_POINT ( 'NONE',  ( 11.55432588269150074, 33.99546521010679356, -47.20121379407340356 ) ) ;
#43253=DIRECTION ( 'NONE',  ( 0.8090169943749478954, 0.5877852522924724710, 0.000000000000000000 ) ) ;
#43254=CARTESIAN_POINT ( 'NONE',  ( 0.5716597375277996385, -15.61618894467929941, -6.649999999999999467 ) ) ;
#43255=CARTESIAN_POINT ( 'NONE',  ( 51.19787128922300212, -52.90300504561889738, -54.04781962224119951 ) ) ;
#43256=ORIENTED_EDGE ( 'NONE', *, *, #10774, .T. ) ;
#43257=DIRECTION ( 'NONE',  ( 0.000000000000000000, 0.000000000000000000, -1.000000000000000000 ) ) ;
#43258=CARTESIAN_POINT ( 'NONE',  ( 10.14147138814020010, -63.21765883073391024, -45.99379265408919792 ) ) ;
#43260=ORIENTED_EDGE ( 'NONE', *, *, #42774, .T. ) ;
#43261=CARTESIAN_POINT ( 'NONE',  ( 68.38970072013677282, -30.34057458802632823, -18.15384971058606922 ) ) ;
#43262=CARTESIAN_POINT ( 'NONE',  ( 56.91872540556310156, 19.41123227373739724, -53.86107397134590258 ) ) ;
#43265=CARTESIAN_POINT ( 'NONE',  ( 52.20740535868762322, 20.17246182719578584, -75.93239680710105688 ) ) ;
#43267=CARTESIAN_POINT ( 'NONE',  ( 57.32828653034319899, -50.41406207962300812, -53.00038473087199975 ) ) ;
#43270=CARTESIAN_POINT ( 'NONE',  ( 63.02123093760216221, 0.4193442080440759612, -17.11446765124405900 ) ) ;
#43273=ORIENTED_EDGE ( 'NONE', *, *, #15367, .F. ) ;
#43274=ORIENTED_EDGE ( 'NONE', *, *, #18506, .F. ) ;
#43278=CARTESIAN_POINT ( 'NONE',  ( 50.77828552747439517, -50.74762180099740050, -76.14999999999999147 ) ) ;
#43280=CARTESIAN_POINT ( 'NONE',  ( 46.76524959757980326, 22.46046862905859598, -75.96071349691810326 ) ) ;
#43281=CARTESIAN_POINT ( 'NONE',  ( 50.03007040746459921, 17.38381105532069881, -78.14999999999999147 ) ) ;
#43283=CARTESIAN_POINT ( 'NONE',  ( 42.39660149645209941, -44.97461146731200898, -5.990492802273720940 ) ) ;
#43284=CARTESIAN_POINT ( 'NONE',  ( 12.00693377043790022, 33.56613978031089118, -16.09314495738659900 ) ) ;
#43286=CARTESIAN_POINT ( 'NONE',  ( 55.91596500572619277, -45.90464019914170279, -25.32542830939949852 ) ) ;
#43288=CARTESIAN_POINT ( 'NONE',  ( 55.34927123575489816, -50.61618894660580281, -76.48225957491609961 ) ) ;
#43289=CARTESIAN_POINT ( 'NONE',  ( -6.318914795328239187, 14.68237235522740036, -4.813384506477039970 ) ) ;
#43292=DIRECTION ( 'NONE',  ( -0.8320502943378438321, 0.000000000000000000, 0.5547001962252288143 ) ) ;
#43293=ORIENTED_EDGE ( 'NONE', *, *, #8678, .F. ) ;
#43294=DIRECTION ( 'NONE',  ( -0.9200120562340502461, 0.3918900565005380976, 0.000000000000000000 ) ) ;
#43295=CARTESIAN_POINT ( 'NONE',  ( 47.74202631360270033, 23.20359536699950098, -54.70726247055279856 ) ) ;
#43296=CARTESIAN_POINT ( 'NONE',  ( 60.02121333775870227, -45.19777382224889806, -26.54063133662459961 ) ) ;
#43297=CARTESIAN_POINT ( 'NONE',  ( 16.15069521921704165, -51.05177107958204630, -15.66900421577824254 ) ) ;
#43298=CARTESIAN_POINT ( 'NONE',  ( 13.22845487704439904, 19.37063177541839920, -21.36464768999449859 ) ) ;
#43299=CARTESIAN_POINT ( 'NONE',  ( 61.02913797987469735, 14.29490916149900137, -47.53473330658249552 ) ) ;
#43301=CARTESIAN_POINT ( 'NONE',  ( 51.29313473418520175, 18.26623787800760113, -76.46030551589480240 ) ) ;
#43302=CARTESIAN_POINT ( 'NONE',  ( 52.96420269150630844, 18.35810234167090016, -48.77461993677670193 ) ) ;
#43305=CARTESIAN_POINT ( 'NONE',  ( 50.11664719554170944, 5.483622036391903265, -76.15000000000003411 ) ) ;
#43309=CARTESIAN_POINT ( 'NONE',  ( 64.35623192390551139, -32.08291323696330011, -17.59133921123940070 ) ) ;
#43314=CARTESIAN_POINT ( 'NONE',  ( 61.12526931739070335, -45.25414475714967466, -27.63398140488572352 ) ) ;
#43315=VERTEX_POINT ( 'NONE', #42924 ) ;
#43316=ORIENTED_EDGE ( 'NONE', *, *, #50815, .F. ) ;
#43318=CARTESIAN_POINT ( 'NONE',  ( 49.91571640700792756, -29.72640275947340172, -15.91623881425632447 ) ) ;
#43320=CARTESIAN_POINT ( 'NONE',  ( 56.23014233047970123, -45.81748423697870010, -25.89964805919260016 ) ) ;
#43322=LINE ( 'NONE', #18424, #28132 ) ;
#43324=CARTESIAN_POINT ( 'NONE',  ( 16.13393739769620083, -15.61618894467929941, -5.740514720465080600 ) ) ;
#43326=CARTESIAN_POINT ( 'NONE',  ( 41.99203386431830154, -44.88537213046480190, -5.712673480947970006 ) ) ;
#43329=CARTESIAN_POINT ( 'NONE',  ( 50.44516630538529967, -45.11618894467940066, -10.60027150187420020 ) ) ;
#43330=CARTESIAN_POINT ( 'NONE',  ( 51.88785155891503109, 1.541422455399617419, -18.83071984855998338 ) ) ;
#43332=EDGE_CURVE ( 'NONE', #29113, #3072, #17371, .T. ) ;
#43333=CARTESIAN_POINT ( 'NONE',  ( 60.21673368439580543, -28.82193623653779824, -15.80468577411680009 ) ) ;
#43335=CARTESIAN_POINT ( 'NONE',  ( 47.30620416954869967, -54.71667077003900204, -74.14999999999999147 ) ) ;
#43338=CARTESIAN_POINT ( 'NONE',  ( 43.92206853057700044, 14.74641057201809957, -8.176270959481939826 ) ) ;
#43340=DIRECTION ( 'NONE',  ( -1.000000000000000000, 0.000000000000000000, 0.000000000000000000 ) ) ;
#43341=CARTESIAN_POINT ( 'NONE',  ( 84.17895764879889953, -44.08298806148399507, -47.20739533566359825 ) ) ;
#43343=CARTESIAN_POINT ( 'NONE',  ( 57.48924594623639450, 13.88381125482189837, -25.32904884043690075 ) ) ;
#43345=VERTEX_POINT ( 'NONE', #51552 ) ;
#43346=DIRECTION ( 'NONE',  ( 0.000000000000000000, -0.7071067811865492381, -0.7071067811865457964 ) ) ;
#43347=CARTESIAN_POINT ( 'NONE',  ( 6.660026050685900145, -59.99599272703940045, -12.48570139134749901 ) ) ;
#43348=CARTESIAN_POINT ( 'NONE',  ( 76.33997785262350533, -14.06269230294210004, -12.53642027154039873 ) ) ;
#43349=CIRCLE ( 'NONE', #2335, 28.31678667024650409 ) ;
#43350=CARTESIAN_POINT ( 'NONE',  ( 75.29505756514645043, 13.38913129781163391, -14.04565979207876936 ) ) ;
#43354=CARTESIAN_POINT ( 'NONE',  ( 7.492845759203720313, 29.94784237631284896, -20.13893727953968948 ) ) ;
#43355=CARTESIAN_POINT ( 'NONE',  ( 82.71798245299019925, -45.49268626692509798, -47.55440761962790219 ) ) ;
#43356=CARTESIAN_POINT ( 'NONE',  ( 57.39790738242900403, -50.56072618960909892, -53.44821462976450732 ) ) ;
#43357=CARTESIAN_POINT ( 'NONE',  ( 42.42327895389549752, 12.56836077726920031, -4.706996716866660435 ) ) ;
#43360=CARTESIAN_POINT ( 'NONE',  ( 16.13393739769620083, -15.61618894467929941, 5.856814007409659517 ) ) ;
#43361=CARTESIAN_POINT ( 'NONE',  ( 70.83393739769717001, -48.11618894467422081, -70.54999999999975557 ) ) ;
#43362=EDGE_CURVE ( 'NONE', #39834, #30210, #11508, .T. ) ;
#43363=CARTESIAN_POINT ( 'NONE',  ( 66.98669698734040878, -1.154848256152869901, -17.21849850612139576 ) ) ;
#43364=CARTESIAN_POINT ( 'NONE',  ( 17.73938417335649831, -51.76348103900169662, -75.62474771911479365 ) ) ;
#43365=CARTESIAN_POINT ( 'NONE',  ( 53.57599294125679990, -43.78057387862440208, -7.454646995071700033 ) ) ;
#43370=CARTESIAN_POINT ( 'NONE',  ( 59.49262858449159808, 17.38381105532069881, -53.92796738110899923 ) ) ;
#43376=CARTESIAN_POINT ( 'NONE',  ( 17.79805963255870083, 20.61263520652270032, -75.69337827730609547 ) ) ;
#43378=VERTEX_POINT ( 'NONE', #38994 ) ;
#43385=ORIENTED_EDGE ( 'NONE', *, *, #16968, .F. ) ;
#43386=FACE_OUTER_BOUND ( 'NONE', #38564, .T. ) ;
#43388=CARTESIAN_POINT ( 'NONE',  ( 10.47406283454438203, -63.11543068638779630, -45.62066736167659542 ) ) ;
#43391=CARTESIAN_POINT ( 'NONE',  ( 51.02815224764380275, -50.88300054698879649, -76.14999943445839392 ) ) ;
#43392=CARTESIAN_POINT ( 'NONE',  ( 60.96828345175140385, 14.29541988433120103, -47.49580120907970127 ) ) ;
#43394=CARTESIAN_POINT ( 'NONE',  ( 40.53658481618179366, -44.74595000644689691, -4.211756420469699336 ) ) ;
#43395=CARTESIAN_POINT ( 'NONE',  ( -10.89069801029419970, 11.10586477277349893, -6.229949705787969805 ) ) ;
#43396=CARTESIAN_POINT ( 'NONE',  ( 47.11356721804862246, 23.41744796771036263, -74.95177798119966894 ) ) ;
#43401=CARTESIAN_POINT ( 'NONE',  ( 44.39988805235839919, 14.85962372618369898, -8.567279085052819099 ) ) ;
#43404=CARTESIAN_POINT ( 'NONE',  ( 13.75381683890269890, 19.05415068650080102, -20.97887788433579814 ) ) ;
#43406=CARTESIAN_POINT ( 'NONE',  ( 12.69621343537160207, 18.74918025219870188, -21.09935757674490020 ) ) ;
#43409=CARTESIAN_POINT ( 'NONE',  ( 48.80641172512370218, -53.96751462272040101, -54.78053361341569882 ) ) ;
#43414=CARTESIAN_POINT ( 'NONE',  ( 47.77489297752619990, 23.22910854708220185, -54.94508266598730017 ) ) ;
#43418=EDGE_CURVE ( 'NONE', #38586, #20094, #2774, .T. ) ;
#43421=CARTESIAN_POINT ( 'NONE',  ( 60.47410467199969730, -45.68409708816510317, -47.42171235821720643 ) ) ;
#43422=CARTESIAN_POINT ( 'NONE',  ( 58.64232589199010448, -46.61555239613360158, -47.49232833693479705 ) ) ;
#43423=CARTESIAN_POINT ( 'NONE',  ( 10.47406283454438203, 8.337936262032100032, -45.62066736167659542 ) ) ;
#43424=CARTESIAN_POINT ( 'NONE',  ( 83.07525583555450055, 14.27202569750270023, -47.60489434516649965 ) ) ;
#43428=CARTESIAN_POINT ( 'NONE',  ( 68.13393739769620083, -43.11618894467930119, -65.65000000000000568 ) ) ;
#43431=VERTEX_POINT ( 'NONE', #44714 ) ;
#43434=CARTESIAN_POINT ( 'NONE',  ( 76.50875310644418903, -28.83273956145659156, -13.26513667399496832 ) ) ;
#43435=CARTESIAN_POINT ( 'NONE',  ( 11.75059328717480156, -65.32411396726729436, -47.38109070371250908 ) ) ;
#43436=EDGE_CURVE ( 'NONE', #36534, #41357, #40784, .T. ) ;
#43441=CARTESIAN_POINT ( 'NONE',  ( 56.47485811939319689, -50.74143557146020100, -53.50470819900189667 ) ) ;
#43443=CARTESIAN_POINT ( 'NONE',  ( 61.39813329574750611, -1.033231316043849768, -16.14322717339910085 ) ) ;
#43445=CARTESIAN_POINT ( 'NONE',  ( 51.68229834213279617, -48.76553687035409723, -77.01558403215359760 ) ) ;
#43446=LINE ( 'NONE', #20800, #13729 ) ;
#43447=ORIENTED_EDGE ( 'NONE', *, *, #18905, .T. ) ;
#43451=VECTOR ( 'NONE', #33580, 1000.000000000000000 ) ;
#43453=CARTESIAN_POINT ( 'NONE',  ( 13.61751436023210005, -50.16766667186070094, -20.94898426184690265 ) ) ;
#43454=CARTESIAN_POINT ( 'NONE',  ( 55.38096894651479829, 19.39060553094100214, -76.22684432684179967 ) ) ;
#43456=CARTESIAN_POINT ( 'NONE',  ( 56.36309497301279947, 13.88381105532070059, -15.20458750986569996 ) ) ;
#43457=CARTESIAN_POINT ( 'NONE',  ( 61.01756443532780594, -45.37431638178470195, -47.00084460110949891 ) ) ;
#43458=CARTESIAN_POINT ( 'NONE',  ( 47.64143405402000297, -54.53488714544439375, -55.14905519569939685 ) ) ;
#43459=EDGE_CURVE ( 'NONE', #13362, #21835, #47789, .T. ) ;
#43462=ORIENTED_EDGE ( 'NONE', *, *, #18905, .F. ) ;
#43463=CARTESIAN_POINT ( 'NONE',  ( 46.40621397470390264, 21.74426214990070250, -76.14873014702980925 ) ) ;
#43466=CARTESIAN_POINT ( 'NONE',  ( 86.75761129539397132, 18.79802461769378397, -60.02031173921621132 ) ) ;
#43468=CARTESIAN_POINT ( 'NONE',  ( 83.89200044194980421, 18.85811933572209753, -52.57651812407429759 ) ) ;
#43470=CARTESIAN_POINT ( 'NONE',  ( 10.97864148259309935, 33.91456773539839986, -18.17421237882080476 ) ) ;
#43471=DIRECTION ( 'NONE',  ( -0.9200120562340476926, -0.3918900565005438708, 0.000000000000000000 ) ) ;
#43472=CARTESIAN_POINT ( 'NONE',  ( 63.02123093760216221, 0.4193442080440759612, -17.11446765124405900 ) ) ;
#43475=CARTESIAN_POINT ( 'NONE',  ( 49.22498099147649953, 22.62797864033339934, -55.23666898610220244 ) ) ;
#43477=EDGE_CURVE ( 'NONE', #39182, #814, #23988, .T. ) ;
#43479=CARTESIAN_POINT ( 'NONE',  ( 52.60258585013299637, -49.82394164341149434, -48.51135465991440299 ) ) ;
#43483=CARTESIAN_POINT ( 'NONE',  ( 14.55219274796575313, 20.46959765477225091, -75.56421372419544014 ) ) ;
#43484=CARTESIAN_POINT ( 'NONE',  ( 8.133937397696209715, -54.80802482921019703, -21.14999999999999858 ) ) ;
#43485=CARTESIAN_POINT ( 'NONE',  ( 51.67587649748560352, -48.69064075877850684, -77.01363636363639387 ) ) ;
#43488=VECTOR ( 'NONE', #37679, 1000.000000000000000 ) ;
#43491=CARTESIAN_POINT ( 'NONE',  ( 56.63382897851940356, -45.18506093673340018, -16.44084196791180119 ) ) ;
#43492=CARTESIAN_POINT ( 'NONE',  ( 55.85841962760110135, 14.74773305113219912, -25.34033445086470238 ) ) ;
#43493=EDGE_LOOP ( 'NONE', ( #16962, #21965, #20802, #5929 ) ) ;
#43497=CARTESIAN_POINT ( 'NONE',  ( 11.61081910261030004, -65.23863181566240144, -17.07039304614280084 ) ) ;
#43498=CARTESIAN_POINT ( 'NONE',  ( 11.02897443665469979, 33.86259216482670098, -47.16934780673829408 ) ) ;
#43501=CARTESIAN_POINT ( 'NONE',  ( 11.54127901367117914, -65.34045536701110279, -22.61052249223064692 ) ) ;
#43505=CARTESIAN_POINT ( 'NONE',  ( 10.97782631398749942, -63.13468953106429638, -44.74264417585560238 ) ) ;
#43506=CARTESIAN_POINT ( 'NONE',  ( 66.23540447448930024, 18.72622661238430553, -73.39853292320987066 ) ) ;
#43507=ORIENTED_EDGE ( 'NONE', *, *, #4296, .F. ) ;
#43509=CARTESIAN_POINT ( 'NONE',  ( 56.68249757595900462, 19.21262946785479997, -52.87688493478909635 ) ) ;
#43513=PLANE ( 'NONE',  #32548 ) ;
#43524=VECTOR ( 'NONE', #35839, 1000.000000000000114 ) ;
#43526=AXIS2_PLACEMENT_3D ( 'NONE', #24498, #20579, #3595 ) ;
#43527=EDGE_CURVE ( 'NONE', #22043, #10696, #4616, .T. ) ;
#43530=EDGE_CURVE ( 'NONE', #45901, #24962, #12800, .T. ) ;
#43531=CARTESIAN_POINT ( 'NONE',  ( 47.15820541288359635, 23.35149450075520150, -75.00623917109859917 ) ) ;
#43532=CIRCLE ( 'NONE', #20914, 15.56227766016840164 ) ;
#43534=ADVANCED_FACE ( 'NONE', ( #17714 ), #36584, .T. ) ;
#43536=CARTESIAN_POINT ( 'NONE',  ( 11.76101335023730066, 33.66270366472770803, -16.31614116035649786 ) ) ;
#43539=CARTESIAN_POINT ( 'NONE',  ( 55.05482395368899518, -50.61618894681969749, -76.63544833123130218 ) ) ;
#43540=CARTESIAN_POINT ( 'NONE',  ( -9.688667659886910144, 11.02459018896860066, -4.264896373567980348 ) ) ;
#43541=CARTESIAN_POINT ( 'NONE',  ( 11.13393739769620616, -55.30245861064820190, -44.08754233725599647 ) ) ;
#43543=CARTESIAN_POINT ( 'NONE',  ( 61.39882506316129707, 13.96060197418889892, -46.69637642908890030 ) ) ;
#43547=CARTESIAN_POINT ( 'NONE',  ( 52.79375803185560301, -49.68041131509039587, -48.48716100244389793 ) ) ;
#43548=CARTESIAN_POINT ( 'NONE',  ( 47.74808848842369713, 23.19578408484800036, -54.68947420106290025 ) ) ;
#43551=CARTESIAN_POINT ( 'NONE',  ( 61.48324830189730505, 14.13192806243720057, -47.33702467829240135 ) ) ;
#43553=CARTESIAN_POINT ( 'NONE',  ( 51.79788809998749599, 18.93511776858189677, -76.50613236165939668 ) ) ;
#43554=CARTESIAN_POINT ( 'NONE',  ( 52.76444409924949497, 18.46836548807459977, -48.64233343848459867 ) ) ;
#43556=DIRECTION ( 'NONE',  ( 1.000000000000000000, 0.000000000000000000, 0.000000000000000000 ) ) ;
#43557=CARTESIAN_POINT ( 'NONE',  ( 52.84731369148330060, -49.65172165314799457, -48.60966827451719752 ) ) ;
#43560=CARTESIAN_POINT ( 'NONE',  ( 47.66631869268250199, -54.51824591515769924, -54.99485691796319742 ) ) ;
#43561=CYLINDRICAL_SURFACE ( 'NONE', #5273, 1.999999999999997113 ) ;
#43563=CARTESIAN_POINT ( 'NONE',  ( 65.05499895842218905, -32.25244862226109888, -17.84090853625750128 ) ) ;
#43568=LINE ( 'NONE', #7668, #30969 ) ;
#43569=CARTESIAN_POINT ( 'NONE',  ( 59.52869410915831594, -45.48984219772450643, -26.73579121603098585 ) ) ;
#43570=VERTEX_POINT ( 'NONE', #9600 ) ;
#43574=VERTEX_POINT ( 'NONE', #1731 ) ;
#43575=CARTESIAN_POINT ( 'NONE',  ( 16.13393739769620083, -15.61618894467929941, 6.072546842075589701 ) ) ;
#43578=CARTESIAN_POINT ( 'NONE',  ( 10.98127921298129728, 33.58944323623821049, -23.21470234273132149 ) ) ;
#43580=CARTESIAN_POINT ( 'NONE',  ( 13.02068638423840063, 34.28679101843700039, -23.33284745141469685 ) ) ;
#43586=CARTESIAN_POINT ( 'NONE',  ( 62.40084614537109786, -29.97498645692460073, -16.17177386113289828 ) ) ;
#43587=CARTESIAN_POINT ( 'NONE',  ( 14.34417029198830029, 19.88381105532299742, -74.14999999999999147 ) ) ;
#43588=CARTESIAN_POINT ( 'NONE',  ( 47.07018870238729846, -54.05275391524939721, -75.65465545553870186 ) ) ;
#43590=CARTESIAN_POINT ( 'NONE',  ( 54.67236884565690502, 14.97126989199350078, -15.88466681443639850 ) ) ;
#43591=CARTESIAN_POINT ( 'NONE',  ( 42.10987924529349868, 14.38172689610610000, -6.748859080943129918 ) ) ;
#43593=CARTESIAN_POINT ( 'NONE',  ( 14.98932716411379928, 21.70054973260339892, -76.14999999999999147 ) ) ;
#43594=EDGE_CURVE ( 'NONE', #49564, #48985, #48430, .T. ) ;
#43595=VECTOR ( 'NONE', #15252, 1000.000000000000114 ) ;
#43597=CARTESIAN_POINT ( 'NONE',  ( 84.38939444912799104, -43.48290221131350108, -47.32729711157580255 ) ) ;
#43598=CARTESIAN_POINT ( 'NONE',  ( 65.36617461242161653, -30.59625171506405295, -16.64867345289078671 ) ) ;
#43601=CARTESIAN_POINT ( 'NONE',  ( 54.75372257292519862, -47.88473616892759566, -26.64369953896449772 ) ) ;
#43602=CARTESIAN_POINT ( 'NONE',  ( 14.70125025179870093, -50.53285427156319543, -20.74420046562639897 ) ) ;
#43603=CARTESIAN_POINT ( 'NONE',  ( 75.70738177086290932, 12.17974452044730072, -13.47559339050390115 ) ) ;
#43604=B_SPLINE_CURVE_WITH_KNOTS ( 'NONE', 3,
 ( #49405, #29458, #4575, #48881, #45463, #12986, #20547, #9561, #36542, #28936 ),
 .UNSPECIFIED., .F., .F.,
 ( 4, 2, 2, 2, 4 ),
 ( 0.000000000000000000, 0.2643499294688712031, 0.4734939176322996990, 0.8917818939591528604, 1.000000000000000000 ),
 .UNSPECIFIED. ) ;
#43605=CARTESIAN_POINT ( 'NONE',  ( 75.45398146315633880, 12.53648618435466133, -13.49434368755179747 ) ) ;
#43606=DIRECTION ( 'NONE',  ( 0.000000000000000000, 0.000000000000000000, -1.000000000000000000 ) ) ;
#43608=CARTESIAN_POINT ( 'NONE',  ( -8.352801854373527846, -44.78526516041389982, -5.739504211299600200 ) ) ;
#43612=CARTESIAN_POINT ( 'NONE',  ( 57.33945454586879720, -50.32221370019689743, -52.87108245925089989 ) ) ;
#43613=CARTESIAN_POINT ( 'NONE',  ( 41.94994391832800318, 12.69230833618010124, -4.524181473528510189 ) ) ;
#43614=CARTESIAN_POINT ( 'NONE',  ( 61.32247977517523907, -45.56437718414176175, -47.63520364883854086 ) ) ;
#43620=CARTESIAN_POINT ( 'NONE',  ( 18.17012112126710122, -52.29987767205400218, -75.77396328158869210 ) ) ;
#43631=ORIENTED_EDGE ( 'NONE', *, *, #47308, .T. ) ;
#43632=CARTESIAN_POINT ( 'NONE',  ( 18.02088350666679872, 20.74698410172580054, -75.72128529899769944 ) ) ;
#43633=ORIENTED_EDGE ( 'NONE', *, *, #48629, .T. ) ;
#43635=FACE_OUTER_BOUND ( 'NONE', #42019, .T. ) ;
#43638=TOROIDAL_SURFACE ( 'NONE', #32704, 18.00000000000000000, 2.000000000000000000 ) ;
#43639=CARTESIAN_POINT ( 'NONE',  ( 61.64525490299610766, 13.96903739949059897, -46.95128602980910415 ) ) ;
#43643=CARTESIAN_POINT ( 'NONE',  ( 16.13393739769579582, -15.61618894467939889, -10.44999999999980034 ) ) ;
#43645=CARTESIAN_POINT ( 'NONE',  ( 83.89200044194980421, -50.61618894467930119, -53.92796738110899923 ) ) ;
#43646=CARTESIAN_POINT ( 'NONE',  ( 16.13393739769620083, -15.61618894467929941, -7.101316701949489385 ) ) ;
#43647=ORIENTED_EDGE ( 'NONE', *, *, #8316, .F. ) ;
#43649=CARTESIAN_POINT ( 'NONE',  ( 52.46419972536169496, -51.19626386910670135, -75.99844944557069937 ) ) ;
#43650=CARTESIAN_POINT ( 'NONE',  ( 60.56461264277469780, 14.52689081580879993, -47.69384697653629956 ) ) ;
#43652=CARTESIAN_POINT ( 'NONE',  ( 11.89321892218980103, 34.20364954172580241, -22.25048313876769868 ) ) ;
#43653=CARTESIAN_POINT ( 'NONE',  ( -9.419262753694910728, 12.55375140257260114, -5.879062740130000186 ) ) ;
#43654=CARTESIAN_POINT ( 'NONE',  ( 46.70834501317497001, 22.49584756229791083, -75.96332490896284639 ) ) ;
#43657=EDGE_LOOP ( 'NONE', ( #34253, #47150, #45362, #13728, #5023 ) ) ;
#43658=CARTESIAN_POINT ( 'NONE',  ( 41.20098873942420425, 14.32627756744839864, -6.156279893315419471 ) ) ;
#43661=CARTESIAN_POINT ( 'NONE',  ( 13.94847430742629868, 19.04672674949359745, -20.89779807318980076 ) ) ;
#43663=VECTOR ( 'NONE', #11420, 1000.000000000000114 ) ;
#43664=CYLINDRICAL_SURFACE ( 'NONE', #15492, 1.999999999999970246 ) ;
#43667=CARTESIAN_POINT ( 'NONE',  ( 48.73678662100309822, -53.88539940205489387, -54.49010856789290358 ) ) ;
#43671=ADVANCED_FACE ( 'NONE', ( #37115 ), #45241, .F. ) ;
#43672=CARTESIAN_POINT ( 'NONE',  ( 47.66548848826279539, 23.29226298427809638, -55.16185052358790131 ) ) ;
#43678=CARTESIAN_POINT ( 'NONE',  ( 60.24866557976200454, -45.78236623157710028, -47.36885438232280165 ) ) ;
#43679=DIRECTION ( 'NONE',  ( 0.000000000000000000, 0.000000000000000000, -1.000000000000000000 ) ) ;
#43680=CARTESIAN_POINT ( 'NONE',  ( 62.09157612670949788, -33.11618894467940066, -65.34607522167520699 ) ) ;
#43682=CARTESIAN_POINT ( 'NONE',  ( 45.07858682377059978, -46.11248607424209922, -9.026855431852869316 ) ) ;
#43683=DIRECTION ( 'NONE',  ( 0.000000000000000000, 0.000000000000000000, -1.000000000000000000 ) ) ;
#43685=ORIENTED_EDGE ( 'NONE', *, *, #12114, .F. ) ;
#43691=CARTESIAN_POINT ( 'NONE',  ( 11.67521959659690012, -65.26890461106869168, -47.24652687432000420 ) ) ;
#43692=VERTEX_POINT ( 'NONE', #17459 ) ;
#43694=CARTESIAN_POINT ( 'NONE',  ( 56.75573796874090249, -45.26196802996069835, -25.29489359144389837 ) ) ;
#43695=CARTESIAN_POINT ( 'NONE',  ( 56.40078553072530099, -50.54434665457389997, -52.89577359589869587 ) ) ;
#43697=CARTESIAN_POINT ( 'NONE',  ( 61.06650679487360378, -1.429311427220590014, -16.00487319935590236 ) ) ;
#43698=CARTESIAN_POINT ( 'NONE',  ( 52.02482082126720542, -49.78138960277850344, -76.90588669317190806 ) ) ;
#43703=CARTESIAN_POINT ( 'NONE',  ( 75.82138965228800487, 12.11553555588150921, -13.50018836794542487 ) ) ;
#43707=CARTESIAN_POINT ( 'NONE',  ( 13.13410622190690091, -50.32702805021810377, -21.17378955277370167 ) ) ;
#43708=CARTESIAN_POINT ( 'NONE',  ( 55.24231505161220213, 19.39098015012699960, -76.29834687610690480 ) ) ;
#43710=PLANE ( 'NONE',  #6713 ) ;
#43711=CARTESIAN_POINT ( 'NONE',  ( 10.72853615272882699, -64.94170179444019197, -18.17421237897245945 ) ) ;
#43712=CARTESIAN_POINT ( 'NONE',  ( 60.80565956584559473, -45.54811607624679937, -47.42904258599709522 ) ) ;
#43720=CARTESIAN_POINT ( 'NONE',  ( 13.63143226142920028, -51.46210362308260500, -74.58518005236030035 ) ) ;
#43723=LINE ( 'NONE', #12019, #18743 ) ;
#43725=CARTESIAN_POINT ( 'NONE',  ( 46.27112185534480204, 13.88381105532070059, -7.639051677656230055 ) ) ;
#43726=CARTESIAN_POINT ( 'NONE',  ( 46.64206449348299799, -53.27165255397410704, -76.10218428122850298 ) ) ;
#43728=DIRECTION ( 'NONE',  ( -0.2517544074889974115, -0.9677911542837451808, 0.000000000000000000 ) ) ;
#43734=CARTESIAN_POINT ( 'NONE',  ( 49.62716556310740401, 22.41720408324059832, -54.74430167493610355 ) ) ;
#43736=CARTESIAN_POINT ( 'NONE',  ( 52.62812534184670454, -49.80011865873639465, -48.49159685222129923 ) ) ;
#43737=ORIENTED_EDGE ( 'NONE', *, *, #945, .F. ) ;
#43741=CARTESIAN_POINT ( 'NONE',  ( 52.15298860272049808, -49.68190537283830110, -77.15976494802958996 ) ) ;
#43744=CARTESIAN_POINT ( 'NONE',  ( 56.71583985100659930, -45.26515517447770520, -17.53022232124200031 ) ) ;
#43746=ORIENTED_EDGE ( 'NONE', *, *, #19457, .T. ) ;
#43748=EDGE_LOOP ( 'NONE', ( #36654, #14029, #3743, #22849, #30383, #25673 ) ) ;
#43749=CARTESIAN_POINT ( 'NONE',  ( 11.99376944390879984, -65.35897423492339442, -17.21195683420090106 ) ) ;
#43750=CARTESIAN_POINT ( 'NONE',  ( 10.06009413933740149, 32.63977898893389806, -46.27041880991490075 ) ) ;
#43752=CARTESIAN_POINT ( 'NONE',  ( 50.70646051152439782, -52.15942487423860285, -52.42739074807799682 ) ) ;
#43753=CARTESIAN_POINT ( 'NONE',  ( 10.97093567021087068, -64.80530225377253828, -23.22645367378097703 ) ) ;
#43754=CYLINDRICAL_SURFACE ( 'NONE', #22479, 2.000000000000000888 ) ;
#43756=ORIENTED_EDGE ( 'NONE', *, *, #2738, .T. ) ;
#43758=CARTESIAN_POINT ( 'NONE',  ( 10.97869545187629825, -63.24704946791390370, -44.74208737706349837 ) ) ;
#43759=CARTESIAN_POINT ( 'NONE',  ( 68.13393739769769297, 18.72622661238600017, -69.60146707679309941 ) ) ;
#43761=CARTESIAN_POINT ( 'NONE',  ( 11.14351459429726177, -63.74727234195290748, -43.82532805256368391 ) ) ;
#43770=DIRECTION ( 'NONE',  ( 0.000000000000000000, 0.000000000000000000, -1.000000000000000000 ) ) ;
#43774=AXIS2_PLACEMENT_3D ( 'NONE', #14468, #2162, #30185 ) ;
#43776=CIRCLE ( 'NONE', #37075, 0.9999999999999991118 ) ;
#43777=CARTESIAN_POINT ( 'NONE',  ( 53.05493175928820193, -49.60024593468599363, -49.10911682558059965 ) ) ;
#43780=ADVANCED_FACE ( 'NONE', ( #28883 ), #45144, .T. ) ;
#43781=CARTESIAN_POINT ( 'NONE',  ( 46.93934609751799769, 22.89847016650290001, -75.65554799883719284 ) ) ;
#43784=CARTESIAN_POINT ( 'NONE',  ( 41.94962124040690554, -44.91063985297350314, -5.752304926970420063 ) ) ;
#43785=CARTESIAN_POINT ( 'NONE',  ( 12.06856799516559953, 33.91524600913400178, -16.61922514010409913 ) ) ;
#43789=CARTESIAN_POINT ( 'NONE',  ( 55.86072899227769994, -50.68028847179019891, -75.53713797333620050 ) ) ;
#43790=CARTESIAN_POINT ( 'NONE',  ( 0.3088433006440429729, 21.43104923585109844, -7.323220502269159660 ) ) ;
#43793=CARTESIAN_POINT ( 'NONE',  ( 61.22799349397990198, 14.06250502558359905, -47.02344481981909752 ) ) ;
#43795=EDGE_CURVE ( 'NONE', #49183, #34590, #19862, .T. ) ;
#43796=CARTESIAN_POINT ( 'NONE',  ( 8.133937397696209715, 8.337936262032100032, -43.74348518090240390 ) ) ;
#43798=CARTESIAN_POINT ( 'NONE',  ( 52.83783599233930062, -49.65668728527659681, -48.61330445836559733 ) ) ;
#43799=CARTESIAN_POINT ( 'NONE',  ( 59.86146244909460279, -45.44095901954209893, -26.83847763191949909 ) ) ;
#43801=CARTESIAN_POINT ( 'NONE',  ( 56.57264709847169826, 14.96115542950509969, -26.26398226818550086 ) ) ;
#43803=CARTESIAN_POINT ( 'NONE',  ( 52.02481131427630601, 18.54900204977309741, -76.90588458405230199 ) ) ;
#43804=CARTESIAN_POINT ( 'NONE',  ( 52.72694658191860384, 18.49028550864479925, -48.50421737598679783 ) ) ;
#43807=ORIENTED_EDGE ( 'NONE', *, *, #17095, .T. ) ;
#43811=CARTESIAN_POINT ( 'NONE',  ( 47.71580729225940587, -54.48068309477200444, -54.87186394391349609 ) ) ;
#43813=CARTESIAN_POINT ( 'NONE',  ( 48.42521416700790127, 25.14253336855949783, -60.76348542011150045 ) ) ;
#43814=CARTESIAN_POINT ( 'NONE',  ( 59.15983391655790058, -28.73665177021000261, -15.68167984968010131 ) ) ;
#43819=CARTESIAN_POINT ( 'NONE',  ( 68.13393739769620083, -48.11618894467930119, -73.25000000000000000 ) ) ;
#43822=EDGE_CURVE ( 'NONE', #32096, #17323, #19007, .T. ) ;
#43823=VERTEX_POINT ( 'NONE', #4789 ) ;
#43825=CARTESIAN_POINT ( 'NONE',  ( 21.08268135459507420, 0.3115492626563509115, -75.56421356237308373 ) ) ;
#43830=CARTESIAN_POINT ( 'NONE',  ( 11.02024616950667557, 33.64882680616562993, -23.17060109525836964 ) ) ;
#43832=CARTESIAN_POINT ( 'NONE',  ( 60.85636071390069901, 14.48090769567980018, -47.74754960808709825 ) ) ;
#43834=TOROIDAL_SURFACE ( 'NONE', #275, 17.39999999999999858, 3.799999999999999822 ) ;
#43838=CARTESIAN_POINT ( 'NONE',  ( 60.83746312569630277, -29.08971170939889817, -15.89330470500829939 ) ) ;
#43839=EDGE_CURVE ( 'NONE', #15227, #3359, #27170, .T. ) ;
#43844=CARTESIAN_POINT ( 'NONE',  ( 41.12836154737230032, 13.96087487792660120, -5.806220427399999551 ) ) ;
#43845=ADVANCED_FACE ( 'NONE', ( #14461 ), #38720, .T. ) ;
#43846=CIRCLE ( 'NONE', #12057, 0.9999999999568487397 ) ;
#43848=CARTESIAN_POINT ( 'NONE',  ( 84.13361756236649569, -43.99383155051249616, -46.96659941728370313 ) ) ;
#43851=ORIENTED_EDGE ( 'NONE', *, *, #8119, .F. ) ;
#43852=CARTESIAN_POINT ( 'NONE',  ( 52.88967915934290431, -49.60939747366519725, -27.87881832530509740 ) ) ;
#43853=CARTESIAN_POINT ( 'NONE',  ( 15.78755803685880110, -51.00425289770759463, -20.74412215666150061 ) ) ;
#43856=DIRECTION ( 'NONE',  ( 1.000000000000000000, 0.000000000000000000, 0.000000000000000000 ) ) ;
#43858=CARTESIAN_POINT ( 'NONE',  ( -5.701502996861630201, -46.97469897207449918, -5.417034474275260081 ) ) ;
#43859=DIRECTION ( 'NONE',  ( -1.000000000000000000, 0.000000000000000000, 0.000000000000000000 ) ) ;
#43860=DIRECTION ( 'NONE',  ( 0.6888026391158329487, 0.7071067811865494601, 0.1598465650148944150 ) ) ;
#43862=CARTESIAN_POINT ( 'NONE',  ( 57.37674695049749829, -50.61618894467930119, -53.87125040983160318 ) ) ;
#43863=CARTESIAN_POINT ( 'NONE',  ( 40.74969953824990654, 13.47525508662189964, -4.809312831994500215 ) ) ;
#43866=DIRECTION ( 'NONE',  ( -0.8732394366197182567, 0.4872913772396111343, 0.000000000000000000 ) ) ;
#43870=CARTESIAN_POINT ( 'NONE',  ( 17.37473796128360348, -52.76520172820870158, -76.12661215459480957 ) ) ;
#43873=CARTESIAN_POINT ( 'NONE',  ( 15.00527006812512987, 19.40301060417740686, -20.65452753591024759 ) ) ;
#43876=ORIENTED_EDGE ( 'NONE', *, *, #10592, .F. ) ;
#43877=CARTESIAN_POINT ( 'NONE',  ( 8.807322927776979782, 32.00291607516390258, -46.67042760097810117 ) ) ;
#43881=CARTESIAN_POINT ( 'NONE',  ( 17.49786823416480175, 21.15196775986840194, -76.02269426304029309 ) ) ;
#43883=ORIENTED_EDGE ( 'NONE', *, *, #20038, .F. ) ;
#43889=EDGE_CURVE ( 'NONE', #29281, #17323, #8366, .T. ) ;
#43893=CARTESIAN_POINT ( 'NONE',  ( 12.36320305029179956, 33.31445045633500257, -15.76422791923680045 ) ) ;
#43898=ORIENTED_EDGE ( 'NONE', *, *, #24481, .F. ) ;
#43900=CARTESIAN_POINT ( 'NONE',  ( 46.53687296277449548, -53.33479509908829641, -76.10218428122850298 ) ) ;
#43901=CARTESIAN_POINT ( 'NONE',  ( 61.23319982858129862, 14.25045713433570072, -47.51874276278900311 ) ) ;
#43902=EDGE_CURVE ( 'NONE', #14173, #40777, #28292, .T. ) ;
#43904=AXIS2_PLACEMENT_3D ( 'NONE', #4772, #11879, #31497 ) ;
#43905=CARTESIAN_POINT ( 'NONE',  ( 41.38588534151550391, -44.01253888900150457, -3.641004148972040166 ) ) ;
#43906=CARTESIAN_POINT ( 'NONE',  ( -3.204312279287770515, 17.11425786164920027, -4.550063412008999997 ) ) ;
#43908=CARTESIAN_POINT ( 'NONE',  ( 58.32293069149620379, 14.27849980386080020, -26.32855658276989885 ) ) ;
#43910=ORIENTED_EDGE ( 'NONE', *, *, #19555, .T. ) ;
#43911=AXIS2_PLACEMENT_3D ( 'NONE', #144, #30805, #15622 ) ;
#43913=CARTESIAN_POINT ( 'NONE',  ( 11.83825639606079960, 33.81473130967069807, -45.42565952151209530 ) ) ;
#43916=VECTOR ( 'NONE', #12418, 1000.000000000000000 ) ;
#43918=CARTESIAN_POINT ( 'NONE',  ( 13.04450223014749888, 18.79195992918549862, -21.04428000939609689 ) ) ;
#43920=CARTESIAN_POINT ( 'NONE',  ( 48.46825551001710153, -54.10363359004039552, -54.77876380330509676 ) ) ;
#43928=EDGE_LOOP ( 'NONE', ( #17200, #37120, #48797, #22795 ) ) ;
#43930=CARTESIAN_POINT ( 'NONE',  ( 60.99523858508899821, -45.40662299616879949, -47.17226579437180334 ) ) ;
#43931=CARTESIAN_POINT ( 'NONE',  ( 47.81335647231890107, -54.39749252969859583, -54.71582838609030119 ) ) ;
#43936=CARTESIAN_POINT ( 'NONE',  ( 56.52536539877749533, 19.51942783438209972, -53.84278118897309895 ) ) ;
#43943=CARTESIAN_POINT ( 'NONE',  ( 53.55317832401189548, -49.41998711946010303, -49.22667755100069797 ) ) ;
#43944=CARTESIAN_POINT ( 'NONE',  ( 55.92234169269686106, 14.66394275432020144, -25.39467821330401165 ) ) ;
#43945=CARTESIAN_POINT ( 'NONE',  ( 76.39108789613560191, -16.41352413642167818, -12.75810673299934628 ) ) ;
#43946=ORIENTED_EDGE ( 'NONE', *, *, #4116, .T. ) ;
#43950=CARTESIAN_POINT ( 'NONE',  ( 57.25641887048840317, -45.13136270895589774, -25.31435934810820143 ) ) ;
#43951=CARTESIAN_POINT ( 'NONE',  ( 56.51998432061900246, -50.75157408873379694, -53.72896419663980083 ) ) ;
#43953=CARTESIAN_POINT ( 'NONE',  ( 59.93368784167530805, -1.201354282306859922, -16.01185523896749885 ) ) ;
#43954=ORIENTED_EDGE ( 'NONE', *, *, #10213, .F. ) ;
#43956=CARTESIAN_POINT ( 'NONE',  ( 53.72304193977469566, -50.62044000525840204, -76.82797321725880124 ) ) ;
#43961=CARTESIAN_POINT ( 'NONE',  ( 12.53340094288019912, -50.34701036924130335, -21.18850769734029882 ) ) ;
#43962=EDGE_CURVE ( 'NONE', #33996, #22272, #48491, .T. ) ;
#43964=CARTESIAN_POINT ( 'NONE',  ( 66.23540447448814916, -49.95860450174473044, -71.35146707679193412 ) ) ;
#43965=CARTESIAN_POINT ( 'NONE',  ( 61.04011644851190255, -45.35928274206209920, -46.86308394475349814 ) ) ;
#43968=AXIS2_PLACEMENT_3D ( 'NONE', #2925, #20950, #17040 ) ;
#43969=DIRECTION ( 'NONE',  ( 0.000000000000000000, 0.000000000000000000, 1.000000000000000000 ) ) ;
#43972=CARTESIAN_POINT ( 'NONE',  ( 13.48116118032930011, -51.59709463796549755, -74.36013246831049628 ) ) ;
#43973=CARTESIAN_POINT ( 'NONE',  ( 47.38854743227360444, -54.66225796327380237, -54.75946254694029847 ) ) ;
#43975=AXIS2_PLACEMENT_3D ( 'NONE', #47095, #3313, #11446 ) ;
#43977=CARTESIAN_POINT ( 'NONE',  ( 60.87559839016541474, -45.45153674070272842, -47.11203263457593948 ) ) ;
#43979=CARTESIAN_POINT ( 'NONE',  ( 11.74201408115419909, 34.19078560508950204, -18.09919823649679671 ) ) ;
#43981=CARTESIAN_POINT ( 'NONE',  ( 83.89200044194980421, -48.61618894467930119, -53.92796738110899923 ) ) ;
#43983=CARTESIAN_POINT ( 'NONE',  ( 4.773435940454120008, -58.71549427862700554, -13.16255389817539978 ) ) ;
#43984=FACE_OUTER_BOUND ( 'NONE', #8756, .T. ) ;
#43985=CARTESIAN_POINT ( 'NONE',  ( 49.69686147736450010, 22.42393137654260116, -54.99388098410930326 ) ) ;
#43986=VERTEX_POINT ( 'NONE', #16007 ) ;
#43987=CARTESIAN_POINT ( 'NONE',  ( 52.89232551375209113, -49.65864638672599796, -48.97387503448329937 ) ) ;
#43988=ORIENTED_EDGE ( 'NONE', *, *, #44165, .T. ) ;
#43992=CARTESIAN_POINT ( 'NONE',  ( 56.84932596551109185, -50.65659107673559447, -53.85230338955700091 ) ) ;
#43993=CARTESIAN_POINT ( 'NONE',  ( 82.68714621053810276, 13.87897394514460103, -46.76937705306080062 ) ) ;
#43994=CARTESIAN_POINT ( 'NONE',  ( 54.97499875616310305, 15.98981385143299860, -26.07547149580530288 ) ) ;
#43996=CARTESIAN_POINT ( 'NONE',  ( 53.27384017177119802, 18.28364788282440045, -49.18478595043859514 ) ) ;
#43997=CARTESIAN_POINT ( 'NONE',  ( 56.98602350126559912, -45.17932659337360235, -17.71533550764939591 ) ) ;
#44005=CARTESIAN_POINT ( 'NONE',  ( 11.11465761659180096, -65.15671412701409793, -17.59315288542880040 ) ) ;
#44006=CARTESIAN_POINT ( 'NONE',  ( 11.05731942293660097, 33.25945548349249492, -45.88168350577869603 ) ) ;
#44007=CARTESIAN_POINT ( 'NONE',  ( 18.51615658030550904, 20.07812231642038370, -15.71022044314043775 ) ) ;
#44008=CARTESIAN_POINT ( 'NONE',  ( 48.16430552237229534, -54.25377568305749776, -54.81723493473039355 ) ) ;
#44009=CARTESIAN_POINT ( 'NONE',  ( 11.62036812317445822, -65.37374231276770331, -22.52863453705835894 ) ) ;
#44010=CARTESIAN_POINT ( 'NONE',  ( 51.29176633094323279, 3.460026447682412964, -76.59668190568126533 ) ) ;
#44012=EDGE_LOOP ( 'NONE', ( #39979, #2877, #7019, #8300 ) ) ;
#44013=CARTESIAN_POINT ( 'NONE',  ( 12.16981617636350066, 18.81688479155219795, -21.14999999999999858 ) ) ;
#44015=CARTESIAN_POINT ( 'NONE',  ( 11.13393739769619906, -63.49867051491490599, -43.75823411798670293 ) ) ;
#44016=CARTESIAN_POINT ( 'NONE',  ( 68.13393739769814772, 19.38381105532029736, -71.50000000000200373 ) ) ;
#44018=CARTESIAN_POINT ( 'NONE',  ( 11.32941444270682751, -64.39195768723817537, -44.31826145974155651 ) ) ;
#44019=CARTESIAN_POINT ( 'NONE',  ( 56.89024914083419304, 19.26467303738039760, -53.06448611529630455 ) ) ;
#44020=FACE_OUTER_BOUND ( 'NONE', #38517, .T. ) ;
#44022=ORIENTED_EDGE ( 'NONE', *, *, #46527, .F. ) ;
#44026=CARTESIAN_POINT ( 'NONE',  ( 51.49741897520730305, 20.33382311736169967, -51.82318133733109988 ) ) ;
#44028=FACE_OUTER_BOUND ( 'NONE', #8825, .T. ) ;
#44029=DIRECTION ( 'NONE',  ( 1.000000000000000000, 0.000000000000000000, 0.000000000000000000 ) ) ;
#44036=CARTESIAN_POINT ( 'NONE',  ( 47.21535380273969906, 23.31245928922829691, -75.00416199656089589 ) ) ;
#44039=CARTESIAN_POINT ( 'NONE',  ( 11.95767227754359929, 33.76040311825810392, -16.37738641794519978 ) ) ;
#44040=CONICAL_SURFACE ( 'NONE', #29766, 55.50000000000000711, 1.262743545771120246 ) ;
#44042=VECTOR ( 'NONE', #1413, 1000.000000000000000 ) ;
#44043=CARTESIAN_POINT ( 'NONE',  ( 56.23763027956269411, -50.62070442378890078, -75.67790624608100813 ) ) ;
#44047=CARTESIAN_POINT ( 'NONE',  ( 61.36576913129360378, 13.98029824516259900, -46.78307081367769626 ) ) ;
#44050=CARTESIAN_POINT ( 'NONE',  ( 53.26660255314480708, -49.43204447085090436, -48.79175800379049832 ) ) ;
#44051=CARTESIAN_POINT ( 'NONE',  ( 57.35811193301260147, -45.61648094041229484, -26.19463098886150476 ) ) ;
#44052=CARTESIAN_POINT ( 'NONE',  ( 57.55751162049570269, -50.09049722528730086, -52.57651812429949700 ) ) ;
#44053=CARTESIAN_POINT ( 'NONE',  ( 56.93939532337000031, 14.49262922001920018, -26.16865613188059925 ) ) ;
#44055=CARTESIAN_POINT ( 'NONE',  ( 50.87835696893989734, 18.59755892215100204, -76.22533640045350012 ) ) ;
#44056=CARTESIAN_POINT ( 'NONE',  ( 52.79145156329050081, 18.45098357012509993, -48.63146327739730168 ) ) ;
#44058=CARTESIAN_POINT ( 'NONE',  ( 68.13393739769620083, 16.88381105532069881, -71.50000000000000000 ) ) ;
#44060=ADVANCED_FACE ( 'NONE', ( #40366 ), #8202, .F. ) ;
#44061=DIRECTION ( 'NONE',  ( 0.2771081164311154366, 0.6505467637364714673, -0.7071067811865496822 ) ) ;
#44062=EDGE_CURVE ( 'NONE', #2875, #19986, #49245, .T. ) ;
#44063=CARTESIAN_POINT ( 'NONE',  ( 47.65526630185220114, -54.48436720726729732, -54.69071458794790175 ) ) ;
#44064=DIRECTION ( 'NONE',  ( 0.000000000000000000, 0.000000000000000000, -1.000000000000000000 ) ) ;
#44066=CARTESIAN_POINT ( 'NONE',  ( 59.16375522681380517, -28.11079332067949821, -15.65965516856539885 ) ) ;
#44071=AXIS2_PLACEMENT_3D ( 'NONE', #39159, #27091, #49217 ) ;
#44072=FACE_OUTER_BOUND ( 'NONE', #14760, .T. ) ;
#44075=ORIENTED_EDGE ( 'NONE', *, *, #19768, .T. ) ;
#44080=CARTESIAN_POINT ( 'NONE',  ( 11.93218508669420075, -65.12546966291930062, -45.62051050307170641 ) ) ;
#44082=CARTESIAN_POINT ( 'NONE',  ( 56.40194557720492696, 19.55619987700153217, -74.41780141112559477 ) ) ;
#44083=VERTEX_POINT ( 'NONE', #29593 ) ;
#44084=CARTESIAN_POINT ( 'NONE',  ( 10.97815053533537544, 33.58448697120250870, -23.21825472827888959 ) ) ;
#44095=CARTESIAN_POINT ( 'NONE',  ( 12.35403558730510021, -65.44380354427669033, -23.29258724847819906 ) ) ;
#44097=CARTESIAN_POINT ( 'NONE',  ( 42.22416114274249566, 14.21574947835240010, -6.646926284411279973 ) ) ;
#44099=CARTESIAN_POINT ( 'NONE',  ( 14.79004452048550000, 21.13934752900200209, -76.01805773991210913 ) ) ;
#44101=CARTESIAN_POINT ( 'NONE',  ( 84.42643369580130752, -43.29356274104110724, -47.38360074682189804 ) ) ;
#44107=CARTESIAN_POINT ( 'NONE',  ( 53.17482295840940054, -49.26994467858509097, -27.24576603800480257 ) ) ;
#44108=CARTESIAN_POINT ( 'NONE',  ( 15.67955243735410065, -50.86262981146630580, -20.14992656220979939 ) ) ;
#44109=CARTESIAN_POINT ( 'NONE',  ( 76.78794120290260139, 10.77102507788350039, -14.46667607172110159 ) ) ;
#44110=DIRECTION ( 'NONE',  ( 0.000000000000000000, 0.000000000000000000, -1.000000000000000000 ) ) ;
#44111=DIRECTION ( 'NONE',  ( 0.000000000000000000, 0.000000000000000000, 1.000000000000000000 ) ) ;
#44115=CARTESIAN_POINT ( 'NONE',  ( 47.32063939835540367, 23.47154167609649988, -54.65735503397459638 ) ) ;
#44116=AXIS2_PLACEMENT_3D ( 'NONE', #47817, #31544, #7732 ) ;
#44119=CARTESIAN_POINT ( 'NONE',  ( 57.42729054907940167, -50.31136290499970443, -52.86014444765240938 ) ) ;
#44120=CARTESIAN_POINT ( 'NONE',  ( 41.02582444074300128, 13.36974427871779980, -4.878402571444859781 ) ) ;
#44123=CARTESIAN_POINT ( 'NONE',  ( 56.24757573095129715, -47.87022910182560054, -48.07122818578029921 ) ) ;
#44124=CARTESIAN_POINT ( 'NONE',  ( 69.22748654599971019, -50.70395984888047991, -72.15645085170115181 ) ) ;
#44126=CARTESIAN_POINT ( 'NONE',  ( 17.93047854176909794, -52.54005950962240235, -75.96018872839380265 ) ) ;
#44127=ADVANCED_FACE ( 'NONE', ( #33267 ), #49791, .T. ) ;
#44129=CARTESIAN_POINT ( 'NONE',  ( 11.89321892218980103, 34.20364954172580241, -22.25048313876769868 ) ) ;
#44131=CARTESIAN_POINT ( 'NONE',  ( 30.63393739769620083, -15.61618894467929941, -6.928362978644219794 ) ) ;
#44132=CARTESIAN_POINT ( 'NONE',  ( 31.69621505786460247, -15.61618894467929763, -8.050000000000000711 ) ) ;
#44135=ADVANCED_FACE ( 'NONE', ( #34296 ), #48349, .T. ) ;
#44137=CARTESIAN_POINT ( 'NONE',  ( 17.96618083103230035, 21.24161264671329974, -75.93682688742939035 ) ) ;
#44139=B_SPLINE_CURVE_WITH_KNOTS ( 'NONE', 3,
 ( #8770, #36793, #32840, #48867, #12974, #28927 ),
 .UNSPECIFIED., .F., .F.,
 ( 4, 2, 4 ),
 ( 0.4969483822624109481, 0.7484741911312053908, 1.000000000000000000 ),
 .UNSPECIFIED. ) ;
#44141=CARTESIAN_POINT ( 'NONE',  ( 56.50458353480760110, -46.26559983311960167, -26.27572163198150079 ) ) ;
#44143=DIRECTION ( 'NONE',  ( -0.8857883891771956009, -0.4640893551880597157, 0.000000000000000000 ) ) ;
#44145=LINE ( 'NONE', #8241, #4197 ) ;
#44146=FACE_OUTER_BOUND ( 'NONE', #45383, .T. ) ;
#44148=DIRECTION ( 'NONE',  ( -0.4808500020228050897, -0.3493579760610313611, 0.8041966675616158966 ) ) ;
#44153=CARTESIAN_POINT ( 'NONE',  ( 46.35275103504449845, -52.90993241930539881, -76.14999999999999147 ) ) ;
#44154=CARTESIAN_POINT ( 'NONE',  ( 60.79127206636130154, 14.45127149603970018, -47.68528058551200388 ) ) ;
#44156=CIRCLE ( 'NONE', #27426, 3.500000000000003109 ) ;
#44158=CARTESIAN_POINT ( 'NONE',  ( -11.32734370190460105, 10.64934056395049922, -6.430192534648650593 ) ) ;
#44159=CARTESIAN_POINT ( 'NONE',  ( 47.18324198357289845, 23.57489020266570279, -74.14999999999999147 ) ) ;
#44160=CARTESIAN_POINT ( 'NONE',  ( 59.14587251186409844, 14.19052952610539897, -26.50944264180050070 ) ) ;
#44163=VERTEX_POINT ( 'NONE', #9187 ) ;
#44164=CARTESIAN_POINT ( 'NONE',  ( 16.13393739769620083, -15.61618894467929941, -20.15000000000000213 ) ) ;
#44165=EDGE_CURVE ( 'NONE', #8693, #43345, #37732, .T. ) ;
#44167=CARTESIAN_POINT ( 'NONE',  ( 53.64461521333896599, -51.26703787289181236, -75.63087492057186978 ) ) ;
#44172=CARTESIAN_POINT ( 'NONE',  ( 46.85494769317200081, 22.79310794512280225, -75.76537854031029440 ) ) ;
#44173=CARTESIAN_POINT ( 'NONE',  ( 48.51671518355920654, -54.02387269257750546, -54.61093961119340179 ) ) ;
#44174=CARTESIAN_POINT ( 'NONE',  ( 52.01928042579915257, -32.98329962954817063, -19.49272405259882390 ) ) ;
#44177=CARTESIAN_POINT ( 'NONE',  ( 57.04834586696819798, 13.88381105532070059, -16.05449549621770089 ) ) ;
#44178=ORIENTED_EDGE ( 'NONE', *, *, #41417, .F. ) ;
#44183=CARTESIAN_POINT ( 'NONE',  ( 60.74338974301230110, -45.55518699895110046, -47.36711274165079999 ) ) ;
#44184=CARTESIAN_POINT ( 'NONE',  ( 56.86634278361329820, 19.42073994026870309, -53.85427493997759285 ) ) ;
#44188=DIRECTION ( 'NONE',  ( 0.8263629291053389281, -0.3519990991164029803, -0.4395690430656890024 ) ) ;
#44193=CARTESIAN_POINT ( 'NONE',  ( 84.44784216359251161, -43.11618894467930119, -47.47585302082339354 ) ) ;
#44194=VERTEX_POINT ( 'NONE', #21983 ) ;
#44199=CARTESIAN_POINT ( 'NONE',  ( 76.42339056421366195, -22.53537624654720162, -12.89730100488529274 ) ) ;
#44200=CARTESIAN_POINT ( 'NONE',  ( 53.17454399592740089, -51.89736142002809771, -53.32454619227790005 ) ) ;
#44201=ORIENTED_EDGE ( 'NONE', *, *, #45674, .F. ) ;
#44203=CARTESIAN_POINT ( 'NONE',  ( 48.71617454467180153, 22.66482838071829775, -54.49917290083569554 ) ) ;
#44204=CARTESIAN_POINT ( 'NONE',  ( 56.87859880284599967, -45.21741274165630387, -25.29773968820679997 ) ) ;
#44205=CARTESIAN_POINT ( 'NONE',  ( 56.52383276625679542, -50.75240083704239424, -53.80484218896539517 ) ) ;
#44210=B_SPLINE_CURVE_WITH_KNOTS ( 'NONE', 3,
 ( #20216, #4246, #24126, #8700, #32769, #565, #314, #33039, #3997, #71, #13171, #44082, #5031, #12903 ),
 .UNSPECIFIED., .F., .F.,
 ( 4, 2, 2, 2, 2, 2, 4 ),
 ( 0.000000000000000000, 0.03186051038564466364, 0.1779947729689404512, 0.2693286870835011615, 0.4519965153126213053, 0.7442650404792127139, 1.000000000000000000 ),
 .UNSPECIFIED. ) ;
#44212=CARTESIAN_POINT ( 'NONE',  ( 54.08403600473499750, -50.62655576154210024, -76.77913599446510773 ) ) ;
#44216=CARTESIAN_POINT ( 'NONE',  ( 12.94869328597129865, -50.11097969449580347, -21.09867881371670251 ) ) ;
#44217=CYLINDRICAL_SURFACE ( 'NONE', #28777, 1.999999999999997113 ) ;
#44220=CARTESIAN_POINT ( 'NONE',  ( 65.43393739769584272, -48.11618894467832064, -70.54999999999975557 ) ) ;
#44225=CARTESIAN_POINT ( 'NONE',  ( -23.86606260230375298, 4.515865522462924275, -53.92777777777781978 ) ) ;
#44226=ORIENTED_EDGE ( 'NONE', *, *, #11827, .T. ) ;
#44227=CARTESIAN_POINT ( 'NONE',  ( 14.39527773360719820, -51.26000396899650013, -74.91994212301220557 ) ) ;
#44228=EDGE_CURVE ( 'NONE', #18800, #23355, #18067, .T. ) ;
#44229=CARTESIAN_POINT ( 'NONE',  ( 47.30647391031549631, -54.71510682645079982, -54.67548368043780016 ) ) ;
#44233=DIRECTION ( 'NONE',  ( 1.000000000000000000, 0.000000000000000000, 0.000000000000000000 ) ) ;
#44234=CARTESIAN_POINT ( 'NONE',  ( 60.89898296291905666, -45.44660769381673049, -47.15703363117398794 ) ) ;
#44235=CARTESIAN_POINT ( 'NONE',  ( 11.89321892218980103, 34.20364954172580241, -18.17421237893020347 ) ) ;
#44237=CARTESIAN_POINT ( 'NONE',  ( 14.58586965385978296, -51.79680896048888172, -75.65449996337102334 ) ) ;
#44238=CARTESIAN_POINT ( 'NONE',  ( 48.74056688299980777, 22.69703636651660261, -54.59336294021409941 ) ) ;
#44240=CARTESIAN_POINT ( 'NONE',  ( 53.05460986333120132, -49.56517142501709827, -48.99361254808879806 ) ) ;
#44241=ORIENTED_EDGE ( 'NONE', *, *, #15203, .T. ) ;
#44244=CARTESIAN_POINT ( 'NONE',  ( 56.86634279045120621, -50.65311782823120268, -53.85427494076709820 ) ) ;
#44245=CARTESIAN_POINT ( 'NONE',  ( 83.85202357338320667, 13.12642060550550127, -46.78691132286910204 ) ) ;
#44246=CARTESIAN_POINT ( 'NONE',  ( 53.47797947282749931, 17.67580957532919683, -26.84483267738330170 ) ) ;
#44248=CARTESIAN_POINT ( 'NONE',  ( 52.62851231361270266, 18.57686390552120059, -48.67161502741990375 ) ) ;
#44249=CARTESIAN_POINT ( 'NONE',  ( 56.80367323221330622, -45.12899470519759859, -16.17916504339369865 ) ) ;
#44254=EDGE_CURVE ( 'NONE', #5735, #42976, #46722, .T. ) ;
#44255=ORIENTED_EDGE ( 'NONE', *, *, #11709, .F. ) ;
#44256=CARTESIAN_POINT ( 'NONE',  ( 11.94685996674130024, -65.31805379620070084, -17.08231279504250111 ) ) ;
#44257=CARTESIAN_POINT ( 'NONE',  ( 10.67951312630159855, 33.37294054514710240, -46.54192847483160023 ) ) ;
#44258=CARTESIAN_POINT ( 'NONE',  ( 18.78952938989682053, 20.37315169409249194, -15.76902864060759590 ) ) ;
#44259=CARTESIAN_POINT ( 'NONE',  ( 48.78564399443680344, -53.86781325685030453, -54.49562672282650055 ) ) ;
#44260=CARTESIAN_POINT ( 'NONE',  ( 8.794764235947729603, 31.93474649087269768, -46.67042062406039804 ) ) ;
#44265=CARTESIAN_POINT ( 'NONE',  ( 53.59003930803689997, -49.40628012469949937, -49.22510501142529904 ) ) ;
#44266=CARTESIAN_POINT ( 'NONE',  ( 11.13393739769619906, -63.29577390112070390, -43.91524999462519929 ) ) ;
#44270=CARTESIAN_POINT ( 'NONE',  ( 50.04022686061209413, -48.91488563423410341, -76.14999999999999147 ) ) ;
#44271=DIRECTION ( 'NONE',  ( -0.3294064756441168473, -0.9441882088883136737, 0.000000000000000000 ) ) ;
#44272=ORIENTED_EDGE ( 'NONE', *, *, #10533, .T. ) ;
#44274=CARTESIAN_POINT ( 'NONE',  ( 11.67619942398487609, 33.65927571709751476, -46.39999999999999858 ) ) ;
#44283=CARTESIAN_POINT ( 'NONE',  ( 52.82328078765490176, -49.70102997746409557, -48.95193629136059599 ) ) ;
#44286=CARTESIAN_POINT ( 'NONE',  ( 46.98204976736620608, 22.87102341606869871, -75.65359354181590845 ) ) ;
#44289=CARTESIAN_POINT ( 'NONE',  ( 61.28610861176739633, -45.23040055550220018, -28.15000000000000213 ) ) ;
#44292=AXIS2_PLACEMENT_3D ( 'NONE', #33527, #13881, #45861 ) ;
#44295=CARTESIAN_POINT ( 'NONE',  ( 54.36664156623190536, -50.61618894733009455, -76.93804975441300087 ) ) ;
#44299=MANIFOLD_SOLID_BREP ( 'Stock-MAS-691-1', #18449 ) ;
#44301=CARTESIAN_POINT ( 'NONE',  ( 61.37776962238909562, 13.97314662197880075, -46.75431274365950429 ) ) ;
#44302=CARTESIAN_POINT ( 'NONE',  ( -0.4147641054085740020, -62.74225160656001066, -49.23002488738299576 ) ) ;
#44304=CARTESIAN_POINT ( 'NONE',  ( 52.92965940600010555, -49.60857842614319679, -48.75165690212650560 ) ) ;
#44305=CARTESIAN_POINT ( 'NONE',  ( 61.43378182061679382, -45.16646909839339941, -28.04045001510230151 ) ) ;
#44307=CARTESIAN_POINT ( 'NONE',  ( 57.38853962498540540, 14.21080702799810069, -26.07334594942189909 ) ) ;
#44309=CARTESIAN_POINT ( 'NONE',  ( 50.30621308613430642, 17.38380720298980009, -76.16272939236809236 ) ) ;
#44310=CARTESIAN_POINT ( 'NONE',  ( 52.95762501200700001, 18.36394703063159994, -48.83320043447420034 ) ) ;
#44312=CARTESIAN_POINT ( 'NONE',  ( 85.38000601716228743, 17.38381105532069881, -60.34000486924599471 ) ) ;
#44313=CARTESIAN_POINT ( 'NONE',  ( 43.40604938376139899, -43.84278571223109822, -5.039288310186040398 ) ) ;
#44314=VERTEX_POINT ( 'NONE', #8078 ) ;
#44317=CARTESIAN_POINT ( 'NONE',  ( 47.77491216306469823, -54.41753965447119867, -54.70980729587230229 ) ) ;
#44320=CARTESIAN_POINT ( 'NONE',  ( 60.62314454574009659, 14.26357126862269986, -47.31713781460809543 ) ) ;
#44327=ORIENTED_EDGE ( 'NONE', *, *, #5964, .F. ) ;
#44328=DIRECTION ( 'NONE',  ( 1.224646799147353207E-16, 1.000000000000000000, -0.000000000000000000 ) ) ;
#44333=CARTESIAN_POINT ( 'NONE',  ( 11.72329413022380074, -64.94052275741300662, -45.18478288877960836 ) ) ;
#44335=AXIS2_PLACEMENT_3D ( 'NONE', #28502, #35860, #216 ) ;
#44344=CIRCLE ( 'NONE', #30070, 1.500000000000001332 ) ;
#44347=ORIENTED_EDGE ( 'NONE', *, *, #47166, .F. ) ;
#44348=CARTESIAN_POINT ( 'NONE',  ( 11.74606379632330011, -63.66956124298060615, -24.76212639862699660 ) ) ;
#44350=CARTESIAN_POINT ( 'NONE',  ( 42.00758169699690114, 14.56552422315210116, -6.830508309558650737 ) ) ;
#44352=CARTESIAN_POINT ( 'NONE',  ( 14.07159887855190128, 21.04516553096049947, -75.75221093576890041 ) ) ;
#44353=ADVANCED_FACE ( 'NONE', ( #8330 ), #12525, .T. ) ;
#44354=CARTESIAN_POINT ( 'NONE',  ( 51.88872868351670320, 18.11352286612800100, -77.07840643951000459 ) ) ;
#44356=CARTESIAN_POINT ( 'NONE',  ( 83.24078296369461327, -44.82564673796089494, -46.48094294253990455 ) ) ;
#44358=ADVANCED_FACE ( 'NONE', ( #35770 ), #19904, .F. ) ;
#44360=ORIENTED_EDGE ( 'NONE', *, *, #49842, .T. ) ;
#44361=CARTESIAN_POINT ( 'NONE',  ( 52.98187407645789904, -49.51877675916850308, -27.67813261086740084 ) ) ;
#44362=CARTESIAN_POINT ( 'NONE',  ( 15.78591284856750043, -50.92509110356280644, -20.28298178678319985 ) ) ;
#44363=CARTESIAN_POINT ( 'NONE',  ( 57.28991729228510366, 19.34649676830889931, -53.44461810997239581 ) ) ;
#44368=AXIS2_PLACEMENT_3D ( 'NONE', #3217, #47504, #39378 ) ;
#44369=CARTESIAN_POINT ( 'NONE',  ( -10.40242566545200020, -42.83441872489630242, -6.165522616775290565 ) ) ;
#44371=CARTESIAN_POINT ( 'NONE',  ( 47.29084618877600121, 23.49490054074589906, -54.73149148133969533 ) ) ;
#44377=CARTESIAN_POINT ( 'NONE',  ( 42.50318722711249819, 12.76421688433049972, -4.913421252035550246 ) ) ;
#44381=CARTESIAN_POINT ( 'NONE',  ( 57.08291034350739324, -47.57583641667570618, -48.30715737835689794 ) ) ;
#44384=CARTESIAN_POINT ( 'NONE',  ( 17.69336951584759987, -52.55982454884319566, -76.04476946176040997 ) ) ;
#44387=CARTESIAN_POINT ( 'NONE',  ( 46.03122142033570441, 13.88381105532070059, -7.582879021622040305 ) ) ;
#44390=CARTESIAN_POINT ( 'NONE',  ( 9.727929673803711097, 31.89460007113610018, -46.30184689934900177 ) ) ;
#44391=FACE_OUTER_BOUND ( 'NONE', #45881, .T. ) ;
#44392=CARTESIAN_POINT ( 'NONE',  ( 67.36984938551290725, -30.01295387514729995, -17.47394132841339598 ) ) ;
#44394=CARTESIAN_POINT ( 'NONE',  ( 18.55689598211829860, 20.32289363718000175, -74.92517623884199907 ) ) ;
#44400=DIRECTION ( 'NONE',  ( -0.8224686640529097481, 0.3976080002595595575, -0.4067593573362710546 ) ) ;
#44401=LINE ( 'NONE', #20528, #36474 ) ;
#44402=CARTESIAN_POINT ( 'NONE',  ( 61.50409081826520463, 14.14169698785779872, -47.35439638855399380 ) ) ;
#44403=ORIENTED_EDGE ( 'NONE', *, *, #9872, .F. ) ;
#44406=CARTESIAN_POINT ( 'NONE',  ( 11.98643035757825892, 34.18553736260165010, -17.50083510588233793 ) ) ;
#44407=ORIENTED_EDGE ( 'NONE', *, *, #23034, .F. ) ;
#44408=CARTESIAN_POINT ( 'NONE',  ( 11.60073034461098551, -64.80729423298977565, -23.92052759426241337 ) ) ;
#44411=VERTEX_POINT ( 'NONE', #11157 ) ;
#44412=ORIENTED_EDGE ( 'NONE', *, *, #38703, .T. ) ;
#44413=DIRECTION ( 'NONE',  ( 0.7800418122827239564, 0.000000000000000000, -0.6257273935913973961 ) ) ;
#44415=VECTOR ( 'NONE', #4753, 1000.000000000000000 ) ;
#44416=CARTESIAN_POINT ( 'NONE',  ( 60.63142620721699672, 14.43203532425889968, -47.55417844658280302 ) ) ;
#44418=CARTESIAN_POINT ( 'NONE',  ( 45.64758709548550542, 13.96552996563729998, -8.164367127537008884 ) ) ;
#44420=CARTESIAN_POINT ( 'NONE',  ( -8.924323233903118435, 12.96044049061340075, -5.352796887738729303 ) ) ;
#44422=CARTESIAN_POINT ( 'NONE',  ( 55.12914169688411192, 14.86070934991266590, -16.25648467340654335 ) ) ;
#44423=EDGE_CURVE ( 'NONE', #19697, #26146, #50724, .T. ) ;
#44427=CARTESIAN_POINT ( 'NONE',  ( 41.31928349002789957, 14.36833702740849894, -6.259994320181990091 ) ) ;
#44432=CARTESIAN_POINT ( 'NONE',  ( 49.39942642721219812, -53.75096344194059128, -54.82511225024550328 ) ) ;
#44433=CARTESIAN_POINT ( 'NONE',  ( -7.973795448866470181, 13.91176078833520080, -5.720958296299230028 ) ) ;
#44434=FACE_OUTER_BOUND ( 'NONE', #28282, .T. ) ;
#44439=VECTOR ( 'NONE', #51349, 1000.000000000000000 ) ;
#44441=CARTESIAN_POINT ( 'NONE',  ( 65.03603135424580728, -29.76883965895079953, -19.52361391316370032 ) ) ;
#44442=VERTEX_POINT ( 'NONE', #31810 ) ;
#44444=CARTESIAN_POINT ( 'NONE',  ( 60.79250979228859819, -45.50810424805050758, -47.25467579807390450 ) ) ;
#44446=CARTESIAN_POINT ( 'NONE',  ( 67.50570755965968317, -43.40455556736388587, -11.14108988509339326 ) ) ;
#44450=DIRECTION ( 'NONE',  ( -1.065814103640149870E-16, 1.000000000000000000, 0.000000000000000000 ) ) ;
#44451=VERTEX_POINT ( 'NONE', #6967 ) ;
#44452=CARTESIAN_POINT ( 'NONE',  ( 83.91175033285890095, -44.80491236700709834, -47.46627397093730139 ) ) ;
#44455=ORIENTED_EDGE ( 'NONE', *, *, #51277, .F. ) ;
#44457=CARTESIAN_POINT ( 'NONE',  ( 53.48381752779376086, -50.52032509664712734, -77.13953785887332515 ) ) ;
#44458=CARTESIAN_POINT ( 'NONE',  ( 76.39938456792719990, -19.35446345062952744, -12.79389377502640102 ) ) ;
#44459=CARTESIAN_POINT ( 'NONE',  ( 50.21208614976480078, -53.15602288804570463, -53.95043619330500206 ) ) ;
#44463=CARTESIAN_POINT ( 'NONE',  ( 48.89501045483829955, 22.56229972626200109, -54.41963477494619639 ) ) ;
#44465=EDGE_CURVE ( 'NONE', #41357, #18363, #41685, .T. ) ;
#44467=DIRECTION ( 'NONE',  ( 0.8090169943749478954, 0.5877852522924724710, 0.000000000000000000 ) ) ;
#44470=ADVANCED_FACE ( 'NONE', ( #8507 ), #48340, .T. ) ;
#44471=ORIENTED_EDGE ( 'NONE', *, *, #20038, .T. ) ;
#44475=CARTESIAN_POINT ( 'NONE',  ( 82.75389963950320293, -45.59493862562369770, -47.67227237921210303 ) ) ;
#44477=CARTESIAN_POINT ( 'NONE',  ( 41.70176439649490163, -44.27974353495149984, -4.832746683949399547 ) ) ;
#44478=CARTESIAN_POINT ( 'NONE',  ( 57.00722761779879733, 13.88381105532070059, -15.97596069844019873 ) ) ;
#44482=( BOUNDED_CURVE ( )  B_SPLINE_CURVE ( 3, ( #44507, #15448, #40062, #35867 ),
 .UNSPECIFIED., .F., .T. ) 
 B_SPLINE_CURVE_WITH_KNOTS ( ( 4, 4 ),
 ( 3.323007232337010119, 3.540281829795995261 ),
 .UNSPECIFIED. ) 
 CURVE ( )  GEOMETRIC_REPRESENTATION_ITEM ( )  RATIONAL_B_SPLINE_CURVE ( ( 1.000000000000000000, 0.9960698467165439718, 0.9960698467165439718, 1.000000000000000000 ) ) 
 REPRESENTATION_ITEM ( '' )  );
#44486=CARTESIAN_POINT ( 'NONE',  ( 18.30487665358372240, -52.23919279727024190, -75.65449996337102334 ) ) ;
#44487=AXIS2_PLACEMENT_3D ( 'NONE', #11482, #27439, #39004 ) ;
#44488=EDGE_CURVE ( 'NONE', #19762, #43431, #25842, .T. ) ;
#44490=CARTESIAN_POINT ( 'NONE',  ( 13.61616881089470077, -51.88814251562879321, -75.11575902016450357 ) ) ;
#44491=CARTESIAN_POINT ( 'NONE',  ( 47.23304785971389919, -54.76875619474640189, -54.67497879625340573 ) ) ;
#44492=SURFACE_STYLE_USAGE ( .BOTH. , #3894 ) ;
#44493=CARTESIAN_POINT ( 'NONE',  ( 10.79909669266985617, 33.81695037846098018, -47.18321592281282761 ) ) ;
#44496=CARTESIAN_POINT ( 'NONE',  ( 57.36082898843075384, 14.38365649012001768, -26.19484475583911021 ) ) ;
#44498=CARTESIAN_POINT ( 'NONE',  ( 47.29473060385306837, 22.86193303853967151, -75.51963295297495904 ) ) ;
#44499=CARTESIAN_POINT ( 'NONE',  ( 11.18117724951066094, 32.79411394922273359, -24.11551136640916582 ) ) ;
#44501=CARTESIAN_POINT ( 'NONE',  ( 48.76908445385270596, 22.82217318232579828, -55.30112621652450144 ) ) ;
#44502=VERTEX_POINT ( 'NONE', #36789 ) ;
#44507=CARTESIAN_POINT ( 'NONE',  ( 11.93174526809839975, 34.20691394249479345, -17.93019253464870033 ) ) ;
#44508=CARTESIAN_POINT ( 'NONE',  ( 83.45793240077850328, 13.44987206900269960, -46.53859470524319875 ) ) ;
#44509=CARTESIAN_POINT ( 'NONE',  ( 54.60893606919109544, 16.53358082662880335, -26.40962254079889959 ) ) ;
#44511=CARTESIAN_POINT ( 'NONE',  ( 52.63952980978569940, 18.56936772728549911, -48.69585515676859444 ) ) ;
#44512=CARTESIAN_POINT ( 'NONE',  ( 55.16770328537340617, -45.48138187130849985, -15.50413919957330044 ) ) ;
#44516=CARTESIAN_POINT ( 'NONE',  ( 11.90855646482620145, -65.23144919529680408, -16.85546526173629900 ) ) ;
#44517=CARTESIAN_POINT ( 'NONE',  ( 12.36168672466449969, 34.19959952941539427, -47.41183413623420506 ) ) ;
#44518=CARTESIAN_POINT ( 'NONE',  ( 61.31733475858135307, -45.31597754466083927, -47.18612592330886457 ) ) ;
#44520=CARTESIAN_POINT ( 'NONE',  ( 52.94338268357279986, -49.52467429185519876, -48.62015017847210174 ) ) ;
#44521=CARTESIAN_POINT ( 'NONE',  ( 11.59132828503483026, -65.36240846161591378, -22.55862962361555546 ) ) ;
#44522=CARTESIAN_POINT ( 'NONE',  ( 61.51122975691189509, -45.14516155341349446, -28.15000000000000213 ) ) ;
#44525=DIRECTION ( 'NONE',  ( 0.000000000000000000, 1.000000000000000000, 0.000000000000000000 ) ) ;
#44526=CARTESIAN_POINT ( 'NONE',  ( 10.97826455356500119, -63.19059205414950497, -44.74194573736729552 ) ) ;
#44530=CARTESIAN_POINT ( 'NONE',  ( 50.20000625561069540, -49.66915949483620096, -76.14999999999999147 ) ) ;
#44533=B_SPLINE_CURVE_WITH_KNOTS ( 'NONE', 3,
 ( #42171, #10462, #35059, #42435 ),
 .UNSPECIFIED., .F., .F.,
 ( 4, 4 ),
 ( 0.000000000000000000, 1.000000000000000000 ),
 .UNSPECIFIED. ) ;
#44539=CARTESIAN_POINT ( 'NONE',  ( 13.81959240756670049, -51.26308380449479785, -23.06522851520879769 ) ) ;
#44540=CARTESIAN_POINT ( 'NONE',  ( 54.72927025131360068, 19.84196400840209762, -75.36035929567221103 ) ) ;
#44542=CARTESIAN_POINT ( 'NONE',  ( 47.44049510014409776, -54.50743786567679905, -74.80726814568210159 ) ) ;
#44543=ORIENTED_EDGE ( 'NONE', *, *, #45907, .T. ) ;
#44546=CARTESIAN_POINT ( 'NONE',  ( 54.17308945056809932, 21.38381105532069881, -77.01198594424270993 ) ) ;
#44547=EDGE_CURVE ( 'NONE', #9596, #17738, #47854, .T. ) ;
#44548=CARTESIAN_POINT ( 'NONE',  ( 47.27157656634140181, 23.02640076397910107, -75.35698732394219235 ) ) ;
#44549=ADVANCED_FACE ( 'NONE', ( #44146 ), #12182, .T. ) ;
#44551=CARTESIAN_POINT ( 'NONE',  ( 75.04939620295753855, -19.22741391667048561, -11.30491871076487875 ) ) ;
#44554=CARTESIAN_POINT ( 'NONE',  ( -5.066062602303800233, -15.61618894467930119, -10.44999999999999929 ) ) ;
#44555=AXIS2_PLACEMENT_3D ( 'NONE', #38370, #18959, #18447 ) ;
#44557=CARTESIAN_POINT ( 'NONE',  ( 57.24934407037070372, -50.61618894527409651, -74.14876594678160870 ) ) ;
#44561=CARTESIAN_POINT ( 'NONE',  ( 61.36075333576579993, 13.96751052759550049, -46.61068689941740217 ) ) ;
#44562=CARTESIAN_POINT ( 'NONE',  ( -12.15512026601220086, -55.59619837851330004, -51.32444474606690221 ) ) ;
#44564=CARTESIAN_POINT ( 'NONE',  ( 52.84703211352019991, -49.65186917973220204, -48.63862332596730198 ) ) ;
#44565=CARTESIAN_POINT ( 'NONE',  ( 57.50445365671880182, -45.11618913266270425, -25.33159055575459817 ) ) ;
#44567=CARTESIAN_POINT ( 'NONE',  ( 56.48403040235340455, 14.55542443240409867, -26.04784922081150000 ) ) ;
#44569=CARTESIAN_POINT ( 'NONE',  ( 51.01627429428619820, 19.33079967119669718, -76.16510837308341308 ) ) ;
#44570=CARTESIAN_POINT ( 'NONE',  ( 53.10865791236649613, 18.28620130409879962, -48.88762731574559695 ) ) ;
#44572=CARTESIAN_POINT ( 'NONE',  ( 42.93197233849399908, -42.55807683903039162, -3.187564294433600232 ) ) ;
#44573=CARTESIAN_POINT ( 'NONE',  ( 74.94086307074489639, -45.11618894467940066, -15.31398699537819930 ) ) ;
#44577=CARTESIAN_POINT ( 'NONE',  ( 47.60865874083440019, -54.51384904987570224, -54.69368874373819978 ) ) ;
#44580=CARTESIAN_POINT ( 'NONE',  ( 40.92757333388370000, 13.18145061293710008, -3.805844904963549880 ) ) ;
#44581=CARTESIAN_POINT ( 'NONE',  ( 58.92073642956109580, -28.10798705511860263, -15.65000675586140311 ) ) ;
#44585=LINE ( 'NONE', #5021, #36851 ) ;
#44587=EDGE_LOOP ( 'NONE', ( #46120, #21562 ) ) ;
#44589=CARTESIAN_POINT ( 'NONE',  ( 57.35590716318880311, 18.90417298996780104, -52.61987026769980247 ) ) ;
#44591=CARTESIAN_POINT ( 'NONE',  ( 16.06904196025218567, -51.02878819236820362, -15.66677487260436230 ) ) ;
#44592=ORIENTED_EDGE ( 'NONE', *, *, #37680, .F. ) ;
#44595=DIRECTION ( 'NONE',  ( -0.2260571801428149230, 0.000000000000000000, 0.9741140340359946137 ) ) ;
#44596=CARTESIAN_POINT ( 'NONE',  ( 52.36900551255840242, 19.49169383700370162, -76.35261119704479427 ) ) ;
#44600=CARTESIAN_POINT ( 'NONE',  ( 60.77958717670829714, 14.50249311732349966, -47.75277892092170617 ) ) ;
#44604=ORIENTED_EDGE ( 'NONE', *, *, #16854, .T. ) ;
#44607=CARTESIAN_POINT ( 'NONE',  ( 40.92585300945609816, 14.21241371935070141, -5.903596487906789925 ) ) ;
#44609=AXIS2_PLACEMENT_3D ( 'NONE', #11304, #35660, #31440 ) ;
#44610=EDGE_CURVE ( 'NONE', #25200, #19643, #10853, .T. ) ;
#44611=CARTESIAN_POINT ( 'NONE',  ( 14.12708840369279883, 20.99064699730730155, -75.77237669558989808 ) ) ;
#44617=CARTESIAN_POINT ( 'NONE',  ( 54.15165173585579339, -48.25669691649810034, -26.60605610731790094 ) ) ;
#44618=CARTESIAN_POINT ( 'NONE',  ( 14.40169973177160045, -50.85784981463910270, -21.38758215361159998 ) ) ;
#44619=DIRECTION ( 'NONE',  ( 0.2260571801428161165, -1.387778780781444597E-17, -0.9741140340359943917 ) ) ;
#44621=DIRECTION ( 'NONE',  ( 0.000000000000000000, 0.7371541402007423249, 0.6757246285173452716 ) ) ;
#44622=AXIS2_PLACEMENT_3D ( 'NONE', #6879, #29916, #6099 ) ;
#44624=CARTESIAN_POINT ( 'NONE',  ( -9.502204115007360841, -43.71455336852960016, -5.942533345529509958 ) ) ;
#44625=VECTOR ( 'NONE', #45305, 1000.000000000000000 ) ;
#44626=CARTESIAN_POINT ( 'NONE',  ( 47.24676140008929082, 23.52564688271890248, -54.63827976033719835 ) ) ;
#44627=CARTESIAN_POINT ( 'NONE',  ( 57.24929578595760660, 21.38381105532069881, -74.14999999999999147 ) ) ;
#44629=CARTESIAN_POINT ( 'NONE',  ( 57.27629350501299399, -50.59351780024810097, -53.60235144059989665 ) ) ;
#44630=CARTESIAN_POINT ( 'NONE',  ( 10.90442930760440099, 33.77248995292200107, -17.54871770534860076 ) ) ;
#44631=DIRECTION ( 'NONE',  ( -1.000000000000000000, -4.829924999999999738E-13, 7.800438000000000694E-12 ) ) ;
#44634=CARTESIAN_POINT ( 'NONE',  ( 53.97718803714800373, -49.20306630607990428, -49.10491108831829621 ) ) ;
#44635=CARTESIAN_POINT ( 'NONE',  ( 68.13393739769840352, -50.61618894467879670, -73.25000000000220268 ) ) ;
#44637=CARTESIAN_POINT ( 'NONE',  ( 17.21347160910390173, -53.11618894467930119, -76.14999999999999147 ) ) ;
#44640=DIRECTION ( 'NONE',  ( 0.000000000000000000, 0.000000000000000000, -1.000000000000000000 ) ) ;
#44641=ORIENTED_EDGE ( 'NONE', *, *, #4669, .T. ) ;
#44642=CARTESIAN_POINT ( 'NONE',  ( 20.06565654289127210, 23.98759296397042462, -19.24283188815232037 ) ) ;
#44643=CARTESIAN_POINT ( 'NONE',  ( 8.965489388580479613, 31.97191824437770080, -46.63273652527719548 ) ) ;
#44644=DIRECTION ( 'NONE',  ( 0.000000000000000000, 0.000000000000000000, -1.000000000000000000 ) ) ;
#44645=CARTESIAN_POINT ( 'NONE',  ( 66.89371529141759254, -30.40426478165719715, -17.19079369877330166 ) ) ;
#44647=CARTESIAN_POINT ( 'NONE',  ( 18.45802431067919969, 20.88378464714680049, -75.46937177410659103 ) ) ;
#44652=CARTESIAN_POINT ( 'NONE',  ( 11.15446670767390103, -64.60906199386440107, -45.98375597346589672 ) ) ;
#44656=CARTESIAN_POINT ( 'NONE',  ( 61.48332870919479376, 13.96258771565810086, -46.85782488637240562 ) ) ;
#44659=CARTESIAN_POINT ( 'NONE',  ( 75.24807542847500486, 3.017609241400042386, -12.28055750973653737 ) ) ;
#44660=ADVANCED_FACE ( 'NONE', ( #14694 ), #18877, .F. ) ;
#44662=ORIENTED_EDGE ( 'NONE', *, *, #2171, .T. ) ;
#44663=CARTESIAN_POINT ( 'NONE',  ( 51.61134830314709632, -46.21250895552949345, -13.62813625026690012 ) ) ;
#44667=VECTOR ( 'NONE', #49738, 1000.000000000000000 ) ;
#44668=ORIENTED_EDGE ( 'NONE', *, *, #12004, .T. ) ;
#44669=CARTESIAN_POINT ( 'NONE',  ( 57.55751162049570269, -50.48013859002959691, -53.20292136905285929 ) ) ;
#44671=CARTESIAN_POINT ( 'NONE',  ( 68.38971107296249841, -30.11618894467929763, -18.15384911730639672 ) ) ;
#44672=CARTESIAN_POINT ( 'NONE',  ( 60.85636071390069901, 14.48090769567980018, -47.74754960808709825 ) ) ;
#44673=CARTESIAN_POINT ( 'NONE',  ( 50.61935581471210099, 13.97259095194099920, -11.61330938592119999 ) ) ;
#44675=CARTESIAN_POINT ( 'NONE',  ( -9.882013117715120032, -40.49932216338130075, -21.14999999999999858 ) ) ;
#44676=CARTESIAN_POINT ( 'NONE',  ( -5.346827492566250228, 15.73560381583549628, -4.480328055642280205 ) ) ;
#44684=DIRECTION ( 'NONE',  ( 6.127627000000000503E-13, 6.320986000000000022E-13, -1.000000000000000000 ) ) ;
#44689=CARTESIAN_POINT ( 'NONE',  ( 49.69686147736390325, -53.65630926590149841, -54.99388098410970116 ) ) ;
#44690=CARTESIAN_POINT ( 'NONE',  ( -7.099872940393900045, 14.68218975379929958, -5.638321079196820129 ) ) ;
#44693=CARTESIAN_POINT ( 'NONE',  ( 11.13393739769619906, 32.28996931002959769, -24.14942631645369886 ) ) ;
#44699=EDGE_LOOP ( 'NONE', ( #11282, #15183, #15856, #32956 ) ) ;
#44701=CARTESIAN_POINT ( 'NONE',  ( 60.43738122508229793, -45.77296434314530416, -47.62750683704569354 ) ) ;
#44703=CARTESIAN_POINT ( 'NONE',  ( 50.47459370284350655, 19.05485954424960227, -76.14999999999999147 ) ) ;
#44709=CARTESIAN_POINT ( 'NONE',  ( 83.89463082533569604, -44.78225339558859730, -47.42987625071230440 ) ) ;
#44711=ORIENTED_EDGE ( 'NONE', *, *, #28118, .F. ) ;
#44713=CARTESIAN_POINT ( 'NONE',  ( 61.73642837792289839, -45.13062012120709454, -46.64899561561870200 ) ) ;
#44714=CARTESIAN_POINT ( 'NONE',  ( 11.93174526809839975, 34.20691394249479345, -17.93019253464870033 ) ) ;
#44715=ADVANCED_FACE ( 'NONE', ( #14436 ), #30407, .T. ) ;
#44716=CARTESIAN_POINT ( 'NONE',  ( 76.39394475779087657, -13.67985447755458850, -12.77041102619445923 ) ) ;
#44717=CARTESIAN_POINT ( 'NONE',  ( 53.36408652092959670, -52.07595258546250250, -53.95637823904670682 ) ) ;
#44718=ADVANCED_FACE ( 'NONE', ( #46429, #26473 ), #42490, .T. ) ;
#44719=ORIENTED_EDGE ( 'NONE', *, *, #13913, .T. ) ;
#44720=ORIENTED_EDGE ( 'NONE', *, *, #16902, .T. ) ;
#44726=LINE ( 'NONE', #1224, #41153 ) ;
#44728=DIRECTION ( 'NONE',  ( 0.000000000000000000, 1.000000000000000000, 0.000000000000000000 ) ) ;
#44729=ORIENTED_EDGE ( 'NONE', *, *, #945, .T. ) ;
#44731=CARTESIAN_POINT ( 'NONE',  ( 53.96532960447419924, -50.61809440848099939, -76.95223789022560368 ) ) ;
#44732=CARTESIAN_POINT ( 'NONE',  ( 60.33694438359644607, 14.62750282847424899, -47.70890968787152531 ) ) ;
#44733=CARTESIAN_POINT ( 'NONE',  ( 60.48811175542340379, 14.41611557752919914, -47.17639167819340429 ) ) ;
#44736=DIRECTION ( 'NONE',  ( -1.000000000000000000, -7.841349000000000539E-12, -8.551771000000000195E-12 ) ) ;
#44739=CARTESIAN_POINT ( 'NONE',  ( 42.88515050504339854, -43.77470902807130670, -4.897272209519029751 ) ) ;
#44741=CARTESIAN_POINT ( 'NONE',  ( 57.50723902594879888, 13.88381105532070059, -17.67941225248179649 ) ) ;
#44742=CARTESIAN_POINT ( 'NONE',  ( 68.03757084111694553, 0.7700511936776454069, -18.68196744858373037 ) ) ;
#44745=CARTESIAN_POINT ( 'NONE',  ( 66.89373992269190694, -0.8281018005762210699, -17.19081051937810045 ) ) ;
#44747=CARTESIAN_POINT ( 'NONE',  ( 14.48971970689060029, -51.52596624575240725, -75.36996982820370761 ) ) ;
#44748=CARTESIAN_POINT ( 'NONE',  ( 47.29014113061550262, -54.72776004820889995, -54.71595221509849694 ) ) ;
#44750=LINE ( 'NONE', #48427, #12952 ) ;
#44755=CARTESIAN_POINT ( 'NONE',  ( 47.76731554892809584, -54.45608225251359613, -54.88059270044120552 ) ) ;
#44758=CARTESIAN_POINT ( 'NONE',  ( 47.26610112325450075, 22.82567072896360116, -75.56421356201970241 ) ) ;
#44761=CARTESIAN_POINT ( 'NONE',  ( 42.48652067987293179, 13.02449555953472426, -5.094659060785825311 ) ) ;
#44762=CARTESIAN_POINT ( 'NONE',  ( 48.63180645979579708, 22.87900943640810070, -55.21523209561640044 ) ) ;
#44763=EDGE_LOOP ( 'NONE', ( #10957, #30328, #1752 ) ) ;
#44766=DIRECTION ( 'NONE',  ( 1.000000000000000000, 0.000000000000000000, 0.000000000000000000 ) ) ;
#44767=DIRECTION ( 'NONE',  ( -0.7286256507163790808, -0.6849121557675359462, 0.000000000000000000 ) ) ;
#44769=CARTESIAN_POINT ( 'NONE',  ( 83.93595989616819963, 13.02949184870690047, -46.83273212233100224 ) ) ;
#44770=CARTESIAN_POINT ( 'NONE',  ( 53.19086730767300253, 17.98371808565390140, -27.08903680673190095 ) ) ;
#44773=CARTESIAN_POINT ( 'NONE',  ( 57.39657356000389399, -45.11618894467940066, -17.44506318542070034 ) ) ;
#44774=B_SPLINE_SURFACE_WITH_KNOTS ( 'NONE', 3, 3, ( 
 ( #33133, #49158, #37347, #13254 ),
 ( #21340, #51472, #15312, #38909 ),
 ( #22637, #10349, #30758, #42581 ),
 ( #46523, #31264, #39421, #38655 ),
 ( #3521, #26308, #22377, #35481 ),
 ( #27349, #35215, #2743, #31015 ),
 ( #26834, #15571, #10869, #11127 ),
 ( #2999, #31527, #51218, #26566 ),
 ( #3256, #42321, #2476, #14790 ),
 ( #34690, #46780, #43099, #43355 ),
 ( #42843, #23146, #6419, #39162 ),
 ( #18714, #18969, #47297, #15048 ) ),
 .UNSPECIFIED., .F., .F., .F.,
 ( 4, 1, 1, 1, 1, 1, 1, 1, 1, 4 ),
 ( 4, 4 ),
 ( 0.000000000000000000, 0.1111111111111110078, 0.2222222222222219878, 0.3333333333333329818, 0.4444444444444439757, 0.5555555555555560243, 0.6666666666666670737, 0.7777777777777779011, 0.8888888888888889506, 1.000000000000000000 ),
 ( -0.2043272503186320255, -0.05091814332707400581 ),
 .UNSPECIFIED. ) ;
#44775=DIRECTION ( 'NONE',  ( 0.5685928097855380559, -0.5944782866685500711, -0.5685928097855370567 ) ) ;
#44776=ORIENTED_EDGE ( 'NONE', *, *, #24084, .F. ) ;
#44777=ORIENTED_EDGE ( 'NONE', *, *, #43436, .T. ) ;
#44778=CARTESIAN_POINT ( 'NONE',  ( 12.06706412657270100, -65.03706746763299407, -16.41672221715840152 ) ) ;
#44779=CARTESIAN_POINT ( 'NONE',  ( 12.01677611816480074, 34.07027331508780321, -47.05243182101040134 ) ) ;
#44780=CARTESIAN_POINT ( 'NONE',  ( 18.54927880441067956, 20.10353310518733139, -15.71463296250362518 ) ) ;
#44782=DIRECTION ( 'NONE',  ( -0.7052114458104683514, 0.7089970498513439301, 0.000000000000000000 ) ) ;
#44785=ORIENTED_EDGE ( 'NONE', *, *, #11364, .F. ) ;
#44787=CARTESIAN_POINT ( 'NONE',  ( 13.61938558678000000, 20.19483563406610216, -23.15000000000000213 ) ) ;
#44788=CARTESIAN_POINT ( 'NONE',  ( 52.82975638541582697, 18.42854252836027484, -28.09160094008685604 ) ) ;
#44789=CARTESIAN_POINT ( 'NONE',  ( -11.32734370190460105, -41.88171845330919751, -19.14999999999999858 ) ) ;
#44791=CARTESIAN_POINT ( 'NONE',  ( 50.46752464413489747, -49.58022540544509837, -76.16325466874729955 ) ) ;
#44795=CARTESIAN_POINT ( 'NONE',  ( 54.34775236769140605, -47.86158002624119945, -25.94360105443890063 ) ) ;
#44798=CYLINDRICAL_SURFACE ( 'NONE', #28464, 1.999999999999999112 ) ;
#44802=CARTESIAN_POINT ( 'NONE',  ( 14.16335351432319989, -51.13178799427510768, -22.70850811651479972 ) ) ;
#44803=CARTESIAN_POINT ( 'NONE',  ( 56.46547423300169299, 19.54384849142039826, -74.28346178225240237 ) ) ;
#44804=CARTESIAN_POINT ( 'NONE',  ( 47.05561704033240034, -53.94108635855520362, -75.73967526752529977 ) ) ;
#44806=CARTESIAN_POINT ( 'NONE',  ( 63.88393739769619373, 4.883811055320659733, -61.44999999999999574 ) ) ;
#44810=CARTESIAN_POINT ( 'NONE',  ( 47.50309827252019801, 23.36724551378910064, -74.17369128426381053 ) ) ;
#44811=CARTESIAN_POINT ( 'NONE',  ( 18.86789271272390067, -51.78678247029300508, -15.81497036395479761 ) ) ;
#44812=CARTESIAN_POINT ( 'NONE',  ( 68.13393739769620083, -43.11618894467930119, -73.25000000000000000 ) ) ;
#44813=CARTESIAN_POINT ( 'NONE',  ( 61.28610861176739633, 13.99802266614350010, -28.15000000000000213 ) ) ;
#44814=EDGE_CURVE ( 'NONE', #7703, #26641, #14072, .T. ) ;
#44815=DIRECTION ( 'NONE',  ( -0.9441882088883087887, 0.3294064756441308917, 0.000000000000000000 ) ) ;
#44819=CARTESIAN_POINT ( 'NONE',  ( 61.13393739769620083, 1.883811055320649963, -84.38499399519520239 ) ) ;
#44820=DIRECTION ( 'NONE',  ( -3.532868000000000128E-12, 2.963302999999999818E-13, 1.000000000000000000 ) ) ;
#44823=CARTESIAN_POINT ( 'NONE',  ( 61.32721378439150328, 13.97792828797489939, -46.50571435523870178 ) ) ;
#44824=CARTESIAN_POINT ( 'NONE',  ( -32.51565489538130294, -20.32396912357229724, -55.84912116621229927 ) ) ;
#44827=CARTESIAN_POINT ( 'NONE',  ( 52.99768783924589854, -49.57341479806719775, -48.81581856325809810 ) ) ;
#44829=CARTESIAN_POINT ( 'NONE',  ( 61.41965047412389822, -45.13055029907879856, -27.46561386188539799 ) ) ;
#44830=AXIS2_PLACEMENT_3D ( 'NONE', #44812, #28288, #1047 ) ;
#44832=CARTESIAN_POINT ( 'NONE',  ( 13.50712872756970029, 19.81166641576820098, -21.90151629162349778 ) ) ;
#44833=CARTESIAN_POINT ( 'NONE',  ( 57.21513657066689973, 14.40326995541390076, -26.18061821942099954 ) ) ;
#44835=CARTESIAN_POINT ( 'NONE',  ( 50.39203494153080243, 18.10371503980149654, -76.16300746228739627 ) ) ;
#44836=CARTESIAN_POINT ( 'NONE',  ( 52.73806344804810209, 18.48670660044059844, -48.65316599148000165 ) ) ;
#44838=CARTESIAN_POINT ( 'NONE',  ( 67.22839177940861077, -44.96269340666319891, -12.13170577700170050 ) ) ;
#44839=TOROIDAL_SURFACE ( 'NONE', #51533, 39.99999906195129995, 1.999999997951819930 ) ;
#44844=CARTESIAN_POINT ( 'NONE',  ( 47.47423769629730117, -54.59780520654420144, -54.66828950685410149 ) ) ;
#44847=CARTESIAN_POINT ( 'NONE',  ( 60.64534134237799634, 14.90352494164799957, -48.24433635901220185 ) ) ;
#44856=CARTESIAN_POINT ( 'NONE',  ( 8.964272521377070646, -63.19719428634219582, -46.63279896585060413 ) ) ;
#44857=CARTESIAN_POINT ( 'NONE',  ( 16.13393739769620083, -15.61618894467929941, 4.450000000000000178 ) ) ;
#44862=CARTESIAN_POINT ( 'NONE',  ( 51.82414486449059865, 18.95706542269019579, -76.50963458223939995 ) ) ;
#44863=ORIENTED_EDGE ( 'NONE', *, *, #26844, .T. ) ;
#44871=EDGE_LOOP ( 'NONE', ( #45333, #36425, #29999, #33364, #664 ) ) ;
#44872=CARTESIAN_POINT ( 'NONE',  ( 11.02107559592020003, -63.90702541208909082, -23.99273296026720104 ) ) ;
#44875=B_SPLINE_CURVE_WITH_KNOTS ( 'NONE', 3,
 ( #21460, #37983, #1558, #42174 ),
 .UNSPECIFIED., .F., .F.,
 ( 4, 4 ),
 ( 0.000000000000000000, 1.000000000000000000 ),
 .UNSPECIFIED. ) ;
#44877=CARTESIAN_POINT ( 'NONE',  ( 14.30169396435220008, 21.24161264671329974, -75.93682688742939035 ) ) ;
#44879=CARTESIAN_POINT ( 'NONE',  ( 83.53868183867639630, -44.62159407410370449, -46.56548196350899360 ) ) ;
#44882=CARTESIAN_POINT ( 'NONE',  ( 52.77203259569630234, -49.67394356405169731, -27.82577599984929861 ) ) ;
#44883=ADVANCED_FACE ( 'NONE', ( #4696 ), #13352, .F. ) ;
#44889=CARTESIAN_POINT ( 'NONE',  ( -10.41395375019419944, -42.81708513381939696, -6.102688242772109639 ) ) ;
#44890=CARTESIAN_POINT ( 'NONE',  ( 47.35959481792740178, 23.44442529656140195, -54.67024274119960126 ) ) ;
#44892=CARTESIAN_POINT ( 'NONE',  ( 55.92134356540361040, -45.89757597650480392, -25.32475626239351740 ) ) ;
#44895=CARTESIAN_POINT ( 'NONE',  ( 10.89208540626749944, 33.76849045686219597, -17.57297890437990162 ) ) ;
#44898=CARTESIAN_POINT ( 'NONE',  ( 53.94120575207560364, -49.17518334734650409, -49.03324901303680150 ) ) ;
#44900=CARTESIAN_POINT ( 'NONE',  ( 52.83863466997060243, 18.42092259931630238, -28.03264406027369660 ) ) ;
#44901=CARTESIAN_POINT ( 'NONE',  ( 17.32335564108290171, -52.96147345225150360, -76.14999999999999147 ) ) ;
#44903=CARTESIAN_POINT ( 'NONE',  ( 17.92370450339669929, -52.11618894467930119, -74.14999999999999147 ) ) ;
#44907=CARTESIAN_POINT ( 'NONE',  ( 8.966094888256401774, 31.97546849540949765, -46.63271503358079428 ) ) ;
#44909=DIRECTION ( 'NONE',  ( 0.000000000000000000, 0.000000000000000000, 1.000000000000000000 ) ) ;
#44910=ORIENTED_EDGE ( 'NONE', *, *, #14498, .F. ) ;
#44912=CARTESIAN_POINT ( 'NONE',  ( 18.42162172276690058, 20.91303491124869751, -75.51792558472189398 ) ) ;
#44913=AXIS2_PLACEMENT_3D ( 'NONE', #27272, #27785, #15236 ) ;
#44915=ORIENTED_EDGE ( 'NONE', *, *, #14061, .F. ) ;
#44916=EDGE_CURVE ( 'NONE', #26391, #9424, #42567, .T. ) ;
#44918=CARTESIAN_POINT ( 'NONE',  ( 11.54287861353399869, -64.87899921766438638, -45.94746754196619776 ) ) ;
#44919=CARTESIAN_POINT ( 'NONE',  ( 57.31690520220239193, -45.30894883373459692, -25.91066051893669808 ) ) ;
#44922=CARTESIAN_POINT ( 'NONE',  ( 61.69575994152130249, 13.91829368062330019, -46.74341057651110276 ) ) ;
#44926=DIRECTION ( 'NONE',  ( 0.000000000000000000, -1.000000000000000000, 0.000000000000000000 ) ) ;
#44928=CARTESIAN_POINT ( 'NONE',  ( 53.39341508398250369, -46.23762566829479681, -14.95068794128250111 ) ) ;
#44929=AXIS2_PLACEMENT_3D ( 'NONE', #30757, #41789, #14276 ) ;
#44935=CARTESIAN_POINT ( 'NONE',  ( 46.69262628625429556, -53.66646348021690471, -75.98411709232810551 ) ) ;
#44938=CARTESIAN_POINT ( 'NONE',  ( 53.44281326324379933, 14.78227628659979942, -14.85152119988429931 ) ) ;
#44940=CARTESIAN_POINT ( 'NONE',  ( -10.89446219731619969, 11.10192921922270060, -6.214546411156319117 ) ) ;
#44941=CARTESIAN_POINT ( 'NONE',  ( 61.04001029137710077, 14.12696047140060074, -46.86320535112459851 ) ) ;
#44942=CARTESIAN_POINT ( 'NONE',  ( 58.54030351516670549, 14.35265200861150170, -26.43833219818329638 ) ) ;
#44945=CARTESIAN_POINT ( 'NONE',  ( 56.64869691665980156, 16.52354571958140284, -48.31614736825900280 ) ) ;
#44946=EDGE_CURVE ( 'NONE', #1406, #9498, #20196, .T. ) ;
#44947=CARTESIAN_POINT ( 'NONE',  ( -8.885774327477038881, -44.39634378508870327, -6.080198097671999591 ) ) ;
#44948=CARTESIAN_POINT ( 'NONE',  ( 13.00893739769619906, 34.28605925116850273, -47.75434321273180416 ) ) ;
#44950=DIRECTION ( 'NONE',  ( -0.2517544074889974115, -0.9677911542837451808, 0.000000000000000000 ) ) ;
#44952=FACE_OUTER_BOUND ( 'NONE', #458, .T. ) ;
#44953=CARTESIAN_POINT ( 'NONE',  ( 49.32346266582219840, -53.57041216484680035, -54.24688575054349826 ) ) ;
#44962=CARTESIAN_POINT ( 'NONE',  ( 83.84453607992982427, -44.32824044336482672, -46.66650892480838309 ) ) ;
#44963=CARTESIAN_POINT ( 'NONE',  ( 61.12529890362679907, -45.61997541134829248, -47.68695910954430417 ) ) ;
#44965=CARTESIAN_POINT ( 'NONE',  ( 61.75019796695541885, 13.88381105532069881, -46.62077719375000129 ) ) ;
#44971=EDGE_LOOP ( 'NONE', ( #5361, #30205, #22826, #14610 ) ) ;
#44972=CARTESIAN_POINT ( 'NONE',  ( 83.76205119356160367, -44.99354611814039373, -47.48604701470450351 ) ) ;
#44974=VERTEX_POINT ( 'NONE', #38224 ) ;
#44978=CARTESIAN_POINT ( 'NONE',  ( 50.03007040746459921, -48.61618894467930119, -78.14999999999999147 ) ) ;
#44979=CARTESIAN_POINT ( 'NONE',  ( 76.39895413544020641, -19.27255048218861688, -12.79204002819740538 ) ) ;
#44980=CARTESIAN_POINT ( 'NONE',  ( 53.97000432569529949, -51.81786419676419797, -53.85145765957989283 ) ) ;
#44983=ORIENTED_EDGE ( 'NONE', *, *, #17177, .T. ) ;
#44985=CARTESIAN_POINT ( 'NONE',  ( 56.61697313468700798, 19.46285310884560005, -53.47849945241240022 ) ) ;
#44986=CARTESIAN_POINT ( 'NONE',  ( 12.73487495346794240, -55.47150669537813883, -75.56421462368682285 ) ) ;
#44988=DIRECTION ( 'NONE',  ( 0.000000000000000000, -1.000000000000000000, 0.000000000000000000 ) ) ;
#44989=B_SPLINE_CURVE_WITH_KNOTS ( 'NONE', 3,
 ( #30045, #49739, #22185, #22444, #2291, #26635, #50770, #9894, #33726, #26119 ),
 .UNSPECIFIED., .F., .F.,
 ( 4, 2, 2, 2, 4 ),
 ( 0.4999997377388590292, 0.5624999999911143300, 0.6624999999941543205, 0.8224999999990194599, 1.000000000000000000 ),
 .UNSPECIFIED. ) ;
#44994=CARTESIAN_POINT ( 'NONE',  ( 52.66506590845860103, -50.10307196442919775, -77.26054838597460162 ) ) ;
#45000=CARTESIAN_POINT ( 'NONE',  ( 42.68710801524959919, -43.36600712485200404, -4.456284347537809332 ) ) ;
#45002=CARTESIAN_POINT ( 'NONE',  ( 68.13393739769841773, -50.61618894467878960, -73.25000000000220268 ) ) ;
#45005=CARTESIAN_POINT ( 'NONE',  ( 65.03565846499330405, 1.015012278467199991, -17.83341330082179965 ) ) ;
#45006=EDGE_LOOP ( 'NONE', ( #32841, #20847, #34242, #4548, #1740 ) ) ;
#45007=CARTESIAN_POINT ( 'NONE',  ( 14.20086869850939948, -51.63908721605620400, -75.44171726276898937 ) ) ;
#45009=CARTESIAN_POINT ( 'NONE',  ( 57.35314493057190077, 19.08815642815629587, -52.86947157453059987 ) ) ;
#45011=DIRECTION ( 'NONE',  ( 0.000000000000000000, 1.000000000000000000, 0.000000000000000000 ) ) ;
#45013=CARTESIAN_POINT ( 'NONE',  ( 56.52536539877740296, -50.75180572374080157, -53.84278118897309895 ) ) ;
#45016=SPHERICAL_SURFACE ( 'NONE', #10541, 2.000000000000000000 ) ;
#45018=CARTESIAN_POINT ( 'NONE',  ( 47.66581657685510010, -54.52382939817299956, -55.09436269531810382 ) ) ;
#45019=DIRECTION ( 'NONE',  ( 0.9441882088883221114, 0.3294064756440927000, 0.000000000000000000 ) ) ;
#45020=CARTESIAN_POINT ( 'NONE',  ( 11.28911561387254636, 33.06253056614959718, -24.06342471125372739 ) ) ;
#45022=CARTESIAN_POINT ( 'NONE',  ( 18.68117707985434706, -55.53437412588283451, -76.07908087643973261 ) ) ;
#45023=CARTESIAN_POINT ( 'NONE',  ( 48.85376873155860267, 22.78610090897890217, -55.25797120370700100 ) ) ;
#45026=ORIENTED_EDGE ( 'NONE', *, *, #3499, .F. ) ;
#45027=CARTESIAN_POINT ( 'NONE',  ( 13.00893739761190027, -65.51843714052189682, -47.75434321210310173 ) ) ;
#45030=CARTESIAN_POINT ( 'NONE',  ( 84.42287661217579853, 12.05518195546730098, -47.36827274406740429 ) ) ;
#45031=CARTESIAN_POINT ( 'NONE',  ( 54.51447658024279974, 16.52301143147950313, -26.25507474854270029 ) ) ;
#45033=CARTESIAN_POINT ( 'NONE',  ( 11.41271396217753065, 33.75416681246611716, -16.69425700585250993 ) ) ;
#45039=CARTESIAN_POINT ( 'NONE',  ( 12.14166061495349958, -65.10571081234380131, -16.52221827438259893 ) ) ;
#45040=CARTESIAN_POINT ( 'NONE',  ( 13.00893739769619906, 34.28605925116850273, -47.75434321273180416 ) ) ;
#45041=CARTESIAN_POINT ( 'NONE',  ( 61.08967272334363230, -45.33611584009540962, -46.92974945990184210 ) ) ;
#45042=CARTESIAN_POINT ( 'NONE',  ( 50.54558668919739972, -52.16494804883890168, -52.27649567391959806 ) ) ;
#45043=CARTESIAN_POINT ( 'NONE',  ( 51.63120318262737385, 2.821641822706145497, -76.94893558361998487 ) ) ;
#45045=CARTESIAN_POINT ( 'NONE',  ( 12.35956436673935954, 18.99725813312436884, -21.15000000013027659 ) ) ;
#45046=CARTESIAN_POINT ( 'NONE',  ( 57.26919357480770145, 14.59258250881100061, -26.26282533821949983 ) ) ;
#45055=CARTESIAN_POINT ( 'NONE',  ( 12.57402232428822764, -55.45745225559931413, -75.39120620928086680 ) ) ;
#45056=AXIS2_PLACEMENT_3D ( 'NONE', #22542, #3166, #50859 ) ;
#45057=FACE_OUTER_BOUND ( 'NONE', #10221, .T. ) ;
#45062=CARTESIAN_POINT ( 'NONE',  ( 47.21823810954259670, -54.28882551123370348, -75.35585495399020317 ) ) ;
#45063=EDGE_LOOP ( 'NONE', ( #48594, #46534, #31038, #9173 ) ) ;
#45064=CARTESIAN_POINT ( 'NONE',  ( 55.72808153907849515, 14.53141219772050086, -16.72868168772430053 ) ) ;
#45065=CARTESIAN_POINT ( 'NONE',  ( 57.28991729228579288, -50.57887465766769708, -53.44461810997250240 ) ) ;
#45068=ORIENTED_EDGE ( 'NONE', *, *, #1174, .F. ) ;
#45069=CARTESIAN_POINT ( 'NONE',  ( 46.57616577472359864, 22.03317133735550115, -76.11243514202939764 ) ) ;
#45072=CARTESIAN_POINT ( 'NONE',  ( 12.24959214049200007, 33.48392698190040306, -15.94651421638729971 ) ) ;
#45081=CARTESIAN_POINT ( 'NONE',  ( 12.77400604982020127, -63.78156501761489494, -45.78449089158930008 ) ) ;
#45083=CARTESIAN_POINT ( 'NONE',  ( 53.18775749951439735, -49.47422114125170367, -48.84930875881670431 ) ) ;
#45084=CIRCLE ( 'NONE', #51777, 3.500000000000003109 ) ;
#45085=CARTESIAN_POINT ( 'NONE',  ( 17.71568183981793609, 20.46959823935371503, -75.56421430877649925 ) ) ;
#45087=CARTESIAN_POINT ( 'NONE',  ( 13.55381709587100048, 19.79410389518359992, -21.89021442387040040 ) ) ;
#45088=CARTESIAN_POINT ( 'NONE',  ( 57.45067094067109537, 14.37644489360019939, -26.20528765251999559 ) ) ;
#45089=VECTOR ( 'NONE', #5372, 1000.000000000000000 ) ;
#45091=CARTESIAN_POINT ( 'NONE',  ( 50.65831132946720317, 18.03884146108959996, -76.22116164240389935 ) ) ;
#45092=CARTESIAN_POINT ( 'NONE',  ( 53.25072070970590232, 18.25720078509660027, -49.09191088899479638 ) ) ;
#45094=CARTESIAN_POINT ( 'NONE',  ( 40.50275677532349761, -44.77423425411610225, -4.148922563335220026 ) ) ;
#45095=CARTESIAN_POINT ( 'NONE',  ( 47.11719193592726640, 22.63726203549512661, -75.76637087366511025 ) ) ;
#45100=CARTESIAN_POINT ( 'NONE',  ( 47.41980604789990394, -54.64426992894529889, -54.80792317606589847 ) ) ;
#45104=CARTESIAN_POINT ( 'NONE',  ( 58.51098925350719782, 17.50221282658370114, -51.08149774042820468 ) ) ;
#45105=CARTESIAN_POINT ( 'NONE',  ( 53.13663690894949809, 18.26775922387509965, -48.80285956119419666 ) ) ;
#45112=ORIENTED_EDGE ( 'NONE', *, *, #26420, .T. ) ;
#45113=CARTESIAN_POINT ( 'NONE',  ( 8.966097822182190313, -63.20784705743349718, -46.63270530499050182 ) ) ;
#45117=FACE_OUTER_BOUND ( 'NONE', #39549, .T. ) ;
#45119=CARTESIAN_POINT ( 'NONE',  ( 51.19067547918189831, 19.52102757408819755, -76.16618596938450025 ) ) ;
#45123=EDGE_CURVE ( 'NONE', #8693, #24585, #2369, .T. ) ;
#45125=EDGE_CURVE ( 'NONE', #44451, #30791, #31632, .T. ) ;
#45126=FACE_OUTER_BOUND ( 'NONE', #12968, .T. ) ;
#45129=ORIENTED_EDGE ( 'NONE', *, *, #47758, .T. ) ;
#45131=CARTESIAN_POINT ( 'NONE',  ( 52.59026075507060227, -49.83798095265300532, -48.57069100191419864 ) ) ;
#45135=CIRCLE ( 'NONE', #31706, 1.000000000000000444 ) ;
#45136=CARTESIAN_POINT ( 'NONE',  ( 14.45708746590530147, 21.37421319461290281, -76.02269426304029309 ) ) ;
#45138=CARTESIAN_POINT ( 'NONE',  ( 83.25003658253979211, -44.84236030505880422, -46.59700837026780107 ) ) ;
#45141=ORIENTED_EDGE ( 'NONE', *, *, #28482, .F. ) ;
#45142=CARTESIAN_POINT ( 'NONE',  ( 55.24793159653169994, -47.06280844521510431, -26.19812636028400021 ) ) ;
#45144=CYLINDRICAL_SURFACE ( 'NONE', #3125, 1.999999999999997113 ) ;
#45145=CARTESIAN_POINT ( 'NONE',  ( 16.13393739769620083, -15.61618894467929941, 4.450000000000000178 ) ) ;
#45146=CARTESIAN_POINT ( 'NONE',  ( 51.02727426391909660, 14.97163178983270093, -13.20164647346950026 ) ) ;
#45148=CARTESIAN_POINT ( 'NONE',  ( -7.441429056736700076, -45.44001222700619991, -5.170794712822120331 ) ) ;
#45149=CARTESIAN_POINT ( 'NONE',  ( 47.30810002566669681, 23.48187059465450233, -54.68911926312569705 ) ) ;
#45150=FACE_OUTER_BOUND ( 'NONE', #7421, .T. ) ;
#45152=CARTESIAN_POINT ( 'NONE',  ( 10.10517893431049963, -55.15925497894330931, -21.14999999999999858 ) ) ;
#45153=CARTESIAN_POINT ( 'NONE',  ( 11.22168587317799826, 33.99689325987720423, -17.68872783567740115 ) ) ;
#45154=CYLINDRICAL_SURFACE ( 'NONE', #15872, 21.50000000000000000 ) ;
#45156=CARTESIAN_POINT ( 'NONE',  ( 58.76827139312189985, -46.69333694941190060, -47.97482660407749933 ) ) ;
#45157=CARTESIAN_POINT ( 'NONE',  ( 52.41358714188920231, 21.24840881348460186, -54.13676513255019529 ) ) ;
#45158=VECTOR ( 'NONE', #30801, 1000.000000000000114 ) ;
#45163=CARTESIAN_POINT ( 'NONE',  ( 8.963664087775370604, 31.96126547328639944, -46.63283018613729780 ) ) ;
#45168=CARTESIAN_POINT ( 'NONE',  ( 68.36214372925699934, -30.78933952734989887, -18.19623527655679851 ) ) ;
#45170=CARTESIAN_POINT ( 'NONE',  ( 18.86790871750899967, 20.55443427335040241, -74.33583724502659607 ) ) ;
#45173=DIRECTION ( 'NONE',  ( 0.000000000000000000, 0.000000000000000000, -1.000000000000000000 ) ) ;
#45176=CARTESIAN_POINT ( 'NONE',  ( 10.92970840452719905, -64.58899151715630182, -46.27302159251959779 ) ) ;
#45177=CARTESIAN_POINT ( 'NONE',  ( 56.37838042625359947, -46.11745970339239875, -26.19141323752749884 ) ) ;
#45180=CARTESIAN_POINT ( 'NONE',  ( 61.37276932190779632, 14.04312170586010033, -47.09682269328109783 ) ) ;
#45183=ORIENTED_EDGE ( 'NONE', *, *, #26025, .F. ) ;
#45185=CARTESIAN_POINT ( 'NONE',  ( 50.30625828053950244, -45.11618894460909956, -10.79703776619339983 ) ) ;
#45188=DIRECTION ( 'NONE',  ( 1.000000000000000000, 0.000000000000000000, 0.000000000000000000 ) ) ;
#45193=CARTESIAN_POINT ( 'NONE',  ( 11.13393739769619906, 24.07008072128950005, -43.74348518090240390 ) ) ;
#45194=CARTESIAN_POINT ( 'NONE',  ( 47.14844574785740150, -54.72867718618289956, -74.72768729699521373 ) ) ;
#45195=CARTESIAN_POINT ( 'NONE',  ( 60.34379256561150129, 14.63564648314799932, -47.72732608210870353 ) ) ;
#45196=CARTESIAN_POINT ( 'NONE',  ( 51.90140114478749922, 14.76431734774619819, -13.70501522390690141 ) ) ;
#45198=FACE_OUTER_BOUND ( 'NONE', #34790, .T. ) ;
#45200=VECTOR ( 'NONE', #7557, 1000.000000000000000 ) ;
#45203=CARTESIAN_POINT ( 'NONE',  ( 60.84489046480559438, 13.88818919943340013, -26.73359653442770067 ) ) ;
#45211=CARTESIAN_POINT ( 'NONE',  ( 76.14068888614369257, -43.36749149024220173, -13.68366341276339959 ) ) ;
#45214=CARTESIAN_POINT ( 'NONE',  ( 50.03007040746459921, -36.85417771443089663, -76.14999999999999147 ) ) ;
#45217=CARTESIAN_POINT ( 'NONE',  ( 49.59615837245039671, -53.70224911814690216, -55.11137432941160341 ) ) ;
#45220=CARTESIAN_POINT ( 'NONE',  ( 17.92366719485290005, -51.11618258419110106, -74.34711752987139732 ) ) ;
#45226=EDGE_LOOP ( 'NONE', ( #30724, #9665, #22232, #34240 ) ) ;
#45228=CARTESIAN_POINT ( 'NONE',  ( 61.29825847224749680, -45.52681296980589565, -47.59225652243559779 ) ) ;
#45230=CARTESIAN_POINT ( 'NONE',  ( 50.39461195648269864, 18.90258328430419965, -76.14999999999999147 ) ) ;
#45232=DIRECTION ( 'NONE',  ( 0.000000000000000000, 0.000000000000000000, 1.000000000000000000 ) ) ;
#45236=ORIENTED_EDGE ( 'NONE', *, *, #46212, .F. ) ;
#45237=ORIENTED_EDGE ( 'NONE', *, *, #12008, .F. ) ;
#45239=CARTESIAN_POINT ( 'NONE',  ( 61.48302575854449969, -45.30855424813389476, -47.22534401859969933 ) ) ;
#45241=CYLINDRICAL_SURFACE ( 'NONE', #6486, 0.9999999999999976685 ) ;
#45244=ORIENTED_EDGE ( 'NONE', *, *, #41352, .F. ) ;
#45245=VERTEX_POINT ( 'NONE', #31363 ) ;
#45247=CARTESIAN_POINT ( 'NONE',  ( 62.09157612670949788, -33.11618894467940066, -65.34607522167520699 ) ) ;
#45251=DIRECTION ( 'NONE',  ( -1.000000000000000000, -1.007258792502662152E-15, 0.000000000000000000 ) ) ;
#45254=DIRECTION ( 'NONE',  ( 0.000000000000000000, 0.000000000000000000, -1.000000000000000000 ) ) ;
#45255=ORIENTED_EDGE ( 'NONE', *, *, #21105, .F. ) ;
#45257=CARTESIAN_POINT ( 'NONE',  ( 52.95141962741540453, -51.03458903264449731, -76.06582098811649928 ) ) ;
#45259=CARTESIAN_POINT ( 'NONE',  ( 60.55537580064579828, 14.38087405962720133, -47.18092733277320150 ) ) ;
#45262=CARTESIAN_POINT ( 'NONE',  ( 42.39659219033849524, 13.74223253253360078, -5.990488029809371007 ) ) ;
#45263=CARTESIAN_POINT ( 'NONE',  ( 41.66707677620669870, -44.64833008590599661, -5.278831885195840457 ) ) ;
#45266=CARTESIAN_POINT ( 'NONE',  ( 67.73241107036501774, 0.07875534547170300048, -17.99564714788500197 ) ) ;
#45267=VERTEX_POINT ( 'NONE', #16170 ) ;
#45268=CARTESIAN_POINT ( 'NONE',  ( 14.09076352594090054, -51.44957460137000282, -75.17186369577468952 ) ) ;
#45269=CARTESIAN_POINT ( 'NONE',  ( 47.18324198357289845, -54.80726809202429450, -54.61058319554170026 ) ) ;
#45273=VECTOR ( 'NONE', #12604, 1000.000000000000000 ) ;
#45276=CARTESIAN_POINT ( 'NONE',  ( 57.38152646595799666, 14.21216655855363875, -26.07295477665448757 ) ) ;
#45277=CARTESIAN_POINT ( 'NONE',  ( 11.14146392938010166, 33.97654110380459969, -17.73105615077219710 ) ) ;
#45279=CARTESIAN_POINT ( 'NONE',  ( 72.13393739769620083, -1.116188944679340045, -20.65000000000000213 ) ) ;
#45282=CARTESIAN_POINT ( 'NONE',  ( 48.60495210931490107, 22.85368323561639770, -54.93239174769010447 ) ) ;
#45285=ORIENTED_EDGE ( 'NONE', *, *, #20913, .F. ) ;
#45289=CARTESIAN_POINT ( 'NONE',  ( 83.70743316420070812, 13.68261143785749923, -47.36488538498209522 ) ) ;
#45290=CARTESIAN_POINT ( 'NONE',  ( 52.56521762488900151, 18.62942129817990278, -28.06242660726239890 ) ) ;
#45292=DIRECTION ( 'NONE',  ( 0.07088902009066748444, 0.000000000000000000, 0.9974842088126432138 ) ) ;
#45296=PRODUCT_DEFINITION ( 'UNKNOWN', '', #30180, #34741 ) ;
#45298=CARTESIAN_POINT ( 'NONE',  ( 12.05606148284189949, -65.16757949402220618, -16.66333073004830112 ) ) ;
#45299=CARTESIAN_POINT ( 'NONE',  ( 12.30109459971790109, 34.11576030229039702, -46.67181612106659827 ) ) ;
#45302=CARTESIAN_POINT ( 'NONE',  ( 10.52748814419759960, -64.93771388453561144, -47.11278010051370302 ) ) ;
#45303=ORIENTED_EDGE ( 'NONE', *, *, #40536, .T. ) ;
#45305=DIRECTION ( 'NONE',  ( 1.000000000000000000, 0.000000000000000000, 0.000000000000000000 ) ) ;
#45306=CARTESIAN_POINT ( 'NONE',  ( 52.82975622904280755, 18.42854261028849905, -28.15000000000000213 ) ) ;
#45308=CARTESIAN_POINT ( 'NONE',  ( 52.92565939194879832, 18.90186872980919830, -50.10275203585430148 ) ) ;
#45310=CARTESIAN_POINT ( 'NONE',  ( 50.31596467094429670, -49.96707859667039742, -76.14999999999999147 ) ) ;
#45311=EDGE_CURVE ( 'NONE', #13640, #4297, #9744, .T. ) ;
#45315=EDGE_CURVE ( 'NONE', #24832, #6439, #49455, .T. ) ;
#45316=CARTESIAN_POINT ( 'NONE',  ( 53.67452698258109933, -48.64253627208800168, -26.37822025900069889 ) ) ;
#45317=CARTESIAN_POINT ( 'NONE',  ( 68.13393739769769297, 18.72622661238300168, -73.39853292320978539 ) ) ;
#45320=CARTESIAN_POINT ( 'NONE',  ( 45.07858682377059978, -46.11248607424209922, -9.026855431852869316 ) ) ;
#45322=EDGE_CURVE ( 'NONE', #16107, #47514, #34825, .T. ) ;
#45324=CARTESIAN_POINT ( 'NONE',  ( 14.05644112269600043, -51.15811488272049701, -22.83288693232809763 ) ) ;
#45325=CARTESIAN_POINT ( 'NONE',  ( 53.68554366443980541, 19.91410632359709965, -75.73797465767289339 ) ) ;
#45326=CARTESIAN_POINT ( 'NONE',  ( 47.24348367421029593, -54.32908577617870094, -75.29143818916560349 ) ) ;
#45327=EDGE_LOOP ( 'NONE', ( #22967, #29891, #50328, #28587, #25624, #30426 ) ) ;
#45328=CARTESIAN_POINT ( 'NONE',  ( 56.08436867299899831, 14.47011214112430011, -17.76910799214320136 ) ) ;
#45332=CARTESIAN_POINT ( 'NONE',  ( 12.40732551566485320, 34.15351444851818030, -23.57257803396428386 ) ) ;
#45333=ORIENTED_EDGE ( 'NONE', *, *, #43822, .T. ) ;
#45334=CARTESIAN_POINT ( 'NONE',  ( 46.85154411375850714, 22.40880507094490071, -75.96071349691810326 ) ) ;
#45337=CARTESIAN_POINT ( 'NONE',  ( 75.16192729188773569, -29.52942022316926440, -11.85564034879345741 ) ) ;
#45344=CARTESIAN_POINT ( 'NONE',  ( 61.23052733764490085, 14.02714310753309945, -46.65867039562650120 ) ) ;
#45346=CARTESIAN_POINT ( 'NONE',  ( -31.82194261889170050, -25.03117784670399715, -55.69495912570319973 ) ) ;
#45347=ORIENTED_EDGE ( 'NONE', *, *, #33917, .F. ) ;
#45348=TOROIDAL_SURFACE ( 'NONE', #32735, 47.00000000000000000, 3.000000000000000000 ) ;
#45349=CARTESIAN_POINT ( 'NONE',  ( 52.93112654626390423, -49.60820240547079862, -48.77840571416800231 ) ) ;
#45352=CARTESIAN_POINT ( 'NONE',  ( 57.40499924366620377, -45.30275284725809826, -25.91811620706180008 ) ) ;
#45353=CARTESIAN_POINT ( 'NONE',  ( 75.04939620295748171, -15.61618894467929941, -11.30491871076499955 ) ) ;
#45354=CARTESIAN_POINT ( 'NONE',  ( 57.48164938133449908, 13.89721140088779983, -25.54051126100410229 ) ) ;
#45357=CARTESIAN_POINT ( 'NONE',  ( 50.23538082579219832, 18.53774256725959901, -76.14999999999999147 ) ) ;
#45358=CARTESIAN_POINT ( 'NONE',  ( 53.21058286982849950, 18.26096715473390120, -49.03901014878070441 ) ) ;
#45360=CARTESIAN_POINT ( 'NONE',  ( 60.71739103784720015, -45.52836762685870298, -47.07893917820750573 ) ) ;
#45361=CARTESIAN_POINT ( 'NONE',  ( 68.66192157695549270, -45.11618894467940066, -13.19177143207549996 ) ) ;
#45362=ORIENTED_EDGE ( 'NONE', *, *, #31656, .F. ) ;
#45365=CARTESIAN_POINT ( 'NONE',  ( 47.39313543291059716, -54.66174527355829582, -54.87093675547399840 ) ) ;
#45368=CARTESIAN_POINT ( 'NONE',  ( 58.69128839982990087, 16.72420414854200033, -50.02955822931539132 ) ) ;
#45369=CARTESIAN_POINT ( 'NONE',  ( 52.96846354095290366, 18.35586996326500042, -48.76456332840290031 ) ) ;
#45375=CARTESIAN_POINT ( 'NONE',  ( 9.275121881254090539, -63.12602292003808913, -46.53341764687979776 ) ) ;
#45377=EDGE_LOOP ( 'NONE', ( #48267, #44201, #28545, #20530, #40919, #51041, #43062, #21531 ) ) ;
#45379=CARTESIAN_POINT ( 'NONE',  ( 84.25370905163079271, 12.95080358240966589, -47.43624044227698278 ) ) ;
#45381=EDGE_CURVE ( 'NONE', #5682, #19762, #29472, .T. ) ;
#45382=CARTESIAN_POINT ( 'NONE',  ( 51.52597262436339776, 19.39045939329939827, -76.24693439086530589 ) ) ;
#45383=EDGE_LOOP ( 'NONE', ( #42403, #2778, #4566, #34138, #9123 ) ) ;
#45385=CARTESIAN_POINT ( 'NONE',  ( 61.28610861176739633, 13.99802266614350010, -46.54508491471729315 ) ) ;
#45390=LINE ( 'NONE', #9495, #16250 ) ;
#45392=ORIENTED_EDGE ( 'NONE', *, *, #29794, .T. ) ;
#45393=AXIS2_PLACEMENT_3D ( 'NONE', #41396, #40881, #33266 ) ;
#45394=CARTESIAN_POINT ( 'NONE',  ( 56.86403139865790024, -45.97907083540439999, -26.24559160732940200 ) ) ;
#45396=CIRCLE ( 'NONE', #4334, 36.00000000000000000 ) ;
#45397=CARTESIAN_POINT ( 'NONE',  ( 52.10267379959660161, 1.883811054221469883, -20.65000000000000213 ) ) ;
#45398=CARTESIAN_POINT ( 'NONE',  ( 14.33270604179080010, 20.31584378320569684, -75.38352342698830455 ) ) ;
#45399=ADVANCED_FACE ( 'NONE', ( #4629 ), #16613, .F. ) ;
#45403=EDGE_LOOP ( 'NONE', ( #15655, #38827, #27941, #15445, #50021 ) ) ;
#45404=CARTESIAN_POINT ( 'NONE',  ( 54.23558483962950305, -48.00900124132819258, -26.19310004703979899 ) ) ;
#45405=CARTESIAN_POINT ( 'NONE',  ( 16.44553025965039694, -51.11619093951029669, -20.85618808646060174 ) ) ;
#45406=CARTESIAN_POINT ( 'NONE',  ( 6.676100005714199703, 28.78052395729680057, -12.44386222061440073 ) ) ;
#45409=ORIENTED_EDGE ( 'NONE', *, *, #7052, .T. ) ;
#45410=( BOUNDED_SURFACE ( )  B_SPLINE_SURFACE ( 2, 2, ( 
 ( #6258, #5737, #5997, #34263, #34010, #50287, #14374, #26148, #10189 ),
 ( #10450, #9423, #2065, #38225, #46363, #30340, #41374, #13607, #22216 ),
 ( #26403, #13859, #29816, #38483, #45833, #2319, #21696, #9667, #45317 ),
 ( #18041, #49767, #18291, #42424, #5488, #50539, #37704, #6514, #22474 ),
 ( #17782, #2583, #18558, #34534, #29312, #25884, #21956, #25373, #21446 ) ),
 .UNSPECIFIED., .F., .T., .T. ) 
 B_SPLINE_SURFACE_WITH_KNOTS ( ( 3, 2, 3 ),
 ( 3, 2, 2, 2, 3 ),
 ( -0.003205554297748039981, 0.8238407534185530068, 1.650887061134849843 ),
 ( -3.141592653589790007, -1.570796326794899889, 0.000000000000000000, 1.570796326794899889, 3.141592653589790007 ),
 .UNSPECIFIED. ) 
 GEOMETRIC_REPRESENTATION_ITEM ( )  RATIONAL_B_SPLINE_SURFACE ( (
 ( 1.000000000000000000, 0.7071067811865480168, 1.000000000000000000, 0.7071067811865480168, 1.000000000000000000, 0.7071067811865480168, 1.000000000000000000, 0.7071067811865480168, 1.000000000000000000),
 ( 0.9157107718030679244, 0.6475052963475169676, 0.9157107718030679244, 0.6475052963475169676, 0.9157107718030679244, 0.6475052963475169676, 0.9157107718030679244, 0.6475052963475169676, 0.9157107718030679244),
 ( 1.000000000000000000, 0.7071067811865480168, 1.000000000000000000, 0.7071067811865480168, 1.000000000000000000, 0.7071067811865480168, 1.000000000000000000, 0.7071067811865480168, 1.000000000000000000),
 ( 0.9157107718030469412, 0.6475052963475019796, 0.9157107718030469412, 0.6475052963475019796, 0.9157107718030469412, 0.6475052963475019796, 0.9157107718030469412, 0.6475052963475019796, 0.9157107718030469412),
 ( 1.000000000000000000, 0.7071067811865480168, 1.000000000000000000, 0.7071067811865480168, 1.000000000000000000, 0.7071067811865480168, 1.000000000000000000, 0.7071067811865480168, 1.000000000000000000) ) ) 
 REPRESENTATION_ITEM ( '' )  SURFACE ( )  );
#45411=CARTESIAN_POINT ( 'NONE',  ( -6.536610114769960234, -46.12166273162970498, -4.851352225809789864 ) ) ;
#45412=B_SPLINE_CURVE_WITH_KNOTS ( 'NONE', 3,
 ( #32061, #36267, #377, #16359, #40466, #4561, #20531, #44659, #8764, #24713, #40730, #17404, #41505, #49389, #1418, #33372, #33631, #13485, #29444 ),
 .UNSPECIFIED., .F., .F.,
 ( 4, 2, 2, 1, 1, 2, 2, 1, 1, 1, 2, 4 ),
 ( 0.000000000000000000, 0.2499999999999918954, 0.3124999999999898970, 0.3281249999999893419, 0.3320312499999892308, 0.3330078124999892308, 0.3339843749999891753, 0.3359374999999891753, 0.3437499999999892863, 0.3749999999999897859, 0.4999999999999917843, 1.000000000000000000 ),
 .UNSPECIFIED. ) ;
#45413=CARTESIAN_POINT ( 'NONE',  ( 47.54190215014880039, 23.33258332477480224, -54.75916635913850428 ) ) ;
#45415=CARTESIAN_POINT ( 'NONE',  ( 56.50435945713609698, -45.38311456361396523, -25.29338994599695667 ) ) ;
#45417=CARTESIAN_POINT ( 'NONE',  ( 57.24929572629130092, -50.61618894467930119, -53.91492775910359114 ) ) ;
#45418=CARTESIAN_POINT ( 'NONE',  ( 11.06646955189519943, 33.78253783233920160, -17.18453609578200059 ) ) ;
#45420=CARTESIAN_POINT ( 'NONE',  ( 52.98014233026830055, 18.34975111832529748, -48.77045026161920305 ) ) ;
#45421=CARTESIAN_POINT ( 'NONE',  ( 15.05440318628160057, -53.11618894467930119, -76.14999999999999147 ) ) ;
#45422=CARTESIAN_POINT ( 'NONE',  ( 55.20159258013029557, -48.56083622538359634, -48.75785604020860120 ) ) ;
#45423=DIRECTION ( 'NONE',  ( 0.000000000000000000, 0.000000000000000000, -1.000000000000000000 ) ) ;
#45425=CARTESIAN_POINT ( 'NONE',  ( 56.30248980166020090, 19.39266325063019991, -52.97169149132179911 ) ) ;
#45428=CARTESIAN_POINT ( 'NONE',  ( 52.06789743686220362, 13.88381105532070059, -11.75767006323859931 ) ) ;
#45429=EDGE_LOOP ( 'NONE', ( #6780, #901, #1091, #46755 ) ) ;
#45431=CARTESIAN_POINT ( 'NONE',  ( 9.739676515705429694, 32.00768368828209987, -46.29753770347090125 ) ) ;
#45433=CARTESIAN_POINT ( 'NONE',  ( 45.24668088971260005, 13.87996455531310147, -7.238505014500240087 ) ) ;
#45434=B_SPLINE_CURVE_WITH_KNOTS ( 'NONE', 3,
 ( #28183, #37102, #8807, #36568, #16660, #9337, #40769, #1199, #4600, #32879, #44184, #17191 ),
 .UNSPECIFIED., .F., .F.,
 ( 4, 2, 2, 2, 2, 4 ),
 ( 0.2986826963453840245, 0.3113669956202789746, 0.6672149786996869336, 0.8896199681243159851, 1.000822462836630011, 1.104809710335580064 ),
 .UNSPECIFIED. ) ;
#45436=CARTESIAN_POINT ( 'NONE',  ( 17.85627069094109842, 20.07361457936550053, -75.01675372117850316 ) ) ;
#45437=VERTEX_POINT ( 'NONE', #42618 ) ;
#45438=ORIENTED_EDGE ( 'NONE', *, *, #21884, .F. ) ;
#45439=CARTESIAN_POINT ( 'NONE',  ( 52.82975622904280755, -49.66092049964720445, -48.47378032971909789 ) ) ;
#45440=ORIENTED_EDGE ( 'NONE', *, *, #39899, .T. ) ;
#45441=CARTESIAN_POINT ( 'NONE',  ( 10.96794134783359986, -64.35858938242169813, -45.78400131938840190 ) ) ;
#45442=CARTESIAN_POINT ( 'NONE',  ( 56.56917054403719902, -45.93657512408730526, -26.17243226664860245 ) ) ;
#45445=CARTESIAN_POINT ( 'NONE',  ( 61.58832133341670101, 13.92430514912590134, -46.73588551253889989 ) ) ;
#45449=EDGE_CURVE ( 'NONE', #37059, #18021, #30534, .T. ) ;
#45451=CARTESIAN_POINT ( 'NONE',  ( 53.63777509634339680, -45.61032762683289832, -14.62067372278509936 ) ) ;
#45453=DIRECTION ( 'NONE',  ( 0.000000000000000000, 0.000000000000000000, -1.000000000000000000 ) ) ;
#45456=CARTESIAN_POINT ( 'NONE',  ( 47.08252998902620590, -54.52665379529010181, -75.17661032366730467 ) ) ;
#45458=CARTESIAN_POINT ( 'NONE',  ( 50.03007040746459921, -48.61618894467930119, -76.14999999999999147 ) ) ;
#45460=CARTESIAN_POINT ( 'NONE',  ( 16.13393739769620083, -15.61618894467929941, -10.44999999999999929 ) ) ;
#45463=CARTESIAN_POINT ( 'NONE',  ( 6.488481933958597736, -58.66853282520657586, -10.99658928318876328 ) ) ;
#45464=CARTESIAN_POINT ( 'NONE',  ( 61.58992610407029389, 13.89565648923180063, -28.08969723792819906 ) ) ;
#45466=VERTEX_POINT ( 'NONE', #22414 ) ;
#45467=DIRECTION ( 'NONE',  ( 1.000000000000000000, 0.000000000000000000, 0.000000000000000000 ) ) ;
#45468=CARTESIAN_POINT ( 'NONE',  ( -9.951751048134941158, -43.31993781838389879, -6.292775219062558989 ) ) ;
#45469=CARTESIAN_POINT ( 'NONE',  ( 75.44426646237340606, -42.28045139918640416, -13.24736862165440066 ) ) ;
#45471=CARTESIAN_POINT ( 'NONE',  ( 11.06646970394739959, -65.01491572843740130, -17.18453585839250053 ) ) ;
#45473=CARTESIAN_POINT ( 'NONE',  ( 47.53479508864854353, -54.39911497212986546, -74.95188530368821489 ) ) ;
#45474=CARTESIAN_POINT ( 'NONE',  ( 48.88899477876550037, -53.95617853557810406, -54.86330888163660546 ) ) ;
#45475=CARTESIAN_POINT ( 'NONE',  ( 78.22251691734010137, -33.11618894467940066, -20.65000000000000213 ) ) ;
#45479=PLANE ( 'NONE',  #41081 ) ;
#45480=CARTESIAN_POINT ( 'NONE',  ( 18.86791100745899996, -51.78681560013630047, -74.34711752987139732 ) ) ;
#45486=VERTEX_POINT ( 'NONE', #22671 ) ;
#45488=CARTESIAN_POINT ( 'NONE',  ( 60.30540951500689317, -45.82523471321780306, -47.61343627861160144 ) ) ;
#45490=CARTESIAN_POINT ( 'NONE',  ( 42.93197233849409855, 11.32569894967160096, -3.187564294433600232 ) ) ;
#45492=CARTESIAN_POINT ( 'NONE',  ( 1.014378609951400056, -15.61618894467929941, -6.721843382729280059 ) ) ;
#45493=CARTESIAN_POINT ( 'NONE',  ( 51.98443728612009096, -51.36758245232200437, -75.98853294935470615 ) ) ;
#45494=DIRECTION ( 'NONE',  ( 0.6676418852213039656, 0.2329255526947077437, 0.7071067811865533459 ) ) ;
#45495=ORIENTED_EDGE ( 'NONE', *, *, #40875, .T. ) ;
#45500=CARTESIAN_POINT ( 'NONE',  ( 61.35985704537380059, -45.28492337451550043, -47.11846253721390099 ) ) ;
#45501=CARTESIAN_POINT ( 'NONE',  ( 52.84261786122310411, -49.69241002008439523, -48.97154812789309375 ) ) ;
#45511=CARTESIAN_POINT ( 'NONE',  ( 52.56495426071009547, -52.43765526798460286, -54.45623365677440120 ) ) ;
#45512=CARTESIAN_POINT ( 'NONE',  ( 58.92073396209919878, -3.116188944679349593, -18.64999999999999858 ) ) ;
#45513=VERTEX_POINT ( 'NONE', #9863 ) ;
#45515=CARTESIAN_POINT ( 'NONE',  ( 52.36900553906810529, -50.72407173529079927, -76.35261119407400088 ) ) ;
#45516=CARTESIAN_POINT ( 'NONE',  ( 60.56101234812630452, 14.37792091447689913, -47.14853648965690525 ) ) ;
#45520=CARTESIAN_POINT ( 'NONE',  ( 41.46797725167870396, 13.65730434570830099, -5.587150232416230544 ) ) ;
#45521=CARTESIAN_POINT ( 'NONE',  ( 43.83393256038859676, -43.46487882048660367, -5.056952191481060233 ) ) ;
#45522=CARTESIAN_POINT ( 'NONE',  ( 68.13393739769840352, -50.61618894467879670, -73.25000000000220268 ) ) ;
#45523=CARTESIAN_POINT ( 'NONE',  ( -7.973795448866470181, 13.91176078833520080, -5.720958296299230028 ) ) ;
#45526=B_SPLINE_CURVE_WITH_KNOTS ( 'NONE', 3,
 ( #29609, #32747, #13397, #36970, #33544, #45095, #48774, #1066, #17063, #25411, #1332, #49039, #9712, #29355 ),
 .UNSPECIFIED., .F., .F.,
 ( 4, 2, 2, 2, 2, 2, 4 ),
 ( 0.000000000000000000, 0.004139501987503274756, 0.1286220642390652202, 0.3277941638415642900, 0.6464695232055646112, 0.9209749313270280124, 1.000000000000000000 ),
 .UNSPECIFIED. ) ;
#45527=CARTESIAN_POINT ( 'NONE',  ( 66.28213684734230071, 1.842697259673649945, -19.91087727140369878 ) ) ;
#45528=ORIENTED_EDGE ( 'NONE', *, *, #39261, .T. ) ;
#45529=CARTESIAN_POINT ( 'NONE',  ( 14.98839781681999916, -52.93030938277399855, -76.14999999999999147 ) ) ;
#45530=CARTESIAN_POINT ( 'NONE',  ( 47.18324198357289845, -54.80726809202429450, -54.61058319554170026 ) ) ;
#45533=CARTESIAN_POINT ( 'NONE',  ( 56.55522355860080097, -46.21195502513410247, -26.26695352263039851 ) ) ;
#45536=CARTESIAN_POINT ( 'NONE',  ( 10.95445192191350081, 33.82498797628089449, -17.59525104008959673 ) ) ;
#45540=CARTESIAN_POINT ( 'NONE',  ( 48.26248612645670022, 22.97322273838690165, -54.82342444101630008 ) ) ;
#45544=CARTESIAN_POINT ( 'NONE',  ( 82.45630311851421368, 13.86034003618500066, -46.38988467804559690 ) ) ;
#45547=CARTESIAN_POINT ( 'NONE',  ( 83.16755290732228900, 13.77093069207690057, -46.93255211562899376 ) ) ;
#45548=CARTESIAN_POINT ( 'NONE',  ( 55.44576274181309827, 15.28165783319309945, -25.46131564888750276 ) ) ;
#45550=CARTESIAN_POINT ( 'NONE',  ( 11.28671401888813719, 33.77463329229922806, -16.86100853830620849 ) ) ;
#45551=CARTESIAN_POINT ( 'NONE',  ( 55.74013705948259911, -45.13221362293969463, -14.86594848831030014 ) ) ;
#45552=DIRECTION ( 'NONE',  ( 0.000000000000000000, 0.7071067811865492381, -0.7071067811865457964 ) ) ;
#45554=VERTEX_POINT ( 'NONE', #50729 ) ;
#45555=VERTEX_POINT ( 'NONE', #25817 ) ;
#45556=CARTESIAN_POINT ( 'NONE',  ( 12.15898433498739983, -65.06882048843399957, -16.45263499446509670 ) ) ;
#45557=CARTESIAN_POINT ( 'NONE',  ( 10.93504234667139841, 32.38329808718709302, -44.92331353542380157 ) ) ;
#45561=CARTESIAN_POINT ( 'NONE',  ( 51.23436977250750601, 3.565853774335477233, -76.55134428789229162 ) ) ;
#45567=CARTESIAN_POINT ( 'NONE',  ( 51.42675427039450398, 19.81429176188510155, -50.04217728894000317 ) ) ;
#45568=EDGE_CURVE ( 'NONE', #50146, #37013, #38885, .T. ) ;
#45569=CARTESIAN_POINT ( 'NONE',  ( 64.91976642084398463, -1.113755444385029936, -16.49433693280849766 ) ) ;
#45570=CARTESIAN_POINT ( 'NONE',  ( 51.30983199192319688, -49.53152618182630107, -76.46178133275020627 ) ) ;
#45574=CARTESIAN_POINT ( 'NONE',  ( 14.56242188612286448, -16.75796179725742974, -7.393828452885189861 ) ) ;
#45579=CARTESIAN_POINT ( 'NONE',  ( 14.08262962865900114, -51.14923377493139611, -22.65114920387059883 ) ) ;
#45580=CARTESIAN_POINT ( 'NONE',  ( 56.44450715656099504, 19.45673396471810079, -74.92602466682960483 ) ) ;
#45582=CARTESIAN_POINT ( 'NONE',  ( 47.53479509476479592, -54.39911496936699820, -74.95188530402140259 ) ) ;
#45584=CARTESIAN_POINT ( 'NONE',  ( 56.35090670788920164, 14.15977167711390017, -17.04118023804650051 ) ) ;
#45586=CARTESIAN_POINT ( 'NONE',  ( 57.25486276105269923, -50.42116208795279420, -53.00955584233389573 ) ) ;
#45590=CARTESIAN_POINT ( 'NONE',  ( 47.43576539955360261, 23.40338254006309882, -74.19735651161070678 ) ) ;
#45592=CARTESIAN_POINT ( 'NONE',  ( 75.16209103024675642, -29.53953162302573787, -11.85643004527870481 ) ) ;
#45600=CARTESIAN_POINT ( 'NONE',  ( 61.06807839133419691, 14.11225480744460015, -46.83711763858070043 ) ) ;
#45601=CARTESIAN_POINT ( 'NONE',  ( -12.15512026600820050, 24.36382048915779919, -51.32444474606599982 ) ) ;
#45603=CARTESIAN_POINT ( 'NONE',  ( 52.87179757757409959, -49.64089313818260507, -48.76566979334150176 ) ) ;
#45605=CARTESIAN_POINT ( 'NONE',  ( 60.62404192237740119, -45.11617399124450145, -26.47736735333209879 ) ) ;
#45607=CARTESIAN_POINT ( 'NONE',  ( 57.55135366195850111, 13.89752427999699869, -25.54668255911809993 ) ) ;
#45609=CARTESIAN_POINT ( 'NONE',  ( 50.36549662992300114, 18.84323467693539911, -76.14999999999999147 ) ) ;
#45610=CARTESIAN_POINT ( 'NONE',  ( 53.05460983997079438, 18.33279354663559957, -48.99361253809119887 ) ) ;
#45612=FACE_OUTER_BOUND ( 'NONE', #21455, .T. ) ;
#45613=CARTESIAN_POINT ( 'NONE',  ( 63.87213755537349158, -43.73219550796380162, -10.18606854234780101 ) ) ;
#45617=CARTESIAN_POINT ( 'NONE',  ( 47.44110378858790256, -54.62521372874980585, -54.71913897434770035 ) ) ;
#45620=CARTESIAN_POINT ( 'NONE',  ( 11.77545672746500216, -65.42605939611310362, -17.95294975585129649 ) ) ;
#45624=CYLINDRICAL_SURFACE ( 'NONE', #9260, 1.999999999999970246 ) ;
#45627=VECTOR ( 'NONE', #26089, 1000.000000000000000 ) ;
#45628=CARTESIAN_POINT ( 'NONE',  ( 8.812257860101720297, -63.26324333009419831, -46.67111697731629505 ) ) ;
#45629=CARTESIAN_POINT ( 'NONE',  ( 82.13853704237929776, 14.40950277491920062, -47.72348187592560009 ) ) ;
#45630=ORIENTED_EDGE ( 'NONE', *, *, #47568, .F. ) ;
#45631=EDGE_CURVE ( 'NONE', #49388, #47619, #45869, .T. ) ;
#45635=CARTESIAN_POINT ( 'NONE',  ( 51.20054136575519976, 19.52715359417319974, -76.16661699907028549 ) ) ;
#45637=ORIENTED_EDGE ( 'NONE', *, *, #19580, .F. ) ;
#45638=CARTESIAN_POINT ( 'NONE',  ( 8.133937397696209715, 31.88305279702909800, -43.74348518090240390 ) ) ;
#45646=B_SPLINE_CURVE_WITH_KNOTS ( 'NONE', 3,
 ( #1649, #50640, #25730, #42263, #6362, #18399, #10556, #34378, #1909, #17888, #33859, #38072 ),
 .UNSPECIFIED., .F., .F.,
 ( 4, 2, 2, 2, 2, 4 ),
 ( 0.000000000000000000, 0.2528991456834384088, 0.3793487185251589455, 0.4425735049460208237, 0.4741858981564516240, 0.5057982913668825908 ),
 .UNSPECIFIED. ) ;
#45648=CARTESIAN_POINT ( 'NONE',  ( 62.09157612670949788, -43.11618894467930119, -65.34607522167520699 ) ) ;
#45650=CARTESIAN_POINT ( 'NONE',  ( 52.57435367313230046, -49.85246693219060177, -48.51308846454130475 ) ) ;
#45652=CARTESIAN_POINT ( 'NONE',  ( 14.35346408579549937, 19.90988454773659910, -74.52171359303420672 ) ) ;
#45654=CARTESIAN_POINT ( 'NONE',  ( 45.28516362987719646, -45.38267274594659995, -8.309856332598471340 ) ) ;
#45655=DIRECTION ( 'NONE',  ( 0.000000000000000000, 0.000000000000000000, -1.000000000000000000 ) ) ;
#45658=CARTESIAN_POINT ( 'NONE',  ( 53.66151296940279991, -48.70894861344299898, -26.71281138883589890 ) ) ;
#45660=CARTESIAN_POINT ( 'NONE',  ( 14.50346589895649885, -50.97187126869069829, -21.59847332898880268 ) ) ;
#45661=CARTESIAN_POINT ( 'NONE',  ( 7.782855510348779760, 30.62954478035329942, -15.35487569384610040 ) ) ;
#45663=EDGE_CURVE ( 'NONE', #34738, #48296, #23946, .T. ) ;
#45665=CARTESIAN_POINT ( 'NONE',  ( 50.20812736443180313, 14.95961625580089915, -12.60693812980999873 ) ) ;
#45666=VERTEX_POINT ( 'NONE', #42877 ) ;
#45667=CARTESIAN_POINT ( 'NONE',  ( -8.360280049586719997, -44.70025899903389899, -5.480459871618819534 ) ) ;
#45669=CARTESIAN_POINT ( 'NONE',  ( 47.57151154772099488, 23.30286101566669998, -54.67895741658460196 ) ) ;
#45670=DIRECTION ( 'NONE',  ( -6.008901426489750921E-29, 1.000000000000000000, 1.065814103640290065E-14 ) ) ;
#45672=CARTESIAN_POINT ( 'NONE',  ( 61.01745591375750877, 14.14199598592190021, -47.00094549329430293 ) ) ;
#45673=CARTESIAN_POINT ( 'NONE',  ( 42.70036220023900597, 12.92082705698970102, -5.071714814876659538 ) ) ;
#45674=EDGE_CURVE ( 'NONE', #26643, #38464, #35518, .T. ) ;
#45675=FACE_OUTER_BOUND ( 'NONE', #15136, .T. ) ;
#45676=CARTESIAN_POINT ( 'NONE',  ( 52.84340576260750311, 18.42139123722009941, -48.59551021507399327 ) ) ;
#45679=DIRECTION ( 'NONE',  ( -0.4640893551880601597, 0.8857883891771953788, 0.000000000000000000 ) ) ;
#45681=CARTESIAN_POINT ( 'NONE',  ( 55.72751318460259995, 19.85814786334140081, -53.82427627174779872 ) ) ;
#45683=CARTESIAN_POINT ( 'NONE',  ( 11.93810467663310071, -65.43945453151620484, -17.87564855520800222 ) ) ;
#45686=CARTESIAN_POINT ( 'NONE',  ( 19.82948959376360776, 23.31066016154319698, -17.79040102455563854 ) ) ;
#45687=CARTESIAN_POINT ( 'NONE',  ( 10.97995777053410116, 32.18935651174339796, -44.74773172946899535 ) ) ;
#45690=CARTESIAN_POINT ( 'NONE',  ( 66.23673192723569514, -31.73979966234530181, -17.49602702209859828 ) ) ;
#45692=CARTESIAN_POINT ( 'NONE',  ( 17.99229889273830096, 19.88380863237500051, -74.14994161014911356 ) ) ;
#45696=ORIENTED_EDGE ( 'NONE', *, *, #11613, .F. ) ;
#45698=CARTESIAN_POINT ( 'NONE',  ( 11.67609344190909937, -65.14710708552239282, -46.80893820645799508 ) ) ;
#45699=CARTESIAN_POINT ( 'NONE',  ( 56.61876495832499501, -45.69764771475809795, -26.04439677746109894 ) ) ;
#45701=CARTESIAN_POINT ( 'NONE',  ( 41.13393739769620794, -15.61618894467929941, 4.450000000000000178 ) ) ;
#45704=AXIS2_PLACEMENT_3D ( 'NONE', #14021, #2228, #29980 ) ;
#45706=CARTESIAN_POINT ( 'NONE',  ( 52.22793003137540069, -45.20715030507830079, -12.77863615568089983 ) ) ;
#45708=DIRECTION ( 'NONE',  ( 0.000000000000000000, 0.000000000000000000, 1.000000000000000000 ) ) ;
#45709=CARTESIAN_POINT ( 'NONE',  ( 16.58032161481230204, 19.88381278803589680, -20.45514663783420062 ) ) ;
#45713=CARTESIAN_POINT ( 'NONE',  ( 46.97135903472899798, -54.28212950231179690, -75.52157719890121257 ) ) ;
#45714=CARTESIAN_POINT ( 'NONE',  ( 66.89072473720391088, 12.48801267837889917, -11.01669209824130036 ) ) ;
#45715=EDGE_CURVE ( 'NONE', #9983, #7868, #7749, .T. ) ;
#45717=CARTESIAN_POINT ( 'NONE',  ( 54.44698107792579833, 13.88381105532070059, -13.49511294515519921 ) ) ;
#45719=CARTESIAN_POINT ( 'NONE',  ( 51.26685560572850164, 19.79157626071939902, -76.14349090804589082 ) ) ;
#45721=CARTESIAN_POINT ( 'NONE',  ( 60.27114510410760317, 14.00925828241220117, -26.79014729864100275 ) ) ;
#45725=CARTESIAN_POINT ( 'NONE',  ( 57.55751162087899786, 18.85811933572220056, -52.57651812407429759 ) ) ;
#45726=FACE_OUTER_BOUND ( 'NONE', #7324, .T. ) ;
#45733=CARTESIAN_POINT ( 'NONE',  ( 12.57902832706879970, 19.10565774180280130, -21.19240428151960032 ) ) ;
#45736=CARTESIAN_POINT ( 'NONE',  ( 56.39270785951039500, 19.29512406318060158, -52.86271188469099513 ) ) ;
#45739=CARTESIAN_POINT ( 'NONE',  ( 75.76193235035715645, -43.34893572151489849, -13.50695346075995573 ) ) ;
#45740=CARTESIAN_POINT ( 'NONE',  ( 17.91323993525340086, -51.14554741935710069, -74.54427505469620030 ) ) ;
#45747=FACE_OUTER_BOUND ( 'NONE', #32426, .T. ) ;
#45748=CARTESIAN_POINT ( 'NONE',  ( 60.40987110273919569, -45.83497225692880050, -47.72180312432629989 ) ) ;
#45753=CARTESIAN_POINT ( 'NONE',  ( 52.20740540343859237, -51.40483972235690402, -75.93239679552310406 ) ) ;
#45754=CARTESIAN_POINT ( 'NONE',  ( 40.71243489632720269, -45.33518156949239852, -5.692226379959530291 ) ) ;
#45757=ORIENTED_EDGE ( 'NONE', *, *, #23122, .T. ) ;
#45760=CARTESIAN_POINT ( 'NONE',  ( 61.19893174391710033, -45.31225206941749661, -47.06093154577280302 ) ) ;
#45761=CARTESIAN_POINT ( 'NONE',  ( 53.23936142806359584, -49.53019510929430425, -49.17934721267350540 ) ) ;
#45765=VERTEX_POINT ( 'NONE', #27132 ) ;
#45768=CARTESIAN_POINT ( 'NONE',  ( 53.42313316096070253, -52.07210377827539816, -54.29429654136570349 ) ) ;
#45772=CARTESIAN_POINT ( 'NONE',  ( 52.02214954632180621, -50.31644395759909827, -76.54113481940019881 ) ) ;
#45773=CARTESIAN_POINT ( 'NONE',  ( 60.54707010150900715, 14.38522564811469984, -47.15409972330730426 ) ) ;
#45777=EDGE_CURVE ( 'NONE', #22647, #14356, #709, .T. ) ;
#45779=CARTESIAN_POINT ( 'NONE',  ( 41.47580373046699975, 13.55635338172790050, -5.433826806151940580 ) ) ;
#45780=CARTESIAN_POINT ( 'NONE',  ( 41.94994391203700701, -43.92468623023520280, -4.524181474801060254 ) ) ;
#45783=CARTESIAN_POINT ( 'NONE',  ( -6.178851728588689696, 15.46435443030710033, -5.588668033364348808 ) ) ;
#45785=DIRECTION ( 'NONE',  ( -0.2260571801428189198, 0.000000000000000000, 0.9741140340359936145 ) ) ;
#45786=CARTESIAN_POINT ( 'NONE',  ( 66.32948755469080027, 1.142895182770250040, -18.17795024893420219 ) ) ;
#45787=ORIENTED_EDGE ( 'NONE', *, *, #2799, .F. ) ;
#45788=CARTESIAN_POINT ( 'NONE',  ( 14.75663690171680109, -52.86216653946310373, -76.12493046668770091 ) ) ;
#45790=CARTESIAN_POINT ( 'NONE',  ( 47.18324198357289845, -54.80726809202429450, -54.61058319554170026 ) ) ;
#45792=DIRECTION ( 'NONE',  ( 1.000000000000000000, 0.000000000000000000, 0.000000000000000000 ) ) ;
#45797=CARTESIAN_POINT ( 'NONE',  ( 47.80730873599560482, -54.40538902786819619, -54.73352113645039907 ) ) ;
#45799=FACE_OUTER_BOUND ( 'NONE', #7216, .T. ) ;
#45800=CARTESIAN_POINT ( 'NONE',  ( 48.01952589465019372, 23.10709900649499815, -54.91785799752790354 ) ) ;
#45805=LINE ( 'NONE', #34504, #44667 ) ;
#45806=VECTOR ( 'NONE', #32, 1000.000000000000000 ) ;
#45809=CARTESIAN_POINT ( 'NONE',  ( 84.44066163939218939, 12.08519577684469937, -47.44491107334449964 ) ) ;
#45810=CARTESIAN_POINT ( 'NONE',  ( 42.93197233849399908, -42.55807683903039162, -3.187564294433600232 ) ) ;
#45813=CARTESIAN_POINT ( 'NONE',  ( 56.21747353221379484, -45.13074185381659476, -15.33522795547970041 ) ) ;
#45815=CARTESIAN_POINT ( 'NONE',  ( 56.61928439928508539, 14.09173447728649720, -17.93019253464870033 ) ) ;
#45816=EDGE_LOOP ( 'NONE', ( #10906, #51303 ) ) ;
#45818=CARTESIAN_POINT ( 'NONE',  ( 12.36320305068320025, -64.54682834576858852, -15.76422791927960176 ) ) ;
#45819=CARTESIAN_POINT ( 'NONE',  ( 12.21269279732720037, 34.11710210141869482, -47.01935258852740418 ) ) ;
#45822=CARTESIAN_POINT ( 'NONE',  ( 51.13862808468330456, 3.739953746215777475, -76.48488464726803215 ) ) ;
#45826=CARTESIAN_POINT ( 'NONE',  ( 52.59914051912740263, -49.82906292203490040, -48.56924359530199808 ) ) ;
#45827=CARTESIAN_POINT ( 'NONE',  ( 49.83651295974559758, 21.41060930851670108, -52.45077174872059800 ) ) ;
#45828=CARTESIAN_POINT ( 'NONE',  ( 59.39915200420649910, -2.757920925504779852, -15.68862214463160143 ) ) ;
#45829=CARTESIAN_POINT ( 'NONE',  ( 50.81500904190379941, -49.69956259698449941, -76.22412500851820027 ) ) ;
#45830=CARTESIAN_POINT ( 'NONE',  ( 60.41046171663749931, -46.68362944077280474, -48.85993508664739693 ) ) ;
#45833=CARTESIAN_POINT ( 'NONE',  ( 68.13393739769769297, 18.72622661238600017, -69.60146707679309941 ) ) ;
#45834=ORIENTED_EDGE ( 'NONE', *, *, #33711, .T. ) ;
#45838=ADVANCED_FACE ( 'NONE', ( #36535 ), #904, .F. ) ;
#45839=CARTESIAN_POINT ( 'NONE',  ( 13.29213509620739941, -50.86275351173860315, -21.61097465929019990 ) ) ;
#45840=CARTESIAN_POINT ( 'NONE',  ( 53.92402291300970063, 19.73846352820710237, -75.87933617372019057 ) ) ;
#45842=CARTESIAN_POINT ( 'NONE',  ( 47.29285256804840287, -54.09193043622850183, -75.52284329973289800 ) ) ;
#45843=ORIENTED_EDGE ( 'NONE', *, *, #13844, .T. ) ;
#45844=EDGE_CURVE ( 'NONE', #47621, #46679, #25252, .T. ) ;
#45845=CARTESIAN_POINT ( 'NONE',  ( 55.87349882819940206, 14.34368325183129933, -16.58361811465810121 ) ) ;
#45847=B_SPLINE_CURVE_WITH_KNOTS ( 'NONE', 3,
 ( #47256, #6378, #22339, #15274, #31229, #18418, #34393, #20212, #51687, #12631, #24647, #28589, #35945, #44589, #4495, #3993 ),
 .UNSPECIFIED., .F., .F.,
 ( 4, 2, 2, 2, 2, 2, 2, 4 ),
 ( 0.2986826963453430017, 0.6144977923521359742, 0.8991761887526290575, 1.077100186502939927, 1.188302685096880085, 1.410707682284769948, 1.766555677785379919, 1.779239977503060066 ),
 .UNSPECIFIED. ) ;
#45848=CARTESIAN_POINT ( 'NONE',  ( 57.32592487833510120, -50.41428338388260499, -53.00067887287889334 ) ) ;
#45849=CARTESIAN_POINT ( 'NONE',  ( 52.88344664573250498, -49.67337909505339866, -49.00461641361030019 ) ) ;
#45853=CARTESIAN_POINT ( 'NONE',  ( 46.40528337222430366, 21.74482207379540100, -76.14872548090239945 ) ) ;
#45855=CARTESIAN_POINT ( 'NONE',  ( 19.98170351883816309, -54.97933364285017888, -18.57148459735737234 ) ) ;
#45856=CARTESIAN_POINT ( 'NONE',  ( 75.15070962298389645, -28.81814377174942621, -11.80138244787392665 ) ) ;
#45859=CARTESIAN_POINT ( 'NONE',  ( 14.16187783161290170, -50.35113599914600258, -20.85710678118659800 ) ) ;
#45860=EDGE_CURVE ( 'NONE', #38938, #15849, #33112, .T. ) ;
#45861=DIRECTION ( 'NONE',  ( 0.000000000000000000, 8.635067969306036542E-13, 1.000000000000000000 ) ) ;
#45862=LINE ( 'NONE', #2088, #14262 ) ;
#45866=CARTESIAN_POINT ( 'NONE',  ( 61.23360558058650582, 14.02553047523030116, -46.60520175737810433 ) ) ;
#45867=CARTESIAN_POINT ( 'NONE',  ( -25.59424942068570275, 9.591493339629250769, -54.31183179444199993 ) ) ;
#45868=ORIENTED_EDGE ( 'NONE', *, *, #16974, .F. ) ;
#45869=( BOUNDED_CURVE ( )  B_SPLINE_CURVE ( 3, ( #31562, #39460, #30792, #47076 ),
 .UNSPECIFIED., .F., .T. ) 
 B_SPLINE_CURVE_WITH_KNOTS ( ( 4, 4 ),
 ( 0.000000000000000000, 0.9725514443758180860 ),
 .UNSPECIFIED. ) 
 CURVE ( )  GEOMETRIC_REPRESENTATION_ITEM ( )  RATIONAL_B_SPLINE_CURVE ( ( 1.000000000000000000, 0.9227196513546164214, 0.9227196513546164214, 1.000000000000000000 ) ) 
 REPRESENTATION_ITEM ( '' )  );
#45870=CARTESIAN_POINT ( 'NONE',  ( 52.87376179874240734, -49.63822605030750168, -48.72414007904549749 ) ) ;
#45872=CARTESIAN_POINT ( 'NONE',  ( -11.32734370190460105, -41.88171845330919751, -19.14999999999999858 ) ) ;
#45876=CARTESIAN_POINT ( 'NONE',  ( -1.566062602303800677, -15.61618894467939889, -6.649999999999999467 ) ) ;
#45877=CARTESIAN_POINT ( 'NONE',  ( 52.68398807097789671, 18.52347269652620199, -48.59016489651170190 ) ) ;
#45878=CARTESIAN_POINT ( 'NONE',  ( 46.63833728752520358, -15.61618894467929586, 7.349999999999999645 ) ) ;
#45879=CARTESIAN_POINT ( 'NONE',  ( 60.51913464264409726, -45.63223970707090160, -47.16508087703120111 ) ) ;
#45881=EDGE_LOOP ( 'NONE', ( #51685, #2642, #49683, #41539 ) ) ;
#45883=DIRECTION ( 'NONE',  ( 0.000000000000000000, 0.000000000000000000, 1.000000000000000000 ) ) ;
#45886=CARTESIAN_POINT ( 'NONE',  ( 11.89339496835929921, -65.43604241733970639, -18.15362147994479614 ) ) ;
#45887=CARTESIAN_POINT ( 'NONE',  ( 52.84340576260759548, 18.42139123722009941, -48.59551021507390089 ) ) ;
#45888=CARTESIAN_POINT ( 'NONE',  ( 65.03603135424580728, -15.61618894467929941, -19.52361391316370032 ) ) ;
#45890=VECTOR ( 'NONE', #25042, 1000.000000000000000 ) ;
#45893=ORIENTED_EDGE ( 'NONE', *, *, #50562, .F. ) ;
#45894=CARTESIAN_POINT ( 'NONE',  ( 8.808591387964359143, -63.24239172143919774, -46.67055361988870033 ) ) ;
#45900=CARTESIAN_POINT ( 'NONE',  ( 52.80343914517980153, 19.25517939188599570, -76.73469608800270692 ) ) ;
#45901=VERTEX_POINT ( 'NONE', #12188 ) ;
#45902=DIRECTION ( 'NONE',  ( 1.000000000000000000, 0.000000000000000000, 0.000000000000000000 ) ) ;
#45907=EDGE_CURVE ( 'NONE', #5766, #39844, #21642, .T. ) ;
#45911=CARTESIAN_POINT ( 'NONE',  ( 18.71088192717838439, 20.68057025370971758, -75.01676221305848458 ) ) ;
#45913=CARTESIAN_POINT ( 'NONE',  ( 53.54323433243279595, -49.41229159844919394, -49.20622374552320366 ) ) ;
#45916=CARTESIAN_POINT ( 'NONE',  ( 14.27557369763509953, 19.88380302201240113, -74.34036667011370980 ) ) ;
#45918=CARTESIAN_POINT ( 'NONE',  ( 40.90034483661249709, -45.10436747181810091, -5.606159996611790319 ) ) ;
#45919=CARTESIAN_POINT ( 'NONE',  ( 72.13393739769620083, -15.61618894467929941, -20.65000000000000213 ) ) ;
#45920=VECTOR ( 'NONE', #2258, 1000.000000000000000 ) ;
#45922=AXIS2_PLACEMENT_3D ( 'NONE', #35367, #7856, #51365 ) ;
#45923=VERTEX_POINT ( 'NONE', #44669 ) ;
#45924=CARTESIAN_POINT ( 'NONE',  ( 55.02169238797419837, -47.04713376395680058, -25.69011823353289969 ) ) ;
#45925=CARTESIAN_POINT ( 'NONE',  ( 56.50576444368559237, -50.74247142358070306, -74.45835159213530119 ) ) ;
#45926=CARTESIAN_POINT ( 'NONE',  ( 10.69487833177709923, 33.67413918231929415, -18.00053523990690252 ) ) ;
#45930=DIRECTION ( 'NONE',  ( -0.8732394366197182567, 0.4872913772396111343, -1.665334536937735304E-16 ) ) ;
#45931=ORIENTED_EDGE ( 'NONE', *, *, #22908, .T. ) ;
#45932=CARTESIAN_POINT ( 'NONE',  ( -2.656266621570580355, -48.72136079459129832, -4.829465372056970018 ) ) ;
#45933=CARTESIAN_POINT ( 'NONE',  ( 47.45846583226310145, 23.39139597829760220, -54.90779131713600236 ) ) ;
#45936=DIRECTION ( 'NONE',  ( -1.224646799147336690E-16, 1.000000000000000000, 1.919972818367720325E-16 ) ) ;
#45937=CARTESIAN_POINT ( 'NONE',  ( 11.70209409420199975, 33.86888164218810005, -16.68277806565760102 ) ) ;
#45943=CARTESIAN_POINT ( 'NONE',  ( 55.73977427824559783, 19.85292510495689910, -53.93776639183540311 ) ) ;
#45945=CARTESIAN_POINT ( 'NONE',  ( 0.1542402430813090142, -50.99248106341759978, -19.14999999999999858 ) ) ;
#45946=DIRECTION ( 'NONE',  ( 0.000000000000000000, 0.000000000000000000, 1.000000000000000000 ) ) ;
#45948=CARTESIAN_POINT ( 'NONE',  ( 20.05501060430114180, 23.95707817317984833, -19.14226881137857106 ) ) ;
#45949=CARTESIAN_POINT ( 'NONE',  ( 11.10572504400830063, 32.22711006948190260, -44.26001407538520027 ) ) ;
#45951=CARTESIAN_POINT ( 'NONE',  ( 65.36111452216670159, -32.61132144897129592, -18.37584006277759840 ) ) ;
#45952=CARTESIAN_POINT ( 'NONE',  ( 12.69291600278502763, 24.23553010417859710, -75.52237511313917651 ) ) ;
#45955=CARTESIAN_POINT ( 'NONE',  ( 48.40744063480869386, 22.97621965999729809, -55.31593188200960043 ) ) ;
#45956=CARTESIAN_POINT ( 'NONE',  ( 49.89456891052482490, -1.537756983171397973, -15.90506407067071848 ) ) ;
#45958=CARTESIAN_POINT ( 'NONE',  ( 12.21878994645900107, -65.31006707541760647, -46.54195938077629791 ) ) ;
#45959=CARTESIAN_POINT ( 'NONE',  ( 56.98013733811719561, -45.52736395732640062, -26.04777137428060030 ) ) ;
#45963=AXIS2_PLACEMENT_3D ( 'NONE', #11041, #20352, #36339 ) ;
#45965=CIRCLE ( 'NONE', #44292, 2.700000000000230216 ) ;
#45968=CARTESIAN_POINT ( 'NONE',  ( 51.09762045080680792, -45.11618894460819718, -11.35987698341929963 ) ) ;
#45969=EDGE_CURVE ( 'NONE', #6259, #40855, #47557, .T. ) ;
#45971=CARTESIAN_POINT ( 'NONE',  ( 14.48916582607680148, 19.87152568006800024, -22.14433180932219969 ) ) ;
#45973=ADVANCED_FACE ( 'NONE', ( #8516 ), #32579, .F. ) ;
#45974=EDGE_CURVE ( 'NONE', #43315, #9983, #45084, .T. ) ;
#45976=CARTESIAN_POINT ( 'NONE',  ( 46.77981249583429957, -53.79990661969940646, -75.90649761523269490 ) ) ;
#45977=CARTESIAN_POINT ( 'NONE',  ( 60.42958242686469816, 13.88381321558630077, -10.92174602670019823 ) ) ;
#45979=CARTESIAN_POINT ( 'NONE',  ( 51.61031096252850148, 13.88381105524890025, -11.72816892371229969 ) ) ;
#45980=CARTESIAN_POINT ( 'NONE',  ( 53.46638755025719547, 20.54076140048909949, -53.27253650584940203 ) ) ;
#45983=CARTESIAN_POINT ( 'NONE',  ( 52.35627133321460036, 19.94929664549539794, -76.02218070044929732 ) ) ;
#45984=EDGE_CURVE ( 'NONE', #28507, #4867, #37568, .T. ) ;
#45985=CARTESIAN_POINT ( 'NONE',  ( 57.93647699516559868, 13.95499690129120118, -25.80740772885510026 ) ) ;
#45988=CARTESIAN_POINT ( 'NONE',  ( 15.21636614235080032, -50.60415920577569437, -15.64999998222989852 ) ) ;
#45989=CARTESIAN_POINT ( 'NONE',  ( -11.09439285730369917, -42.12527450341799806, -6.431386034134429330 ) ) ;
#45990=CARTESIAN_POINT ( 'NONE',  ( 76.62358681188410969, -34.82467708757799585, -13.75998128426440026 ) ) ;
#45992=EDGE_CURVE ( 'NONE', #47951, #51345, #14972, .T. ) ;
#45993=CARTESIAN_POINT ( 'NONE',  ( 75.01912134484176420, -45.11618894467940066, -15.00305751307385371 ) ) ;
#45995=CIRCLE ( 'NONE', #16641, 1.999999999999999778 ) ;
#45997=AXIS2_PLACEMENT_3D ( 'NONE', #41158, #40128, #16798 ) ;
#45999=AXIS2_PLACEMENT_3D ( 'NONE', #37814, #42006, #17887 ) ;
#46000=CARTESIAN_POINT ( 'NONE',  ( 42.94731284509209246, 11.34112180473979947, -3.548345704167709780 ) ) ;
#46003=LINE ( 'NONE', #10091, #9703 ) ;
#46004=CARTESIAN_POINT ( 'NONE',  ( 76.40330808254813633, -43.26114854291000000, -13.96576318196657596 ) ) ;
#46005=CARTESIAN_POINT ( 'NONE',  ( 18.32671526132769912, -51.19325459173029458, -74.14992922886710858 ) ) ;
#46006=DIRECTION ( 'NONE',  ( -0.5685928097855378338, 0.5944782866685498490, 0.5685928097855378338 ) ) ;
#46007=ORIENTED_EDGE ( 'NONE', *, *, #4116, .F. ) ;
#46021=VERTEX_POINT ( 'NONE', #10067 ) ;
#46024=CARTESIAN_POINT ( 'NONE',  ( 61.38174641265649711, -45.18824807282129541, -46.54645048572430710 ) ) ;
#46026=CARTESIAN_POINT ( 'NONE',  ( 68.13393739769620083, 4.883811055320659733, -65.65000000000000568 ) ) ;
#46030=CARTESIAN_POINT ( 'NONE',  ( 52.85072064880949938, -52.31592968273889710, -54.40017261481339972 ) ) ;
#46034=VERTEX_POINT ( 'NONE', #38107 ) ;
#46036=CARTESIAN_POINT ( 'NONE',  ( 52.80343917019639832, -50.48755729126909841, -76.73469608504859707 ) ) ;
#46037=AXIS2_PLACEMENT_3D ( 'NONE', #43281, #38835, #23831 ) ;
#46038=CARTESIAN_POINT ( 'NONE',  ( 60.44851881380330383, 14.43911564095640010, -47.27117109066509926 ) ) ;
#46043=B_SPLINE_CURVE_WITH_KNOTS ( 'NONE', 3,
 ( #35682, #19434, #15510, #31464, #7652, #39614 ),
 .UNSPECIFIED., .F., .F.,
 ( 4, 2, 4 ),
 ( 0.000000000000000000, 0.1329384993766630774, 0.2774707949478909530 ),
 .UNSPECIFIED. ) ;
#46044=CARTESIAN_POINT ( 'NONE',  ( 41.11636130713259973, 13.67919800510379957, -5.497150100476379642 ) ) ;
#46045=CIRCLE ( 'NONE', #834, 40.00000000000000711 ) ;
#46046=CARTESIAN_POINT ( 'NONE',  ( 42.10819013297950164, -43.62195994593520254, -4.221348723911680700 ) ) ;
#46048=CARTESIAN_POINT ( 'NONE',  ( -3.454818612163319536, 17.59177618004110144, -5.676727923997320069 ) ) ;
#46053=CARTESIAN_POINT ( 'NONE',  ( -3.610905026690430120, -50.40327272064629938, -4.296538310234230273 ) ) ;
#46058=CARTESIAN_POINT ( 'NONE',  ( 46.53687296277449548, -53.33479509908829641, -76.10218428122850298 ) ) ;
#46060=CARTESIAN_POINT ( 'NONE',  ( 48.21566362429800279, -54.17964390236579675, -54.67775470772419766 ) ) ;
#46063=CARTESIAN_POINT ( 'NONE',  ( 42.26864913071712238, 13.12941410808000242, -5.126484831624812166 ) ) ;
#46064=CARTESIAN_POINT ( 'NONE',  ( 47.88656099864510196, 23.18744658311759821, -55.03929334947260088 ) ) ;
#46071=FACE_OUTER_BOUND ( 'NONE', #35035, .T. ) ;
#46073=CARTESIAN_POINT ( 'NONE',  ( 84.01174786492798319, 13.38463874174230028, -47.41946551740999638 ) ) ;
#46076=CIRCLE ( 'NONE', #30154, 2.745157762967529447 ) ;
#46078=CIRCLE ( 'NONE', #7575, 40.00000000000000711 ) ;
#46082=EDGE_LOOP ( 'NONE', ( #27685, #14363, #14100, #28648 ) ) ;
#46084=EDGE_CURVE ( 'NONE', #34653, #19900, #26664, .T. ) ;
#46088=CARTESIAN_POINT ( 'NONE',  ( 12.17975455547079910, -64.68546118318118943, -15.92303081430319978 ) ) ;
#46091=CARTESIAN_POINT ( 'NONE',  ( 50.95940558857264335, 4.060833044306336070, -76.37898308257572921 ) ) ;
#46092=ORIENTED_EDGE ( 'NONE', *, *, #36893, .T. ) ;
#46093=ORIENTED_EDGE ( 'NONE', *, *, #24385, .F. ) ;
#46095=DIRECTION ( 'NONE',  ( 0.000000000000000000, -1.000000000000000000, 0.000000000000000000 ) ) ;
#46096=CARTESIAN_POINT ( 'NONE',  ( 52.99306741825720479, 18.23831009604760212, -48.55383660268419987 ) ) ;
#46097=CARTESIAN_POINT ( 'NONE',  ( 61.61391020117169859, -1.934278441492739864, -16.00420058451779681 ) ) ;
#46098=CARTESIAN_POINT ( 'NONE',  ( 51.47090657186449647, -50.21087343025810412, -76.34335276480290133 ) ) ;
#46099=CARTESIAN_POINT ( 'NONE',  ( 60.02266206094759582, -46.59019202402480886, -48.66142267842249680 ) ) ;
#46104=ORIENTED_EDGE ( 'NONE', *, *, #19963, .T. ) ;
#46105=CARTESIAN_POINT ( 'NONE',  ( 54.17308945005400034, -50.61618894467930119, -77.01198594373980200 ) ) ;
#46106=CARTESIAN_POINT ( 'NONE',  ( 53.59007319875249920, 18.17385789302069554, -49.22505640236219904 ) ) ;
#46109=CARTESIAN_POINT ( 'NONE',  ( 13.97043394117600101, -50.94378507946090195, -21.74715833460999903 ) ) ;
#46110=CARTESIAN_POINT ( 'NONE',  ( 55.28123845478469889, 19.42107725494309989, -76.05360625656349782 ) ) ;
#46111=CARTESIAN_POINT ( 'NONE',  ( 47.64143405400680109, -54.53488714545009941, -74.14999999999999147 ) ) ;
#46113=CARTESIAN_POINT ( 'NONE',  ( 55.90707799132489697, 14.33971025050679948, -16.63726872277679902 ) ) ;
#46116=CARTESIAN_POINT ( 'NONE',  ( 57.28557293626779767, -50.57890658449659327, -53.44460714491770403 ) ) ;
#46119=VECTOR ( 'NONE', #3928, 1000.000000000000000 ) ;
#46120=ORIENTED_EDGE ( 'NONE', *, *, #2973, .F. ) ;
#46121=CARTESIAN_POINT ( 'NONE',  ( 47.35407109286579441, 23.03649510332309802, -75.29485535639010152 ) ) ;
#46124=CARTESIAN_POINT ( 'NONE',  ( 12.70130225181580741, -65.47524089349515464, -23.44891406722884142 ) ) ;
#46126=CARTESIAN_POINT ( 'NONE',  ( 82.75519962004040053, 14.36566124015802082, -47.67565474709540041 ) ) ;
#46131=CARTESIAN_POINT ( 'NONE',  ( 6.264007226343670354, 32.14677423655729882, -47.23119725298469973 ) ) ;
#46133=CARTESIAN_POINT ( 'NONE',  ( 53.35042868538379679, -49.41591823479419787, -49.00406147840819671 ) ) ;
#46134=ORIENTED_EDGE ( 'NONE', *, *, #33300, .F. ) ;
#46136=CARTESIAN_POINT ( 'NONE',  ( 53.62552786343490396, -51.33071804962359153, -75.58099297212140755 ) ) ;
#46137=CARTESIAN_POINT ( 'NONE',  ( 13.75275436563869924, 20.07553849835239745, -22.95880022689469868 ) ) ;
#46138=CARTESIAN_POINT ( 'NONE',  ( 56.24035600606469387, 14.32860529291999896, -25.36904170088440225 ) ) ;
#46141=CARTESIAN_POINT ( 'NONE',  ( 53.23494276941970327, 18.29173816151630305, -49.16096157153140211 ) ) ;
#46143=DIRECTION ( 'NONE',  ( 0.3918900565165093774, -0.9200120562272470215, -1.682577688288945566E-10 ) ) ;
#46145=B_SPLINE_CURVE_WITH_KNOTS ( 'NONE', 3,
 ( #35799, #51784, #11964, #29212, #33139, #41279, #25005, #24750 ),
 .UNSPECIFIED., .F., .F.,
 ( 4, 2, 2, 4 ),
 ( 0.000000000000000000, 0.2018913194515775666, 0.4037826389031551333, 0.8075652778063105997 ),
 .UNSPECIFIED. ) ;
#46149=FACE_OUTER_BOUND ( 'NONE', #36157, .T. ) ;
#46153=CARTESIAN_POINT ( 'NONE',  ( 10.63085527530649976, -64.83908867352720051, -18.12439166849010164 ) ) ;
#46156=AXIS2_PLACEMENT_3D ( 'NONE', #36456, #15534, #47511 ) ;
#46157=AXIS2_PLACEMENT_3D ( 'NONE', #22275, #50598, #50345 ) ;
#46158=CARTESIAN_POINT ( 'NONE',  ( 62.09157612670949788, -33.11618894467940066, -65.34607522167520699 ) ) ;
#46161=CARTESIAN_POINT ( 'NONE',  ( 10.49214094476729997, -63.29059696784919709, -45.62564302952420547 ) ) ;
#46165=CARTESIAN_POINT ( 'NONE',  ( 57.25859902321930406, 19.38378582711590070, -53.75766468042880319 ) ) ;
#46166=DIRECTION ( 'NONE',  ( 0.000000000000000000, 0.000000000000000000, -1.000000000000000000 ) ) ;
#46167=CARTESIAN_POINT ( 'NONE',  ( 52.43830859903380315, 18.75446654067290098, -77.15472074777260048 ) ) ;
#46168=ORIENTED_EDGE ( 'NONE', *, *, #47758, .F. ) ;
#46183=CARTESIAN_POINT ( 'NONE',  ( 14.43211210535319999, 20.28384221772149942, -75.35480091913980516 ) ) ;
#46184=CARTESIAN_POINT ( 'NONE',  ( 72.13393739769620083, -30.11618894467929763, -20.65000000000000213 ) ) ;
#46185=AXIS2_PLACEMENT_3D ( 'NONE', #33000, #29339, #12594 ) ;
#46186=( BOUNDED_CURVE ( )  B_SPLINE_CURVE ( 3, ( #8682, #28061, #36189, #36976 ),
 .UNSPECIFIED., .F., .T. ) 
 B_SPLINE_CURVE_WITH_KNOTS ( ( 4, 4 ),
 ( 2.742903481755264661, 2.960178077714945122 ),
 .UNSPECIFIED. ) 
 CURVE ( )  GEOMETRIC_REPRESENTATION_ITEM ( )  RATIONAL_B_SPLINE_CURVE ( ( 1.000000000000000000, 0.9960698467707308490, 0.9960698467707308490, 1.000000000000000000 ) ) 
 REPRESENTATION_ITEM ( '' )  );
#46187=CARTESIAN_POINT ( 'NONE',  ( 43.31517999238410255, -45.11752382326270094, -6.625465738846780361 ) ) ;
#46190=CIRCLE ( 'NONE', #22736, 20.00000000000000355 ) ;
#46194=CARTESIAN_POINT ( 'NONE',  ( 52.61926156638589447, -49.80650514857250499, -27.99463703858910080 ) ) ;
#46195=CARTESIAN_POINT ( 'NONE',  ( 56.01738229311430217, -50.84638869582439469, -74.81998313493859598 ) ) ;
#46196=CARTESIAN_POINT ( 'NONE',  ( 9.944906686717320810, 32.89002097141860048, -17.55162828126229613 ) ) ;
#46198=DIRECTION ( 'NONE',  ( 0.9316796806447995571, 5.770384170489247332E-14, 0.3632808454537678755 ) ) ;
#46201=CARTESIAN_POINT ( 'NONE',  ( -7.645228210567119653, -45.25745332872840265, -5.002875026096710087 ) ) ;
#46202=CARTESIAN_POINT ( 'NONE',  ( 47.44137716603319888, 23.39923864022719968, -54.82496924537529992 ) ) ;
#46204=CARTESIAN_POINT ( 'NONE',  ( 1.260912450620399916, -15.61618894467929763, -7.225658350974740074 ) ) ;
#46205=CARTESIAN_POINT ( 'NONE',  ( 60.96910362672209516, 14.16411045968260041, -46.92511258430779719 ) ) ;
#46206=CARTESIAN_POINT ( 'NONE',  ( 11.92291169285739905, 34.11167932846120010, -17.18421408354569735 ) ) ;
#46207=CARTESIAN_POINT ( 'NONE',  ( 51.68229834221979502, 17.53315898051910082, -77.01558403217930504 ) ) ;
#46208=CARTESIAN_POINT ( 'NONE',  ( 53.30280620372429468, 18.18069847459639732, -48.78464136231010428 ) ) ;
#46209=CARTESIAN_POINT ( 'NONE',  ( -9.882013117715120032, 9.266944274022621997, -19.14999999999999858 ) ) ;
#46211=CARTESIAN_POINT ( 'NONE',  ( 56.05988273593580118, 15.17408758016209980, -26.21244545727219943 ) ) ;
#46212=EDGE_CURVE ( 'NONE', #16411, #28603, #35037, .T. ) ;
#46213=CARTESIAN_POINT ( 'NONE',  ( 53.36385794813689643, 20.84367329114500222, -53.95571242954590474 ) ) ;
#46215=CARTESIAN_POINT ( 'NONE',  ( 53.41952757764659765, 18.23162460577420063, -49.21226385651820578 ) ) ;
#46216=CARTESIAN_POINT ( 'NONE',  ( 49.87147262927059899, -45.11618894467940066, -8.489676102032369442 ) ) ;
#46217=DIRECTION ( 'NONE',  ( -0.9200120562340469155, 0.3918900565005459247, -8.326672684688669123E-17 ) ) ;
#46218=CARTESIAN_POINT ( 'NONE',  ( 11.10555358749919996, 32.08123220696739253, -44.25270282110179920 ) ) ;
#46220=CARTESIAN_POINT ( 'NONE',  ( 67.77237640127140139, -32.48158740639239994, -19.08110272389540185 ) ) ;
#46221=CARTESIAN_POINT ( 'NONE',  ( 18.12954728147380123, 19.89797661840560039, -74.34810712130391153 ) ) ;
#46224=CARTESIAN_POINT ( 'NONE',  ( 48.17397874823690529, 23.07566552192859888, -55.30238548989590441 ) ) ;
#46225=CARTESIAN_POINT ( 'NONE',  ( 76.55823188635187648, 0.1748944968071982631, -13.47834810069977962 ) ) ;
#46227=CARTESIAN_POINT ( 'NONE',  ( 12.95205822670359908, -65.51487522867400060, -47.64438479393490411 ) ) ;
#46228=CARTESIAN_POINT ( 'NONE',  ( 56.42422650276310492, -45.43209815878279301, -25.36438790313970060 ) ) ;
#46233=DIRECTION ( 'NONE',  ( 0.8535492322835283030, 0.3460892239715681606, 0.3894559758418881801 ) ) ;
#46238=CARTESIAN_POINT ( 'NONE',  ( 47.34305974329570432, -45.94041436994260152, -10.43357978122729968 ) ) ;
#46239=CARTESIAN_POINT ( 'NONE',  ( 51.85727070035964203, 1.492828087247280999, -18.71161526954956500 ) ) ;
#46240=CARTESIAN_POINT ( 'NONE',  ( 15.46269294852310061, 19.79576386060080040, -21.20027565686660154 ) ) ;
#46241=EDGE_CURVE ( 'NONE', #679, #9344, #1578, .T. ) ;
#46245=CARTESIAN_POINT ( 'NONE',  ( 47.22775207516579599, -54.56828855535529499, -74.94674070344109396 ) ) ;
#46246=CARTESIAN_POINT ( 'NONE',  ( 56.62345902695000177, 12.22720384556450135, -8.191343754504078589 ) ) ;
#46248=B_SPLINE_SURFACE_WITH_KNOTS ( 'NONE', 3, 3, ( 
 ( #7199, #23153, #35489, #31023, #39170, #27103, #19240, #35222 ),
 ( #7967, #51226, #31273, #43363, #15579, #39682, #31534, #19997 ),
 ( #35747, #41325, #2010, #44745, #9108, #29522, #21906, #9875 ),
 ( #21395, #13304, #9622, #20884, #25057, #45266, #25832, #5440 ),
 ( #21138, #41845, #49469, #48954, #37398, #33705, #41074, #49722 ),
 ( #13810, #1500, #32925, #29768, #979, #17737, #5948, #5187 ),
 ( #41583, #1242, #37917, #5694, #45786, #37652, #8850, #17485 ),
 ( #37145, #13056, #28746, #32657, #4911, #9379, #17231, #13560 ),
 ( #48688, #12788, #24800, #29264, #36879, #40811, #16979, #29009 ),
 ( #45005, #33191, #49211, #25322, #33449, #45527, #25578, #21647 ) ),
 .UNSPECIFIED., .F., .F., .F.,
 ( 4, 1, 1, 1, 1, 1, 1, 4 ),
 ( 4, 2, 2, 4 ),
 ( -3.286467431787650260E-05, 0.1428571428571430157, 0.2857142857142860315, 0.4285714285714289917, 0.5714285714285709528, 0.7142857142857139685, 0.8571428571428569843, 1.000000000000000000 ),
 ( -2.169191898319330125, -2.161509015541720036, -1.792610411306549967, -1.570647066508290113 ),
 .UNSPECIFIED. ) ;
#46249=CARTESIAN_POINT ( 'NONE',  ( 52.01748107372789320, 19.87890217953579963, -76.09025191937530508 ) ) ;
#46250=CARTESIAN_POINT ( 'NONE',  ( 61.50603079699979503, 13.91190901698290006, -28.03580912474989972 ) ) ;
#46253=LINE ( 'NONE', #45725, #29686 ) ;
#46254=CARTESIAN_POINT ( 'NONE',  ( 9.942311330327790131, -63.79309159654170003, -15.97126716329570151 ) ) ;
#46258=DIRECTION ( 'NONE',  ( 0.3294064756441091313, -0.9441882088883163382, 0.000000000000000000 ) ) ;
#46259=CIRCLE ( 'NONE', #6935, 38.61618927352878217 ) ;
#46260=B_SPLINE_CURVE_WITH_KNOTS ( 'NONE', 3,
 ( #42570, #14520, #19218, #26556, #15298, #48294, #20751, #844, #4782, #24148, #36738 ),
 .UNSPECIFIED., .F., .F.,
 ( 4, 1, 1, 1, 1, 1, 1, 1, 4 ),
 ( 0.000000000000000000, 0.1250003856707712080, 0.2500003305749467497, 0.3750002754791222914, 0.5000002203832978331, 0.6250001652874733749, 0.7500001101916489166, 0.8750000550958244583, 1.000000000000000000 ),
 .UNSPECIFIED. ) ;
#46264=DIRECTION ( 'NONE',  ( -0.7071067811865475727, 0.000000000000000000, 0.7071067811865475727 ) ) ;
#46265=CARTESIAN_POINT ( 'NONE',  ( 42.33768682474920553, 11.92978350657940112, -3.566431340207619982 ) ) ;
#46269=DIRECTION ( 'NONE',  ( 0.8732394366197182567, 0.4872913772396111343, 1.665334536937735304E-16 ) ) ;
#46274=EDGE_CURVE ( 'NONE', #22043, #47824, #50966, .T. ) ;
#46279=CARTESIAN_POINT ( 'NONE',  ( 8.133937397696209715, -59.33545798990849818, -21.14999999999999858 ) ) ;
#46284=ORIENTED_EDGE ( 'NONE', *, *, #46751, .T. ) ;
#46287=CARTESIAN_POINT ( 'NONE',  ( 52.69317937239979699, -49.76927390646469718, -48.79657040945900803 ) ) ;
#46288=CARTESIAN_POINT ( 'NONE',  ( 82.54524994490415679, -45.15149953693300944, -46.85688790748942978 ) ) ;
#46290=B_SPLINE_CURVE_WITH_KNOTS ( 'NONE', 3,
 ( #32151, #48428, #12796, #32665, #16708, #40818, #27974, #43977, #20115, #48169, #8597, #44234, #36108, #8081, #8334, #24287, #4398, #20368, #12529, #28495, #24544, #4652, #20624, #4919, #20890, #15041, #50689, #2739, #18712, #43096, #38124, #42577, #14275, #13312, #18458 ),
 .UNSPECIFIED., .F., .F.,
 ( 4, 1, 1, 1, 2, 2, 2, 2, 1, 2, 2, 2, 1, 2, 2, 2, 2, 2, 2, 4 ),
 ( 0.000000000000000000, 0.06249999999973548936, 0.09374999999960900721, 0.1093749999995292238, 0.1171874999994964028, 0.1249999999994635680, 0.1874999999994682309, 0.2187499999994763356, 0.2343749999994887978, 0.2421874999994946820, 0.2499999999995005662, 0.3749999999996987410, 0.4374999999997912226, 0.4687499999998307465, 0.4999999999998703260, 0.6249999999999318323, 0.6874999999999624745, 0.7187499999999693578, 0.7499999999999762412, 1.000000000000000000 ),
 .UNSPECIFIED. ) ;
#46291=EDGE_LOOP ( 'NONE', ( #13547, #20042, #40431, #46860 ) ) ;
#46292=DIRECTION ( 'NONE',  ( 1.000000000000000000, -2.206290999999999941E-14, -3.490044999999999999E-12 ) ) ;
#46293=CARTESIAN_POINT ( 'NONE',  ( 54.99091206896520134, -51.40428974184509769, -54.03945093368859887 ) ) ;
#46298=VECTOR ( 'NONE', #48408, 1000.000000000000000 ) ;
#46299=CARTESIAN_POINT ( 'NONE',  ( 53.07814503768779701, -50.87410907760390444, -76.24016814631330874 ) ) ;
#46300=CARTESIAN_POINT ( 'NONE',  ( 60.61844477880759996, 14.36317300640260086, -47.31023525542560293 ) ) ;
#46302=LINE ( 'NONE', #5940, #45627 ) ;
#46303=CARTESIAN_POINT ( 'NONE',  ( 43.71660380195360318, 13.90300536042119894, -6.831405570051200193 ) ) ;
#46304=CARTESIAN_POINT ( 'NONE',  ( 42.63139189943180440, -42.85457206599819813, -3.312314667595840589 ) ) ;
#46312=CARTESIAN_POINT ( 'NONE',  ( 14.48354644325280027, -52.62916658892859800, -76.03098605356829864 ) ) ;
#46314=CARTESIAN_POINT ( 'NONE',  ( 57.38765468553089732, 19.36030170222889879, -53.60535509370559737 ) ) ;
#46316=CARTESIAN_POINT ( 'NONE',  ( 11.36895923993938951, 33.23916916631637974, -44.41074867393047043 ) ) ;
#46317=CARTESIAN_POINT ( 'NONE',  ( 47.13698192568809731, -54.70277146169920712, -74.81178025453719727 ) ) ;
#46323=CARTESIAN_POINT ( 'NONE',  ( 47.79465657660569633, 23.23647380393689943, -55.14967471148109723 ) ) ;
#46324=EDGE_LOOP ( 'NONE', ( #48275, #39902, #32594, #39186, #23464 ) ) ;
#46328=ADVANCED_FACE ( 'NONE', ( #24923 ), #49990, .T. ) ;
#46334=CARTESIAN_POINT ( 'NONE',  ( 16.13393739769620083, -15.61618894467929941, -76.14999999999999147 ) ) ;
#46336=CARTESIAN_POINT ( 'NONE',  ( 83.33882225295539570, 13.76147914917100046, -47.09476873026769539 ) ) ;
#46337=CARTESIAN_POINT ( 'NONE',  ( 54.86175021155899856, 16.01064883855890031, -25.75780955478559875 ) ) ;
#46345=VERTEX_POINT ( 'NONE', #49595 ) ;
#46346=ORIENTED_EDGE ( 'NONE', *, *, #46212, .T. ) ;
#46347=FACE_OUTER_BOUND ( 'NONE', #46913, .T. ) ;
#46349=CARTESIAN_POINT ( 'NONE',  ( -12.74484839417802640, 25.82459822544487693, -53.24848714985387943 ) ) ;
#46350=DIRECTION ( 'NONE',  ( 1.000000000000000000, 0.000000000000000000, 0.000000000000000000 ) ) ;
#46357=CARTESIAN_POINT ( 'NONE',  ( 62.46918019396079558, -1.552292481998720053, -16.13637721537210012 ) ) ;
#46358=ADVANCED_FACE ( 'NONE', ( #41196 ), #5815, .F. ) ;
#46359=CARTESIAN_POINT ( 'NONE',  ( 51.12155915768349246, -49.71343516829359999, -76.32652955267910500 ) ) ;
#46360=CARTESIAN_POINT ( 'NONE',  ( 57.85642988081749394, -49.00357350458359917, -51.22892263933690060 ) ) ;
#46363=CARTESIAN_POINT ( 'NONE',  ( 68.13393739769706769, 17.98087126524919555, -68.79648330188412331 ) ) ;
#46366=CARTESIAN_POINT ( 'NONE',  ( 46.60731581406910351, -45.11618894467940066, -7.962945791737540802 ) ) ;
#46368=CARTESIAN_POINT ( 'NONE',  ( 12.86000738318819892, -50.64304082809789520, -21.34825274859070277 ) ) ;
#46369=CARTESIAN_POINT ( 'NONE',  ( 56.66430192519659670, 19.40095727286280081, -75.08551389032560053 ) ) ;
#46371=CARTESIAN_POINT ( 'NONE',  ( 46.42817262113109678, -53.00400577820990122, -76.14999999999999147 ) ) ;
#46372=CARTESIAN_POINT ( 'NONE',  ( 56.98602282140059572, 13.94694871494499999, -17.93020696514379964 ) ) ;
#46375=CARTESIAN_POINT ( 'NONE',  ( 56.87927062415320023, -50.65046521877609820, -53.72034555678590806 ) ) ;
#46377=EDGE_CURVE ( 'NONE', #44083, #43986, #5306, .T. ) ;
#46381=EDGE_CURVE ( 'NONE', #31681, #29113, #21302, .T. ) ;
#46382=CARTESIAN_POINT ( 'NONE',  ( 46.61291010390670664, 22.01119584692700215, -76.11300884098571373 ) ) ;
#46383=CARTESIAN_POINT ( 'NONE',  ( 20.01239153654114133, -55.06729567945755832, -18.78855326316173091 ) ) ;
#46384=CARTESIAN_POINT ( 'NONE',  ( 60.91959772890204050, -45.69583638042096396, -47.74153617882512179 ) ) ;
#46387=CARTESIAN_POINT ( 'NONE',  ( 82.57811023567160191, 13.96421234425040048, -47.00700744241340345 ) ) ;
#46390=CARTESIAN_POINT ( 'NONE',  ( 47.64143405400680109, 23.30250925609140111, -74.14999999999999147 ) ) ;
#46393=CARTESIAN_POINT ( 'NONE',  ( -17.64362745039410285, 19.90889109872690099, -52.54414402675289608 ) ) ;
#46395=EDGE_CURVE ( 'NONE', #19952, #50462, #25781, .T. ) ;
#46396=CARTESIAN_POINT ( 'NONE',  ( 52.90334279678310736, -49.62746727120449464, -48.83356295429710059 ) ) ;
#46397=ORIENTED_EDGE ( 'NONE', *, *, #51417, .F. ) ;
#46398=CARTESIAN_POINT ( 'NONE',  ( 17.68281250479444111, 20.56215755416158686, -75.65677362358465530 ) ) ;
#46400=CARTESIAN_POINT ( 'NONE',  ( 13.68007976385719893, 20.13478144958939708, -22.99347874021080074 ) ) ;
#46401=CARTESIAN_POINT ( 'NONE',  ( 55.83218870901129804, 14.79097304268890056, -25.40764975850709817 ) ) ;
#46403=CARTESIAN_POINT ( 'NONE',  ( 51.02818947082010226, 19.65064782392149567, -76.14999999999999147 ) ) ;
#46404=CARTESIAN_POINT ( 'NONE',  ( 52.59812796910519950, 18.59560619956539895, -48.49245696013879581 ) ) ;
#46406=CARTESIAN_POINT ( 'NONE',  ( 55.68556815085590017, -45.89590543237220288, -16.87789993209419848 ) ) ;
#46408=EDGE_LOOP ( 'NONE', ( #35769, #16104, #6968, #20786, #49445, #32481 ) ) ;
#46411=CARTESIAN_POINT ( 'NONE',  ( 10.60681015439949881, 33.67700033712320362, -47.04781549457079848 ) ) ;
#46413=CARTESIAN_POINT ( 'NONE',  ( 10.85466640526500015, -64.96697012889119094, -17.55961383757770022 ) ) ;
#46414=CARTESIAN_POINT ( 'NONE',  ( 53.23850466849069818, -49.52901910977941924, -49.17578823945778765 ) ) ;
#46415=DIRECTION ( 'NONE',  ( 0.000000000000000000, -1.000000000000000000, 0.000000000000000000 ) ) ;
#46421=CARTESIAN_POINT ( 'NONE',  ( 10.13631591262990028, -63.14180753440869154, -45.99667195303850065 ) ) ;
#46423=VERTEX_POINT ( 'NONE', #45648 ) ;
#46424=FACE_OUTER_BOUND ( 'NONE', #21648, .T. ) ;
#46425=CARTESIAN_POINT ( 'NONE',  ( 57.03107157439150399, 18.99627872735710099, -52.68131390763750233 ) ) ;
#46427=CARTESIAN_POINT ( 'NONE',  ( 52.97782966775210411, 19.06886046639999677, -77.23919107660618977 ) ) ;
#46429=FACE_BOUND ( 'NONE', #50374, .T. ) ;
#46431=CARTESIAN_POINT ( 'NONE',  ( 14.55219274796575313, 20.46959765477225091, -75.56421372419544014 ) ) ;
#46436=ORIENTED_EDGE ( 'NONE', *, *, #10725, .T. ) ;
#46439=CARTESIAN_POINT ( 'NONE',  ( 53.02879952360030558, -49.61047114518110135, -49.09530619433559906 ) ) ;
#46440=EDGE_CURVE ( 'NONE', #40276, #37478, #37556, .T. ) ;
#46446=CARTESIAN_POINT ( 'NONE',  ( 14.35303864406479946, 20.08140804309819671, -75.03330975078259257 ) ) ;
#46448=DIRECTION ( 'NONE',  ( 0.000000000000000000, 0.000000000000000000, -1.000000000000000000 ) ) ;
#46449=CARTESIAN_POINT ( 'NONE',  ( 41.59982226866920030, -45.03802502177139644, -5.840267740712650202 ) ) ;
#46453=CARTESIAN_POINT ( 'NONE',  ( 53.95391475063919984, -48.32190372696410208, -26.18290555829409882 ) ) ;
#46454=CARTESIAN_POINT ( 'NONE',  ( 56.18713067680260309, -50.81645256829099822, -74.69754235492649741 ) ) ;
#46455=CARTESIAN_POINT ( 'NONE',  ( 10.89817501250260179, 33.55262736970569648, -16.84305400789989804 ) ) ;
#46457=DIRECTION ( 'NONE',  ( 0.000000000000000000, 0.000000000000000000, 1.000000000000000000 ) ) ;
#46458=CARTESIAN_POINT ( 'NONE',  ( 52.56521937542130019, 18.62941943741099848, -48.47378147059570352 ) ) ;
#46461=CARTESIAN_POINT ( 'NONE',  ( 47.52047993193150432, 23.35084913806530338, -54.81408765803269745 ) ) ;
#46464=CARTESIAN_POINT ( 'NONE',  ( 57.25554329372283036, 13.89079948346292426, -25.31272176079182046 ) ) ;
#46465=CARTESIAN_POINT ( 'NONE',  ( 12.01336145399789856, 34.10065735964469269, -17.10865966561200224 ) ) ;
#46466=CARTESIAN_POINT ( 'NONE',  ( 51.75737834632590051, 17.97862913216729908, -76.97426711872269323 ) ) ;
#46467=CARTESIAN_POINT ( 'NONE',  ( 52.84702947235859938, 18.41949267415209945, -48.63861689686890344 ) ) ;
#46468=ADVANCED_FACE ( 'NONE', ( #14704 ), #7365, .T. ) ;
#46471=CARTESIAN_POINT ( 'NONE',  ( 54.62137568764190121, 16.83476236174520224, -26.74064760761449833 ) ) ;
#46473=CARTESIAN_POINT ( 'NONE',  ( 50.22318599631050517, 21.91893947206089877, -53.94766427587659763 ) ) ;
#46475=CARTESIAN_POINT ( 'NONE',  ( 12.12757547495970023, -65.18777574590600921, -16.69244762554430039 ) ) ;
#46478=CARTESIAN_POINT ( 'NONE',  ( 10.49497832658790131, 32.13626875971579722, -45.62743361653370044 ) ) ;
#46480=CARTESIAN_POINT ( 'NONE',  ( 65.88232195992709705, -31.40292976940219916, -17.13915762891529937 ) ) ;
#46481=CARTESIAN_POINT ( 'NONE',  ( 12.55379742719071423, 24.22322520218094510, -75.36448431259415770 ) ) ;
#46483=ORIENTED_EDGE ( 'NONE', *, *, #50213, .F. ) ;
#46485=CARTESIAN_POINT ( 'NONE',  ( 76.64291727984071656, 3.898797979677915748, -13.84327006523654724 ) ) ;
#46486=VERTEX_POINT ( 'NONE', #23310 ) ;
#46487=CARTESIAN_POINT ( 'NONE',  ( 13.00893739769619906, -65.51843714052719747, -47.75434321273180416 ) ) ;
#46488=CARTESIAN_POINT ( 'NONE',  ( 56.06952239910840063, -46.00521685138409822, -25.91862699754300081 ) ) ;
#46492=ORIENTED_EDGE ( 'NONE', *, *, #26165, .T. ) ;
#46495=CARTESIAN_POINT ( 'NONE',  ( 11.81052567943170040, 33.80623951028800178, -23.83776314781059824 ) ) ;
#46499=CARTESIAN_POINT ( 'NONE',  ( 15.49194271727560057, 19.88381105247059821, -21.93290768619809938 ) ) ;
#46502=( BOUNDED_CURVE ( )  B_SPLINE_CURVE ( 3, ( #16957, #20596, #9088, #1222 ),
 .UNSPECIFIED., .F., .T. ) 
 B_SPLINE_CURVE_WITH_KNOTS ( ( 4, 4 ),
 ( 5.387239059105120020, 5.497787143782099761 ),
 .UNSPECIFIED. ) 
 CURVE ( )  GEOMETRIC_REPRESENTATION_ITEM ( )  RATIONAL_B_SPLINE_CURVE ( ( 1.000000000000000000, 0.9989818526761096162, 0.9989818526761096162, 1.000000000000000000 ) ) 
 REPRESENTATION_ITEM ( '' )  );
#46504=CARTESIAN_POINT ( 'NONE',  ( 47.17277128744060377, -54.46428745205209765, -75.17211772295890171 ) ) ;
#46505=CARTESIAN_POINT ( 'NONE',  ( 52.41232212662860235, 12.25270176512410103, -7.106922988313540301 ) ) ;
#46508=ADVANCED_FACE ( 'NONE', ( #46699 ), #11301, .T. ) ;
#46509=CARTESIAN_POINT ( 'NONE',  ( 55.90187131499349960, 19.50246216333230009, -52.91463811749139978 ) ) ;
#46510=CARTESIAN_POINT ( 'NONE',  ( 53.62559109437130189, 20.09832781307389737, -75.58097986859370110 ) ) ;
#46514=CARTESIAN_POINT ( 'NONE',  ( 53.59007319875249920, 18.17385789302069554, -49.22505640236219904 ) ) ;
#46515=AXIS2_PLACEMENT_3D ( 'NONE', #39987, #15370, #3058 ) ;
#46516=CARTESIAN_POINT ( 'NONE',  ( 5.758794882113630109, -59.74571218704659969, -13.93823224276430039 ) ) ;
#46517=CARTESIAN_POINT ( 'NONE',  ( 76.80246720768819557, 9.534583119364619108, -14.53080372693380085 ) ) ;
#46518=FACE_OUTER_BOUND ( 'NONE', #23049, .T. ) ;
#46520=ADVANCED_FACE ( 'NONE', ( #50612 ), #22551, .T. ) ;
#46522=LINE ( 'NONE', #22375, #48254 ) ;
#46523=CARTESIAN_POINT ( 'NONE',  ( 82.13853704237929776, -45.14107598135520050, -46.70066698695239893 ) ) ;
#46524=LINE ( 'NONE', #1254, #36513 ) ;
#46525=CARTESIAN_POINT ( 'NONE',  ( 42.87450601175959974, 11.54281269022849798, -3.882344406277799642 ) ) ;
#46526=CARTESIAN_POINT ( 'NONE',  ( 47.57068389241495510, -54.44477986412701398, -74.81178025424496525 ) ) ;
#46527=EDGE_CURVE ( 'NONE', #31811, #13386, #47262, .T. ) ;
#46529=CARTESIAN_POINT ( 'NONE',  ( 70.03247032090770574, -49.95860450174030376, -73.25000000000169109 ) ) ;
#46530=CARTESIAN_POINT ( 'NONE',  ( 76.23482020618884292, -43.29050810403887795, -13.80236124015438826 ) ) ;
#46531=CARTESIAN_POINT ( 'NONE',  ( 18.05524586885999838, -51.28949470891399898, -74.96248001586319276 ) ) ;
#46532=EDGE_CURVE ( 'NONE', #9610, #10111, #10000, .T. ) ;
#46533=CARTESIAN_POINT ( 'NONE',  ( 58.33770897141780409, -45.11618894467940066, -10.68148127205489928 ) ) ;
#46534=ORIENTED_EDGE ( 'NONE', *, *, #9099, .T. ) ;
#46538=CARTESIAN_POINT ( 'NONE',  ( 17.21347160910339724, 21.88381105532300097, -76.14999999999999147 ) ) ;
#46539=FACE_BOUND ( 'NONE', #7413, .T. ) ;
#46541=CARTESIAN_POINT ( 'NONE',  ( 7.635415421591210894, -60.86027260432054931, -20.56421356237310150 ) ) ;
#46544=CARTESIAN_POINT ( 'NONE',  ( 43.05622625292409822, -45.98099562716309663, -7.622810454742059427 ) ) ;
#46546=AXIS2_PLACEMENT_3D ( 'NONE', #28233, #15174, #35070 ) ;
#46549=CARTESIAN_POINT ( 'NONE',  ( 57.50723796702470025, -45.11618894467940066, -17.68293338560010142 ) ) ;
#46550=CARTESIAN_POINT ( 'NONE',  ( 61.29995204656449914, -45.28261984157529696, -47.06184258649409458 ) ) ;
#46551=CARTESIAN_POINT ( 'NONE',  ( 52.56521993351449851, 18.62941884369810097, -48.47378146976069502 ) ) ;
#46553=ORIENTED_EDGE ( 'NONE', *, *, #37984, .T. ) ;
#46558=CARTESIAN_POINT ( 'NONE',  ( 51.76047954393799699, -51.31561834827489577, -76.04144536748918881 ) ) ;
#46559=CARTESIAN_POINT ( 'NONE',  ( 60.23362534523680267, 14.54944813804890025, -47.26357634580340061 ) ) ;
#46560=AXIS2_PLACEMENT_3D ( 'NONE', #41646, #5753, #6012 ) ;
#46561=AXIS2_PLACEMENT_3D ( 'NONE', #3133, #40056, #35077 ) ;
#46562=CARTESIAN_POINT ( 'NONE',  ( 78.22251691734010137, -33.11618894467940066, -20.65000000000000213 ) ) ;
#46564=CARTESIAN_POINT ( 'NONE',  ( 42.53933706901050016, -43.26083871179729812, -4.182107870964270724 ) ) ;
#46565=FACE_OUTER_BOUND ( 'NONE', #20059, .T. ) ;
#46566=CARTESIAN_POINT ( 'NONE',  ( 74.93037820153030282, 13.88381105528979909, -15.31096251095349992 ) ) ;
#46569=CARTESIAN_POINT ( 'NONE',  ( 85.66799001034409855, -50.61618894467930119, -61.58097075742929860 ) ) ;
#46572=ORIENTED_EDGE ( 'NONE', *, *, #45907, .F. ) ;
#46573=CARTESIAN_POINT ( 'NONE',  ( 14.46756122145940004, -52.43578441516969946, -75.98739629952659413 ) ) ;
#46574=CARTESIAN_POINT ( 'NONE',  ( 57.49472010668189625, 18.97758529344320166, -52.71592469185309682 ) ) ;
#46578=CARTESIAN_POINT ( 'NONE',  ( 47.17210187534929844, -54.78212032244810104, -74.50474471063260751 ) ) ;
#46580=CARTESIAN_POINT ( 'NONE',  ( 47.83393063578119353, -54.38673743207299793, -54.71871010756789389 ) ) ;
#46583=CARTESIAN_POINT ( 'NONE',  ( 68.13393739769620083, 17.38381105532069881, -85.65000000000000568 ) ) ;
#46584=EDGE_CURVE ( 'NONE', #33786, #17592, #35388, .T. ) ;
#46585=CARTESIAN_POINT ( 'NONE',  ( 48.19394580060259869, 22.96827044948890162, -54.70769519783490153 ) ) ;
#46586=ORIENTED_EDGE ( 'NONE', *, *, #43418, .F. ) ;
#46588=ORIENTED_EDGE ( 'NONE', *, *, #11027, .T. ) ;
#46592=DIRECTION ( 'NONE',  ( -1.000000000000000000, 0.000000000000000000, 0.000000000000000000 ) ) ;
#46593=CARTESIAN_POINT ( 'NONE',  ( 82.73840718283250339, 14.31743462620540086, -47.62304481396600409 ) ) ;
#46603=ORIENTED_EDGE ( 'NONE', *, *, #31022, .T. ) ;
#46604=CARTESIAN_POINT ( 'NONE',  ( 12.32380480341289974, -64.64187183429430661, -15.85794303741049838 ) ) ;
#46607=CARTESIAN_POINT ( 'NONE',  ( 10.75232472717069854, -64.66152432599189126, -46.57791568324620357 ) ) ;
#46608=AXIS2_PLACEMENT_3D ( 'NONE', #8086, #8600, #32671 ) ;
#46611=CIRCLE ( 'NONE', #34000, 1.999999999999997558 ) ;
#46612=LINE ( 'NONE', #6248, #26215 ) ;
#46613=CARTESIAN_POINT ( 'NONE',  ( 50.28419523648629763, 21.33947418011459973, -52.92671477066360097 ) ) ;
#46614=CARTESIAN_POINT ( 'NONE',  ( 62.52134720042879223, -1.849972813426850049, -16.13391758643249929 ) ) ;
#46615=CARTESIAN_POINT ( 'NONE',  ( 50.77884678341099800, -50.22802738765170005, -76.16429375959108938 ) ) ;
#46616=CARTESIAN_POINT ( 'NONE',  ( 59.16347915308939776, -47.65516984601120498, -49.82822139732490285 ) ) ;
#46624=CARTESIAN_POINT ( 'NONE',  ( 12.82931844094959928, -50.64771532553120181, -21.34049561054089850 ) ) ;
#46625=AXIS2_PLACEMENT_3D ( 'NONE', #14451, #42764, #25257 ) ;
#46626=CARTESIAN_POINT ( 'NONE',  ( 54.14333229794100077, 19.38381105532069881, -76.93437042524608671 ) ) ;
#46628=CARTESIAN_POINT ( 'NONE',  ( 46.97184464991040187, -53.68621135916810516, -75.90842213619210099 ) ) ;
#46629=CARTESIAN_POINT ( 'NONE',  ( 57.22120921428249574, 13.89541071290600094, -17.46027851202169856 ) ) ;
#46630=CARTESIAN_POINT ( 'NONE',  ( 8.978915886419921222, 32.05342364452790349, -46.63388789120410394 ) ) ;
#46631=ADVANCED_FACE ( 'NONE', ( #19148 ), #50429, .T. ) ;
#46637=ORIENTED_EDGE ( 'NONE', *, *, #2069, .F. ) ;
#46638=CARTESIAN_POINT ( 'NONE',  ( 47.51352477951299846, 23.17639757702380265, -74.95061759547310487 ) ) ;
#46640=CARTESIAN_POINT ( 'NONE',  ( 44.61938837358319887, -46.10030783221859707, -8.716654097462109618 ) ) ;
#46642=CARTESIAN_POINT ( 'NONE',  ( 15.67962062493140074, -50.86266781791879765, -20.15000000000000213 ) ) ;
#46643=CARTESIAN_POINT ( 'NONE',  ( 61.75019796695539753, -45.11618894467940066, -28.15000000000000213 ) ) ;
#46644=VECTOR ( 'NONE', #25096, 1000.000000000000114 ) ;
#46645=EDGE_CURVE ( 'NONE', #17870, #20534, #19015, .T. ) ;
#46646=CARTESIAN_POINT ( 'NONE',  ( 46.50380985604989803, -53.09853600777310589, -76.13981661584659832 ) ) ;
#46647=CARTESIAN_POINT ( 'NONE',  ( 82.54643970977650724, 14.35786247387079939, -47.66714700205459820 ) ) ;
#46653=CARTESIAN_POINT ( 'NONE',  ( -33.14787555410379838, -5.864628912960290208, -57.37579723497079698 ) ) ;
#46654=ORIENTED_EDGE ( 'NONE', *, *, #18550, .T. ) ;
#46655=CARTESIAN_POINT ( 'NONE',  ( 52.66273262193210059, -49.77080232680150118, -48.50782009810659900 ) ) ;
#46656=EDGE_LOOP ( 'NONE', ( #27434, #26948, #27476, #26385, #20210 ) ) ;
#46659=CARTESIAN_POINT ( 'NONE',  ( 13.71439950624830040, 19.91720079445899927, -22.21277075379959953 ) ) ;
#46660=CARTESIAN_POINT ( 'NONE',  ( 13.58669771564977502, 24.30199623652838881, -76.07908087647429340 ) ) ;
#46663=CARTESIAN_POINT ( 'NONE',  ( 53.22811889490370163, 18.28257712635599930, -49.13101610134690134 ) ) ;
#46664=CARTESIAN_POINT ( 'NONE',  ( 55.45160347463279749, -46.01556803493200221, -16.61970326677620236 ) ) ;
#46671=CARTESIAN_POINT ( 'NONE',  ( 11.11361097577930046, -65.20138656326300008, -17.79075125677969993 ) ) ;
#46672=CARTESIAN_POINT ( 'NONE',  ( 52.56522529778620623, -49.86179102641759897, -48.47379134784809906 ) ) ;
#46679=VERTEX_POINT ( 'NONE', #15864 ) ;
#46680=CARTESIAN_POINT ( 'NONE',  ( 10.48646698228519902, -63.14537606440271134, -45.62814768381470287 ) ) ;
#46684=CARTESIAN_POINT ( 'NONE',  ( 57.35094531453410127, 19.00534567308480050, -52.73804475687700233 ) ) ;
#46685=CARTESIAN_POINT ( 'NONE',  ( 52.19766866516950188, 18.93657527451279776, -76.74438384267088509 ) ) ;
#46691=AXIS2_PLACEMENT_3D ( 'NONE', #44978, #36581, #36072 ) ;
#46692=CARTESIAN_POINT ( 'NONE',  ( 57.35094531453579947, -50.23772356244409565, -52.73804475687759918 ) ) ;
#46694=FACE_OUTER_BOUND ( 'NONE', #12760, .T. ) ;
#46699=FACE_OUTER_BOUND ( 'NONE', #32376, .T. ) ;
#46701=CARTESIAN_POINT ( 'NONE',  ( 52.97667589433369528, -49.63212252085850196, -49.06651684377270328 ) ) ;
#46704=B_SPLINE_CURVE_WITH_KNOTS ( 'NONE', 3,
 ( #48900, #39732, #23719, #44174, #3837, #19810, #35798, #15886, #31839, #20055, #36046, #156, #8272, #24222, #4339, #13257, #9326, #5898, #17433, #25273, #17182, #37597, #33138 ),
 .UNSPECIFIED., .F., .F.,
 ( 4, 2, 2, 1, 1, 2, 2, 2, 2, 1, 1, 1, 2, 4 ),
 ( 0.000000000000000000, 0.1072084829650507831, 0.1608127244475765771, 0.1876148451888395019, 0.2010159055594712973, 0.2077164357447871257, 0.2144169659301028985, 0.3216254488951440504, 0.3752296903776636272, 0.4020318111189224441, 0.4154328714895532682, 0.4221334016748690687, 0.4254836667675259143, 0.4288339318601827599 ),
 .UNSPECIFIED. ) ;
#46707=DIRECTION ( 'NONE',  ( 0.000000000000000000, 0.000000000000000000, 1.000000000000000000 ) ) ;
#46708=B_SPLINE_CURVE_WITH_KNOTS ( 'NONE', 3,
 ( #12467, #36297, #8019, #5135, #12736, #16651, #32609, #37094 ),
 .UNSPECIFIED., .F., .F.,
 ( 4, 2, 2, 4 ),
 ( 0.000000000000000000, 0.3707862687908220489, 0.9874243036154037867, 1.000000000000000000 ),
 .UNSPECIFIED. ) ;
#46709=CARTESIAN_POINT ( 'NONE',  ( 45.47878560697390071, -45.37428362319629827, -8.420277137582820259 ) ) ;
#46712=ORIENTED_EDGE ( 'NONE', *, *, #47661, .F. ) ;
#46714=CARTESIAN_POINT ( 'NONE',  ( 53.64274194304960020, -51.26763427440859999, -75.63099620592139161 ) ) ;
#46715=CARTESIAN_POINT ( 'NONE',  ( -0.8795253323679090851, 21.57280389172689894, -9.219647602998469083 ) ) ;
#46719=ORIENTED_EDGE ( 'NONE', *, *, #42677, .F. ) ;
#46721=CARTESIAN_POINT ( 'NONE',  ( 47.84139276221520021, 23.14568351075850217, -54.70178033708860710 ) ) ;
#46722=CIRCLE ( 'NONE', #16540, 22.00000000000000355 ) ;
#46723=CARTESIAN_POINT ( 'NONE',  ( 41.50323316430841203, -44.79455443392685510, -5.449105696209454841 ) ) ;
#46725=CARTESIAN_POINT ( 'NONE',  ( 61.29280341538199650, 14.32362702051400127, -47.63129005651870074 ) ) ;
#46726=CARTESIAN_POINT ( 'NONE',  ( 11.81751872167160045, 34.08285254420739818, -17.14434883937219922 ) ) ;
#46727=CARTESIAN_POINT ( 'NONE',  ( 51.78350020499539852, 17.91029486332229936, -77.04630018135540581 ) ) ;
#46728=CARTESIAN_POINT ( 'NONE',  ( 52.93112653136360279, 18.37582452390590149, -48.77840570252370611 ) ) ;
#46729=DIRECTION ( 'NONE',  ( 0.000000000000000000, 0.000000000000000000, -1.000000000000000000 ) ) ;
#46731=CARTESIAN_POINT ( 'NONE',  ( 56.52276590765480080, 15.01206069354710060, -26.27186043794959858 ) ) ;
#46732=CARTESIAN_POINT ( 'NONE',  ( 49.64260032845869830, 22.42839500882750059, -54.78414101162800165 ) ) ;
#46733=CARTESIAN_POINT ( 'NONE',  ( 53.70440469537284400, -48.89725131568911820, -27.13824717588386903 ) ) ;
#46734=CARTESIAN_POINT ( 'NONE',  ( 52.60294686985729840, 18.59530815018699812, -48.60888033553569443 ) ) ;
#46737=CARTESIAN_POINT ( 'NONE',  ( 10.77336949205099970, 32.10438947587439884, -45.20591960971059819 ) ) ;
#46740=DIRECTION ( 'NONE',  ( 0.000000000000000000, 0.000000000000000000, 1.000000000000000000 ) ) ;
#46745=CARTESIAN_POINT ( 'NONE',  ( 68.59772359096709238, -1.116188944679340045, -21.89807540431120358 ) ) ;
#46746=CARTESIAN_POINT ( 'NONE',  ( 76.87859648677320479, 11.88381402801379849, -14.85884684523960075 ) ) ;
#46748=CARTESIAN_POINT ( 'NONE',  ( 10.97811661469409827, -63.90378363857650612, -45.04831364494010160 ) ) ;
#46749=CARTESIAN_POINT ( 'NONE',  ( 57.51881368209140533, -45.19501142122329895, -25.74532814797139935 ) ) ;
#46751=EDGE_CURVE ( 'NONE', #3494, #38460, #6074, .T. ) ;
#46753=CARTESIAN_POINT ( 'NONE',  ( 16.13393739769620083, -15.61618894467929941, -28.02168704970069868 ) ) ;
#46754=B_SPLINE_CURVE_WITH_KNOTS ( 'NONE', 3,
 ( #11067, #14985, #22316, #46982, #42782, #42257, #42523, #34893, #18655, #50893, #43039, #10807, #46723, #14730 ),
 .UNSPECIFIED., .F., .F.,
 ( 4, 2, 2, 2, 2, 2, 4 ),
 ( 0.000000000000000000, 0.06287436669111368115, 0.3602487949084645091, 0.6184358969147355500, 0.8245813718801661141, 0.9276541093628823953, 1.000000000000000000 ),
 .UNSPECIFIED. ) ;
#46755=ORIENTED_EDGE ( 'NONE', *, *, #6582, .T. ) ;
#46758=CARTESIAN_POINT ( 'NONE',  ( 12.05844419658449951, 34.05022214372210243, -23.57277994855740033 ) ) ;
#46759=EDGE_LOOP ( 'NONE', ( #37833, #45141, #3095, #40944, #33230 ) ) ;
#46764=CARTESIAN_POINT ( 'NONE',  ( 46.81139557655359340, -53.78025948612990703, -75.90528168595349712 ) ) ;
#46765=CARTESIAN_POINT ( 'NONE',  ( 52.39839370536370211, 12.55527397068519946, -7.161984143140530001 ) ) ;
#46769=CARTESIAN_POINT ( 'NONE',  ( 65.03603135455020379, -32.24781572988710110, -17.83403478221860183 ) ) ;
#46772=CARTESIAN_POINT ( 'NONE',  ( 54.32193552160570249, -48.29328850758490432, -26.80441240787190083 ) ) ;
#46773=CARTESIAN_POINT ( 'NONE',  ( 1.775250261842860056, -55.58081467171729884, -10.96136838756989818 ) ) ;
#46774=CARTESIAN_POINT ( 'NONE',  ( 75.37466888843739810, -30.01699399069740082, -11.89334001646519923 ) ) ;
#46777=CARTESIAN_POINT ( 'NONE',  ( 19.61576842239554352, -55.46436179167167069, -75.47957398524580697 ) ) ;
#46780=CARTESIAN_POINT ( 'NONE',  ( 82.33636376959559300, -45.53544251379970120, -47.60086788096420207 ) ) ;
#46781=FACE_OUTER_BOUND ( 'NONE', #43657, .T. ) ;
#46782=CARTESIAN_POINT ( 'NONE',  ( 40.60988597354600671, 13.46376186705429845, -4.337423628782890006 ) ) ;
#46785=CARTESIAN_POINT ( 'NONE',  ( 68.13393739769745139, -49.21324915460109395, -75.95351669811962836 ) ) ;
#46786=DIRECTION ( 'NONE',  ( 0.000000000000000000, -1.000000000000000000, 0.000000000000000000 ) ) ;
#46787=CARTESIAN_POINT ( 'NONE',  ( 17.66909654327109536, -51.94403353591209793, -75.77396328158869210 ) ) ;
#46788=CARTESIAN_POINT ( 'NONE',  ( 58.76844946023069838, -44.34544036321329941, -9.066887851337279258 ) ) ;
#46792=VERTEX_POINT ( 'NONE', #29455 ) ;
#46793=CARTESIAN_POINT ( 'NONE',  ( -7.152475357492779295, 15.01427191330900079, -6.869070896293750117 ) ) ;
#46794=CARTESIAN_POINT ( 'NONE',  ( 60.83524288460380802, -45.71913028275810120, -47.74946701498309665 ) ) ;
#46796=VECTOR ( 'NONE', #22926, 1000.000000000000000 ) ;
#46800=CARTESIAN_POINT ( 'NONE',  ( 42.77858091870550084, -45.71739890479680213, -7.241831254560019637 ) ) ;
#46802=EDGE_CURVE ( 'NONE', #47075, #12119, #40481, .T. ) ;
#46814=DIRECTION ( 'NONE',  ( 0.000000000000000000, 1.000000000000000000, 0.000000000000000000 ) ) ;
#46818=CARTESIAN_POINT ( 'NONE',  ( 51.30756349522820159, -50.82514498746949982, -76.17053261049738921 ) ) ;
#46820=CARTESIAN_POINT ( 'NONE',  ( 60.56605300001870518, 14.40753913078479975, -47.40713001077759969 ) ) ;
#46823=EDGE_CURVE ( 'NONE', #22850, #38811, #37591, .T. ) ;
#46824=CARTESIAN_POINT ( 'NONE',  ( 40.60804131356049851, -44.74569051554189514, -4.641941792357479279 ) ) ;
#46826=CARTESIAN_POINT ( 'NONE',  ( -6.415573901255199551, 15.04311249118519989, -5.150318756231260231 ) ) ;
#46827=VECTOR ( 'NONE', #34991, 999.9999999999998863 ) ;
#46832=EDGE_LOOP ( 'NONE', ( #18795, #45834, #29566, #32763, #6642, #12045 ) ) ;
#46833=DIRECTION ( 'NONE',  ( -0.005554557064135746090, -0.7535009559967822401, -0.6574233462600460598 ) ) ;
#46834=CARTESIAN_POINT ( 'NONE',  ( 45.07858682377059978, 14.88010818488339915, -9.026855431852879974 ) ) ;
#46838=CARTESIAN_POINT ( 'NONE',  ( 14.70125025181300060, 19.30047638221009976, -20.74420046562330100 ) ) ;
#46841=CARTESIAN_POINT ( 'NONE',  ( 61.08966779969438932, 14.10374125018732983, -46.92974023940308825 ) ) ;
#46842=CARTESIAN_POINT ( 'NONE',  ( 48.05050519812169796, -54.35518933397780472, -55.13482086050959197 ) ) ;
#46843=FACE_OUTER_BOUND ( 'NONE', #11547, .T. ) ;
#46844=CARTESIAN_POINT ( 'NONE',  ( -6.554330339767415303, -46.10323663958071450, -4.693995882122231400 ) ) ;
#46846=CARTESIAN_POINT ( 'NONE',  ( 47.79402269939749459, 23.21147026759410181, -54.88834611196039504 ) ) ;
#46847=ORIENTED_EDGE ( 'NONE', *, *, #27392, .T. ) ;
#46851=CARTESIAN_POINT ( 'NONE',  ( 60.23889825737560244, -45.78059604851859632, -47.30579064662349964 ) ) ;
#46852=CARTESIAN_POINT ( 'NONE',  ( 57.08448514777830241, -47.43174880974720509, -47.79773139290959705 ) ) ;
#46859=DIRECTION ( 'NONE',  ( 1.000000000000000000, 0.000000000000000000, 0.000000000000000000 ) ) ;
#46860=ORIENTED_EDGE ( 'NONE', *, *, #22824, .T. ) ;
#46862=B_SPLINE_CURVE_WITH_KNOTS ( 'NONE', 3,
 ( #46834, #38707, #42373, #27400, #35269, #43401, #7501, #19542, #10921, #51522, #22427, #38435, #18514, #26885, #20553, #8006, #11694, #39724, #20044, #35789, #12201, #51772, #145, #28423, #27657, #44427, #43658, #3827, #16123, #19800, #31831, #12454, #8529, #32084 ),
 .UNSPECIFIED., .F., .F.,
 ( 4, 3, 3, 3, 3, 3, 3, 3, 3, 3, 3, 4 ),
 ( -6.893222615345909965, -6.545934836083509900, -5.829966074818360156, -5.113218181026589981, -4.902226309511959812, -4.188682698346940292, -3.475139087181930542, -2.862484081209690778, -2.335777911127269846, -1.843229489558059875, -1.766097323099939942, -1.366260745963329803 ),
 .UNSPECIFIED. ) ;
#46864=CARTESIAN_POINT ( 'NONE',  ( 12.29622276840649953, -64.73592984932109573, -15.96315064375670012 ) ) ;
#46869=CARTESIAN_POINT ( 'NONE',  ( 11.59770002601669958, -65.28329604816460119, -47.33594395550530720 ) ) ;
#46871=ORIENTED_EDGE ( 'NONE', *, *, #20485, .T. ) ;
#46872=CIRCLE ( 'NONE', #18369, 2.700000000000230216 ) ;
#46875=SPHERICAL_SURFACE ( 'NONE', #1121, 2.000000000000000000 ) ;
#46877=CARTESIAN_POINT ( 'NONE',  ( 63.34240831626450330, -0.3547437479215780343, -16.56187347819639655 ) ) ;
#46878=CARTESIAN_POINT ( 'NONE',  ( 56.91685934183519890, -50.04301054400669813, -52.37184532886749366 ) ) ;
#46883=DIRECTION ( 'NONE',  ( 0.000000000000000000, -1.000000000000000000, 0.000000000000000000 ) ) ;
#46884=DIRECTION ( 'NONE',  ( 0.000000000000000000, -1.000000000000000000, 0.000000000000000000 ) ) ;
#46886=CARTESIAN_POINT ( 'NONE',  ( 13.99896632404920105, -51.14831594409909599, -22.43872229512260219 ) ) ;
#46887=CARTESIAN_POINT ( 'NONE',  ( 57.21094436373439862, 19.38381105532069881, -74.14882592923370908 ) ) ;
#46890=CARTESIAN_POINT ( 'NONE',  ( 54.99584801749529817, 14.10383798426820157, -15.06529325330870073 ) ) ;
#46892=CARTESIAN_POINT ( 'NONE',  ( 56.61697313395120545, -50.69523099840940006, -53.47849945248049863 ) ) ;
#46895=CARTESIAN_POINT ( 'NONE',  ( 47.21787081358019833, 22.79230847309320040, -75.61358154568520717 ) ) ;
#46897=AXIS2_PLACEMENT_3D ( 'NONE', #21378, #37381, #33433 ) ;
#46900=VECTOR ( 'NONE', #39541, 1000.000000000000000 ) ;
#46901=CARTESIAN_POINT ( 'NONE',  ( 15.65806070092803992, -50.85540152079837384, -20.25522491696300875 ) ) ;
#46902=CARTESIAN_POINT ( 'NONE',  ( 14.19855276898660001, 24.33696219936630101, -76.14999999999999147 ) ) ;
#46904=CARTESIAN_POINT ( 'NONE',  ( 16.13393739769579582, -15.61618894467939889, -10.44999999999980034 ) ) ;
#46905=CARTESIAN_POINT ( 'NONE',  ( 82.13853704237929776, 13.88834436876070200, -46.53690974066719832 ) ) ;
#46907=CARTESIAN_POINT ( 'NONE',  ( 53.99784731903601909, 19.38381105527493986, -77.02981984151007566 ) ) ;
#46910=CARTESIAN_POINT ( 'NONE',  ( 49.47774481438250405, 22.52031088949399873, -55.14135542417720615 ) ) ;
#46912=CARTESIAN_POINT ( 'NONE',  ( 53.13943618043249728, -49.50838218133899460, -48.93645286566210473 ) ) ;
#46913=EDGE_LOOP ( 'NONE', ( #30041, #47565, #43136, #6226 ) ) ;
#46916=CARTESIAN_POINT ( 'NONE',  ( 13.61938558664210142, 20.19483563600030251, -23.00040036072980243 ) ) ;
#46917=CARTESIAN_POINT ( 'NONE',  ( 51.90728548701680012, -49.37557664627889409, -77.08408650135000073 ) ) ;
#46919=CARTESIAN_POINT ( 'NONE',  ( 52.74572841191380235, 18.49240759515019761, -48.77971847666659500 ) ) ;
#46920=CARTESIAN_POINT ( 'NONE',  ( 55.49574894575610529, -45.93699121200089763, -16.59260285522099920 ) ) ;
#46921=CARTESIAN_POINT ( 'NONE',  ( 16.57664560245815366, 19.88381105532340598, -15.67533231080279954 ) ) ;
#46923=EDGE_CURVE ( 'NONE', #5062, #34403, #45995, .T. ) ;
#46926=EDGE_CURVE ( 'NONE', #48001, #29313, #30023, .T. ) ;
#46927=CARTESIAN_POINT ( 'NONE',  ( 11.88601304140500048, -65.43528728455630983, -17.88642721559120119 ) ) ;
#46928=CARTESIAN_POINT ( 'NONE',  ( 9.949440222175219617, 33.40288359707810173, -46.96299386755929817 ) ) ;
#46930=CARTESIAN_POINT ( 'NONE',  ( 47.99888731038549849, -54.67877686907520030, -55.58081006888029663 ) ) ;
#46931=CARTESIAN_POINT ( 'NONE',  ( 68.13393739769620083, 11.88381105532070059, -71.50000000000000000 ) ) ;
#46932=EDGE_CURVE ( 'NONE', #3421, #48088, #40934, .T. ) ;
#46933=CARTESIAN_POINT ( 'NONE',  ( 63.02122824129657630, -31.65172625870799195, -17.11446970408973201 ) ) ;
#46934=CARTESIAN_POINT ( 'NONE',  ( 51.54415332628170177, -52.59067900109340599, -53.64346124582210251 ) ) ;
#46935=EDGE_CURVE ( 'NONE', #5682, #39834, #18324, .T. ) ;
#46936=ORIENTED_EDGE ( 'NONE', *, *, #10313, .F. ) ;
#46937=CARTESIAN_POINT ( 'NONE',  ( 61.47023863363166640, 14.17716911753344888, -47.41726777464327114 ) ) ;
#46938=ORIENTED_EDGE ( 'NONE', *, *, #11786, .F. ) ;
#46939=CARTESIAN_POINT ( 'NONE',  ( 10.14330270683290181, -63.24555248048280021, -45.99329719495809599 ) ) ;
#46940=CARTESIAN_POINT ( 'NONE',  ( 67.04038824939809160, 19.47158195952359705, -70.40645085170191919 ) ) ;
#46941=ORIENTED_EDGE ( 'NONE', *, *, #50037, .F. ) ;
#46942=CARTESIAN_POINT ( 'NONE',  ( 67.77185288443023126, -32.48144925312345777, -19.08055328465526301 ) ) ;
#46943=CARTESIAN_POINT ( 'NONE',  ( 57.24718409514530038, 19.38381105959480166, -53.91456318647720281 ) ) ;
#46944=CARTESIAN_POINT ( 'NONE',  ( 52.62506680556380445, 18.89058939249819957, -77.17021719700440485 ) ) ;
#46950=ADVANCED_FACE ( 'NONE', ( #12984 ), #3300, .T. ) ;
#46962=CARTESIAN_POINT ( 'NONE',  ( 54.55527866260889880, 13.97782061053390024, -14.50547701147139890 ) ) ;
#46966=B_SPLINE_CURVE_WITH_KNOTS ( 'NONE', 3,
 ( #44787, #35885, #28006, #40338, #8371, #494, #12564, #8890, #45045, #44013 ),
 .UNSPECIFIED., .F., .F.,
 ( 4, 2, 2, 2, 4 ),
 ( 0.000000000000000000, 0.2500000000000000000, 0.5000000000000000000, 0.7500000000000000000, 1.000000000000000000 ),
 .UNSPECIFIED. ) ;
#46967=FACE_OUTER_BOUND ( 'NONE', #27718, .T. ) ;
#46969=CARTESIAN_POINT ( 'NONE',  ( 12.24533245416119875, 33.66790095091289459, -16.17634614694899753 ) ) ;
#46970=EDGE_CURVE ( 'NONE', #22246, #26340, #9144, .T. ) ;
#46973=CARTESIAN_POINT ( 'NONE',  ( 54.01624284205600190, -50.84298546714590117, -76.06981002096979694 ) ) ;
#46974=CARTESIAN_POINT ( 'NONE',  ( -9.775776935431979453, 11.10229679186929985, -4.376631905210299323 ) ) ;
#46979=CARTESIAN_POINT ( 'NONE',  ( -7.651755816370680030, -45.25221342018689796, -4.961742078189089966 ) ) ;
#46981=CARTESIAN_POINT ( 'NONE',  ( 47.53086264803540217, 23.35184965363709964, -54.93563586120320252 ) ) ;
#46982=CARTESIAN_POINT ( 'NONE',  ( 45.24652675828470194, -45.11233960980349877, -7.238436661000799965 ) ) ;
#46984=CARTESIAN_POINT ( 'NONE',  ( 61.50420652560170254, 14.14157561437649946, -47.35413546943329521 ) ) ;
#46986=CARTESIAN_POINT ( 'NONE',  ( 11.43875273179329888, 33.77160878647529785, -16.70124317896340216 ) ) ;
#46987=CARTESIAN_POINT ( 'NONE',  ( 51.12541109834690189, 17.80355093173099945, -76.44562399623239912 ) ) ;
#46988=CARTESIAN_POINT ( 'NONE',  ( 52.88731326962020063, 18.39838686409170165, -48.71031098948949989 ) ) ;
#46989=FACE_OUTER_BOUND ( 'NONE', #28796, .T. ) ;
#46990=CARTESIAN_POINT ( 'NONE',  ( 52.98014239974310158, -49.58212897128409935, -48.77045029443840463 ) ) ;
#46991=CARTESIAN_POINT ( 'NONE',  ( 55.58239951895799891, 15.93248589216560163, -26.45503902670689911 ) ) ;
#46992=CARTESIAN_POINT ( 'NONE',  ( 51.37525108058719070, 21.43002075209610169, -53.68096604571569941 ) ) ;
#46993=CARTESIAN_POINT ( 'NONE',  ( 11.13393739769619906, -63.52234721269329754, -43.76018303787720498 ) ) ;
#46994=CARTESIAN_POINT ( 'NONE',  ( 52.95065142214180298, 18.41081157851500194, -49.05053735721260466 ) ) ;
#46995=CARTESIAN_POINT ( 'NONE',  ( 64.42629863252790301, -31.83020107878950355, -17.29446360647740022 ) ) ;
#46998=CARTESIAN_POINT ( 'NONE',  ( 11.13393739769619906, 32.17451011075910117, -43.75199058894809667 ) ) ;
#47002=EDGE_LOOP ( 'NONE', ( #36651, #4182, #16703, #29847 ) ) ;
#47004=CARTESIAN_POINT ( 'NONE',  ( 42.78018059643970616, 11.47668021806869909, -3.187564294433590462 ) ) ;
#47005=CARTESIAN_POINT ( 'NONE',  ( 49.22133579550766314, -2.537587427789457450, -15.68296696295392501 ) ) ;
#47006=EDGE_LOOP ( 'NONE', ( #21937, #35655 ) ) ;
#47007=CARTESIAN_POINT ( 'NONE',  ( 10.93332211232449858, -63.42973977545160125, -44.88523379654579770 ) ) ;
#47008=CARTESIAN_POINT ( 'NONE',  ( 57.62157700287180262, -45.13389161508140290, -25.55380843324740070 ) ) ;
#47012=CARTESIAN_POINT ( 'NONE',  ( 11.08507654941954534, 33.73697186712689700, -23.09805566017817569 ) ) ;
#47015=ORIENTED_EDGE ( 'NONE', *, *, #8252, .F. ) ;
#47020=CARTESIAN_POINT ( 'NONE',  ( 59.40244065973389809, -28.47955681903010117, -15.68910098019369848 ) ) ;
#47022=CARTESIAN_POINT ( 'NONE',  ( 14.35343152256950994, 19.90989047429600944, -74.52173647802527512 ) ) ;
#47023=CARTESIAN_POINT ( 'NONE',  ( 46.98322821459649390, -54.10563643341230033, -75.65564156953989539 ) ) ;
#47025=CARTESIAN_POINT ( 'NONE',  ( 55.78773384471490004, 14.70281777721210048, -17.21511389756160071 ) ) ;
#47026=AXIS2_PLACEMENT_3D ( 'NONE', #20250, #36242, #16336 ) ;
#47027=CARTESIAN_POINT ( 'NONE',  ( 9.125156155671129810, 23.76650935141284648, -46.59639583156063480 ) ) ;
#47028=CARTESIAN_POINT ( 'NONE',  ( 84.14547009360870788, -44.02225889889389521, -47.04794573760770504 ) ) ;
#47029=CARTESIAN_POINT ( 'NONE',  ( 61.72354608828829470, 13.88380460775019998, -28.15154712750929988 ) ) ;
#47032=ORIENTED_EDGE ( 'NONE', *, *, #42556, .F. ) ;
#47033=CARTESIAN_POINT ( 'NONE',  ( 53.11151013220920447, -49.41761562391879892, -27.57048291557959985 ) ) ;
#47035=CARTESIAN_POINT ( 'NONE',  ( 9.785108495119239080, -62.20228083952999754, -13.76464713449209931 ) ) ;
#47036=CARTESIAN_POINT ( 'NONE',  ( 76.39184943767510561, -14.06485864167870048, -12.76139016365400103 ) ) ;
#47037=CARTESIAN_POINT ( 'NONE',  ( 75.06368319349118678, 13.82630467214183412, -14.84994213268719498 ) ) ;
#47039=CARTESIAN_POINT ( 'NONE',  ( 68.13393739769620083, -38.11618894467930119, -73.25000000000000000 ) ) ;
#47040=CARTESIAN_POINT ( 'NONE',  ( 57.55751162087899786, 18.85811933572220056, -52.57651812407429759 ) ) ;
#47041=CARTESIAN_POINT ( 'NONE',  ( 57.44002002155969677, -50.11795781616180534, -52.60481300423919748 ) ) ;
#47042=CARTESIAN_POINT ( 'NONE',  ( 41.78486011480440254, 12.44044499274069970, -3.688051965452270320 ) ) ;
#47044=CARTESIAN_POINT ( 'NONE',  ( 62.35658816052890074, -45.11618894467940066, -11.77117279798510019 ) ) ;
#47045=CARTESIAN_POINT ( 'NONE',  ( 60.24058964203589994, -45.77817723718830223, -47.32689780713820227 ) ) ;
#47048=CARTESIAN_POINT ( 'NONE',  ( 18.33110477860099863, -51.54257389744909545, -75.18091805976320074 ) ) ;
#47049=CARTESIAN_POINT ( 'NONE',  ( 50.26724122796470340, -44.37275934281500156, -6.890686952535750365 ) ) ;
#47057=CARTESIAN_POINT ( 'NONE',  ( 60.68789125469650259, -45.76122483411000275, -47.75606074947319968 ) ) ;
#47060=CARTESIAN_POINT ( 'NONE',  ( 41.81949136886859719, -45.55672709288079858, -6.527086829740709639 ) ) ;
#47063=CARTESIAN_POINT ( 'NONE',  ( 17.84878478542360014, 21.14718688187949880, -75.96082109999758814 ) ) ;
#47064=ORIENTED_EDGE ( 'NONE', *, *, #2678, .T. ) ;
#47067=CARTESIAN_POINT ( 'NONE',  ( 56.29021670269609956, -45.11618894467940066, -14.97294918829250143 ) ) ;
#47069=B_SPLINE_CURVE_WITH_KNOTS ( 'NONE', 3,
 ( #37183, #25875, #49250, #36644, #45046, #750, #9149, #32699, #25100, #12828, #42413, #47131, #10961, #50278, #2053, #30068, #22980, #14365, #7029, #18804, #11217, #34784, #18549, #18284, #19064, #42675, #50531, #14622 ),
 .UNSPECIFIED., .F., .F.,
 ( 4, 3, 3, 3, 3, 3, 3, 3, 3, 4 ),
 ( -0.9179856196245679278, -0.8858225628240299354, -0.7263688044477000227, -0.6319066474211799678, -0.6008308638451469452, -0.4562725788532379645, -0.3116808554209890003, -0.1741802918957590096, -0.08002528894982974261, 1.110223024625156540E-14 ),
 .UNSPECIFIED. ) ;
#47075=VERTEX_POINT ( 'NONE', #21583 ) ;
#47076=CARTESIAN_POINT ( 'NONE',  ( 65.46029542295769943, -29.76883965895079953, -16.55376543218019947 ) ) ;
#47077=CARTESIAN_POINT ( 'NONE',  ( 52.57481654442310059, -51.43204889509869560, -75.83555718502590537 ) ) ;
#47078=CARTESIAN_POINT ( 'NONE',  ( 60.42999794199359798, 14.45817062996879976, -47.35267888851409879 ) ) ;
#47079=CARTESIAN_POINT ( 'NONE',  ( 53.02886665414099809, -49.60598562230889996, -49.08317483300949391 ) ) ;
#47083=CARTESIAN_POINT ( 'NONE',  ( -6.439182911200170167, 15.15458290544269992, -5.455094394028799698 ) ) ;
#47084=AXIS2_PLACEMENT_3D ( 'NONE', #444, #27706, #15415 ) ;
#47089=CARTESIAN_POINT ( 'NONE',  ( -4.666062602402590187, -15.61618894541809865, -10.44999999999999929 ) ) ;
#47090=ADVANCED_FACE ( 'NONE', ( #34152 ), #50679, .T. ) ;
#47091=CARTESIAN_POINT ( 'NONE',  ( 57.49777519800270653, 18.87230500023909840, -52.59199339445650168 ) ) ;
#47095=CARTESIAN_POINT ( 'NONE',  ( 71.71126032029680175, -47.11618894467930119, -46.37203261889099792 ) ) ;
#47100=CARTESIAN_POINT ( 'NONE',  ( 48.21059767299840360, -54.29128262287709816, -55.22668602961379491 ) ) ;
#47102=CARTESIAN_POINT ( 'NONE',  ( -2.623662905471100260, -48.66391853184789795, -4.296538310234220504 ) ) ;
#47110=CARTESIAN_POINT ( 'NONE',  ( 57.68257350692169894, -47.11839356109889820, -47.67368955113449402 ) ) ;
#47111=DIRECTION ( 'NONE',  ( 0.000000000000000000, 0.000000000000000000, 1.000000000000000000 ) ) ;
#47116=DIRECTION ( 'NONE',  ( 0.000000000000000000, 0.000000000000000000, -1.000000000000000000 ) ) ;
#47117=EDGE_CURVE ( 'NONE', #45466, #15596, #32587, .T. ) ;
#47123=DIRECTION ( 'NONE',  ( -0.1594746274825657728, 0.3043827052124084553, -0.9391054317577303134 ) ) ;
#47125=CARTESIAN_POINT ( 'NONE',  ( 13.00893739761190027, 34.28605925116320208, -47.75434321210310173 ) ) ;
#47126=CARTESIAN_POINT ( 'NONE',  ( 13.00893739769619906, -65.51843714052719747, -47.75434321273180416 ) ) ;
#47129=EDGE_LOOP ( 'NONE', ( #48179, #49776, #43910, #19053, #49167 ) ) ;
#47130=CARTESIAN_POINT ( 'NONE',  ( 52.85039779125390424, 21.08368931838850102, -54.40094741851120119 ) ) ;
#47131=CARTESIAN_POINT ( 'NONE',  ( 57.06093750417669952, 14.65527943800320010, -26.24896182640730302 ) ) ;
#47134=CARTESIAN_POINT ( 'NONE',  ( 60.94255391806049715, -0.9960295973751170928, -16.13088049791909739 ) ) ;
#47136=ORIENTED_EDGE ( 'NONE', *, *, #17260, .F. ) ;
#47140=CARTESIAN_POINT ( 'NONE',  ( 58.40467996479630131, -46.88273201699870185, -48.03872346596099874 ) ) ;
#47142=CARTESIAN_POINT ( 'NONE',  ( 13.44518348434099941, -50.59875081391439977, -21.34306233502189798 ) ) ;
#47143=VECTOR ( 'NONE', #44684, 1000.000000000000000 ) ;
#47144=CARTESIAN_POINT ( 'NONE',  ( 85.66799001034409855, 19.38381105532069881, -61.58097075742929860 ) ) ;
#47145=CARTESIAN_POINT ( 'NONE',  ( 56.98602380624170394, 13.94694869911280044, -17.71226892537560005 ) ) ;
#47146=CARTESIAN_POINT ( 'NONE',  ( 61.31744649544350523, -45.31589417655599306, -47.18592553472910822 ) ) ;
#47147=CARTESIAN_POINT ( 'NONE',  ( 56.57438608668749680, -50.73277124350089906, -53.83822343189740423 ) ) ;
#47150=ORIENTED_EDGE ( 'NONE', *, *, #11786, .T. ) ;
#47154=B_SPLINE_CURVE_WITH_KNOTS ( 'NONE', 3,
 ( #14746, #22846, #22072, #2178 ),
 .UNSPECIFIED., .F., .F.,
 ( 4, 4 ),
 ( 3.672098967893400179, 3.795380006766150061 ),
 .UNSPECIFIED. ) ;
#47156=CARTESIAN_POINT ( 'NONE',  ( 14.34417029198879945, -51.11618894467930119, -74.14999999999999147 ) ) ;
#47160=CARTESIAN_POINT ( 'NONE',  ( 82.24889378705110232, 13.88381105532070059, -46.39515231851169830 ) ) ;
#47162=CARTESIAN_POINT ( 'NONE',  ( 53.48381654129486407, 19.28794686715378148, -77.13953808112664490 ) ) ;
#47166=EDGE_CURVE ( 'NONE', #16412, #17711, #21946, .T. ) ;
#47167=ORIENTED_EDGE ( 'NONE', *, *, #15430, .F. ) ;
#47168=CARTESIAN_POINT ( 'NONE',  ( 53.05608043003729790, -49.55636941894550063, -48.95471306266509970 ) ) ;
#47172=CARTESIAN_POINT ( 'NONE',  ( 13.97075918456510024, 19.71140667683069836, -21.74703671737670163 ) ) ;
#47175=CARTESIAN_POINT ( 'NONE',  ( 53.11770069264709804, 18.32755088687749989, -49.09731758340100072 ) ) ;
#47176=CARTESIAN_POINT ( 'NONE',  ( 55.48508049412749443, -46.00754199590999605, -16.66510032532799812 ) ) ;
#47177=ADVANCED_FACE ( 'NONE', ( #6659 ), #6404, .F. ) ;
#47178=CARTESIAN_POINT ( 'NONE',  ( 52.61984545813550085, 18.57124442378090023, -27.71374801268470023 ) ) ;
#47179=AXIS2_PLACEMENT_3D ( 'NONE', #47679, #24559, #19876 ) ;
#47183=ORIENTED_EDGE ( 'NONE', *, *, #32815, .F. ) ;
#47184=CARTESIAN_POINT ( 'NONE',  ( 10.90442937958139957, -65.00486786560159658, -17.54871756388219950 ) ) ;
#47185=CARTESIAN_POINT ( 'NONE',  ( 11.42615977560179985, 33.94857426019389379, -47.15336837400249692 ) ) ;
#47187=CYLINDRICAL_SURFACE ( 'NONE', #16812, 20.00000000000000355 ) ;
#47188=CARTESIAN_POINT ( 'NONE',  ( 52.66149646884395708, -49.78765645775953885, -48.73888008360702173 ) ) ;
#47189=CARTESIAN_POINT ( 'NONE',  ( 78.22251691734010137, 1.883811055320649963, -20.65000000000000213 ) ) ;
#47190=CARTESIAN_POINT ( 'NONE',  ( 53.27999729874670010, -52.01684321318150239, -53.62834481722440216 ) ) ;
#47192=CARTESIAN_POINT ( 'NONE',  ( 61.35881578103422385, 14.29392436355511364, -47.58695754661491861 ) ) ;
#47193=CARTESIAN_POINT ( 'NONE',  ( 10.14066804511660003, -63.20557169619659987, -45.99409303117819547 ) ) ;
#47194=CARTESIAN_POINT ( 'NONE',  ( 65.43042069958036677, 17.98087126524680102, -74.20351669811765305 ) ) ;
#47196=CARTESIAN_POINT ( 'NONE',  ( 11.65682018745774862, -64.87102229922230379, -45.04374105511057991 ) ) ;
#47197=CARTESIAN_POINT ( 'NONE',  ( 57.19888499978009833, 19.03589688392159829, -52.76365438364319260 ) ) ;
#47203=DIRECTION ( 'NONE',  ( -0.6911981449639417185, -0.7226652920947607139, 0.000000000000000000 ) ) ;
#47204=CARTESIAN_POINT ( 'NONE',  ( 83.89200044194980421, 17.38381105532069881, -53.92796738110899923 ) ) ;
#47212=CARTESIAN_POINT ( 'NONE',  ( 43.09344256554030750, -43.96039878386999789, -5.051331041927119792 ) ) ;
#47214=CARTESIAN_POINT ( 'NONE',  ( 53.36461353568410004, -49.48324289032530032, -49.20419813977639478 ) ) ;
#47215=CARTESIAN_POINT ( 'NONE',  ( 52.95374953453699618, 13.97573486333550008, -13.31304720699000121 ) ) ;
#47217=CARTESIAN_POINT ( 'NONE',  ( 47.13235806812529916, 23.29804346876840171, -75.11910897646329488 ) ) ;
#47218=EDGE_CURVE ( 'NONE', #22335, #29281, #11627, .T. ) ;
#47219=CARTESIAN_POINT ( 'NONE',  ( 56.81484139663320576, 20.15189430791300040, -54.62103799614550326 ) ) ;
#47221=CARTESIAN_POINT ( 'NONE',  ( 11.84964338388230054, 33.70977198295789634, -16.34215248989290004 ) ) ;
#47224=CARTESIAN_POINT ( 'NONE',  ( 55.15102684342360106, -50.65538451641219808, -76.12015560185260199 ) ) ;
#47225=CARTESIAN_POINT ( 'NONE',  ( -7.078151497284870253, 15.05307759385980049, -6.383383382925239324 ) ) ;
#47228=DIRECTION ( 'NONE',  ( 0.000000000000000000, 0.7071067811865492381, -0.7071067811865457964 ) ) ;
#47231=CARTESIAN_POINT ( 'NONE',  ( -11.32734370190460105, -41.88171845330919751, -6.430192534648670133 ) ) ;
#47232=CARTESIAN_POINT ( 'NONE',  ( 47.58873109027090464, 23.32547039982940262, -55.09264702773990052 ) ) ;
#47235=CARTESIAN_POINT ( 'NONE',  ( 60.90934541243480282, 14.25332586616640107, -47.35593111936199762 ) ) ;
#47237=CARTESIAN_POINT ( 'NONE',  ( 51.30983197266640161, 18.29914825542120127, -76.46178133104609742 ) ) ;
#47238=CARTESIAN_POINT ( 'NONE',  ( 53.20890753634210313, 18.22989461729919825, -48.81584866255500543 ) ) ;
#47240=CARTESIAN_POINT ( 'NONE',  ( 53.18486246474859769, -49.47487039336269987, -48.80133351323340207 ) ) ;
#47241=CARTESIAN_POINT ( 'NONE',  ( 56.18000000035269892, 15.25008180819560089, -26.28768301911490113 ) ) ;
#47242=CARTESIAN_POINT ( 'NONE',  ( 51.12251285489129771, 21.70267151109249681, -54.06580525727419939 ) ) ;
#47246=DIRECTION ( 'NONE',  ( 0.000000000000000000, -1.000000000000000000, 0.000000000000000000 ) ) ;
#47247=CARTESIAN_POINT ( 'NONE',  ( 59.10134146846650083, -28.39131499980770101, -15.65497502716749878 ) ) ;
#47249=CARTESIAN_POINT ( 'NONE',  ( 11.13393739769619906, 32.26595438701649243, -43.75820627627399517 ) ) ;
#47251=PLANE ( 'NONE',  #22592 ) ;
#47253=ORIENTED_EDGE ( 'NONE', *, *, #13678, .F. ) ;
#47256=CARTESIAN_POINT ( 'NONE',  ( 56.39270785951039500, 19.29512406318060158, -52.86271188469099513 ) ) ;
#47257=CARTESIAN_POINT ( 'NONE',  ( 49.24615177809619837, -28.72712112006723473, -15.65000000390069701 ) ) ;
#47259=CARTESIAN_POINT ( 'NONE',  ( 57.54769658797620480, -45.19536826720690215, -25.74814785595830102 ) ) ;
#47262=( BOUNDED_CURVE ( )  B_SPLINE_CURVE ( 3, ( #42500, #2661, #10785, #42761 ),
 .UNSPECIFIED., .F., .T. ) 
 B_SPLINE_CURVE_WITH_KNOTS ( ( 4, 4 ),
 ( 5.310633862803790350, 6.283185307179586232 ),
 .UNSPECIFIED. ) 
 CURVE ( )  GEOMETRIC_REPRESENTATION_ITEM ( )  RATIONAL_B_SPLINE_CURVE ( ( 1.000000000000000000, 0.9227196513546198631, 0.9227196513546198631, 1.000000000000000000 ) ) 
 REPRESENTATION_ITEM ( '' )  );
#47264=DIRECTION ( 'NONE',  ( 0.000000000000000000, 0.000000000000000000, 1.000000000000000000 ) ) ;
#47266=CARTESIAN_POINT ( 'NONE',  ( 11.07146966777600028, 33.73992739275750097, -23.11170492349029715 ) ) ;
#47267=AXIS2_PLACEMENT_3D ( 'NONE', #12269, #45011, #44233 ) ;
#47269=CARTESIAN_POINT ( 'NONE',  ( 49.60975479659560250, -45.11618894467940066, -10.01352555590809956 ) ) ;
#47270=CARTESIAN_POINT ( 'NONE',  ( 51.77632738753401753, 1.364313919546259690, -18.40931367100264282 ) ) ;
#47271=AXIS2_PLACEMENT_3D ( 'NONE', #43033, #42517, #34887 ) ;
#47274=CARTESIAN_POINT ( 'NONE',  ( 59.28498838297480233, -28.11220559536460328, -15.67198671759989814 ) ) ;
#47276=CARTESIAN_POINT ( 'NONE',  ( 47.24371072983239372, -54.76060195732999603, -74.17405913703889553 ) ) ;
#47279=CARTESIAN_POINT ( 'NONE',  ( 44.92064326928819895, 14.77810806019170009, -8.851633222648910504 ) ) ;
#47281=CARTESIAN_POINT ( 'NONE',  ( 8.784728771152170879, 23.70287936274029761, -46.67204636145419983 ) ) ;
#47282=ADVANCED_FACE ( 'NONE', ( #19216 ), #39656, .T. ) ;
#47283=CARTESIAN_POINT ( 'NONE',  ( 84.16059178761608450, -44.05199403092819210, -47.12825410637790213 ) ) ;
#47284=CARTESIAN_POINT ( 'NONE',  ( 60.89367646889060381, 13.88379791406190122, -26.67319840941520326 ) ) ;
#47285=ADVANCED_FACE ( 'NONE', ( #7177 ), #18957, .T. ) ;
#47288=CARTESIAN_POINT ( 'NONE',  ( 52.86782176627269791, -49.62820118223199728, -27.93072220815099982 ) ) ;
#47290=CARTESIAN_POINT ( 'NONE',  ( 6.488565178738439521, -58.66849328915790096, -10.99653483109780083 ) ) ;
#47291=CARTESIAN_POINT ( 'NONE',  ( 76.16277554039029951, -12.50013975853289949, -12.12674910689150032 ) ) ;
#47292=CARTESIAN_POINT ( 'NONE',  ( 75.29346835912031111, 13.39413235022868065, -14.05117889852984625 ) ) ;
#47293=CARTESIAN_POINT ( 'NONE',  ( 13.04440776820920078, -50.02432107381629578, -21.04429564000059827 ) ) ;
#47297=CARTESIAN_POINT ( 'NONE',  ( 82.55449471509389525, -45.62610142152509951, -47.70626815655899833 ) ) ;
#47298=CARTESIAN_POINT ( 'NONE',  ( 57.28394106512169515, -50.61203249062990039, -53.75940136370459754 ) ) ;
#47299=CARTESIAN_POINT ( 'NONE',  ( 41.90536141990470043, 12.91317781275290066, -4.781910917352909962 ) ) ;
#47300=CARTESIAN_POINT ( 'NONE',  ( 49.72648160330889766, -53.64673639094029767, -55.11972614036120177 ) ) ;
#47302=CARTESIAN_POINT ( 'NONE',  ( 56.28816863880509658, -47.87332787221669150, -48.23685133742169739 ) ) ;
#47303=CARTESIAN_POINT ( 'NONE',  ( 65.43393739769584272, -48.11618894467832064, -70.54999999999975557 ) ) ;
#47306=CARTESIAN_POINT ( 'NONE',  ( 18.06700609687609926, -51.63908721605620400, -75.44171726276898937 ) ) ;
#47307=CARTESIAN_POINT ( 'NONE',  ( 49.40539548398250247, -53.49785366680099941, -54.15746054658189479 ) ) ;
#47308=EDGE_CURVE ( 'NONE', #37620, #17080, #38215, .T. ) ;
#47310=CARTESIAN_POINT ( 'NONE',  ( 14.22007337546138217, 19.13837226738661101, -20.84587542004114269 ) ) ;
#47313=CARTESIAN_POINT ( 'NONE',  ( 11.13393739769619906, -63.48206547090349972, -24.15000000000000213 ) ) ;
#47314=CARTESIAN_POINT ( 'NONE',  ( 12.06284766121009966, -63.44323389162830296, -22.25048313876769868 ) ) ;
#47319=CARTESIAN_POINT ( 'NONE',  ( 17.62323348321739758, 20.99223335001410007, -75.94942944171690158 ) ) ;
#47320=VERTEX_POINT ( 'NONE', #7434 ) ;
#47322=DIRECTION ( 'NONE',  ( 0.000000000000000000, 0.000000000000000000, -1.000000000000000000 ) ) ;
#47324=ADVANCED_FACE ( 'NONE', ( #39404 ), #6065, .T. ) ;
#47333=CARTESIAN_POINT ( 'NONE',  ( 51.52597209567689873, -50.62283699257580594, -76.24693437788890549 ) ) ;
#47334=CARTESIAN_POINT ( 'NONE',  ( 60.84128266275949670, 14.46818691485590058, -47.72667381315689994 ) ) ;
#47335=CARTESIAN_POINT ( 'NONE',  ( 15.52232237619649879, 19.54251322374230071, -15.65194197319980063 ) ) ;
#47336=CARTESIAN_POINT ( 'NONE',  ( 40.92757250301959715, -44.41382921904099845, -3.805845460188720164 ) ) ;
#47337=CARTESIAN_POINT ( 'NONE',  ( -8.886174488814990724, 13.01408101563770003, -5.600219702328329774 ) ) ;
#47338=ADVANCED_FACE ( 'NONE', ( #35396 ), #27271, .F. ) ;
#47339=CARTESIAN_POINT ( 'NONE',  ( 47.18306311723954849, 23.57448638813150765, -74.19778950654082905 ) ) ;
#47341=ADVANCED_FACE ( 'NONE', ( #31696 ), #22553, .F. ) ;
#47343=ORIENTED_EDGE ( 'NONE', *, *, #14660, .F. ) ;
#47344=CARTESIAN_POINT ( 'NONE',  ( 55.55365133010059964, 13.88381105532070059, -14.32025150907159983 ) ) ;
#47345=CARTESIAN_POINT ( 'NONE',  ( 57.27298807692499594, 19.38381105532069881, -53.86413101184700736 ) ) ;
#47346=CARTESIAN_POINT ( 'NONE',  ( 11.77497055818396277, -65.42596200258911665, -22.36958828292143764 ) ) ;
#47348=CARTESIAN_POINT ( 'NONE',  ( 15.67955243735830173, 19.63025192210979952, -20.14992656220960043 ) ) ;
#47349=B_SPLINE_CURVE_WITH_KNOTS ( 'NONE', 3,
 ( #45544, #37671, #38722, #10157, #38450, #2818, #41864, #2554, #18531, #18785, #34763, #33977, #50769, #9639, #47363 ),
 .UNSPECIFIED., .F., .F.,
 ( 4, 1, 1, 1, 1, 1, 1, 1, 1, 3, 4 ),
 ( 0.000000000000000000, 0.1110915318836693672, 0.2222019412356212309, 0.3333123505875730808, 0.4444227599395249584, 0.5555331692914780017, 0.6666435786434299349, 0.7777539879953816460, 0.8888643973473335791, 0.9999748066992855122, 1.000000000000000000 ),
 .UNSPECIFIED. ) ;
#47351=AXIS2_PLACEMENT_3D ( 'NONE', #7641, #35918, #11573 ) ;
#47352=CARTESIAN_POINT ( 'NONE',  ( 48.31539888355000301, -54.23126901101980479, -55.06275371778509964 ) ) ;
#47354=CARTESIAN_POINT ( 'NONE',  ( -26.88703640771693770, -41.87805570297800273, -56.26548710561216637 ) ) ;
#47357=CARTESIAN_POINT ( 'NONE',  ( 38.13393739769620083, -15.61618894467929941, -14.65000000000000036 ) ) ;
#47360=ORIENTED_EDGE ( 'NONE', *, *, #37853, .F. ) ;
#47362=CARTESIAN_POINT ( 'NONE',  ( 60.47158259472089981, -45.65949564325300258, -47.26531013111339519 ) ) ;
#47363=CARTESIAN_POINT ( 'NONE',  ( 82.75389963950189554, 14.36256073625980001, -47.67227237920639737 ) ) ;
#47364=DIRECTION ( 'NONE',  ( 0.000000000000000000, 0.000000000000000000, 1.000000000000000000 ) ) ;
#47365=CARTESIAN_POINT ( 'NONE',  ( 83.36355911687300591, 14.11444734287620051, -47.55049236202179230 ) ) ;
#47367=DIRECTION ( 'NONE',  ( 1.000000000000000000, 0.000000000000000000, 0.000000000000000000 ) ) ;
#47374=CARTESIAN_POINT ( 'NONE',  ( 16.13393739769620083, -15.61618894467929941, -4.296538310234230273 ) ) ;
#47375=CARTESIAN_POINT ( 'NONE',  ( 76.43224147390343148, -23.40681064887490948, -12.93543775027620590 ) ) ;
#47376=CARTESIAN_POINT ( 'NONE',  ( 11.39576525640170068, -65.16962161578030077, -47.14206625977179499 ) ) ;
#47378=ORIENTED_EDGE ( 'NONE', *, *, #48211, .F. ) ;
#47379=EDGE_CURVE ( 'NONE', #22075, #47835, #11433, .T. ) ;
#47384=EDGE_CURVE ( 'NONE', #40276, #5858, #35663, .T. ) ;
#47387=CARTESIAN_POINT ( 'NONE',  ( 60.11982335476029959, -1.682419521057920031, -15.87057978292740223 ) ) ;
#47388=CARTESIAN_POINT ( 'NONE',  ( 51.78790344664380285, -49.82581277545029508, -76.67262344587960854 ) ) ;
#47399=CARTESIAN_POINT ( 'NONE',  ( 12.22498024391630089, -50.02555233757460229, -21.14999999988710400 ) ) ;
#47401=CARTESIAN_POINT ( 'NONE',  ( 57.07557850792819920, 13.89582767481270054, -16.81759313181460058 ) ) ;
#47403=CARTESIAN_POINT ( 'NONE',  ( 56.72454650921010000, -50.66101676095649253, -53.46416969206939740 ) ) ;
#47407=ORIENTED_EDGE ( 'NONE', *, *, #30735, .F. ) ;
#47411=CARTESIAN_POINT ( 'NONE',  ( 14.51932309042026503, -51.60941532109461605, -75.47165350116152638 ) ) ;
#47413=CARTESIAN_POINT ( 'NONE',  ( 46.51095038332250198, 13.88381105532070059, -7.695532444495968960 ) ) ;
#47415=FACE_OUTER_BOUND ( 'NONE', #2138, .T. ) ;
#47417=CARTESIAN_POINT ( 'NONE',  ( 11.89539497636670085, 34.20383474698349602, -18.11027658847759980 ) ) ;
#47420=CARTESIAN_POINT ( 'NONE',  ( 11.33851678214776904, 33.17161558030153401, -24.03999305115578622 ) ) ;
#47421=CARTESIAN_POINT ( 'NONE',  ( -6.046668638016009290, -47.40279893552259693, -7.123474707974530418 ) ) ;
#47422=CARTESIAN_POINT ( 'NONE',  ( 49.51533122679629884, 22.46701370878599846, -54.78532408268279852 ) ) ;
#47424=CARTESIAN_POINT ( 'NONE',  ( 52.59421258935810073, -49.83180061336119593, -48.47378032971909789 ) ) ;
#47429=CARTESIAN_POINT ( 'NONE',  ( 82.13853704237929776, -45.25223929932899125, -47.09707863094710945 ) ) ;
#47430=CARTESIAN_POINT ( 'NONE',  ( 84.41931940662119871, 12.04917885348629980, -47.35294421590279512 ) ) ;
#47432=DIRECTION ( 'NONE',  ( 0.000000000000000000, 0.000000000000000000, 1.000000000000000000 ) ) ;
#47433=CARTESIAN_POINT ( 'NONE',  ( 55.01975381464660586, -46.11950308459810088, -16.15585483520260013 ) ) ;
#47438=CARTESIAN_POINT ( 'NONE',  ( 11.23165357234419837, -65.23063573490379952, -17.66286047794729797 ) ) ;
#47439=CARTESIAN_POINT ( 'NONE',  ( 10.25855798689609877, 33.30687331164079978, -46.73983890664589325 ) ) ;
#47441=CARTESIAN_POINT ( 'NONE',  ( 48.47947973770610020, -54.28987983540550033, -55.11210649539159334 ) ) ;
#47442=FACE_OUTER_BOUND ( 'NONE', #4411, .T. ) ;
#47446=CARTESIAN_POINT ( 'NONE',  ( 11.13393739769619906, -63.16362662756800006, -43.74366009427609470 ) ) ;
#47447=EDGE_CURVE ( 'NONE', #40665, #38928, #28069, .T. ) ;
#47452=EDGE_CURVE ( 'NONE', #29481, #22521, #20868, .T. ) ;
#47454=ORIENTED_EDGE ( 'NONE', *, *, #15850, .T. ) ;
#47456=FACE_OUTER_BOUND ( 'NONE', #51366, .T. ) ;
#47463=ORIENTED_EDGE ( 'NONE', *, *, #22147, .F. ) ;
#47471=CARTESIAN_POINT ( 'NONE',  ( 47.32878498007210055, 23.37072882834580057, -74.72254318496639769 ) ) ;
#47474=DIRECTION ( 'NONE',  ( -0.7226652920947592706, -0.6911981449639433839, 0.000000000000000000 ) ) ;
#47475=CARTESIAN_POINT ( 'NONE',  ( 12.09242720216389877, 33.69063605648580761, -16.23377612491680111 ) ) ;
#47476=B_SPLINE_CURVE_WITH_KNOTS ( 'NONE', 3,
 ( #2704, #6635, #22598, #47005, #42023, #26531, #30723, #2435, #18679, #38873, #42282, #50914, #14239, #45956, #34394, #11090, #37832, #27057, #2961, #34652, #43061, #50406, #10050, #26012, #6123, #22079, #50659, #18935, #34916, #51436, #3221, #12118, #40144 ),
 .UNSPECIFIED., .F., .F.,
 ( 4, 2, 2, 1, 2, 2, 2, 2, 2, 2, 1, 2, 2, 2, 2, 2, 1, 4 ),
 ( 0.000000000000000000, 0.06597993765965722013, 0.09896990648948590652, 0.1154648909044010269, 0.1237123831118577544, 0.1319598753193144680, 0.1979398129789769478, 0.2309297818088088539, 0.2474247662237250012, 0.2515485123274531776, 0.2556722584311812985, 0.2639197506386373182, 0.3958796259579234755, 0.4618595636175666375, 0.4948495324473878298, 0.5030970246548429614, 0.5113445168622979820, 0.5278395012772089112 ),
 .UNSPECIFIED. ) ;
#47479=CARTESIAN_POINT ( 'NONE',  ( 54.18612455227970059, -50.67005945099250397, -76.49079485251020571 ) ) ;
#47480=CARTESIAN_POINT ( 'NONE',  ( -8.714254634004609201, 12.03702151998610148, -4.336387236750419483 ) ) ;
#47482=CARTESIAN_POINT ( 'NONE',  ( 67.78236843376264176, -1.116188944679348483, -17.74895402404429845 ) ) ;
#47484=CARTESIAN_POINT ( 'NONE',  ( 53.20889695217059767, -49.46227805200189920, -48.81584933005299831 ) ) ;
#47485=CARTESIAN_POINT ( 'NONE',  ( 47.66159700762720064, 23.24898935426730162, -54.69403258753950325 ) ) ;
#47486=CARTESIAN_POINT ( 'NONE',  ( 57.82682226305900741, -45.74154291786189930, -26.33630567069459616 ) ) ;
#47487=DIRECTION ( 'NONE',  ( -0.000000000000000000, 1.000000000000000000, 0.000000000000000000 ) ) ;
#47488=CARTESIAN_POINT ( 'NONE',  ( 61.31744659937159980, 14.08351620583249897, -47.18592528150829679 ) ) ;
#47490=CARTESIAN_POINT ( 'NONE',  ( 51.67724278084540401, 18.81853346939729832, -76.49491148620110437 ) ) ;
#47491=CARTESIAN_POINT ( 'NONE',  ( 53.31242401630019145, 18.17684692666709978, -48.83993031500360615 ) ) ;
#47498=CARTESIAN_POINT ( 'NONE',  ( 58.97981359800899526, -28.45462689055629824, -15.64989485168480066 ) ) ;
#47500=CARTESIAN_POINT ( 'NONE',  ( 11.13393739769619906, 32.05275509628890518, -43.74635191486320451 ) ) ;
#47502=VECTOR ( 'NONE', #8821, 1000.000000000000114 ) ;
#47503=DIRECTION ( 'NONE',  ( 0.1686178020941810352, -0.6660492713794512465, -0.7265992051412042407 ) ) ;
#47504=DIRECTION ( 'NONE',  ( 0.000000000000000000, 1.000000000000000000, 0.000000000000000000 ) ) ;
#47507=CARTESIAN_POINT ( 'NONE',  ( 41.55663457306080488, 12.62725083537310056, -3.466044030332980252 ) ) ;
#47510=VERTEX_POINT ( 'NONE', #18893 ) ;
#47511=DIRECTION ( 'NONE',  ( -0.6676418852213141797, -0.2329255526946994725, -0.7071067811865463515 ) ) ;
#47514=VERTEX_POINT ( 'NONE', #34614 ) ;
#47517=FACE_OUTER_BOUND ( 'NONE', #40779, .T. ) ;
#47518=CARTESIAN_POINT ( 'NONE',  ( 8.133937397696209715, 23.57564693985150228, -21.14999999999999858 ) ) ;
#47522=CARTESIAN_POINT ( 'NONE',  ( 65.43690392504990427, -30.18759754294940123, -16.56995554360160128 ) ) ;
#47524=CARTESIAN_POINT ( 'NONE',  ( 47.27157043358619859, -54.25876962900459688, -75.35700034530711378 ) ) ;
#47526=CARTESIAN_POINT ( 'NONE',  ( 57.77564497937559906, -28.11618894467929763, -20.65000000000000213 ) ) ;
#47527=CARTESIAN_POINT ( 'NONE',  ( 41.19620264348169769, 14.26403794320130025, -6.107565110250690488 ) ) ;
#47528=EDGE_CURVE ( 'NONE', #17711, #24756, #18368, .T. ) ;
#47529=CARTESIAN_POINT ( 'NONE',  ( 15.05440318628110141, 21.88381105532300097, -76.14999999999999147 ) ) ;
#47530=CARTESIAN_POINT ( 'NONE',  ( 82.96870692852718321, -45.28007837109379352, -47.29707907477579454 ) ) ;
#47532=DIRECTION ( 'NONE',  ( -0.8732394366197168134, -0.4872913772396139098, 0.000000000000000000 ) ) ;
#47536=CARTESIAN_POINT ( 'NONE',  ( 16.22101879094850219, -51.07051632261300256, -20.26096174765880065 ) ) ;
#47537=CARTESIAN_POINT ( 'NONE',  ( 75.15216820663748365, -30.02682016727950298, -11.82535899278000002 ) ) ;
#47538=AXIS2_PLACEMENT_3D ( 'NONE', #13972, #22329, #10037 ) ;
#47543=FACE_OUTER_BOUND ( 'NONE', #26576, .T. ) ;
#47546=CARTESIAN_POINT ( 'NONE',  ( 57.35071418803849497, -50.23458714926779578, -52.74072012029530043 ) ) ;
#47547=CARTESIAN_POINT ( 'NONE',  ( 42.20562667456769645, 13.08589554890109952, -5.077271921742569916 ) ) ;
#47549=DIRECTION ( 'NONE',  ( 1.000000000000000000, 0.000000000000000000, 0.000000000000000000 ) ) ;
#47550=CARTESIAN_POINT ( 'NONE',  ( 0.5406133260286669628, -43.55985091651039909, -20.15000000000000213 ) ) ;
#47553=CARTESIAN_POINT ( 'NONE',  ( 18.32697385714070037, -51.82372487085179813, -75.44171726276898937 ) ) ;
#47554=CARTESIAN_POINT ( 'NONE',  ( 49.94506962897090574, -45.11618894467940066, -8.192301891433340089 ) ) ;
#47557=( BOUNDED_CURVE ( )  B_SPLINE_CURVE ( 3, ( #639, #40476, #28666, #24199 ),
 .UNSPECIFIED., .F., .T. ) 
 B_SPLINE_CURVE_WITH_KNOTS ( ( 4, 4 ),
 ( 4.712388980593780197, 6.283185307179586232 ),
 .UNSPECIFIED. ) 
 CURVE ( )  GEOMETRIC_REPRESENTATION_ITEM ( )  RATIONAL_B_SPLINE_CURVE ( ( 1.000000000000000000, 0.8047378541736481816, 0.8047378541736481816, 1.000000000000000000 ) ) 
 REPRESENTATION_ITEM ( '' )  );
#47558=CARTESIAN_POINT ( 'NONE',  ( 52.56658475560080035, -54.17900319927549191, -56.87455298638129619 ) ) ;
#47561=DIRECTION ( 'NONE',  ( 1.000000000000000000, 0.000000000000000000, 0.000000000000000000 ) ) ;
#47565=ORIENTED_EDGE ( 'NONE', *, *, #30644, .T. ) ;
#47566=CARTESIAN_POINT ( 'NONE',  ( 18.19627591683260093, 21.04516553096049947, -75.75221093576890041 ) ) ;
#47568=EDGE_CURVE ( 'NONE', #48985, #21823, #47676, .T. ) ;
#47569=EDGE_LOOP ( 'NONE', ( #31663, #34131, #6237, #16309 ) ) ;
#47570=CARTESIAN_POINT ( 'NONE',  ( 52.10267382257649871, 1.883811055284760005, -77.60820171200670359 ) ) ;
#47572=LINE ( 'NONE', #15341, #34838 ) ;
#47574=CARTESIAN_POINT ( 'NONE',  ( 61.74755533198759849, 13.88658087425049992, -46.49353895741179343 ) ) ;
#47576=ORIENTED_EDGE ( 'NONE', *, *, #14001, .F. ) ;
#47582=ORIENTED_EDGE ( 'NONE', *, *, #28109, .F. ) ;
#47584=CARTESIAN_POINT ( 'NONE',  ( 51.93758451744589877, -50.81981950107080337, -76.23465793669190305 ) ) ;
#47585=CARTESIAN_POINT ( 'NONE',  ( 60.50469153357809660, 14.48475327612959873, -47.56295389503220150 ) ) ;
#47586=CARTESIAN_POINT ( 'NONE',  ( 15.67962062511290000, 19.63028992866140143, -15.65622423491010196 ) ) ;
#47587=ADVANCED_FACE ( 'NONE', ( #28550 ), #20949, .T. ) ;
#47588=CARTESIAN_POINT ( 'NONE',  ( 40.95606683356889732, -44.38928517632400172, -3.881684254074280194 ) ) ;
#47589=CARTESIAN_POINT ( 'NONE',  ( -7.093926665547340527, 14.66186757398629936, -5.595729436106440247 ) ) ;
#47590=CARTESIAN_POINT ( 'NONE',  ( 46.35275103504439898, 21.67755452994670406, -76.14999999999999147 ) ) ;
#47591=CARTESIAN_POINT ( 'NONE',  ( -11.32734370190460105, -41.88171845330919751, -6.430192534648670133 ) ) ;
#47593=ORIENTED_EDGE ( 'NONE', *, *, #11733, .F. ) ;
#47594=CARTESIAN_POINT ( 'NONE',  ( 54.20961013379049831, 17.70559848872130360, -48.50941760523620161 ) ) ;
#47599=CYLINDRICAL_SURFACE ( 'NONE', #49909, 1.999999999999999112 ) ;
#47600=EDGE_CURVE ( 'NONE', #30115, #16412, #23364, .T. ) ;
#47601=CARTESIAN_POINT ( 'NONE',  ( 12.89656437218379992, 18.76901985379959825, -21.06838189303089948 ) ) ;
#47603=CARTESIAN_POINT ( 'NONE',  ( 48.84331286892799540, -53.99784967936330560, -54.98158588870150254 ) ) ;
#47606=CARTESIAN_POINT ( 'NONE',  ( 47.71251016117639665, 23.27152831638220221, -55.11640457198600274 ) ) ;
#47612=CARTESIAN_POINT ( 'NONE',  ( 60.26025110216870218, -45.78774436170850493, -47.43140372362439905 ) ) ;
#47613=CARTESIAN_POINT ( 'NONE',  ( 55.49599478882979753, -48.26400341526489512, -48.16694294531149723 ) ) ;
#47614=CARTESIAN_POINT ( 'NONE',  ( 83.62039299881514864, 13.30922359856841908, -46.55140764634001016 ) ) ;
#47619=VERTEX_POINT ( 'NONE', #48229 ) ;
#47620=CARTESIAN_POINT ( 'NONE',  ( 16.13393739769620083, -15.61618894467929941, -7.225658350974740074 ) ) ;
#47621=VERTEX_POINT ( 'NONE', #16001 ) ;
#47622=VERTEX_POINT ( 'NONE', #1046 ) ;
#47626=CARTESIAN_POINT ( 'NONE',  ( 9.127478409050889141, -63.94375969884499966, -46.75102855002580071 ) ) ;
#47631=CARTESIAN_POINT ( 'NONE',  ( 56.50306487293649838, -50.76048388989789828, -53.80671209316210479 ) ) ;
#47633=CARTESIAN_POINT ( 'NONE',  ( 58.97986318629950375, -2.782461215938549781, -15.64991376612959861 ) ) ;
#47634=CARTESIAN_POINT ( 'NONE',  ( 51.69077941763050177, -49.33148676370400665, -76.83272514207421011 ) ) ;
#47639=CARTESIAN_POINT ( 'NONE',  ( 60.32372535534924651, 14.61230269747045440, -47.67141866289382079 ) ) ;
#47640=AXIS2_PLACEMENT_3D ( 'NONE', #24728, #20545, #16374 ) ;
#47642=AXIS2_PLACEMENT_3D ( 'NONE', #51592, #15948, #28234 ) ;
#47645=CARTESIAN_POINT ( 'NONE',  ( 12.91624052176669935, -50.10753798784559621, -21.10293742790859994 ) ) ;
#47646=CARTESIAN_POINT ( 'NONE',  ( 54.86383200389320081, 19.39201119830140030, -76.47890740922589714 ) ) ;
#47649=CARTESIAN_POINT ( 'NONE',  ( 57.33235504379430125, 13.88381105532070059, -16.73838572529449920 ) ) ;
#47653=CARTESIAN_POINT ( 'NONE',  ( 11.13393739769619906, -63.52234721269329754, -43.76018303787720498 ) ) ;
#47655=CARTESIAN_POINT ( 'NONE',  ( 46.61750669718259843, 22.00845647425120077, -76.11314270330180420 ) ) ;
#47659=CARTESIAN_POINT ( 'NONE',  ( 14.70129800643555740, -50.53293986238711710, -20.74427331569097177 ) ) ;
#47661=EDGE_CURVE ( 'NONE', #15006, #10642, #7492, .T. ) ;
#47663=CARTESIAN_POINT ( 'NONE',  ( 10.83005342333859922, 33.77654421452230338, -17.86451960232090030 ) ) ;
#47668=CARTESIAN_POINT ( 'NONE',  ( 14.80173184006769382, -52.40467206551404189, -76.02665054607155071 ) ) ;
#47670=CARTESIAN_POINT ( 'NONE',  ( 49.04086831984160000, 22.53609092988610030, -54.46858570338200423 ) ) ;
#47673=VECTOR ( 'NONE', #25111, 1000.000000000000000 ) ;
#47674=CARTESIAN_POINT ( 'NONE',  ( 52.96692110958939992, -49.60671036882420282, -48.95117873441440537 ) ) ;
#47676=CIRCLE ( 'NONE', #6674, 4.065467063327089292 ) ;
#47679=CARTESIAN_POINT ( 'NONE',  ( 16.13393739769620083, -15.61618894467929941, -48.64999999999999858 ) ) ;
#47682=CARTESIAN_POINT ( 'NONE',  ( 52.77399500191609860, 18.49248106158579930, -48.90117827005099826 ) ) ;
#47683=CARTESIAN_POINT ( 'NONE',  ( 56.63448749956920381, -45.12949307036979718, -15.89371657090130086 ) ) ;
#47688=CARTESIAN_POINT ( 'NONE',  ( 11.44080321505469833, -65.29620232506569266, -17.48917031883349793 ) ) ;
#47689=CARTESIAN_POINT ( 'NONE',  ( 11.47750026906150111, 33.80079264447829956, -46.66654629083320316 ) ) ;
#47692=CARTESIAN_POINT ( 'NONE',  ( 53.41103307671369294, -49.40180341210120218, -49.08863635434799733 ) ) ;
#47693=CARTESIAN_POINT ( 'NONE',  ( 10.96077434704564801, -64.78872648947765356, -23.23801892677574088 ) ) ;
#47698=CARTESIAN_POINT ( 'NONE',  ( 11.13393739769619906, -63.47497630073510777, -43.75645565886269850 ) ) ;
#47699=CARTESIAN_POINT ( 'NONE',  ( 13.42155525365338065, 20.57173965391032411, -74.52173647802152345 ) ) ;
#47702=CARTESIAN_POINT ( 'NONE',  ( 56.57206750253590855, 19.50115452726630139, -53.72158482572499594 ) ) ;
#47703=B_SPLINE_CURVE_WITH_KNOTS ( 'NONE', 3,
 ( #23297, #43261, #39318, #51627, #15982, #46942, #3422, #31678, #14948, #11803 ),
 .UNSPECIFIED., .F., .F.,
 ( 4, 1, 1, 1, 1, 1, 1, 4 ),
 ( 0.000000000000000000, 0.1428420414407585159, 0.2857017012006322632, 0.4285613609605059549, 0.5714210207203787029, 0.7142806804802525056, 0.8571403402401261973, 1.000000000000000000 ),
 .UNSPECIFIED. ) ;
#47707=CARTESIAN_POINT ( 'NONE',  ( 51.08534821908290269, 19.80328544295542770, -76.14824059617301089 ) ) ;
#47710=DIRECTION ( 'NONE',  ( 1.000000000000000000, 0.000000000000000000, 0.000000000000000000 ) ) ;
#47712=ORIENTED_EDGE ( 'NONE', *, *, #23096, .F. ) ;
#47721=CARTESIAN_POINT ( 'NONE',  ( 46.66794420925759823, 22.33509408192179890, -76.02748009641369720 ) ) ;
#47724=CARTESIAN_POINT ( 'NONE',  ( 11.90346178787130071, 33.73586922521850084, -16.35924802166870151 ) ) ;
#47727=EDGE_CURVE ( 'NONE', #10101, #21277, #13715, .T. ) ;
#47728=CARTESIAN_POINT ( 'NONE',  ( 56.02466961400099876, -50.67465440105149810, -75.43166099610559172 ) ) ;
#47729=CARTESIAN_POINT ( 'NONE',  ( 1.192719620188050111, 22.32378988226099992, -7.795412869570020220 ) ) ;
#47732=CARTESIAN_POINT ( 'NONE',  ( 61.41101597850759930, 13.95334023698869963, -46.65852037685949938 ) ) ;
#47735=ORIENTED_EDGE ( 'NONE', *, *, #41234, .T. ) ;
#47736=CARTESIAN_POINT ( 'NONE',  ( 52.96420272660349582, -49.59048021264120365, -48.77461995705460396 ) ) ;
#47737=CARTESIAN_POINT ( 'NONE',  ( 61.43364071597069653, -45.16647806383540598, -28.15110207759829919 ) ) ;
#47739=CARTESIAN_POINT ( 'NONE',  ( 60.96771750282989899, 14.26879997633939823, -47.44758383409369884 ) ) ;
#47741=CARTESIAN_POINT ( 'NONE',  ( 51.62537654974559587, 17.96288684338239960, -76.81862610352639820 ) ) ;
#47742=CARTESIAN_POINT ( 'NONE',  ( 52.74228737775210618, 18.48090198830360009, -48.57744821062869534 ) ) ;
#47744=CARTESIAN_POINT ( 'NONE',  ( 53.05372066228549954, -49.54357925801589602, -48.79446872794070345 ) ) ;
#47748=CARTESIAN_POINT ( 'NONE',  ( 47.63173516101420546, -54.51015595446700246, -54.75624560665560381 ) ) ;
#47752=CARTESIAN_POINT ( 'NONE',  ( 61.44797978346510803, -30.90289317591489748, -16.49569814832250003 ) ) ;
#47754=CARTESIAN_POINT ( 'NONE',  ( 11.13393739769619906, 32.13925317360830292, -43.75007275908160409 ) ) ;
#47758=EDGE_CURVE ( 'NONE', #15596, #42552, #33259, .T. ) ;
#47764=CARTESIAN_POINT ( 'NONE',  ( 87.61621807841599718, -33.11618894467940066, -61.12885639714370001 ) ) ;
#47765=ORIENTED_EDGE ( 'NONE', *, *, #39396, .F. ) ;
#47766=CARTESIAN_POINT ( 'NONE',  ( 56.67587010945499770, -45.29461281360359948, -25.29358288562269763 ) ) ;
#47769=CARTESIAN_POINT ( 'NONE',  ( 11.41737698698953629, 34.03946597324494405, -22.74029088214029670 ) ) ;
#47775=( LENGTH_UNIT ( ) NAMED_UNIT ( * ) SI_UNIT ( .MILLI., .METRE. ) );
#47776=CARTESIAN_POINT ( 'NONE',  ( 59.79173912391249246, -28.94653353880099900, -15.75539910036690294 ) ) ;
#47779=CARTESIAN_POINT ( 'NONE',  ( 55.83251375037820452, 14.69215176195739936, -17.34604097549789969 ) ) ;
#47780=CARTESIAN_POINT ( 'NONE',  ( 41.62257857717389697, 13.94622149448480108, -6.029585542484710459 ) ) ;
#47781=CARTESIAN_POINT ( 'NONE',  ( 14.97490622639899982, 21.71079195693500097, -76.14999999999999147 ) ) ;
#47782=AXIS2_PLACEMENT_3D ( 'NONE', #8274, #7771, #27920 ) ;
#47783=CARTESIAN_POINT ( 'NONE',  ( 82.84359872746441056, -45.06894711141969623, -46.75796921614900015 ) ) ;
#47785=CIRCLE ( 'NONE', #50301, 17.39999999999999503 ) ;
#47788=CARTESIAN_POINT ( 'NONE',  ( 85.66799001034409855, -48.61618894467930119, -61.58097075742929860 ) ) ;
#47789=B_SPLINE_CURVE_WITH_KNOTS ( 'NONE', 3,
 ( #24245, #32630, #4360, #16416, #178, #51804 ),
 .UNSPECIFIED., .F., .F.,
 ( 4, 2, 4 ),
 ( 0.5025462808315325214, 0.7512731404157662052, 1.000000000000000000 ),
 .UNSPECIFIED. ) ;
#47791=CARTESIAN_POINT ( 'NONE',  ( 15.65736449272620057, -50.94086818095720304, -20.65166207265509968 ) ) ;
#47792=CARTESIAN_POINT ( 'NONE',  ( 50.92696022065899086, -35.35053649607394988, -76.36237708703390581 ) ) ;
#47794=CARTESIAN_POINT ( 'NONE',  ( 13.29196628753849829, -50.07647855290770167, -21.00283603508880148 ) ) ;
#47797=CARTESIAN_POINT ( 'NONE',  ( 47.21472468777420062, 23.54994789198669736, -54.62442519253269779 ) ) ;
#47800=CARTESIAN_POINT ( 'NONE',  ( 57.46727618224160494, -50.61618894467939356, -53.87377490133690117 ) ) ;
#47801=CARTESIAN_POINT ( 'NONE',  ( 42.11495618719890643, 12.77424371615120080, -4.742906899983229785 ) ) ;
#47804=CARTESIAN_POINT ( 'NONE',  ( 68.13393739769630031, -48.11618894467930119, -73.25000000000000000 ) ) ;
#47808=B_SPLINE_SURFACE_WITH_KNOTS ( 'NONE', 3, 3, ( 
 ( #21299, #49634, #9536, #44392, #1140, #40974, #32823, #37043 ),
 ( #24699, #24440, #13216, #40454, #36514, #37304, #17652, #29167 ),
 ( #45168, #4547, #17136, #17391, #44645, #33356, #33087, #49118 ),
 ( #20519, #8751, #40718, #13472, #16875, #29428, #21559, #5604 ),
 ( #25487, #4814, #20781, #36773, #38083, #26007, #38867, #50909 ),
 ( #46220, #6118, #18414, #2179, #45690, #29934, #34125, #46480 ),
 ( #26268, #10043, #9791, #14233, #18927, #34646, #22073, #25742 ),
 ( #1921, #50135, #22847, #37827, #34911, #41749, #13978, #38609 ),
 ( #2956, #17899, #29679, #5856, #42275, #21819, #6629, #33871 ),
 ( #26787, #22593, #49882, #42800, #45951, #34388, #42016, #18159 ) ),
 .UNSPECIFIED., .F., .F., .F.,
 ( 4, 1, 1, 1, 1, 1, 1, 4 ),
 ( 4, 2, 2, 4 ),
 ( -3.285243819981630014E-05, 0.1428571428571430157, 0.2857142857142860315, 0.4285714285714289917, 0.5714285714285709528, 0.7142857142857139685, 0.8571428571428569843, 1.000000000000000000 ),
 ( 1.570647095086020073, 1.792618180878300160, 2.161517997136110036, 2.169191869667270289 ),
 .UNSPECIFIED. ) ;
#47809=EDGE_CURVE ( 'NONE', #40337, #7646, #13374, .T. ) ;
#47811=CARTESIAN_POINT ( 'NONE',  ( 15.67962062493570130, 19.63028992856250099, -20.15000000000000213 ) ) ;
#47812=CARTESIAN_POINT ( 'NONE',  ( 60.36614594669769929, -45.86778937511110144, -47.74314716484730070 ) ) ;
#47814=CARTESIAN_POINT ( 'NONE',  ( 8.802044555037090490, 31.97380483823370056, -46.67015369154350424 ) ) ;
#47817=CARTESIAN_POINT ( 'NONE',  ( 68.13393739769620083, -50.61618894467930119, -65.65000000000000568 ) ) ;
#47821=CARTESIAN_POINT ( 'NONE',  ( 17.35064738833469988, 21.75175735174070013, -76.14999999999999147 ) ) ;
#47822=ORIENTED_EDGE ( 'NONE', *, *, #48877, .T. ) ;
#47823=ADVANCED_FACE ( 'NONE', ( #34575 ), #11828, .T. ) ;
#47824=VERTEX_POINT ( 'NONE', #4937 ) ;
#47829=ORIENTED_EDGE ( 'NONE', *, *, #27906, .F. ) ;
#47830=VECTOR ( 'NONE', #39245, 1000.000000000000000 ) ;
#47833=CARTESIAN_POINT ( 'NONE',  ( 11.37681742080861724, -64.48564029933889685, -24.02179917343915605 ) ) ;
#47835=VERTEX_POINT ( 'NONE', #37171 ) ;
#47838=CARTESIAN_POINT ( 'NONE',  ( 60.76566018258669999, 14.49059974634529979, -47.73209457277470591 ) ) ;
#47841=CARTESIAN_POINT ( 'NONE',  ( -7.613869289485230674, 14.13164915896370033, -5.447993287580489508 ) ) ;
#47843=CARTESIAN_POINT ( 'NONE',  ( 61.28586840673359859, 13.99814824549559944, -28.15105127600999779 ) ) ;
#47849=CARTESIAN_POINT ( 'NONE',  ( 11.13287445219570060, 32.39951296077789777, -43.97623713944630452 ) ) ;
#47853=VECTOR ( 'NONE', #23214, 1000.000000000000000 ) ;
#47854=( BOUNDED_CURVE ( )  B_SPLINE_CURVE ( 3, ( #128, #16618, #32062, #16892 ),
 .UNSPECIFIED., .F., .T. ) 
 B_SPLINE_CURVE_WITH_KNOTS ( ( 4, 4 ),
 ( 4.774929739927229910, 4.797305365512180231 ),
 .UNSPECIFIED. ) 
 CURVE ( )  GEOMETRIC_REPRESENTATION_ITEM ( )  RATIONAL_B_SPLINE_CURVE ( ( 1.000000000000000000, 0.9999582780501610202, 0.9999582780501610202, 1.000000000000000000 ) ) 
 REPRESENTATION_ITEM ( '' )  );
#47855=CIRCLE ( 'NONE', #26062, 1.994283377130261936 ) ;
#47858=FACE_OUTER_BOUND ( 'NONE', #27926, .T. ) ;
#47860=CARTESIAN_POINT ( 'NONE',  ( 48.30230902372879598, -54.16106876602380282, -54.73485062140290580 ) ) ;
#47864=CARTESIAN_POINT ( 'NONE',  ( 47.79361911714689626, 23.20098628971269861, -54.82768723803160071 ) ) ;
#47867=DIRECTION ( 'NONE',  ( 0.1686178020941689892, -0.6660492713794449182, -0.7265992051412129005 ) ) ;
#47870=CARTESIAN_POINT ( 'NONE',  ( 60.60270475073690477, -45.62234656557190249, -47.40029600766140305 ) ) ;
#47871=CARTESIAN_POINT ( 'NONE',  ( 48.44331161791654239, -54.05217057865579022, -54.60670978497837069 ) ) ;
#47878=CARTESIAN_POINT ( 'NONE',  ( 8.133937397696209715, -63.11543068638779630, -43.74348518090240390 ) ) ;
#47881=ORIENTED_EDGE ( 'NONE', *, *, #17029, .T. ) ;
#47883=CARTESIAN_POINT ( 'NONE',  ( 52.28356688864503354, -49.79961370504300078, -77.20029278302882858 ) ) ;
#47884=CARTESIAN_POINT ( 'NONE',  ( 76.39135428410857287, -16.88413607353903956, -12.75926757094217834 ) ) ;
#47885=ORIENTED_EDGE ( 'NONE', *, *, #31858, .T. ) ;
#47888=CARTESIAN_POINT ( 'NONE',  ( 57.40229053555950145, -45.11825314355339600, -25.32419692437829895 ) ) ;
#47889=CARTESIAN_POINT ( 'NONE',  ( 56.46192173573589912, -50.77770442342179535, -53.81433447105879253 ) ) ;
#47891=CARTESIAN_POINT ( 'NONE',  ( 63.27737188425489023, -0.05603756615965699989, -16.72622626800460210 ) ) ;
#47892=CARTESIAN_POINT ( 'NONE',  ( 51.62357988847099932, -48.69300505533869483, -76.93789418233480149 ) ) ;
#47893=B_SPLINE_CURVE_WITH_KNOTS ( 'NONE', 3,
 ( #17793, #2328, #21967, #6268, #37715, #14639, #10716, #30609, #37977, #46630, #6524 ),
 .UNSPECIFIED., .F., .F.,
 ( 4, 1, 1, 1, 1, 1, 1, 1, 4 ),
 ( 0.000000000000000000, 0.1250000000000000000, 0.2500000000000000000, 0.3750000000000000000, 0.5000000000000000000, 0.6250000000000000000, 0.7500000000000000000, 0.8750000000000000000, 1.000000000000000000 ),
 .UNSPECIFIED. ) ;
#47894=AXIS2_PLACEMENT_3D ( 'NONE', #50065, #10237, #6826 ) ;
#47898=CARTESIAN_POINT ( 'NONE',  ( 52.34620911275789723, -49.91415201639770771, -77.13858419677869449 ) ) ;
#47902=CARTESIAN_POINT ( 'NONE',  ( 13.68912331542219896, -50.41132277470529743, -21.10135350628850048 ) ) ;
#47905=CARTESIAN_POINT ( 'NONE',  ( 56.87728296015039575, 13.88381105532070059, -15.74456185640559980 ) ) ;
#47906=CARTESIAN_POINT ( 'NONE',  ( 60.86534162328889863, -45.45085216985310694, -47.04167545792570593 ) ) ;
#47911=CARTESIAN_POINT ( 'NONE',  ( 13.48116687393109991, -51.59710020169690381, -74.14993170018701107 ) ) ;
#47913=CARTESIAN_POINT ( 'NONE',  ( 47.40275506224949709, -54.64653644620720030, -54.66607417010540360 ) ) ;
#47914=( NAMED_UNIT ( * ) PLANE_ANGLE_UNIT ( ) SI_UNIT ( $, .RADIAN. ) );
#47920=CARTESIAN_POINT ( 'NONE',  ( 47.02070054993090054, -53.74782267376620126, -75.86501933388160523 ) ) ;
#47922=CARTESIAN_POINT ( 'NONE',  ( 11.46916641887110089, 34.13456839452390312, -17.97103954068960263 ) ) ;
#47925=CARTESIAN_POINT ( 'NONE',  ( -5.738263256628330033, -47.06162393351850426, -5.576567369078139436 ) ) ;
#47928=CARTESIAN_POINT ( 'NONE',  ( 48.98237048593380649, 22.65102318943320014, -54.72464718890729785 ) ) ;
#47931=CARTESIAN_POINT ( 'NONE',  ( 52.98400451483280449, -49.60704343698500196, -48.99793967229260261 ) ) ;
#47936=CARTESIAN_POINT ( 'NONE',  ( 83.56294434887010425, 13.44742886806319859, -46.81484486652620092 ) ) ;
#47938=CARTESIAN_POINT ( 'NONE',  ( 52.70127179790330274, 18.52894807824059953, -48.78999762614679980 ) ) ;
#47939=CARTESIAN_POINT ( 'NONE',  ( 56.17223871318630302, -45.28676914461929925, -16.17739736399530059 ) ) ;
#47945=CARTESIAN_POINT ( 'NONE',  ( 11.22384634879449905, -65.01277928531338546, -16.94931743789749845 ) ) ;
#47946=CARTESIAN_POINT ( 'NONE',  ( 12.41878523604639994, 34.20092968456749816, -47.33836379614209733 ) ) ;
#47948=CARTESIAN_POINT ( 'NONE',  ( 50.15663463400569810, -52.84355308394439987, -53.36882020266619975 ) ) ;
#47949=CARTESIAN_POINT ( 'NONE',  ( 11.02457163261952822, -64.89120435510172058, -23.16550869442561833 ) ) ;
#47950=CARTESIAN_POINT ( 'NONE',  ( 51.35983792756474742, 3.333806696842658290, -76.65609622433946413 ) ) ;
#47951=VERTEX_POINT ( 'NONE', #10164 ) ;
#47952=DIRECTION ( 'NONE',  ( 1.000000000000000000, 0.000000000000000000, 0.000000000000000000 ) ) ;
#47953=CARTESIAN_POINT ( 'NONE',  ( 11.13393739769619906, -63.20944975704810531, -43.74432592331839942 ) ) ;
#47955=CARTESIAN_POINT ( 'NONE',  ( 68.13393739769810509, 19.38381105532030091, -71.50000000000198952 ) ) ;
#47958=CARTESIAN_POINT ( 'NONE',  ( 56.73072851102580216, 19.11736299019269936, -52.75329813363410381 ) ) ;
#47959=CARTESIAN_POINT ( 'NONE',  ( 12.13393739769638913, 24.18330853958551074, -22.88372919474997857 ) ) ;
#47965=CARTESIAN_POINT ( 'NONE',  ( 51.97663139176439984, 19.86204042051310026, -51.25532567384490079 ) ) ;
#47968=CARTESIAN_POINT ( 'NONE',  ( 53.29384558423090112, 19.31433099946569953, -28.15000000000000213 ) ) ;
#47969=CARTESIAN_POINT ( 'NONE',  ( 73.38393739769610136, 4.883811055320659733, -84.94863984844540994 ) ) ;
#47971=VERTEX_POINT ( 'NONE', #51546 ) ;
#47973=AXIS2_PLACEMENT_3D ( 'NONE', #19845, #24268, #35836 ) ;
#47974=CARTESIAN_POINT ( 'NONE',  ( 1.027904703268269992, 11.45423359053189927, -15.65000000000000036 ) ) ;
#47976=CARTESIAN_POINT ( 'NONE',  ( 47.27371103217519988, 23.27521486086419955, -75.00312280669810150 ) ) ;
#47979=EDGE_CURVE ( 'NONE', #3425, #28507, #4353, .T. ) ;
#47980=CARTESIAN_POINT ( 'NONE',  ( 12.06706412657739946, 33.80468957826779786, -16.41672221714649993 ) ) ;
#47984=CARTESIAN_POINT ( 'NONE',  ( 57.13425863431969987, -50.61839434688920392, -74.14885654434310425 ) ) ;
#47989=CARTESIAN_POINT ( 'NONE',  ( 61.25468486569459969, 14.04656514930960043, -46.98529749939520173 ) ) ;
#47992=CARTESIAN_POINT ( 'NONE',  ( 52.81905794073989568, -49.66695704333110228, -48.62057682596950059 ) ) ;
#47993=CARTESIAN_POINT ( 'NONE',  ( 57.34862278082039921, -45.74573972699900537, -26.25059263399790410 ) ) ;
#47995=CARTESIAN_POINT ( 'NONE',  ( 56.98351099668879982, 14.61386344210539789, -26.22547853219269953 ) ) ;
#47997=CARTESIAN_POINT ( 'NONE',  ( 51.46000097675949547, 18.08790154638520065, -76.62475863243518859 ) ) ;
#47998=CARTESIAN_POINT ( 'NONE',  ( 53.33641448323419354, 18.17849414707670164, -48.94981348398439991 ) ) ;
#48000=CARTESIAN_POINT ( 'NONE',  ( 53.06963669637619319, -49.53524040181889632, -48.79723990372919218 ) ) ;
#48001=VERTEX_POINT ( 'NONE', #23733 ) ;
#48004=CARTESIAN_POINT ( 'NONE',  ( 47.75094631897339781, -54.46528010514310125, -54.88743874810780454 ) ) ;
#48007=CARTESIAN_POINT ( 'NONE',  ( 61.28317973945440400, -30.65315163351740324, -16.34104759998400169 ) ) ;
#48009=DIRECTION ( 'NONE',  ( 1.000000000000000000, 0.000000000000000000, 0.000000000000000000 ) ) ;
#48010=AXIS2_PLACEMENT_3D ( 'NONE', #26530, #50404, #51435 ) ;
#48012=CARTESIAN_POINT ( 'NONE',  ( 50.97850582344351977, -35.25929517202420271, -76.38917648635938917 ) ) ;
#48013=CARTESIAN_POINT ( 'NONE',  ( 61.26569908036744039, -45.23341354807755721, -27.95968211902695799 ) ) ;
#48018=EDGE_LOOP ( 'NONE', ( #23209, #27109, #11671, #39696, #16227, #36973 ) ) ;
#48025=EDGE_CURVE ( 'NONE', #35705, #2432, #859, .T. ) ;
#48027=CARTESIAN_POINT ( 'NONE',  ( 52.71325343205820246, -49.75453022050439955, -48.80820688877259528 ) ) ;
#48031=CARTESIAN_POINT ( 'NONE',  ( 10.85466640524320070, 33.73459223951330443, -17.55961383757199812 ) ) ;
#48033=EDGE_CURVE ( 'NONE', #8205, #30697, #17601, .T. ) ;
#48035=CARTESIAN_POINT ( 'NONE',  ( 11.59229128443909929, -65.37912454849278276, -22.55625441136039910 ) ) ;
#48037=CARTESIAN_POINT ( 'NONE',  ( 43.41855353999969935, 14.15426166984780032, -7.209154067359100360 ) ) ;
#48038=B_SPLINE_CURVE_WITH_KNOTS ( 'NONE', 3,
 ( #30124, #46921, #34576, #11007, #37750, #38009, #30641, #21742, #18082, #26450 ),
 .UNSPECIFIED., .F., .F.,
 ( 4, 2, 2, 2, 4 ),
 ( 0.000000000000000000, 0.2493604919034558554, 0.3740407378551894313, 0.4363808608310561499, 0.4987209838069229795 ),
 .UNSPECIFIED. ) ;
#48039=CARTESIAN_POINT ( 'NONE',  ( 13.96110342106720026, 21.00531966820119933, -75.65676662446109901 ) ) ;
#48040=CARTESIAN_POINT ( 'NONE',  ( 52.08783364885010059, 18.38123939400390228, -77.13960933460720071 ) ) ;
#48041=CARTESIAN_POINT ( 'NONE',  ( 83.30156758793411598, -44.93098646499529991, -46.93423283396209911 ) ) ;
#48044=EDGE_CURVE ( 'NONE', #13074, #16879, #16864, .T. ) ;
#48046=CARTESIAN_POINT ( 'NONE',  ( 53.56320387222690016, -48.99516858426609645, -27.18005901862589724 ) ) ;
#48047=CARTESIAN_POINT ( 'NONE',  ( 14.01533392342379969, -50.49302913403720083, -21.05253849812260114 ) ) ;
#48052=ORIENTED_EDGE ( 'NONE', *, *, #9245, .F. ) ;
#48054=CARTESIAN_POINT ( 'NONE',  ( 47.32853495261879573, 23.46463025610070119, -54.63689417515509916 ) ) ;
#48057=CARTESIAN_POINT ( 'NONE',  ( 57.46594764351250006, -50.61618894467939356, -53.92796738109959875 ) ) ;
#48058=CARTESIAN_POINT ( 'NONE',  ( 41.74202016262009352, 12.84695517036499979, -4.572451372512130519 ) ) ;
#48060=DIRECTION ( 'NONE',  ( 1.000000000000000000, 0.000000000000000000, 0.000000000000000000 ) ) ;
#48061=CARTESIAN_POINT ( 'NONE',  ( 55.06144681897199433, -48.49167527187719884, -48.36672530871140196 ) ) ;
#48062=CARTESIAN_POINT ( 'NONE',  ( 68.13393739769840352, -50.61618894467879670, -73.25000000000220268 ) ) ;
#48065=CARTESIAN_POINT ( 'NONE',  ( 17.21347160910390173, -53.11618894467930119, -76.14999999999999147 ) ) ;
#48068=ORIENTED_EDGE ( 'NONE', *, *, #23765, .T. ) ;
#48074=CARTESIAN_POINT ( 'NONE',  ( 18.30677137431719714, 21.00531966820109986, -75.65676662446099954 ) ) ;
#48077=ORIENTED_EDGE ( 'NONE', *, *, #44165, .F. ) ;
#48078=CARTESIAN_POINT ( 'NONE',  ( 56.62831714707169795, -46.14027970578780469, -26.25643374699650323 ) ) ;
#48082=CARTESIAN_POINT ( 'NONE',  ( 12.13393739769649926, 24.18330853958550364, -74.14999999999999147 ) ) ;
#48086=EDGE_CURVE ( 'NONE', #7993, #6837, #31778, .T. ) ;
#48088=VERTEX_POINT ( 'NONE', #48125 ) ;
#48091=CARTESIAN_POINT ( 'NONE',  ( 60.30540951500729818, 14.59285682385899996, -47.61343627861140249 ) ) ;
#48094=CARTESIAN_POINT ( 'NONE',  ( 40.50275677532349761, -44.77423425411610225, -4.148922563335220026 ) ) ;
#48095=CARTESIAN_POINT ( 'NONE',  ( -2.629620175395499970, 17.44203635409839848, -4.565428260498799240 ) ) ;
#48097=CARTESIAN_POINT ( 'NONE',  ( 61.28594175748709461, 13.99813740456359845, -28.10457713912520106 ) ) ;
#48100=ORIENTED_EDGE ( 'NONE', *, *, #39936, .T. ) ;
#48101=CARTESIAN_POINT ( 'NONE',  ( 57.27937794702199170, 16.09726112234089968, -47.83631691340819714 ) ) ;
#48103=LINE ( 'NONE', #11954, #11882 ) ;
#48104=CARTESIAN_POINT ( 'NONE',  ( 12.75847677699380078, 34.25788405236250611, -47.26854789447209271 ) ) ;
#48108=DIRECTION ( 'NONE',  ( 0.000000000000000000, -1.000000000000000000, 0.000000000000000000 ) ) ;
#48109=CARTESIAN_POINT ( 'NONE',  ( 46.70834335223779732, 22.49584860873379810, -75.96332501265769110 ) ) ;
#48110=CARTESIAN_POINT ( 'NONE',  ( 48.54167993331880382, -54.06704517894050355, -54.75887336934849259 ) ) ;
#48111=CARTESIAN_POINT ( 'NONE',  ( -8.870287765918970280, 13.09110620826400151, -5.844096418666690163 ) ) ;
#48113=DIRECTION ( 'NONE',  ( 0.000000000000000000, 0.000000000000000000, 1.000000000000000000 ) ) ;
#48115=ORIENTED_EDGE ( 'NONE', *, *, #50166, .T. ) ;
#48120=CARTESIAN_POINT ( 'NONE',  ( 60.39135641171679936, -45.74253818135839822, -47.49811677804770227 ) ) ;
#48125=CARTESIAN_POINT ( 'NONE',  ( 16.15069456443260520, -51.05177125324679110, -20.15000000000000213 ) ) ;
#48128=CARTESIAN_POINT ( 'NONE',  ( 83.05638573198200447, -45.46258680162930688, -47.55746740334460299 ) ) ;
#48129=AXIS2_PLACEMENT_3D ( 'NONE', #51383, #8131, #39584 ) ;
#48131=VERTEX_POINT ( 'NONE', #19825 ) ;
#48133=CARTESIAN_POINT ( 'NONE',  ( 52.38380618068715933, -49.88586802196508785, -77.22917115513992314 ) ) ;
#48134=CARTESIAN_POINT ( 'NONE',  ( 76.39110052345097301, -16.48608635013552615, -12.75816298384496683 ) ) ;
#48135=CARTESIAN_POINT ( 'NONE',  ( 49.44978923146539529, -53.54099393320139910, -54.25462396068540016 ) ) ;
#48137=ORIENTED_EDGE ( 'NONE', *, *, #36167, .T. ) ;
#48138=CARTESIAN_POINT ( 'NONE',  ( 47.81335647225210295, 23.16511464041720103, -54.71582838624409817 ) ) ;
#48139=CARTESIAN_POINT ( 'NONE',  ( 57.45483112941150239, -45.11618894539299873, -25.32823465277989783 ) ) ;
#48140=CARTESIAN_POINT ( 'NONE',  ( 56.38083218843890165, -50.72507171055699615, -53.29065863793299229 ) ) ;
#48148=CARTESIAN_POINT ( 'NONE',  ( 52.78679729302229617, -50.32040557307429651, -76.98734330441610041 ) ) ;
#48149=CARTESIAN_POINT ( 'NONE',  ( 60.23130391297029718, 14.55066440145539985, -47.24246919202519734 ) ) ;
#48152=CARTESIAN_POINT ( 'NONE',  ( 12.32752820270880001, -50.13317366860820101, -21.15176873371889954 ) ) ;
#48153=CARTESIAN_POINT ( 'NONE',  ( 18.80380761535086265, -51.60309332616136402, -15.76544335866666913 ) ) ;
#48155=CARTESIAN_POINT ( 'NONE',  ( 61.31460642264700311, -45.57262733401680777, -47.65164362830709877 ) ) ;
#48163=CARTESIAN_POINT ( 'NONE',  ( 13.78482046302009856, -51.32863061914500236, -74.59027663913769857 ) ) ;
#48164=CARTESIAN_POINT ( 'NONE',  ( 47.31045676778030185, -54.71408003619829685, -54.75273663584969341 ) ) ;
#48169=CARTESIAN_POINT ( 'NONE',  ( 60.88209114001612932, -45.44978581739131585, -47.12495023380284920 ) ) ;
#48175=CARTESIAN_POINT ( 'NONE',  ( 14.55219295556159409, -51.70197612871098869, -75.56421430877743717 ) ) ;
#48176=CARTESIAN_POINT ( 'NONE',  ( 48.56282070406520290, 22.79147592108370191, -54.65722455203289343 ) ) ;
#48178=CARTESIAN_POINT ( 'NONE',  ( 52.64536150580070029, -49.78637824963190184, -48.56191546059360320 ) ) ;
#48179=ORIENTED_EDGE ( 'NONE', *, *, #34207, .T. ) ;
#48182=CARTESIAN_POINT ( 'NONE',  ( 83.09574564639500238, 13.66248835152879870, -46.39644155595900799 ) ) ;
#48183=CARTESIAN_POINT ( 'NONE',  ( 53.22743915834050199, 17.91784085086679923, -26.91023106930159869 ) ) ;
#48185=CARTESIAN_POINT ( 'NONE',  ( 52.82750199176329886, 18.46317551911579713, -48.94276306907110552 ) ) ;
#48186=CARTESIAN_POINT ( 'NONE',  ( 56.73667485601559690, -45.26434324106369900, -17.73083290624459707 ) ) ;
#48187=CARTESIAN_POINT ( 'NONE',  ( 14.34417029198879945, -51.11618894467930119, -22.49240188329099865 ) ) ;
#48188=CIRCLE ( 'NONE', #38166, 1.000000000000000000 ) ;
#48189=ORIENTED_EDGE ( 'NONE', *, *, #11891, .T. ) ;
#48192=CARTESIAN_POINT ( 'NONE',  ( 11.06646970394739959, -65.01491572843740130, -17.18453585839250053 ) ) ;
#48193=CARTESIAN_POINT ( 'NONE',  ( 10.31246831649800022, 32.20023774900970182, -45.84855598906619889 ) ) ;
#48195=CARTESIAN_POINT ( 'NONE',  ( 52.30324767688179577, -50.21879278929849733, -49.47276378316949774 ) ) ;
#48196=CARTESIAN_POINT ( 'NONE',  ( 8.813920544456330219, 32.04044820803110127, -46.67144773886860065 ) ) ;
#48200=CARTESIAN_POINT ( 'NONE',  ( 11.07421741897729284, 24.06268098812965306, -44.42833502052770456 ) ) ;
#48201=AXIS2_PLACEMENT_3D ( 'NONE', #21979, #2086, #26172 ) ;
#48202=CARTESIAN_POINT ( 'NONE',  ( 11.10547680587540142, -63.25111298948629468, -44.25103578592439391 ) ) ;
#48207=CARTESIAN_POINT ( 'NONE',  ( 50.21099649970649637, -49.38019754356140112, -76.14999999999999147 ) ) ;
#48210=ORIENTED_EDGE ( 'NONE', *, *, #48086, .T. ) ;
#48211=EDGE_CURVE ( 'NONE', #45437, #24734, #4318, .T. ) ;
#48214=CARTESIAN_POINT ( 'NONE',  ( 85.38000601716228743, 17.38381105532069881, -60.34000486924599471 ) ) ;
#48215=CARTESIAN_POINT ( 'NONE',  ( 54.87556897361960040, 20.83392887628360057, -54.55337246671039964 ) ) ;
#48219=CARTESIAN_POINT ( 'NONE',  ( 53.80998019303380175, 20.00543317080720129, -75.59559825915250997 ) ) ;
#48221=ORIENTED_EDGE ( 'NONE', *, *, #36658, .T. ) ;
#48228=CARTESIAN_POINT ( 'NONE',  ( 47.22777443111749562, 23.33595295215160093, -74.94663380581128820 ) ) ;
#48229=CARTESIAN_POINT ( 'NONE',  ( 65.46029542295769943, -29.76883965895079953, -16.55376543218019947 ) ) ;
#48230=EDGE_CURVE ( 'NONE', #47951, #20243, #5402, .T. ) ;
#48231=CARTESIAN_POINT ( 'NONE',  ( 58.92073349695134965, -28.77068650667426652, -15.64999999999993463 ) ) ;
#48232=CARTESIAN_POINT ( 'NONE',  ( 41.30532100959469943, -44.77888729448210370, -5.382426867826140438 ) ) ;
#48237=CARTESIAN_POINT ( 'NONE',  ( 57.14052290629950193, -50.61618793416369755, -74.67958084187151258 ) ) ;
#48241=CARTESIAN_POINT ( 'NONE',  ( 61.28176046677850053, 14.00199778307229970, -46.64755189084589659 ) ) ;
#48244=CARTESIAN_POINT ( 'NONE',  ( 52.83236148840860125, -49.65955553127109567, -48.53481065559509489 ) ) ;
#48246=CARTESIAN_POINT ( 'NONE',  ( 61.51111410063019491, -45.14410897695700697, -28.03257470884280167 ) ) ;
#48247=PLANE ( 'NONE',  #9302 ) ;
#48248=CARTESIAN_POINT ( 'NONE',  ( 56.81905678432669760, 14.35807671477110148, -26.04401432792739968 ) ) ;
#48250=CARTESIAN_POINT ( 'NONE',  ( 50.84617524826920487, 17.60923104663729788, -76.31370213949210779 ) ) ;
#48251=CARTESIAN_POINT ( 'NONE',  ( 52.94386159154990423, 18.37106777961130177, -48.82486937432109642 ) ) ;
#48253=CARTESIAN_POINT ( 'NONE',  ( 41.50224532540739375, -43.90848951166570657, -3.489448901339209819 ) ) ;
#48254=VECTOR ( 'NONE', #2742, 1000.000000000000114 ) ;
#48257=CARTESIAN_POINT ( 'NONE',  ( 47.61941804400159839, -54.52212999301320195, -54.78915954509680120 ) ) ;
#48260=CARTESIAN_POINT ( 'NONE',  ( 58.90205675725459145, 16.74204408721319837, -50.17799186399640377 ) ) ;
#48267=ORIENTED_EDGE ( 'NONE', *, *, #7745, .F. ) ;
#48271=ORIENTED_EDGE ( 'NONE', *, *, #20614, .T. ) ;
#48273=CARTESIAN_POINT ( 'NONE',  ( 11.83663281541470091, -65.04952182729299182, -45.42313283646279842 ) ) ;
#48275=ORIENTED_EDGE ( 'NONE', *, *, #8398, .T. ) ;
#48276=CARTESIAN_POINT ( 'NONE',  ( 68.13393739769620083, -43.11618894467930119, -73.25000000000000000 ) ) ;
#48277=LINE ( 'NONE', #13175, #24254 ) ;
#48283=CARTESIAN_POINT ( 'NONE',  ( 76.30797822825405774, 13.29802461769379818, -14.99128760117880432 ) ) ;
#48287=CARTESIAN_POINT ( 'NONE',  ( 11.99583947690149976, -64.75022670770579225, -24.44537524834330355 ) ) ;
#48289=CARTESIAN_POINT ( 'NONE',  ( 41.81948262126999794, 14.32434734326079884, -6.527080060687969976 ) ) ;
#48290=CARTESIAN_POINT ( 'NONE',  ( 13.93534818368129891, 20.80550406818660036, -75.55956264724760274 ) ) ;
#48292=CARTESIAN_POINT ( 'NONE',  ( 82.81259997840240317, -45.03397381929850241, -46.56543266184489482 ) ) ;
#48294=CARTESIAN_POINT ( 'NONE',  ( 11.35626934711086911, 34.06258129802085222, -17.73521848465946249 ) ) ;
#48296=VERTEX_POINT ( 'NONE', #943 ) ;
#48297=CARTESIAN_POINT ( 'NONE',  ( 52.81005256294240269, -49.67124369057780342, -28.09291909505480334 ) ) ;
#48298=CARTESIAN_POINT ( 'NONE',  ( 13.79543417967100005, -50.43786691665530242, -21.08562091374989933 ) ) ;
#48301=CYLINDRICAL_SURFACE ( 'NONE', #17293, 1.999999999999996669 ) ;
#48303=CARTESIAN_POINT ( 'NONE',  ( -3.519180701196159777, -48.70869051177000131, -5.604219821670230139 ) ) ;
#48304=CARTESIAN_POINT ( 'NONE',  ( 47.40246354955809949, 23.42001344289909781, -54.74579969459569639 ) ) ;
#48310=CARTESIAN_POINT ( 'NONE',  ( 41.06416708622129619, 13.46295351750030100, -5.123099498004559216 ) ) ;
#48314=CARTESIAN_POINT ( 'NONE',  ( 55.64908854110159808, -48.32622745761450034, -48.64133301306080170 ) ) ;
#48318=CARTESIAN_POINT ( 'NONE',  ( 17.59215364258619729, -52.29221104373319662, -75.97756937697440094 ) ) ;
#48324=CARTESIAN_POINT ( 'NONE',  ( 9.273487956746869543, 31.88305279702909800, -46.53410025525219851 ) ) ;
#48325=CARTESIAN_POINT ( 'NONE',  ( 51.63351621991599671, -50.61618894467930119, -66.86356675664690385 ) ) ;
#48328=CARTESIAN_POINT ( 'NONE',  ( 18.74040570297340125, 20.57970132932399920, -74.87640169473949925 ) ) ;
#48331=ORIENTED_EDGE ( 'NONE', *, *, #23034, .T. ) ;
#48332=DIRECTION ( 'NONE',  ( -0.1999849291396485207, 0.9797989733190221040, 0.000000000000000000 ) ) ;
#48336=ORIENTED_EDGE ( 'NONE', *, *, #40504, .F. ) ;
#48338=B_SPLINE_SURFACE_WITH_KNOTS ( 'NONE', 3, 3, ( 
 ( #22461, #33490, #41885, #26135, #33741, #2048, #42146, #5984, #29301, #13593, #45302, #33994, #25360, #5477, #50009, #3606, #27176, #47626, #26649, #35567, #31609, #51039 ),
 ( #42668, #19577, #27432, #30838, #34521, #43435, #46869, #7538, #3091, #3346, #2834, #31096, #23744, #23483, #18799, #35033, #38996, #51554, #39506, #31351, #42926, #26920 ),
 ( #47126, #6768, #15653, #11731, #27693, #10956, #43691, #47376, #7024, #11213, #7793, #7276, #15397, #23229, #22976, #2572, #19322, #18544, #50526, #43183, #50785, #22720 ),
 ( #38738, #51301, #14875, #14617, #19060, #15140, #30587, #39246, #35303, #11475, #34778, #46607, #10694, #1147, #9543, #1670, #5611, #16607, #9798, #32829, #17397, #17658 ),
 ( #37051, #33365, #9020, #21308, #25234, #48596, #33624, #45698, #41241, #5354, #1410, #48855, #45176, #21048, #13732, #49641, #5094, #37310, #17144, #41497, #24964, #888 ),
 ( #12961, #40982, #49382, #21566, #32565, #33095, #13478, #36520, #29435, #12696, #28650, #49126, #44652, #4820, #45441, #39758, #8759, #24707, #4556, #40725, #9288, #25495 ),
 ( #20788, #624, #28913, #36780, #37561, #16883, #29688, #13225, #29174, #20525, #44918, #6637, #18167, #6125, #41756, #1928, #38348, #46748, #38875, #42808, #17910, #47007 ),
 ( #46487, #10316, #10577, #34918, #10052, #34654, #45958, #26014, #26277, #26533, #42547, #14495, #22601, #18937, #22854, #33879, #29944, #2438, #22081, #49892, #5862, #13987 ),
 ( #26796, #34133, #38091, #50916, #25748, #42025, #42284, #2187, #37834, #2963, #38616, #2706, #18681, #15010, #50142, #34396, #50661, #6381, #14755, #30725, #30211, #30980 ),
 ( #14241, #46227, #22342, #18421, #50408, #10830, #30467, #15533, #4760, #13416, #32767, #48792, #5550, #12901, #29118, #40661, #28592, #12368, #24388, #8963, #17341, #9484 ) ),
 .UNSPECIFIED., .F., .F., .F.,
 ( 4, 1, 1, 1, 1, 1, 1, 4 ),
 ( 4, 2, 2, 2, 2, 2, 2, 2, 2, 2, 4 ),
 ( -2.340994999999999938E-10, 0.1428571428571430157, 0.2857142857142860315, 0.4285714285714289917, 0.5714285714285709528, 0.7142857142857139685, 0.8571428571428569843, 1.000000707733940120 ),
 ( -8.605215962919450234, -8.065295817754250862, -6.871057666229980043, -6.124658821527319219, -5.378259976824650401, -4.302607981459720676, -3.764781983777250041, -2.904260387485310346, -2.013455357812269586, -0.8451718638598000322, 7.077339579999999566E-07 ),
 .UNSPECIFIED. ) ;
#48339=ADVANCED_FACE ( 'NONE', ( #21103 ), #5666, .F. ) ;
#48340=PLANE ( 'NONE',  #14044 ) ;
#48344=ORIENTED_EDGE ( 'NONE', *, *, #1727, .F. ) ;
#48345=VERTEX_POINT ( 'NONE', #22136 ) ;
#48346=CARTESIAN_POINT ( 'NONE',  ( 61.75019796695539753, -46.11618894467930119, -28.15000000000000213 ) ) ;
#48348=CARTESIAN_POINT ( 'NONE',  ( 61.24574273693410476, 14.30988654607880051, -47.60649862612909544 ) ) ;
#48349=TOROIDAL_SURFACE ( 'NONE', #4014, 36.00000000000000000, 2.000000000000000000 ) ;
#48350=CARTESIAN_POINT ( 'NONE',  ( 52.57642278611140085, 14.37083706895390023, -13.82862052991180057 ) ) ;
#48353=CARTESIAN_POINT ( 'NONE',  ( -7.078137695061969659, 14.49478530863819969, -5.101446175793999949 ) ) ;
#48355=CARTESIAN_POINT ( 'NONE',  ( 61.30494512497919857, 13.98627961912009887, -28.05574256500980113 ) ) ;
#48358=CARTESIAN_POINT ( 'NONE',  ( 54.27527969986719114, 17.69567147495890325, -48.75594442643640036 ) ) ;
#48360=CARTESIAN_POINT ( 'NONE',  ( 11.19262701750870015, 32.79550126274290278, -44.18375550860420020 ) ) ;
#48364=CARTESIAN_POINT ( 'NONE',  ( 47.20319459038839227, 23.55908258955629719, -74.14999581977149035 ) ) ;
#48365=CARTESIAN_POINT ( 'NONE',  ( 48.63379746627050082, -53.98620851929000253, -54.63257371341549629 ) ) ;
#48372=ORIENTED_EDGE ( 'NONE', *, *, #51653, .F. ) ;
#48375=ORIENTED_EDGE ( 'NONE', *, *, #40678, .F. ) ;
#48377=CARTESIAN_POINT ( 'NONE',  ( 60.35316404808119728, -45.72939249500469572, -47.36338488644539524 ) ) ;
#48379=AXIS2_PLACEMENT_3D ( 'NONE', #20688, #16780, #6285 ) ;
#48380=CARTESIAN_POINT ( 'NONE',  ( 75.47966807050509885, -43.37310274687460065, -13.40512917118210012 ) ) ;
#48385=ORIENTED_EDGE ( 'NONE', *, *, #19676, .F. ) ;
#48386=CARTESIAN_POINT ( 'NONE',  ( 83.98295738300248559, -44.57976106941110572, -47.35112499062080360 ) ) ;
#48388=ORIENTED_EDGE ( 'NONE', *, *, #31521, .F. ) ;
#48392=CARTESIAN_POINT ( 'NONE',  ( 76.39982225080902367, -19.43572751922974362, -12.79577862347393058 ) ) ;
#48393=CARTESIAN_POINT ( 'NONE',  ( 54.02518786316219490, -51.81565143108780092, -54.18996768095620098 ) ) ;
#48397=DIRECTION ( 'NONE',  ( 0.000000000000000000, 0.000000000000000000, -1.000000000000000000 ) ) ;
#48400=DIRECTION ( 'NONE',  ( -0.6911981449639439390, -0.7226652920947588266, 0.000000000000000000 ) ) ;
#48402=CARTESIAN_POINT ( 'NONE',  ( 64.56306260708079492, 0.8160381106275480523, -17.55137208659099812 ) ) ;
#48403=CARTESIAN_POINT ( 'NONE',  ( 51.95832570932330441, -49.45171451879549807, -77.09974002837380169 ) ) ;
#48405=CARTESIAN_POINT ( 'NONE',  ( 3.754239621849577713, 24.69916076480114242, -9.121771190811498897 ) ) ;
#48406=CARTESIAN_POINT ( 'NONE',  ( 54.14345801646960155, -50.61618316771350834, -76.93443301864958528 ) ) ;
#48407=CARTESIAN_POINT ( 'NONE',  ( 60.23362534523688794, 14.54944813804885229, -47.26357634580340061 ) ) ;
#48408=DIRECTION ( 'NONE',  ( -0.8732394366197178126, 0.4872913772396119114, 0.000000000000000000 ) ) ;
#48412=CARTESIAN_POINT ( 'NONE',  ( 42.42327894872600069, -43.80073867009950561, -4.706996717213810300 ) ) ;
#48414=CARTESIAN_POINT ( 'NONE',  ( 60.83133137330749918, -45.46867109277970087, -47.01992810568810199 ) ) ;
#48415=CARTESIAN_POINT ( 'NONE',  ( 68.36163520449862574, -0.4430167382633080631, -18.19591820036098895 ) ) ;
#48419=CARTESIAN_POINT ( 'NONE',  ( 17.21347160910390173, -53.11618894467930119, -76.14999999999999147 ) ) ;
#48422=CARTESIAN_POINT ( 'NONE',  ( 14.24028704233020015, -52.17195122215589720, -75.81086730487160708 ) ) ;
#48423=CARTESIAN_POINT ( 'NONE',  ( 47.31562538347599656, -54.71039600610800591, -54.74027837518219997 ) ) ;
#48424=VECTOR ( 'NONE', #22322, 999.9999999999998863 ) ;
#48425=CARTESIAN_POINT ( 'NONE',  ( 16.13393739769620083, -15.61618894467929941, -11.65000000000000036 ) ) ;
#48427=CARTESIAN_POINT ( 'NONE',  ( 56.84932592767840021, 19.42421310868259354, -63.99406948319570887 ) ) ;
#48428=CARTESIAN_POINT ( 'NONE',  ( 60.83844611352238019, -45.46494382793184741, -47.03527794730813127 ) ) ;
#48429=CARTESIAN_POINT ( 'NONE',  ( 11.89321892219109955, 34.20364954172590188, -18.16392793332829925 ) ) ;
#48430=B_SPLINE_CURVE_WITH_KNOTS ( 'NONE', 3,
 ( #37896, #33936, #1988, #33160, #33682, #41557, #1470, #41300 ),
 .UNSPECIFIED., .F., .F.,
 ( 4, 2, 2, 4 ),
 ( 0.000000000000000000, 0.3677848396155383170, 0.7599019565052781422, 1.000000000000000000 ),
 .UNSPECIFIED. ) ;
#48432=CARTESIAN_POINT ( 'NONE',  ( -2.927979189508790103, -49.19984425798019601, -5.740620115512199639 ) ) ;
#48434=CARTESIAN_POINT ( 'NONE',  ( 15.05440318628160057, -53.11618894467930119, -76.14999999999999147 ) ) ;
#48436=CARTESIAN_POINT ( 'NONE',  ( 48.84657211724849901, 22.78726586394800080, -55.19002503342879606 ) ) ;
#48438=CARTESIAN_POINT ( 'NONE',  ( 52.73507376017240489, -49.73068395995180424, -48.76329240581910085 ) ) ;
#48443=CARTESIAN_POINT ( 'NONE',  ( 83.96875769672529088, 13.10122437207289892, -47.04741150093960300 ) ) ;
#48444=CARTESIAN_POINT ( 'NONE',  ( 52.72675226946439864, 18.45992442769729891, -27.59442653021299918 ) ) ;
#48446=CARTESIAN_POINT ( 'NONE',  ( 52.88663098474060575, 18.43548364359019942, -48.99336406855329784 ) ) ;
#48447=CARTESIAN_POINT ( 'NONE',  ( 55.17415142466310130, -45.32842442549269890, -15.17933028536879903 ) ) ;
#48448=DIRECTION ( 'NONE',  ( -0.8224686640529101922, -0.3976080002595576146, -0.4067593573362719428 ) ) ;
#48449=ORIENTED_EDGE ( 'NONE', *, *, #38834, .F. ) ;
#48450=VERTEX_POINT ( 'NONE', #38402 ) ;
#48451=CARTESIAN_POINT ( 'NONE',  ( 11.62518889158189950, -65.06178593564310120, -16.65848135031670196 ) ) ;
#48452=CARTESIAN_POINT ( 'NONE',  ( 9.904144631292190581, 32.27789939431119848, -46.22502649936210162 ) ) ;
#48453=CARTESIAN_POINT ( 'NONE',  ( 18.69872345376407807, 20.24981416582376070, -15.74255600669635236 ) ) ;
#48454=CARTESIAN_POINT ( 'NONE',  ( 47.21685942418269377, -54.78066203677720125, -54.66846264793990429 ) ) ;
#48455=CARTESIAN_POINT ( 'NONE',  ( 11.28041403274951548, -65.17108450666793829, -22.88566713088593119 ) ) ;
#48457=AXIS2_PLACEMENT_3D ( 'NONE', #20805, #5112, #24463 ) ;
#48460=ORIENTED_EDGE ( 'NONE', *, *, #11428, .T. ) ;
#48462=CARTESIAN_POINT ( 'NONE',  ( 10.97797866599409922, -63.15395481739809469, -44.74230776638400187 ) ) ;
#48472=CARTESIAN_POINT ( 'NONE',  ( 56.39270784227079503, -50.52750194671250483, -52.86271187454359932 ) ) ;
#48473=CARTESIAN_POINT ( 'NONE',  ( 53.24328890024050054, 22.35687538065929658, -56.22661043126620228 ) ) ;
#48478=CARTESIAN_POINT ( 'NONE',  ( 46.59688917077139791, -53.29855585819780117, -76.10130133987269119 ) ) ;
#48479=ORIENTED_EDGE ( 'NONE', *, *, #17789, .F. ) ;
#48482=CARTESIAN_POINT ( 'NONE',  ( 13.00893796619580023, 34.28605843179359880, -23.32157451048000141 ) ) ;
#48483=CARTESIAN_POINT ( 'NONE',  ( 47.36067941193029895, 23.15755082926289887, -75.11690455987650239 ) ) ;
#48484=CARTESIAN_POINT ( 'NONE',  ( 19.55308497633217968, -53.75077074604085681, -16.86504912222391184 ) ) ;
#48486=CARTESIAN_POINT ( 'NONE',  ( 10.47385409520754784, -55.21366976880749888, -45.62050209441289894 ) ) ;
#48488=AXIS2_PLACEMENT_3D ( 'NONE', #24986, #29193, #48618 ) ;
#48491=LINE ( 'NONE', #28817, #14006 ) ;
#48493=EDGE_CURVE ( 'NONE', #26115, #19986, #10108, .T. ) ;
#48495=CARTESIAN_POINT ( 'NONE',  ( 61.32101085468809742, 13.98954918084040067, -46.71870344728709767 ) ) ;
#48496=CARTESIAN_POINT ( 'NONE',  ( -26.59371227466860077, -41.52207930017120674, -54.97277084359720334 ) ) ;
#48499=CARTESIAN_POINT ( 'NONE',  ( 52.83531802359640039, -49.65800651964969603, -48.55820785177999710 ) ) ;
#48500=ADVANCED_FACE ( 'NONE', ( #41490 ), #12953, .T. ) ;
#48501=CARTESIAN_POINT ( 'NONE',  ( 61.72368837927260188, -45.11618267598419862, -28.01092661157059993 ) ) ;
#48503=CARTESIAN_POINT ( 'NONE',  ( 56.38589515732069657, 14.45185451966650092, -25.89150152932120363 ) ) ;
#48506=CARTESIAN_POINT ( 'NONE',  ( 50.76151235490149816, 18.34449058292550205, -76.22310723605730232 ) ) ;
#48507=CARTESIAN_POINT ( 'NONE',  ( 52.80018040210159569, 18.44894719811759742, -48.71454912288499628 ) ) ;
#48512=CARTESIAN_POINT ( 'NONE',  ( 54.47259832750690123, -46.25232753665150653, -15.76422791930239953 ) ) ;
#48513=CARTESIAN_POINT ( 'NONE',  ( 47.59376055414519868, -54.54431305457409707, -54.85521038714039577 ) ) ;
#48514=CARTESIAN_POINT ( 'NONE',  ( -4.848012345405839696, 16.07167109151949802, -4.416243737290190374 ) ) ;
#48515=CARTESIAN_POINT ( 'NONE',  ( 41.83063930790589779, 12.37849180622510126, -3.362295849109719903 ) ) ;
#48516=CARTESIAN_POINT ( 'NONE',  ( 60.41972385647800081, 15.56736444559500043, -48.98660369848109752 ) ) ;
#48523=ORIENTED_EDGE ( 'NONE', *, *, #27723, .T. ) ;
#48525=CARTESIAN_POINT ( 'NONE',  ( 16.00829429484023692, -51.00984973828658298, -15.66512534869403694 ) ) ;
#48529=CARTESIAN_POINT ( 'NONE',  ( 55.89446496821490484, -45.93182254271150100, -25.32793047687500021 ) ) ;
#48536=CARTESIAN_POINT ( 'NONE',  ( 60.96148484106869603, 14.45202308121209889, -47.73691995860960446 ) ) ;
#48537=AXIS2_PLACEMENT_3D ( 'NONE', #34449, #42860, #6433 ) ;
#48543=ORIENTED_EDGE ( 'NONE', *, *, #45311, .T. ) ;
#48547=ADVANCED_FACE ( 'NONE', ( #9280 ), #47808, .T. ) ;
#48549=CARTESIAN_POINT ( 'NONE',  ( 13.89974045593869967, 20.77108261440800163, -75.51240970683940645 ) ) ;
#48550=CARTESIAN_POINT ( 'NONE',  ( 51.67587649748560352, 17.38381105532069881, -77.01363636363639387 ) ) ;
#48551=CARTESIAN_POINT ( 'NONE',  ( 83.66401895982360770, -44.51498057501240169, -46.61643406624109787 ) ) ;
#48554=ORIENTED_EDGE ( 'NONE', *, *, #15659, .T. ) ;
#48555=CARTESIAN_POINT ( 'NONE',  ( 53.88285922114570070, -48.70220139524560210, -27.00085731554899837 ) ) ;
#48556=CARTESIAN_POINT ( 'NONE',  ( 14.09495638488309943, -50.67789608235420218, -21.23638623580770357 ) ) ;
#48558=CARTESIAN_POINT ( 'NONE',  ( 75.44813142283744867, 12.59560967597626657, -13.51485765024892771 ) ) ;
#48562=EDGE_LOOP ( 'NONE', ( #40786, #20084 ) ) ;
#48564=CARTESIAN_POINT ( 'NONE',  ( -7.616042036189179854, -45.40507477012349824, -5.569053195681480162 ) ) ;
#48565=ADVANCED_FACE ( 'NONE', ( #6372 ), #22334, .F. ) ;
#48567=CARTESIAN_POINT ( 'NONE',  ( 47.28643180688370506, 23.49801600062669849, -54.74208605995080035 ) ) ;
#48571=CARTESIAN_POINT ( 'NONE',  ( 54.63655771189059607, 16.82059223505549994, -26.73578643762699869 ) ) ;
#48572=CIRCLE ( 'NONE', #21772, 1.999999999999996669 ) ;
#48573=CARTESIAN_POINT ( 'NONE',  ( 11.23165351422320057, 33.99825783758829800, -17.66286062877820129 ) ) ;
#48574=ADVANCED_FACE ( 'NONE', ( #26525 ), #50400, .T. ) ;
#48578=CARTESIAN_POINT ( 'NONE',  ( 54.33046565385170368, -48.97104959639300148, -48.91876050846019552 ) ) ;
#48581=CARTESIAN_POINT ( 'NONE',  ( 56.42542598226509654, 19.53946997070610081, -53.51082495327469246 ) ) ;
#48582=FACE_OUTER_BOUND ( 'NONE', #15806, .T. ) ;
#48584=PLANE ( 'NONE',  #16546 ) ;
#48586=CARTESIAN_POINT ( 'NONE',  ( 20.12219014770483483, 24.14963702508532606, -19.95441604237223743 ) ) ;
#48587=CARTESIAN_POINT ( 'NONE',  ( 10.48584413461309950, 31.89781099419320043, -45.62883909305980268 ) ) ;
#48588=CARTESIAN_POINT ( 'NONE',  ( 44.76368420724840291, 13.86998310020809910, -7.024004829805569727 ) ) ;
#48591=CARTESIAN_POINT ( 'NONE',  ( 17.86297238746119831, 20.47201121247589839, -75.55956264724760274 ) ) ;
#48594=ORIENTED_EDGE ( 'NONE', *, *, #11084, .T. ) ;
#48595=EDGE_CURVE ( 'NONE', #22140, #25228, #34289, .T. ) ;
#48596=CARTESIAN_POINT ( 'NONE',  ( 12.01839223830350001, -65.30369916784260909, -47.05360386500180425 ) ) ;
#48599=CARTESIAN_POINT ( 'NONE',  ( 61.67010585289130375, 13.90326159682560103, -46.64609547319909666 ) ) ;
#48604=CARTESIAN_POINT ( 'NONE',  ( 61.33486291256839706, -45.61980825670960371, -47.69940288585109300 ) ) ;
#48606=EDGE_LOOP ( 'NONE', ( #37918, #18382, #34243, #40656, #6240 ) ) ;
#48608=EDGE_LOOP ( 'NONE', ( #44915, #16013, #30652, #20787 ) ) ;
#48612=CARTESIAN_POINT ( 'NONE',  ( 71.10514731706700786, 12.15699934429280127, -12.15279640865730038 ) ) ;
#48615=ADVANCED_FACE ( 'NONE', ( #44072 ), #25079, .F. ) ;
#48616=CARTESIAN_POINT ( 'NONE',  ( 49.63401988979710211, 13.97123100121650197, -10.90947558922509941 ) ) ;
#48618=DIRECTION ( 'NONE',  ( 1.000000000000000000, 0.000000000000000000, 0.000000000000000000 ) ) ;
#48619=CARTESIAN_POINT ( 'NONE',  ( -6.140345869213950536, 15.17335822531540046, -4.613862302043099994 ) ) ;
#48621=CARTESIAN_POINT ( 'NONE',  ( 58.29889914173639909, 14.43956164479439863, -26.41833035305619859 ) ) ;
#48626=CARTESIAN_POINT ( 'NONE',  ( 12.96176040339469893, 34.28310491318730158, -47.67058438006289833 ) ) ;
#48629=EDGE_CURVE ( 'NONE', #6528, #11300, #28067, .T. ) ;
#48632=CARTESIAN_POINT ( 'NONE',  ( 49.35390693627829961, -53.59897724190700075, -54.31982765639760657 ) ) ;
#48633=CARTESIAN_POINT ( 'NONE',  ( -5.431977005845720186, 16.07634798542799714, -5.576406780277120667 ) ) ;
#48636=CYLINDRICAL_SURFACE ( 'NONE', #7047, 40.00000000000000000 ) ;
#48637=LINE ( 'NONE', #8020, #18891 ) ;
#48641=ORIENTED_EDGE ( 'NONE', *, *, #11364, .T. ) ;
#48642=CARTESIAN_POINT ( 'NONE',  ( 54.53726589893891230, -46.02701840152597157, -15.67785061177839978 ) ) ;
#48644=CARTESIAN_POINT ( 'NONE',  ( 61.03140963465120450, -45.55308648458009912, -47.57043735694709596 ) ) ;
#48646=CARTESIAN_POINT ( 'NONE',  ( 50.29495134167750336, 18.68575087643539945, -76.14999999999999147 ) ) ;
#48649=CIRCLE ( 'NONE', #46157, 3.000000000000000000 ) ;
#48650=CARTESIAN_POINT ( 'NONE',  ( 52.57481654442310059, -51.43204889509869560, -75.83555718502590537 ) ) ;
#48651=LINE ( 'NONE', #29227, #31959 ) ;
#48653=CARTESIAN_POINT ( 'NONE',  ( 83.30448183675909490, -45.24061545150300390, -47.41172112684520101 ) ) ;
#48655=ORIENTED_EDGE ( 'NONE', *, *, #28769, .F. ) ;
#48658=CARTESIAN_POINT ( 'NONE',  ( 52.47677897125242197, -49.96156889689471114, -77.24546347434363724 ) ) ;
#48659=CARTESIAN_POINT ( 'NONE',  ( 76.44816630901640053, -6.457295309286853247, -13.00405914655548578 ) ) ;
#48660=CARTESIAN_POINT ( 'NONE',  ( 49.64260032845790249, -53.66077289818650087, -54.78414101162699978 ) ) ;
#48665=CYLINDRICAL_SURFACE ( 'NONE', #36205, 31.00000000000000000 ) ;
#48666=FACE_OUTER_BOUND ( 'NONE', #29140, .T. ) ;
#48667=CARTESIAN_POINT ( 'NONE',  ( 64.04792041323590013, 0.7580616222945849580, -17.48146414341379895 ) ) ;
#48671=CARTESIAN_POINT ( 'NONE',  ( 53.53698447494460311, -50.55136415298420616, -77.03764851654500490 ) ) ;
#48673=CARTESIAN_POINT ( 'NONE',  ( 60.71265700703109758, 14.29847002888300089, -47.11594162556460219 ) ) ;
#48674=EDGE_CURVE ( 'NONE', #24567, #17140, #32407, .T. ) ;
#48676=EDGE_CURVE ( 'NONE', #39784, #27219, #43568, .T. ) ;
#48678=CARTESIAN_POINT ( 'NONE',  ( 41.98453321725290266, -44.09319621180809889, -4.765379593933540825 ) ) ;
#48681=CARTESIAN_POINT ( 'NONE',  ( 57.14903038794999901, 13.88381105532070059, -16.26185532857629923 ) ) ;
#48682=CARTESIAN_POINT ( 'NONE',  ( 61.44133198084610115, -45.34716915528590420, -47.30158679574340397 ) ) ;
#48683=CONICAL_SURFACE ( 'NONE', #36135, 1.942499999999999227, 0.8266833912447979493 ) ;
#48688=CARTESIAN_POINT ( 'NONE',  ( 65.13280820348710165, 0.9471869900316070012, -17.73393088427939901 ) ) ;
#48690=CARTESIAN_POINT ( 'NONE',  ( 13.72816481212180051, -51.57539031256769846, -74.98719232987430416 ) ) ;
#48691=CARTESIAN_POINT ( 'NONE',  ( 47.33080767030429570, -54.69887959644039910, -54.70291218041550252 ) ) ;
#48697=EDGE_CURVE ( 'NONE', #35884, #46345, #39123, .T. ) ;
#48698=CARTESIAN_POINT ( 'NONE',  ( 47.70337372003230314, -54.50475343038620224, -55.04617154330599504 ) ) ;
#48702=CARTESIAN_POINT ( 'NONE',  ( 48.73758251462950142, 22.81230782973970150, -55.00444999029969750 ) ) ;
#48705=ORIENTED_EDGE ( 'NONE', *, *, #3829, .F. ) ;
#48706=DIRECTION ( 'NONE',  ( 0.000000000000000000, 0.000000000000000000, 1.000000000000000000 ) ) ;
#48709=CARTESIAN_POINT ( 'NONE',  ( 84.22920232233479965, 12.56550928184170068, -47.02060905303799387 ) ) ;
#48710=CARTESIAN_POINT ( 'NONE',  ( 53.51583085569070164, 17.59825481099489863, -26.65935230799360056 ) ) ;
#48713=CARTESIAN_POINT ( 'NONE',  ( 55.78663148921049952, -45.30254049228850732, -15.70162090623030160 ) ) ;
#48714=CYLINDRICAL_SURFACE ( 'NONE', #28937, 6.049999999999999822 ) ;
#48715=EDGE_LOOP ( 'NONE', ( #16876, #34189, #20939, #21571 ) ) ;
#48716=ORIENTED_EDGE ( 'NONE', *, *, #28778, .F. ) ;
#48717=CARTESIAN_POINT ( 'NONE',  ( 11.65450058716879944, -65.12719674309839490, -16.76600934541859900 ) ) ;
#48718=CARTESIAN_POINT ( 'NONE',  ( 11.95077454560339980, 34.11711772380790109, -47.35066886291930643 ) ) ;
#48721=CARTESIAN_POINT ( 'NONE',  ( 50.39481201540360189, -52.19103705647920322, -52.11755584844750189 ) ) ;
#48722=CARTESIAN_POINT ( 'NONE',  ( 74.17629866868290378, 1.883811055320649963, -65.34607522167520699 ) ) ;
#48724=VERTEX_POINT ( 'NONE', #35698 ) ;
#48726=CARTESIAN_POINT ( 'NONE',  ( 53.11475001244221517, 18.18247718396222368, -27.56270898827361293 ) ) ;
#48727=CARTESIAN_POINT ( 'NONE',  ( 50.39592751844079999, 21.35098830175070006, -53.02100607687120259 ) ) ;
#48729=CARTESIAN_POINT ( 'NONE',  ( 50.31585484890159421, -48.88982717754599605, -76.16276048729439196 ) ) ;
#48732=DIRECTION ( 'NONE',  ( 0.000000000000000000, 1.000000000000000000, 0.000000000000000000 ) ) ;
#48733=DIRECTION ( 'NONE',  ( 0.000000000000000000, 0.000000000000000000, -1.000000000000000000 ) ) ;
#48734=ORIENTED_EDGE ( 'NONE', *, *, #48230, .T. ) ;
#48735=CARTESIAN_POINT ( 'NONE',  ( 57.27851914992729832, -50.15376702335620251, -52.63313635724109929 ) ) ;
#48736=CARTESIAN_POINT ( 'NONE',  ( 55.91507730363359485, 15.44714545385880022, -45.94138956033829402 ) ) ;
#48738=ADVANCED_FACE ( 'NONE', ( #31730, #11863 ), #47251, .T. ) ;
#48739=CARTESIAN_POINT ( 'NONE',  ( 14.30978967243840039, -51.11618894516979594, -22.40422843537090003 ) ) ;
#48740=CARTESIAN_POINT ( 'NONE',  ( 55.28540664048680497, 19.68320257923529937, -75.28129500772568861 ) ) ;
#48742=CARTESIAN_POINT ( 'NONE',  ( 47.36065766533170063, -54.38989670583089975, -75.11697231728020085 ) ) ;
#48743=ORIENTED_EDGE ( 'NONE', *, *, #3736, .F. ) ;
#48744=DIRECTION ( 'NONE',  ( -1.000000000000000000, 0.000000000000000000, 0.000000000000000000 ) ) ;
#48746=CARTESIAN_POINT ( 'NONE',  ( 53.12230990226080252, -49.57349283027179609, -49.13891823708339501 ) ) ;
#48748=CARTESIAN_POINT ( 'NONE',  ( 47.39179696941629771, 23.33325173635930128, -74.72254318496639769 ) ) ;
#48752=AXIS2_PLACEMENT_3D ( 'NONE', #1867, #41185, #46166 ) ;
#48762=CARTESIAN_POINT ( 'NONE',  ( 61.32020094034120916, 13.98164174484680089, -46.53643907696579873 ) ) ;
#48763=CARTESIAN_POINT ( 'NONE',  ( -33.07468191286329784, -25.33318566548249962, -56.92399776842329828 ) ) ;
#48765=CARTESIAN_POINT ( 'NONE',  ( 53.45012425295129788, -49.34429749072780425, -48.87690323766360478 ) ) ;
#48766=CARTESIAN_POINT ( 'NONE',  ( 61.72858909456450505, -45.11618897281839935, -27.86494589658979848 ) ) ;
#48768=CARTESIAN_POINT ( 'NONE',  ( 56.96266382495790026, 14.69614837228800042, -26.24591337028120108 ) ) ;
#48770=CARTESIAN_POINT ( 'NONE',  ( 50.62541591231190097, 17.89847220828429997, -76.22054775280069805 ) ) ;
#48771=CARTESIAN_POINT ( 'NONE',  ( 52.69435528435500515, 18.51371064498010099, -48.50601979887200343 ) ) ;
#48773=DIRECTION ( 'NONE',  ( -1.224646799147355179E-16, 1.000000000000000000, -2.054487543405498457E-16 ) ) ;
#48774=CARTESIAN_POINT ( 'NONE',  ( 47.06135413360298259, 22.56673458786644559, -75.82639806858723830 ) ) ;
#48779=CARTESIAN_POINT ( 'NONE',  ( 47.74639995886609967, -54.45100479285450490, -54.79047585474189930 ) ) ;
#48790=DIRECTION ( 'NONE',  ( 0.000000000000000000, 0.7071067811865521247, 0.7071067811865429098 ) ) ;
#48792=CARTESIAN_POINT ( 'NONE',  ( 11.70307022357610016, -64.92107323957129950, -45.14224943014770020 ) ) ;
#48795=CARTESIAN_POINT ( 'NONE',  ( 51.93051863921090217, 19.02772527816939885, -76.53037500023199868 ) ) ;
#48797=ORIENTED_EDGE ( 'NONE', *, *, #16648, .T. ) ;
#48799=DIRECTION ( 'NONE',  ( 0.1686178020941670186, 0.6660492713794450292, -0.7265992051412130115 ) ) ;
#48806=B_SPLINE_CURVE_WITH_KNOTS ( 'NONE', 3,
 ( #24558, #17755, #40832, #25345, #1774, #37417, #36900, #29286 ),
 .UNSPECIFIED., .F., .F.,
 ( 4, 1, 3, 4 ),
 ( 0.000000000000000000, 0.4999600334511122846, 0.9999200669022245691, 1.000000000000000000 ),
 .UNSPECIFIED. ) ;
#48807=ORIENTED_EDGE ( 'NONE', *, *, #25587, .F. ) ;
#48808=CARTESIAN_POINT ( 'NONE',  ( 11.44746559451110102, -65.00817642577131039, -23.48109952293140168 ) ) ;
#48811=CIRCLE ( 'NONE', #32013, 24.90000000000000213 ) ;
#48812=CARTESIAN_POINT ( 'NONE',  ( 14.83771907029349890, 21.57872223484060115, -76.12922349804929922 ) ) ;
#48813=CARTESIAN_POINT ( 'NONE',  ( 52.25095813476680462, 18.53891199752670005, -77.19024044419620623 ) ) ;
#48817=CARTESIAN_POINT ( 'NONE',  ( 52.98091703242110384, -49.46538585664740140, -27.45852672937839856 ) ) ;
#48818=CARTESIAN_POINT ( 'NONE',  ( 14.72196958648260079, -51.10496628337289593, -22.05098504494149836 ) ) ;
#48820=CARTESIAN_POINT ( 'NONE',  ( 57.15189004838642717, 12.22388545694372475, -8.325998452327215915 ) ) ;
#48821=TOROIDAL_SURFACE ( 'NONE', #30400, 40.00000000000310507, 2.000000000000059952 ) ;
#48824=CARTESIAN_POINT ( 'NONE',  ( 16.13393739769620083, -15.61618894467929941, 7.849999999999999645 ) ) ;
#48827=CARTESIAN_POINT ( 'NONE',  ( -10.42019467055720128, -42.80886955819109829, -6.071270369134899703 ) ) ;
#48829=CARTESIAN_POINT ( 'NONE',  ( 47.29954908011710302, 23.48849187898310120, -54.71030354338810042 ) ) ;
#48830=CARTESIAN_POINT ( 'NONE',  ( 41.64265090550279780, 15.19461330350340056, -4.296538310234330638 ) ) ;
#48833=CARTESIAN_POINT ( 'NONE',  ( 11.49541394825649832, 34.11692877016390213, -17.78290644886299887 ) ) ;
#48837=CARTESIAN_POINT ( 'NONE',  ( 56.37928484793929584, -47.94447020180829355, -48.46568738789210329 ) ) ;
#48840=CARTESIAN_POINT ( 'NONE',  ( 17.28435301021069748, -52.93377250084219554, -76.14999999999999147 ) ) ;
#48841=DIRECTION ( 'NONE',  ( 0.000000000000000000, 0.000000000000000000, -1.000000000000000000 ) ) ;
#48843=DIRECTION ( 'NONE',  ( 0.000000000000000000, -1.000000000000000000, 0.000000000000000000 ) ) ;
#48846=CARTESIAN_POINT ( 'NONE',  ( 10.14833759260570112, 32.09291264738480010, -45.99364918638399757 ) ) ;
#48850=CARTESIAN_POINT ( 'NONE',  ( 17.88374330215040331, 20.42705216602020357, -75.51240970683940645 ) ) ;
#48853=VECTOR ( 'NONE', #27871, 1000.000000000000000 ) ;
#48854=ORIENTED_EDGE ( 'NONE', *, *, #18086, .T. ) ;
#48855=CARTESIAN_POINT ( 'NONE',  ( 10.98852721706949964, -64.64787429366180049, -46.31523117561389569 ) ) ;
#48856=CARTESIAN_POINT ( 'NONE',  ( 57.21760545298290879, -45.83745218208000693, -26.25839754709659957 ) ) ;
#48858=CARTESIAN_POINT ( 'NONE',  ( 61.68928001772049896, 13.92480326227030041, -46.77635756133729927 ) ) ;
#48859=B_SPLINE_CURVE_WITH_KNOTS ( 'NONE', 3,
 ( #33, #43541, #43032, #15502, #7891, #35142, #23838, #3707, #39860, #51401 ),
 .UNSPECIFIED., .F., .F.,
 ( 4, 2, 2, 2, 4 ),
 ( 0.000000000000000000, 0.2484741911312051410, 0.3727112866968076976, 0.4348298344796093229, 0.4969483822624109481 ),
 .UNSPECIFIED. ) ;
#48862=CARTESIAN_POINT ( 'NONE',  ( 14.34417029198879945, -52.11618894467940066, -76.14999999999999147 ) ) ;
#48864=CARTESIAN_POINT ( 'NONE',  ( 11.23834934692502152, -64.16154010852214640, -24.08812103644450886 ) ) ;
#48867=CARTESIAN_POINT ( 'NONE',  ( 9.446522296386651973, -55.05387195732045313, -46.46219560139201121 ) ) ;
#48868=ORIENTED_EDGE ( 'NONE', *, *, #47979, .F. ) ;
#48875=FACE_OUTER_BOUND ( 'NONE', #40916, .T. ) ;
#48877=EDGE_CURVE ( 'NONE', #260, #37257, #44585, .T. ) ;
#48878=CARTESIAN_POINT ( 'NONE',  ( 54.71777084300830296, 14.38502104920799951, -15.43676058607329971 ) ) ;
#48880=CARTESIAN_POINT ( 'NONE',  ( -5.330649352083970172, 15.78836655736939854, -4.865133846375759852 ) ) ;
#48881=CARTESIAN_POINT ( 'NONE',  ( 7.530128794764829436, -59.71029400208423965, -11.77223857309723876 ) ) ;
#48882=EDGE_CURVE ( 'NONE', #45245, #23772, #14263, .T. ) ;
#48883=CARTESIAN_POINT ( 'NONE',  ( 55.91595795151388160, 14.67227240940072619, -17.77972436534847489 ) ) ;
#48885=ORIENTED_EDGE ( 'NONE', *, *, #50483, .T. ) ;
#48886=CARTESIAN_POINT ( 'NONE',  ( 60.31639983755090384, 14.60307186445300154, -47.65366050515999774 ) ) ;
#48887=CIRCLE ( 'NONE', #7031, 20.00000000000000355 ) ;
#48888=CARTESIAN_POINT ( 'NONE',  ( -9.460678678543580133, -42.97416197475250499, -4.641705569678379106 ) ) ;
#48889=CARTESIAN_POINT ( 'NONE',  ( 12.91457160164050144, 34.27847415573319978, -47.58661663221230498 ) ) ;
#48897=CARTESIAN_POINT ( 'NONE',  ( 13.73527021832360084, 18.97497658011020150, -20.93080062246889739 ) ) ;
#48898=CARTESIAN_POINT ( 'NONE',  ( 47.18058539754699865, 23.56890317375210131, -74.36261486341250304 ) ) ;
#48899=CARTESIAN_POINT ( 'NONE',  ( 49.29272341951170233, -53.68831444397299890, -54.48007718848410263 ) ) ;
#48900=CARTESIAN_POINT ( 'NONE',  ( 52.10267380154080286, -33.11618894367330057, -20.65000000000000213 ) ) ;
#48904=CARTESIAN_POINT ( 'NONE',  ( 57.20485010882750743, 13.88381105532070059, -16.39258517501439982 ) ) ;
#48906=CIRCLE ( 'NONE', #31294, 1.999999999999999778 ) ;
#48912=CARTESIAN_POINT ( 'NONE',  ( 61.03746773581080021, -45.60543099132259925, -47.65219250438730825 ) ) ;
#48914=CARTESIAN_POINT ( 'NONE',  ( 50.95182575631829991, 19.71852405838109945, -76.14999999999999147 ) ) ;
#48917=EDGE_CURVE ( 'NONE', #5478, #6259, #4490, .T. ) ;
#48921=CARTESIAN_POINT ( 'NONE',  ( 83.47359158205320284, -45.21853209118459915, -47.48415154309300590 ) ) ;
#48922=ORIENTED_EDGE ( 'NONE', *, *, #17468, .T. ) ;
#48925=CARTESIAN_POINT ( 'NONE',  ( 61.75020040397059518, -45.11618894740859531, -46.37192837855609895 ) ) ;
#48927=CARTESIAN_POINT ( 'NONE',  ( 76.44636440943230582, -6.604755038381281196, -12.99629449306532258 ) ) ;
#48928=CARTESIAN_POINT ( 'NONE',  ( 55.95663929814069348, -50.71146718310139789, -52.90773913244279214 ) ) ;
#48933=CARTESIAN_POINT ( 'NONE',  ( 82.75389963950189554, 14.36256073625980001, -47.67227237920639737 ) ) ;
#48936=CARTESIAN_POINT ( 'NONE',  ( 16.13393739769620083, -15.61618894467929941, -10.44999999999999929 ) ) ;
#48938=ORIENTED_EDGE ( 'NONE', *, *, #46440, .F. ) ;
#48940=CARTESIAN_POINT ( 'NONE',  ( 62.99574006268588988, -29.46349362153740259, -16.20168838671330036 ) ) ;
#48942=AXIS2_PLACEMENT_3D ( 'NONE', #36353, #32403, #12528 ) ;
#48945=CARTESIAN_POINT ( 'NONE',  ( 66.10673863877181589, -15.61618894467929941, -16.72118890776879852 ) ) ;
#48948=CARTESIAN_POINT ( 'NONE',  ( 43.13712996743589656, -43.01636457780150380, -4.491635650860489548 ) ) ;
#48949=CARTESIAN_POINT ( 'NONE',  ( 47.18325654339099628, 23.57487866773040253, -54.61058579560449289 ) ) ;
#48950=CARTESIAN_POINT ( 'NONE',  ( 68.13393739769790614, -49.95860450174320277, -71.35146707679190570 ) ) ;
#48951=CARTESIAN_POINT ( 'NONE',  ( 53.48663704682130771, 18.10898805450162641, -49.00013169075777597 ) ) ;
#48953=CARTESIAN_POINT ( 'NONE',  ( 18.12477645186772079, -52.38391192226545456, -75.82251645564105047 ) ) ;
#48954=CARTESIAN_POINT ( 'NONE',  ( 66.48976749052368973, 0.09766644518992799451, -17.32442665463599951 ) ) ;
#48955=EDGE_LOOP ( 'NONE', ( #7020, #1205, #31398, #15736 ) ) ;
#48956=CARTESIAN_POINT ( 'NONE',  ( 14.44096052350820081, -51.53888401296669741, -75.38689171750549178 ) ) ;
#48957=CARTESIAN_POINT ( 'NONE',  ( 47.35766191916879819, -54.68311227971920374, -54.77973256522179923 ) ) ;
#48962=CARTESIAN_POINT ( 'NONE',  ( 55.63793626104714463, -45.97093497612764423, -16.89987028075756825 ) ) ;
#48963=CARTESIAN_POINT ( 'NONE',  ( 8.133937397696213267, -59.85907068714528378, -21.15000000000000213 ) ) ;
#48965=CARTESIAN_POINT ( 'NONE',  ( 13.68997053917030016, 20.12589560518139820, -23.13969474027650364 ) ) ;
#48966=CARTESIAN_POINT ( 'NONE',  ( 11.31889512729030045, 33.13089011102178461, -24.04922472088885499 ) ) ;
#48969=CARTESIAN_POINT ( 'NONE',  ( 48.76071015510490270, 22.82394617647319990, -55.20190746668970405 ) ) ;
#48972=ORIENTED_EDGE ( 'NONE', *, *, #42774, .F. ) ;
#48973=CARTESIAN_POINT ( 'NONE',  ( 18.45989064939156421, -52.11463163841762736, -75.47165350116151217 ) ) ;
#48975=CARTESIAN_POINT ( 'NONE',  ( 84.12790934798559306, 12.74340675664220157, -46.91176635807769912 ) ) ;
#48976=CARTESIAN_POINT ( 'NONE',  ( 53.35110984091899411, 17.85830479598100240, -27.09316622667170193 ) ) ;
#48977=EDGE_CURVE ( 'NONE', #29501, #2815, #34587, .T. ) ;
#48979=CARTESIAN_POINT ( 'NONE',  ( 10.97564820803404828, 33.77114500669411967, -17.33480536923671167 ) ) ;
#48980=CARTESIAN_POINT ( 'NONE',  ( 57.41961354596299572, -45.11618894467940066, -17.68838722488590065 ) ) ;
#48984=EDGE_LOOP ( 'NONE', ( #24959, #37374, #31079, #30522 ) ) ;
#48985=VERTEX_POINT ( 'NONE', #10762 ) ;
#48987=CARTESIAN_POINT ( 'NONE',  ( 11.79626796993740001, -64.91451392858408553, -16.32611600088480230 ) ) ;
#48988=CARTESIAN_POINT ( 'NONE',  ( 11.16916691016460028, 32.84040665082629573, -44.61689804176330654 ) ) ;
#48989=DIRECTION ( 'NONE',  ( -0.7226652920947586045, -0.6911981449639438280, 0.000000000000000000 ) ) ;
#48990=CARTESIAN_POINT ( 'NONE',  ( 51.50963138327329460, -50.97627007566619994, -50.14470441323439331 ) ) ;
#48991=CARTESIAN_POINT ( 'NONE',  ( 51.67587649748470113, 2.735120682347050192, -77.01363636363508647 ) ) ;
#48996=LINE ( 'NONE', #8894, #25831 ) ;
#48997=CARTESIAN_POINT ( 'NONE',  ( 50.62459508413220277, -49.95149871030799460, -76.16377488398599382 ) ) ;
#48999=ORIENTED_EDGE ( 'NONE', *, *, #14896, .T. ) ;
#49003=CARTESIAN_POINT ( 'NONE',  ( 56.22026493956754933, -50.82405358938415674, -74.67349521025255399 ) ) ;
#49004=DIRECTION ( 'NONE',  ( -1.000000000000000000, 0.000000000000000000, 0.000000000000000000 ) ) ;
#49005=ADVANCED_FACE ( 'NONE', ( #34063 ), #45624, .F. ) ;
#49007=AXIS2_PLACEMENT_3D ( 'NONE', #23440, #39972, #15862 ) ;
#49008=CARTESIAN_POINT ( 'NONE',  ( 13.68007965596629916, -51.36715864978960155, -22.99348026275350065 ) ) ;
#49010=CARTESIAN_POINT ( 'NONE',  ( 47.33318413658150092, -54.47214429496199983, -75.00321679105040573 ) ) ;
#49011=ORIENTED_EDGE ( 'NONE', *, *, #47384, .T. ) ;
#49012=CARTESIAN_POINT ( 'NONE',  ( 55.26140197345470284, 14.75560134660129918, -16.31640509964899977 ) ) ;
#49019=CARTESIAN_POINT ( 'NONE',  ( 47.44054024740749753, 23.27512645068789610, -74.80705470093730014 ) ) ;
#49020=DIRECTION ( 'NONE',  ( 0.3918900565003997638, 0.9200120562341090880, -1.214306433184117618E-13 ) ) ;
#49023=CARTESIAN_POINT ( 'NONE',  ( 52.10267380154080286, -33.11618894367330057, -20.65000000000000213 ) ) ;
#49024=CARTESIAN_POINT ( 'NONE',  ( 83.89200044194980421, -50.09049722508079583, -52.57651812407429759 ) ) ;
#49027=CARTESIAN_POINT ( 'NONE',  ( 61.24618047107790630, 14.01894199962020160, -46.62624509076869828 ) ) ;
#49028=CARTESIAN_POINT ( 'NONE',  ( 12.76594342643529956, -64.30274611092340820, -45.89070534480079999 ) ) ;
#49030=CARTESIAN_POINT ( 'NONE',  ( 53.01430333496330860, -49.56473660178939866, -48.82220832852659953 ) ) ;
#49033=CARTESIAN_POINT ( 'NONE',  ( 56.04052241335789830, 14.81222946749389990, -25.92335767470229868 ) ) ;
#49035=CARTESIAN_POINT ( 'NONE',  ( 51.25913404859330313, 18.70661076787169819, -76.33308050540989598 ) ) ;
#49036=CARTESIAN_POINT ( 'NONE',  ( 53.46721369579029925, 18.16710752707049892, -49.11454780549119903 ) ) ;
#49038=FACE_OUTER_BOUND ( 'NONE', #42986, .T. ) ;
#49039=CARTESIAN_POINT ( 'NONE',  ( 46.40621397443668172, 21.74426215006149121, -76.14873014702847343 ) ) ;
#49040=EDGE_CURVE ( 'NONE', #13057, #4375, #30135, .T. ) ;
#49046=CARTESIAN_POINT ( 'NONE',  ( 47.38650124322969504, -54.66575521192519460, -54.85296598789229705 ) ) ;
#49049=CARTESIAN_POINT ( 'NONE',  ( 56.58402530372350014, 19.32354596816890080, -53.00599679597699776 ) ) ;
#49051=FACE_BOUND ( 'NONE', #47006, .T. ) ;
#49055=ORIENTED_EDGE ( 'NONE', *, *, #7860, .T. ) ;
#49057=CARTESIAN_POINT ( 'NONE',  ( 8.958479335714679692, -63.16393755107500851, -46.63341780269549730 ) ) ;
#49061=FACE_OUTER_BOUND ( 'NONE', #9551, .T. ) ;
#49064=CARTESIAN_POINT ( 'NONE',  ( 51.83314622386949821, 18.96308757159359715, -76.51145678373148939 ) ) ;
#49070=ADVANCED_FACE ( 'NONE', ( #7091 ), #42044, .T. ) ;
#49076=EDGE_LOOP ( 'NONE', ( #3862, #32689, #28855, #19458 ) ) ;
#49077=CARTESIAN_POINT ( 'NONE',  ( 10.87442115971020051, -64.65679685997820059, -23.33560984931219906 ) ) ;
#49082=CARTESIAN_POINT ( 'NONE',  ( 14.58630607399789980, 20.67960354982550086, -75.75221093576881515 ) ) ;
#49088=CARTESIAN_POINT ( 'NONE',  ( 52.77132806972499424, -49.69320935574780407, -28.15000000000000213 ) ) ;
#49090=CARTESIAN_POINT ( 'NONE',  ( 16.06830620277110100, -51.06210401962729861, -20.66285861647710220 ) ) ;
#49091=CARTESIAN_POINT ( 'NONE',  ( 85.38000601716228743, -48.61618894467930119, -60.34000486924599471 ) ) ;
#49093=CARTESIAN_POINT ( 'NONE',  ( 46.19337157655569825, 14.89803173164150074, -9.780203716366939304 ) ) ;
#49094=ORIENTED_EDGE ( 'NONE', *, *, #38309, .F. ) ;
#49096=CARTESIAN_POINT ( 'NONE',  ( -9.094368388026579098, -44.04680377273619740, -5.580026499916369787 ) ) ;
#49097=CARTESIAN_POINT ( 'NONE',  ( 47.23303514576589635, 23.53638779022370286, -54.67236707882319990 ) ) ;
#49102=CARTESIAN_POINT ( 'NONE',  ( 11.51051956401449949, 34.11712030960200082, -17.72953785340450139 ) ) ;
#49104=CARTESIAN_POINT ( 'NONE',  ( 53.36496928958640495, 18.14812949222240235, -48.76946463831480116 ) ) ;
#49106=CARTESIAN_POINT ( 'NONE',  ( 53.59153692563230464, -49.40734274623049771, -49.22791863457509720 ) ) ;
#49107=AXIS2_PLACEMENT_3D ( 'NONE', #1847, #14672, #14156 ) ;
#49110=CARTESIAN_POINT ( 'NONE',  ( 53.27977303602300196, 20.78456751779900102, -53.62768324064160197 ) ) ;
#49115=CARTESIAN_POINT ( 'NONE',  ( 9.297729852059489986, 32.05137213967839926, -46.53031076905089947 ) ) ;
#49118=CARTESIAN_POINT ( 'NONE',  ( 66.54986627545559941, -30.20275677880469800, -16.95609989249500060 ) ) ;
#49119=ORIENTED_EDGE ( 'NONE', *, *, #2722, .F. ) ;
#49120=CARTESIAN_POINT ( 'NONE',  ( 18.33252661170309850, 20.80550406818660036, -75.55956264724760274 ) ) ;
#49121=AXIS2_PLACEMENT_3D ( 'NONE', #31188, #7886, #3446 ) ;
#49123=ORIENTED_EDGE ( 'NONE', *, *, #30938, .T. ) ;
#49124=CARTESIAN_POINT ( 'NONE',  ( 47.66548848826279539, 23.29226298427809638, -55.16185052358790131 ) ) ;
#49125=EDGE_LOOP ( 'NONE', ( #34500, #17534, #4240 ) ) ;
#49126=CARTESIAN_POINT ( 'NONE',  ( 11.20501727608539788, -64.66700489968309284, -46.03640593563060435 ) ) ;
#49127=CARTESIAN_POINT ( 'NONE',  ( 56.78593216331930194, -45.94738399931370054, -26.22487339609619994 ) ) ;
#49129=CARTESIAN_POINT ( 'NONE',  ( 61.46960199815709558, 14.08860104859740048, -47.25189778830119991 ) ) ;
#49132=DIRECTION ( 'NONE',  ( 0.000000000000000000, 0.000000000000000000, 1.000000000000000000 ) ) ;
#49133=CARTESIAN_POINT ( 'NONE',  ( 12.04669066983540660, 34.10719178353053849, -17.12210551403972403 ) ) ;
#49135=CARTESIAN_POINT ( 'NONE',  ( 50.27336491350419578, -45.97712286795240288, -12.51542028137719953 ) ) ;
#49136=CIRCLE ( 'NONE', #36559, 36.00000000000000000 ) ;
#49140=ORIENTED_EDGE ( 'NONE', *, *, #46084, .F. ) ;
#49142=CARTESIAN_POINT ( 'NONE',  ( 46.97440434136990461, -54.33447984715540002, -75.47461153638509757 ) ) ;
#49143=CARTESIAN_POINT ( 'NONE',  ( 16.13393739769620083, -15.61618894467929941, 6.072546842075589701 ) ) ;
#49144=CARTESIAN_POINT ( 'NONE',  ( 11.51160566532390028, -51.12796951774690513, -21.14999999999999858 ) ) ;
#49147=CARTESIAN_POINT ( 'NONE',  ( -3.785122221975860235, 16.81208508831930004, -4.794476613499900175 ) ) ;
#49150=CARTESIAN_POINT ( 'NONE',  ( 58.73226909804809281, 13.89440744020959961, -25.79432472329149917 ) ) ;
#49153=CARTESIAN_POINT ( 'NONE',  ( 56.68070624494579590, 16.55316904772309883, -48.38861384420910383 ) ) ;
#49154=CARTESIAN_POINT ( 'NONE',  ( 74.17629866868290378, 4.883811055320659733, -65.34607522167520699 ) ) ;
#49155=CARTESIAN_POINT ( 'NONE',  ( 76.82820232143379258, -43.20601130791419564, -14.64016038542719933 ) ) ;
#49158=CARTESIAN_POINT ( 'NONE',  ( 82.24889277099100582, -45.11618894467940066, -46.39515210564750447 ) ) ;
#49160=CARTESIAN_POINT ( 'NONE',  ( 49.47752793838059659, -53.68558960755940035, -54.66603854467830104 ) ) ;
#49162=EDGE_CURVE ( 'NONE', #1409, #25812, #5159, .T. ) ;
#49163=B_SPLINE_CURVE_WITH_KNOTS ( 'NONE', 3,
 ( #36271, #40218, #12438, #5108, #32066, #31814, #20537, #21063 ),
 .UNSPECIFIED., .F., .F.,
 ( 4, 2, 2, 4 ),
 ( 0.000000000000000000, 0.1059767115674661170, 0.3294825338126947112, 0.3562431257904284942 ),
 .UNSPECIFIED. ) ;
#49165=CARTESIAN_POINT ( 'NONE',  ( 17.92366493563939756, -51.11618894649849665, -74.14993593045390696 ) ) ;
#49167=ORIENTED_EDGE ( 'NONE', *, *, #46440, .T. ) ;
#49170=EDGE_CURVE ( 'NONE', #40777, #33786, #10119, .T. ) ;
#49174=CARTESIAN_POINT ( 'NONE',  ( 60.79136938041280303, -45.68357609118859841, -47.68552353186040449 ) ) ;
#49176=CARTESIAN_POINT ( 'NONE',  ( 50.08385623533860098, 18.00127108905680018, -76.14999999999999147 ) ) ;
#49178=DIRECTION ( 'NONE',  ( 0.000000000000000000, 0.000000000000000000, 1.000000000000000000 ) ) ;
#49180=CARTESIAN_POINT ( 'NONE',  ( 53.09962450323771321, -51.41544088504546295, -75.69942452463016025 ) ) ;
#49183=VERTEX_POINT ( 'NONE', #34191 ) ;
#49185=CARTESIAN_POINT ( 'NONE',  ( 61.52464553311489937, -45.32266663462549872, -47.25836995145800046 ) ) ;
#49189=ORIENTED_EDGE ( 'NONE', *, *, #4848, .T. ) ;
#49191=ORIENTED_EDGE ( 'NONE', *, *, #13135, .T. ) ;
#49192=CARTESIAN_POINT ( 'NONE',  ( 56.77563393123009661, 19.41451721634069827, -53.45922468568930697 ) ) ;
#49196=EDGE_CURVE ( 'NONE', #33088, #29183, #3028, .T. ) ;
#49199=CARTESIAN_POINT ( 'NONE',  ( 52.47790443081309775, -50.33621177253660051, -76.75890347598199526 ) ) ;
#49201=CARTESIAN_POINT ( 'NONE',  ( 60.74510967839550091, 14.28146716509339953, -47.06535153140909244 ) ) ;
#49203=DIRECTION ( 'NONE',  ( 0.000000000000000000, 0.000000000000000000, -1.000000000000000000 ) ) ;
#49204=CARTESIAN_POINT ( 'NONE',  ( 42.30721679385599998, 13.79944185400150047, -6.083977230941699510 ) ) ;
#49205=CARTESIAN_POINT ( 'NONE',  ( 42.53968774367980643, -44.23115725350800176, -5.088323970340629998 ) ) ;
#49208=EDGE_CURVE ( 'NONE', #14040, #14545, #39405, .T. ) ;
#49211=CARTESIAN_POINT ( 'NONE',  ( 65.04837026172849335, 1.029399159225240057, -17.85459962871380313 ) ) ;
#49212=ORIENTED_EDGE ( 'NONE', *, *, #49275, .F. ) ;
#49213=CARTESIAN_POINT ( 'NONE',  ( 14.21603903184900020, -51.93578155835659516, -75.67800190747080080 ) ) ;
#49214=CARTESIAN_POINT ( 'NONE',  ( 57.35719032655089933, 19.00113118003429591, -52.73978338582610803 ) ) ;
#49216=CARTESIAN_POINT ( 'NONE',  ( 83.84453607997100733, 13.09586255422381562, -46.66650892571503562 ) ) ;
#49217=DIRECTION ( 'NONE',  ( 0.8090169943749475623, 0.5877852522924730261, 0.000000000000000000 ) ) ;
#49218=( GEOMETRIC_REPRESENTATION_CONTEXT ( 3 ) GLOBAL_UNCERTAINTY_ASSIGNED_CONTEXT ( ( #23193 ) ) GLOBAL_UNIT_ASSIGNED_CONTEXT ( ( #24024, #47914, #27970 ) ) REPRESENTATION_CONTEXT ( 'NONE', 'WORKASPACE' ) );
#49220=DIRECTION ( 'NONE',  ( 1.000000000000000000, 0.000000000000000000, 0.000000000000000000 ) ) ;
#49221=CARTESIAN_POINT ( 'NONE',  ( 47.75515754607209828, -54.46163821482410583, -54.87660553739389968 ) ) ;
#49225=CARTESIAN_POINT ( 'NONE',  ( 56.43116028100519799, 19.50260086978540031, -53.39630102202139739 ) ) ;
#49226=CARTESIAN_POINT ( 'NONE',  ( 48.63696446388820505, 22.87845126040230070, -55.31022682284879721 ) ) ;
#49227=ORIENTED_EDGE ( 'NONE', *, *, #49298, .T. ) ;
#49229=EDGE_LOOP ( 'NONE', ( #32734, #7322, #2398, #36454, #44471, #37309 ) ) ;
#49230=CYLINDRICAL_SURFACE ( 'NONE', #42959, 1.999999999999997780 ) ;
#49231=CARTESIAN_POINT ( 'NONE',  ( 69.89373504110861290, -33.11618894431183691, -20.65000000000000213 ) ) ;
#49232=CARTESIAN_POINT ( 'NONE',  ( 57.24507234304070380, -50.61619228913700397, -53.91419826543189942 ) ) ;
#49233=CARTESIAN_POINT ( 'NONE',  ( 82.96870692852729690, 14.04770048173509878, -47.29707907477579454 ) ) ;
#49234=CARTESIAN_POINT ( 'NONE',  ( 53.28513676268730137, 17.88318008810170312, -27.00290219004990178 ) ) ;
#49236=CARTESIAN_POINT ( 'NONE',  ( 11.88460916116891575, 33.59273172673112384, -16.16716782997541202 ) ) ;
#49238=CARTESIAN_POINT ( 'NONE',  ( 55.55440406777280060, -45.13279848311309905, -14.71482509943139938 ) ) ;
#49240=ORIENTED_EDGE ( 'NONE', *, *, #39326, .F. ) ;
#49242=CARTESIAN_POINT ( 'NONE',  ( 11.93287529298650007, -65.09933430725659775, -16.56789608242559808 ) ) ;
#49243=CARTESIAN_POINT ( 'NONE',  ( 11.10070370541949991, 32.46195726624170419, -44.39283574477070005 ) ) ;
#49245=( BOUNDED_CURVE ( )  B_SPLINE_CURVE ( 3, ( #22242, #42186, #38250, #5761 ),
 .UNSPECIFIED., .F., .T. ) 
 B_SPLINE_CURVE_WITH_KNOTS ( ( 4, 4 ),
 ( 0.08942664019426993516, 0.6257761648869514248 ),
 .UNSPECIFIED. ) 
 CURVE ( )  GEOMETRIC_REPRESENTATION_ITEM ( )  RATIONAL_B_SPLINE_CURVE ( ( 1.000000000000000000, 0.9761707593066137889, 0.9761707593066137889, 1.000000000000000000 ) ) 
 REPRESENTATION_ITEM ( '' )  );
#49246=CARTESIAN_POINT ( 'NONE',  ( 50.05726953842039961, -52.36002610383659572, -51.66910864135500248 ) ) ;
#49247=CARTESIAN_POINT ( 'NONE',  ( 46.35275103504449845, -52.90993241930539881, -76.14999999999999147 ) ) ;
#49248=EDGE_LOOP ( 'NONE', ( #45392, #11344, #47136, #23986 ) ) ;
#49250=CARTESIAN_POINT ( 'NONE',  ( 57.32810207127130298, 14.58245081771279850, -26.26943966852299894 ) ) ;
#49251=DIRECTION ( 'NONE',  ( 0.000000000000000000, 0.000000000000000000, 1.000000000000000000 ) ) ;
#49256=ORIENTED_EDGE ( 'NONE', *, *, #9104, .F. ) ;
#49258=FACE_OUTER_BOUND ( 'NONE', #23271, .T. ) ;
#49262=CARTESIAN_POINT ( 'NONE',  ( 48.60192926749129327, -46.16789356278570011, -11.45750196660969955 ) ) ;
#49264=CARTESIAN_POINT ( 'NONE',  ( 13.95361866583219879, -51.19462969149069664, -22.78638230707139911 ) ) ;
#49265=CARTESIAN_POINT ( 'NONE',  ( 54.86522692285650038, 19.64335628441130055, -75.60900715747830247 ) ) ;
#49266=CARTESIAN_POINT ( 'NONE',  ( 47.37714334366550162, -54.54225709709379544, -74.80639350504939955 ) ) ;
#49268=CARTESIAN_POINT ( 'NONE',  ( 55.16747951314059861, 14.77612155303600083, -16.22375705186960104 ) ) ;
#49269=CARTESIAN_POINT ( 'NONE',  ( 57.35590717504809533, -50.13655087669759780, -52.61987026566970371 ) ) ;
#49270=CARTESIAN_POINT ( 'NONE',  ( 52.67086496592249745, -49.78228103073629995, -48.75851410805960029 ) ) ;
#49275=EDGE_CURVE ( 'NONE', #31649, #49183, #7220, .T. ) ;
#49276=CARTESIAN_POINT ( 'NONE',  ( 47.14077604958600176, 22.83395626750060003, -75.60950524211389734 ) ) ;
#49278=CARTESIAN_POINT ( 'NONE',  ( 75.24176788607847755, -33.88749087479735067, -12.24369074004802016 ) ) ;
#49279=CARTESIAN_POINT ( 'NONE',  ( 12.26282170032090058, 33.38295891277739713, -15.83707920940340053 ) ) ;
#49282=CARTESIAN_POINT ( 'NONE',  ( 57.17871029158580143, -50.61618894532200130, -74.69286753486250063 ) ) ;
#49285=CARTESIAN_POINT ( 'NONE',  ( 61.75019796695539753, 14.88381105532069881, -46.37203261889099792 ) ) ;
#49286=CARTESIAN_POINT ( 'NONE',  ( -12.78066350546869856, -57.03146538805550136, -53.01233286176620396 ) ) ;
#49287=ORIENTED_EDGE ( 'NONE', *, *, #10278, .F. ) ;
#49289=CARTESIAN_POINT ( 'NONE',  ( 53.19189387552519577, -49.47595491150869407, -48.89717368174490275 ) ) ;
#49290=VECTOR ( 'NONE', #16899, 1000.000000000000000 ) ;
#49291=CARTESIAN_POINT ( 'NONE',  ( 61.55075694485340421, -45.11618134123870050, -27.39088103713649858 ) ) ;
#49292=CARTESIAN_POINT ( 'NONE',  ( 47.75291977277740330, -54.48739848013089926, -55.20309039576500254 ) ) ;
#49293=CARTESIAN_POINT ( 'NONE',  ( 57.57552615852310396, 13.96395657264059942, -25.75103562460460083 ) ) ;
#49296=CARTESIAN_POINT ( 'NONE',  ( 50.29495134167750336, 18.68575087643539945, -76.14999999999999147 ) ) ;
#49297=CARTESIAN_POINT ( 'NONE',  ( 53.38247603630389904, 18.20190482432069956, -49.11032166583889591 ) ) ;
#49298=EDGE_CURVE ( 'NONE', #6528, #5619, #4877, .T. ) ;
#49301=CARTESIAN_POINT ( 'NONE',  ( 67.49343310951690000, -43.71773202259419833, -11.18492891670890010 ) ) ;
#49302=ORIENTED_EDGE ( 'NONE', *, *, #33887, .T. ) ;
#49306=CARTESIAN_POINT ( 'NONE',  ( 47.47143074607309643, -54.61084340594300102, -54.78606453627770634 ) ) ;
#49307=DIRECTION ( 'NONE',  ( 0.000000000000000000, -1.000000000000000000, 0.000000000000000000 ) ) ;
#49309=CARTESIAN_POINT ( 'NONE',  ( 58.29681012269350049, 17.45128343075899835, -50.95499530789079756 ) ) ;
#49317=CARTESIAN_POINT ( 'NONE',  ( 8.803322232233091071, -63.21315167929310519, -46.67017412665830278 ) ) ;
#49318=LINE ( 'NONE', #41181, #11847 ) ;
#49321=CARTESIAN_POINT ( 'NONE',  ( 83.95017420394412966, 13.51629706050414370, -47.46180916972096497 ) ) ;
#49323=CARTESIAN_POINT ( 'NONE',  ( 52.76002509195300405, 19.59599347919969858, -76.29651901294879224 ) ) ;
#49326=DIRECTION ( 'NONE',  ( -0.2138226895232112068, -0.2149704985134071045, -0.9529257800133007494 ) ) ;
#49331=ORIENTED_EDGE ( 'NONE', *, *, #1937, .F. ) ;
#49332=CARTESIAN_POINT ( 'NONE',  ( 18.42160731955080522, 20.91301623499861151, -75.51793353187491675 ) ) ;
#49338=ADVANCED_FACE ( 'NONE', ( #39189 ), #33516, .T. ) ;
#49340=CARTESIAN_POINT ( 'NONE',  ( 13.69873651028019879, 20.72643819036770196, -75.26885115310530239 ) ) ;
#49342=CARTESIAN_POINT ( 'NONE',  ( 82.13853704237929776, -47.11618894467930119, -46.37203261889099792 ) ) ;
#49343=CARTESIAN_POINT ( 'NONE',  ( 82.62217614637160068, -45.06710035710920437, -46.37143498965749444 ) ) ;
#49346=CARTESIAN_POINT ( 'NONE',  ( 52.97741287737559901, -49.44182383634679923, -27.32735893619970113 ) ) ;
#49347=CARTESIAN_POINT ( 'NONE',  ( 15.59055465918129890, -51.07878210359169913, -21.35214379961709952 ) ) ;
#49348=CARTESIAN_POINT ( 'NONE',  ( 5.837997345208469469, 28.59614577856129713, -13.72651855969540158 ) ) ;
#49350=DIRECTION ( 'NONE',  ( 1.000000000000000000, 0.000000000000000000, 0.000000000000000000 ) ) ;
#49352=CARTESIAN_POINT ( 'NONE',  ( -10.87682430560830049, -42.35274797428079552, -6.258335782129580416 ) ) ;
#49353=CARTESIAN_POINT ( 'NONE',  ( 47.38355736121539508, 23.43506509291880135, -54.85967685610170008 ) ) ;
#49354=DIRECTION ( 'NONE',  ( 1.000000000000000000, 0.000000000000000000, 0.000000000000000000 ) ) ;
#49357=CARTESIAN_POINT ( 'NONE',  ( 11.24176296214520043, 33.99927896084999901, -17.63707693806219723 ) ) ;
#49360=ADVANCED_FACE ( 'NONE', ( #34978 ), #15077, .F. ) ;
#49361=DIRECTION ( 'NONE',  ( -0.5110015285683598973, 0.4887508954475665024, -0.7071067811865485719 ) ) ;
#49362=CARTESIAN_POINT ( 'NONE',  ( 54.36726455973389704, -49.00028188061180856, -48.99340372004090227 ) ) ;
#49363=CARTESIAN_POINT ( 'NONE',  ( 53.71520252225610648, 17.65497178273479761, -27.13662481516249869 ) ) ;
#49364=CARTESIAN_POINT ( 'NONE',  ( 56.06025071900570111, 19.69505054709740222, -53.55197912626789503 ) ) ;
#49369=CARTESIAN_POINT ( 'NONE',  ( 46.59920180852409288, 13.88381105532070059, -7.957592738636480867 ) ) ;
#49371=CARTESIAN_POINT ( 'NONE',  ( 19.04602951442133474, 21.06500373477386034, -15.95264016292855658 ) ) ;
#49372=CARTESIAN_POINT ( 'NONE',  ( 9.735422304259749637, 31.96558444038419822, -46.29845817061509905 ) ) ;
#49375=DIRECTION ( 'NONE',  ( -0.7288689868556610385, 0.6846531968814593139, 0.000000000000000000 ) ) ;
#49376=CARTESIAN_POINT ( 'NONE',  ( 17.91483615131959795, 20.08140804309819671, -75.03330975078259257 ) ) ;
#49377=ORIENTED_EDGE ( 'NONE', *, *, #22925, .T. ) ;
#49379=DIRECTION ( 'NONE',  ( 0.000000000000000000, 1.000000000000000000, 0.000000000000000000 ) ) ;
#49380=CIRCLE ( 'NONE', #35094, 1.000000000000000444 ) ;
#49381=ORIENTED_EDGE ( 'NONE', *, *, #2060, .T. ) ;
#49382=CARTESIAN_POINT ( 'NONE',  ( 12.84259407419289900, -65.50421454171720370, -47.60240834020890333 ) ) ;
#49383=CARTESIAN_POINT ( 'NONE',  ( 57.29351084095430480, -45.75340000471780399, -26.24431632910020085 ) ) ;
#49384=CARTESIAN_POINT ( 'NONE',  ( 16.13393739769620083, -15.61618894467929941, -11.65000000000000036 ) ) ;
#49386=CARTESIAN_POINT ( 'NONE',  ( 61.68720307896570176, 13.88748677907970119, -46.48647000020920217 ) ) ;
#49388=VERTEX_POINT ( 'NONE', #24451 ) ;
#49389=CARTESIAN_POINT ( 'NONE',  ( 75.23597853791552836, 2.430820170349590192, -12.22130859511000622 ) ) ;
#49391=CARTESIAN_POINT ( 'NONE',  ( 46.27378782115770406, -45.92656169234390262, -9.695123937814390302 ) ) ;
#49396=CARTESIAN_POINT ( 'NONE',  ( 47.11354740527600171, -54.64978104499210332, -74.95188530402140259 ) ) ;
#49398=CARTESIAN_POINT ( 'NONE',  ( 50.44903216339780272, 14.35615507604409835, -12.26919617389220107 ) ) ;
#49405=CARTESIAN_POINT ( 'NONE',  ( 12.36324357420019915, -64.54680782163349306, -15.76420532458509882 ) ) ;
#49406=CARTESIAN_POINT ( 'NONE',  ( 58.68274678269510503, 13.94184647788599918, -25.96024197693940039 ) ) ;
#49409=B_SPLINE_SURFACE_WITH_KNOTS ( 'NONE', 3, 3, ( 
 ( #35342, #3649, #43985, #19101, #43734, #51082, #15180, #51344, #35610, #19620, #39545 ),
 ( #27983, #31907, #10996, #39038, #47422, #31138, #7068, #19870, #27216, #4147, #8091 ),
 ( #43228, #46910, #34822, #26961, #15954, #15442, #51598, #24035, #7320, #11776, #31395 ),
 ( #43475, #23267, #39286, #3395, #7835, #15693, #11515, #35861, #47670, #7582, #31648 ),
 ( #23784, #42973, #27474, #27735, #3905, #51850, #47928, #50826, #14918, #23018, #12804 ),
 ( #37160, #45023, #48436, #40566, #28503, #25073, #41090, #29279, #44238, #5201, #17244 ),
 ( #44501, #1257, #48969, #12536, #48702, #21152, #24818, #16458, #41340, #33208, #28760 ),
 ( #49226, #217, #44762, #29026, #13320, #45282, #32160, #9391, #48176, #25338, #8865 ),
 ( #20635, #20123, #36622, #995, #40311, #16202, #4407, #36116, #32413, #40827, #12278 ),
 ( #28240, #4926, #8342, #13073, #24296, #9122, #8603, #16993, #20374, #36363, #471 ),
 ( #20897, #36895, #32942, #24553, #4662, #724, #16717, #32675, #18007, #37663, #29535 ),
 ( #1769, #41857, #6480, #13823, #17750, #14594, #26629, #45540, #21921, #33719, #17498 ),
 ( #22179, #26110, #42121, #30564, #9635, #14079, #49734, #37411, #5962, #46585, #10414 ),
 ( #1513, #25591, #22438, #29781, #38445, #18258, #10673, #21410, #41597, #14337, #5457 ),
 ( #10153, #2027, #25845, #38189, #6222, #13572, #45800, #21659, #33972, #30040, #33466 ),
 ( #2284, #49486, #34499, #18526, #46064, #37931, #5704, #26367, #9889, #49986, #34227 ),
 ( #50247, #30306, #46323, #42383, #2545, #50504, #38716, #19554, #18780, #30818, #43162 ),
 ( #7002, #39486, #47606, #15633, #51536, #43414, #46846, #11453, #3584, #35546, #22953 ),
 ( #43672, #31585, #51279, #10932, #26899, #35801, #11706, #47864, #7772, #42646, #15376 ),
 ( #31075, #3322, #11967, #38975, #22700, #27411, #3067, #42906, #6743, #23722, #7515 ) ),
 .UNSPECIFIED., .F., .F., .F.,
 ( 4, 2, 2, 2, 2, 2, 2, 2, 2, 4 ),
 ( 4, 1, 1, 1, 1, 1, 1, 1, 4 ),
 ( -3.516439999999999908E-13, 0.4027787201731649613, 0.8630972575143259773, 1.150796343352550100, 1.294645886271670099, 1.524805154942250107, 1.789982511918259966, 2.002124397499069897, 2.214266283079879827, 2.301592686705460356 ),
 ( 0.000000000000000000, 0.1250000000000000000, 0.2500000000000000000, 0.3750000000000000000, 0.5000000000000000000, 0.6250000000000000000, 0.7500000000000000000, 0.8750000000000000000, 1.000000000000000000 ),
 .UNSPECIFIED. ) ;
#49412=CARTESIAN_POINT ( 'NONE',  ( -10.74377218051129823, -41.32309662373379666, -4.375840798615800331 ) ) ;
#49417=CARTESIAN_POINT ( 'NONE',  ( 47.48063017294606425, -54.33024059656849403, -75.12266286251488623 ) ) ;
#49419=CARTESIAN_POINT ( 'NONE',  ( 49.13578581667089651, -53.89835027320589944, -55.25235944000669974 ) ) ;
#49421=CARTESIAN_POINT ( 'NONE',  ( 76.87859684847769870, -43.11619168008749625, -14.85884840380859906 ) ) ;
#49429=CARTESIAN_POINT ( 'NONE',  ( 60.46305695989290285, -45.79448408183320396, -47.68939924749230386 ) ) ;
#49431=CARTESIAN_POINT ( 'NONE',  ( 12.44373460634760065, 18.75032478515380063, -21.13286269215250002 ) ) ;
#49434=CARTESIAN_POINT ( 'NONE',  ( 50.95182575631829991, -50.95090194773979420, -76.14999999999999147 ) ) ;
#49438=ORIENTED_EDGE ( 'NONE', *, *, #28835, .T. ) ;
#49439=CARTESIAN_POINT ( 'NONE',  ( 61.44117429376609607, -45.34731734014510351, -47.30190162006350363 ) ) ;
#49441=CARTESIAN_POINT ( 'NONE',  ( 60.93032024860885798, 14.20921469949021976, -47.21540920729788127 ) ) ;
#49443=VECTOR ( 'NONE', #1213, 1000.000000000000000 ) ;
#49445=ORIENTED_EDGE ( 'NONE', *, *, #7249, .T. ) ;
#49455=LINE ( 'NONE', #9361, #45890 ) ;
#49456=CARTESIAN_POINT ( 'NONE',  ( 51.83314574864460411, -50.19546514301369911, -76.51145668752809570 ) ) ;
#49457=CARTESIAN_POINT ( 'NONE',  ( 7.517033938252880354, -61.58399597082019739, -19.14999999999999858 ) ) ;
#49460=CARTESIAN_POINT ( 'NONE',  ( 11.51160566532330165, 19.89559162839070083, -23.15000000000000213 ) ) ;
#49461=CARTESIAN_POINT ( 'NONE',  ( 42.61258517392390388, 13.83109901667380015, -6.251412676332040341 ) ) ;
#49463=B_SPLINE_CURVE_WITH_KNOTS ( 'NONE', 3,
 ( #14943, #46937, #26991, #47192, #35370, #7093 ),
 .UNSPECIFIED., .F., .F.,
 ( 4, 2, 4 ),
 ( 0.000000000000000000, 0.5400851465932335893, 1.000000000000000000 ),
 .UNSPECIFIED. ) ;
#49464=CARTESIAN_POINT ( 'NONE',  ( 42.74124888519239818, -44.04278178416409872, -5.015693368613340475 ) ) ;
#49466=DIRECTION ( 'NONE',  ( -0.9200120562340469155, 0.3918900565005459247, -8.326672684688669123E-17 ) ) ;
#49469=CARTESIAN_POINT ( 'NONE',  ( 66.14676216358580518, -0.1907523817752760087, -17.02976572029630020 ) ) ;
#49471=CARTESIAN_POINT ( 'NONE',  ( 14.10861501657639927, -52.01891576978010079, -75.67066142420200947 ) ) ;
#49472=CARTESIAN_POINT ( 'NONE',  ( 57.35780230080800379, 18.93711611908999970, -52.65865528046390409 ) ) ;
#49475=LINE ( 'NONE', #14587, #33463 ) ;
#49477=AXIS2_PLACEMENT_3D ( 'NONE', #123, #40726, #20526 ) ;
#49478=ADVANCED_FACE ( 'NONE', ( #32060 ), #22797, .T. ) ;
#49481=CARTESIAN_POINT ( 'NONE',  ( 47.71207051903009955, -54.49607191801889883, -54.98518041347480079 ) ) ;
#49484=CARTESIAN_POINT ( 'NONE',  ( 41.66707738213217738, 13.41595190789255554, -5.278831647791760062 ) ) ;
#49485=ADVANCED_FACE ( 'NONE', ( #1832 ), #5518, .T. ) ;
#49486=CARTESIAN_POINT ( 'NONE',  ( 47.84365481784320195, 23.21637092124190360, -55.21126586928509994 ) ) ;
#49488=ORIENTED_EDGE ( 'NONE', *, *, #17164, .F. ) ;
#49489=CARTESIAN_POINT ( 'NONE',  ( 18.84360118837656017, -51.80630187018725508, -74.54430098193516585 ) ) ;
#49492=CARTESIAN_POINT ( 'NONE',  ( 84.44784216359251161, 11.88381105532070059, -47.47585302082339354 ) ) ;
#49493=CARTESIAN_POINT ( 'NONE',  ( 52.56521993400819781, 18.62941884317319818, -28.15003746460830314 ) ) ;
#49495=DIRECTION ( 'NONE',  ( 0.000000000000000000, 0.000000000000000000, 1.000000000000000000 ) ) ;
#49498=ORIENTED_EDGE ( 'NONE', *, *, #7411, .T. ) ;
#49500=CARTESIAN_POINT ( 'NONE',  ( 11.86574223144489970, -65.07138037345019654, -16.54426240394709779 ) ) ;
#49501=CARTESIAN_POINT ( 'NONE',  ( 12.58777455595629924, 34.22037323676799758, -47.11705430144780138 ) ) ;
#49503=CARTESIAN_POINT ( 'NONE',  ( 12.18715281636350056, 34.05328359738290089, -46.13824078902359815 ) ) ;
#49508=CARTESIAN_POINT ( 'NONE',  ( 47.54344196522969668, 23.41772573375219935, -55.12343871991259903 ) ) ;
#49509=CARTESIAN_POINT ( 'NONE',  ( 64.42654594965659953, -1.187628165131600078, -16.42224863846029947 ) ) ;
#49510=CARTESIAN_POINT ( 'NONE',  ( 50.92009741000290290, -50.43920147318139868, -76.16477593974259719 ) ) ;
#49514=DIRECTION ( 'NONE',  ( 1.000000000000000000, 0.000000000000000000, 0.000000000000000000 ) ) ;
#49519=CARTESIAN_POINT ( 'NONE',  ( 50.59865606475919719, -46.19775965174260079, -12.88937197673160107 ) ) ;
#49522=CARTESIAN_POINT ( 'NONE',  ( 54.50221993657880404, 19.67977562750719756, -75.72703011672629714 ) ) ;
#49524=CARTESIAN_POINT ( 'NONE',  ( 47.38033551737640181, -54.20286183426010496, -75.36291177546809195 ) ) ;
#49526=CARTESIAN_POINT ( 'NONE',  ( 55.76738788914159528, 14.35627483231789903, -16.42583790588760095 ) ) ;
#49528=CARTESIAN_POINT ( 'NONE',  ( 57.26283657379369885, -50.61618895537380070, -53.75815476539319349 ) ) ;
#49529=CARTESIAN_POINT ( 'NONE',  ( 52.70598057219940102, -49.76175563869689711, -48.81476139346880672 ) ) ;
#49531=CARTESIAN_POINT ( 'NONE',  ( 53.70552627772385534, -51.31509389902640095, -75.56421117895261830 ) ) ;
#49532=EDGE_CURVE ( 'NONE', #14446, #48131, #40226, .T. ) ;
#49533=CARTESIAN_POINT ( 'NONE',  ( 47.16864635708899556, 22.97736630563930049, -75.46775895608919882 ) ) ;
#49535=CARTESIAN_POINT ( 'NONE',  ( 41.43967002271349287, -45.63915426718229895, -6.362515298815959675 ) ) ;
#49540=CARTESIAN_POINT ( 'NONE',  ( 60.83133136721959744, 14.23629320661039976, -47.01992809069390233 ) ) ;
#49541=CARTESIAN_POINT ( 'NONE',  ( 57.24955896891499663, -50.61618894527399704, -74.42081638965770196 ) ) ;
#49544=CARTESIAN_POINT ( 'NONE',  ( 61.34010611512319855, 13.97110158644820110, -46.37202112184679947 ) ) ;
#49547=CARTESIAN_POINT ( 'NONE',  ( -26.15868020285170203, 9.963078067300591201, -54.51850539491499603 ) ) ;
#49551=CARTESIAN_POINT ( 'NONE',  ( 52.83031072168890319, -49.66267504922139864, -48.71029889621100040 ) ) ;
#49554=CARTESIAN_POINT ( 'NONE',  ( 59.16460309383230509, -45.16598951315400257, -26.08201338363890187 ) ) ;
#49556=CARTESIAN_POINT ( 'NONE',  ( 13.38185851215770050, 19.61017703320019834, -21.60458205337010185 ) ) ;
#49557=CARTESIAN_POINT ( 'NONE',  ( 56.57085133330490123, 14.20563404004749941, -25.70412341356980335 ) ) ;
#49560=CARTESIAN_POINT ( 'NONE',  ( 52.91120708058170408, 18.40136555541419838, -48.91474115954339652 ) ) ;
#49562=CARTESIAN_POINT ( 'NONE',  ( 73.88940586792639920, -43.69535901349680529, -12.99103297813889846 ) ) ;
#49564=VERTEX_POINT ( 'NONE', #5258 ) ;
#49567=CARTESIAN_POINT ( 'NONE',  ( 47.47394861760930240, -54.61301726039770443, -54.85049212571620103 ) ) ;
#49571=CARTESIAN_POINT ( 'NONE',  ( 11.00562562889980001, -65.16137108100819830, -18.07900588240499928 ) ) ;
#49572=CARTESIAN_POINT ( 'NONE',  ( 52.82975622904289992, 18.42854261028849905, -48.47378032971769812 ) ) ;
#49579=CARTESIAN_POINT ( 'NONE',  ( 9.285734567762460756, -63.19748911377190126, -46.53048861919899792 ) ) ;
#49582=CARTESIAN_POINT ( 'NONE',  ( 84.44784216359251161, 11.88381105532070059, -47.47585302082339354 ) ) ;
#49584=CARTESIAN_POINT ( 'NONE',  ( 51.40458829710209443, 19.31600304772210208, -76.23573209377541104 ) ) ;
#49590=DIRECTION ( 'NONE',  ( 1.000000000000000000, 0.000000000000000000, 0.000000000000000000 ) ) ;
#49592=ORIENTED_EDGE ( 'NONE', *, *, #19521, .F. ) ;
#49595=CARTESIAN_POINT ( 'NONE',  ( 57.55751162087899786, 19.24776070067099099, -53.20292136905285929 ) ) ;
#49597=AXIS2_PLACEMENT_3D ( 'NONE', #13533, #21881, #26070 ) ;
#49601=CARTESIAN_POINT ( 'NONE',  ( 13.58362953646680005, 20.62786770048269958, -75.03330975078259257 ) ) ;
#49602=LINE ( 'NONE', #25970, #3097 ) ;
#49603=CARTESIAN_POINT ( 'NONE',  ( 41.22889096848290080, -44.82821486788269993, -5.431173202240829667 ) ) ;
#49606=VERTEX_POINT ( 'NONE', #2614 ) ;
#49607=CARTESIAN_POINT ( 'NONE',  ( 54.88272693801879853, -47.33106691389519938, -26.10537818549139999 ) ) ;
#49608=CARTESIAN_POINT ( 'NONE',  ( 56.15371975346319999, -50.83714413667020438, -74.67436945125109560 ) ) ;
#49609=CARTESIAN_POINT ( 'NONE',  ( -0.04430710383532700247, 22.44604592029679679, -9.692299893202831029 ) ) ;
#49610=LINE ( 'NONE', #13448, #11268 ) ;
#49613=CARTESIAN_POINT ( 'NONE',  ( -9.541283486264569902, -43.63710254895489982, -5.656394099422319854 ) ) ;
#49614=CARTESIAN_POINT ( 'NONE',  ( 47.40067335528860326, 23.42405946800979777, -54.81948824301620249 ) ) ;
#49615=DIRECTION ( 'NONE',  ( 0.000000000000000000, 0.000000000000000000, -1.000000000000000000 ) ) ;
#49617=CARTESIAN_POINT ( 'NONE',  ( 61.02217321269120731, 14.13630581668499886, -46.91830674221320407 ) ) ;
#49618=CARTESIAN_POINT ( 'NONE',  ( 11.88236604821910092, 34.20274920972010335, -17.91369388827870068 ) ) ;
#49619=CARTESIAN_POINT ( 'NONE',  ( 52.08783726412929838, 18.38123683491329885, -77.13961689194590576 ) ) ;
#49620=CARTESIAN_POINT ( 'NONE',  ( 52.85589143289899994, 18.41484964472980224, -48.63420543068679791 ) ) ;
#49621=CYLINDRICAL_SURFACE ( 'NONE', #41725, 1.500000000000001332 ) ;
#49622=CARTESIAN_POINT ( 'NONE',  ( 59.94065709827619770, -46.08170771231470297, -47.78792003745029859 ) ) ;
#49624=CARTESIAN_POINT ( 'NONE',  ( 55.53286969579190213, 19.65994446189469969, -52.96077464504600130 ) ) ;
#49626=CARTESIAN_POINT ( 'NONE',  ( 11.93174526809839975, -65.43929183185349530, -17.93019253464870033 ) ) ;
#49628=ORIENTED_EDGE ( 'NONE', *, *, #6555, .F. ) ;
#49630=CARTESIAN_POINT ( 'NONE',  ( 10.97882797226870188, 32.03231419732679797, -44.74228707380109427 ) ) ;
#49631=AXIS2_PLACEMENT_3D ( 'NONE', #3170, #27253, #19401 ) ;
#49632=DIRECTION ( 'NONE',  ( 1.000000000000000000, 0.000000000000000000, 0.000000000000000000 ) ) ;
#49634=CARTESIAN_POINT ( 'NONE',  ( 68.16820022677380564, -30.11594836049780355, -18.00617522382760072 ) ) ;
#49639=CARTESIAN_POINT ( 'NONE',  ( 49.72648160330989953, 22.41435850158119791, -55.11972614036179863 ) ) ;
#49641=CARTESIAN_POINT ( 'NONE',  ( 10.57222913045199952, -64.13241197350170353, -46.01869289140690000 ) ) ;
#49642=CARTESIAN_POINT ( 'NONE',  ( 57.36243933490059987, -45.44515605360940214, -26.07079599989479846 ) ) ;
#49643=DIRECTION ( 'NONE',  ( 0.000000000000000000, 1.000000000000000000, 0.000000000000000000 ) ) ;
#49646=DIRECTION ( 'NONE',  ( 0.000000000000000000, 1.000000000000000000, 0.000000000000000000 ) ) ;
#49647=ORIENTED_EDGE ( 'NONE', *, *, #31979, .T. ) ;
#49650=CARTESIAN_POINT ( 'NONE',  ( 49.79071638101620323, -45.11618894460959694, -10.43288004981720007 ) ) ;
#49653=CARTESIAN_POINT ( 'NONE',  ( 16.22100018022290158, 19.83813723611639901, -20.14984494908090085 ) ) ;
#49654=CARTESIAN_POINT ( 'NONE',  ( 47.64143405400680109, -54.53488714545009941, -74.14999999999999147 ) ) ;
#49655=VERTEX_POINT ( 'NONE', #39544 ) ;
#49657=CARTESIAN_POINT ( 'NONE',  ( 47.02180052276420241, -54.30164223407509638, -75.47109442055590023 ) ) ;
#49658=CARTESIAN_POINT ( 'NONE',  ( 60.46644818218479855, 14.58403685241730230, -47.72755095986849483 ) ) ;
#49659=ADVANCED_FACE ( 'NONE', ( #7834 ), #27570, .F. ) ;
#49660=CARTESIAN_POINT ( 'NONE',  ( 51.92534425568300094, 13.88381105524860004, -11.95547866172319829 ) ) ;
#49662=AXIS2_PLACEMENT_3D ( 'NONE', #7958, #11904, #28110 ) ;
#49664=CARTESIAN_POINT ( 'NONE',  ( 51.08534821908229873, 19.80328544295599968, -76.14824059617301089 ) ) ;
#49665=CARTESIAN_POINT ( 'NONE',  ( 58.39402530481319786, 14.02893895274939950, -26.06414309828389975 ) ) ;
#49668=DIRECTION ( 'NONE',  ( 0.000000000000000000, -1.000000000000000000, 0.000000000000000000 ) ) ;
#49670=CARTESIAN_POINT ( 'NONE',  ( 76.07020619028889996, -41.07279695184679724, -13.36374665373399928 ) ) ;
#49672=DIRECTION ( 'NONE',  ( 1.000000000000000000, 0.000000000000000000, 0.000000000000000000 ) ) ;
#49675=CARTESIAN_POINT ( 'NONE',  ( 49.42992454522379830, -53.75819112648869691, -54.94336248455510230 ) ) ;
#49678=CARTESIAN_POINT ( 'NONE',  ( 18.76043506954900053, -51.62277378238609771, -74.57010117178208475 ) ) ;
#49683=ORIENTED_EDGE ( 'NONE', *, *, #45715, .T. ) ;
#49684=CARTESIAN_POINT ( 'NONE',  ( 60.48124862545850533, -45.81154431168629770, -47.72914257570420205 ) ) ;
#49685=FACE_OUTER_BOUND ( 'NONE', #33676, .T. ) ;
#49690=CARTESIAN_POINT ( 'NONE',  ( 40.92586417822920453, -45.44479669594549875, -5.903607078647769235 ) ) ;
#49691=ORIENTED_EDGE ( 'NONE', *, *, #15741, .F. ) ;
#49692=EDGE_CURVE ( 'NONE', #38543, #11477, #30485, .T. ) ;
#49693=ORIENTED_EDGE ( 'NONE', *, *, #28660, .T. ) ;
#49696=EDGE_CURVE ( 'NONE', #30733, #25873, #39878, .T. ) ;
#49700=AXIS2_PLACEMENT_3D ( 'NONE', #12056, #40083, #20150 ) ;
#49702=EDGE_LOOP ( 'NONE', ( #22248, #16571, #4759, #45868, #36312 ) ) ;
#49709=CARTESIAN_POINT ( 'NONE',  ( 52.68970890597619672, -50.62244288377420531, -76.51771729656020682 ) ) ;
#49710=CARTESIAN_POINT ( 'NONE',  ( 47.47987492626153738, -54.61017751298710010, -54.97289024313108285 ) ) ;
#49713=DIRECTION ( 'NONE',  ( 6.891865000000000139E-13, 0.000000000000000000, 1.000000000000000000 ) ) ;
#49715=CARTESIAN_POINT ( 'NONE',  ( 43.46649277351350094, 13.81022299180570023, -6.433241829987640159 ) ) ;
#49717=CARTESIAN_POINT ( 'NONE',  ( 42.78269187991680411, -42.70656023264469781, -3.305184689553219979 ) ) ;
#49718=CARTESIAN_POINT ( 'NONE',  ( 68.13393739769840352, -50.61618894467879670, -73.25000000000220268 ) ) ;
#49722=CARTESIAN_POINT ( 'NONE',  ( 68.03809923644278967, 0.7701806829035969804, -18.68243761347000031 ) ) ;
#49724=CARTESIAN_POINT ( 'NONE',  ( 14.14308403988269980, -52.38392585211880714, -75.82251062550821530 ) ) ;
#49725=CARTESIAN_POINT ( 'NONE',  ( 47.18324198357289845, -54.80726809202429450, -54.61058319554170026 ) ) ;
#49730=CARTESIAN_POINT ( 'NONE',  ( 47.64143405403320486, -54.53488714543879468, -55.14905519569939685 ) ) ;
#49733=CARTESIAN_POINT ( 'NONE',  ( 42.05805489752406601, 13.23020005006048905, -5.167112208590642020 ) ) ;
#49734=CARTESIAN_POINT ( 'NONE',  ( 48.19553001536780101, 23.02471837077230177, -54.91104515267559805 ) ) ;
#49737=ORIENTED_EDGE ( 'NONE', *, *, #41821, .F. ) ;
#49738=DIRECTION ( 'NONE',  ( 0.000000000000000000, 1.000000000000000000, 0.000000000000000000 ) ) ;
#49739=CARTESIAN_POINT ( 'NONE',  ( 83.91174613973400653, 13.57252892771816732, -47.46626505588888989 ) ) ;
#49740=DIRECTION ( 'NONE',  ( -1.000000000000000000, 0.000000000000000000, 0.000000000000000000 ) ) ;
#49741=CARTESIAN_POINT ( 'NONE',  ( 82.66152712818241355, 14.12170720462269990, -47.35223793503389800 ) ) ;
#49742=CARTESIAN_POINT ( 'NONE',  ( 54.18967173931659431, 16.81490735217020216, -26.03594187494229928 ) ) ;
#49746=DIRECTION ( 'NONE',  ( 0.000000000000000000, 0.000000000000000000, -1.000000000000000000 ) ) ;
#49747=CARTESIAN_POINT ( 'NONE',  ( 88.13393739769620083, 1.883811055320649963, -65.65000000000000568 ) ) ;
#49749=VERTEX_POINT ( 'NONE', #27733 ) ;
#49752=CARTESIAN_POINT ( 'NONE',  ( 12.36320305068320025, -64.54682834576858852, -15.76422791927960176 ) ) ;
#49753=CARTESIAN_POINT ( 'NONE',  ( 11.77948378290679976, 33.84506898935639185, -46.26038317283799728 ) ) ;
#49756=CARTESIAN_POINT ( 'NONE',  ( 17.71568204744891517, -51.70197554413384466, -75.56421372420066973 ) ) ;
#49761=CARTESIAN_POINT ( 'NONE',  ( 53.29257619825270353, 18.13512485574420197, -48.87373464042530458 ) ) ;
#49762=CARTESIAN_POINT ( 'NONE',  ( 61.22205614462959744, -2.031833448078650406, -15.94823484607219655 ) ) ;
#49763=CARTESIAN_POINT ( 'NONE',  ( 51.21390658375870686, -49.87096767598450953, -76.33091596763159714 ) ) ;
#49764=CARTESIAN_POINT ( 'NONE',  ( 59.80201330047449915, -46.57845792207670144, -48.51050247853770259 ) ) ;
#49767=CARTESIAN_POINT ( 'NONE',  ( 67.04038824939809160, 19.47158195952189885, -72.59354914830210248 ) ) ;
#49770=DIRECTION ( 'NONE',  ( 0.000000000000000000, -1.000000000000000000, 0.000000000000000000 ) ) ;
#49772=CARTESIAN_POINT ( 'NONE',  ( 13.61938558558030010, -51.42721352468510077, -23.15000001641110217 ) ) ;
#49773=CARTESIAN_POINT ( 'NONE',  ( 57.13444748808839790, 19.38601733984990005, -74.39740555932930022 ) ) ;
#49775=CARTESIAN_POINT ( 'NONE',  ( 47.56768146174049861, -54.56043035528880125, -74.36236381585459299 ) ) ;
#49776=ORIENTED_EDGE ( 'NONE', *, *, #31306, .T. ) ;
#49777=CARTESIAN_POINT ( 'NONE',  ( 54.97172322994220650, 14.66436157010849861, -15.90382766587370256 ) ) ;
#49779=CARTESIAN_POINT ( 'NONE',  ( 56.87954272222179952, -50.36565961963330551, -52.82794281175259954 ) ) ;
#49780=CARTESIAN_POINT ( 'NONE',  ( 53.59080506097220109, -49.40678926383840519, -49.22648751775089693 ) ) ;
#49783=CARTESIAN_POINT ( 'NONE',  ( 47.18687257106159905, 22.80862807082690225, -75.61154398021749046 ) ) ;
#49785=CARTESIAN_POINT ( 'NONE',  ( 60.97391253512203235, -45.68106840025293280, -47.73524043326641220 ) ) ;
#49791=CYLINDRICAL_SURFACE ( 'NONE', #5700, 20.00000000000000355 ) ;
#49793=AXIS2_PLACEMENT_3D ( 'NONE', #6988, #3573, #22941 ) ;
#49794=CARTESIAN_POINT ( 'NONE',  ( 61.28421865660900636, 13.99901274604590107, -46.52379755071130063 ) ) ;
#49796=CARTESIAN_POINT ( 'NONE',  ( -33.86606230032689524, -10.73522994510449990, -57.75543702565100546 ) ) ;
#49798=CARTESIAN_POINT ( 'NONE',  ( 53.06503247311130167, -49.53825076443170161, -48.83676475835459740 ) ) ;
#49802=CARTESIAN_POINT ( 'NONE',  ( 56.12571583893210203, 14.42962552814590005, -25.37490595678350402 ) ) ;
#49805=CARTESIAN_POINT ( 'NONE',  ( 53.51329535014789940, 18.12655912379110035, -49.05665458396899936 ) ) ;
#49807=CARTESIAN_POINT ( 'NONE',  ( 85.84022851002180232, -48.61618894467930119, -53.47585302082339354 ) ) ;
#49808=CARTESIAN_POINT ( 'NONE',  ( 53.29384558423090112, -50.54670888882439783, -28.15000000000000213 ) ) ;
#49809=ORIENTED_EDGE ( 'NONE', *, *, #39829, .T. ) ;
#49812=EDGE_CURVE ( 'NONE', #42606, #11477, #4405, .T. ) ;
#49814=CARTESIAN_POINT ( 'NONE',  ( 47.44876575161689658, -54.61831544581649922, -54.69911453683820213 ) ) ;
#49817=CARTESIAN_POINT ( 'NONE',  ( 11.73422653529650006, -65.42249382734249252, -18.16216258087879964 ) ) ;
#49818=CARTESIAN_POINT ( 'NONE',  ( 52.83011278983949666, 18.42835579809699809, -48.49876830664469907 ) ) ;
#49820=FACE_OUTER_BOUND ( 'NONE', #28533, .T. ) ;
#49827=CARTESIAN_POINT ( 'NONE',  ( 13.99027006115310101, -51.18075678835780451, -22.90513383071120401 ) ) ;
#49828=DIRECTION ( 'NONE',  ( 0.000000000000000000, 0.000000000000000000, -1.000000000000000000 ) ) ;
#49831=CYLINDRICAL_SURFACE ( 'NONE', #26862, 2.999999999999998668 ) ;
#49833=CARTESIAN_POINT ( 'NONE',  ( 53.10748494364860051, 19.23566068709549981, -76.94545507200430734 ) ) ;
#49835=CYLINDRICAL_SURFACE ( 'NONE', #50995, 2.000000000000070610 ) ;
#49842=EDGE_CURVE ( 'NONE', #46792, #9610, #41704, .T. ) ;
#49844=CARTESIAN_POINT ( 'NONE',  ( 57.79488012710090317, -49.04752211200187872, -51.23200826419654419 ) ) ;
#49846=CARTESIAN_POINT ( 'NONE',  ( 52.82359347161860086, -49.70062430464940206, -48.95125679539609820 ) ) ;
#49848=CARTESIAN_POINT ( 'NONE',  ( 13.81167868887400019, 20.68589454807339933, -75.38352342698830455 ) ) ;
#49849=CARTESIAN_POINT ( 'NONE',  ( 17.69924730496158816, -51.74825541295913922, -75.61049359302290895 ) ) ;
#49850=( BOUNDED_CURVE ( )  B_SPLINE_CURVE ( 3, ( #25724, #1385, #17372, #37808 ),
 .UNSPECIFIED., .F., .F. ) 
 B_SPLINE_CURVE_WITH_KNOTS ( ( 4, 4 ),
 ( 6.016222070146150180, 6.100653022355360555 ),
 .UNSPECIFIED. ) 
 CURVE ( )  GEOMETRIC_REPRESENTATION_ITEM ( )  RATIONAL_B_SPLINE_CURVE ( ( 1.000000000000000000, 0.9994060394106761835, 0.9994060394106761835, 1.000000000000000000 ) ) 
 REPRESENTATION_ITEM ( '' )  );
#49851=CARTESIAN_POINT ( 'NONE',  ( 45.63983941734740313, -45.14183948007230640, -7.778235319476010545 ) ) ;
#49857=CARTESIAN_POINT ( 'NONE',  ( 52.66674514831180431, -49.75608620355440337, -27.77093084507739817 ) ) ;
#49858=AXIS2_PLACEMENT_3D ( 'NONE', #7445, #6936, #27092 ) ;
#49859=CARTESIAN_POINT ( 'NONE',  ( 16.29169529782430104, -51.11619123902680428, -21.10106358378050118 ) ) ;
#49860=CARTESIAN_POINT ( 'NONE',  ( 11.66464388782040196, 33.90635028133640105, -16.69887918881750011 ) ) ;
#49863=CARTESIAN_POINT ( 'NONE',  ( 68.88393739769620083, 6.883811055320649963, -71.50000000000000000 ) ) ;
#49865=CARTESIAN_POINT ( 'NONE',  ( -5.660060735539860666, -46.84109022912470266, -5.074035175912159801 ) ) ;
#49866=CARTESIAN_POINT ( 'NONE',  ( 47.55021976886940394, 23.31604569652889936, -54.67535596069880199 ) ) ;
#49867=CARTESIAN_POINT ( 'NONE',  ( 56.04842253387821671, -45.73510956901836977, -25.30965062165876844 ) ) ;
#49869=DIRECTION ( 'NONE',  ( 0.000000000000000000, 0.000000000000000000, -1.000000000000000000 ) ) ;
#49870=CARTESIAN_POINT ( 'NONE',  ( 11.62518889158750035, 33.82940804628189824, -16.65848135030810084 ) ) ;
#49871=CARTESIAN_POINT ( 'NONE',  ( 52.25096257474319827, 18.53891021417129892, -77.19024871130291388 ) ) ;
#49872=DIRECTION ( 'NONE',  ( 1.000000000000000000, 0.000000000000000000, 0.000000000000000000 ) ) ;
#49875=CARTESIAN_POINT ( 'NONE',  ( 54.79203463286849995, 20.14039653249960082, -53.38038282636030374 ) ) ;
#49879=CARTESIAN_POINT ( 'NONE',  ( 20.04766857768572308, 23.93603348987157631, -19.07533074137708695 ) ) ;
#49880=CARTESIAN_POINT ( 'NONE',  ( 11.10565272881359888, 32.16441030637599852, -44.25626093647380088 ) ) ;
#49882=CARTESIAN_POINT ( 'NONE',  ( 66.28212128162849126, -33.07507224467300233, -19.91085132854729878 ) ) ;
#49886=CARTESIAN_POINT ( 'NONE',  ( 18.78671181058629713, 20.36471648394369893, -74.34810712130391153 ) ) ;
#49890=CARTESIAN_POINT ( 'NONE',  ( 76.73335235168207191, 7.326484823470851282, -14.23296824953687256 ) ) ;
#49892=CARTESIAN_POINT ( 'NONE',  ( 11.09888617399270139, -63.65665293880989850, -44.37975584975329468 ) ) ;
#49893=CARTESIAN_POINT ( 'NONE',  ( 57.09481130578469532, -45.80449631822029488, -26.22977073655889768 ) ) ;
#49899=CARTESIAN_POINT ( 'NONE',  ( 51.49217680742329861, -45.11618894460779927, -11.64292740565939965 ) ) ;
#49902=CARTESIAN_POINT ( 'NONE',  ( 16.36414204282080220, 19.86444509156779858, -20.27640028196680078 ) ) ;
#49906=CARTESIAN_POINT ( 'NONE',  ( 47.16774318698460178, -54.71371846786210114, -74.72677413543641478 ) ) ;
#49907=CARTESIAN_POINT ( 'NONE',  ( 43.38948054135340016, 13.16722536039579872, -5.306502943738020228 ) ) ;
#49909=AXIS2_PLACEMENT_3D ( 'NONE', #8267, #24218, #11699 ) ;
#49911=CARTESIAN_POINT ( 'NONE',  ( 50.97250237377529913, 19.73188199481569782, -76.14992204905399831 ) ) ;
#49912=CARTESIAN_POINT ( 'NONE',  ( 57.61853615479979851, 14.19444255287990053, -26.09622215295719982 ) ) ;
#49916=AXIS2_PLACEMENT_3D ( 'NONE', #12291, #31406, #28252 ) ;
#49917=FACE_OUTER_BOUND ( 'NONE', #5405, .T. ) ;
#49919=CARTESIAN_POINT ( 'NONE',  ( -10.77672099032110076, -41.59961327471660297, -4.617929491435150524 ) ) ;
#49921=B_SPLINE_CURVE_WITH_KNOTS ( 'NONE', 3,
 ( #4845, #41007, #1435, #17421, #28417, #20812 ),
 .UNSPECIFIED., .F., .F.,
 ( 4, 2, 4 ),
 ( 0.4974519944936803828, 0.7487259972468401914, 1.000000000000000000 ),
 .UNSPECIFIED. ) ;
#49924=LINE ( 'NONE', #38653, #7254 ) ;
#49927=CARTESIAN_POINT ( 'NONE',  ( 41.46604563068979843, 12.80054222763110161, -4.103344234634350052 ) ) ;
#49929=CARTESIAN_POINT ( 'NONE',  ( 19.69385247111841153, 24.22507436623365606, -75.39120620925201877 ) ) ;
#49930=AXIS2_PLACEMENT_3D ( 'NONE', #30684, #46707, #11567 ) ;
#49932=CARTESIAN_POINT ( 'NONE',  ( 75.97210306049274209, -43.32603839517573618, -13.61663700222281115 ) ) ;
#49933=CARTESIAN_POINT ( 'NONE',  ( 57.39341912848639993, 13.88381105532070059, -16.95659913784360029 ) ) ;
#49935=ADVANCED_FACE ( 'NONE', ( #45799 ), #31876, .T. ) ;
#49948=ORIENTED_EDGE ( 'NONE', *, *, #22165, .T. ) ;
#49952=CARTESIAN_POINT ( 'NONE',  ( 61.23124000452309446, -45.25914701332289525, -46.66814466197200062 ) ) ;
#49956=VERTEX_POINT ( 'NONE', #46583 ) ;
#49960=CARTESIAN_POINT ( 'NONE',  ( 17.92370450339669929, -51.11618894467930119, -74.14999999999999147 ) ) ;
#49963=CARTESIAN_POINT ( 'NONE',  ( 52.19766841848610284, -50.16895301260710482, -76.74438382457309160 ) ) ;
#49964=CARTESIAN_POINT ( 'NONE',  ( 60.62574835426579511, 14.40422389669799941, -47.47763332278800164 ) ) ;
#49968=CARTESIAN_POINT ( 'NONE',  ( 41.12781764322979683, 13.68286643970050065, -5.505755319031189643 ) ) ;
#49969=CARTESIAN_POINT ( 'NONE',  ( 41.35854777540759386, -44.05358766536809867, -3.852418435177789924 ) ) ;
#49971=CARTESIAN_POINT ( 'NONE',  ( -4.967261132674519963, 16.44508974743529706, -5.583919853821729617 ) ) ;
#49974=EDGE_LOOP ( 'NONE', ( #21042, #855, #4836, #24911 ) ) ;
#49975=CARTESIAN_POINT ( 'NONE',  ( 14.80537258320890004, -52.82751997460400162, -76.12812327221449493 ) ) ;
#49977=CARTESIAN_POINT ( 'NONE',  ( 57.33486091049710609, 19.16628497504979833, -53.00729108527669808 ) ) ;
#49978=EDGE_CURVE ( 'NONE', #9812, #30733, #6135, .T. ) ;
#49979=CARTESIAN_POINT ( 'NONE',  ( 9.188454688893768818, 32.78433166890278727, -46.76666145959791265 ) ) ;
#49981=CARTESIAN_POINT ( 'NONE',  ( 47.14844574785740150, -54.72867718618289956, -74.72768729699521373 ) ) ;
#49983=CARTESIAN_POINT ( 'NONE',  ( 48.21897519948650057, -54.20455510793630083, -54.75400547047010491 ) ) ;
#49984=DIRECTION ( 'NONE',  ( 0.9741140340359945027, 0.000000000000000000, 0.2260571801428156169 ) ) ;
#49986=CARTESIAN_POINT ( 'NONE',  ( 47.94507101407240413, 23.10143656816769919, -54.74296229181740614 ) ) ;
#49989=ORIENTED_EDGE ( 'NONE', *, *, #50060, .T. ) ;
#49990=B_SPLINE_SURFACE_WITH_KNOTS ( 'NONE', 3, 3, ( 
 ( #16832, #40932, #12915, #19968, #12646, #48287, #325, #40163, #44348, #8455 ),
 ( #24402, #4776, #44095, #39911, #8195, #28871, #20228, #28605, #21006, #1100 ),
 ( #40416, #5047, #36730, #17099, #48808, #12382, #24138, #44872, #33051, #35965 ),
 ( #4509, #838, #48035, #36216, #20479, #49077, #32514, #16310, #28342, #29131 ) ),
 .UNSPECIFIED., .F., .F., .F.,
 ( 4, 4 ),
 ( 4, 1, 1, 1, 1, 1, 1, 4 ),
 ( -1.508899358212140163, -1.485879941667409998 ),
 ( -1.180912899999999983E-08, 0.1428571428571430157, 0.2857142857142860315, 0.4285714285714289917, 0.5714285714285709528, 0.7142857142857139685, 0.8571428571428569843, 1.000000000000000000 ),
 .UNSPECIFIED. ) ;
#49993=FACE_OUTER_BOUND ( 'NONE', #27563, .T. ) ;
#49995=CARTESIAN_POINT ( 'NONE',  ( 83.01976156432699838, 14.15119948029169983, -47.45812318453789658 ) ) ;
#49996=CARTESIAN_POINT ( 'NONE',  ( 52.92421614290409337, 18.24372338732509746, -27.16729016564240240 ) ) ;
#49999=CARTESIAN_POINT ( 'NONE',  ( 55.68773921495960622, -45.11618894467940066, -14.55197505337829966 ) ) ;
#50000=EDGE_CURVE ( 'NONE', #49749, #38938, #14335, .T. ) ;
#50006=CARTESIAN_POINT ( 'NONE',  ( 12.28024544113980099, -64.62291823860830675, -15.84304030210369874 ) ) ;
#50009=CARTESIAN_POINT ( 'NONE',  ( 9.758904647714020442, -64.50914077245040801, -46.91371261844790297 ) ) ;
#50014=CARTESIAN_POINT ( 'NONE',  ( 53.57971248429669942, 18.11494520363680039, -49.11439736689410296 ) ) ;
#50015=CARTESIAN_POINT ( 'NONE',  ( 64.37314994972929583, -0.8120157797042090175, -16.48846350816869943 ) ) ;
#50016=CARTESIAN_POINT ( 'NONE',  ( 51.81521015446659817, -50.18342081774120089, -76.50775191966720001 ) ) ;
#50017=CARTESIAN_POINT ( 'NONE',  ( 57.10526040051080088, -50.46725872370470256, -52.98753066802770206 ) ) ;
#50021=ORIENTED_EDGE ( 'NONE', *, *, #17254, .T. ) ;
#50025=CARTESIAN_POINT ( 'NONE',  ( 13.77851400210420074, -50.96568734215840379, -21.81884038058960229 ) ) ;
#50026=CARTESIAN_POINT ( 'NONE',  ( 56.90585954735670526, 19.41242710917140002, -74.35847077477819767 ) ) ;
#50027=CARTESIAN_POINT ( 'NONE',  ( 47.42016093597910498, -54.35903067314299619, -75.11917674890220553 ) ) ;
#50029=CARTESIAN_POINT ( 'NONE',  ( 55.70104770110099679, 14.66019162433090095, -16.90779946243160126 ) ) ;
#50034=CARTESIAN_POINT ( 'NONE',  ( 22.41796512503769989, 0.7774003680457489684, -74.14999999999999147 ) ) ;
#50036=CARTESIAN_POINT ( 'NONE',  ( 46.40063036093010140, 21.74762169565689973, -76.14870948285189911 ) ) ;
#50037=EDGE_CURVE ( 'NONE', #33088, #4775, #51851, .T. ) ;
#50039=CARTESIAN_POINT ( 'NONE',  ( 61.22429803220455824, -45.61587231938426612, -47.69140452323649271 ) ) ;
#50041=CARTESIAN_POINT ( 'NONE',  ( 50.95182575631829991, -50.95090194773979420, -78.14999999999999147 ) ) ;
#50043=CARTESIAN_POINT ( 'NONE',  ( 82.75628319263068988, 14.36882076953894050, -47.67910150642000389 ) ) ;
#50048=CARTESIAN_POINT ( 'NONE',  ( -29.90810223010410240, 4.891254745981789220, -56.68161292995529976 ) ) ;
#50049=ORIENTED_EDGE ( 'NONE', *, *, #3071, .F. ) ;
#50050=CARTESIAN_POINT ( 'NONE',  ( 52.97367367441350439, -49.59674172301600237, -48.91755411389170405 ) ) ;
#50054=CARTESIAN_POINT ( 'NONE',  ( 53.70552627772385534, -51.31509389902640095, -75.56421117895261830 ) ) ;
#50055=CARTESIAN_POINT ( 'NONE',  ( 57.44728655615209334, 13.96276471381350071, -25.73862226050399826 ) ) ;
#50057=CARTESIAN_POINT ( 'NONE',  ( 50.61163702139570120, 19.09625748281729685, -76.14999999999999147 ) ) ;
#50058=CARTESIAN_POINT ( 'NONE',  ( 53.34806562330150115, 18.23528164705630061, -49.15545160539839742 ) ) ;
#50060=EDGE_CURVE ( 'NONE', #19900, #49606, #27675, .T. ) ;
#50061=FACE_OUTER_BOUND ( 'NONE', #41178, .T. ) ;
#50065=CARTESIAN_POINT ( 'NONE',  ( 53.29384558423090112, -50.54670888882439783, -48.47378032971909789 ) ) ;
#50068=CARTESIAN_POINT ( 'NONE',  ( 11.73319001777059967, -65.42240559785089715, -18.17421237902190256 ) ) ;
#50069=CARTESIAN_POINT ( 'NONE',  ( 52.86023839377149613, 18.41257215013510162, -48.64479331233690829 ) ) ;
#50076=CARTESIAN_POINT ( 'NONE',  ( 9.735166606402680500, -63.19548571361389833, -46.29854363928350125 ) ) ;
#50078=ORIENTED_EDGE ( 'NONE', *, *, #518, .F. ) ;
#50080=CARTESIAN_POINT ( 'NONE',  ( 57.25486274975099832, 19.18878419988909911, -53.00955584377039287 ) ) ;
#50082=CARTESIAN_POINT ( 'NONE',  ( 53.44459215460110357, 19.29420487410069995, -77.05819720518759652 ) ) ;
#50083=VERTEX_POINT ( 'NONE', #36296 ) ;
#50091=EDGE_LOOP ( 'NONE', ( #35862, #15181, #46712, #15562, #27422, #7025, #12563, #37175, #2236 ) ) ;
#50092=CARTESIAN_POINT ( 'NONE',  ( 56.90686501081929549, -45.95685669975489418, -26.24565630313109921 ) ) ;
#50094=CARTESIAN_POINT ( 'NONE',  ( 53.41295794315580281, -49.45825314767390068, -49.19565172947730503 ) ) ;
#50097=CARTESIAN_POINT ( 'NONE',  ( 13.48116775261750000, 20.36472114263469990, -74.14993923597720027 ) ) ;
#50101=ADVANCED_FACE ( 'NONE', ( #28172 ), #9307, .F. ) ;
#50102=CARTESIAN_POINT ( 'NONE',  ( 45.96729298043059941, -45.11618877348409740, -7.679810998475620210 ) ) ;
#50107=CIRCLE ( 'NONE', #45922, 20.00000000000000355 ) ;
#50109=CARTESIAN_POINT ( 'NONE',  ( 52.66238559624279958, -49.77034287296790183, -28.15000000000000213 ) ) ;
#50110=CARTESIAN_POINT ( 'NONE',  ( 54.51194644580689896, -51.02658531394220631, -75.53932869989588994 ) ) ;
#50111=CARTESIAN_POINT ( 'NONE',  ( 2.523152121134959902, 24.51152417802100203, -9.568711433707859371 ) ) ;
#50114=FACE_OUTER_BOUND ( 'NONE', #8277, .T. ) ;
#50117=CARTESIAN_POINT ( 'NONE',  ( 47.45089865496730397, 23.39580635657319974, -54.92520380177580108 ) ) ;
#50119=CARTESIAN_POINT ( 'NONE',  ( 84.44784216359251161, -43.11618894467930119, -47.47585302082339354 ) ) ;
#50120=CARTESIAN_POINT ( 'NONE',  ( 16.13393739769620083, -15.61618894467929941, 7.849999999999999645 ) ) ;
#50121=CARTESIAN_POINT ( 'NONE',  ( 11.51020347527180121, 33.95873866478400060, -17.03655015074090073 ) ) ;
#50122=CARTESIAN_POINT ( 'NONE',  ( 51.63018455917120519, 17.53790506105039881, -76.93968096218729613 ) ) ;
#50124=FACE_OUTER_BOUND ( 'NONE', #50718, .T. ) ;
#50125=CARTESIAN_POINT ( 'NONE',  ( 57.24929578232330130, -50.61618894764249887, -53.91492796143979405 ) ) ;
#50126=CARTESIAN_POINT ( 'NONE',  ( 54.58029846603599822, 16.81705030249620236, -26.70560246487150025 ) ) ;
#50127=CARTESIAN_POINT ( 'NONE',  ( 53.69314142483850105, 20.72471266374249765, -54.13035041278149606 ) ) ;
#50130=CARTESIAN_POINT ( 'NONE',  ( 12.16177399482889854, -65.11171494345551025, -16.53048058985559976 ) ) ;
#50133=CARTESIAN_POINT ( 'NONE',  ( 10.98008937475129976, 32.20858435228970507, -44.74889856825390666 ) ) ;
#50134=DIRECTION ( 'NONE',  ( 0.000000000000000000, -1.000000000000000000, 0.000000000000000000 ) ) ;
#50135=CARTESIAN_POINT ( 'NONE',  ( 66.86287292282169403, -33.02813482287280067, -19.74633365862219847 ) ) ;
#50138=ORIENTED_EDGE ( 'NONE', *, *, #30748, .T. ) ;
#50139=DIRECTION ( 'NONE',  ( 0.8857883891771971552, 0.4640893551880569956, 0.000000000000000000 ) ) ;
#50140=CARTESIAN_POINT ( 'NONE',  ( 76.52646094036225577, -1.396720341220584194, -13.34144236586088184 ) ) ;
#50141=ORIENTED_EDGE ( 'NONE', *, *, #35145, .F. ) ;
#50142=CARTESIAN_POINT ( 'NONE',  ( 11.45649489523620090, -64.61824938533239049, -44.81425297044399514 ) ) ;
#50143=CARTESIAN_POINT ( 'NONE',  ( 57.45125141795639934, -45.60879174519349988, -26.20535967303949931 ) ) ;
#50146=VERTEX_POINT ( 'NONE', #8018 ) ;
#50148=AXIS2_PLACEMENT_3D ( 'NONE', #22293, #17860, #13435 ) ;
#50154=CARTESIAN_POINT ( 'NONE',  ( 47.86554978023400508, -45.20111752495729718, -9.670171237329979519 ) ) ;
#50156=CARTESIAN_POINT ( 'NONE',  ( 16.29169529782900128, 19.88381334967050051, -21.10106358377919733 ) ) ;
#50157=LINE ( 'NONE', #5873, #12581 ) ;
#50161=CARTESIAN_POINT ( 'NONE',  ( 46.54186286179869825, -53.33175941191459657, -76.10201724918678678 ) ) ;
#50162=CARTESIAN_POINT ( 'NONE',  ( 43.10178961967590539, 13.88381303978850134, -6.597083906273729426 ) ) ;
#50163=CARTESIAN_POINT ( 'NONE',  ( 52.88720174400599916, 13.88381105532070059, -12.35033059861759952 ) ) ;
#50166=EDGE_CURVE ( 'NONE', #12686, #35762, #46145, .T. ) ;
#50167=CARTESIAN_POINT ( 'NONE',  ( 53.09964054308650105, 20.18306253101129855, -75.69942035651190793 ) ) ;
#50168=CARTESIAN_POINT ( 'NONE',  ( 58.00476136467050026, 13.88377196530409918, -25.49213187376239986 ) ) ;
#50171=ORIENTED_EDGE ( 'NONE', *, *, #40471, .F. ) ;
#50173=CARTESIAN_POINT ( 'NONE',  ( -0.2744351088561370333, -53.43781633194900138, -9.661156741874108889 ) ) ;
#50176=FACE_OUTER_BOUND ( 'NONE', #30834, .T. ) ;
#50178=AXIS2_PLACEMENT_3D ( 'NONE', #26552, #22620, #13751 ) ;
#50182=CARTESIAN_POINT ( 'NONE',  ( 13.52985239415419905, 18.98897015258729937, -21.01296976105329861 ) ) ;
#50183=CARTESIAN_POINT ( 'NONE',  ( 11.51160566532330165, 19.89559162839070083, -23.15000000000000213 ) ) ;
#50185=CARTESIAN_POINT ( 'NONE',  ( 43.12694253603230266, 11.52171575524780067, -4.223455518406679765 ) ) ;
#50186=CARTESIAN_POINT ( 'NONE',  ( 47.26610112325450075, -54.05804861832230301, -75.56421356201970241 ) ) ;
#50189=CARTESIAN_POINT ( 'NONE',  ( 75.82340458658627824, -43.34274047612557013, -13.53568841794259825 ) ) ;
#50191=ADVANCED_FACE ( 'NONE', ( #44434 ), #45479, .F. ) ;
#50192=ORIENTED_EDGE ( 'NONE', *, *, #2134, .T. ) ;
#50196=CARTESIAN_POINT ( 'NONE',  ( 5.772828151193539981, 28.52800643874740061, -13.89629191288699950 ) ) ;
#50197=DIRECTION ( 'NONE',  ( 1.000000000000000000, 0.000000000000000000, 0.000000000000000000 ) ) ;
#50198=CARTESIAN_POINT ( 'NONE',  ( 16.13393739769620083, -15.61618894467929941, 8.349999999999999645 ) ) ;
#50202=CARTESIAN_POINT ( 'NONE',  ( 45.07859124156069441, -46.11251916928470251, -9.026881350141310989 ) ) ;
#50207=CARTESIAN_POINT ( 'NONE',  ( 61.26666816648369718, -45.24236673898500527, -46.69299359672859850 ) ) ;
#50208=CARTESIAN_POINT ( 'NONE',  ( 82.74184831039019627, -45.55978498551615274, -47.63392295364009499 ) ) ;
#50211=EDGE_LOOP ( 'NONE', ( #22722, #4244, #7080, #28098 ) ) ;
#50213=EDGE_CURVE ( 'NONE', #20534, #30077, #6785, .T. ) ;
#50217=AXIS2_PLACEMENT_3D ( 'NONE', #36797, #36023, #16110 ) ;
#50220=CARTESIAN_POINT ( 'NONE',  ( 53.10073094383309211, -50.72614047099949630, -76.45474612258288971 ) ) ;
#50222=CARTESIAN_POINT ( 'NONE',  ( 60.52368085848160462, 14.45009813934579945, -47.49050240135510137 ) ) ;
#50225=CARTESIAN_POINT ( 'NONE',  ( 85.66799001034409855, 17.38381105532069881, -61.58097075742929860 ) ) ;
#50226=CARTESIAN_POINT ( 'NONE',  ( 41.35841886795890332, 13.63164803163950012, -5.517442860631740054 ) ) ;
#50228=CARTESIAN_POINT ( 'NONE',  ( 41.57451192618589886, -43.86192582434640030, -3.761783080649049982 ) ) ;
#50229=CARTESIAN_POINT ( 'NONE',  ( 65.30823784209736971, -0.2426529040835342932, -16.78605341132611883 ) ) ;
#50230=CARTESIAN_POINT ( 'NONE',  ( 65.03603135454920903, 1.015437840524759938, -17.83403478221330118 ) ) ;
#50231=ADVANCED_FACE ( 'NONE', ( #14798 ), #30764, .T. ) ;
#50238=CARTESIAN_POINT ( 'NONE',  ( 57.36367400179620546, 19.00004687350629951, -52.73881526266769271 ) ) ;
#50243=CARTESIAN_POINT ( 'NONE',  ( 48.31044912363459787, -54.24991223489359982, -55.31379430672990338 ) ) ;
#50245=CARTESIAN_POINT ( 'NONE',  ( -11.32734370190460105, -41.88171845330919751, -6.430192534648670133 ) ) ;
#50247=CARTESIAN_POINT ( 'NONE',  ( 47.77526208095149940, 23.24550361938769782, -55.21131733320120105 ) ) ;
#50256=CARTESIAN_POINT ( 'NONE',  ( 14.27688361489088464, 19.15751927551417211, -20.83437801695187019 ) ) ;
#50257=CARTESIAN_POINT ( 'NONE',  ( 84.05638291250180316, 13.23271651793530168, -47.35165316785450074 ) ) ;
#50258=CARTESIAN_POINT ( 'NONE',  ( 52.84013465215829797, 18.33475784595760061, -27.28929192048029861 ) ) ;
#50259=AXIS2_PLACEMENT_3D ( 'NONE', #14501, #26802, #42031 ) ;
#50265=B_SPLINE_SURFACE_WITH_KNOTS ( 'NONE', 3, 3, ( 
 ( #28377, #8486, #48581, #12682, #45425, #9272 ),
 ( #38075, #42010, #49364, #6109, #17891, #17383 ),
 ( #45943, #45681, #37296, #10297, #22065, #49624 ),
 ( #2172, #21034, #13718, #49875, #18151, #10032 ),
 ( #25999, #17128, #34117, #17644, #25477, #41481 ),
 ( #5596, #50127, #13465, #21551, #33081, #14223 ),
 ( #29672, #30196, #46213, #49110, #40961, #33348 ),
 ( #5079, #29925, #29420, #21812, #37035, #1132 ),
 ( #37547, #33610, #25220, #13209, #29159, #9529 ),
 ( #5339, #9782, #45157, #41224, #21291, #1394 ),
 ( #1652, #25734, #41741, #5847, #37819, #1912 ),
 ( #33864, #13970, #38332, #7397, #43048, #46992 ),
 ( #35420, #30450, #34903, #47242, #23345, #3469 ),
 ( #31215, #18664, #22326, #50393, #30710, #46473 ),
 ( #7145, #15516, #42267, #10559, #35159, #39367 ),
 ( #22838, #19180, #46732, #23097, #11077, #34381 ) ),
 .UNSPECIFIED., .F., .F., .F.,
 ( 4, 2, 2, 2, 2, 2, 2, 4 ),
 ( 4, 1, 1, 4 ),
 ( 0.1345845834583700162, 1.324410793755629978, 2.838023129476340056, 3.784030839301789850, 4.257034694214520520, 5.013840862074870230, 6.224730730651439892, 7.568061678603579701 ),
 ( 0.000000000000000000, 0.3333333333333329818, 0.6666666666666670737, 1.000000000000000000 ),
 .UNSPECIFIED. ) ;
#50269=ORIENTED_EDGE ( 'NONE', *, *, #25134, .F. ) ;
#50273=CARTESIAN_POINT ( 'NONE',  ( 50.96089686506987704, 4.058150859599502169, -76.37981214989946466 ) ) ;
#50274=ORIENTED_EDGE ( 'NONE', *, *, #15850, .F. ) ;
#50275=EDGE_CURVE ( 'NONE', #26913, #13640, #9834, .T. ) ;
#50278=CARTESIAN_POINT ( 'NONE',  ( 57.00663126403959780, 14.67647015083939976, -26.24686370817770253 ) ) ;
#50281=CARTESIAN_POINT ( 'NONE',  ( 63.56762109228700552, -1.686163729233590036, -16.28338591870409857 ) ) ;
#50282=CARTESIAN_POINT ( 'NONE',  ( 51.59929363246539680, -50.34116866607159579, -76.34973346688259710 ) ) ;
#50284=CARTESIAN_POINT ( 'NONE',  ( 57.04794059879459667, -50.06337071255109805, -52.46643742010060407 ) ) ;
#50285=ORIENTED_EDGE ( 'NONE', *, *, #17029, .F. ) ;
#50287=CARTESIAN_POINT ( 'NONE',  ( 70.83393739769690001, 16.88381105531960458, -68.79999999999942872 ) ) ;
#50292=CARTESIAN_POINT ( 'NONE',  ( 13.45430947954159961, -50.82897305452650016, -21.59563960679350103 ) ) ;
#50293=CARTESIAN_POINT ( 'NONE',  ( 56.61615004124559647, 19.47122561338359858, -74.49138732573949540 ) ) ;
#50294=CARTESIAN_POINT ( 'NONE',  ( 47.55554092369170149, -54.54384586952379976, -74.50311761397450994 ) ) ;
#50295=CARTESIAN_POINT ( 'NONE',  ( 56.96371428459909936, 13.94730734397229988, -17.49295389172720050 ) ) ;
#50297=CARTESIAN_POINT ( 'NONE',  ( 56.41694091142689871, -50.57803607321029915, -52.96189704198110348 ) ) ;
#50301=AXIS2_PLACEMENT_3D ( 'NONE', #8625, #21174, #8886 ) ;
#50304=CARTESIAN_POINT ( 'NONE',  ( 47.04893601651119894, 22.57350237217389832, -75.82551461053719777 ) ) ;
#50306=CARTESIAN_POINT ( 'NONE',  ( 75.16029866046824282, -29.42847402270892232, -11.84778187433581387 ) ) ;
#50308=CARTESIAN_POINT ( 'NONE',  ( 54.17308944977700236, 19.38381105532069881, -77.01198594365929750 ) ) ;
#50315=CARTESIAN_POINT ( 'NONE',  ( -31.60239111126589862, -6.246724563331800262, -55.64697389277930029 ) ) ;
#50317=CARTESIAN_POINT ( 'NONE',  ( 52.71274985523909606, -49.73402172576329860, -48.58383670079809491 ) ) ;
#50321=CARTESIAN_POINT ( 'NONE',  ( 13.76823759339399977, 19.89277676745740209, -22.18388608259699879 ) ) ;
#50322=CARTESIAN_POINT ( 'NONE',  ( 56.12094024660369485, 14.43398220991280034, -25.30520633357740223 ) ) ;
#50325=CARTESIAN_POINT ( 'NONE',  ( 52.98400444558360078, 18.37466557939660206, -48.99793963464180280 ) ) ;
#50326=CARTESIAN_POINT ( 'NONE',  ( 55.79023370591369968, -45.75302572798440082, -16.82963326627560363 ) ) ;
#50327=DIRECTION ( 'NONE',  ( -0.3294064756442134922, -0.9441882088882800339, 8.551492847173810438E-14 ) ) ;
#50328=ORIENTED_EDGE ( 'NONE', *, *, #40875, .F. ) ;
#50333=CARTESIAN_POINT ( 'NONE',  ( 11.89321892218999999, -65.43602743108449715, -18.16392793341869805 ) ) ;
#50334=CARTESIAN_POINT ( 'NONE',  ( 52.77399506770057513, -49.72485891806022096, -48.90117834109282313 ) ) ;
#50338=VECTOR ( 'NONE', #23750, 1000.000000000000000 ) ;
#50340=ORIENTED_EDGE ( 'NONE', *, *, #6498, .F. ) ;
#50342=EDGE_LOOP ( 'NONE', ( #48655, #18497, #36829, #25983 ) ) ;
#50343=CARTESIAN_POINT ( 'NONE',  ( 10.77427761093600012, -63.38637133307939564, -45.20767421870360181 ) ) ;
#50344=ADVANCED_FACE ( 'NONE', ( #43107 ), #46248, .T. ) ;
#50345=DIRECTION ( 'NONE',  ( 0.1414213562373085320, 0.000000000000000000, 0.9899494936611666907 ) ) ;
#50346=ORIENTED_EDGE ( 'NONE', *, *, #45381, .T. ) ;
#50348=CARTESIAN_POINT ( 'NONE',  ( 57.26071802442650238, 19.38379676217989811, -53.75790974344070605 ) ) ;
#50349=CARTESIAN_POINT ( 'NONE',  ( 52.69947341743939973, 19.21175676992940140, -76.74590226668858861 ) ) ;
#50358=ORIENTED_EDGE ( 'NONE', *, *, #35532, .T. ) ;
#50359=CARTESIAN_POINT ( 'NONE',  ( 57.15880063199809769, -45.85422939174420520, -26.25419981771649702 ) ) ;
#50361=CARTESIAN_POINT ( 'NONE',  ( 52.95065152567730138, -49.64318942350850250, -49.05053742289099716 ) ) ;
#50363=EDGE_CURVE ( 'NONE', #5918, #51131, #37401, .T. ) ;
#50364=FACE_OUTER_BOUND ( 'NONE', #9406, .T. ) ;
#50366=CARTESIAN_POINT ( 'NONE',  ( 14.32606013829879998, 20.01251569944690090, -74.87640169473949925 ) ) ;
#50367=CARTESIAN_POINT ( 'NONE',  ( 17.34548134648386863, -52.74445246667860232, -76.12392058103051795 ) ) ;
#50369=CARTESIAN_POINT ( 'NONE',  ( 40.99540311694470063, -44.99959555961480362, -5.546226915801610424 ) ) ;
#50374=EDGE_LOOP ( 'NONE', ( #50622, #48385 ) ) ;
#50375=CARTESIAN_POINT ( 'NONE',  ( 53.10609841537830533, -49.27737300328959691, -26.94345523169370082 ) ) ;
#50376=CARTESIAN_POINT ( 'NONE',  ( 56.72469771552999873, -50.67197071006459907, -74.53479304648951143 ) ) ;
#50377=CARTESIAN_POINT ( 'NONE',  ( 3.241158669444910156, 25.60760945040669867, -10.70730181694110072 ) ) ;
#50379=DIRECTION ( 'NONE',  ( 0.000000000000000000, -3.399867999999999948E-10, 1.000000000000000000 ) ) ;
#50380=CARTESIAN_POINT ( 'NONE',  ( 48.43113447640888580, 22.58636222950222816, -53.38348114488076845 ) ) ;
#50381=EDGE_LOOP ( 'NONE', ( #43898, #31589, #36988, #41438 ) ) ;
#50383=CARTESIAN_POINT ( 'NONE',  ( 47.49124202022650110, 23.36933501918910494, -54.82949043996080007 ) ) ;
#50386=CARTESIAN_POINT ( 'NONE',  ( 56.70490786469932942, 14.04930731085842233, -25.29390771195738807 ) ) ;
#50387=CARTESIAN_POINT ( 'NONE',  ( 11.37461205174560064, 33.83526575001669556, -16.88571183838750045 ) ) ;
#50388=CARTESIAN_POINT ( 'NONE',  ( 51.70989473322139673, 17.69254021111469655, -77.02394377317959595 ) ) ;
#50389=CARTESIAN_POINT ( 'NONE',  ( 53.36907892687840160, 18.14597633810089761, -48.78904877098699444 ) ) ;
#50392=CARTESIAN_POINT ( 'NONE',  ( 52.77196772020159443, 18.44163949243500156, -27.80225394247760207 ) ) ;
#50393=CARTESIAN_POINT ( 'NONE',  ( 50.34648245260830635, 22.03267857139280039, -54.24922544986609552 ) ) ;
#50395=CARTESIAN_POINT ( 'NONE',  ( 52.62851231361270266, 18.57686390552120059, -48.67161502741990375 ) ) ;
#50396=CARTESIAN_POINT ( 'NONE',  ( 58.33770897141780409, -45.11618894467940066, -10.68148127205489928 ) ) ;
#50398=CARTESIAN_POINT ( 'NONE',  ( 10.97829214564769984, 31.96174209507660180, -44.74190632825920488 ) ) ;
#50400=CYLINDRICAL_SURFACE ( 'NONE', #16766, 1.999999999999997113 ) ;
#50401=CARTESIAN_POINT ( 'NONE',  ( 18.50685669558849966, 20.06273926763419979, -74.14993629405250886 ) ) ;
#50403=ORIENTED_EDGE ( 'NONE', *, *, #13135, .F. ) ;
#50404=DIRECTION ( 'NONE',  ( 3.251616519950084978E-22, -1.000000000000000000, 1.784227544494129940E-11 ) ) ;
#50405=EDGE_CURVE ( 'NONE', #814, #51345, #42508, .T. ) ;
#50406=CARTESIAN_POINT ( 'NONE',  ( 50.31290364262088843, -0.9070165658829743016, -16.15042132747201364 ) ) ;
#50408=CARTESIAN_POINT ( 'NONE',  ( 12.58828388404580068, -65.45077111865299457, -46.93561936501430409 ) ) ;
#50409=CARTESIAN_POINT ( 'NONE',  ( 56.19278121266829373, -45.59700403742969144, -25.37063597392850056 ) ) ;
#50412=B_SPLINE_CURVE_WITH_KNOTS ( 'NONE', 3,
 ( #8341, #4406, #4661, #994, #24552, #20633, #41089, #36621, #44761, #24817, #46063, #49733, #18006, #49484, #26365, #22437 ),
 .UNSPECIFIED., .F., .F.,
 ( 4, 2, 2, 2, 2, 2, 2, 4 ),
 ( 0.000000000000000000, 0.1750000000000000444, 0.3750000000000012768, 0.5000000000000000000, 0.5625000000000006661, 0.6600291104134125009, 0.8160756870748754332, 1.000000000000000000 ),
 .UNSPECIFIED. ) ;
#50413=CARTESIAN_POINT ( 'NONE',  ( 13.51895031977020523, -51.88237913636656629, -74.91995119715397777 ) ) ;
#50415=AXIS2_PLACEMENT_3D ( 'NONE', #35711, #31493, #39137 ) ;
#50421=CARTESIAN_POINT ( 'NONE',  ( 14.59756433006669951, 19.88381105111769642, -22.39374700643550042 ) ) ;
#50425=CARTESIAN_POINT ( 'NONE',  ( 47.31501038023650096, -54.57921746145999720, -74.80639350504939955 ) ) ;
#50426=CARTESIAN_POINT ( 'NONE',  ( 41.58069270221000124, 12.33221690508110058, -4.585379893427648845 ) ) ;
#50428=CARTESIAN_POINT ( 'NONE',  ( 53.17432493994039788, 20.66509266784749954, -53.32388713517680401 ) ) ;
#50429=B_SPLINE_SURFACE_WITH_KNOTS ( 'NONE', 3, 3, ( 
 ( #35126, #15486, #15230, #31181, #47212, #27261, #41069, #49205, #33186, #17478, #37138, #13297, #1235, #45263, #29002, #28739 ),
 ( #45521, #33445, #29517, #40547, #9371, #49464, #5179, #25317, #37646, #13553, #41320, #25571, #9617, #24531, #21134, #36601 ),
 ( #16697, #12781, #5434, #20878, #44739, #20610, #21388, #37393, #41577, #1495, #5689, #21639, #36872, #17225, #12514, #16439 ),
 ( #4636, #24794, #705, #971, #32392, #48412, #8842, #28480, #32651, #48678, #16972, #44477, #40801, #8586, #4903, #32918 ),
 ( #29258, #48948, #13049, #45000, #9100, #25051, #29761, #30539, #45780, #26609, #10392, #22932, #13805, #30019, #50484, #42883 ),
 ( #14834, #42360, #34206, #46564, #41840, #46046, #14316, #30796, #26348, #21900, #42099, #10913, #18503, #17987, #6463, #2786 ),
 ( #18757, #10652, #34731, #22420, #2005, #50734, #37912, #38695, #26875, #10134, #6204, #42622, #22158, #6978, #6721, #46824 ),
 ( #9869, #38423, #38170, #26091, #33951, #2265, #18239, #1746, #50228, #34475, #49969, #33700, #14060, #22677, #30286, #2526 ),
 ( #17730, #49717, #46304, #25824, #5942, #14574, #27900, #27393, #39201, #43905, #12193, #15094, #47588, #4065, #43394, #3819 ),
 ( #31568, #19792, #7489, #7237, #3043, #16113, #36030, #138, #51514, #38952, #51765, #39974, #47336, #35262, #48094, #8254 ) ),
 .UNSPECIFIED., .F., .F., .F.,
 ( 4, 1, 1, 1, 1, 1, 1, 4 ),
 ( 4, 2, 2, 2, 2, 2, 2, 4 ),
 ( 0.000000000000000000, 0.1428571428571430157, 0.2857142857142860315, 0.4285714285714289917, 0.5714285714285709528, 0.7142857142857139685, 0.8571428571428569843, 1.000000000000000000 ),
 ( -3.863343447353519977, -3.187258344066659976, -2.414589654595949764, -1.931671723676759989, -1.690212758217169986, -1.313423695611309894, -0.7105611954419280840, 0.000000000000000000 ),
 .UNSPECIFIED. ) ;
#50430=CARTESIAN_POINT ( 'NONE',  ( 53.19108282174769897, 19.98230769539780027, -75.83523926356809852 ) ) ;
#50431=FACE_OUTER_BOUND ( 'NONE', #14599, .T. ) ;
#50434=CARTESIAN_POINT ( 'NONE',  ( 15.21636614235080032, 19.37178131641699963, -15.64999999240779971 ) ) ;
#50435=CARTESIAN_POINT ( 'NONE',  ( 1.828123248987350014, -55.63609750716739910, -10.79459774355089863 ) ) ;
#50436=CARTESIAN_POINT ( 'NONE',  ( 75.41210043417740394, 0.5916036937065950463, -12.07275756619249840 ) ) ;
#50437=DIRECTION ( 'NONE',  ( 0.2260571801428161165, -2.775557561562891043E-17, -0.9741140340359943917 ) ) ;
#50438=CARTESIAN_POINT ( 'NONE',  ( 19.75452741144124502, -55.45190691955212969, -75.31104072282781203 ) ) ;
#50439=CARTESIAN_POINT ( 'NONE',  ( 12.84043731220637596, -55.48023558917851261, -75.66007724753696095 ) ) ;
#50441=CARTESIAN_POINT ( 'NONE',  ( 7.571123728786862905, 29.74412437438943613, -20.43741446242724180 ) ) ;
#50443=CARTESIAN_POINT ( 'NONE',  ( 13.64046745046540110, 19.01922438765150147, -20.99582705430550078 ) ) ;
#50444=PLANE ( 'NONE',  #8096 ) ;
#50445=CARTESIAN_POINT ( 'NONE',  ( 40.95606765393399940, 13.15690657785849993, -3.881683722126650249 ) ) ;
#50448=CARTESIAN_POINT ( 'NONE',  ( 68.13393739769745139, -49.21324915460503036, -70.54648330188275906 ) ) ;
#50449=CARTESIAN_POINT ( 'NONE',  ( 75.92401563033300249, -43.33178766826745232, -13.58799118537118567 ) ) ;
#50450=CARTESIAN_POINT ( 'NONE',  ( 18.15925977880919717, -52.01891576978010079, -75.67066142420200947 ) ) ;
#50451=CARTESIAN_POINT ( 'NONE',  ( 53.10211901724390060, -45.11618894467940066, -9.306651317679861535 ) ) ;
#50452=ORIENTED_EDGE ( 'NONE', *, *, #7745, .T. ) ;
#50456=DIRECTION ( 'NONE',  ( -0.4640893551880381218, 0.8857883891772070362, 0.000000000000000000 ) ) ;
#50458=CARTESIAN_POINT ( 'NONE',  ( 74.93037295002240228, -43.11618894467930119, -15.31098073120859837 ) ) ;
#50462=VERTEX_POINT ( 'NONE', #38702 ) ;
#50467=CARTESIAN_POINT ( 'NONE',  ( 61.29004561485690061, -45.22833724571190572, -46.51650915558359856 ) ) ;
#50469=DIRECTION ( 'NONE',  ( 1.000000000000000000, 0.000000000000000000, 0.000000000000000000 ) ) ;
#50473=ORIENTED_EDGE ( 'NONE', *, *, #28960, .F. ) ;
#50475=LINE ( 'NONE', #25306, #37664 ) ;
#50479=AXIS2_PLACEMENT_3D ( 'NONE', #9096, #16967, #25565 ) ;
#50480=CARTESIAN_POINT ( 'NONE',  ( 52.61550136881809436, -51.35813298341240341, -75.86880934735940230 ) ) ;
#50481=CARTESIAN_POINT ( 'NONE',  ( 60.23889825737590087, 14.54821815915980032, -47.30579064662340016 ) ) ;
#50482=FACE_BOUND ( 'NONE', #10674, .T. ) ;
#50483=EDGE_CURVE ( 'NONE', #9344, #12214, #10398, .T. ) ;
#50484=CARTESIAN_POINT ( 'NONE',  ( 41.02582416393729403, -44.60212236685470089, -4.878402777628929599 ) ) ;
#50486=CARTESIAN_POINT ( 'NONE',  ( 65.04225540962447383, 1.022507349525342502, -17.84440820854044674 ) ) ;
#50488=CARTESIAN_POINT ( 'NONE',  ( 82.13853704237929776, 13.88381105532070059, -46.37203261889099792 ) ) ;
#50489=DIRECTION ( 'NONE',  ( 1.000000000000000000, 0.000000000000000000, 0.000000000000000000 ) ) ;
#50491=ORIENTED_EDGE ( 'NONE', *, *, #36012, .T. ) ;
#50492=CARTESIAN_POINT ( 'NONE',  ( 14.72298240475299913, -52.26337343415740122, -75.96669286083250938 ) ) ;
#50493=CARTESIAN_POINT ( 'NONE',  ( 57.48794426520840517, 19.15268824649449897, -52.98983914114159433 ) ) ;
#50498=ADVANCED_FACE ( 'NONE', ( #26615 ), #38430, .T. ) ;
#50500=CARTESIAN_POINT ( 'NONE',  ( 47.98474431824940467, -54.38356013217800466, -55.12640935544759913 ) ) ;
#50502=CIRCLE ( 'NONE', #1238, 2.000000000000001332 ) ;
#50503=CARTESIAN_POINT ( 'NONE',  ( 56.48750710943370024, 19.52146772179129997, -53.61740591960349889 ) ) ;
#50504=CARTESIAN_POINT ( 'NONE',  ( 47.84723601610939880, 23.19681007510559922, -54.96539816047189930 ) ) ;
#50508=CIRCLE ( 'NONE', #48010, 3.400000000022780799 ) ;
#50512=DIRECTION ( 'NONE',  ( 0.000000000000000000, 0.000000000000000000, -1.000000000000000000 ) ) ;
#50513=DIRECTION ( 'NONE',  ( 0.3281607301299682700, -0.6263469766835021435, 0.7071067811865493491 ) ) ;
#50514=CARTESIAN_POINT ( 'NONE',  ( 52.58854596461549846, 18.60460160505449778, -27.97794855353080123 ) ) ;
#50516=DIRECTION ( 'NONE',  ( 0.000000000000000000, 0.000000000000000000, -1.000000000000000000 ) ) ;
#50519=ORIENTED_EDGE ( 'NONE', *, *, #8981, .T. ) ;
#50521=EDGE_LOOP ( 'NONE', ( #10250, #28711, #5748, #20076 ) ) ;
#50523=CARTESIAN_POINT ( 'NONE',  ( 12.16812838079169978, -64.68014690341630057, -15.91929859869470043 ) ) ;
#50524=CARTESIAN_POINT ( 'NONE',  ( 57.50723796702219914, -46.11618894467930119, -25.33268370472680076 ) ) ;
#50525=CARTESIAN_POINT ( 'NONE',  ( 11.83825639585159983, 33.81473130949329686, -45.42565952194429713 ) ) ;
#50526=CARTESIAN_POINT ( 'NONE',  ( 9.511520510868781031, -63.71643849929780856, -46.52942082108589261 ) ) ;
#50529=EDGE_CURVE ( 'NONE', #38543, #5918, #30545, .T. ) ;
#50530=CARTESIAN_POINT ( 'NONE',  ( 54.91646384901320488, 20.20362395552419699, -54.04939823774940066 ) ) ;
#50531=CARTESIAN_POINT ( 'NONE',  ( 56.57310015978940498, 14.96172080682539907, -26.26426129276709887 ) ) ;
#50532=CARTESIAN_POINT ( 'NONE',  ( 53.11770077000060297, -49.55992874389239233, -49.09731761359610402 ) ) ;
#50533=CARTESIAN_POINT ( 'NONE',  ( 48.79723671898879900, 22.41103229812440034, -53.89287427470050318 ) ) ;
#50535=CARTESIAN_POINT ( 'NONE',  ( 50.72974178121339150, -49.49305235525400093, -76.22250671080470852 ) ) ;
#50536=CARTESIAN_POINT ( 'NONE',  ( 56.98397757690029408, -50.69327631065389994, -53.23409530833590253 ) ) ;
#50537=ORIENTED_EDGE ( 'NONE', *, *, #8461, .T. ) ;
#50539=CARTESIAN_POINT ( 'NONE',  ( 69.22748654599826068, 19.47158195952208004, -70.40645085170191919 ) ) ;
#50542=CARTESIAN_POINT ( 'NONE',  ( 49.92842301023320317, -45.11618894467940066, -10.23644921203369940 ) ) ;
#50544=CARTESIAN_POINT ( 'NONE',  ( 13.76822423289859998, -51.12516065014939670, -22.18389327967700098 ) ) ;
#50545=CARTESIAN_POINT ( 'NONE',  ( 55.34187454801539729, 19.38381105532069881, -76.48031925771689998 ) ) ;
#50546=CARTESIAN_POINT ( 'NONE',  ( 47.57128498443769615, -54.56535262155699684, -74.19815949659729881 ) ) ;
#50547=CARTESIAN_POINT ( 'NONE',  ( 55.17360652619739625, 13.97791545909459998, -14.82785752668969792 ) ) ;
#50548=CARTESIAN_POINT ( 'NONE',  ( 47.69785024206510116, 23.27647591315859898, -55.07623521634459962 ) ) ;
#50550=CARTESIAN_POINT ( 'NONE',  ( 56.50450790981899729, -50.73896967485040221, -53.50133212754479928 ) ) ;
#50554=CARTESIAN_POINT ( 'NONE',  ( 47.62448412835980349, 23.28090870184360028, -74.50417146787160050 ) ) ;
#50556=CARTESIAN_POINT ( 'NONE',  ( 43.63773095450489592, -46.04023181038529344, -8.037430359857850704 ) ) ;
#50558=CARTESIAN_POINT ( 'NONE',  ( 57.55751162049570269, -48.61618894467930119, -53.92796738110899923 ) ) ;
#50561=CARTESIAN_POINT ( 'NONE',  ( 82.13853704237929776, 13.98942268381949994, -47.02038781679129897 ) ) ;
#50562=EDGE_CURVE ( 'NONE', #51441, #39898, #33628, .T. ) ;
#50568=CARTESIAN_POINT ( 'NONE',  ( -33.86606230032689524, -20.49714794425430142, -57.75543702565100546 ) ) ;
#50571=CARTESIAN_POINT ( 'NONE',  ( 52.86125339900270603, -49.65852478324119801, -48.87400161482390359 ) ) ;
#50573=CARTESIAN_POINT ( 'NONE',  ( 17.64670642448523097, 20.66383147154662581, -75.74021525116319253 ) ) ;
#50575=CARTESIAN_POINT ( 'NONE',  ( 13.64848238802169966, 20.16422653727189740, -23.00152640757379885 ) ) ;
#50579=CARTESIAN_POINT ( 'NONE',  ( 53.56302256524990213, 18.15423094141489813, -49.17075139047800292 ) ) ;
#50580=CARTESIAN_POINT ( 'NONE',  ( 55.52984664395540193, -45.92959713896109264, -16.63879282810290050 ) ) ;
#50585=CARTESIAN_POINT ( 'NONE',  ( 11.93488811383480019, -65.43955691952199061, -17.90291648171000105 ) ) ;
#50586=CARTESIAN_POINT ( 'NONE',  ( 9.742037140472790568, 33.13719944107199922, -46.80840188538130064 ) ) ;
#50588=CARTESIAN_POINT ( 'NONE',  ( 10.66246720348149957, -64.86660773051299600, -18.01843150775420099 ) ) ;
#50592=DIRECTION ( 'NONE',  ( 1.000000000000000000, 0.000000000000000000, 0.000000000000000000 ) ) ;
#50593=ORIENTED_EDGE ( 'NONE', *, *, #44228, .T. ) ;
#50597=CARTESIAN_POINT ( 'NONE',  ( 9.729212633477690275, -63.13885989062299586, -46.30111529514049806 ) ) ;
#50598=DIRECTION ( 'NONE',  ( 0.000000000000000000, -1.000000000000000000, 0.000000000000000000 ) ) ;
#50601=CARTESIAN_POINT ( 'NONE',  ( 56.87125374609500028, 19.41964089708080010, -53.85479923334150243 ) ) ;
#50602=CARTESIAN_POINT ( 'NONE',  ( 54.14345801728809704, 19.38380527828979893, -76.93443301949999125 ) ) ;
#50605=CARTESIAN_POINT ( 'NONE',  ( 16.13393739769620083, -15.61618894467929941, 1.600000000000000089 ) ) ;
#50611=ORIENTED_EDGE ( 'NONE', *, *, #8021, .F. ) ;
#50612=FACE_OUTER_BOUND ( 'NONE', #7156, .T. ) ;
#50615=LINE ( 'NONE', #3183, #28307 ) ;
#50618=CARTESIAN_POINT ( 'NONE',  ( 52.68908936341578908, -49.75029824513269716, -48.47378032971909789 ) ) ;
#50619=CARTESIAN_POINT ( 'NONE',  ( 45.38207380022019777, -45.37872504213810032, -8.365231906245979232 ) ) ;
#50622=ORIENTED_EDGE ( 'NONE', *, *, #27475, .F. ) ;
#50623=CARTESIAN_POINT ( 'NONE',  ( 52.73888932328210188, -49.67618315451370137, -27.47948615241350012 ) ) ;
#50625=CARTESIAN_POINT ( 'NONE',  ( 56.50063657765719682, -50.76119911934350171, -74.14935534434708586 ) ) ;
#50626=CARTESIAN_POINT ( 'NONE',  ( -2.574198652525490072, 19.80097958437369954, -8.360332649887961765 ) ) ;
#50628=CARTESIAN_POINT ( 'NONE',  ( 47.32222669057270537, -54.70165496723960530, -54.63504270530570039 ) ) ;
#50629=CYLINDRICAL_SURFACE ( 'NONE', #18065, 1.000000000000001110 ) ;
#50631=ORIENTED_EDGE ( 'NONE', *, *, #45311, .F. ) ;
#50632=CARTESIAN_POINT ( 'NONE',  ( 52.82975622904280755, -49.66092049964720445, -48.48626292588439668 ) ) ;
#50633=CARTESIAN_POINT ( 'NONE',  ( 47.79460208473339833, 23.17020998024509737, -54.69564055610090492 ) ) ;
#50635=CARTESIAN_POINT ( 'NONE',  ( 84.42051414649773733, -43.53095039421000223, -47.44928429663789160 ) ) ;
#50637=CARTESIAN_POINT ( 'NONE',  ( 12.05606148284509871, 33.93520160465880053, -16.66333073003769627 ) ) ;
#50639=CARTESIAN_POINT ( 'NONE',  ( 53.30584942118750291, 18.17910404770230315, -48.80307101436750372 ) ) ;
#50640=CARTESIAN_POINT ( 'NONE',  ( 18.38892583657722923, 24.32148015893219650, -76.14999999999999147 ) ) ;
#50641=DIRECTION ( 'NONE',  ( 0.4145156864928219442, -0.9100421669633690369, 0.000000000000000000 ) ) ;
#50642=CARTESIAN_POINT ( 'NONE',  ( 52.89288899001359567, 18.34731072048720080, -27.71426086418919965 ) ) ;
#50644=CARTESIAN_POINT ( 'NONE',  ( 50.61900101762439874, 4.651609355440132987, -76.23853349069526075 ) ) ;
#50646=CARTESIAN_POINT ( 'NONE',  ( 52.70698220066480388, 18.52838197885590077, -48.81385519956149466 ) ) ;
#50649=CARTESIAN_POINT ( 'NONE',  ( 10.77427333304090062, 32.15375400438119868, -45.20766266540499601 ) ) ;
#50651=CARTESIAN_POINT ( 'NONE',  ( 13.20770907579910158, -46.26637462015160196, -23.15000000000000213 ) ) ;
#50654=ORIENTED_EDGE ( 'NONE', *, *, #40911, .T. ) ;
#50659=CARTESIAN_POINT ( 'NONE',  ( 51.01907554470725614, 0.1776427667142097822, -16.88746765477635847 ) ) ;
#50660=ORIENTED_EDGE ( 'NONE', *, *, #23318, .F. ) ;
#50661=CARTESIAN_POINT ( 'NONE',  ( 11.30321776117639843, -64.33719732150139237, -44.46574515417460560 ) ) ;
#50662=CARTESIAN_POINT ( 'NONE',  ( 55.86565860574650344, -45.97208290794810637, -25.40205046782289955 ) ) ;
#50668=CARTESIAN_POINT ( 'NONE',  ( 11.36486248725049997, 32.41286963914479458, -24.38092508955430304 ) ) ;
#50669=ORIENTED_EDGE ( 'NONE', *, *, #34835, .T. ) ;
#50671=DIRECTION ( 'NONE',  ( 0.000000000000000000, 0.000000000000000000, -1.000000000000000000 ) ) ;
#50672=CARTESIAN_POINT ( 'NONE',  ( 14.34399776555499884, 19.88381105071939814, -22.49261467888849708 ) ) ;
#50675=CARTESIAN_POINT ( 'NONE',  ( 47.30599826317899215, -54.71628134471639981, -74.19801721955809626 ) ) ;
#50676=CARTESIAN_POINT ( 'NONE',  ( 52.00606832011370528, 13.88381313913080106, -8.714322203361728469 ) ) ;
#50679=PLANE ( 'NONE',  #3347 ) ;
#50680=CARTESIAN_POINT ( 'NONE',  ( 61.65645849501900244, 13.88380407631539981, -27.60631482466889963 ) ) ;
#50682=B_SPLINE_SURFACE_WITH_KNOTS ( 'NONE', 3, 3, ( 
 ( #42732, #35098, #23285, #35362, #39308, #6559, #2632, #46928, #27491, #6827, #11012, #19119, #22779, #22524, #18341, #31411, #51361, #11534, #3411, #34582, #38799, #2893 ),
 ( #2363, #26983, #18858, #34843, #14934, #7600, #50586, #34318, #23036, #23544, #46411, #51099, #43498, #39058, #50843, #3151, #14419, #38536, #27232, #18604, #14676, #19379 ),
 ( #30387, #30899, #42990, #15198, #7086, #30646, #10499, #47439, #15461, #42470, #10754, #26713, #31157, #47185, #43250, #35877, #48718, #8884, #27753, #4166, #15970, #40583 ),
 ( #12047, #741, #48452, #4681, #43750, #36132, #39816, #12557, #44257, #31924, #20653, #486, #12298, #20394, #39562, #32430, #24570, #44517, #8364, #16475, #237, #34365 ),
 ( #32177, #48193, #51616, #19638, #40073, #36638, #28520, #3668, #16739, #8623, #12822, #32693, #47689, #28257, #7852, #44779, #3926, #47946, #24313, #36381, #28780, #35630 ),
 ( #19886, #28000, #40331, #11793, #15709, #31666, #23802, #44006, #8109, #24055, #20143, #16222, #4424, #37431, #37688, #25609, #45819, #9655, #33487, #33738, #40843, #5474 ),
 ( #4942, #1786, #45557, #21428, #13092, #29044, #41880, #20917, #5217, #13589, #9907, #13843, #49753, #1529, #29298, #17011, #5723, #36911, #1013, #1274, #17515, #45040 ),
 ( #29801, #32959, #49243, #29554, #48988, #41614, #9139, #25095, #13338, #41107, #21172, #21677, #37177, #17767, #17265, #45299, #33225, #49501, #25865, #24836, #9408, #41359 ),
 ( #25356, #47849, #24740, #48360, #4330, #20299, #28943, #36289, #655, #39982, #51773, #4075, #40751, #16124, #8530, #32859, #12993, #16913, #399, #48889, #48626, #44948 ),
 ( #9048, #20046, #28681, #36038, #146, #4851, #12726, #32085, #24215, #24995, #43913, #32341, #28163, #16638, #16383, #919, #41014, #20818, #48104, #19801, #35790, #15878 ) ),
 .UNSPECIFIED., .F., .F., .F.,
 ( 4, 1, 1, 1, 1, 1, 1, 4 ),
 ( 4, 2, 2, 2, 2, 2, 2, 2, 2, 2, 4 ),
 ( -2.341432999999999973E-10, 0.1428571428571430157, 0.2857142857142860315, 0.4285714285714289917, 0.5714285714285709528, 0.7142857142857139685, 0.8571428571428569843, 1.000000000234150033 ),
 ( -8.594361155364929061, -7.576833180893860487, -6.384773949355639466, -5.367405169037740009, -4.291753173673400035, -3.753927175991219833, -2.893405579699740215, -2.204988302666559985, -1.516571025633369985, -0.4151033823802809941, 0.01085480778399900044 ),
 .UNSPECIFIED. ) ;
#50684=CARTESIAN_POINT ( 'NONE',  ( 54.05043764316730659, -48.58749351201610267, -26.96881999329520241 ) ) ;
#50686=CARTESIAN_POINT ( 'NONE',  ( -5.040141449686119657, -47.05667976586999401, -4.957448605375669892 ) ) ;
#50687=CARTESIAN_POINT ( 'NONE',  ( 76.35984344540050017, -21.83182212063609740, -12.62201988643909978 ) ) ;
#50688=CARTESIAN_POINT ( 'NONE',  ( 75.16286580954648855, 13.70473030084525767, -14.50431359832863620 ) ) ;
#50689=CARTESIAN_POINT ( 'NONE',  ( 61.09721242536592456, -45.48235634517234161, -47.46777540746526824 ) ) ;
#50692=AXIS2_PLACEMENT_3D ( 'NONE', #42399, #18793, #45552 ) ;
#50695=CARTESIAN_POINT ( 'NONE',  ( 41.39168664676449794, 12.97209261023169979, -4.419063984731860018 ) ) ;
#50697=CARTESIAN_POINT ( 'NONE',  ( 49.42204313923179626, -53.51403126671309707, -54.19389682688790089 ) ) ;
#50700=CARTESIAN_POINT ( 'NONE',  ( 75.79443952681172902, -43.34572367340545185, -13.52171987147115750 ) ) ;
#50701=CARTESIAN_POINT ( 'NONE',  ( 18.01252544226889896, -51.38128844478560353, -75.14498753491579919 ) ) ;
#50702=CARTESIAN_POINT ( 'NONE',  ( 60.59355682701219337, -44.96618261540349692, -10.31481105180509950 ) ) ;
#50707=DIRECTION ( 'NONE',  ( 0.000000000000000000, 0.000000000000000000, 1.000000000000000000 ) ) ;
#50711=AXIS2_PLACEMENT_3D ( 'NONE', #24749, #406, #27666 ) ;
#50713=CARTESIAN_POINT ( 'NONE',  ( 45.22526645711639759, -45.57792172170950806, -8.601017710285070450 ) ) ;
#50714=ORIENTED_EDGE ( 'NONE', *, *, #39212, .T. ) ;
#50718=EDGE_LOOP ( 'NONE', ( #3336, #39053, #45129, #17610 ) ) ;
#50720=CARTESIAN_POINT ( 'NONE',  ( 61.09780586005280156, -45.32905657884899853, -46.84341276801610121 ) ) ;
#50724=LINE ( 'NONE', #31555, #7356 ) ;
#50726=DIRECTION ( 'NONE',  ( 1.000000000000000000, 0.000000000000000000, 0.000000000000000000 ) ) ;
#50727=CARTESIAN_POINT ( 'NONE',  ( 83.89200044194980421, -50.61618894467930119, -53.92796738110899923 ) ) ;
#50729=CARTESIAN_POINT ( 'NONE',  ( 60.83133137330749918, -45.46867109277970087, -47.01992810568810199 ) ) ;
#50730=CARTESIAN_POINT ( 'NONE',  ( 51.42345331545769227, -50.56011499177679980, -76.23764483251279955 ) ) ;
#50731=CARTESIAN_POINT ( 'NONE',  ( 60.63179223956819897, 14.34380986286560145, -47.21451266482660714 ) ) ;
#50734=CARTESIAN_POINT ( 'NONE',  ( 41.98583910622449622, -43.58195263108250117, -3.946145645806039770 ) ) ;
#50736=CARTESIAN_POINT ( 'NONE',  ( 57.50723796702470025, 15.88381105532069704, -17.93019253464870033 ) ) ;
#50737=CARTESIAN_POINT ( 'NONE',  ( -7.073749351297280441, 14.53014294518820115, -5.239700901386809662 ) ) ;
#50739=VECTOR ( 'NONE', #20827, 1000.000000000000000 ) ;
#50743=VERTEX_POINT ( 'NONE', #45701 ) ;
#50746=CARTESIAN_POINT ( 'NONE',  ( 14.74661529360900047, -52.24941868644869913, -75.96018872839380265 ) ) ;
#50753=CARTESIAN_POINT ( 'NONE',  ( 15.53208191794040083, 19.63190946341060084, -20.56249370038050017 ) ) ;
#50756=EDGE_CURVE ( 'NONE', #47619, #31811, #17662, .T. ) ;
#50758=CARTESIAN_POINT ( 'NONE',  ( 48.02969574711249834, -54.30226728297670036, -54.78113594584849722 ) ) ;
#50762=ORIENTED_EDGE ( 'NONE', *, *, #7474, .T. ) ;
#50769=CARTESIAN_POINT ( 'NONE',  ( 82.75389495153045516, 14.36254469553479574, -47.67225488023363766 ) ) ;
#50770=CARTESIAN_POINT ( 'NONE',  ( 83.36355414428213351, 14.11443836545216968, -47.55048134665359783 ) ) ;
#50772=CARTESIAN_POINT ( 'NONE',  ( 83.69028489729539899, 13.83794172252809851, -47.49660994411200221 ) ) ;
#50779=ORIENTED_EDGE ( 'NONE', *, *, #34759, .F. ) ;
#50780=ADVANCED_FACE ( 'NONE', ( #44020 ), #32585, .F. ) ;
#50782=CARTESIAN_POINT ( 'NONE',  ( 11.88460916115749910, -64.82510961609500555, -16.16716782998640056 ) ) ;
#50783=CARTESIAN_POINT ( 'NONE',  ( 7.695097139525112873, -60.75237708241192536, -20.68192065308969418 ) ) ;
#50784=CARTESIAN_POINT ( 'NONE',  ( 76.49394062354240020, -27.97249612882005465, -13.20130748058310388 ) ) ;
#50785=CARTESIAN_POINT ( 'NONE',  ( 9.381135691567910939, -63.38818850907809832, -46.50683779583690125 ) ) ;
#50786=AXIS2_PLACEMENT_3D ( 'NONE', #467, #12026, #27731 ) ;
#50787=ORIENTED_EDGE ( 'NONE', *, *, #10867, .F. ) ;
#50788=ORIENTED_EDGE ( 'NONE', *, *, #30266, .F. ) ;
#50791=LINE ( 'NONE', #39002, #31223 ) ;
#50793=CARTESIAN_POINT ( 'NONE',  ( 64.61005101894130576, 0.6433700368313129969, -17.35087735437779699 ) ) ;
#50794=CARTESIAN_POINT ( 'NONE',  ( 52.19990148684729547, -49.79086060043429995, -77.09681897153029695 ) ) ;
#50795=CARTESIAN_POINT ( 'NONE',  ( 58.72540476535390042, -48.17849370114159768, -50.40155767129670039 ) ) ;
#50798=DIRECTION ( 'NONE',  ( 0.6415444970810866288, 0.4854844151940982400, 0.5939070136550167467 ) ) ;
#50801=DIRECTION ( 'NONE',  ( 1.000000000000000000, 0.000000000000000000, 0.000000000000000000 ) ) ;
#50804=CARTESIAN_POINT ( 'NONE',  ( 14.01755875199390111, -51.05430465436170806, -22.03916537273070020 ) ) ;
#50805=LINE ( 'NONE', #31628, #39335 ) ;
#50806=CARTESIAN_POINT ( 'NONE',  ( 57.06558336992600289, 13.88381105532070059, -16.29907433820719831 ) ) ;
#50807=CARTESIAN_POINT ( 'NONE',  ( 60.66036723437029821, -45.55824399519830337, -47.11242429048819957 ) ) ;
#50810=CARTESIAN_POINT ( 'NONE',  ( 75.47966807050509885, -43.37310274687460065, -13.40512917118210012 ) ) ;
#50811=EDGE_LOOP ( 'NONE', ( #48999, #13993 ) ) ;
#50812=CARTESIAN_POINT ( 'NONE',  ( 47.61774400735439627, 23.31213713685490418, -74.19770771130870912 ) ) ;
#50814=CARTESIAN_POINT ( 'NONE',  ( 44.67725961099969822, -46.10245440686500018, -8.756022344162619930 ) ) ;
#50815=EDGE_CURVE ( 'NONE', #6439, #29653, #17995, .T. ) ;
#50818=CIRCLE ( 'NONE', #27348, 1.999999999999996669 ) ;
#50819=DIRECTION ( 'NONE',  ( 0.000000000000000000, -1.000000000000000000, 0.000000000000000000 ) ) ;
#50821=CARTESIAN_POINT ( 'NONE',  ( 82.51403489249999268, 13.88629484321260144, -46.70334943848269660 ) ) ;
#50823=CARTESIAN_POINT ( 'NONE',  ( 52.97776614862323896, 19.06888045206829574, -77.23905649707201349 ) ) ;
#50824=DIRECTION ( 'NONE',  ( 0.000000000000000000, 1.000000000000000000, 0.000000000000000000 ) ) ;
#50826=CARTESIAN_POINT ( 'NONE',  ( 48.95529619442159941, 22.62706584891199668, -54.62080953740519362 ) ) ;
#50828=CARTESIAN_POINT ( 'NONE',  ( 52.89023673218689936, -49.63844819782259776, -48.86102656628040108 ) ) ;
#50832=CARTESIAN_POINT ( 'NONE',  ( 13.99025901751500101, 19.94838289472389903, -22.90514570209199974 ) ) ;
#50833=CARTESIAN_POINT ( 'NONE',  ( 52.26504646883520167, -49.78354544620959388, -77.19463087837650050 ) ) ;
#50835=CARTESIAN_POINT ( 'NONE',  ( 53.02886661541120361, 18.37360774895879700, -49.08317481420909445 ) ) ;
#50836=CARTESIAN_POINT ( 'NONE',  ( 55.92660166244869657, -45.72950351173099648, -17.10190867576899976 ) ) ;
#50840=EDGE_CURVE ( 'NONE', #34516, #42834, #32868, .T. ) ;
#50841=VERTEX_POINT ( 'NONE', #42551 ) ;
#50843=CARTESIAN_POINT ( 'NONE',  ( 11.46849097211869939, 34.01295885014749842, -47.29791990983230221 ) ) ;
#50845=FACE_OUTER_BOUND ( 'NONE', #7211, .T. ) ;
#50846=CARTESIAN_POINT ( 'NONE',  ( 53.41693480164780539, 18.12090330447910347, -48.75416851879779756 ) ) ;
#50847=CARTESIAN_POINT ( 'NONE',  ( -2.927827710953269769, 17.96742650791509988, -5.740515240579870060 ) ) ;
#50848=CARTESIAN_POINT ( 'NONE',  ( 51.07994173643560032, -52.78781467787970882, -53.74568964421160189 ) ) ;
#50851=ORIENTED_EDGE ( 'NONE', *, *, #24513, .T. ) ;
#50852=CARTESIAN_POINT ( 'NONE',  ( 9.731586802489630372, -63.16114365233679706, -46.29992529111800081 ) ) ;
#50854=ORIENTED_EDGE ( 'NONE', *, *, #23701, .F. ) ;
#50855=CARTESIAN_POINT ( 'NONE',  ( 11.13393739769619906, -63.52234721269329754, -43.76018303787720498 ) ) ;
#50856=CARTESIAN_POINT ( 'NONE',  ( 57.00264671592019994, 19.39868990108010038, -53.72993498978910054 ) ) ;
#50857=CARTESIAN_POINT ( 'NONE',  ( 52.00136199551640459, 18.79993947043690028, -76.70561737979799943 ) ) ;
#50859=DIRECTION ( 'NONE',  ( 1.000000000000000000, 0.000000000000000000, 0.000000000000000000 ) ) ;
#50861=CARTESIAN_POINT ( 'NONE',  ( 51.84413674030108155, 20.10506014047227197, -76.02231598272827284 ) ) ;
#50862=DIRECTION ( 'NONE',  ( 0.6415444970810866288, 0.4854844151940982400, 0.5939070136550167467 ) ) ;
#50870=AXIS2_PLACEMENT_3D ( 'NONE', #2952, #29674, #9785 ) ;
#50873=CARTESIAN_POINT ( 'NONE',  ( 16.13393739769620083, -15.61618894467929941, -76.14999999999999147 ) ) ;
#50879=EDGE_CURVE ( 'NONE', #37502, #23561, #4179, .T. ) ;
#50880=CARTESIAN_POINT ( 'NONE',  ( 12.21104395315670033, 33.65513056404519432, -16.16308188030659920 ) ) ;
#50884=CARTESIAN_POINT ( 'NONE',  ( 53.82849609051940121, -50.85534700936450747, -76.11669736854409507 ) ) ;
#50885=CARTESIAN_POINT ( 'NONE',  ( -9.937296257482078232, 11.24462281463240032, -4.618840561276110535 ) ) ;
#50886=PLANE ( 'NONE',  #18863 ) ;
#50887=CARTESIAN_POINT ( 'NONE',  ( 47.21829295900949575, -54.77949880278709571, -54.61684610847309784 ) ) ;
#50888=DIRECTION ( 'NONE',  ( 0.000000000000000000, 1.000000000000000000, 0.000000000000000000 ) ) ;
#50891=CARTESIAN_POINT ( 'NONE',  ( 47.75992848858749795, 23.21189837656569921, -54.79446835205050803 ) ) ;
#50893=CARTESIAN_POINT ( 'NONE',  ( 41.99203386431830154, -44.88537213046480190, -5.712673480947970006 ) ) ;
#50895=CARTESIAN_POINT ( 'NONE',  ( 61.41197480388229479, 14.20364326968670099, -47.45949227984320373 ) ) ;
#50896=CARTESIAN_POINT ( 'NONE',  ( 11.65337899615939854, 33.98458825826539709, -16.97470857289490098 ) ) ;
#50897=CARTESIAN_POINT ( 'NONE',  ( 51.51548137838339869, 17.54834764421520177, -76.79511588530829158 ) ) ;
#50898=CARTESIAN_POINT ( 'NONE',  ( 52.79375783669770072, 18.44803353500160270, -48.48715717239780076 ) ) ;
#50900=CARTESIAN_POINT ( 'NONE',  ( 53.02240710655760125, -49.55998530720779627, -48.78672999826209633 ) ) ;
#50901=CARTESIAN_POINT ( 'NONE',  ( 56.36055665625740119, 14.84967702978789994, -26.17082522920440013 ) ) ;
#50904=CARTESIAN_POINT ( 'NONE',  ( 12.24533245415720017, -64.90027884028160088, -16.17634614696339668 ) ) ;
#50905=CARTESIAN_POINT ( 'NONE',  ( 62.63757649181060572, -31.25222801252620286, -16.75027474776850411 ) ) ;
#50907=CARTESIAN_POINT ( 'NONE',  ( 11.13393739769619906, 32.16464604112239556, -43.91975316531460294 ) ) ;
#50909=CARTESIAN_POINT ( 'NONE',  ( 66.13282620745420104, -31.02979715315369802, -17.01779704780440028 ) ) ;
#50913=DIRECTION ( 'NONE',  ( -0.5481519472162221795, 0.4595820247375140832, -0.6987945372577201164 ) ) ;
#50914=CARTESIAN_POINT ( 'NONE',  ( 49.69240448927909171, -1.840319678862813557, -15.81291498579800603 ) ) ;
#50916=CARTESIAN_POINT ( 'NONE',  ( 12.69791550947999959, -65.47883885079799882, -47.19956182400449762 ) ) ;
#50917=CARTESIAN_POINT ( 'NONE',  ( 56.67873295854410287, -45.30972226631099886, -25.50361698670420196 ) ) ;
#50922=CARTESIAN_POINT ( 'NONE',  ( 10.65677182350291297, 32.67421915925709186, -23.61757666224062291 ) ) ;
#50924=CARTESIAN_POINT ( 'NONE',  ( 10.65234009212060151, 32.64172376425219824, -23.62431477846339689 ) ) ;
#50928=CARTESIAN_POINT ( 'NONE',  ( 51.19326779044995845, 0.4483973451604243987, -17.14369881442766541 ) ) ;
#50929=CARTESIAN_POINT ( 'NONE',  ( 10.61754762155600140, 33.59328422689429772, -18.17417937929459981 ) ) ;
#50931=ADVANCED_FACE ( 'NONE', ( #13349 ), #30745, .T. ) ;
#50932=CARTESIAN_POINT ( 'NONE',  ( 60.03835289033210643, -29.28719532749419940, -15.81793802652529912 ) ) ;
#50934=CARTESIAN_POINT ( 'NONE',  ( 46.69862573999040478, -53.56655740942600374, -76.01558715013979395 ) ) ;
#50935=CARTESIAN_POINT ( 'NONE',  ( 60.34784213368690331, 13.88381105527400017, -11.22423537798319870 ) ) ;
#50942=CARTESIAN_POINT ( 'NONE',  ( 54.27327278922639664, -48.38567173727960125, -26.87344227122169826 ) ) ;
#50943=B_SPLINE_CURVE_WITH_KNOTS ( 'NONE', 3,
 ( #16476, #4425, #44258, #48453, #12558, #21173, #28521, #44780, #32178, #44007, #12299, #32960, #8365 ),
 .UNSPECIFIED., .F., .F.,
 ( 4, 2, 2, 1, 2, 2, 4 ),
 ( 0.000000000000000000, 0.2499999999999940048, 0.3749999999999943379, 0.4374999999999973910, 0.4687499999999962808, 0.4999999999999952260, 1.000000000000000000 ),
 .UNSPECIFIED. ) ;
#50944=CARTESIAN_POINT ( 'NONE',  ( 8.049435107523031263, -62.14063497384629642, -15.83799620030899824 ) ) ;
#50945=CARTESIAN_POINT ( 'NONE',  ( 76.06651092694269778, 9.716726065570350457, -13.34696153651469963 ) ) ;
#50946=DIRECTION ( 'NONE',  ( 0.6888026391158329487, -0.7071067811865494601, 0.1598465650148944150 ) ) ;
#50947=CARTESIAN_POINT ( 'NONE',  ( 14.19855276898660001, 24.33696219936630101, -76.14999999999999147 ) ) ;
#50948=DIRECTION ( 'NONE',  ( -0.7675009104025394269, -0.5576220516902739011, 0.3162277660168423266 ) ) ;
#50949=CARTESIAN_POINT ( 'NONE',  ( 47.18324198357279897, 23.57489020266570279, -54.61058319554400242 ) ) ;
#50950=CARTESIAN_POINT ( 'NONE',  ( 57.42460124420632894, 18.88910505960214437, -52.60814507333387979 ) ) ;
#50951=CARTESIAN_POINT ( 'NONE',  ( 57.49235397115290169, -50.30295757539000334, -52.84913016542050457 ) ) ;
#50952=CARTESIAN_POINT ( 'NONE',  ( 42.65512910241979938, 11.62675827516850013, -3.541891443476870016 ) ) ;
#50954=CARTESIAN_POINT ( 'NONE',  ( 66.97218591609239979, -45.11618894467940066, -13.04694144512030007 ) ) ;
#50955=CARTESIAN_POINT ( 'NONE',  ( 59.41577471975829638, -46.21032088470760613, -47.36236646002819839 ) ) ;
#50958=CARTESIAN_POINT ( 'NONE',  ( 18.50067234189449650, -52.01740915708810320, -75.38689171750549178 ) ) ;
#50959=FACE_OUTER_BOUND ( 'NONE', #45403, .T. ) ;
#50962=ORIENTED_EDGE ( 'NONE', *, *, #46923, .F. ) ;
#50963=CARTESIAN_POINT ( 'NONE',  ( -3.470035664683920107, 18.86435654622399838, -8.135935225242089786 ) ) ;
#50966=CIRCLE ( 'NONE', #2396, 15.29999999999999716 ) ;
#50970=CARTESIAN_POINT ( 'NONE',  ( 41.93137151579249888, -45.40097046374709322, -6.436558053594640505 ) ) ;
#50972=CARTESIAN_POINT ( 'NONE',  ( 17.21347160910339724, 21.88381105532300097, -76.14999999999999147 ) ) ;
#50975=CARTESIAN_POINT ( 'NONE',  ( 57.50723796702470025, -45.11618894467940066, -17.93019253464870033 ) ) ;
#50980=DIRECTION ( 'NONE',  ( -8.592609827796581962E-15, 1.919972818367709724E-16, -1.000000000000000000 ) ) ;
#50985=ORIENTED_EDGE ( 'NONE', *, *, #29390, .T. ) ;
#50987=CARTESIAN_POINT ( 'NONE',  ( 52.69948128945090104, -51.21643021819709674, -75.94570035807549857 ) ) ;
#50989=CARTESIAN_POINT ( 'NONE',  ( 60.99523858508910479, 14.17424510680999994, -47.17226579437169676 ) ) ;
#50992=CARTESIAN_POINT ( 'NONE',  ( 65.41765731850109944, -1.045745731241882526, -16.56748124947237244 ) ) ;
#50993=CARTESIAN_POINT ( 'NONE',  ( -8.870889643038399441, 13.08137690754710114, -5.817308098515409753 ) ) ;
#50995=AXIS2_PLACEMENT_3D ( 'NONE', #38555, #42225, #6325 ) ;
#50998=CARTESIAN_POINT ( 'NONE',  ( 16.13393739769620083, -15.61618894467929941, -12.65000000000000036 ) ) ;
#50999=VECTOR ( 'NONE', #10730, 999.9999999999998863 ) ;
#51004=CARTESIAN_POINT ( 'NONE',  ( 59.65718820948480783, 14.85145970413650041, -47.32570903220330649 ) ) ;
#51005=CARTESIAN_POINT ( 'NONE',  ( 57.37145085794500687, 19.38381105532069881, -53.92454733977369585 ) ) ;
#51006=CIRCLE ( 'NONE', #18374, 1.000000000000003109 ) ;
#51007=UNCERTAINTY_MEASURE_WITH_UNIT (LENGTH_MEASURE( 1.000000000000000082E-05 ), #47775, 'distance_accuracy_value', 'NONE');
#51011=FACE_OUTER_BOUND ( 'NONE', #22658, .T. ) ;
#51014=CARTESIAN_POINT ( 'NONE',  ( 47.90035703882499973, -54.39486251246400172, -54.90987639013900434 ) ) ;
#51020=ORIENTED_EDGE ( 'NONE', *, *, #15367, .T. ) ;
#51022=CARTESIAN_POINT ( 'NONE',  ( 60.41625431243939914, -45.68614159457540325, -47.22708700711559970 ) ) ;
#51024=CARTESIAN_POINT ( 'NONE',  ( 7.441840577107667443, 30.27300150430266967, -19.49871569355902423 ) ) ;
#51025=CARTESIAN_POINT ( 'NONE',  ( 84.44421879469800274, 12.09119879402660125, -47.46023938497990002 ) ) ;
#51030=ORIENTED_EDGE ( 'NONE', *, *, #40177, .F. ) ;
#51033=VERTEX_POINT ( 'NONE', #16429 ) ;
#51035=VECTOR ( 'NONE', #22604, 1000.000000000000000 ) ;
#51038=CARTESIAN_POINT ( 'NONE',  ( 76.43497123267530924, -23.65911996861112598, -12.94720032858890235 ) ) ;
#51039=CARTESIAN_POINT ( 'NONE',  ( 8.815605888606221185, -63.28267529256429924, -46.67186389937329949 ) ) ;
#51041=ORIENTED_EDGE ( 'NONE', *, *, #11247, .F. ) ;
#51042=CIRCLE ( 'NONE', #35130, 49.07571608970690846 ) ;
#51044=CARTESIAN_POINT ( 'NONE',  ( 51.65752907925210025, 21.59180590640109898, -54.64640228080400419 ) ) ;
#51048=VECTOR ( 'NONE', #27496, 1000.000000000000000 ) ;
#51050=CARTESIAN_POINT ( 'NONE',  ( 59.95447645319909924, -1.253371738758830123, -15.99147373105880021 ) ) ;
#51051=CARTESIAN_POINT ( 'NONE',  ( 51.65858043925479848, -48.93466924497870707, -76.94737799441629988 ) ) ;
#51052=LINE ( 'NONE', #35578, #10390 ) ;
#51053=ORIENTED_EDGE ( 'NONE', *, *, #44488, .T. ) ;
#51059=CARTESIAN_POINT ( 'NONE',  ( 13.64784227573900033, -51.18487036888380004, -22.24579103685289994 ) ) ;
#51061=CARTESIAN_POINT ( 'NONE',  ( 55.65694285038450317, 13.96926599109930045, -15.18560201429809986 ) ) ;
#51062=CARTESIAN_POINT ( 'NONE',  ( 61.18408626113220805, -45.35865915913219482, -47.22189121640219867 ) ) ;
#51064=EDGE_CURVE ( 'NONE', #12739, #18289, #24519, .T. ) ;
#51068=FACE_OUTER_BOUND ( 'NONE', #2150, .T. ) ;
#51071=CARTESIAN_POINT ( 'NONE',  ( 42.67726216907190206, -45.92311385897509979, -7.341706899958339250 ) ) ;
#51072=CARTESIAN_POINT ( 'NONE',  ( 54.74839138441483755, -47.94984410803592567, -26.69632610202470602 ) ) ;
#51073=CONICAL_SURFACE ( 'NONE', #856, 1.587553672713209574, 1.249045772398249987 ) ;
#51074=CARTESIAN_POINT ( 'NONE',  ( 66.37097987491060280, 13.88381105532070059, -12.87817958664409979 ) ) ;
#51076=VECTOR ( 'NONE', #10259, 1000.000000000000000 ) ;
#51077=CARTESIAN_POINT ( 'NONE',  ( 82.13853704237929776, 13.88381105532070059, -46.37203261889099792 ) ) ;
#51079=CARTESIAN_POINT ( 'NONE',  ( 47.51796364507180215, 23.14532756813578018, -75.00952367038003388 ) ) ;
#51082=CARTESIAN_POINT ( 'NONE',  ( 49.58793114173270311, 22.40222048251530040, -54.62161527680250117 ) ) ;
#51084=CARTESIAN_POINT ( 'NONE',  ( 52.92152590114420718, -49.62269093325190283, -48.88490684695970145 ) ) ;
#51088=CARTESIAN_POINT ( 'NONE',  ( 13.48683992790090080, 20.06883863126540035, -22.27491888996000213 ) ) ;
#51089=DIRECTION ( 'NONE',  ( 0.000000000000000000, 0.000000000000000000, 1.000000000000000000 ) ) ;
#51091=CARTESIAN_POINT ( 'NONE',  ( 53.05395538955789903, 18.35446051233180143, -49.07041595412979262 ) ) ;
#51092=CARTESIAN_POINT ( 'NONE',  ( 55.97242077277940098, -45.56436908181329670, -16.74564425458379802 ) ) ;
#51094=EDGE_LOOP ( 'NONE', ( #48479, #474, #21907, #42219, #15398 ) ) ;
#51097=CIRCLE ( 'NONE', #28483, 20.00000000000000355 ) ;
#51098=FACE_OUTER_BOUND ( 'NONE', #25112, .T. ) ;
#51099=CARTESIAN_POINT ( 'NONE',  ( 10.86442074884469911, 33.79593519927429668, -47.12165869429840370 ) ) ;
#51102=CARTESIAN_POINT ( 'NONE',  ( 52.70698372528335796, -49.76075902929102313, -48.81385732385554377 ) ) ;
#51104=CARTESIAN_POINT ( 'NONE',  ( 53.27996121806150143, -52.13308956689839846, -54.32024439625410395 ) ) ;
#51107=CARTESIAN_POINT ( 'NONE',  ( 10.48585289546009847, -63.13039971493990521, -45.62882785086220139 ) ) ;
#51109=CARTESIAN_POINT ( 'NONE',  ( 68.13393739769819035, 19.47158195952109594, -72.59354914830207406 ) ) ;
#51112=CARTESIAN_POINT ( 'NONE',  ( 57.24507234422829782, 19.38381439976799925, -53.91419826612269617 ) ) ;
#51113=AXIS2_PLACEMENT_3D ( 'NONE', #13235, #13997, #29186 ) ;
#51120=DIRECTION ( 'NONE',  ( 0.000000000000000000, 1.000000000000000000, 0.000000000000000000 ) ) ;
#51122=CARTESIAN_POINT ( 'NONE',  ( 14.62116837088475485, 20.66383147155319122, -75.74021525116816633 ) ) ;
#51124=AXIS2_PLACEMENT_3D ( 'NONE', #2849, #18814, #34794 ) ;
#51126=B_SPLINE_SURFACE_WITH_KNOTS ( 'NONE', 3, 3, ( 
 ( #1131, #37545, #44900, #5338, #9006, #37295, #1393, #17380, #1651, #49363, #13464, #17643, #33609, #14993, #46471, #30959, #26515, #31214, #46991, #23095, #11076, #18150, #46731, #10558 ),
 ( #22324, #2947, #11332, #39114, #6108, #14739, #42531, #6619, #18663, #27991, #38330, #38074, #26774, #22064, #50126, #38858, #15259, #42792, #22583, #6887, #47241, #42265, #27042, #26260 ),
 ( #3208, #38600, #22837, #2691, #50642, #18918, #34637, #6364, #2170, #35158, #19179, #43047, #2420, #30709, #34902, #7143, #14476, #18401, #34115, #14221, #46211, #10815, #30195, #50901 ),
 ( #10296, #51166, #34380, #50392, #30449, #17253, #1003, #9131, #48976, #4157, #32683, #32421, #36371, #24304, #28512, #44509, #1265, #8612, #24827, #12287, #24043, #28248, #13082, #40320 ),
 ( #12814, #13329, #36123, #40835, #33217, #28768, #24561, #44770, #49234, #44246, #17003, #8352, #4416, #12545, #40574, #45031, #40064, #43994, #16210, #4671, #16466, #4934, #20644, #25084 ),
 ( #20382, #36630, #8874, #41098, #48444, #732, #8100, #20131, #48183, #16728, #48710, #5209, #20906, #36903, #32950, #29035, #21162, #37168, #227, #9643, #9399, #13832, #34507, #34235 ),
 ( #2035, #10161, #50514, #22188, #14345, #50258, #49996, #6232, #41868, #41606, #30315, #21668, #14087, #6490, #41348, #25348, #29789, #46337, #38198, #29289, #26376, #2294, #38454, #42393 ),
 ( #49493, #45290, #29545, #25599, #18267, #33729, #5711, #33475, #10424, #22447, #2558, #5465, #21419, #37420, #49742, #30048, #1521, #17506, #13580, #45548, #37941, #37675, #1777, #17758 ) ),
 .UNSPECIFIED., .F., .F., .F.,
 ( 4, 1, 1, 1, 1, 4 ),
 ( 4, 2, 2, 2, 2, 2, 2, 2, 2, 2, 2, 4 ),
 ( -3.746466027699999873E-05, 0.2000000000000000111, 0.4000000000000000222, 0.5999999999999999778, 0.8000000000000000444, 1.000000000000000000 ),
 ( -3.746466027699999873E-05, 0.2627958365207210267, 0.8013173561513319276, 1.332723478065980016, 1.850236617094970004, 2.367749756123960214, 3.156999674831939995, 3.551624634185940099, 4.183024569152329342, 5.193264465098549998, 6.167115316339319975, 6.314004134380339472 ),
 .UNSPECIFIED. ) ;
#51129=CARTESIAN_POINT ( 'NONE',  ( 61.28610861176739633, -45.23040055550220018, -46.37203261889099792 ) ) ;
#51131=VERTEX_POINT ( 'NONE', #49960 ) ;
#51132=ORIENTED_EDGE ( 'NONE', *, *, #34990, .T. ) ;
#51135=CARTESIAN_POINT ( 'NONE',  ( 53.27382404857079479, -49.51603170232989726, -49.18478183594810105 ) ) ;
#51136=CARTESIAN_POINT ( 'NONE',  ( 55.55365748065509734, 13.88381105532070059, -14.32025611302120005 ) ) ;
#51138=FACE_OUTER_BOUND ( 'NONE', #4887, .T. ) ;
#51139=CARTESIAN_POINT ( 'NONE',  ( 61.50409964636570237, 14.14168666559669951, -47.35437808293550432 ) ) ;
#51140=EDGE_CURVE ( 'NONE', #45267, #23479, #50475, .T. ) ;
#51142=CARTESIAN_POINT ( 'NONE',  ( 12.05049839503350029, 33.67281946323389263, -16.21910226667979771 ) ) ;
#51145=CARTESIAN_POINT ( 'NONE',  ( 56.79309010641989630, -50.66781749968460247, -74.34195920670471480 ) ) ;
#51146=CARTESIAN_POINT ( 'NONE',  ( -5.006796579080280196, 16.35122532122439765, -5.448334583328020564 ) ) ;
#51147=CARTESIAN_POINT ( 'NONE',  ( 47.59368629830048292, 23.27965873589448620, -54.68140488027380997 ) ) ;
#51149=CARTESIAN_POINT ( 'NONE',  ( 20.13393739768839552, 24.18330853958629945, -74.14999999999999147 ) ) ;
#51150=CARTESIAN_POINT ( 'NONE',  ( 11.01107138704560029, -65.03344997371249292, -17.34607880264680091 ) ) ;
#51153=CARTESIAN_POINT ( 'NONE',  ( -2.623662900533460185, -48.66391853465049877, -4.296538300593259585 ) ) ;
#51155=CARTESIAN_POINT ( 'NONE',  ( 47.50821162171600065, 23.36490262398820050, -54.98790728447610121 ) ) ;
#51157=CARTESIAN_POINT ( 'NONE',  ( 58.54073765571180132, -45.63607917995849306, -26.46024503793289995 ) ) ;
#51159=CARTESIAN_POINT ( 'NONE',  ( 61.28260267805470107, 14.10897515434229987, -47.23932327355679917 ) ) ;
#51160=CIRCLE ( 'NONE', #28538, 25.00000000000000355 ) ;
#51162=CARTESIAN_POINT ( 'NONE',  ( 51.54546934566289451, 17.72378080735539996, -76.80150978094809489 ) ) ;
#51163=CARTESIAN_POINT ( 'NONE',  ( 52.94089227972619938, 18.37031531951570074, -48.75998158604740240 ) ) ;
#51166=CARTESIAN_POINT ( 'NONE',  ( 52.71556636524050532, 18.49758259741449962, -28.08016480817499883 ) ) ;
#51168=CARTESIAN_POINT ( 'NONE',  ( 57.24929578234380045, 19.38381105828390361, -53.91492796160409284 ) ) ;
#51171=CARTESIAN_POINT ( 'NONE',  ( 65.12655588804669549, -32.00338151092800132, -17.50916650718779977 ) ) ;
#51173=CARTESIAN_POINT ( 'NONE',  ( 11.13393739769619906, 31.90680957093530168, -43.74348518090240390 ) ) ;
#51176=CARTESIAN_POINT ( 'NONE',  ( 60.29344216025802439, -45.37694481291970305, -27.03112392671941322 ) ) ;
#51182=CARTESIAN_POINT ( 'NONE',  ( 56.92872317984839725, -45.28411505133909998, -25.70904297234619662 ) ) ;
#51185=VERTEX_POINT ( 'NONE', #25815 ) ;
#51189=CARTESIAN_POINT ( 'NONE',  ( 41.35567059317689598, -44.75886416236139809, -5.363894289339560473 ) ) ;
#51190=ADVANCED_FACE ( 'NONE', ( #14307 ), #5933, .T. ) ;
#51191=VERTEX_POINT ( 'NONE', #14050 ) ;
#51192=CARTESIAN_POINT ( 'NONE',  ( 46.60731143751889505, -45.11618894467940066, -7.962942859665570694 ) ) ;
#51193=CARTESIAN_POINT ( 'NONE',  ( 51.45118121745367290, 0.8518969343010126538, -17.60358367641750732 ) ) ;
#51195=CARTESIAN_POINT ( 'NONE',  ( 64.73577143960351066, -30.09401345844290177, -16.46742189103860099 ) ) ;
#51198=CARTESIAN_POINT ( 'NONE',  ( 47.24371072983239372, -54.76060195732999603, -74.14999999999999147 ) ) ;
#51202=VECTOR ( 'NONE', #28468, 1000.000000000000000 ) ;
#51203=CARTESIAN_POINT ( 'NONE',  ( 44.26797775832170601, 14.17447024376930109, -7.721004194715090030 ) ) ;
#51204=DIRECTION ( 'NONE',  ( -0.9987374001630935361, 0.000000000000000000, -0.05023550054956103100 ) ) ;
#51205=CARTESIAN_POINT ( 'NONE',  ( 83.48374992014450413, -44.73979101690569848, -46.79909128427029685 ) ) ;
#51206=CARTESIAN_POINT ( 'NONE',  ( 59.40674124460660721, 13.88381117262120057, -25.82779764205569961 ) ) ;
#51209=CARTESIAN_POINT ( 'NONE',  ( 56.55524560877629625, -46.21195526465520231, -26.26695727885629950 ) ) ;
#51210=CARTESIAN_POINT ( 'NONE',  ( 8.291970543062280541, -62.33611482735770437, -15.32312980843789951 ) ) ;
#51211=CARTESIAN_POINT ( 'NONE',  ( 75.24914379931091446, -35.01601405374659493, -12.30266221336199983 ) ) ;
#51213=CARTESIAN_POINT ( 'NONE',  ( 75.11247970983615119, 13.77271509087269408, -14.67931599322431957 ) ) ;
#51214=DIRECTION ( 'NONE',  ( 0.000000000000000000, -1.000000000000000000, 0.000000000000000000 ) ) ;
#51216=CARTESIAN_POINT ( 'NONE',  ( 8.133937397696209715, -54.80802482921019703, -21.14999999999999858 ) ) ;
#51217=ADVANCED_FACE ( 'NONE', ( #9359 ), #30011, .F. ) ;
#51218=CARTESIAN_POINT ( 'NONE',  ( 82.48251884290169755, -45.34700424204849867, -47.31937152333360075 ) ) ;
#51219=CARTESIAN_POINT ( 'NONE',  ( 57.55751162049190128, -50.61618894467939356, -53.92796738110899923 ) ) ;
#51220=CARTESIAN_POINT ( 'NONE',  ( 41.41708261413649694, 13.08600793429160092, -4.679819212124120220 ) ) ;
#51221=CARTESIAN_POINT ( 'NONE',  ( 0.5406133260286609676, 12.32747302715160131, -20.15000000000000213 ) ) ;
#51223=CARTESIAN_POINT ( 'NONE',  ( 55.55538329330519787, -48.25727492885060599, -48.41463972625499679 ) ) ;
#51224=CARTESIAN_POINT ( 'NONE',  ( 14.55219295556159409, -51.70197612871098869, -75.56421430877743717 ) ) ;
#51226=CARTESIAN_POINT ( 'NONE',  ( 66.66073096664889874, -1.315816564741499883, -17.00118905793410207 ) ) ;
#51227=CARTESIAN_POINT ( 'NONE',  ( 17.74852555148360267, -51.60940715663139855, -75.47164421335219231 ) ) ;
#51228=B_SPLINE_CURVE_WITH_KNOTS ( 'NONE', 3,
 ( #36484, #40427, #24675, #7706, #16324, #589, #40688, #32529, #3773, #28618, #19739, #36743, #4269, #12147, #28101, #850, #8208, #4521, #47792, #35732, #11898, #32796 ),
 .UNSPECIFIED., .F., .F.,
 ( 4, 2, 2, 2, 2, 2, 2, 1, 2, 2, 1, 4 ),
 ( 0.000000000000000000, 0.1311013905112042854, 0.1966520857668051792, 0.2294274333946048072, 0.2622027810224044075, 0.3933041715336068056, 0.4588548667892080601, 0.4916302144170072164, 0.4998240513239579075, 0.5039209697774372776, 0.5080178882309165367, 0.5244055620448262456 ),
 .UNSPECIFIED. ) ;
#51229=CARTESIAN_POINT ( 'NONE',  ( 41.17242569490439763, -45.11618894467940066, -6.491241765574168987 ) ) ;
#51230=EDGE_CURVE ( 'NONE', #38024, #13386, #20, .T. ) ;
#51241=CARTESIAN_POINT ( 'NONE',  ( 40.85470386722510483, -45.35371597153389445, -5.792869590957399950 ) ) ;
#51243=CARTESIAN_POINT ( 'NONE',  ( 17.77325585800819852, 21.34486587698399873, -76.03043890231919022 ) ) ;
#51248=CARTESIAN_POINT ( 'NONE',  ( 17.41829529840355306, -14.68304830863572619, -11.23251175440650051 ) ) ;
#51251=DIRECTION ( 'NONE',  ( -1.000000000000000000, -0.000000000000000000, -0.000000000000000000 ) ) ;
#51252=EDGE_LOOP ( 'NONE', ( #1485, #23478, #10451, #44863, #28176 ) ) ;
#51254=DIRECTION ( 'NONE',  ( 1.000000000000000000, 0.000000000000000000, 0.000000000000000000 ) ) ;
#51255=VERTEX_POINT ( 'NONE', #35773 ) ;
#51257=CARTESIAN_POINT ( 'NONE',  ( 52.75030668772299691, -51.36013153243110452, -75.83477191552309193 ) ) ;
#51258=CARTESIAN_POINT ( 'NONE',  ( 60.38681717586829478, 14.58921176390859920, -47.68186590178469686 ) ) ;
#51260=CARTESIAN_POINT ( 'NONE',  ( -10.87940544930430065, 11.11767143334649965, -6.276159589371210323 ) ) ;
#51261=AXIS2_PLACEMENT_3D ( 'NONE', #43064, #39385, #15012 ) ;
#51263=CARTESIAN_POINT ( 'NONE',  ( 46.80617081706476768, 22.71927041949727766, -75.82639806882809808 ) ) ;
#51267=CARTESIAN_POINT ( 'NONE',  ( 59.94414702407019746, 14.70111394113749981, -47.28272102067069937 ) ) ;
#51268=CARTESIAN_POINT ( 'NONE',  ( 16.13393739769620083, -15.61618894467929941, -17.93019253464870033 ) ) ;
#51271=CARTESIAN_POINT ( 'NONE',  ( 13.86889551668940079, 19.40587202548489998, -21.27403962367360180 ) ) ;
#51274=CARTESIAN_POINT ( 'NONE',  ( 61.44121465274793081, 14.11489996882993481, -47.30179314246718292 ) ) ;
#51275=CARTESIAN_POINT ( 'NONE',  ( 48.76069114195910714, -54.05633143203520063, -55.20115406384710610 ) ) ;
#51277=EDGE_CURVE ( 'NONE', #15326, #26727, #38518, .T. ) ;
#51279=CARTESIAN_POINT ( 'NONE',  ( 47.68893187850459725, 23.28158913229470173, -55.10584722141680203 ) ) ;
#51281=ORIENTED_EDGE ( 'NONE', *, *, #45663, .F. ) ;
#51286=CARTESIAN_POINT ( 'NONE',  ( 60.52894022340500157, 14.10979985953984261, -27.14274995353532915 ) ) ;
#51287=CARTESIAN_POINT ( 'NONE',  ( 82.78853260243879220, 13.78813726657122807, -46.36933949695569623 ) ) ;
#51288=CARTESIAN_POINT ( 'NONE',  ( 83.76205119356160367, 13.76116822878180024, -47.48604701470450351 ) ) ;
#51293=ORIENTED_EDGE ( 'NONE', *, *, #11247, .T. ) ;
#51297=CARTESIAN_POINT ( 'NONE',  ( 73.38393739769610136, -15.61618894467929941, -84.94863984844540994 ) ) ;
#51300=CARTESIAN_POINT ( 'NONE',  ( 76.42687394393672662, -22.88878007474863452, -12.91230967307213007 ) ) ;
#51301=CARTESIAN_POINT ( 'NONE',  ( 12.90826365979919998, -65.51213270651270193, -47.70124197908979369 ) ) ;
#51303=ORIENTED_EDGE ( 'NONE', *, *, #1477, .F. ) ;
#51304=VERTEX_POINT ( 'NONE', #15082 ) ;
#51308=CARTESIAN_POINT ( 'NONE',  ( 56.42320082141079496, -50.66862966398220181, -53.17468687661730797 ) ) ;
#51311=CARTESIAN_POINT ( 'NONE',  ( 63.40479749674490506, -0.6709863343795420265, -16.43330761011030106 ) ) ;
#51312=CARTESIAN_POINT ( 'NONE',  ( 52.22857431453279276, -49.81596975065740196, -77.10487740174859539 ) ) ;
#51313=DIRECTION ( 'NONE',  ( 1.000000000000000000, 0.000000000000000000, 0.000000000000000000 ) ) ;
#51320=CARTESIAN_POINT ( 'NONE',  ( 13.79563961991189913, -50.43795090918690249, -21.08562558917969909 ) ) ;
#51322=CARTESIAN_POINT ( 'NONE',  ( 57.21115044914409964, 19.38381105532069881, -74.41047019428449971 ) ) ;
#51324=CARTESIAN_POINT ( 'NONE',  ( 56.95254701797419727, 13.89618346210419908, -16.49528551305159851 ) ) ;
#51326=CARTESIAN_POINT ( 'NONE',  ( 56.70659705506859893, -50.55677919107559859, -53.10139024712660216 ) ) ;
#51329=VERTEX_POINT ( 'NONE', #50727 ) ;
#51330=CARTESIAN_POINT ( 'NONE',  ( 11.73319001777203674, -65.42240559785102505, -18.17421237900516573 ) ) ;
#51333=CIRCLE ( 'NONE', #6971, 3.799999999999829736 ) ;
#51336=CARTESIAN_POINT ( 'NONE',  ( 51.93064585340319894, 13.88381105532070059, -9.012777190992919074 ) ) ;
#51337=CARTESIAN_POINT ( 'NONE',  ( 46.97184464991040187, -53.68621135916810516, -75.90842213619210099 ) ) ;
#51338=CARTESIAN_POINT ( 'NONE',  ( 10.74148174184799842, 33.72025021587940330, -18.12706498523149889 ) ) ;
#51340=DIRECTION ( 'NONE',  ( 0.3805321250008310008, 0.000000000000000000, -0.9247677015566404535 ) ) ;
#51341=CARTESIAN_POINT ( 'NONE',  ( 11.37984272568584565, 33.25260846225116751, -24.02068460187723531 ) ) ;
#51343=CARTESIAN_POINT ( 'NONE',  ( -9.957798083463760719, -43.31361333265569868, -6.454122150048999806 ) ) ;
#51344=CARTESIAN_POINT ( 'NONE',  ( 49.50151222301030174, 22.34932762003050044, -54.38302206046260068 ) ) ;
#51345=VERTEX_POINT ( 'NONE', #31051 ) ;
#51346=CARTESIAN_POINT ( 'NONE',  ( 52.68730831268639747, -49.75855573695199752, -48.67468093701120324 ) ) ;
#51349=DIRECTION ( 'NONE',  ( 0.000000000000000000, 0.000000000000000000, -1.000000000000000000 ) ) ;
#51350=CARTESIAN_POINT ( 'NONE',  ( 13.79433266918769974, 20.04646218605449803, -22.92985858714899905 ) ) ;
#51351=CARTESIAN_POINT ( 'NONE',  ( 52.25096198472439823, -49.77129323599559996, -77.19024164398209109 ) ) ;
#51353=CARTESIAN_POINT ( 'NONE',  ( 52.57474326386780206, 18.61928770101469865, -48.47378032971769812 ) ) ;
#51354=CARTESIAN_POINT ( 'NONE',  ( 55.91594474632509559, -45.90466738476499842, -17.78184253245080271 ) ) ;
#51359=VERTEX_POINT ( 'NONE', #42616 ) ;
#51360=CARTESIAN_POINT ( 'NONE',  ( 11.55844482067919898, -65.17238045331160379, -16.94284742230230023 ) ) ;
#51361=CARTESIAN_POINT ( 'NONE',  ( 11.86093866196219970, 34.13069104538590182, -47.45833196181009583 ) ) ;
#51364=DIRECTION ( 'NONE',  ( 0.000000000000000000, 1.000000000000000000, 0.000000000000000000 ) ) ;
#51365=DIRECTION ( 'NONE',  ( 1.000000000000000000, 0.000000000000000000, 0.000000000000000000 ) ) ;
#51366=EDGE_LOOP ( 'NONE', ( #25169, #35437, #17139, #17973, #24801 ) ) ;
#51368=CARTESIAN_POINT ( 'NONE',  ( 11.13393739769619906, -63.30209769551670007, -43.74698219623469697 ) ) ;
#51369=DIRECTION ( 'NONE',  ( 0.8732394366197182567, 0.4872913772396111343, 1.665334536937735304E-16 ) ) ;
#51374=CARTESIAN_POINT ( 'NONE',  ( 31.25349618544100139, -15.61618894467929763, -6.721843382729280059 ) ) ;
#51377=AXIS2_PLACEMENT_3D ( 'NONE', #36097, #40039, #4130 ) ;
#51380=CARTESIAN_POINT ( 'NONE',  ( 83.23750471064099088, -44.81947890601180262, -46.42261246043593559 ) ) ;
#51383=CARTESIAN_POINT ( 'NONE',  ( 53.53273701459760048, -33.11618894467940066, -56.74709961107230782 ) ) ;
#51386=ORIENTED_EDGE ( 'NONE', *, *, #15557, .T. ) ;
#51390=CARTESIAN_POINT ( 'NONE',  ( 50.03007040746459921, -48.76509257287760590, -76.14999999999999147 ) ) ;
#51393=CARTESIAN_POINT ( 'NONE',  ( 46.35275103504439898, 21.67755452994670406, -76.14999999999999147 ) ) ;
#51394=CARTESIAN_POINT ( 'NONE',  ( 41.64265090550279780, -46.42699119286230314, -4.296538310234280011 ) ) ;
#51395=PLANE ( 'NONE',  #23846 ) ;
#51396=CARTESIAN_POINT ( 'NONE',  ( 11.92234616937149916, 33.79182978746079868, -16.43998781664420150 ) ) ;
#51398=CARTESIAN_POINT ( 'NONE',  ( 55.01074116390060453, -47.06068843752029807, -25.62222821926209804 ) ) ;
#51399=CARTESIAN_POINT ( 'NONE',  ( 57.13447189169250606, -50.61839380715989734, -74.40093450475029613 ) ) ;
#51400=CARTESIAN_POINT ( 'NONE',  ( -2.611054804631980364, 19.76244294662099676, -8.524286943195571453 ) ) ;
#51401=CARTESIAN_POINT ( 'NONE',  ( 10.47385409520754784, -55.21366976880749888, -45.62050209441289894 ) ) ;
#51406=B_SPLINE_CURVE_WITH_KNOTS ( 'NONE', 3,
 ( #26837, #43614, #34436, #2746, #7717, #18717 ),
 .UNSPECIFIED., .F., .F.,
 ( 4, 2, 4 ),
 ( 0.000000000000000000, 0.4606906889216966228, 1.000000000000000000 ),
 .UNSPECIFIED. ) ;
#51410=CARTESIAN_POINT ( 'NONE',  ( 53.13650397927179370, -49.50020675881640386, -48.81774254784100009 ) ) ;
#51412=CARTESIAN_POINT ( 'NONE',  ( 47.66026032047859928, 23.29152205301619816, -55.04550996317009748 ) ) ;
#51413=CARTESIAN_POINT ( 'NONE',  ( 60.37605544241890243, -45.23483286569010176, -26.84318989901830221 ) ) ;
#51415=CARTESIAN_POINT ( 'NONE',  ( 61.10200072402039240, 14.51600081101689987, -47.83148716568879877 ) ) ;
#51417=EDGE_CURVE ( 'NONE', #12711, #33975, #28492, .T. ) ;
#51418=CARTESIAN_POINT ( 'NONE',  ( 51.59666223323370104, 18.72863052202810152, -76.48753527057338886 ) ) ;
#51419=CARTESIAN_POINT ( 'NONE',  ( 53.39565654316790244, 18.13205158027290054, -48.78219270784469330 ) ) ;
#51422=CARTESIAN_POINT ( 'NONE',  ( 50.84162296648852220, 4.268840990914108069, -76.32020521981469585 ) ) ;
#51424=FACE_OUTER_BOUND ( 'NONE', #10897, .T. ) ;
#51426=CARTESIAN_POINT ( 'NONE',  ( 59.04060495528540287, -28.42300215364210203, -15.65182665779249760 ) ) ;
#51428=CARTESIAN_POINT ( 'NONE',  ( 11.13393739769619906, 31.92895765439750377, -43.91250086627189120 ) ) ;
#51432=EDGE_LOOP ( 'NONE', ( #51852, #17765, #10632, #9109, #11518 ) ) ;
#51434=VECTOR ( 'NONE', #33047, 1000.000000000000000 ) ;
#51435=DIRECTION ( 'NONE',  ( 0.000000000000000000, -1.784214116308896674E-11, -1.000000000000000000 ) ) ;
#51436=CARTESIAN_POINT ( 'NONE',  ( 51.09505050758819777, 0.2955707463199704899, -16.99481687198596092 ) ) ;
#51437=ORIENTED_EDGE ( 'NONE', *, *, #27186, .T. ) ;
#51439=CARTESIAN_POINT ( 'NONE',  ( 11.69948082737000128, -64.91643855301771282, -45.13443972449930186 ) ) ;
#51441=VERTEX_POINT ( 'NONE', #43388 ) ;
#51444=CARTESIAN_POINT ( 'NONE',  ( 11.46164187755220176, 33.11604602725170565, -24.23493799255319914 ) ) ;
#51446=ORIENTED_EDGE ( 'NONE', *, *, #30870, .F. ) ;
#51451=CARTESIAN_POINT ( 'NONE',  ( 61.53134167473509564, -29.71365059239380102, -16.03273234134309888 ) ) ;
#51453=CARTESIAN_POINT ( 'NONE',  ( 47.11382581093260313, -54.35277270616690259, -75.35700034530711378 ) ) ;
#51455=CARTESIAN_POINT ( 'NONE',  ( 35.69765375167399668, -15.61618894467929941, 7.849999999999999645 ) ) ;
#51456=ADVANCED_FACE ( 'NONE', ( #39458 ), #3555, .T. ) ;
#51457=CARTESIAN_POINT ( 'NONE',  ( 45.32091059241599851, 14.34211425166129850, -8.659579894684350521 ) ) ;
#51458=CARTESIAN_POINT ( 'NONE',  ( 15.05440318628110141, 21.88381105532300097, -76.14999999999999147 ) ) ;
#51459=CARTESIAN_POINT ( 'NONE',  ( 83.75509190357360012, -44.57363762736590473, -46.98971415009500419 ) ) ;
#51463=CARTESIAN_POINT ( 'NONE',  ( -2.623662905471100260, -48.66391853184789795, -4.296538310234220504 ) ) ;
#51465=CARTESIAN_POINT ( 'NONE',  ( 15.45245043279190078, -50.80479114967339882, -20.50565891244549732 ) ) ;
#51466=CARTESIAN_POINT ( 'NONE',  ( 75.89808373934218366, -34.96973134563179997, -12.58107089590020067 ) ) ;
#51472=CARTESIAN_POINT ( 'NONE',  ( 82.25187930537960312, -45.11682425727330070, -46.44925488524950197 ) ) ;
#51473=CARTESIAN_POINT ( 'NONE',  ( 57.55751162049750036, -50.61618894467939356, -53.87300832422299379 ) ) ;
#51474=CARTESIAN_POINT ( 'NONE',  ( 42.16594883133879534, 12.74031567877150017, -4.735301441621479590 ) ) ;
#51475=ADVANCED_FACE ( 'NONE', ( #20279 ), #35200, .F. ) ;
#51479=CARTESIAN_POINT ( 'NONE',  ( 68.13393739769841773, -50.61618894467878960, -73.25000000000220268 ) ) ;
#51481=CARTESIAN_POINT ( 'NONE',  ( 18.52893073613670083, -52.05919180694159820, -75.36996982820370761 ) ) ;
#51482=CARTESIAN_POINT ( 'NONE',  ( 53.58981775341219844, -43.47668491205899954, -7.400685398707020468 ) ) ;
#51485=FACE_OUTER_BOUND ( 'NONE', #12537, .T. ) ;
#51486=ORIENTED_EDGE ( 'NONE', *, *, #26777, .F. ) ;
#51487=CYLINDRICAL_SURFACE ( 'NONE', #20045, 1.999999999999997113 ) ;
#51493=CARTESIAN_POINT ( 'NONE',  ( 18.27939235371979976, 20.97417580057950204, -75.67041253543310120 ) ) ;
#51496=EDGE_CURVE ( 'NONE', #29113, #7609, #49163, .T. ) ;
#51497=CARTESIAN_POINT ( 'NONE',  ( -5.366062602303915519, -15.61618894467939889, -10.44999999999999929 ) ) ;
#51504=CARTESIAN_POINT ( 'NONE',  ( 82.13853704237929776, 14.40950277491920062, -47.72348187592560009 ) ) ;
#51506=CARTESIAN_POINT ( 'NONE',  ( 17.92370450339669929, -52.11618894467930119, -76.14999999999999147 ) ) ;
#51509=CARTESIAN_POINT ( 'NONE',  ( 51.55044215929650164, -51.25128868776180013, -76.08578283986020097 ) ) ;
#51510=CARTESIAN_POINT ( 'NONE',  ( 60.58512182557269909, 14.48389043468630000, -47.62866706370459724 ) ) ;
#51514=CARTESIAN_POINT ( 'NONE',  ( 41.50224532540739375, -43.90848951166579894, -3.489448901339209819 ) ) ;
#51516=CARTESIAN_POINT ( 'NONE',  ( -6.905748412548989634, 14.77189088641519987, -5.492407866796149563 ) ) ;
#51521=CARTESIAN_POINT ( 'NONE',  ( 55.00867404205050093, 17.28694651894000245, -48.28813249775050309 ) ) ;
#51522=CARTESIAN_POINT ( 'NONE',  ( 43.61538151352439741, 14.80464860828879914, -8.020992654718998693 ) ) ;
#51528=CARTESIAN_POINT ( 'NONE',  ( 68.13393739769620083, 19.38381105532069881, -67.99999999999998579 ) ) ;
#51532=CARTESIAN_POINT ( 'NONE',  ( 48.51115049231150067, -54.01384098269380019, -54.58190071400479582 ) ) ;
#51533=AXIS2_PLACEMENT_3D ( 'NONE', #12023, #39539, #3126 ) ;
#51536=CARTESIAN_POINT ( 'NONE',  ( 47.75491787206179595, 23.24500768174080179, -55.00204154977200233 ) ) ;
#51542=CARTESIAN_POINT ( 'NONE',  ( 60.63631542821100595, -45.63186250400350019, -47.47615296169890087 ) ) ;
#51543=CARTESIAN_POINT ( 'NONE',  ( 48.21566362429802410, -54.17964390236606675, -54.67775470772499347 ) ) ;
#51546=CARTESIAN_POINT ( 'NONE',  ( 74.17629866868290378, -43.11618894467930119, -65.34607522167520699 ) ) ;
#51548=EDGE_LOOP ( 'NONE', ( #13665, #36929, #10264, #17486, #19374, #51437, #5994, #50669, #28272, #34042 ) ) ;
#51551=PLANE ( 'NONE',  #20258 ) ;
#51552=CARTESIAN_POINT ( 'NONE',  ( 7.517033938252880354, -61.58399597082019739, -19.14999999999999858 ) ) ;
#51554=CARTESIAN_POINT ( 'NONE',  ( 9.286360118224829208, -63.91023846612779380, -46.69215455456279784 ) ) ;
#51559=CARTESIAN_POINT ( 'NONE',  ( 56.48879402914270287, -50.71168639969660319, -53.39119800914449598 ) ) ;
#51561=CARTESIAN_POINT ( 'NONE',  ( 61.99554605869259660, -0.5193312204098330387, -16.39842119712499979 ) ) ;
#51562=CARTESIAN_POINT ( 'NONE',  ( 51.63757889171279913, -49.63238467538800336, -76.65049610660180690 ) ) ;
#51566=CYLINDRICAL_SURFACE ( 'NONE', #23393, 1.999999999999997113 ) ;
#51573=CARTESIAN_POINT ( 'NONE',  ( 13.18306315670809958, -50.33123850494190066, -21.16866690708240029 ) ) ;
#51574=CARTESIAN_POINT ( 'NONE',  ( 55.84450736765219858, 19.38381105532069881, -76.10951658791620389 ) ) ;
#51575=DIRECTION ( 'NONE',  ( -0.05023550054956202326, 0.000000000000000000, -0.9987374001630934250 ) ) ;
#51576=EDGE_CURVE ( 'NONE', #483, #13261, #27881, .T. ) ;
#51577=CARTESIAN_POINT ( 'NONE',  ( 65.43042069957887463, -49.21324915460706961, -70.54648330188271643 ) ) ;
#51578=CARTESIAN_POINT ( 'NONE',  ( 61.00628429235199945, -45.37700835658660736, -46.89453324795130129 ) ) ;
#51583=CARTESIAN_POINT ( 'NONE',  ( 11.89321892217540011, -65.43602743108330344, -18.17421237901570308 ) ) ;
#51586=LINE ( 'NONE', #24026, #17135 ) ;
#51592=CARTESIAN_POINT ( 'NONE',  ( 11.13393739770549828, 31.88334419040860013, -48.70288603379470516 ) ) ;
#51593=CARTESIAN_POINT ( 'NONE',  ( 69.63393739769620083, -38.11618894467930119, -73.25000000000000000 ) ) ;
#51596=EDGE_CURVE ( 'NONE', #40337, #45245, #4224, .T. ) ;
#51598=CARTESIAN_POINT ( 'NONE',  ( 49.33374094960719702, 22.48211379487710104, -54.59177036145960216 ) ) ;
#51600=CARTESIAN_POINT ( 'NONE',  ( 52.66298673388549645, -49.77964374310990081, -48.68532682492069341 ) ) ;
#51606=CARTESIAN_POINT ( 'NONE',  ( 84.37071767335301331, 12.21453624936390092, -47.23470317516540007 ) ) ;
#51608=DIRECTION ( 'NONE',  ( 0.000000000000000000, 0.000000000000000000, 1.000000000000000000 ) ) ;
#51609=CARTESIAN_POINT ( 'NONE',  ( 57.12685297953459695, -45.12805850059309876, -16.97874220678049895 ) ) ;
#51610=CARTESIAN_POINT ( 'NONE',  ( 11.13393739769619906, -63.52234720672429802, -24.14942632405960055 ) ) ;
#51615=CARTESIAN_POINT ( 'NONE',  ( 11.79333632018079925, -65.42240134614850433, -17.82631581233690099 ) ) ;
#51616=CARTESIAN_POINT ( 'NONE',  ( 10.32625535581710174, 32.28964825586200504, -45.85549233471310515 ) ) ;
#51619=CARTESIAN_POINT ( 'NONE',  ( 8.804713206766638933, 31.98843531701869836, -46.67024040703379484 ) ) ;
#51623=CARTESIAN_POINT ( 'NONE',  ( 11.13393739769619906, -63.38752784187269640, -43.91920917233640154 ) ) ;
#51624=AXIS2_PLACEMENT_3D ( 'NONE', #11639, #43859, #42842 ) ;
#51625=CARTESIAN_POINT ( 'NONE',  ( 68.13393739769819035, 19.47158195952109594, -72.59354914830207406 ) ) ;
#51627=CARTESIAN_POINT ( 'NONE',  ( 68.23750916396743094, -31.42880183748190959, -18.38207368453976187 ) ) ;
#51628=CARTESIAN_POINT ( 'NONE',  ( 56.76664444808910304, 19.44233945464709734, -53.84360320718689508 ) ) ;
#51629=CARTESIAN_POINT ( 'NONE',  ( 52.27433152305400199, 18.55914638219779889, -77.19764549399749853 ) ) ;
#51632=CARTESIAN_POINT ( 'NONE',  ( 51.55044211529342135, 20.01891078301827775, -76.08578284841361494 ) ) ;
#51635=CARTESIAN_POINT ( 'NONE',  ( 57.88659593186079633, 17.67030499234060059, -51.07754743084770155 ) ) ;
#51637=EDGE_CURVE ( 'NONE', #9653, #41755, #20023, .T. ) ;
#51642=ORIENTED_EDGE ( 'NONE', *, *, #27500, .T. ) ;
#51644=CARTESIAN_POINT ( 'NONE',  ( 53.02879415315700129, -49.61082998701090219, -49.09627670324169202 ) ) ;
#51648=CARTESIAN_POINT ( 'NONE',  ( 47.18785506009880493, 23.26044294672620083, -75.11690455987650239 ) ) ;
#51649=DIRECTION ( 'NONE',  ( 0.3294064756441309472, 0.9441882088883087887, 3.053113317719179500E-16 ) ) ;
#51651=CARTESIAN_POINT ( 'NONE',  ( 12.04145588158159974, 33.83966319556200375, -16.48289738545560112 ) ) ;
#51653=EDGE_CURVE ( 'NONE', #39898, #26913, #44139, .T. ) ;
#51654=CARTESIAN_POINT ( 'NONE',  ( 52.61990787174079998, -49.80354421666699949, -27.74322489265380298 ) ) ;
#51655=CARTESIAN_POINT ( 'NONE',  ( 56.50763749952780302, -50.63556182365589819, -75.24339335911510318 ) ) ;
#51656=CARTESIAN_POINT ( 'NONE',  ( 1.322326434189930122, 22.25801372082519691, -7.691437081604280301 ) ) ;
#51661=CARTESIAN_POINT ( 'NONE',  ( 61.28671122457539866, 13.99937605583419931, -46.63577450329929519 ) ) ;
#51664=CARTESIAN_POINT ( 'NONE',  ( 53.20760851556250515, -49.46295310004039436, -48.79936141346989587 ) ) ;
#51665=CARTESIAN_POINT ( 'NONE',  ( 59.87633579703659592, -45.40677854013640058, -26.81043307918650243 ) ) ;
#51667=CARTESIAN_POINT ( 'NONE',  ( 61.30642482279199612, 14.15530932967999966, -47.35784862597040501 ) ) ;
#51669=CARTESIAN_POINT ( 'NONE',  ( 52.11523513670289276, 18.63129512089459894, -76.92610540732999880 ) ) ;
#51670=CARTESIAN_POINT ( 'NONE',  ( 52.98105868624149650, 18.35548441844140299, -48.88375723731650169 ) ) ;
#51672=CARTESIAN_POINT ( 'NONE',  ( 53.41693480158270546, -49.35328119387190071, -48.75416851881869462 ) ) ;
#51673=ORIENTED_EDGE ( 'NONE', *, *, #13678, .T. ) ;
#51675=CARTESIAN_POINT ( 'NONE',  ( 47.65034348264629926, -54.52133088470490208, -54.93304805868889673 ) ) ;
#51678=CARTESIAN_POINT ( 'NONE',  ( 64.37958960603660330, -32.00321536173649406, -17.48880570145399815 ) ) ;
#51684=SPHERICAL_SURFACE ( 'NONE', #44368, 3.000000000000159872 ) ;
#51685=ORIENTED_EDGE ( 'NONE', *, *, #9685, .F. ) ;
#51686=ORIENTED_EDGE ( 'NONE', *, *, #41882, .T. ) ;
#51687=CARTESIAN_POINT ( 'NONE',  ( 56.95883372640280129, 19.02269652816849899, -52.69722348556799574 ) ) ;
#51688=DIRECTION ( 'NONE',  ( 0.3294064756440925335, -0.9441882088883221114, -3.330669073875470607E-16 ) ) ;
#51690=CARTESIAN_POINT ( 'NONE',  ( 12.17133826609699909, -65.27733561067250889, -46.10644761563530380 ) ) ;
#51693=CARTESIAN_POINT ( 'NONE',  ( 11.39514780622933721, 34.02490255884188741, -22.76376844004561306 ) ) ;
#51697=EDGE_CURVE ( 'NONE', #23772, #17962, #37713, .T. ) ;
#51701=CARTESIAN_POINT ( 'NONE',  ( 62.83001711768829267, -30.40726919850919785, -16.32748532433430100 ) ) ;
#51703=CARTESIAN_POINT ( 'NONE',  ( 85.66799001034409855, -48.61618894467930119, -61.58097075742929860 ) ) ;
#51706=CARTESIAN_POINT ( 'NONE',  ( 43.16103038202970055, 14.52412741791340167, -7.511464010228710464 ) ) ;
#51707=CARTESIAN_POINT ( 'NONE',  ( 14.91722740704980055, 21.75175735174070013, -76.14999999999999147 ) ) ;
#51708=CARTESIAN_POINT ( 'NONE',  ( 83.51014914612841267, -44.78785608086950276, -46.95038033932869581 ) ) ;
#51714=CARTESIAN_POINT ( 'NONE',  ( 14.17150143963580078, -50.41474702392260099, -20.90975112687990034 ) ) ;
#51716=CARTESIAN_POINT ( 'NONE',  ( 61.75019796695539753, -45.11618894467940066, -46.37203261889099792 ) ) ;
#51717=EDGE_CURVE ( 'NONE', #29806, #25078, #33637, .T. ) ;
#51720=CARTESIAN_POINT ( 'NONE',  ( -5.738263256628330033, -47.06162393351850426, -5.576567369078139436 ) ) ;
#51721=CARTESIAN_POINT ( 'NONE',  ( 47.21574955295219667, 23.54913593804809935, -54.62186942783370114 ) ) ;
#51724=CARTESIAN_POINT ( 'NONE',  ( 57.55751162062720283, -50.12763441343680171, -52.61703142046619774 ) ) ;
#51725=CARTESIAN_POINT ( 'NONE',  ( 42.60880854190150302, 12.70305552983409925, -4.906336349105670180 ) ) ;
#51728=DIRECTION ( 'NONE',  ( 0.000000000000000000, 8.635067969306036542E-13, 1.000000000000000000 ) ) ;
#51731=CARTESIAN_POINT ( 'NONE',  ( 17.21347160910390173, -53.11618894467930119, -76.14999999999999147 ) ) ;
#51733=CARTESIAN_POINT ( 'NONE',  ( 15.67961730780073282, 19.63028885021686776, -20.20261264479897179 ) ) ;
#51734=CARTESIAN_POINT ( 'NONE',  ( 54.21268375596449829, -52.70726339247860182, -55.25757456134129342 ) ) ;
#51735=ORIENTED_EDGE ( 'NONE', *, *, #2738, .F. ) ;
#51743=CARTESIAN_POINT ( 'NONE',  ( 17.82930383619740056, 21.38897561371040013, -76.01805773991210913 ) ) ;
#51745=VERTEX_POINT ( 'NONE', #10065 ) ;
#51746=CARTESIAN_POINT ( 'NONE',  ( 56.99379046497180212, -45.91441743241509243, -26.24653381559409837 ) ) ;
#51749=AXIS2_PLACEMENT_3D ( 'NONE', #40345, #15987, #3942 ) ;
#51750=EDGE_LOOP ( 'NONE', ( #27907, #46104, #15117, #48868 ) ) ;
#51752=VERTEX_POINT ( 'NONE', #26290 ) ;
#51754=EDGE_CURVE ( 'NONE', #2432, #35705, #6744, .T. ) ;
#51756=ORIENTED_EDGE ( 'NONE', *, *, #2197, .F. ) ;
#51757=ORIENTED_EDGE ( 'NONE', *, *, #32784, .F. ) ;
#51758=EDGE_CURVE ( 'NONE', #24567, #36534, #50157, .T. ) ;
#51761=CARTESIAN_POINT ( 'NONE',  ( 60.73162164295760590, 14.50084501932449932, -47.73368171119290082 ) ) ;
#51762=EDGE_CURVE ( 'NONE', #1516, #18021, #3379, .T. ) ;
#51765=CARTESIAN_POINT ( 'NONE',  ( 41.27829218924360077, -44.10783499397969365, -3.596739496640999789 ) ) ;
#51766=CARTESIAN_POINT ( 'NONE',  ( -10.88316963630090051, 11.11373587982220101, -6.260756294843470293 ) ) ;
#51768=CARTESIAN_POINT ( 'NONE',  ( 60.53218407266430034, 14.08784413439149930, -27.12214479265229983 ) ) ;
#51772=CARTESIAN_POINT ( 'NONE',  ( 41.83246392257819934, 14.51853978555750224, -6.687642457104619353 ) ) ;
#51773=CARTESIAN_POINT ( 'NONE',  ( 11.79571167639570106, 33.77864909481949951, -45.51356534913389851 ) ) ;
#51777=AXIS2_PLACEMENT_3D ( 'NONE', #37066, #384, #12441 ) ;
#51781=CARTESIAN_POINT ( 'NONE',  ( 61.05617857231141699, 14.11849002744650861, -46.88538215577281676 ) ) ;
#51782=CARTESIAN_POINT ( 'NONE',  ( 48.59175220363999870, -54.13008784871289691, -55.28206484397910003 ) ) ;
#51783=FACE_OUTER_BOUND ( 'NONE', #739, .T. ) ;
#51784=CARTESIAN_POINT ( 'NONE',  ( 58.92073384691924076, -2.788940267406039730, -15.64999999999991687 ) ) ;
#51791=CARTESIAN_POINT ( 'NONE',  ( 60.74032281998740501, -45.58551599716069802, -47.45715664104950093 ) ) ;
#51796=ADVANCED_FACE ( 'NONE', ( #9554 ), #39368, .F. ) ;
#51799=ORIENTED_EDGE ( 'NONE', *, *, #39411, .F. ) ;
#51800=DIRECTION ( 'NONE',  ( 0.000000000000000000, -1.000000000000000000, 0.000000000000000000 ) ) ;
#51804=CARTESIAN_POINT ( 'NONE',  ( 12.13393739769600010, -55.41568642894409180, -23.15000000000000213 ) ) ;
#51805=CARTESIAN_POINT ( 'NONE',  ( 76.39120699412700333, -16.72954576041491492, -12.75862843308438244 ) ) ;
#51806=CIRCLE ( 'NONE', #9126, 2.999999999999997780 ) ;
#51809=CARTESIAN_POINT ( 'NONE',  ( 47.90440150906960071, 23.11714053132569902, -54.72371951289599679 ) ) ;
#51810=CARTESIAN_POINT ( 'NONE',  ( 57.30561799036939874, -45.12637755034730702, -25.31757343247140213 ) ) ;
#51811=CARTESIAN_POINT ( 'NONE',  ( 56.46551886492290606, -50.77617157417189730, -53.85226995702900155 ) ) ;
#51813=CARTESIAN_POINT ( 'NONE',  ( 62.22754354791340603, -0.4274600148359939955, -16.45757208976800001 ) ) ;
#51814=CARTESIAN_POINT ( 'NONE',  ( 51.50850416226440132, -48.61618662830229454, -76.79363219169609067 ) ) ;
#51815=EDGE_CURVE ( 'NONE', #12214, #17870, #22095, .T. ) ;
#51816=AXIS2_PLACEMENT_3D ( 'NONE', #43324, #47264, #15018 ) ;
#51819=CARTESIAN_POINT ( 'NONE',  ( 52.26507113493899936, -49.78346811056199783, -77.19475928984779500 ) ) ;
#51821=AXIS2_PLACEMENT_3D ( 'NONE', #5371, #10597, #17928 ) ;
#51825=ADVANCED_FACE ( 'NONE', ( #41253 ), #5364, .T. ) ;
#51830=LINE ( 'NONE', #35054, #45200 ) ;
#51831=CARTESIAN_POINT ( 'NONE',  ( 57.39590324383170383, 13.88381105532070059, -17.43811253406409989 ) ) ;
#51834=DIRECTION ( 'NONE',  ( 1.000000000000000000, 0.000000000000000000, 0.000000000000000000 ) ) ;
#51838=CARTESIAN_POINT ( 'NONE',  ( 11.49562787866076619, -65.37291902649519670, -18.17421237899758779 ) ) ;
#51839=CARTESIAN_POINT ( 'NONE',  ( 47.23516258507500254, -54.76715534530099916, -54.66979262849320520 ) ) ;
#51845=CARTESIAN_POINT ( 'NONE',  ( 11.06596496317180112, 33.95392516474009881, -17.90443099699100316 ) ) ;
#51850=CARTESIAN_POINT ( 'NONE',  ( 49.00738943425649552, 22.66954927679429943, -54.83009724927129724 ) ) ;
#51851=CIRCLE ( 'NONE', #31740, 1.000000000000001554 ) ;
#51852=ORIENTED_EDGE ( 'NONE', *, *, #46970, .T. ) ;
#51854=CARTESIAN_POINT ( 'NONE',  ( 53.11419549839710186, -49.54851579802859618, -49.05615260309770065 ) ) ;
#51855=VERTEX_POINT ( 'NONE', #33378 ) ;
#51856=AXIS2_PLACEMENT_3D ( 'NONE', #22362, #3762, #15296 ) ;
#51859=CARTESIAN_POINT ( 'NONE',  ( 14.12259462364040097, 19.90775691718999951, -22.75706045377140185 ) ) ;
#51860=CARTESIAN_POINT ( 'NONE',  ( 82.81259997840240317, 13.80159592993990003, -46.56543266184489482 ) ) ;
#51863=CARTESIAN_POINT ( 'NONE',  ( 52.95214313111540605, 18.40625499070019799, -49.03964310582890107 ) ) ;
#51864=CARTESIAN_POINT ( 'NONE',  ( 55.00335051654970187, -45.49428894239379417, -15.38805630266439906 ) ) ;
#51865=CARTESIAN_POINT ( 'NONE',  ( 54.85035616863599728, 16.02459751768909868, -25.69268928997570001 ) ) ;
#51866=B_SPLINE_CURVE_WITH_KNOTS ( 'NONE', 3,
 ( #8310, #44732, #47639, #35835, #4121, #28212, #195, #443, #16433, #48407, #48149 ),
 .UNSPECIFIED., .F., .F.,
 ( 4, 1, 1, 1, 1, 1, 1, 1, 4 ),
 ( 0.000000000000000000, 0.1250000000000000000, 0.2500000000000000000, 0.3750000000000000000, 0.5000000000000000000, 0.6250000000000000000, 0.7500000000000000000, 0.8750000000000000000, 1.000000000000000000 ),
 .UNSPECIFIED. ) ;
#51870=EDGE_LOOP ( 'NONE', ( #9165, #28517, #30777, #39067, #20109 ) ) ;
#51872=ORIENTED_EDGE ( 'NONE', *, *, #28733, .F. ) ;
ENDSEC;
END-ISO-10303-21;
